ISO-10303-21;
HEADER;
FILE_DESCRIPTION (('STEP AP214'),
    '1' );
FILE_NAME ('Body.step',
    '2026-10-07T19:06:49',
    ( '' ),
    ( '' ),
    'SwSTEP 2.0',
    'SolidWorks 2020',
    '' );
FILE_SCHEMA (( 'AUTOMOTIVE_DESIGN' ));
ENDSEC;

DATA;
#3=EDGE_CURVE ( 'NONE', #26450, #22997, #2825, .T. ) ;
#8=CARTESIAN_POINT ( 'NONE',  ( 7.169653208691478596, -77.87460860825220266, -9.346314528427997814 ) ) ;
#9=CARTESIAN_POINT ( 'NONE',  ( -3.165411199172024848, -1.020833333333333703, -0.8506806241676611036 ) ) ;
#11=ORIENTED_EDGE ( 'NONE', *, *, #14208, .F. ) ;
#12=CARTESIAN_POINT ( 'NONE',  ( -9.835237363953000411, -54.71864156536999957, -7.760968332694998750 ) ) ;
#14=EDGE_CURVE ( 'NONE', #5429, #41516, #2225, .T. ) ;
#15=EDGE_LOOP ( 'NONE', ( #31939, #1109, #23065, #57706 ) ) ;
#17=CARTESIAN_POINT ( 'NONE',  ( -7.954951288349001004, -60.04999999966999980, 9.722718241315000398 ) ) ;
#19=VERTEX_POINT ( 'NONE', #36148 ) ;
#22=CARTESIAN_POINT ( 'NONE',  ( 11.95031029473000039, -77.77814994903998524, 5.399609419473999417 ) ) ;
#28=ORIENTED_EDGE ( 'NONE', *, *, #14602, .F. ) ;
#30=CARTESIAN_POINT ( 'NONE',  ( -9.844172144369998989, -76.00075078459998679, 7.391061701651999272 ) ) ;
#36=CARTESIAN_POINT ( 'NONE',  ( -0.9024763166187672603, -2.953607843777506403, -3.403194172902606951 ) ) ;
#38=CARTESIAN_POINT ( 'NONE',  ( 12.71658872084999992, -23.31584731985000047, 1.931087888240000217 ) ) ;
#40=CARTESIAN_POINT ( 'NONE',  ( -9.243123480579969353, -61.71653773535206966, -8.441201026360992898 ) ) ;
#43=CARTESIAN_POINT ( 'NONE',  ( 10.81044927328497174, -77.33600844987223866, 5.253279465540470206 ) ) ;
#45=CARTESIAN_POINT ( 'NONE',  ( 3.708203932500000022, -75.80000000000001137, 11.41267819554000162 ) ) ;
#52=CARTESIAN_POINT ( 'NONE',  ( 8.130811096541000538, -24.68523690389000080, 9.546858433121998999 ) ) ;
#53=EDGE_CURVE ( 'NONE', #3236, #26282, #39951, .T. ) ;
#57=CARTESIAN_POINT ( 'NONE',  ( -1.698401934078999975, -54.57985954063000378, -12.66748707609000135 ) ) ;
#58=CARTESIAN_POINT ( 'NONE',  ( 8.691395350247656637, -76.00817847884788137, 7.907189969528280571 ) ) ;
#61=ORIENTED_EDGE ( 'NONE', *, *, #20316, .F. ) ;
#62=CARTESIAN_POINT ( 'NONE',  ( 11.83799436920362957, -75.81835910994890071, 2.768346231419584136 ) ) ;
#64=AXIS2_PLACEMENT_3D ( 'NONE', #12751, #31031, #13327 ) ;
#65=CARTESIAN_POINT ( 'NONE',  ( -14.00000000000000000, -46.09579702914000165, 0.000000000000000000 ) ) ;
#71=ORIENTED_EDGE ( 'NONE', *, *, #32080, .F. ) ;
#74=CARTESIAN_POINT ( 'NONE',  ( 7.921865660077126670, -75.80000000000001137, -8.886071780246803442 ) ) ;
#81=DIRECTION ( 'NONE',  ( -0.7071067811865475727, 0.000000000000000000, -0.7071067811865475727 ) ) ;
#82=CARTESIAN_POINT ( 'NONE',  ( 10.98965142020543517, -23.51557447649318888, -0.4775239249309967127 ) ) ;
#84=TOROIDAL_SURFACE ( 'NONE', #10300, 17.50000000000000000, 5.000000000000000000 ) ;
#86=CARTESIAN_POINT ( 'NONE',  ( -12.00000000000000000, -60.04999999966999980, -1.250000000000000000 ) ) ;
#90=EDGE_CURVE ( 'NONE', #54593, #16250, #40282, .T. ) ;
#92=CARTESIAN_POINT ( 'NONE',  ( 0.000000000000000000, -18.75000000000000000, 12.00000000000000000 ) ) ;
#95=CARTESIAN_POINT ( 'NONE',  ( -12.02296678431999943, -78.53620577153000681, 2.418109797047000242 ) ) ;
#97=CARTESIAN_POINT ( 'NONE',  ( 7.956422463014998669, -24.52889896183999596, 9.787948076355000637 ) ) ;
#99=CARTESIAN_POINT ( 'NONE',  ( 7.342356150419300675, -55.61035107871643390, -8.190836719257356791 ) ) ;
#106=ORIENTED_EDGE ( 'NONE', *, *, #28761, .F. ) ;
#110=CARTESIAN_POINT ( 'NONE',  ( -9.778086933892000232, -75.88734000069999297, -8.273004691245001041 ) ) ;
#114=CARTESIAN_POINT ( 'NONE',  ( 12.61117324689999997, -18.78448536116999890, -1.798979683802999885 ) ) ;
#120=CONICAL_SURFACE ( 'NONE', #10463, 13.94999999997000018, 0.7853981633972997312 ) ;
#126=AXIS2_PLACEMENT_3D ( 'NONE', #7144, #26004, #48189 ) ;
#128=CYLINDRICAL_SURFACE ( 'NONE', #42114, 0.5000000000000004441 ) ;
#135=ORIENTED_EDGE ( 'NONE', *, *, #46483, .F. ) ;
#136=CARTESIAN_POINT ( 'NONE',  ( 2.839779323407650047, -1.393182233394845593, 1.634486084188475852 ) ) ;
#137=CARTESIAN_POINT ( 'NONE',  ( 0.5154756746320998673, -53.66759400203999775, 12.66205448068000017 ) ) ;
#139=CARTESIAN_POINT ( 'NONE',  ( -9.850507815892395769, -24.30508874547875564, 7.836744050302930198 ) ) ;
#142=CYLINDRICAL_SURFACE ( 'NONE', #54331, 3.250000000000000000 ) ;
#143=CARTESIAN_POINT ( 'NONE',  ( -1.484804496640999893, -61.51869153350000374, 12.77261165612999960 ) ) ;
#144=CARTESIAN_POINT ( 'NONE',  ( 12.72554264791999934, -18.79839278105999867, 1.930240062458999928 ) ) ;
#147=CARTESIAN_POINT ( 'NONE',  ( 10.31444587876999996, -54.49924218061999426, -7.758886158083000417 ) ) ;
#148=AXIS2_PLACEMENT_3D ( 'NONE', #56838, #53267, #47996 ) ;
#151=EDGE_CURVE ( 'NONE', #15969, #4126, #39694, .T. ) ;
#154=CARTESIAN_POINT ( 'NONE',  ( -1.722320550025187025, -61.03663688784200048, 12.71171904440437928 ) ) ;
#155=DIRECTION ( 'NONE',  ( -0.0001230612157835738363, 0.000000000000000000, 0.9999999924279686647 ) ) ;
#156=CARTESIAN_POINT ( 'NONE',  ( -12.72394223973000038, -60.02159774832999517, 1.930881086224999876 ) ) ;
#160=LINE ( 'NONE', #46472, #43214 ) ;
#161=ORIENTED_EDGE ( 'NONE', *, *, #35079, .T. ) ;
#162=DIRECTION ( 'NONE',  ( 0.000000000000000000, 1.000000000000000000, 0.000000000000000000 ) ) ;
#165=CARTESIAN_POINT ( 'NONE',  ( -12.50000000000000000, -17.31762331506999786, -1.005384022379999909 ) ) ;
#166=ORIENTED_EDGE ( 'NONE', *, *, #27076, .T. ) ;
#168=ORIENTED_EDGE ( 'NONE', *, *, #42200, .F. ) ;
#172=ORIENTED_EDGE ( 'NONE', *, *, #44103, .T. ) ;
#174=ORIENTED_EDGE ( 'NONE', *, *, #20456, .F. ) ;
#175=CIRCLE ( 'NONE', #40670, 12.90000000000000036 ) ;
#177=CARTESIAN_POINT ( 'NONE',  ( 3.250000000000000000, -1.250000000000000000, 0.000000000000000000 ) ) ;
#180=CARTESIAN_POINT ( 'NONE',  ( 2.061649843245999758, -23.20561307587000144, -12.83797346714000120 ) ) ;
#184=CARTESIAN_POINT ( 'NONE',  ( -12.05956633327999938, -78.83299827204000110, -0.2332108555899000124 ) ) ;
#190=EDGE_CURVE ( 'NONE', #21248, #3192, #25838, .T. ) ;
#193=CARTESIAN_POINT ( 'NONE',  ( -3.331828115504000376, -76.81423739310000087, 12.52045872913000046 ) ) ;
#202=CARTESIAN_POINT ( 'NONE',  ( 7.624341766639000539, -23.26485146254000114, 10.42531125024000005 ) ) ;
#204=EDGE_CURVE ( 'NONE', #1538, #36787, #12747, .T. ) ;
#209=EDGE_CURVE ( 'NONE', #23895, #25757, #23322, .T. ) ;
#210=ORIENTED_EDGE ( 'NONE', *, *, #29786, .F. ) ;
#211=CARTESIAN_POINT ( 'NONE',  ( -0.5999663639300912843, -23.18964892095168295, 10.98362601162691199 ) ) ;
#212=CARTESIAN_POINT ( 'NONE',  ( 8.130813118348999780, -54.11476110100999648, -9.546856411313999757 ) ) ;
#213=DIRECTION ( 'NONE',  ( 0.000000000000000000, 0.000000000000000000, 1.000000000000000000 ) ) ;
#214=CARTESIAN_POINT ( 'NONE',  ( 1.931087888049999979, -60.11584477251999203, 12.71658889743999943 ) ) ;
#215=CARTESIAN_POINT ( 'NONE',  ( -10.59876350475000173, -77.46807671118999394, 7.550195564144000393 ) ) ;
#216=AXIS2_PLACEMENT_3D ( 'NONE', #10223, #37949, #14925 ) ;
#218=CARTESIAN_POINT ( 'NONE',  ( 12.82904109062999964, -23.32452273707999879, -2.062673488410000200 ) ) ;
#220=DIRECTION ( 'NONE',  ( 0.7071067811865475727, 0.000000000000000000, 0.7071067811865475727 ) ) ;
#223=CARTESIAN_POINT ( 'NONE',  ( 7.678690995204998870, -21.75648180056000314, -10.59551070212000035 ) ) ;
#226=CARTESIAN_POINT ( 'NONE',  ( -1.182840957218999955, -1.349210179781999752, -3.838043326965000279 ) ) ;
#231=DIRECTION ( 'NONE',  ( -1.000000000000000000, 0.000000000000000000, 0.000000000000000000 ) ) ;
#234=ORIENTED_EDGE ( 'NONE', *, *, #57744, .T. ) ;
#237=VERTEX_POINT ( 'NONE', #51785 ) ;
#239=ORIENTED_EDGE ( 'NONE', *, *, #27026, .F. ) ;
#240=ORIENTED_EDGE ( 'NONE', *, *, #54504, .F. ) ;
#241=LINE ( 'NONE', #35610, #56530 ) ;
#243=CARTESIAN_POINT ( 'NONE',  ( 2.866892793968622843, -1.159673730758707721, 2.818444692989894751 ) ) ;
#245=VERTEX_POINT ( 'NONE', #11335 ) ;
#249=ADVANCED_FACE ( 'NONE', ( #43204 ), #20212, .F. ) ;
#250=CARTESIAN_POINT ( 'NONE',  ( -0.3116081092031571242, -18.31315380223933786, 10.99615594221668857 ) ) ;
#251=CARTESIAN_POINT ( 'NONE',  ( 3.075537641221509411, -77.15416666666668277, 11.44417895085272008 ) ) ;
#252=EDGE_CURVE ( 'NONE', #52871, #40540, #47362, .T. ) ;
#253=AXIS2_PLACEMENT_3D ( 'NONE', #30100, #47864, #51996 ) ;
#254=DIRECTION ( 'NONE',  ( 0.9957542217973192056, 0.04890179604787090600, -0.07798810240099150748 ) ) ;
#255=CARTESIAN_POINT ( 'NONE',  ( 7.642147947524999374, -56.01514526721999943, -10.55910102243999837 ) ) ;
#257=CARTESIAN_POINT ( 'NONE',  ( -10.18949719146000099, -23.21529250218000229, 7.645392405660000001 ) ) ;
#259=CARTESIAN_POINT ( 'NONE',  ( 0.9082395157416487397, -78.08405139807857154, -12.04149494368141227 ) ) ;
#264=FACE_BOUND ( 'NONE', #18208, .T. ) ;
#265=CARTESIAN_POINT ( 'NONE',  ( -0.005119011380138999839, -24.93813862189000119, 12.43705489344000092 ) ) ;
#268=AXIS2_PLACEMENT_3D ( 'NONE', #41715, #55289, #29005 ) ;
#269=CARTESIAN_POINT ( 'NONE',  ( -3.200978647831000501, -0.8315460165489000355, 2.321879312794999706 ) ) ;
#270=CARTESIAN_POINT ( 'NONE',  ( 7.686918321195999937, -58.55560170965000566, 10.48771805380999922 ) ) ;
#272=CARTESIAN_POINT ( 'NONE',  ( 12.70556836347999941, -25.22772277227999993, 2.424222353299999887E-09 ) ) ;
#274=CARTESIAN_POINT ( 'NONE',  ( 12.65989858210999941, -61.74344101100000159, -0.9743214026256999949 ) ) ;
#276=CARTESIAN_POINT ( 'NONE',  ( -12.99510751537000353, -26.30294702886003222, -6.911973076623003642 ) ) ;
#281=CARTESIAN_POINT ( 'NONE',  ( 0.000000000000000000, -3.000000000000000000, 0.000000000000000000 ) ) ;
#285=ADVANCED_FACE ( 'NONE', ( #47941, #16045, #34029, #6309 ), #29659, .T. ) ;
#293=CARTESIAN_POINT ( 'NONE',  ( 12.20990109347999919, -76.98480431993999673, -3.270330254029999661 ) ) ;
#295=FACE_OUTER_BOUND ( 'NONE', #22680, .T. ) ;
#296=CARTESIAN_POINT ( 'NONE',  ( -1.799490220168999954, -56.02870851050000311, 12.64502302235999842 ) ) ;
#297=ORIENTED_EDGE ( 'NONE', *, *, #43829, .F. ) ;
#298=CARTESIAN_POINT ( 'NONE',  ( 1.495357591673911246, -54.24123662600908347, -12.70444646756140550 ) ) ;
#299=DIRECTION ( 'NONE',  ( 0.000000000000000000, -1.000000000000000000, 1.006602208993000011E-13 ) ) ;
#300=LINE ( 'NONE', #27694, #13909 ) ;
#302=AXIS2_PLACEMENT_3D ( 'NONE', #58162, #9457, #44888 ) ;
#303=CARTESIAN_POINT ( 'NONE',  ( -12.82904109059999875, -55.47547726255000100, -2.062673488410000200 ) ) ;
#304=CARTESIAN_POINT ( 'NONE',  ( 10.98960559191261765, -23.51693928699155833, 0.4813395862318616270 ) ) ;
#306=DIRECTION ( 'NONE',  ( 0.000000000000000000, -1.000000000000000000, 0.000000000000000000 ) ) ;
#308=VERTEX_POINT ( 'NONE', #1507 ) ;
#309=TOROIDAL_SURFACE ( 'NONE', #16338, 13.50000000000000000, 0.5000000000000000000 ) ;
#310=CARTESIAN_POINT ( 'NONE',  ( -7.605690612596999856, -55.37434870709000023, -10.52682230156000109 ) ) ;
#317=ORIENTED_EDGE ( 'NONE', *, *, #37608, .T. ) ;
#326=VERTEX_POINT ( 'NONE', #36627 ) ;
#331=CARTESIAN_POINT ( 'NONE',  ( 1.081559480311999888, -3.500000000000000000, -3.328697807033000000 ) ) ;
#332=CARTESIAN_POINT ( 'NONE',  ( 12.53241208775999915, -19.23537109840999904, 1.667936697358999965 ) ) ;
#337=CARTESIAN_POINT ( 'NONE',  ( 11.73341735579898248, -77.28263860279511732, -2.603816878860229167 ) ) ;
#338=CARTESIAN_POINT ( 'NONE',  ( 12.29321436482372754, -76.17567889517343360, -4.311296892563305505 ) ) ;
#339=AXIS2_PLACEMENT_3D ( 'NONE', #14294, #32288, #37316 ) ;
#340=B_SPLINE_SURFACE_WITH_KNOTS ( 'NONE', 3, 3, ( 
 ( #36923, #41947, #19221, #6213, #37214, #50233, #55227, #23928, #24228, #31902, #42247, #37801, #55822, #49944, #39721, #48600, #53600, #44746, #26424, #44446, #4297, #3998, #30274, #3150, #13435, #57729, #35875, #48887, #58323, #53307, #57447, #21432, #39146, #8430, #34703 ),
 ( #8725, #16720, #57155, #3713, #48315, #49172, #22002, #22298, #43587, #52734, #17286, #48037, #12850, #34988, #44166, #12285, #26718, #21716, #7855, #40314, #40008, #17886, #21139, #25855, #35274, #7567, #30850, #53017, #58025, #43884, #53904, #3430, #12570, #13140, #17586 ),
 ( #35573, #39440, #17006, #31133, #30567, #8146, #26145, #25567, #18470, #45931, #36461, #54769, #4602, #32306, #1348, #14311, #4892, #1063, #19341, #50354, #5464, #5751, #19052, #46227, #31729, #14024, #45049, #41773, #27596, #37336, #18758, #18182, #54488, #36177, #37041 ),
 ( #55058, #50064, #27310, #14605, #45341, #32600, #40901, #45638, #49476, #50648, #778, #23183, #41189, #9027, #27013, #22600, #22889, #490, #19628, #2500, #42945, #56231, #1935, #15781, #20505, #38502, #24051, #32892, #56518, #15194, #52095, #43230, #7208, #2219, #50937 ) ),
 .UNSPECIFIED., .F., .F., .F.,
 ( 4, 4 ),
 ( 4, 1, 1, 1, 1, 1, 1, 1, 1, 1, 1, 1, 1, 1, 1, 1, 1, 1, 1, 1, 1, 1, 1, 1, 1, 1, 1, 1, 1, 1, 1, 1, 4 ),
 ( -0.02000000000000999936, 1.020000000000000018 ),
 ( 0.1112507840917000002, 0.1395687738142999956, 0.1678867635369000189, 0.1962047532594000110, 0.2245227429820000065, 0.2528407327046000019, 0.2811587224271000496, 0.3094767121496999618, 0.3377947018722999850, 0.3661126915947999771, 0.3944306813174000004, 0.4227486710400000236, 0.4510666607625000157, 0.4793846504851000390, 0.5077026402076999512, 0.5360206299302000543, 0.5643386196528000776, 0.5926566093753999898, 0.6209745990978999819, 0.6492925888205000051, 0.6776105785431000283, 0.7059285682657000516, 0.7342465579881999327, 0.7625645477107999559, 0.7908825374333999791, 0.8192005271558999713, 0.8475185168785001055, 0.8758365066010999067, 0.9041544963236000099, 0.9324724860462000331, 0.9607904757688000563, 0.9891084654913000485, 1.017426455213999992 ),
 .UNSPECIFIED. ) ;
#344=FACE_OUTER_BOUND ( 'NONE', #38978, .T. ) ;
#350=CARTESIAN_POINT ( 'NONE',  ( 8.381754473445653275, -76.01120442237058228, 8.234170154212950621 ) ) ;
#354=AXIS2_PLACEMENT_3D ( 'NONE', #7083, #38659, #33359 ) ;
#355=CARTESIAN_POINT ( 'NONE',  ( -7.450482419345999752, -76.12327025406412417, -9.799277032148999922 ) ) ;
#356=EDGE_CURVE ( 'NONE', #56848, #20424, #2309, .T. ) ;
#363=ORIENTED_EDGE ( 'NONE', *, *, #29731, .T. ) ;
#365=CARTESIAN_POINT ( 'NONE',  ( 12.74331394907039261, -55.27353206544193398, 1.980611464663725618 ) ) ;
#366=CARTESIAN_POINT ( 'NONE',  ( 2.782842193290164801, -75.80000000000001137, -11.52882899609856082 ) ) ;
#372=EDGE_CURVE ( 'NONE', #4267, #17174, #51583, .T. ) ;
#375=VECTOR ( 'NONE', #25081, 1000.000000000000000 ) ;
#377=DIRECTION ( 'NONE',  ( 0.000000000000000000, -1.000000000000000000, 0.000000000000000000 ) ) ;
#378=VERTEX_POINT ( 'NONE', #14185 ) ;
#379=EDGE_LOOP ( 'NONE', ( #35458, #39042, #39899, #1106 ) ) ;
#380=DIRECTION ( 'NONE',  ( 0.000000000000000000, -1.000000000000000000, 0.000000000000000000 ) ) ;
#384=ORIENTED_EDGE ( 'NONE', *, *, #55559, .T. ) ;
#385=CARTESIAN_POINT ( 'NONE',  ( 7.620012114215000132, -23.20560398649000078, 10.53562503194000044 ) ) ;
#392=CARTESIAN_POINT ( 'NONE',  ( 12.00000000000000000, -60.04999999966999980, 0.000000000000000000 ) ) ;
#393=VERTEX_POINT ( 'NONE', #50514 ) ;
#394=CARTESIAN_POINT ( 'NONE',  ( -9.848022987176388909, -24.82869493595770649, 8.114799025119214804 ) ) ;
#398=DIRECTION ( 'NONE',  ( -0.7071067811865475727, 0.000000000000000000, 0.7071067811865475727 ) ) ;
#400=CARTESIAN_POINT ( 'NONE',  ( -9.898328264071000859, -75.97442085042999338, -8.374737995046999117 ) ) ;
#403=CARTESIAN_POINT ( 'NONE',  ( -8.838834764832000701, -60.04999999966999980, 8.838834764832000701 ) ) ;
#405=EDGE_CURVE ( 'NONE', #17140, #15196, #41355, .T. ) ;
#406=CARTESIAN_POINT ( 'NONE',  ( -10.18114973714000016, -23.39009320411999937, -7.633087466104000463 ) ) ;
#407=CARTESIAN_POINT ( 'NONE',  ( -11.49731019796060316, -76.68331092814908345, 2.423775870982253444 ) ) ;
#415=CARTESIAN_POINT ( 'NONE',  ( -0.8506806241676722058, -3.395833333333332593, 3.165411199172022627 ) ) ;
#416=CARTESIAN_POINT ( 'NONE',  ( -11.44417895085270942, -78.32083333333335418, -3.075537641221545826 ) ) ;
#417=DIRECTION ( 'NONE',  ( 0.000000000000000000, -1.000000000000000000, 0.000000000000000000 ) ) ;
#418=DIRECTION ( 'NONE',  ( -6.735242868878000753E-11, 1.000000000000000000, 0.000000000000000000 ) ) ;
#423=CARTESIAN_POINT ( 'NONE',  ( -3.250000000000002665, -1.989583333333334147, 0.4254240051736044581 ) ) ;
#425=VERTEX_POINT ( 'NONE', #23343 ) ;
#429=EDGE_CURVE ( 'NONE', #41458, #33230, #30416, .T. ) ;
#430=CARTESIAN_POINT ( 'NONE',  ( -1.382299254417000078, -2.123118309747999977, 3.546132182520000065 ) ) ;
#434=DIRECTION ( 'NONE',  ( 0.000000000000000000, -1.000000000000000000, 0.000000000000000000 ) ) ;
#437=CARTESIAN_POINT ( 'NONE',  ( 12.57354471038000021, -18.27622323986999930, 1.757967544833999973 ) ) ;
#440=CARTESIAN_POINT ( 'NONE',  ( 9.992014434659999722, -54.63915351680999777, -7.762970980286999279 ) ) ;
#446=CARTESIAN_POINT ( 'NONE',  ( -12.43410103870000150, -61.24137177736000126, 1.192638008239000014 ) ) ;
#453=CIRCLE ( 'NONE', #45692, 1.750000000000001332 ) ;
#454=FACE_OUTER_BOUND ( 'NONE', #42226, .T. ) ;
#456=VERTEX_POINT ( 'NONE', #36913 ) ;
#459=EDGE_LOOP ( 'NONE', ( #6292, #27187, #8033, #17546, #22644, #44404 ) ) ;
#460=EDGE_CURVE ( 'NONE', #4894, #43600, #23630, .T. ) ;
#461=CARTESIAN_POINT ( 'NONE',  ( -2.062312494845999655, -18.77284340107000205, 12.83634740209000036 ) ) ;
#462=CARTESIAN_POINT ( 'NONE',  ( -12.50000000000000000, -60.04999999966999980, 0.000000000000000000 ) ) ;
#465=CONICAL_SURFACE ( 'NONE', #46690, 11.09999999881999955, 0.7853981633972997312 ) ;
#467=DIRECTION ( 'NONE',  ( 0.000000000000000000, 1.000000000000000000, 0.000000000000000000 ) ) ;
#468=CARTESIAN_POINT ( 'NONE',  ( -9.088900789933001434, -78.68843598616000179, 7.702160993204000050 ) ) ;
#469=VERTEX_POINT ( 'NONE', #14763 ) ;
#470=VERTEX_POINT ( 'NONE', #32760 ) ;
#471=CARTESIAN_POINT ( 'NONE',  ( 0.000000000000000000, -32.88214388149999934, 0.000000000000000000 ) ) ;
#476=CARTESIAN_POINT ( 'NONE',  ( -10.59551070215999857, -20.24351820077000141, 7.678690995240000206 ) ) ;
#477=CARTESIAN_POINT ( 'NONE',  ( -9.134707332315000983, -77.39321223492000001, -8.964724163292999037 ) ) ;
#479=CARTESIAN_POINT ( 'NONE',  ( -12.56594317823000040, -23.25000001387000026, 1.750000000000000000 ) ) ;
#480=CARTESIAN_POINT ( 'NONE',  ( 12.56594317825999951, -60.05000001354000005, -1.750000000000000000 ) ) ;
#481=EDGE_CURVE ( 'NONE', #23446, #29038, #48572, .T. ) ;
#484=CARTESIAN_POINT ( 'NONE',  ( 12.65375411752000012, -20.25022861081000158, 1.750000000000000000 ) ) ;
#485=CARTESIAN_POINT ( 'NONE',  ( -10.66325342011819188, -78.26486258876667534, 5.043235781625580394 ) ) ;
#488=FACE_BOUND ( 'NONE', #45895, .T. ) ;
#490=CARTESIAN_POINT ( 'NONE',  ( -0.3113020967593000399, -2.733516015699999802, 3.793306396812999637 ) ) ;
#492=ORIENTED_EDGE ( 'NONE', *, *, #5295, .T. ) ;
#494=CARTESIAN_POINT ( 'NONE',  ( 1.569236785184999737E-14, 0.000000000000000000, 0.000000000000000000 ) ) ;
#495=LINE ( 'NONE', #35880, #7209 ) ;
#496=VECTOR ( 'NONE', #9749, 1000.000000000000114 ) ;
#497=EDGE_CURVE ( 'NONE', #24745, #8613, #21219, .T. ) ;
#501=CARTESIAN_POINT ( 'NONE',  ( 12.55073801092999908, -77.24605814734000830, -3.437763296274999991 ) ) ;
#505=ORIENTED_EDGE ( 'NONE', *, *, #666, .F. ) ;
#506=VECTOR ( 'NONE', #47712, 1000.000000000000000 ) ;
#509=CARTESIAN_POINT ( 'NONE',  ( 7.705119999441000012, -20.24828923609000242, -10.24996238031000040 ) ) ;
#512=CARTESIAN_POINT ( 'NONE',  ( -1.488596180559999871, -0.8774472721615999005, -3.730054860412999940 ) ) ;
#517=FACE_OUTER_BOUND ( 'NONE', #48566, .T. ) ;
#523=DIRECTION ( 'NONE',  ( 0.000000000000000000, 1.000000000000000000, 0.000000000000000000 ) ) ;
#525=VERTEX_POINT ( 'NONE', #2664 ) ;
#527=ORIENTED_EDGE ( 'NONE', *, *, #54959, .T. ) ;
#528=EDGE_LOOP ( 'NONE', ( #13546, #35244, #44133, #4500 ) ) ;
#529=ADVANCED_FACE ( 'NONE', ( #2091 ), #20293, .T. ) ;
#530=CARTESIAN_POINT ( 'NONE',  ( -0.4127567104095349881, -2.716300734224319946, -3.229589481510274585 ) ) ;
#531=EDGE_CURVE ( 'NONE', #49275, #46028, #19327, .T. ) ;
#532=CARTESIAN_POINT ( 'NONE',  ( -1.750000000000000000, -18.75000000310999937, -12.50000000000000000 ) ) ;
#537=EDGE_LOOP ( 'NONE', ( #15741, #44098, #34888 ) ) ;
#539=CIRCLE ( 'NONE', #2291, 14.00000000000000000 ) ;
#542=VECTOR ( 'NONE', #54840, 1000.000000000000114 ) ;
#544=CARTESIAN_POINT ( 'NONE',  ( 0.000000000000000000, -15.89905023022000030, 0.000000000000000000 ) ) ;
#545=CARTESIAN_POINT ( 'NONE',  ( 14.00000000000000000, -46.09579702914000165, 0.000000000000000000 ) ) ;
#550=CARTESIAN_POINT ( 'NONE',  ( -13.94241847916999966, -9.539970597795999652, -4.312626734363999664E-05 ) ) ;
#553=CARTESIAN_POINT ( 'NONE',  ( 10.26699006316251683, -76.59166666666665435, 5.917523019358090330 ) ) ;
#556=LINE ( 'NONE', #14374, #7797 ) ;
#557=LINE ( 'NONE', #55415, #9432 ) ;
#558=CARTESIAN_POINT ( 'NONE',  ( -0.5506765233277000071, -25.25954292244000143, 12.77514798311000099 ) ) ;
#561=CARTESIAN_POINT ( 'NONE',  ( -2.851845075913000294, -2.090913946620000186, -1.354809779547999860 ) ) ;
#564=CARTESIAN_POINT ( 'NONE',  ( 0.7999999999999001243, -18.84999999997999964, 12.00000000000000000 ) ) ;
#566=CARTESIAN_POINT ( 'NONE',  ( 7.686941364964000378, -58.55472017773000459, -10.48774103561000182 ) ) ;
#567=CARTESIAN_POINT ( 'NONE',  ( -3.465920916155000420, -3.052832871923000013, -0.3696040369545000037 ) ) ;
#570=CARTESIAN_POINT ( 'NONE',  ( -8.485281374238999419, -23.25000000000000000, -8.485281374238999419 ) ) ;
#571=CARTESIAN_POINT ( 'NONE',  ( 0.000000000000000000, -18.75000000000000000, -12.00000000000000000 ) ) ;
#583=CARTESIAN_POINT ( 'NONE',  ( -12.59654320151999940, -77.26232752475000609, -1.064070293361000008 ) ) ;
#585=CARTESIAN_POINT ( 'NONE',  ( -8.441176280277392863, -61.71652561705167983, 9.243148036170415693 ) ) ;
#586=DIRECTION ( 'NONE',  ( 0.000000000000000000, -1.000000000000000000, 0.000000000000000000 ) ) ;
#587=VERTEX_POINT ( 'NONE', #21516 ) ;
#588=AXIS2_PLACEMENT_3D ( 'NONE', #42436, #2004, #24713 ) ;
#590=DIRECTION ( 'NONE',  ( 0.7071067811865969777, 1.533578360404995178E-11, 0.7071067811864980568 ) ) ;
#592=DIRECTION ( 'NONE',  ( -1.000000000000000000, 0.000000000000000000, 0.000000000000000000 ) ) ;
#594=CARTESIAN_POINT ( 'NONE',  ( -12.53239398061000109, -59.56486430393999854, -1.667936688463999895 ) ) ;
#597=CARTESIAN_POINT ( 'NONE',  ( -12.70556836347999941, -25.22772277227999993, -2.424223956931999920E-09 ) ) ;
#598=EDGE_LOOP ( 'NONE', ( #27192, #166, #40123, #43861 ) ) ;
#599=ORIENTED_EDGE ( 'NONE', *, *, #4461, .F. ) ;
#600=CARTESIAN_POINT ( 'NONE',  ( -10.53495272788000214, -55.57289072595000334, -7.618387390351999855 ) ) ;
#602=( LENGTH_UNIT ( ) NAMED_UNIT ( * ) SI_UNIT ( .MILLI., .METRE. ) );
#605=DIRECTION ( 'NONE',  ( -1.000000000000000000, 0.000000000000000000, 0.000000000000000000 ) ) ;
#608=ORIENTED_EDGE ( 'NONE', *, *, #33338, .F. ) ;
#612=CARTESIAN_POINT ( 'NONE',  ( -13.06702859930000038, -77.00108497556999509, -1.103813699724999875 ) ) ;
#615=CARTESIAN_POINT ( 'NONE',  ( -1.232226823824171147, -24.52290911267661144, 12.50408896749710053 ) ) ;
#618=CARTESIAN_POINT ( 'NONE',  ( -12.22985280536000019, -76.56108432191999214, -1.402219185755000153 ) ) ;
#620=CIRCLE ( 'NONE', #30735, 0.5000000000000000000 ) ;
#621=CARTESIAN_POINT ( 'NONE',  ( 0.9174690372081734102, -2.203321940176160343, 3.400067753488194011 ) ) ;
#622=CARTESIAN_POINT ( 'NONE',  ( 12.60552522436000089, -18.71082434677000350, 1.799501877760999902 ) ) ;
#623=CARTESIAN_POINT ( 'NONE',  ( -11.55418265775999842, -78.99013131216000261, 4.110954701505000308 ) ) ;
#628=CARTESIAN_POINT ( 'NONE',  ( 1.347303718401573480, -77.41606322048822619, 11.98951635918131764 ) ) ;
#629=CARTESIAN_POINT ( 'NONE',  ( -9.971217743844798420, -75.89688248555343364, 8.384385000145641698 ) ) ;
#631=ORIENTED_EDGE ( 'NONE', *, *, #11984, .F. ) ;
#633=CARTESIAN_POINT ( 'NONE',  ( 8.838834764832000701, -18.75000000000000000, 8.838834764832000701 ) ) ;
#639=CARTESIAN_POINT ( 'NONE',  ( 0.007133794492888097249, -76.07462582236088622, 11.74977943346025455 ) ) ;
#648=DIRECTION ( 'NONE',  ( 0.7071067811865473507, 1.433669009702094715E-08, 0.7071067811865473507 ) ) ;
#649=CARTESIAN_POINT ( 'NONE',  ( 7.618386520043000765, -18.77287536652999833, -10.53495200520000097 ) ) ;
#650=CARTESIAN_POINT ( 'NONE',  ( 12.51072239526000196, -63.10294702885996543, 0.7871079366006996647 ) ) ;
#653=CARTESIAN_POINT ( 'NONE',  ( 12.70457850620686990, -16.82128713317816704, 0.5106122238172051686 ) ) ;
#656=EDGE_CURVE ( 'NONE', #20949, #16041, #34601, .T. ) ;
#657=CARTESIAN_POINT ( 'NONE',  ( 11.41636098306275215, -76.43082762775702577, -2.781676017839413539 ) ) ;
#659=CARTESIAN_POINT ( 'NONE',  ( 1.250000000000000000, -23.25000000000000000, -12.00000000000000000 ) ) ;
#660=CARTESIAN_POINT ( 'NONE',  ( 10.48771805367000098, -20.24439828562999821, 7.686918321060999482 ) ) ;
#664=CIRCLE ( 'NONE', #23179, 0.5000000000000006661 ) ;
#666=EDGE_CURVE ( 'NONE', #18159, #52919, #43291, .T. ) ;
#669=TOROIDAL_SURFACE ( 'NONE', #20457, 1.250000000000000000, 0.5000000000000000000 ) ;
#675=CARTESIAN_POINT ( 'NONE',  ( -12.49999991316347270, -39.30476017083000073, -0.001473401919593436823 ) ) ;
#676=CARTESIAN_POINT ( 'NONE',  ( 8.643979526155998627, -25.25953772911000073, 9.422807787372999400 ) ) ;
#677=ADVANCED_FACE ( 'NONE', ( #12656 ), #53694, .F. ) ;
#678=CARTESIAN_POINT ( 'NONE',  ( 8.870414881026999154, -61.86963060230000622, 8.878264461126001095 ) ) ;
#683=EDGE_CURVE ( 'NONE', #40118, #56133, #44534, .T. ) ;
#685=CARTESIAN_POINT ( 'NONE',  ( 7.958776490642000212, -61.27699850017000216, -9.723157983989999309 ) ) ;
#689=DIRECTION ( 'NONE',  ( 0.000000000000000000, 1.000000000000000000, 0.000000000000000000 ) ) ;
#691=CARTESIAN_POINT ( 'NONE',  ( -2.192937812663000141, -76.11726098207999769, -12.93882154009999930 ) ) ;
#696=CARTESIAN_POINT ( 'NONE',  ( -7.633478499826000352, -23.20098177597000344, -10.36292345935000014 ) ) ;
#697=CARTESIAN_POINT ( 'NONE',  ( -7.452378523309739045, -60.34721902435786234, 8.090910852015730015 ) ) ;
#699=ORIENTED_EDGE ( 'NONE', *, *, #33110, .F. ) ;
#704=ADVANCED_FACE ( 'NONE', ( #4089 ), #7371, .F. ) ;
#708=CARTESIAN_POINT ( 'NONE',  ( 1.320786595080246428, -2.595329183020129271, 3.336226784969741566 ) ) ;
#714=VECTOR ( 'NONE', #13948, 1000.000000000000000 ) ;
#717=CARTESIAN_POINT ( 'NONE',  ( -0.5366960857496999582, -3.191422503149000001, 3.929767262548999884 ) ) ;
#721=CARTESIAN_POINT ( 'NONE',  ( 7.620037246293000166, -23.20567269824999812, -10.53559750859000133 ) ) ;
#723=CARTESIAN_POINT ( 'NONE',  ( -11.75000000000000000, -76.79999999999999716, -1.435311119447000145E-14 ) ) ;
#724=CARTESIAN_POINT ( 'NONE',  ( 12.55458938220999876, -17.83720883386000011, 1.575070636625000242 ) ) ;
#726=CARTESIAN_POINT ( 'NONE',  ( -7.624341764923000753, -18.73514850530999709, -10.42531124853000080 ) ) ;
#727=CARTESIAN_POINT ( 'NONE',  ( 10.18948933931000234, -55.58467389893999666, -7.645397892281000196 ) ) ;
#736=ORIENTED_EDGE ( 'NONE', *, *, #4110, .T. ) ;
#738=EDGE_CURVE ( 'NONE', #45494, #38673, #46264, .T. ) ;
#739=FACE_OUTER_BOUND ( 'NONE', #12321, .T. ) ;
#743=ORIENTED_EDGE ( 'NONE', *, *, #12057, .F. ) ;
#746=ORIENTED_EDGE ( 'NONE', *, *, #37529, .T. ) ;
#747=CIRCLE ( 'NONE', #43161, 1.750000000000000000 ) ;
#748=EDGE_LOOP ( 'NONE', ( #31767, #5492, #24875, #32117, #7880, #37736, #17183, #44247, #13256, #15462, #16551 ) ) ;
#749=CARTESIAN_POINT ( 'NONE',  ( -1.798336774608999988, -18.80355501948000096, 12.61277771566000006 ) ) ;
#750=FACE_OUTER_BOUND ( 'NONE', #23794, .T. ) ;
#755=CARTESIAN_POINT ( 'NONE',  ( 0.4408833872559000389, -78.45936893705000159, -12.05376079588999971 ) ) ;
#757=ORIENTED_EDGE ( 'NONE', *, *, #19037, .T. ) ;
#761=VECTOR ( 'NONE', #45339, 1000.000000000000000 ) ;
#762=LINE ( 'NONE', #36733, #5023 ) ;
#764=AXIS2_PLACEMENT_3D ( 'NONE', #15536, #51568, #1982 ) ;
#766=CARTESIAN_POINT ( 'NONE',  ( -10.55911395187000146, -19.21538333566000034, 7.642160924884000117 ) ) ;
#767=CARTESIAN_POINT ( 'NONE',  ( -9.194628130165000357, -76.98075131598999121, -9.128060447331000304 ) ) ;
#769=CARTESIAN_POINT ( 'NONE',  ( -12.92177931904999966, -21.75736537952000305, -2.062503053667999797 ) ) ;
#770=CARTESIAN_POINT ( 'NONE',  ( 10.07627163191000008, -18.75000000310999937, 7.601397897754999633 ) ) ;
#774=CARTESIAN_POINT ( 'NONE',  ( 2.986710853074932448, -2.883334572040014088, 1.279778411999374477 ) ) ;
#778=CARTESIAN_POINT ( 'NONE',  ( 3.594201416108000036, -3.128676228555999916, 1.252117639952999850 ) ) ;
#782=CARTESIAN_POINT ( 'NONE',  ( 8.140250184781665510, -60.25160423313176494, -7.398464061246547097 ) ) ;
#783=CARTESIAN_POINT ( 'NONE',  ( -9.344422729779601866, -77.64679824576278122, 7.168946966961233791 ) ) ;
#785=CARTESIAN_POINT ( 'NONE',  ( -12.97295173694999981, -77.52358135215001766, -1.020668466325000079 ) ) ;
#788=CARTESIAN_POINT ( 'NONE',  ( -8.611000706001480154, -61.97488119190911959, -9.355851007328045199 ) ) ;
#790=ORIENTED_EDGE ( 'NONE', *, *, #51975, .F. ) ;
#797=CARTESIAN_POINT ( 'NONE',  ( -3.616527695712999702, -1.828510311347000039, -0.5438149879621999583 ) ) ;
#800=VERTEX_POINT ( 'NONE', #46611 ) ;
#802=FACE_OUTER_BOUND ( 'NONE', #19750, .T. ) ;
#803=TOROIDAL_SURFACE ( 'NONE', #14878, 17.50000000000000000, 5.000000000000000000 ) ;
#805=ORIENTED_EDGE ( 'NONE', *, *, #405, .F. ) ;
#808=CARTESIAN_POINT ( 'NONE',  ( 12.50000000000000000, -63.73717104351998586, 1.868318442826999995E-13 ) ) ;
#809=ORIENTED_EDGE ( 'NONE', *, *, #15642, .T. ) ;
#812=EDGE_LOOP ( 'NONE', ( #37953, #24356, #35317, #52754 ) ) ;
#813=ORIENTED_EDGE ( 'NONE', *, *, #41982, .F. ) ;
#814=DIRECTION ( 'NONE',  ( 0.000000000000000000, 1.000000000000000000, 0.000000000000000000 ) ) ;
#815=ORIENTED_EDGE ( 'NONE', *, *, #52470, .F. ) ;
#817=CARTESIAN_POINT ( 'NONE',  ( -12.80088938722999892, -22.76256651757000071, -1.980532758767000301 ) ) ;
#819=ORIENTED_EDGE ( 'NONE', *, *, #11465, .T. ) ;
#822=VERTEX_POINT ( 'NONE', #43035 ) ;
#824=DIRECTION ( 'NONE',  ( 0.000000000000000000, 0.000000000000000000, 1.000000000000000000 ) ) ;
#826=DIRECTION ( 'NONE',  ( 0.000000000000000000, -1.000000000000000000, 0.000000000000000000 ) ) ;
#827=CARTESIAN_POINT ( 'NONE',  ( -10.61943132853148697, -78.49189918985904058, -6.134787038820419092 ) ) ;
#831=LINE ( 'NONE', #40059, #35552 ) ;
#832=CARTESIAN_POINT ( 'NONE',  ( -7.627487525433000570, -60.09778754156999980, -10.35845608626999947 ) ) ;
#834=CARTESIAN_POINT ( 'NONE',  ( -0.4515105396345309163, -23.54721902468446615, -10.99076531923747169 ) ) ;
#837=CARTESIAN_POINT ( 'NONE',  ( 6.877869950458871173, -78.27974359454508146, 9.927636754982094303 ) ) ;
#842=LINE ( 'NONE', #22663, #35837 ) ;
#844=CARTESIAN_POINT ( 'NONE',  ( 2.076026496572000113, -1.729178536415000078, -2.969150124377000211 ) ) ;
#847=CARTESIAN_POINT ( 'NONE',  ( 12.70722176274191106, -24.41036110619398869, -1.610175936229214955 ) ) ;
#849=CARTESIAN_POINT ( 'NONE',  ( 13.98934701301999972, -69.37813015403000350, 1.420884290687999928E-05 ) ) ;
#850=CARTESIAN_POINT ( 'NONE',  ( 0.5999999999999999778, -18.84999999999999787, -12.00000000000000000 ) ) ;
#851=EDGE_CURVE ( 'NONE', #37067, #54376, #38681, .T. ) ;
#853=LINE ( 'NONE', #23260, #22232 ) ;
#861=DIRECTION ( 'NONE',  ( -1.205798306211979422E-11, -1.868136817095964273E-07, -0.9999999999999824585 ) ) ;
#863=CARTESIAN_POINT ( 'NONE',  ( 12.54981748959999877, -53.75163512338999539, 0.03767836620429999839 ) ) ;
#864=CARTESIAN_POINT ( 'NONE',  ( -3.180509609271000127, -77.65086001149001049, 12.23476839664999893 ) ) ;
#867=ORIENTED_EDGE ( 'NONE', *, *, #17371, .T. ) ;
#868=CARTESIAN_POINT ( 'NONE',  ( 1.779623408300066600, -54.66369130952791267, -12.71471627654026193 ) ) ;
#871=CARTESIAN_POINT ( 'NONE',  ( 9.533274928461036524, -75.89964387654679001, -6.929128638878494506 ) ) ;
#873=CARTESIAN_POINT ( 'NONE',  ( -12.50000000000000000, -17.31762331506999786, -1.005384022379999909 ) ) ;
#875=ORIENTED_EDGE ( 'NONE', *, *, #15950, .F. ) ;
#876=EDGE_CURVE ( 'NONE', #34959, #39806, #20595, .T. ) ;
#879=CARTESIAN_POINT ( 'NONE',  ( -2.062597265787999845, -19.21538333566000034, 12.87024489160000051 ) ) ;
#880=ORIENTED_EDGE ( 'NONE', *, *, #55863, .T. ) ;
#881=AXIS2_PLACEMENT_3D ( 'NONE', #18000, #35097, #17705 ) ;
#882=CARTESIAN_POINT ( 'NONE',  ( 12.50485692589171194, -24.86593462704852797, -0.6924071800257274312 ) ) ;
#883=SHAPE_REPRESENTATION_RELATIONSHIP ( 'NONE' , 'NONE' ,  #7439, #51784 ) ;
#888=CARTESIAN_POINT ( 'NONE',  ( 7.861032689861890077, -24.46660299217103329, -10.10708926022225107 ) ) ;
#890=EDGE_CURVE ( 'NONE', #52925, #8280, #49060, .T. ) ;
#891=VERTEX_POINT ( 'NONE', #42458 ) ;
#893=DIRECTION ( 'NONE',  ( -0.7071067811865475727, 0.000000000000000000, 0.7071067811865475727 ) ) ;
#895=CARTESIAN_POINT ( 'NONE',  ( 0.5135400119170026034, -16.82131466139542297, -12.70453250098683284 ) ) ;
#902=CARTESIAN_POINT ( 'NONE',  ( 6.153863461931999623, -76.18399160466999831, -10.66140155521000032 ) ) ;
#904=CARTESIAN_POINT ( 'NONE',  ( -0.05152873501919019023, -1.973120583389267546, -3.519131412915782242 ) ) ;
#905=CIRCLE ( 'NONE', #55587, 0.5000000000000001110 ) ;
#907=CARTESIAN_POINT ( 'NONE',  ( 12.49306764015999960, -18.71943464842000182, 1.667917367065999912 ) ) ;
#908=CARTESIAN_POINT ( 'NONE',  ( 10.16243366810999937, -79.22005705677000265, -6.864696462387000153 ) ) ;
#911=CARTESIAN_POINT ( 'NONE',  ( 1.337313094397592161, -2.759813985991205865, -2.961831082111990643 ) ) ;
#913=CARTESIAN_POINT ( 'NONE',  ( -1.206136157490516725, -77.16700393412037329, -11.95863077309826750 ) ) ;
#915=EDGE_LOOP ( 'NONE', ( #29593, #53331, #24815, #5796 ) ) ;
#920=DIRECTION ( 'NONE',  ( 0.000000000000000000, -0.7071067811866525998, -0.7071067811864425456 ) ) ;
#921=CARTESIAN_POINT ( 'NONE',  ( 7.970414252932632060, -24.52292089079952930, 9.713036876646206963 ) ) ;
#923=CONICAL_SURFACE ( 'NONE', #8425, 0.6999999997695030007, 0.7853981633972997312 ) ;
#926=CARTESIAN_POINT ( 'NONE',  ( 1.068457326610549929, -76.06767717856887145, 11.70300179015460351 ) ) ;
#930=ADVANCED_FACE ( 'NONE', ( #13751 ), #32043, .F. ) ;
#934=CARTESIAN_POINT ( 'NONE',  ( 12.50483450299711130, -17.13545441866522623, -0.6958183770738737284 ) ) ;
#936=CARTESIAN_POINT ( 'NONE',  ( 8.533817832784000856, -16.99473856456000220, -9.213092693308000847 ) ) ;
#937=CARTESIAN_POINT ( 'NONE',  ( 8.096452064242996016, -56.01421830980998351, -13.15643568217000769 ) ) ;
#938=ORIENTED_EDGE ( 'NONE', *, *, #40154, .T. ) ;
#943=CARTESIAN_POINT ( 'NONE',  ( -7.713973254602257690, -76.88321291978049032, 9.284400534344989353 ) ) ;
#946=B_SPLINE_CURVE_WITH_KNOTS ( 'NONE', 3,
 ( #53761, #12615, #7899, #26191, #7041, #7324 ),
 .UNSPECIFIED., .F., .F.,
 ( 4, 1, 1, 4 ),
 ( 0.000000000000000000, 0.3333333333333000081, 0.6666666666667000474, 1.000000000000000000 ),
 .UNSPECIFIED. ) ;
#947=LINE ( 'NONE', #41653, #22243 ) ;
#948=DIRECTION ( 'NONE',  ( -1.000000000000000000, 0.000000000000000000, 0.000000000000000000 ) ) ;
#953=DIRECTION ( 'NONE',  ( -1.000000000000000000, 0.000000000000000000, 0.000000000000000000 ) ) ;
#954=ORIENTED_EDGE ( 'NONE', *, *, #20729, .T. ) ;
#962=AXIS2_PLACEMENT_3D ( 'NONE', #18788, #9054, #54519 ) ;
#963=CARTESIAN_POINT ( 'NONE',  ( 8.950141054477999347, -62.00112627243999697, 8.958565985388998953 ) ) ;
#964=DIRECTION ( 'NONE',  ( 0.9999548435846228323, 0.000000000000000000, 0.009503199022040118363 ) ) ;
#970=ORIENTED_EDGE ( 'NONE', *, *, #39826, .F. ) ;
#975=CARTESIAN_POINT ( 'NONE',  ( 6.139551537448999063, -76.07905556059000673, 11.06116137296999824 ) ) ;
#976=ADVANCED_FACE ( 'NONE', ( #22913 ), #84, .F. ) ;
#982=CARTESIAN_POINT ( 'NONE',  ( -7.981656248348999227, -24.71865039503999739, -10.08154475890999890 ) ) ;
#983=CARTESIAN_POINT ( 'NONE',  ( -7.387512494710427369, -60.21532333328988784, 8.150146600852218981 ) ) ;
#985=EDGE_LOOP ( 'NONE', ( #21475, #16744, #42328, #26988, #17962 ) ) ;
#986=DIRECTION ( 'NONE',  ( 0.000000000000000000, 1.000000000000000000, 0.000000000000000000 ) ) ;
#990=CARTESIAN_POINT ( 'NONE',  ( -12.70556836352000118, -62.02772277195000328, -2.424224025342999716E-09 ) ) ;
#991=LINE ( 'NONE', #50567, #22240 ) ;
#992=CARTESIAN_POINT ( 'NONE',  ( 1.577025133314267302, -2.911963968962991700, -3.150092931446307087 ) ) ;
#1002=CARTESIAN_POINT ( 'NONE',  ( 2.352429030880999861, -3.130096044169000447, 3.193304126848000024 ) ) ;
#1005=CARTESIAN_POINT ( 'NONE',  ( 9.422842877294000274, -25.25952027282999879, -8.643944052295999825 ) ) ;
#1006=LINE ( 'NONE', #27243, #16655 ) ;
#1008=CARTESIAN_POINT ( 'NONE',  ( -8.485281374238999419, -55.54999999966999980, -8.485281374238999419 ) ) ;
#1010=CIRCLE ( 'NONE', #13211, 1.250000000000000444 ) ;
#1011=CARTESIAN_POINT ( 'NONE',  ( 12.00000000000000000, -23.15000000000000213, -0.5999999999999999778 ) ) ;
#1012=VECTOR ( 'NONE', #4692, 1000.000000000000114 ) ;
#1013=CARTESIAN_POINT ( 'NONE',  ( -10.48774103543000180, -21.75472018390999907, -7.686941364778000718 ) ) ;
#1015=CARTESIAN_POINT ( 'NONE',  ( 9.414496040419999545, -53.53736393982000408, -8.652369398682999702 ) ) ;
#1025=VERTEX_POINT ( 'NONE', #19004 ) ;
#1029=CARTESIAN_POINT ( 'NONE',  ( -0.7999999999999001243, -23.15000000002000036, 12.00000000000000000 ) ) ;
#1030=ORIENTED_EDGE ( 'NONE', *, *, #26943, .F. ) ;
#1031=EDGE_LOOP ( 'NONE', ( #26691, #45091, #56194 ) ) ;
#1034=B_SPLINE_CURVE_WITH_KNOTS ( 'NONE', 3,
 ( #49375, #18950, #54094, #41384, #54954, #14506, #40408, #3520, #4396, #22091, #26235, #52821, #30938, #21521, #13236, #12660, #58118 ),
 .UNSPECIFIED., .F., .F.,
 ( 4, 2, 1, 2, 2, 2, 2, 2, 4 ),
 ( 0.000000000000000000, 0.1250000000000000278, 0.2500000000000000555, 0.3750000000000001110, 0.5000000000000001110, 0.6250000000000001110, 0.7500000000000002220, 0.8750000000000002220, 1.000000000000000000 ),
 .UNSPECIFIED. ) ;
#1035=ORIENTED_EDGE ( 'NONE', *, *, #29087, .T. ) ;
#1036=DIRECTION ( 'NONE',  ( -0.7071067811865474617, 0.000000000000000000, -0.7071067811865474617 ) ) ;
#1037=FACE_OUTER_BOUND ( 'NONE', #4709, .T. ) ;
#1041=LINE ( 'NONE', #37019, #38264 ) ;
#1044=AXIS2_PLACEMENT_3D ( 'NONE', #18633, #54064, #19210 ) ;
#1045=CARTESIAN_POINT ( 'NONE',  ( -1.733997378023027114, -18.47616783230456861, -12.54437956612009764 ) ) ;
#1047=CARTESIAN_POINT ( 'NONE',  ( 0.2494208068450905480, -17.00711039237138422, 12.50614183113019529 ) ) ;
#1050=DIRECTION ( 'NONE',  ( -1.000000000000000000, 0.000000000000000000, 0.000000000000000000 ) ) ;
#1052=CARTESIAN_POINT ( 'NONE',  ( 5.488127745643000210, -77.17119367106998595, 11.56242237764000080 ) ) ;
#1061=DIRECTION ( 'NONE',  ( -1.000000000000000000, 0.000000000000000000, 0.000000000000000000 ) ) ;
#1063=CARTESIAN_POINT ( 'NONE',  ( -0.3113020967593000399, -2.698849349032999889, 3.793306396812999637 ) ) ;
#1067=CARTESIAN_POINT ( 'NONE',  ( -1.230457122653977109, -78.91666666666665719, -11.75000000000022737 ) ) ;
#1068=EDGE_CURVE ( 'NONE', #47711, #11745, #22843, .T. ) ;
#1069=CARTESIAN_POINT ( 'NONE',  ( 7.555116226634086551, -60.48684619743404056, -7.995796640818108258 ) ) ;
#1073=CARTESIAN_POINT ( 'NONE',  ( 12.50409217856652511, -17.47871355535288629, -1.233808107085542449 ) ) ;
#1076=CARTESIAN_POINT ( 'NONE',  ( 8.356119038218036366, -78.50935930058759027, 8.269166890618505406 ) ) ;
#1081=CARTESIAN_POINT ( 'NONE',  ( 0.7999999997951999786, -18.85000000927000130, -11.99999999979999821 ) ) ;
#1085=CARTESIAN_POINT ( 'NONE',  ( 3.165411199172024848, -2.770833333333333481, 0.8506806241676669877 ) ) ;
#1098=ORIENTED_EDGE ( 'NONE', *, *, #44386, .F. ) ;
#1100=EDGE_CURVE ( 'NONE', #27284, #51275, #44330, .T. ) ;
#1101=VERTEX_POINT ( 'NONE', #40564 ) ;
#1102=EDGE_LOOP ( 'NONE', ( #2121, #31598, #23793, #22455 ) ) ;
#1103=EDGE_LOOP ( 'NONE', ( #58066, #39904, #42472, #9931 ) ) ;
#1105=CARTESIAN_POINT ( 'NONE',  ( -8.343860018000999190, -60.54999999966955926, 8.343860018000999190 ) ) ;
#1106=ORIENTED_EDGE ( 'NONE', *, *, #18235, .F. ) ;
#1109=ORIENTED_EDGE ( 'NONE', *, *, #57711, .T. ) ;
#1113=LINE ( 'NONE', #19098, #19955 ) ;
#1115=DIRECTION ( 'NONE',  ( 0.000000000000000000, -1.000000000000000000, 0.000000000000000000 ) ) ;
#1116=CARTESIAN_POINT ( 'NONE',  ( -7.641012386020999969, -55.51082434643999619, -10.18589234707000202 ) ) ;
#1118=CARTESIAN_POINT ( 'NONE',  ( 2.296255511297609964, -76.55894423758236655, 11.52317862450651198 ) ) ;
#1122=CARTESIAN_POINT ( 'NONE',  ( 11.23426925451733283, -78.17300239647218518, -4.441224278447778673 ) ) ;
#1125=CARTESIAN_POINT ( 'NONE',  ( -1.750000000001000089, -55.54999998977000075, 12.56594317853999954 ) ) ;
#1132=CARTESIAN_POINT ( 'NONE',  ( 10.38645071868999992, -56.02180874340999850, 7.655542440077000244 ) ) ;
#1135=DIRECTION ( 'NONE',  ( 0.000000000000000000, 1.000000000000000000, 0.000000000000000000 ) ) ;
#1137=CARTESIAN_POINT ( 'NONE',  ( -7.864802647417423742, -24.45123893519480163, -10.10444599041134417 ) ) ;
#1139=LINE ( 'NONE', #27384, #57130 ) ;
#1140=CARTESIAN_POINT ( 'NONE',  ( 2.065550207748000133, -60.22565079297999802, 12.82162303857000119 ) ) ;
#1142=CARTESIAN_POINT ( 'NONE',  ( -11.56077433994999915, -76.14243477331000065, 3.934723564722999445 ) ) ;
#1143=ORIENTED_EDGE ( 'NONE', *, *, #46270, .T. ) ;
#1146=EDGE_CURVE ( 'NONE', #4486, #43269, #17668, .T. ) ;
#1147=( GEOMETRIC_REPRESENTATION_CONTEXT ( 3 ) GLOBAL_UNCERTAINTY_ASSIGNED_CONTEXT ( ( #42560 ) ) GLOBAL_UNIT_ASSIGNED_CONTEXT ( ( #602, #9716, #54595 ) ) REPRESENTATION_CONTEXT ( 'NONE', 'WORKASPACE' ) );
#1149=FACE_OUTER_BOUND ( 'NONE', #35371, .T. ) ;
#1151=CARTESIAN_POINT ( 'NONE',  ( 12.43645963087999995, -53.88248289507999544, 0.05235777564056001004 ) ) ;
#1157=CARTESIAN_POINT ( 'NONE',  ( 1.980611416588874185, -55.27402268162217780, -12.74335092660349389 ) ) ;
#1160=EDGE_LOOP ( 'NONE', ( #26593, #42845, #38961, #39472 ) ) ;
#1162=DIRECTION ( 'NONE',  ( 0.000000000000000000, -1.000000000000000000, 5.958196898821999917E-14 ) ) ;
#1163=ORIENTED_EDGE ( 'NONE', *, *, #16816, .F. ) ;
#1166=CARTESIAN_POINT ( 'NONE',  ( 8.838834764832000701, -55.54999999966999980, -8.838834764832000701 ) ) ;
#1167=AXIS2_PLACEMENT_3D ( 'NONE', #42050, #50336, #23163 ) ;
#1168=ORIENTED_EDGE ( 'NONE', *, *, #49819, .F. ) ;
#1169=AXIS2_PLACEMENT_3D ( 'NONE', #31596, #41353, #13599 ) ;
#1170=ORIENTED_EDGE ( 'NONE', *, *, #30015, .T. ) ;
#1171=CARTESIAN_POINT ( 'NONE',  ( 12.50728630770444560, -24.99975539312146822, -0.1757873578727420505 ) ) ;
#1174=CARTESIAN_POINT ( 'NONE',  ( 12.44180763921999855, -54.70743932605000026, 1.459474665415000150 ) ) ;
#1176=CARTESIAN_POINT ( 'NONE',  ( -12.61117499582000079, -23.21550664553999965, -1.798980867984000032 ) ) ;
#1179=DIRECTION ( 'NONE',  ( 0.000000000000000000, -1.000000000000000000, 0.000000000000000000 ) ) ;
#1181=CARTESIAN_POINT ( 'NONE',  ( 0.9935076046793005489, -17.03183812245195483, -12.70250268216991962 ) ) ;
#1185=CARTESIAN_POINT ( 'NONE',  ( -1.618935784642312470, -23.92751168673102669, 12.52134385800258798 ) ) ;
#1186=VERTEX_POINT ( 'NONE', #51887 ) ;
#1187=CARTESIAN_POINT ( 'NONE',  ( -9.662446363796000526, -76.46415837332999388, 7.627099640079999965 ) ) ;
#1190=CARTESIAN_POINT ( 'NONE',  ( -3.184394476902560722, -2.314159630480875141, 1.502279350439443606 ) ) ;
#1191=CARTESIAN_POINT ( 'NONE',  ( 7.647735717269999789, -60.52294882350999927, -10.13404777204000062 ) ) ;
#1192=CARTESIAN_POINT ( 'NONE',  ( 7.914613980750001332, -79.36968659573999219, 9.019916049260999102 ) ) ;
#1195=DIRECTION ( 'NONE',  ( 0.7071067811865475727, 0.000000000000000000, -0.7071067811865475727 ) ) ;
#1196=CARTESIAN_POINT ( 'NONE',  ( -8.811774560614452412, -78.10987123251830155, -8.257849517617557922 ) ) ;
#1198=ORIENTED_EDGE ( 'NONE', *, *, #12691, .T. ) ;
#1200=EDGE_CURVE ( 'NONE', #35836, #20895, #57455, .T. ) ;
#1201=CARTESIAN_POINT ( 'NONE',  ( -3.075537641221531615, -77.90416666666671119, -11.44417895085270942 ) ) ;
#1202=CARTESIAN_POINT ( 'NONE',  ( 9.841120606706802221, -24.83627250047061352, 8.121699444506939258 ) ) ;
#1203=AXIS2_PLACEMENT_3D ( 'NONE', #10695, #42275, #13936 ) ;
#1205=CARTESIAN_POINT ( 'NONE',  ( 1.785023577804000228, -3.459384265120000190, -3.219039020423000164 ) ) ;
#1208=CARTESIAN_POINT ( 'NONE',  ( 1.986041313562282973, -76.06139900838468293, 11.58506530393337286 ) ) ;
#1215=EDGE_CURVE ( 'NONE', #44340, #8841, #2830, .T. ) ;
#1216=CARTESIAN_POINT ( 'NONE',  ( 0.000000000000000000, -46.43897132165000130, 0.000000000000000000 ) ) ;
#1218=EDGE_CURVE ( 'NONE', #30942, #41447, #16073, .T. ) ;
#1221=CARTESIAN_POINT ( 'NONE',  ( 8.950130560568000604, -16.79887407354000217, -8.958576480220999727 ) ) ;
#1222=CARTESIAN_POINT ( 'NONE',  ( -7.714303428875997959, -63.10294702886003648, -12.53545825868000385 ) ) ;
#1223=ORIENTED_EDGE ( 'NONE', *, *, #43625, .T. ) ;
#1227=CARTESIAN_POINT ( 'NONE',  ( -1.720923278860959860, -77.83943615250160519, 11.89782049558834487 ) ) ;
#1228=CIRCLE ( 'NONE', #34175, 0.5000000000000006661 ) ;
#1233=EDGE_CURVE ( 'NONE', #47045, #42541, #31119, .T. ) ;
#1239=VERTEX_POINT ( 'NONE', #21149 ) ;
#1242=EDGE_LOOP ( 'NONE', ( #57133, #25375, #53679, #42631 ) ) ;
#1243=LINE ( 'NONE', #28361, #50083 ) ;
#1245=EDGE_CURVE ( 'NONE', #20659, #25961, #47754, .T. ) ;
#1248=CARTESIAN_POINT ( 'NONE',  ( 7.753906807064999462, -61.08933445950000163, 10.31979621052999896 ) ) ;
#1249=CARTESIAN_POINT ( 'NONE',  ( 8.190859204290999784, -55.64999999967000122, -7.342331066867000544 ) ) ;
#1251=AXIS2_PLACEMENT_3D ( 'NONE', #2632, #56072, #6466 ) ;
#1253=VERTEX_POINT ( 'NONE', #11443 ) ;
#1254=DIRECTION ( 'NONE',  ( 0.000000000000000000, -1.000000000000000000, 0.000000000000000000 ) ) ;
#1261=CARTESIAN_POINT ( 'NONE',  ( 6.675876141078999737, -76.41361125212999639, -10.74461650742999907 ) ) ;
#1262=CARTESIAN_POINT ( 'NONE',  ( -0.1360749694821127842, -2.121642350341124139, -3.272092924714451456 ) ) ;
#1266=CARTESIAN_POINT ( 'NONE',  ( 12.70259419122522360, -61.53882758488509808, 1.314635108493669824 ) ) ;
#1267=CARTESIAN_POINT ( 'NONE',  ( 12.82904091336000008, -55.47547470607999998, -2.062673488738000049 ) ) ;
#1273=CARTESIAN_POINT ( 'NONE',  ( -7.618386520043000765, -18.77287536652999833, 10.53495200520000097 ) ) ;
#1275=CARTESIAN_POINT ( 'NONE',  ( -3.520054962697148238, -3.246692171245472824, 0.1437326420056305454 ) ) ;
#1284=CARTESIAN_POINT ( 'NONE',  ( -7.342331066867000544, -55.64999999967000122, 8.190859204290999784 ) ) ;
#1287=CARTESIAN_POINT ( 'NONE',  ( 7.760939450736999312, -24.23085356333000107, -10.15321588359000060 ) ) ;
#1290=CARTESIAN_POINT ( 'NONE',  ( 0.000000000000000000, -0.09999999858569999511, -8.899999998586000771 ) ) ;
#1291=DIRECTION ( 'NONE',  ( 0.000000000000000000, 1.000000000000000000, 0.000000000000000000 ) ) ;
#1294=AXIS2_PLACEMENT_3D ( 'NONE', #2770, #29610, #20769 ) ;
#1295=CARTESIAN_POINT ( 'NONE',  ( 10.53494359612999887, -55.57285042800999264, -7.618393753177000072 ) ) ;
#1296=B_SPLINE_SURFACE_WITH_KNOTS ( 'NONE', 3, 3, ( 
 ( #3151, #6406, #48038, #56011 ),
 ( #43015, #29125, #29984, #25282 ),
 ( #24422, #37986, #38571, #46877 ),
 ( #15852, #24994, #15561, #7568 ),
 ( #51877, #52446, #7280, #33554 ),
 ( #20853, #16433, #16145, #34122 ),
 ( #2571, #43300, #11721, #51592 ),
 ( #25568, #57156, #16721, #43588 ) ),
 .UNSPECIFIED., .F., .F., .F.,
 ( 4, 1, 1, 1, 1, 4 ),
 ( 4, 4 ),
 ( -0.01200407345747999885, 0.000000000000000000, 0.3333333333333000081, 0.6666666666667000474, 1.000000000000000000, 1.011997855551999947 ),
 ( -0.3559705542741000150, 1.355970554273999928 ),
 .UNSPECIFIED. ) ;
#1302=CARTESIAN_POINT ( 'NONE',  ( -13.86363625866555438, -46.43897132165000130, -0.001706075946091080518 ) ) ;
#1310=EDGE_CURVE ( 'NONE', #19532, #6714, #17878, .T. ) ;
#1312=CARTESIAN_POINT ( 'NONE',  ( 8.799999998347999508, 1.651506244335999933E-09, 5.811483786157999589E-09 ) ) ;
#1314=ORIENTED_EDGE ( 'NONE', *, *, #47629, .F. ) ;
#1318=CARTESIAN_POINT ( 'NONE',  ( 1.761265949708000100, -18.29141781213999707, 12.57448205042999945 ) ) ;
#1322=EDGE_CURVE ( 'NONE', #23950, #1742, #20864, .T. ) ;
#1324=LINE ( 'NONE', #28445, #17527 ) ;
#1325=ORIENTED_EDGE ( 'NONE', *, *, #7961, .F. ) ;
#1330=CARTESIAN_POINT ( 'NONE',  ( -1.247385801055000076, -17.52277743740000204, 12.50301438876999960 ) ) ;
#1333=CARTESIAN_POINT ( 'NONE',  ( -10.04115011118000211, -22.76486430425999785, 7.682331425175999762 ) ) ;
#1336=AXIS2_PLACEMENT_3D ( 'NONE', #29778, #12086, #56675 ) ;
#1337=EDGE_CURVE ( 'NONE', #38648, #12253, #38058, .T. ) ;
#1339=CARTESIAN_POINT ( 'NONE',  ( 0.1632771479509232126, -76.57380765581523008, 11.74886050266104220 ) ) ;
#1340=B_SPLINE_CURVE_WITH_KNOTS ( 'NONE', 3,
 ( #54873, #14420, #882, #32417, #1171, #1749 ),
 .UNSPECIFIED., .F., .F.,
 ( 4, 2, 4 ),
 ( 0.000000000000000000, 0.5000000000000001110, 1.000000000000000000 ),
 .UNSPECIFIED. ) ;
#1347=FACE_BOUND ( 'NONE', #23375, .T. ) ;
#1348=CARTESIAN_POINT ( 'NONE',  ( -3.054513261463999818, -2.868203725971999685, -2.270689576097000284 ) ) ;
#1351=CARTESIAN_POINT ( 'NONE',  ( 0.8205724371039223586, -3.500000000000000000, -3.402696673547657813 ) ) ;
#1352=DIRECTION ( 'NONE',  ( -5.380858151921000126E-11, -1.000000000000000000, 8.802973286544000911E-11 ) ) ;
#1354=CARTESIAN_POINT ( 'NONE',  ( 1.931086388455000025, -60.09778595451999905, 12.71798280857999863 ) ) ;
#1355=FACE_OUTER_BOUND ( 'NONE', #6251, .T. ) ;
#1358=CARTESIAN_POINT ( 'NONE',  ( -12.00000000000000000, -23.15000000002000036, -0.7999999999999001243 ) ) ;
#1360=CIRCLE ( 'NONE', #7946, 12.50000000000000000 ) ;
#1362=LINE ( 'NONE', #9627, #50266 ) ;
#1365=CARTESIAN_POINT ( 'NONE',  ( -1.818468715484000065E-14, -79.21250000010999770, 0.000000000000000000 ) ) ;
#1372=LINE ( 'NONE', #42391, #21489 ) ;
#1373=ORIENTED_EDGE ( 'NONE', *, *, #42922, .T. ) ;
#1375=AXIS2_PLACEMENT_3D ( 'NONE', #5775, #23782, #51256 ) ;
#1376=DIRECTION ( 'NONE',  ( 0.000000000000000000, -1.000000000000000000, 0.000000000000000000 ) ) ;
#1377=CARTESIAN_POINT ( 'NONE',  ( -8.414570695956999913, -60.64999999943950826, -8.414570695956999913 ) ) ;
#1378=EDGE_LOOP ( 'NONE', ( #40195, #20507, #12745, #17622 ) ) ;
#1381=VECTOR ( 'NONE', #38761, 1000.000000000000000 ) ;
#1384=CARTESIAN_POINT ( 'NONE',  ( 8.180687091746225548, -60.10655143787244725, 7.353725627631166439 ) ) ;
#1388=CARTESIAN_POINT ( 'NONE',  ( -12.80090744921000123, -19.23767312576000066, -1.980532734072999901 ) ) ;
#1389=ORIENTED_EDGE ( 'NONE', *, *, #429, .F. ) ;
#1391=CARTESIAN_POINT ( 'NONE',  ( -7.678690995210999404, -58.55648180022999583, 10.59551070212999946 ) ) ;
#1392=ORIENTED_EDGE ( 'NONE', *, *, #10378, .T. ) ;
#1400=EDGE_CURVE ( 'NONE', #3338, #53933, #13132, .T. ) ;
#1401=CARTESIAN_POINT ( 'NONE',  ( -3.250000000000000000, -3.100000000000000089, 0.000000000000000000 ) ) ;
#1402=EDGE_CURVE ( 'NONE', #2960, #30023, #33196, .T. ) ;
#1403=AXIS2_PLACEMENT_3D ( 'NONE', #46658, #38348, #55199 ) ;
#1404=CARTESIAN_POINT ( 'NONE',  ( -7.640030139773000606, -60.10716934574000447, -10.18491068061999982 ) ) ;
#1406=CARTESIAN_POINT ( 'NONE',  ( 8.944043683863377225, -76.50578467936081495, 7.623615284876848364 ) ) ;
#1407=CARTESIAN_POINT ( 'NONE',  ( -0.5200379331645087477, -23.45155696398142808, -10.98772212209864385 ) ) ;
#1409=VECTOR ( 'NONE', #7391, 1000.000000000000000 ) ;
#1411=CARTESIAN_POINT ( 'NONE',  ( -0.5668640744825168554, -61.71659694886608349, -12.50470739229184325 ) ) ;
#1414=PLANE ( 'NONE',  #5891 ) ;
#1419=B_SPLINE_CURVE_WITH_KNOTS ( 'NONE', 3,
 ( #10060, #14755, #10346, #5902, #41633, #10938, #24210, #19206, #32754, #50801 ),
 .UNSPECIFIED., .F., .F.,
 ( 4, 2, 2, 2, 4 ),
 ( 0.000000000000000000, 0.2500000000000000000, 0.5000000000000000000, 0.7500000000000000000, 1.000000000000000000 ),
 .UNSPECIFIED. ) ;
#1420=CARTESIAN_POINT ( 'NONE',  ( -10.53494356941000021, -60.02715052954999919, -7.618393677181999557 ) ) ;
#1424=CARTESIAN_POINT ( 'NONE',  ( -1.669849926071999890, -23.37228600417000024, -12.48404299553000030 ) ) ;
#1425=CARTESIAN_POINT ( 'NONE',  ( -3.170501611485000204, -2.010283069270999867, 1.448148066727999783 ) ) ;
#1427=CARTESIAN_POINT ( 'NONE',  ( -7.712213536729100483, -24.06179137615005814, -10.27334987165781399 ) ) ;
#1428=EDGE_CURVE ( 'NONE', #49604, #32986, #23478, .T. ) ;
#1430=CARTESIAN_POINT ( 'NONE',  ( 7.651160336710000287, -19.23767313813999991, 10.45205658995999976 ) ) ;
#1432=CARTESIAN_POINT ( 'NONE',  ( -6.591778134092000307, -75.74638372273000186, -9.790090750544999665 ) ) ;
#1433=ORIENTED_EDGE ( 'NONE', *, *, #28938, .T. ) ;
#1437=CYLINDRICAL_SURFACE ( 'NONE', #24296, 1.750000000000000000 ) ;
#1439=CARTESIAN_POINT ( 'NONE',  ( 10.28132586880103894, -76.61033914466867145, -6.022081058836299405 ) ) ;
#1445=CARTESIAN_POINT ( 'NONE',  ( 3.599999993293999889, -0.2000000067061999953, 5.600095136020000205E-09 ) ) ;
#1446=DIRECTION ( 'NONE',  ( 0.000000000000000000, 1.000000000000000000, 0.000000000000000000 ) ) ;
#1451=EDGE_LOOP ( 'NONE', ( #14582, #26391, #19013, #53979, #53142, #45615, #22892 ) ) ;
#1454=AXIS2_PLACEMENT_3D ( 'NONE', #14439, #40440, #50479 ) ;
#1455=CARTESIAN_POINT ( 'NONE',  ( 10.10447584125107490, -61.25118490511742664, -7.864774383105173960 ) ) ;
#1458=FACE_OUTER_BOUND ( 'NONE', #537, .T. ) ;
#1459=EDGE_CURVE ( 'NONE', #10086, #28795, #8421, .T. ) ;
#1460=AXIS2_PLACEMENT_3D ( 'NONE', #35793, #57963, #39088 ) ;
#1462=VERTEX_POINT ( 'NONE', #46530 ) ;
#1463=CARTESIAN_POINT ( 'NONE',  ( -7.639893379675799068, -55.41284423887100985, 10.11462454828661528 ) ) ;
#1464=CARTESIAN_POINT ( 'NONE',  ( 10.20678250197623882, -24.23575784472138039, -7.770339463571165339 ) ) ;
#1466=ORIENTED_EDGE ( 'NONE', *, *, #21295, .F. ) ;
#1470=CARTESIAN_POINT ( 'NONE',  ( 1.718598679953219799, -17.75037066952814513, -12.71111582767946935 ) ) ;
#1472=EDGE_CURVE ( 'NONE', #35427, #47711, #38605, .T. ) ;
#1476=CARTESIAN_POINT ( 'NONE',  ( -12.19234209666000091, -75.99367673319000005, -1.697737568323999913 ) ) ;
#1477=B_SPLINE_SURFACE_WITH_KNOTS ( 'NONE', 3, 3, ( 
 ( #29757, #29477, #47536, #7061 ),
 ( #47814, #25632, #43360, #2643 ),
 ( #43655, #39208, #20920, #26489 ),
 ( #4368, #26785, #58389, #17355 ),
 ( #13799, #44814, #22670, #30914 ),
 ( #28475, #58092, #45415, #22369 ),
 ( #18253, #274, #32898, #27378 ),
 ( #40381, #17951, #50943, #10490 ),
 ( #46526, #45121, #8493, #35943 ),
 ( #4958, #53366, #53970, #6050 ),
 ( #57797, #36245, #53668, #44513 ) ),
 .UNSPECIFIED., .F., .F., .F.,
 ( 4, 1, 1, 1, 1, 1, 1, 1, 4 ),
 ( 4, 4 ),
 ( -0.02001474922158999817, 0.000000000000000000, 0.1666666666667000196, 0.3333333333333000081, 0.5000000000000000000, 0.6666666666667000474, 0.8333333333333000637, 1.000000000000000000, 1.020283381528000133 ),
 ( -0.3582002740342999925, 1.358862457857999972 ),
 .UNSPECIFIED. ) ;
#1478=CARTESIAN_POINT ( 'NONE',  ( -3.219784822078160857, -2.382367439899148565, -1.420610107900855068 ) ) ;
#1479=CARTESIAN_POINT ( 'NONE',  ( 7.762981007074000850, -60.96089459184000248, -9.992000916374999875 ) ) ;
#1480=CARTESIAN_POINT ( 'NONE',  ( 11.03890801094999929, -78.69679818280999939, -5.342433469444999972 ) ) ;
#1483=CARTESIAN_POINT ( 'NONE',  ( 10.12290050255000118, -60.04999997790999799, -7.648026768390999486 ) ) ;
#1484=CARTESIAN_POINT ( 'NONE',  ( 11.55486890050020143, -78.32335062082758270, 3.501387709252974823 ) ) ;
#1486=AXIS2_PLACEMENT_3D ( 'NONE', #44518, #48386, #13514 ) ;
#1487=ORIENTED_EDGE ( 'NONE', *, *, #35079, .F. ) ;
#1490=CARTESIAN_POINT ( 'NONE',  ( 7.730443418312603399, -24.12191635826273739, 10.25197760564498140 ) ) ;
#1492=CARTESIAN_POINT ( 'NONE',  ( -0.4714591427245999888, -2.679096200086999779, 3.841621304652000024 ) ) ;
#1495=CARTESIAN_POINT ( 'NONE',  ( -11.06942781765597239, -76.17262117212699479, 3.959973230732274807 ) ) ;
#1496=CARTESIAN_POINT ( 'NONE',  ( 0.000000000000000000, -28.92928575306000383, 0.000000000000000000 ) ) ;
#1500=CARTESIAN_POINT ( 'NONE',  ( 12.70249480706760359, -24.96498603299019692, 0.9989402950733060615 ) ) ;
#1502=DIRECTION ( 'NONE',  ( 0.000000000000000000, 0.000000000000000000, -1.000000000000000000 ) ) ;
#1504=DIRECTION ( 'NONE',  ( 0.000000000000000000, -1.000000000000000000, 0.000000000000000000 ) ) ;
#1506=CARTESIAN_POINT ( 'NONE',  ( 10.31444587878999997, -17.69924218095000157, -7.758886158107999975 ) ) ;
#1507=CARTESIAN_POINT ( 'NONE',  ( -8.130813118010999929, -17.31476110167000115, 9.546856411653001473 ) ) ;
#1511=CARTESIAN_POINT ( 'NONE',  ( 12.70619604129601754, -54.33855724441239943, 1.571828507126210583 ) ) ;
#1514=CARTESIAN_POINT ( 'NONE',  ( -5.207681435413956450, -77.36354831110318742, 10.89428926699400613 ) ) ;
#1518=CARTESIAN_POINT ( 'NONE',  ( 10.98676125741665643, -23.41445108201793346, -0.5397229578417962470 ) ) ;
#1519=CARTESIAN_POINT ( 'NONE',  ( 1.980532734072999901, -22.76232686847000153, 12.80090744964000038 ) ) ;
#1521=AXIS2_PLACEMENT_3D ( 'NONE', #570, #37410, #50142 ) ;
#1528=EDGE_LOOP ( 'NONE', ( #31135, #36616, #40114, #40612 ) ) ;
#1530=VECTOR ( 'NONE', #9099, 1000.000000000000227 ) ;
#1532=CIRCLE ( 'NONE', #49613, 10.20000000000000107 ) ;
#1533=CARTESIAN_POINT ( 'NONE',  ( 10.01749676171999859, -59.99181054660999735, 7.660430254678000317 ) ) ;
#1534=DIRECTION ( 'NONE',  ( 0.000000000000000000, 0.000000000000000000, -1.000000000000000000 ) ) ;
#1537=EDGE_CURVE ( 'NONE', #26186, #2183, #11950, .T. ) ;
#1538=VERTEX_POINT ( 'NONE', #8091 ) ;
#1545=FACE_OUTER_BOUND ( 'NONE', #50328, .T. ) ;
#1550=CARTESIAN_POINT ( 'NONE',  ( -7.646092217281999837, -23.70851177913000285, -10.13691708057999996 ) ) ;
#1551=CARTESIAN_POINT ( 'NONE',  ( 12.60552511008000032, -55.51082276539999327, -1.799501877793999949 ) ) ;
#1554=PLANE ( 'NONE',  #49481 ) ;
#1558=CARTESIAN_POINT ( 'NONE',  ( -7.761025538858000061, -17.91850014421000026, 9.835174270523999951 ) ) ;
#1560=CARTESIAN_POINT ( 'NONE',  ( 3.432173245281677776, -3.481906583660260068, -0.7953295766101289299 ) ) ;
#1565=CARTESIAN_POINT ( 'NONE',  ( 3.350260413882198751, -0.8997395809787506193, -0.4376960103309309735 ) ) ;
#1567=VERTEX_POINT ( 'NONE', #3093 ) ;
#1569=CARTESIAN_POINT ( 'NONE',  ( -1.288488638071999981, -61.33564939335000332, -12.54709296486000092 ) ) ;
#1575=DIRECTION ( 'NONE',  ( -0.7071067811865475727, 0.000000000000000000, 0.7071067811865475727 ) ) ;
#1576=CARTESIAN_POINT ( 'NONE',  ( 7.601397897754999633, -60.04999999966999980, 9.369164850722000892 ) ) ;
#1577=VECTOR ( 'NONE', #43379, 1000.000000000000114 ) ;
#1578=EDGE_CURVE ( 'NONE', #53933, #18065, #51819, .T. ) ;
#1582=EDGE_CURVE ( 'NONE', #30942, #30461, #15044, .T. ) ;
#1583=CARTESIAN_POINT ( 'NONE',  ( 8.220399303298000504, -53.98050618241000365, -9.523318109972001011 ) ) ;
#1593=CARTESIAN_POINT ( 'NONE',  ( -9.164374456753368037, -53.58432317374141007, 8.803712804513708079 ) ) ;
#1597=CARTESIAN_POINT ( 'NONE',  ( -8.061017305527000687, -55.64999999967000122, -8.909545442949999838 ) ) ;
#1599=ORIENTED_EDGE ( 'NONE', *, *, #8311, .T. ) ;
#1601=EDGE_CURVE ( 'NONE', #6077, #42913, #31029, .T. ) ;
#1614=CARTESIAN_POINT ( 'NONE',  ( 12.56594317991999965, -60.04999999381999487, 1.750000000001000089 ) ) ;
#1617=EDGE_CURVE ( 'NONE', #32631, #55158, #12186, .T. ) ;
#1618=CIRCLE ( 'NONE', #53470, 5.000000000000000888 ) ;
#1619=CARTESIAN_POINT ( 'NONE',  ( -1.495357591794768792, -61.35876337328221553, -12.70444646763206187 ) ) ;
#1621=CARTESIAN_POINT ( 'NONE',  ( 1.750000000000000000, -23.24999999758999536, 12.50000000000000000 ) ) ;
#1622=CARTESIAN_POINT ( 'NONE',  ( -10.35845608625999859, -23.29778754190000001, 7.627487525415999947 ) ) ;
#1623=VECTOR ( 'NONE', #17349, 1000.000000000000000 ) ;
#1626=CARTESIAN_POINT ( 'NONE',  ( 8.414570695956999913, -55.64999999967000122, 8.414570695956999913 ) ) ;
#1627=CARTESIAN_POINT ( 'NONE',  ( -7.814543345298289978, -76.63258160818318743, 8.778123181643341155 ) ) ;
#1629=AXIS2_PLACEMENT_3D ( 'NONE', #41502, #32619, #24074 ) ;
#1630=CARTESIAN_POINT ( 'NONE',  ( -10.18114972180999978, -55.40990354248999950, 7.633087078966999783 ) ) ;
#1633=CARTESIAN_POINT ( 'NONE',  ( 1.930989144707000005, -20.24634220924000161, -12.80900240957999969 ) ) ;
#1634=CARTESIAN_POINT ( 'NONE',  ( -7.954951288349001004, -55.35321828636000419, 9.722718241315000398 ) ) ;
#1635=CARTESIAN_POINT ( 'NONE',  ( 0.5045596072230998930, -16.86471086961999788, -12.66210649709999991 ) ) ;
#1636=ADVANCED_FACE ( 'NONE', ( #3379 ), #43531, .F. ) ;
#1637=DIRECTION ( 'NONE',  ( 0.000000000000000000, 1.000000000000000000, 0.000000000000000000 ) ) ;
#1642=CARTESIAN_POINT ( 'NONE',  ( -1.729821627806567008, -3.500000000000000000, -2.913428096262390632 ) ) ;
#1644=CARTESIAN_POINT ( 'NONE',  ( -0.4820079653506728623, -18.48385402702410119, -10.98957811953281904 ) ) ;
#1648=CARTESIAN_POINT ( 'NONE',  ( 7.349802007153999561, -77.62076194170001031, -10.73869877321999944 ) ) ;
#1655=DIRECTION ( 'NONE',  ( 0.000000000000000000, 1.000000000000000000, 0.000000000000000000 ) ) ;
#1658=CARTESIAN_POINT ( 'NONE',  ( 7.655983890326024444, -55.09663439855413714, 10.06694524866116147 ) ) ;
#1663=DIRECTION ( 'NONE',  ( -1.000000000000000000, 0.000000000000000000, 0.000000000000000000 ) ) ;
#1665=ORIENTED_EDGE ( 'NONE', *, *, #51212, .F. ) ;
#1666=ORIENTED_EDGE ( 'NONE', *, *, #14435, .T. ) ;
#1670=VECTOR ( 'NONE', #32559, 1000.000000000000000 ) ;
#1671=ORIENTED_EDGE ( 'NONE', *, *, #7254, .T. ) ;
#1673=ORIENTED_EDGE ( 'NONE', *, *, #15183, .F. ) ;
#1675=CARTESIAN_POINT ( 'NONE',  ( 7.889735440107603637, -60.55042584425824259, 7.666647577135394798 ) ) ;
#1676=CIRCLE ( 'NONE', #40298, 12.80000000000000071 ) ;
#1677=VERTEX_POINT ( 'NONE', #34934 ) ;
#1681=DIRECTION ( 'NONE',  ( 0.000000000000000000, -1.000000000000000000, 0.000000000000000000 ) ) ;
#1682=CARTESIAN_POINT ( 'NONE',  ( -7.655555357447999754, -59.57795407677000554, 10.38646360829999971 ) ) ;
#1688=CARTESIAN_POINT ( 'NONE',  ( 1.514295266944117202, -0.9609374997565883758, 2.965304924911553286 ) ) ;
#1692=CARTESIAN_POINT ( 'NONE',  ( -7.612971414731999786, -60.12452529330000317, -10.53003223724999948 ) ) ;
#1694=CARTESIAN_POINT ( 'NONE',  ( 4.595623807310805553, -76.54268455229363610, 10.81386401082669302 ) ) ;
#1698=CARTESIAN_POINT ( 'NONE',  ( -3.069186940681134068, -3.074782183695690563, 1.066787720914930793 ) ) ;
#1705=CARTESIAN_POINT ( 'NONE',  ( -8.748876674203279080, -76.25764068747936619, -7.844724932001823525 ) ) ;
#1707=B_SPLINE_SURFACE_WITH_KNOTS ( 'NONE', 3, 3, ( 
 ( #44007, #38, #17722, #54031 ),
 ( #7983, #35403, #57286, #25981 ),
 ( #57568, #17132, #35115, #53149 ),
 ( #12696, #30691, #8271, #26273 ),
 ( #44287, #17417, #18889, #10035 ),
 ( #41906, #36303, #45770, #332 ),
 ( #27140, #41322, #622, #907 ),
 ( #45181, #36882, #32729, #55189 ) ),
 .UNSPECIFIED., .F., .F., .F.,
 ( 4, 1, 1, 1, 1, 4 ),
 ( 4, 4 ),
 ( -0.01200407347462000007, 0.000000000000000000, 0.3333333333333000081, 0.6666666666667000474, 1.000000000000000000, 1.011997855551999947 ),
 ( -0.3559705542741999906, 1.355970554273999928 ),
 .UNSPECIFIED. ) ;
#1708=CARTESIAN_POINT ( 'NONE',  ( 0.9356112518272206025, -24.74107830239327299, 12.50329130247346221 ) ) ;
#1709=DIRECTION ( 'NONE',  ( 0.000000000000000000, 1.000000000000000000, 0.000000000000000000 ) ) ;
#1710=AXIS2_PLACEMENT_3D ( 'NONE', #14779, #1816, #28063 ) ;
#1712=DIRECTION ( 'NONE',  ( -0.7071067811865475727, 0.000000000000000000, -0.7071067811865475727 ) ) ;
#1714=DIRECTION ( 'NONE',  ( -0.7071067811865975328, 0.7071067811864976127, -4.569514892260985645E-09 ) ) ;
#1717=CARTESIAN_POINT ( 'NONE',  ( 7.764656528435081917, -78.37973930036693559, -8.854160864976853063 ) ) ;
#1718=AXIS2_PLACEMENT_3D ( 'NONE', #37899, #17194, #40515 ) ;
#1720=CARTESIAN_POINT ( 'NONE',  ( 6.025108025436000325, -76.50248118292999777, 10.62222322076999959 ) ) ;
#1722=ADVANCED_FACE ( 'NONE', ( #34071 ), #52108, .F. ) ;
#1726=CARTESIAN_POINT ( 'NONE',  ( 12.66315196852000113, -61.97802884675999735, -0.06065366946605000448 ) ) ;
#1728=CARTESIAN_POINT ( 'NONE',  ( 12.44209697057999975, -54.71557297424000410, -1.464771213333999844 ) ) ;
#1731=DIRECTION ( 'NONE',  ( -0.9999999999999998890, 1.433665241479999788E-08, 0.000000000000000000 ) ) ;
#1733=ORIENTED_EDGE ( 'NONE', *, *, #18790, .F. ) ;
#1734=CARTESIAN_POINT ( 'NONE',  ( -12.00000000000000000, -18.84999999997999964, 0.7999999999999001243 ) ) ;
#1742=VERTEX_POINT ( 'NONE', #48830 ) ;
#1748=AXIS2_PLACEMENT_3D ( 'NONE', #19915, #3558, #48166 ) ;
#1749=CARTESIAN_POINT ( 'NONE',  ( 12.50745077490000057, -24.99994448286999926, 2.662071812989000278E-09 ) ) ;
#1752=EDGE_LOOP ( 'NONE', ( #3176, #25878, #22986, #48986 ) ) ;
#1753=CARTESIAN_POINT ( 'NONE',  ( 12.77568125274000010, -53.53490786090000597, 0.5296379231471999294 ) ) ;
#1754=DIRECTION ( 'NONE',  ( 0.0001230612157847738313, 0.000000000000000000, -0.9999999924279686647 ) ) ;
#1755=VERTEX_POINT ( 'NONE', #50010 ) ;
#1756=CARTESIAN_POINT ( 'NONE',  ( -12.46165725306000027, -23.67155322522999938, -1.631637378453000053 ) ) ;
#1757=CARTESIAN_POINT ( 'NONE',  ( 8.130811096541000538, -24.68523690389000080, 9.546858433121998999 ) ) ;
#1758=DIRECTION ( 'NONE',  ( 0.000000000000000000, 1.000000000000000000, 0.000000000000000000 ) ) ;
#1759=TOROIDAL_SURFACE ( 'NONE', #4568, 26.50000000000000000, 14.00000000000000000 ) ;
#1761=DIRECTION ( 'NONE',  ( -0.7071067810866970005, -6.386274622742979319E-09, -0.7071067812863980340 ) ) ;
#1767=CARTESIAN_POINT ( 'NONE',  ( 3.295079792876999925, -76.33610278377001634, 11.86077433336000020 ) ) ;
#1769=CARTESIAN_POINT ( 'NONE',  ( 3.456100946708223542, -2.083958273693990115, -0.6710332831642513707 ) ) ;
#1770=FACE_OUTER_BOUND ( 'NONE', #2963, .T. ) ;
#1771=CARTESIAN_POINT ( 'NONE',  ( -4.802691730569000228, -78.35556385665999812, 11.09149278351999968 ) ) ;
#1774=CARTESIAN_POINT ( 'NONE',  ( 2.314286229412385598, -2.788778792593855638, -2.281192321292274894 ) ) ;
#1775=CARTESIAN_POINT ( 'NONE',  ( 8.405332047648236937, -77.73628230296297659, -8.661069329411425599 ) ) ;
#1777=B_SPLINE_CURVE_WITH_KNOTS ( 'NONE', 3,
 ( #32109, #22978, #18559, #18266, #22683, #13818 ),
 .UNSPECIFIED., .F., .F.,
 ( 4, 1, 1, 4 ),
 ( 0.000000000000000000, 0.3333333333333000081, 0.6666666666667000474, 1.000000000000000000 ),
 .UNSPECIFIED. ) ;
#1778=ORIENTED_EDGE ( 'NONE', *, *, #11133, .F. ) ;
#1781=CARTESIAN_POINT ( 'NONE',  ( -1.750000000000000000, -23.24999999758999536, -12.50000000000000000 ) ) ;
#1782=DIRECTION ( 'NONE',  ( 1.000000000000000000, 0.000000000000000000, 0.000000000000000000 ) ) ;
#1783=CARTESIAN_POINT ( 'NONE',  ( 0.5334547282266999257, -3.244990180630999976, 3.675578036170999763 ) ) ;
#1787=CARTESIAN_POINT ( 'NONE',  ( -8.706989617445008989, -76.14134214265790490, 7.890437978471732450 ) ) ;
#1792=CARTESIAN_POINT ( 'NONE',  ( 12.74366183107850858, -23.52185227222615183, 1.980611001122018822 ) ) ;
#1793=FACE_OUTER_BOUND ( 'NONE', #34736, .T. ) ;
#1794=CARTESIAN_POINT ( 'NONE',  ( -1.997276839918484148, -2.427083333333333481, 2.598917237794077018 ) ) ;
#1796=CARTESIAN_POINT ( 'NONE',  ( -1.821913034590999979E-14, -80.79999999999999716, -12.24999999999996980 ) ) ;
#1798=CARTESIAN_POINT ( 'NONE',  ( 7.761025538858000061, -17.91850014422000115, -9.835174270523999951 ) ) ;
#1800=ORIENTED_EDGE ( 'NONE', *, *, #8778, .F. ) ;
#1803=TOROIDAL_SURFACE ( 'NONE', #34751, 13.50000000000000000, 0.5000000000000000000 ) ;
#1804=CARTESIAN_POINT ( 'NONE',  ( 12.50386430097127999, -54.01495444323656869, 0.8574444996622476722 ) ) ;
#1806=CARTESIAN_POINT ( 'NONE',  ( -13.99609303072000088, -45.84137733103999324, -3.303213538035000172E-05 ) ) ;
#1807=CARTESIAN_POINT ( 'NONE',  ( -9.420089102920373492, -77.39912871045925158, 7.564612592004372082 ) ) ;
#1809=EDGE_CURVE ( 'NONE', #22170, #17027, #27255, .T. ) ;
#1810=CARTESIAN_POINT ( 'NONE',  ( -12.50409217853025190, -54.27871355468437287, 1.233808106764427315 ) ) ;
#1812=CARTESIAN_POINT ( 'NONE',  ( 13.98934701867000108, -9.421869816320000979, 1.420930502849999897E-05 ) ) ;
#1814=CARTESIAN_POINT ( 'NONE',  ( -1.980532734072999901, -19.23767313188999850, 12.80090744966999949 ) ) ;
#1816=DIRECTION ( 'NONE',  ( 0.000000000000000000, 1.000000000000000000, 0.000000000000000000 ) ) ;
#1822=ORIENTED_EDGE ( 'NONE', *, *, #37892, .T. ) ;
#1824=CARTESIAN_POINT ( 'NONE',  ( 7.619389775686000732, -18.59213701582999789, 10.35398629635000134 ) ) ;
#1827=CARTESIAN_POINT ( 'NONE',  ( -4.665534009026000462, -78.15194258207000644, 10.77473627194999928 ) ) ;
#1828=CARTESIAN_POINT ( 'NONE',  ( 9.643350356198000739, -61.74034317005999384, 8.260133465614998727 ) ) ;
#1837=VECTOR ( 'NONE', #32904, 1000.000000000000114 ) ;
#1841=CARTESIAN_POINT ( 'NONE',  ( -8.838834764832000701, -18.75000000000000000, 8.838834764832000701 ) ) ;
#1842=TOROIDAL_SURFACE ( 'NONE', #25412, 13.50000000000000000, 0.5000000000000000000 ) ;
#1846=CARTESIAN_POINT ( 'NONE',  ( 10.98362417419999915, -23.15000000000000213, 0.5999999999999999778 ) ) ;
#1847=CARTESIAN_POINT ( 'NONE',  ( 12.70556836333273409, -62.02772277294081960, 0.2642470008508416290 ) ) ;
#1848=DIRECTION ( 'NONE',  ( 0.000000000000000000, -1.000000000000000000, 0.000000000000000000 ) ) ;
#1850=ORIENTED_EDGE ( 'NONE', *, *, #25889, .F. ) ;
#1855=CARTESIAN_POINT ( 'NONE',  ( -8.588893914429998944, -16.86760216306999993, 9.317954958010000510 ) ) ;
#1857=CARTESIAN_POINT ( 'NONE',  ( 3.354383128917739487, -2.975290926151756832, -1.074698072248829295 ) ) ;
#1860=DIRECTION ( 'NONE',  ( 0.000000000000000000, -1.000000000000000000, 0.000000000000000000 ) ) ;
#1866=EDGE_CURVE ( 'NONE', #50613, #31027, #57970, .T. ) ;
#1867=CARTESIAN_POINT ( 'NONE',  ( 1.890224871705999954, -60.54789247981999267, -12.68696160876999990 ) ) ;
#1872=CARTESIAN_POINT ( 'NONE',  ( 8.596763593952999827, -25.13532396123000012, -9.310159863706001460 ) ) ;
#1874=CARTESIAN_POINT ( 'NONE',  ( -9.546819346760001324, -61.48527546573999558, 8.130850182904000079 ) ) ;
#1875=CARTESIAN_POINT ( 'NONE',  ( -11.79999999999999893, -18.84999999999000053, 0.5999999999999999778 ) ) ;
#1876=EDGE_LOOP ( 'NONE', ( #7673, #4757, #30532, #1778 ) ) ;
#1878=VECTOR ( 'NONE', #57307, 1000.000000000000000 ) ;
#1880=CARTESIAN_POINT ( 'NONE',  ( 7.606021555054999439, -55.37841460039999930, -10.52692944503000128 ) ) ;
#1885=CARTESIAN_POINT ( 'NONE',  ( 10.98362417419999915, -23.15000000000000213, -0.5999999999999999778 ) ) ;
#1887=CIRCLE ( 'NONE', #6584, 13.79999999999999893 ) ;
#1889=CARTESIAN_POINT ( 'NONE',  ( -1.980584515752000119, -18.73514853375999678, -12.76303204602000108 ) ) ;
#1891=CARTESIAN_POINT ( 'NONE',  ( 0.000000000000000000, -13.07071424677999971, 0.000000000000000000 ) ) ;
#1895=B_SPLINE_CURVE_WITH_KNOTS ( 'NONE', 3,
 ( #56841, #11971, #44130, #11685, #30534, #51843 ),
 .UNSPECIFIED., .F., .F.,
 ( 4, 2, 4 ),
 ( 0.000000000000000000, 0.5000000000000000000, 1.000000000000000000 ),
 .UNSPECIFIED. ) ;
#1897=VERTEX_POINT ( 'NONE', #18415 ) ;
#1900=ORIENTED_EDGE ( 'NONE', *, *, #42868, .F. ) ;
#1901=ORIENTED_EDGE ( 'NONE', *, *, #36924, .F. ) ;
#1902=CARTESIAN_POINT ( 'NONE',  ( -0.9113424693944999211, -17.17464206440000041, 12.54674099557999867 ) ) ;
#1910=AXIS2_PLACEMENT_3D ( 'NONE', #58084, #57214, #26204 ) ;
#1913=CARTESIAN_POINT ( 'NONE',  ( -12.70722176274329485, -24.41036110618716748, 1.610175936224433002 ) ) ;
#1914=ADVANCED_FACE ( 'NONE', ( #13969 ), #18807, .F. ) ;
#1917=FACE_OUTER_BOUND ( 'NONE', #16158, .T. ) ;
#1919=CARTESIAN_POINT ( 'NONE',  ( 8.743470003752999986, -79.05248508179001021, 7.836700939358999030 ) ) ;
#1922=CARTESIAN_POINT ( 'NONE',  ( 1.330267261658839351, -76.56584803886862289, 11.68086291702384116 ) ) ;
#1925=VECTOR ( 'NONE', #56762, 1000.000000000000000 ) ;
#1926=B_SPLINE_CURVE_WITH_KNOTS ( 'NONE', 3,
 ( #18537, #14092, #32091, #50131, #9673, #9970 ),
 .UNSPECIFIED., .F., .F.,
 ( 4, 2, 4 ),
 ( 0.000000000000000000, 0.4999999999999998890, 1.000000000000000000 ),
 .UNSPECIFIED. ) ;
#1929=CARTESIAN_POINT ( 'NONE',  ( 1.799501877760999902, -18.71082434677000350, -12.60552522436000089 ) ) ;
#1930=VECTOR ( 'NONE', #10304, 1000.000000000000114 ) ;
#1933=DIRECTION ( 'NONE',  ( 0.000000000000000000, 3.441642669434999888E-11, 1.000000000000000000 ) ) ;
#1934=DIRECTION ( 'NONE',  ( 0.000000000000000000, -1.000000000000000000, 0.000000000000000000 ) ) ;
#1935=CARTESIAN_POINT ( 'NONE',  ( -1.209804193477999945, -2.451258720802000024, -3.608664049297999998 ) ) ;
#1936=CARTESIAN_POINT ( 'NONE',  ( -3.463096647710298903, -1.235411181636255629, 0.6470415087195192649 ) ) ;
#1937=ORIENTED_EDGE ( 'NONE', *, *, #30455, .T. ) ;
#1939=CARTESIAN_POINT ( 'NONE',  ( -0.6999999999999999556, -21.00000000000000000, -11.90000000000000036 ) ) ;
#1943=LINE ( 'NONE', #9911, #18716 ) ;
#1944=DIRECTION ( 'NONE',  ( -0.7071067811865475727, 0.000000000000000000, -0.7071067811865475727 ) ) ;
#1950=AXIS2_PLACEMENT_3D ( 'NONE', #10801, #37352, #28487 ) ;
#1956=CARTESIAN_POINT ( 'NONE',  ( 0.8506806241676515556, -2.854166666666666963, 3.165411199172028844 ) ) ;
#1967=ORIENTED_EDGE ( 'NONE', *, *, #20245, .T. ) ;
#1970=EDGE_LOOP ( 'NONE', ( #26913, #5398, #49202, #22425, #58036, #56197 ) ) ;
#1971=EDGE_LOOP ( 'NONE', ( #53330, #3740, #34324, #47946 ) ) ;
#1973=ADVANCED_FACE ( 'NONE', ( #17526 ), #8669, .F. ) ;
#1974=ORIENTED_EDGE ( 'NONE', *, *, #13655, .T. ) ;
#1977=ORIENTED_EDGE ( 'NONE', *, *, #13124, .T. ) ;
#1980=CARTESIAN_POINT ( 'NONE',  ( -7.613962745591999592, -55.49360215019999742, 10.53101990617999917 ) ) ;
#1981=ORIENTED_EDGE ( 'NONE', *, *, #44185, .T. ) ;
#1982=DIRECTION ( 'NONE',  ( 0.000000000000000000, 0.000000000000000000, -1.000000000000000000 ) ) ;
#1987=CARTESIAN_POINT ( 'NONE',  ( 9.708203932494999577, -79.25000000000000000, 7.053423027515000499 ) ) ;
#1993=CARTESIAN_POINT ( 'NONE',  ( -7.642160924870000649, -56.01538333533000014, -10.55911395186000057 ) ) ;
#1995=CARTESIAN_POINT ( 'NONE',  ( 4.502314056123180919, -76.54333886560480948, 10.85294518812557563 ) ) ;
#1996=AXIS2_PLACEMENT_3D ( 'NONE', #18789, #8756, #54801 ) ;
#2003=LINE ( 'NONE', #37697, #3765 ) ;
#2004=DIRECTION ( 'NONE',  ( 0.000000000000000000, -1.000000000000000000, 0.000000000000000000 ) ) ;
#2005=CARTESIAN_POINT ( 'NONE',  ( -8.485281374238999419, -59.94999999967000548, 8.485281374238999419 ) ) ;
#2008=VECTOR ( 'NONE', #20832, 1000.000000000000000 ) ;
#2010=CARTESIAN_POINT ( 'NONE',  ( 12.43571054526000097, -24.87980566418999828, 0.4385525234353999657 ) ) ;
#2013=CARTESIAN_POINT ( 'NONE',  ( 5.209066090324155240, -78.35914083083440573, -10.56088534199699858 ) ) ;
#2015=CARTESIAN_POINT ( 'NONE',  ( 5.951017151798000171, -76.58956203265999818, 10.49160152982999961 ) ) ;
#2020=CARTESIAN_POINT ( 'NONE',  ( 8.532671860860467916, -53.67201063362983859, 9.433519686857682274 ) ) ;
#2022=DIRECTION ( 'NONE',  ( 1.000000000000000000, 0.000000000000000000, 0.000000000000000000 ) ) ;
#2029=EDGE_LOOP ( 'NONE', ( #48789, #6811, #30313 ) ) ;
#2033=ORIENTED_EDGE ( 'NONE', *, *, #37633, .F. ) ;
#2039=ORIENTED_EDGE ( 'NONE', *, *, #54936, .F. ) ;
#2040=EDGE_CURVE ( 'NONE', #43546, #45130, #55631, .T. ) ;
#2046=CARTESIAN_POINT ( 'NONE',  ( -12.70451681027687130, -25.17641660207490872, -0.5206746370451510453 ) ) ;
#2050=CARTESIAN_POINT ( 'NONE',  ( -12.83677138648000060, -23.22737696056999823, -2.062839765281999860 ) ) ;
#2052=CIRCLE ( 'NONE', #46344, 5.000000000000000000 ) ;
#2053=DIRECTION ( 'NONE',  ( -0.7071067811865475727, 0.000000000000000000, 0.7071067811865475727 ) ) ;
#2054=CARTESIAN_POINT ( 'NONE',  ( 1.308715794663198873, -17.25595500802067406, -12.70256747357078453 ) ) ;
#2056=EDGE_CURVE ( 'NONE', #14405, #24318, #19041, .T. ) ;
#2060=CARTESIAN_POINT ( 'NONE',  ( -10.62397638184999948, -76.05947304082000926, -6.218250916117999516 ) ) ;
#2062=CARTESIAN_POINT ( 'NONE',  ( 10.08161778468999970, -61.51855282861000518, -7.981584069293999661 ) ) ;
#2063=CARTESIAN_POINT ( 'NONE',  ( 9.889431646000000242, -78.74835367037000822, 7.252463523969000292 ) ) ;
#2066=CARTESIAN_POINT ( 'NONE',  ( 9.756232907440029578, -78.35003554436862316, 7.102215872803408381 ) ) ;
#2073=CARTESIAN_POINT ( 'NONE',  ( 11.75000000000000178, -78.03958333333331154, -1.538071403319980268 ) ) ;
#2076=CARTESIAN_POINT ( 'NONE',  ( 1.070339692688000000, -2.147081610292000065, 3.719502945170999997 ) ) ;
#2079=CARTESIAN_POINT ( 'NONE',  ( -11.24578562917078628, -76.17646087094038876, 3.410865946175021257 ) ) ;
#2082=CYLINDRICAL_SURFACE ( 'NONE', #50228, 0.6000000000000008660 ) ;
#2084=CARTESIAN_POINT ( 'NONE',  ( -11.84062247810999935, -76.52795558657410879, 3.366775603358000080 ) ) ;
#2085=DIRECTION ( 'NONE',  ( 0.000000000000000000, -1.000000000000000000, 0.000000000000000000 ) ) ;
#2086=DIRECTION ( 'NONE',  ( -1.000000000000000000, 0.000000000000000000, 0.000000000000000000 ) ) ;
#2087=CARTESIAN_POINT ( 'NONE',  ( -9.108250977419000805, -61.67811334458999539, 8.478720681770999690 ) ) ;
#2090=CARTESIAN_POINT ( 'NONE',  ( 0.8495058540349734733, -3.246012347106654428, -3.252519878219170213 ) ) ;
#2091=FACE_OUTER_BOUND ( 'NONE', #22774, .T. ) ;
#2092=ORIENTED_EDGE ( 'NONE', *, *, #33501, .T. ) ;
#2098=CARTESIAN_POINT ( 'NONE',  ( 8.408834629392076820, -77.63929640612045091, -8.664705538047067890 ) ) ;
#2102=FACE_OUTER_BOUND ( 'NONE', #15724, .T. ) ;
#2112=ORIENTED_EDGE ( 'NONE', *, *, #54091, .F. ) ;
#2113=CARTESIAN_POINT ( 'NONE',  ( 9.996785040898998886, -17.84937852891999910, 7.758588586541999454 ) ) ;
#2115=CARTESIAN_POINT ( 'NONE',  ( 8.961184493456999078, -79.22664678124000659, 8.031836662962000162 ) ) ;
#2116=DIRECTION ( 'NONE',  ( -1.000000000000000000, 0.000000000000000000, 0.000000000000000000 ) ) ;
#2117=DIRECTION ( 'NONE',  ( -0.7071067811865474617, 0.000000000000000000, 0.7071067811865474617 ) ) ;
#2118=EDGE_CURVE ( 'NONE', #2960, #53336, #53536, .T. ) ;
#2119=CARTESIAN_POINT ( 'NONE',  ( 10.18499221075000172, -21.74977139925000102, 7.710118476595999581 ) ) ;
#2121=ORIENTED_EDGE ( 'NONE', *, *, #46302, .T. ) ;
#2122=CARTESIAN_POINT ( 'NONE',  ( -1.929239059888873564, -78.18805851086665371, 11.63526571105258434 ) ) ;
#2123=ORIENTED_EDGE ( 'NONE', *, *, #50879, .T. ) ;
#2131=CARTESIAN_POINT ( 'NONE',  ( -7.691916945395000482, -21.75365779208000205, 10.42274798264000069 ) ) ;
#2134=AXIS2_PLACEMENT_3D ( 'NONE', #3276, #56998, #16849 ) ;
#2135=EDGE_CURVE ( 'NONE', #40540, #25833, #3746, .T. ) ;
#2137=VERTEX_POINT ( 'NONE', #21308 ) ;
#2140=LINE ( 'NONE', #2715, #54946 ) ;
#2142=CARTESIAN_POINT ( 'NONE',  ( -9.636775127282000142, -17.55967715742000124, 7.948072248883998547 ) ) ;
#2143=CIRCLE ( 'NONE', #6843, 13.86363636363999952 ) ;
#2145=CARTESIAN_POINT ( 'NONE',  ( 2.360403478625465734, -2.432488435963918949, -2.699818710255091680 ) ) ;
#2148=CARTESIAN_POINT ( 'NONE',  ( 2.062312494845999655, -55.57284340075000273, -12.83634740207000036 ) ) ;
#2150=DIRECTION ( 'NONE',  ( -0.7071067811865475727, 0.000000000000000000, -0.7071067811865475727 ) ) ;
#2152=ORIENTED_EDGE ( 'NONE', *, *, #25335, .T. ) ;
#2155=CARTESIAN_POINT ( 'NONE',  ( 0.005523896503684000252, -61.86963456192999899, -12.55021156886000000 ) ) ;
#2159=CARTESIAN_POINT ( 'NONE',  ( 10.48771805367000098, -58.55560171494000343, -7.686918321054999836 ) ) ;
#2163=CARTESIAN_POINT ( 'NONE',  ( 6.004401788877678392, -78.53175237169041623, 10.09960146651490298 ) ) ;
#2165=VERTEX_POINT ( 'NONE', #16600 ) ;
#2167=CARTESIAN_POINT ( 'NONE',  ( 8.130811096204000776, -61.48523690322999613, 9.546858433459998849 ) ) ;
#2168=CARTESIAN_POINT ( 'NONE',  ( 7.646091287746999754, -55.09149945095000334, -10.13691902390999999 ) ) ;
#2170=CARTESIAN_POINT ( 'NONE',  ( -11.57893382125400450, -79.13802082858391884, -3.110875827410843009 ) ) ;
#2173=VECTOR ( 'NONE', #15689, 1000.000000000000000 ) ;
#2176=DIRECTION ( 'NONE',  ( 0.9999999924279685537, 0.000000000000000000, 0.0001230612157848962919 ) ) ;
#2182=ORIENTED_EDGE ( 'NONE', *, *, #27467, .F. ) ;
#2183=VERTEX_POINT ( 'NONE', #34586 ) ;
#2184=CARTESIAN_POINT ( 'NONE',  ( -12.49989298246999958, -55.60773379962999741, -1.666426105558999948 ) ) ;
#2185=VERTEX_POINT ( 'NONE', #2167 ) ;
#2187=ORIENTED_EDGE ( 'NONE', *, *, #1402, .T. ) ;
#2188=CARTESIAN_POINT ( 'NONE',  ( 1.801614160558000055, -18.61347738095000182, 12.59687422887999908 ) ) ;
#2189=AXIS2_PLACEMENT_3D ( 'NONE', #21585, #8882, #43453 ) ;
#2190=DIRECTION ( 'NONE',  ( 0.7071067811865974218, -0.7071067811864975017, -1.156399806128994869E-08 ) ) ;
#2192=CARTESIAN_POINT ( 'NONE',  ( -7.850076762416701825, -61.11471440996241711, 9.837736659316185239 ) ) ;
#2194=EDGE_CURVE ( 'NONE', #37084, #11745, #25450, .T. ) ;
#2196=ORIENTED_EDGE ( 'NONE', *, *, #30060, .T. ) ;
#2197=EDGE_CURVE ( 'NONE', #36484, #7601, #29291, .T. ) ;
#2200=CARTESIAN_POINT ( 'NONE',  ( -12.76303204294999993, -23.26485150694999859, 1.980584515756000030 ) ) ;
#2201=CARTESIAN_POINT ( 'NONE',  ( -12.72558241039000038, -60.00131830475000072, -1.930284820929999867 ) ) ;
#2203=CARTESIAN_POINT ( 'NONE',  ( 7.792426477869834223, -61.09102098674993186, 10.18245125510161131 ) ) ;
#2205=CARTESIAN_POINT ( 'NONE',  ( 7.688584395383999848, -79.06206532115000130, 8.762320683322998960 ) ) ;
#2207=PLANE ( 'NONE',  #6327 ) ;
#2209=CARTESIAN_POINT ( 'NONE',  ( 0.9387899161113768542, -79.20703122369496896, -11.95703176532392398 ) ) ;
#2219=CARTESIAN_POINT ( 'NONE',  ( -3.593558748265999636, -1.849109825020999853, 0.1459214154804999997 ) ) ;
#2220=DIRECTION ( 'NONE',  ( 0.000000000000000000, -1.000000000000000000, 0.000000000000000000 ) ) ;
#2222=VECTOR ( 'NONE', #57565, 1000.000000000000000 ) ;
#2223=FACE_OUTER_BOUND ( 'NONE', #45378, .T. ) ;
#2225=B_SPLINE_CURVE_WITH_KNOTS ( 'NONE', 3,
 ( #47429, #38538, #51559, #11117, #15820, #33807, #20822, #51846, #11402, #29381, #6958, #24963, #42982, #20543, #4569, #21971, #57419, #45015 ),
 .UNSPECIFIED., .F., .F.,
 ( 4, 2, 2, 2, 2, 2, 2, 2, 4 ),
 ( 0.000000000000000000, 0.1249999999999999722, 0.2499999999999999445, 0.3749999999999998890, 0.4999999999999998890, 0.6249999999999998890, 0.7499999999999997780, 0.8749999999999998890, 1.000000000000000000 ),
 .UNSPECIFIED. ) ;
#2227=CARTESIAN_POINT ( 'NONE',  ( 11.79660191402999914, -76.73268768631000114, 5.494707494196000575 ) ) ;
#2228=CARTESIAN_POINT ( 'NONE',  ( 0.000000000000000000, 0.000000000000000000, 0.000000000000000000 ) ) ;
#2231=AXIS2_PLACEMENT_3D ( 'NONE', #19491, #14471, #24792 ) ;
#2232=DIRECTION ( 'NONE',  ( 0.000000000000000000, 1.000000000000000000, 0.000000000000000000 ) ) ;
#2240=CARTESIAN_POINT ( 'NONE',  ( 1.997276839918466829, -2.822916666666666075, 2.598917237794090784 ) ) ;
#2248=CYLINDRICAL_SURFACE ( 'NONE', #10550, 0.5999999999999999778 ) ;
#2249=VERTEX_POINT ( 'NONE', #43471 ) ;
#2251=VERTEX_POINT ( 'NONE', #3027 ) ;
#2252=VERTEX_POINT ( 'NONE', #24877 ) ;
#2254=ORIENTED_EDGE ( 'NONE', *, *, #19076, .T. ) ;
#2255=CONICAL_SURFACE ( 'NONE', #42789, 0.6999999997695000031, 0.7853981633972997312 ) ;
#2260=ORIENTED_EDGE ( 'NONE', *, *, #33418, .F. ) ;
#2261=CARTESIAN_POINT ( 'NONE',  ( -7.653559502261000347, -55.50150862742999891, 10.01234990226999955 ) ) ;
#2268=AXIS2_PLACEMENT_3D ( 'NONE', #57745, #35003, #12584 ) ;
#2270=CARTESIAN_POINT ( 'NONE',  ( -5.531931755322890609, -79.03797283330507639, -10.94557777195214676 ) ) ;
#2276=EDGE_CURVE ( 'NONE', #22563, #51850, #43604, .T. ) ;
#2281=CARTESIAN_POINT ( 'NONE',  ( -12.50000000000000000, -49.87071424677999687, 0.000000000000000000 ) ) ;
#2286=DIRECTION ( 'NONE',  ( 0.000000000000000000, 0.000000000000000000, -1.000000000000000000 ) ) ;
#2287=DIRECTION ( 'NONE',  ( 1.000000000000000000, 0.000000000000000000, 0.000000000000000000 ) ) ;
#2289=CARTESIAN_POINT ( 'NONE',  ( -0.04193593611713257452, -25.01009741336690695, 12.50649570005664835 ) ) ;
#2290=CARTESIAN_POINT ( 'NONE',  ( 8.909545442949999838, -57.79999999967000690, -7.919595949288999570 ) ) ;
#2291=AXIS2_PLACEMENT_3D ( 'NONE', #47733, #33824, #24695 ) ;
#2296=CARTESIAN_POINT ( 'NONE',  ( -5.915252869412679360, -78.28189657008987012, -10.26004535388594796 ) ) ;
#2298=CARTESIAN_POINT ( 'NONE',  ( -6.510718906818000029, -75.83346457246000227, -9.669701809193998798 ) ) ;
#2299=EDGE_LOOP ( 'NONE', ( #39171, #41298, #39758, #31302, #44069 ) ) ;
#2303=DIRECTION ( 'NONE',  ( -1.000000000000000000, 0.000000000000000000, 0.000000000000000000 ) ) ;
#2305=CARTESIAN_POINT ( 'NONE',  ( 12.72558083408000051, -55.59866855809999464, -1.930284430576000076 ) ) ;
#2308=CARTESIAN_POINT ( 'NONE',  ( 12.56594317989000054, -23.24999999414999863, 1.750000000001000089 ) ) ;
#2309=CIRCLE ( 'NONE', #46646, 12.50000000000000000 ) ;
#2311=ORIENTED_EDGE ( 'NONE', *, *, #32214, .T. ) ;
#2313=DIRECTION ( 'NONE',  ( 0.000000000000000000, 0.000000000000000000, 1.000000000000000000 ) ) ;
#2316=EDGE_CURVE ( 'NONE', #21151, #28651, #53186, .T. ) ;
#2318=CARTESIAN_POINT ( 'NONE',  ( 12.64500484464999808, -59.57152778012000027, 1.799490225533999732 ) ) ;
#2329=ORIENTED_EDGE ( 'NONE', *, *, #876, .T. ) ;
#2330=CARTESIAN_POINT ( 'NONE',  ( 12.66319948253000049, -53.61851729328000005, 0.1456213732515000137 ) ) ;
#2334=CARTESIAN_POINT ( 'NONE',  ( 8.385799987677961198, -24.88809827229000504, 9.298537617329934335 ) ) ;
#2335=CYLINDRICAL_SURFACE ( 'NONE', #12144, 1.750000000000001332 ) ;
#2336=CARTESIAN_POINT ( 'NONE',  ( 8.610991514544377168, -16.82512235768486875, -9.355860133801421341 ) ) ;
#2340=CARTESIAN_POINT ( 'NONE',  ( -12.70255494774433558, -17.25391159035561728, -1.306413223700355397 ) ) ;
#2344=CARTESIAN_POINT ( 'NONE',  ( 9.569482281372000188, -76.64386216769000271, -7.743360016082000641 ) ) ;
#2347=CARTESIAN_POINT ( 'NONE',  ( 8.878335097443999402, -61.86963071710999884, -8.870344075662000449 ) ) ;
#2348=CARTESIAN_POINT ( 'NONE',  ( 7.914613980750001332, -79.26568659574000719, 9.019916049260999102 ) ) ;
#2350=CARTESIAN_POINT ( 'NONE',  ( -10.12290050126000196, -60.04999999958999979, -7.648026767103999646 ) ) ;
#2351=CARTESIAN_POINT ( 'NONE',  ( 6.038193122641423827, -78.21661092667235948, -10.45819121534531959 ) ) ;
#2353=ORIENTED_EDGE ( 'NONE', *, *, #23929, .T. ) ;
#2355=FACE_OUTER_BOUND ( 'NONE', #50391, .T. ) ;
#2356=CARTESIAN_POINT ( 'NONE',  ( 1.798336774608999988, -23.19644498052000259, 12.61277771566000006 ) ) ;
#2357=CARTESIAN_POINT ( 'NONE',  ( 1.704789469149671666, -23.70346161525050732, 12.53199752960681046 ) ) ;
#2358=CARTESIAN_POINT ( 'NONE',  ( -3.234369484799000549, -2.340565377978999884, 1.825734147243999850 ) ) ;
#2362=CARTESIAN_POINT ( 'NONE',  ( -7.782531694773533459, -76.13256886044052862, 8.804557435548110433 ) ) ;
#2367=CARTESIAN_POINT ( 'NONE',  ( 10.35453599130000057, -76.75783510652000530, -6.064947188958000446 ) ) ;
#2370=CARTESIAN_POINT ( 'NONE',  ( 2.598917237794081014, -2.302083333333333481, 1.997276839918480373 ) ) ;
#2371=CARTESIAN_POINT ( 'NONE',  ( -7.633501923173000137, -60.00104675737999571, 10.36289748054999826 ) ) ;
#2372=VECTOR ( 'NONE', #47862, 1000.000000000000114 ) ;
#2377=VERTEX_POINT ( 'NONE', #4176 ) ;
#2379=CARTESIAN_POINT ( 'NONE',  ( 12.99999999999509726, -6.000000000000000000, 2.526608922437675593E-09 ) ) ;
#2380=DIRECTION ( 'NONE',  ( 0.9999999999999992228, 4.158397913305990963E-08, 7.906211578309984016E-12 ) ) ;
#2382=ADVANCED_FACE ( 'NONE', ( #17167 ), #55596, .F. ) ;
#2386=LINE ( 'NONE', #21813, #29769 ) ;
#2388=CARTESIAN_POINT ( 'NONE',  ( -1.980584515756000030, -18.73514849905999924, 12.76303204340999997 ) ) ;
#2390=CARTESIAN_POINT ( 'NONE',  ( -7.919595949288999570, -59.94999999967000548, -9.050966799188000067 ) ) ;
#2391=ORIENTED_EDGE ( 'NONE', *, *, #24170, .T. ) ;
#2396=CARTESIAN_POINT ( 'NONE',  ( 9.966229686710001090, -18.33098097385000003, 7.657726530248999630 ) ) ;
#2397=CARTESIAN_POINT ( 'NONE',  ( -0.5135400117351243132, -53.62131466101166666, 12.70453250094476516 ) ) ;
#2398=CARTESIAN_POINT ( 'NONE',  ( -9.073214995490001655, -78.31691570303000560, -8.802385182600000135 ) ) ;
#2400=CARTESIAN_POINT ( 'NONE',  ( 9.369164850722000892, -60.04999999966999980, 7.601397897754999633 ) ) ;
#2403=AXIS2_PLACEMENT_3D ( 'NONE', #38804, #8601, #34361 ) ;
#2405=LINE ( 'NONE', #47002, #2998 ) ;
#2408=CARTESIAN_POINT ( 'NONE',  ( 0.7999999997951000585, -23.14999999072999870, 11.99999999979999821 ) ) ;
#2413=CARTESIAN_POINT ( 'NONE',  ( 0.000000000000000000, -51.86282895648000135, 0.000000000000000000 ) ) ;
#2414=DIRECTION ( 'NONE',  ( 0.000000000000000000, -1.000000000000000000, 0.000000000000000000 ) ) ;
#2416=CARTESIAN_POINT ( 'NONE',  ( -7.627487606609999915, -23.29778595484999926, 10.35845616727999996 ) ) ;
#2418=DIRECTION ( 'NONE',  ( 0.000000000000000000, -1.000000000000000000, 0.000000000000000000 ) ) ;
#2419=SURFACE_STYLE_USAGE ( .BOTH. , #47885 ) ;
#2421=ORIENTED_EDGE ( 'NONE', *, *, #5439, .F. ) ;
#2426=CARTESIAN_POINT ( 'NONE',  ( -7.606021555073000151, -18.57841460072999951, 10.52692944505000128 ) ) ;
#2428=CARTESIAN_POINT ( 'NONE',  ( 0.006631491796348466111, -2.124900358190759064, 3.523059322413071737 ) ) ;
#2437=ORIENTED_EDGE ( 'NONE', *, *, #52656, .F. ) ;
#2440=CARTESIAN_POINT ( 'NONE',  ( 1.930009203933999995, -60.00099032284000344, -12.72537718780000127 ) ) ;
#2441=CARTESIAN_POINT ( 'NONE',  ( -8.137215171344880815, -55.34844303569388302, 7.401770473313843191 ) ) ;
#2444=DIRECTION ( 'NONE',  ( 1.000000000000000000, 0.000000000000000000, 0.000000000000000000 ) ) ;
#2447=CARTESIAN_POINT ( 'NONE',  ( 10.52222799053675040, -78.48640825465236048, 5.259909153984513530 ) ) ;
#2449=ORIENTED_EDGE ( 'NONE', *, *, #8622, .F. ) ;
#2455=FACE_OUTER_BOUND ( 'NONE', #28665, .T. ) ;
#2456=CARTESIAN_POINT ( 'NONE',  ( -5.917523019358107206, -77.71666666666666856, 10.26699006316250795 ) ) ;
#2460=CIRCLE ( 'NONE', #38381, 1.750000000000001332 ) ;
#2461=CARTESIAN_POINT ( 'NONE',  ( -10.42531124903999995, -55.53514851492000304, 7.624341765436000173 ) ) ;
#2462=EDGE_CURVE ( 'NONE', #36137, #45005, #30194, .T. ) ;
#2463=ORIENTED_EDGE ( 'NONE', *, *, #10305, .T. ) ;
#2464=CARTESIAN_POINT ( 'NONE',  ( 8.061017305527000687, -55.64999999967000122, 8.909545442950999927 ) ) ;
#2465=EDGE_CURVE ( 'NONE', #25083, #50457, #31895, .T. ) ;
#2466=DIRECTION ( 'NONE',  ( 0.7071067811865475727, 0.000000000000000000, -0.7071067811865475727 ) ) ;
#2468=ORIENTED_EDGE ( 'NONE', *, *, #26760, .T. ) ;
#2469=CARTESIAN_POINT ( 'NONE',  ( -12.83836748059999877, -55.59372227128000077, -2.062147040909000140 ) ) ;
#2470=EDGE_LOOP ( 'NONE', ( #31332, #13621, #31069, #19559 ) ) ;
#2471=VERTEX_POINT ( 'NONE', #23922 ) ;
#2477=ORIENTED_EDGE ( 'NONE', *, *, #1582, .F. ) ;
#2482=CARTESIAN_POINT ( 'NONE',  ( -12.57434559700999976, -60.51110719467000365, -1.760800161976000089 ) ) ;
#2490=CARTESIAN_POINT ( 'NONE',  ( -10.07615509324000058, -54.07367739666999285, 7.986954869161998261 ) ) ;
#2493=CARTESIAN_POINT ( 'NONE',  ( 2.062670899148999926, -18.69360374348000065, -12.83044039274999903 ) ) ;
#2495=CARTESIAN_POINT ( 'NONE',  ( -7.954951288349001004, -60.04999999966999980, -9.722718241315000398 ) ) ;
#2500=CARTESIAN_POINT ( 'NONE',  ( 3.702420020526000055, -2.620613097741000264, 0.8821385418971999792 ) ) ;
#2502=CARTESIAN_POINT ( 'NONE',  ( -1.720719981710890023, -0.8344193358160810758, -3.082755224493606949 ) ) ;
#2503=AXIS2_PLACEMENT_3D ( 'NONE', #8887, #27462, #35737 ) ;
#2505=CARTESIAN_POINT ( 'NONE',  ( -3.250000000000000000, -3.500000000000000000, -1.188926645705999921E-13 ) ) ;
#2507=CARTESIAN_POINT ( 'NONE',  ( -2.065550207748000133, -55.37434920636000157, 12.82162303852000029 ) ) ;
#2511=DIRECTION ( 'NONE',  ( 0.000000000000000000, 0.000000000000000000, -1.000000000000000000 ) ) ;
#2512=CARTESIAN_POINT ( 'NONE',  ( 1.930628539543000066, -60.02124444054000207, 12.72375828107000117 ) ) ;
#2519=CARTESIAN_POINT ( 'NONE',  ( -0.1560029832145526929, -76.32376738114049886, -11.74899260739961804 ) ) ;
#2522=LINE ( 'NONE', #6942, #57537 ) ;
#2525=CARTESIAN_POINT ( 'NONE',  ( 3.250000000000000000, -2.750000000000000000, 0.000000000000000000 ) ) ;
#2527=DIRECTION ( 'NONE',  ( 1.000000000000000000, 0.000000000000000000, 0.000000000000000000 ) ) ;
#2531=ADVANCED_FACE ( 'NONE', ( #7655 ), #43683, .T. ) ;
#2532=CARTESIAN_POINT ( 'NONE',  ( 5.940599228801999379E-14, -5.950000000028880187, 0.000000000000000000 ) ) ;
#2534=CARTESIAN_POINT ( 'NONE',  ( 1.779623408257821504, -24.13630869023482717, 12.71471627657148318 ) ) ;
#2538=CARTESIAN_POINT ( 'NONE',  ( -3.165411199172029288, -1.479166666666666075, 0.8506806241676482250 ) ) ;
#2539=ORIENTED_EDGE ( 'NONE', *, *, #55559, .F. ) ;
#2545=ORIENTED_EDGE ( 'NONE', *, *, #17350, .T. ) ;
#2546=CARTESIAN_POINT ( 'NONE',  ( -3.380225385341000255, -3.046741667230000061, 0.3787538185775999877 ) ) ;
#2552=EDGE_CURVE ( 'NONE', #2471, #47498, #21656, .T. ) ;
#2562=DIRECTION ( 'NONE',  ( -0.7071067811865475727, 0.000000000000000000, 0.7071067811865475727 ) ) ;
#2566=EDGE_CURVE ( 'NONE', #11618, #52988, #6796, .T. ) ;
#2570=CARTESIAN_POINT ( 'NONE',  ( -10.86515771069091407, -76.23152734406622244, -4.589020684590622068 ) ) ;
#2571=CARTESIAN_POINT ( 'NONE',  ( 10.53101998747000145, -23.30639625649999758, 7.613962827179999948 ) ) ;
#2572=CARTESIAN_POINT ( 'NONE',  ( -9.414507962650999318, -62.06263135892999827, -8.652357372810001834 ) ) ;
#2573=DIRECTION ( 'NONE',  ( -0.7071067811865475727, 0.000000000000000000, 0.7071067811865475727 ) ) ;
#2577=CARTESIAN_POINT ( 'NONE',  ( -9.692839446179998930, -78.50182691516999967, 7.074522137259999788 ) ) ;
#2581=CARTESIAN_POINT ( 'NONE',  ( 0.2678032735093955896, -25.21432775290392314, -12.70526550768988372 ) ) ;
#2582=CARTESIAN_POINT ( 'NONE',  ( -5.751871349228999897, -76.75451366967000411, -10.77263286324999925 ) ) ;
#2583=ORIENTED_EDGE ( 'NONE', *, *, #23290, .T. ) ;
#2585=ADVANCED_FACE ( 'NONE', ( #20377 ), #10662, .F. ) ;
#2588=AXIS2_PLACEMENT_3D ( 'NONE', #52566, #57277, #38977 ) ;
#2589=EDGE_CURVE ( 'NONE', #44855, #52059, #25295, .T. ) ;
#2591=CARTESIAN_POINT ( 'NONE',  ( 6.047694738970999850, -79.33324558444999752, -11.09599207243999963 ) ) ;
#2592=CARTESIAN_POINT ( 'NONE',  ( 12.83677071375000089, -55.57261389723999656, -2.062839858856999609 ) ) ;
#2594=VECTOR ( 'NONE', #28469, 1000.000000000000000 ) ;
#2602=ORIENTED_EDGE ( 'NONE', *, *, #53719, .T. ) ;
#2605=EDGE_CURVE ( 'NONE', #6077, #44782, #26365, .T. ) ;
#2606=DIRECTION ( 'NONE',  ( 0.7071067811865474617, 0.000000000000000000, -0.7071067811865474617 ) ) ;
#2615=VERTEX_POINT ( 'NONE', #33204 ) ;
#2620=AXIS2_PLACEMENT_3D ( 'NONE', #24627, #10470, #24038 ) ;
#2621=CARTESIAN_POINT ( 'NONE',  ( 7.758899961864000439, -54.49918178063000340, 10.31442855571999928 ) ) ;
#2626=CIRCLE ( 'NONE', #15812, 0.8000000000000011546 ) ;
#2631=EDGE_CURVE ( 'NONE', #49572, #20471, #39419, .T. ) ;
#2632=CARTESIAN_POINT ( 'NONE',  ( -1.343382297838000047E-14, -80.79999999999999716, 0.000000000000000000 ) ) ;
#2633=CARTESIAN_POINT ( 'NONE',  ( 10.36222489920000100, -60.02120223818999989, -7.631889817968999346 ) ) ;
#2634=VECTOR ( 'NONE', #50400, 1000.000000000000114 ) ;
#2636=CARTESIAN_POINT ( 'NONE',  ( -12.26143800982999998, -78.98420536356999833, -0.2371146996492999870 ) ) ;
#2638=CARTESIAN_POINT ( 'NONE',  ( 13.94827576517086065, -33.10361340872000113, 0.001644113314434763381 ) ) ;
#2643=CARTESIAN_POINT ( 'NONE',  ( 12.49830695671999869, -60.00970582242000262, -1.666977511085999897 ) ) ;
#2644=CARTESIAN_POINT ( 'NONE',  ( 2.065550207748000133, -23.42565079331000177, 12.82162303854000029 ) ) ;
#2645=CARTESIAN_POINT ( 'NONE',  ( 12.70556836347999941, -16.77227722772000007, -1.774194455291999869E-09 ) ) ;
#2646=CARTESIAN_POINT ( 'NONE',  ( 2.191379079411999609, -3.651279784235999859, -2.470611052852000000 ) ) ;
#2647=B_SPLINE_SURFACE_WITH_KNOTS ( 'NONE', 3, 3, ( 
 ( #16906, #53793, #40201, #49069, #95, #36064, #8617, #54084, #8038, #30172, #7754, #3331, #21326, #52918, #26325, #44339, #3892, #21895, #53491, #26602, #14155, #13869, #15031, #5016, #33027, #28602, #41907, #54895, #49905, #23316, #27438, #46649, #36304, #51073, #1192 ),
 ( #50779, #9452, #5305, #18606, #10621, #6176, #5586, #24186, #50485, #41611, #10036, #28018, #27727, #32153, #10325, #46064, #23599, #41032, #45474, #28305, #45771, #623, #46356, #23020, #42204, #9739, #18312, #41323, #55484, #908, #36595, #19182, #54328, #18890, #54617 ),
 ( #50192, #31863, #36883, #14445, #37463, #32440, #37177, #55190, #14731, #32731, #5880, #23888, #1480, #19470, #10916, #16493, #25626, #7625, #34472, #29469, #11777, #15912, #2636, #38631, #47525, #7054, #28896, #2914, #52220, #47806, #20064, #7338, #33323, #25053, #47233 ),
 ( #51659, #1771, #6761, #38915, #24771, #42494, #20630, #48094, #11207, #46943, #43076, #12061, #25338, #29185, #56075, #2063, #52503, #30041, #38052, #56933, #19765, #37761, #43354, #20912, #15620, #56649, #55783, #42784, #15333, #51360, #6468, #16206, #33615, #24479, #2348 ) ),
 .UNSPECIFIED., .F., .F., .F.,
 ( 4, 4 ),
 ( 4, 1, 1, 1, 1, 1, 1, 1, 1, 1, 1, 1, 1, 1, 1, 1, 1, 1, 1, 1, 1, 1, 1, 1, 1, 1, 1, 1, 1, 1, 1, 1, 4 ),
 ( -0.02000000000005000209, 1.020000000000000018 ),
 ( -0.01035614953205000154, 0.006472593457530000441, 0.02330133644711000068, 0.04013007943667999677, 0.05695882242625999875, 0.07378756541584000073, 0.09061630840541000376, 0.1074450513949999908, 0.1242737943845999976, 0.1411025373741000011, 0.1579312803636999940, 0.1747600233533000147, 0.1915887663428999799, 0.2084175093325000006, 0.2252462523220000179, 0.2420749953115999831, 0.2589037383012000038, 0.2757324812907999689, 0.2925612242803000140, 0.3093899672698999792, 0.3262187102594999999, 0.3430474532491000206, 0.3598761962385999547, 0.3767049392282000309, 0.3935336822177999960, 0.4103624252073999612, 0.4271911681970000374, 0.4440199111864999715, 0.4608486541761000477, 0.4776773971657000128, 0.4945061401552999780, 0.5113348831447999121, 0.5281636261344000438 ),
 .UNSPECIFIED. ) ;
#2650=CARTESIAN_POINT ( 'NONE',  ( -9.690163305986116526, -76.15162990441653790, 6.645162696918485601 ) ) ;
#2654=ORIENTED_EDGE ( 'NONE', *, *, #15989, .T. ) ;
#2655=CARTESIAN_POINT ( 'NONE',  ( 0.000000000000000000, -9.295797029142999435, 0.000000000000000000 ) ) ;
#2658=ADVANCED_FACE ( 'NONE', ( #5771 ), #36744, .F. ) ;
#2659=DIRECTION ( 'NONE',  ( 0.000000000000000000, 0.000000000000000000, -1.000000000000000000 ) ) ;
#2660=DIRECTION ( 'NONE',  ( 0.000000000000000000, 0.000000000000000000, -1.000000000000000000 ) ) ;
#2661=FACE_OUTER_BOUND ( 'NONE', #36438, .T. ) ;
#2664=CARTESIAN_POINT ( 'NONE',  ( -10.42531125072000009, -55.53514854654000032, -7.624341767124000135 ) ) ;
#2665=ORIENTED_EDGE ( 'NONE', *, *, #47411, .F. ) ;
#2666=DIRECTION ( 'NONE',  ( -1.000000000000000000, 0.000000000000000000, 0.000000000000000000 ) ) ;
#2671=EDGE_CURVE ( 'NONE', #5427, #13118, #49955, .T. ) ;
#2672=ORIENTED_EDGE ( 'NONE', *, *, #23098, .F. ) ;
#2675=CARTESIAN_POINT ( 'NONE',  ( 1.667936697358999965, -56.03537109808000594, -12.53241208775000004 ) ) ;
#2676=EDGE_CURVE ( 'NONE', #13401, #36778, #51252, .T. ) ;
#2680=ORIENTED_EDGE ( 'NONE', *, *, #10718, .F. ) ;
#2681=ORIENTED_EDGE ( 'NONE', *, *, #1428, .F. ) ;
#2684=B_SPLINE_CURVE_WITH_KNOTS ( 'NONE', 3,
 ( #37567, #33128, #50876, #37271, #28407, #41712 ),
 .UNSPECIFIED., .F., .F.,
 ( 4, 1, 1, 4 ),
 ( 0.000000000000000000, 0.3333333333333000081, 0.6666666666667000474, 1.000000000000000000 ),
 .UNSPECIFIED. ) ;
#2685=ORIENTED_EDGE ( 'NONE', *, *, #47049, .F. ) ;
#2686=CARTESIAN_POINT ( 'NONE',  ( 7.618394506893999996, -18.77286435802000142, 10.53494428259999971 ) ) ;
#2687=B_SPLINE_CURVE_WITH_KNOTS ( 'NONE', 3,
 ( #52094, #29913, #38787, #11652, #16651, #43815 ),
 .UNSPECIFIED., .F., .F.,
 ( 4, 1, 1, 4 ),
 ( 0.000000000000000000, 0.3333333333333000081, 0.6666666666667000474, 1.000000000000000000 ),
 .UNSPECIFIED. ) ;
#2689=EDGE_CURVE ( 'NONE', #13177, #23377, #36586, .T. ) ;
#2690=CARTESIAN_POINT ( 'NONE',  ( 1.782734487931668887, -54.67754631410036836, 12.71547286922865183 ) ) ;
#2691=CARTESIAN_POINT ( 'NONE',  ( 11.69353635062999963, -78.45185341714999083, 5.202647212677000255 ) ) ;
#2692=DIRECTION ( 'NONE',  ( 0.000000000000000000, -1.000000000000000000, 0.000000000000000000 ) ) ;
#2694=DIRECTION ( 'NONE',  ( 0.000000000000000000, -1.000000000000000000, 3.571217395878000445E-14 ) ) ;
#2696=CARTESIAN_POINT ( 'NONE',  ( 11.75000000000000000, -75.95000000000000284, 0.000000000000000000 ) ) ;
#2698=CARTESIAN_POINT ( 'NONE',  ( 6.818082927312866026, -78.12593218097666181, 9.623674802968025688 ) ) ;
#2699=ORIENTED_EDGE ( 'NONE', *, *, #1617, .T. ) ;
#2710=CARTESIAN_POINT ( 'NONE',  ( -12.80090744921000123, -59.56232687415000271, 1.980532734072999901 ) ) ;
#2711=CARTESIAN_POINT ( 'NONE',  ( -3.288309003486036275, -1.962318126216331837, -0.5433950876430284627 ) ) ;
#2712=ORIENTED_EDGE ( 'NONE', *, *, #5626, .F. ) ;
#2715=CARTESIAN_POINT ( 'NONE',  ( 7.601397897754999633, -18.75000000310999937, -10.07627163191000008 ) ) ;
#2720=CARTESIAN_POINT ( 'NONE',  ( 3.520922223394743256, -1.998246443813628703, -0.07578465938312391181 ) ) ;
#2729=CARTESIAN_POINT ( 'NONE',  ( 10.98521938008762078, -18.65929923595093243, -0.5702549022801662870 ) ) ;
#2736=CARTESIAN_POINT ( 'NONE',  ( 11.75000000000000000, -78.45000000000000284, 0.000000000000000000 ) ) ;
#2737=CARTESIAN_POINT ( 'NONE',  ( -8.838834764832000701, -23.25000000000000000, 8.838834764832000701 ) ) ;
#2738=VERTEX_POINT ( 'NONE', #28784 ) ;
#2742=CARTESIAN_POINT ( 'NONE',  ( -9.522678871818975210, -79.15755207139983440, -7.317142126971875271 ) ) ;
#2743=CARTESIAN_POINT ( 'NONE',  ( -1.164828128805999992E-14, -72.75000000040999737, 0.000000000000000000 ) ) ;
#2744=CARTESIAN_POINT ( 'NONE',  ( -10.12290050122000018, -55.54999999974999980, 7.648026767069000087 ) ) ;
#2747=ORIENTED_EDGE ( 'NONE', *, *, #47978, .T. ) ;
#2748=CARTESIAN_POINT ( 'NONE',  ( 2.062597299672999540, -19.21514526754999963, 12.87022657274000004 ) ) ;
#2749=CARTESIAN_POINT ( 'NONE',  ( -12.49830695668999958, -23.20970582274999927, 1.666977511086999986 ) ) ;
#2752=CARTESIAN_POINT ( 'NONE',  ( -12.66319948253000049, -53.61851729328000005, -0.1456213732515000137 ) ) ;
#2753=AXIS2_PLACEMENT_3D ( 'NONE', #26508, #35071, #17088 ) ;
#2758=VECTOR ( 'NONE', #47296, 1000.000000000000227 ) ;
#2760=EDGE_CURVE ( 'NONE', #2165, #27203, #12636, .T. ) ;
#2763=EDGE_CURVE ( 'NONE', #13397, #16171, #42966, .T. ) ;
#2766=ORIENTED_EDGE ( 'NONE', *, *, #22856, .F. ) ;
#2767=ORIENTED_EDGE ( 'NONE', *, *, #15574, .F. ) ;
#2769=CARTESIAN_POINT ( 'NONE',  ( -12.70305380112262661, -25.03154493769341116, 0.8725910145369886184 ) ) ;
#2770=CARTESIAN_POINT ( 'NONE',  ( 0.000000000000000000, -33.10361340872000113, 0.000000000000000000 ) ) ;
#2772=CARTESIAN_POINT ( 'NONE',  ( 7.635227771910129135, -60.56609606924865119, 10.36745004612414789 ) ) ;
#2775=ADVANCED_FACE ( 'NONE', ( #43538 ), #24489, .F. ) ;
#2780=DIRECTION ( 'NONE',  ( 0.000000000000000000, -1.000000000000000000, 0.000000000000000000 ) ) ;
#2781=CARTESIAN_POINT ( 'NONE',  ( 12.50000000000000000, -26.93717104351999936, 1.868110276009999908E-13 ) ) ;
#2784=LINE ( 'NONE', #20784, #31718 ) ;
#2786=EDGE_CURVE ( 'NONE', #49814, #47867, #21668, .T. ) ;
#2788=CARTESIAN_POINT ( 'NONE',  ( -3.295646577751982331, -1.720822363418331502, 1.264561824618803509 ) ) ;
#2790=CARTESIAN_POINT ( 'NONE',  ( 9.000000000000000000, -4.000000000000000000, 0.000000000000000000 ) ) ;
#2791=DIRECTION ( 'NONE',  ( 0.000000000000000000, 1.000000000000000000, 0.000000000000000000 ) ) ;
#2793=CARTESIAN_POINT ( 'NONE',  ( 9.931063219240325424, -17.87724209358196958, -7.763994033417543683 ) ) ;
#2795=CARTESIAN_POINT ( 'NONE',  ( -1.215810657191000121, -1.729405165122000154, -3.437332899015999921 ) ) ;
#2799=CARTESIAN_POINT ( 'NONE',  ( -12.54715396797999993, -54.26815137240999576, 1.292200816717000045 ) ) ;
#2802=CARTESIAN_POINT ( 'NONE',  ( -0.8506806241676574398, -3.104166666666666963, -3.165411199172027068 ) ) ;
#2805=CARTESIAN_POINT ( 'NONE',  ( 1.750000000000000000, -55.55000000209000177, -12.50000000000000000 ) ) ;
#2807=CARTESIAN_POINT ( 'NONE',  ( -0.4507512596549299033, -76.32183930805716443, -11.74168627474140969 ) ) ;
#2811=CARTESIAN_POINT ( 'NONE',  ( 10.12290050126000196, -60.04999999958999979, 7.648026767103999646 ) ) ;
#2816=CARTESIAN_POINT ( 'NONE',  ( -10.41172548051528146, -18.47988211125538527, -7.610718780881579271 ) ) ;
#2821=CARTESIAN_POINT ( 'NONE',  ( -0.1380878923284744875, -25.22734402323948544, 12.70555840932578384 ) ) ;
#2824=LINE ( 'NONE', #53275, #12192 ) ;
#2825=LINE ( 'NONE', #43856, #18308 ) ;
#2828=ORIENTED_EDGE ( 'NONE', *, *, #38049, .T. ) ;
#2829=DIRECTION ( 'NONE',  ( 0.000000000000000000, -1.000000000000000000, 0.000000000000000000 ) ) ;
#2830=B_SPLINE_CURVE_WITH_KNOTS ( 'NONE', 3,
 ( #21725, #52455, #48325, #29423, #34425, #52174, #43598, #12013 ),
 .UNSPECIFIED., .F., .F.,
 ( 4, 2, 2, 4 ),
 ( 0.000000000000000000, 0.4999999999999971134, 0.7499999999999985567, 1.000000000000000000 ),
 .UNSPECIFIED. ) ;
#2842=EDGE_CURVE ( 'NONE', #11057, #27205, #1887, .T. ) ;
#2849=CARTESIAN_POINT ( 'NONE',  ( 2.187994190098494052, -2.916594878656368461, 2.403360964150264234 ) ) ;
#2855=CARTESIAN_POINT ( 'NONE',  ( -9.152251458167393494, -76.25350003968078738, -7.375437608540630130 ) ) ;
#2856=CARTESIAN_POINT ( 'NONE',  ( 12.50000000000000000, -18.75000000240999753, 1.750000000000000000 ) ) ;
#2857=CARTESIAN_POINT ( 'NONE',  ( -8.220407391966000787, -61.61950084198999633, -9.523310056136001123 ) ) ;
#2858=EDGE_CURVE ( 'NONE', #28634, #6364, #35852, .T. ) ;
#2861=CIRCLE ( 'NONE', #24517, 1.749999999999997113 ) ;
#2863=B_SPLINE_CURVE_WITH_KNOTS ( 'NONE', 3,
 ( #16101, #25813, #3388, #43257, #8100, #38525, #21099, #56540, #29937, #16962, #34944, #43841 ),
 .UNSPECIFIED., .F., .F.,
 ( 4, 2, 2, 2, 2, 4 ),
 ( 0.000000000000000000, 0.1250000000000000000, 0.2500000000000000000, 0.5000000000000000000, 0.7500000000000000000, 1.000000000000000000 ),
 .UNSPECIFIED. ) ;
#2864=CARTESIAN_POINT ( 'NONE',  ( 5.512103878356000131, -76.85752566061000834, 11.78783395355999986 ) ) ;
#2865=CARTESIAN_POINT ( 'NONE',  ( 1.750000000001000089, -18.75000001325000198, 12.56594318051000059 ) ) ;
#2866=DIRECTION ( 'NONE',  ( 0.000000000000000000, 1.000000000000000000, 0.000000000000000000 ) ) ;
#2867=CARTESIAN_POINT ( 'NONE',  ( 10.98849124983000003, -76.88653068653000844, -4.660349322786999871 ) ) ;
#2872=CARTESIAN_POINT ( 'NONE',  ( -3.310367643023999662, -78.77244978676999665, -12.19650721378999947 ) ) ;
#2877=DIRECTION ( 'NONE',  ( -0.7071067811865475727, 0.000000000000000000, -0.7071067811865475727 ) ) ;
#2882=AXIS2_PLACEMENT_3D ( 'NONE', #53196, #12740, #12457 ) ;
#2884=ORIENTED_EDGE ( 'NONE', *, *, #49299, .T. ) ;
#2886=CARTESIAN_POINT ( 'NONE',  ( 12.58338334673999981, -57.05199022587000002, 1.667961445601999992 ) ) ;
#2888=ORIENTED_EDGE ( 'NONE', *, *, #53523, .F. ) ;
#2890=VERTEX_POINT ( 'NONE', #1885 ) ;
#2894=ORIENTED_EDGE ( 'NONE', *, *, #30754, .T. ) ;
#2897=CARTESIAN_POINT ( 'NONE',  ( 6.688645397968000950, -78.87909499590685414, 10.27915892414000076 ) ) ;
#2899=CARTESIAN_POINT ( 'NONE',  ( 9.523369619434999933, -53.98054357652999613, 8.220347091585999522 ) ) ;
#2900=CARTESIAN_POINT ( 'NONE',  ( 7.712209501881797102, -17.93822238229371635, -10.27335463211299960 ) ) ;
#2901=FACE_OUTER_BOUND ( 'NONE', #7102, .T. ) ;
#2907=EDGE_CURVE ( 'NONE', #54376, #12596, #51474, .T. ) ;
#2908=CARTESIAN_POINT ( 'NONE',  ( -6.024415200221000077, -76.36369539903000714, 10.73507988388000101 ) ) ;
#2909=VECTOR ( 'NONE', #648, 1000.000000000000227 ) ;
#2913=DIRECTION ( 'NONE',  ( -0.7272727272724163194, -0.6863485850246158204, -6.703676216865156901E-07 ) ) ;
#2914=CARTESIAN_POINT ( 'NONE',  ( 3.086017585447000222, -79.12790895394999779, -11.86910201801999953 ) ) ;
#2917=CARTESIAN_POINT ( 'NONE',  ( 12.00000000000000000, -55.54999999966999980, 0.000000000000000000 ) ) ;
#2918=EDGE_CURVE ( 'NONE', #44143, #27639, #11924, .T. ) ;
#2923=CARTESIAN_POINT ( 'NONE',  ( -3.258626092852999534, -3.578756257025999865, -0.9749691283561999766 ) ) ;
#2926=DIRECTION ( 'NONE',  ( 0.7071067811865475727, 0.000000000000000000, 0.7071067811865475727 ) ) ;
#2927=CARTESIAN_POINT ( 'NONE',  ( -7.648026768024999811, -18.75000001589999954, 10.12290050218000026 ) ) ;
#2929=FACE_OUTER_BOUND ( 'NONE', #54276, .T. ) ;
#2931=CARTESIAN_POINT ( 'NONE',  ( -10.35845616727999996, -23.29778595484999926, -7.627487606609999915 ) ) ;
#2935=CIRCLE ( 'NONE', #28370, 12.50000000000000000 ) ;
#2937=CARTESIAN_POINT ( 'NONE',  ( -8.652376385632999600, -62.06264602932999708, 9.414489258850998965 ) ) ;
#2938=CARTESIAN_POINT ( 'NONE',  ( -3.395341895239999630, -1.598905165122000094, 1.471171784242000014 ) ) ;
#2942=ORIENTED_EDGE ( 'NONE', *, *, #37152, .F. ) ;
#2946=CARTESIAN_POINT ( 'NONE',  ( -10.59551070212999946, -58.55648180022999583, -7.678690995210999404 ) ) ;
#2949=CARTESIAN_POINT ( 'NONE',  ( -12.50679926046298363, -54.49581646307559879, 1.424414840068720212 ) ) ;
#2952=CARTESIAN_POINT ( 'NONE',  ( 1.931043742978000077, -56.02204592290999585, -12.75763395696999858 ) ) ;
#2953=EDGE_CURVE ( 'NONE', #7307, #45201, #24594, .T. ) ;
#2954=CIRCLE ( 'NONE', #39731, 0.5000000000000004441 ) ;
#2955=CARTESIAN_POINT ( 'NONE',  ( -12.83044027758000105, -55.49360215019999742, 2.062670899361999766 ) ) ;
#2959=ORIENTED_EDGE ( 'NONE', *, *, #5783, .F. ) ;
#2960=VERTEX_POINT ( 'NONE', #5994 ) ;
#2963=EDGE_LOOP ( 'NONE', ( #1974, #5440, #29962, #48704, #22807 ) ) ;
#2964=CARTESIAN_POINT ( 'NONE',  ( 9.422860735135998311, -16.74048607655000254, 8.643926020477998406 ) ) ;
#2966=CARTESIAN_POINT ( 'NONE',  ( -0.9935076048178934638, -53.83183812217039588, 12.70250268212202371 ) ) ;
#2967=CARTESIAN_POINT ( 'NONE',  ( -3.331828115504000376, -76.97715654337000046, 12.52045872913000046 ) ) ;
#2970=B_SPLINE_CURVE_WITH_KNOTS ( 'NONE', 3,
 ( #52532, #3518, #43682, #44839, #21228, #52819, #16522, #53696, #39233, #12937, #39524, #17379, #35665, #8820, #30935, #13234 ),
 .UNSPECIFIED., .F., .F.,
 ( 4, 2, 2, 2, 2, 2, 2, 4 ),
 ( 0.000000000000000000, 0.2500000000000003886, 0.3750000000000005551, 0.5000000000000007772, 0.6250000000000009992, 0.6875000000000039968, 0.7500000000000069944, 1.000000000000000000 ),
 .UNSPECIFIED. ) ;
#2974=ORIENTED_EDGE ( 'NONE', *, *, #24005, .F. ) ;
#2975=CARTESIAN_POINT ( 'NONE',  ( 7.836763323982919083, -54.49488832206740341, -9.850488778787754640 ) ) ;
#2977=ORIENTED_EDGE ( 'NONE', *, *, #21236, .F. ) ;
#2982=CARTESIAN_POINT ( 'NONE',  ( -9.722718241315000398, -55.54999999966999980, 7.247844507162001015 ) ) ;
#2983=CARTESIAN_POINT ( 'NONE',  ( -14.00000000000000000, -80.70000000000000284, 0.000000000000000000 ) ) ;
#2985=DIRECTION ( 'NONE',  ( 0.000000000000000000, -1.000000000000000000, 0.000000000000000000 ) ) ;
#2989=CARTESIAN_POINT ( 'NONE',  ( -7.654537165468999760, -23.28056535155999995, 10.01332852689000141 ) ) ;
#2993=DIRECTION ( 'NONE',  ( 0.000000000000000000, 1.000000000000000000, 0.000000000000000000 ) ) ;
#2998=VECTOR ( 'NONE', #29245, 1000.000000000000000 ) ;
#3003=CARTESIAN_POINT ( 'NONE',  ( -12.71758670598746122, -17.93493368773759400, 1.809547514117124667 ) ) ;
#3005=CARTESIAN_POINT ( 'NONE',  ( -0.5480261397617977037, -1.862545821266776924, -3.476873622539977671 ) ) ;
#3010=DIRECTION ( 'NONE',  ( 0.000000000000000000, 1.000000000000000000, 0.000000000000000000 ) ) ;
#3018=CARTESIAN_POINT ( 'NONE',  ( 12.00000000000000000, -18.75000000000000000, 0.000000000000000000 ) ) ;
#3019=CARTESIAN_POINT ( 'NONE',  ( -1.980611416588530682, -18.47402268192283259, 12.74335092662909297 ) ) ;
#3021=CARTESIAN_POINT ( 'NONE',  ( 3.202676180380386928, -78.55085330470771510, 11.30378351636584533 ) ) ;
#3022=CARTESIAN_POINT ( 'NONE',  ( 9.369164850722000892, -23.25000000000000000, -7.601397897754999633 ) ) ;
#3027=CARTESIAN_POINT ( 'NONE',  ( 10.42531124905999995, -18.73514851523999880, -7.624341765453999997 ) ) ;
#3030=FACE_OUTER_BOUND ( 'NONE', #39334, .T. ) ;
#3035=ADVANCED_FACE ( 'NONE', ( #38742 ), #27342, .F. ) ;
#3036=VERTEX_POINT ( 'NONE', #39321 ) ;
#3039=LINE ( 'NONE', #30166, #27305 ) ;
#3041=CARTESIAN_POINT ( 'NONE',  ( -12.72554383680000001, -23.20159311629000243, 1.930239506950999884 ) ) ;
#3043=VERTEX_POINT ( 'NONE', #25454 ) ;
#3044=CARTESIAN_POINT ( 'NONE',  ( -12.82202470518000048, -55.37373556845999900, -2.066041976111999467 ) ) ;
#3045=CIRCLE ( 'NONE', #31280, 13.89999999999999858 ) ;
#3046=ORIENTED_EDGE ( 'NONE', *, *, #17079, .F. ) ;
#3054=ORIENTED_EDGE ( 'NONE', *, *, #21803, .T. ) ;
#3059=CARTESIAN_POINT ( 'NONE',  ( -12.77302471396000172, -61.52230123271999673, -1.481949986260999941 ) ) ;
#3062=CARTESIAN_POINT ( 'NONE',  ( 9.073558136327573465, -62.02808769462804861, 8.894842552356555743 ) ) ;
#3063=CARTESIAN_POINT ( 'NONE',  ( 1.750000000001000089, -23.25000000990999993, 12.56594317857000043 ) ) ;
#3069=CARTESIAN_POINT ( 'NONE',  ( -7.981651535783000462, -54.08135615453999634, 10.08154952393999970 ) ) ;
#3071=EDGE_CURVE ( 'NONE', #23838, #21348, #26020, .T. ) ;
#3073=CARTESIAN_POINT ( 'NONE',  ( -10.47840693002000023, -18.21310507181999938, -7.622759963130000038 ) ) ;
#3074=CARTESIAN_POINT ( 'NONE',  ( 7.654537085048000122, -60.08056692637000396, 10.01332844639000008 ) ) ;
#3075=CARTESIAN_POINT ( 'NONE',  ( -7.958776490640000034, -61.27699850015999772, 9.723157983991999487 ) ) ;
#3080=CARTESIAN_POINT ( 'NONE',  ( 2.391208922872818832, -3.499999999999999556, 2.442030068879051719 ) ) ;
#3081=CARTESIAN_POINT ( 'NONE',  ( -0.5774875637779700588, -1.362040185579431295, -3.482711565813724874 ) ) ;
#3082=EDGE_LOOP ( 'NONE', ( #19165, #46778, #46668, #48073, #384 ) ) ;
#3084=CARTESIAN_POINT ( 'NONE',  ( 0.000000000000000000, -0.2000000000000000111, 0.000000000000000000 ) ) ;
#3085=CARTESIAN_POINT ( 'NONE',  ( -12.53239398062000198, -19.23513569609999863, 1.667936688463999895 ) ) ;
#3086=CARTESIAN_POINT ( 'NONE',  ( -3.006336704280999861, -1.519671397434999793, 0.9646084678590001182 ) ) ;
#3088=AXIS2_PLACEMENT_3D ( 'NONE', #8858, #40447, #22134 ) ;
#3089=CARTESIAN_POINT ( 'NONE',  ( -12.49837451343999994, -55.59042109264999709, 1.667049596277000001 ) ) ;
#3091=DIRECTION ( 'NONE',  ( 0.000000000000000000, 1.000000000000000000, 0.000000000000000000 ) ) ;
#3093=CARTESIAN_POINT ( 'NONE',  ( 11.79999999988000070, -18.85000000520999919, 0.5999999998848000171 ) ) ;
#3098=CARTESIAN_POINT ( 'NONE',  ( 6.439298073612021334, -76.37065965127577272, -9.837794316883584855 ) ) ;
#3101=CARTESIAN_POINT ( 'NONE',  ( -10.07627163191000008, -23.24999999688999708, 7.601397897754999633 ) ) ;
#3103=DIRECTION ( 'NONE',  ( -0.6489586447433819405, 0.04890182323493858646, 0.7592504784964787534 ) ) ;
#3104=CARTESIAN_POINT ( 'NONE',  ( -0.8506806241676574398, -2.604166666666666519, -3.165411199172027068 ) ) ;
#3107=DIRECTION ( 'NONE',  ( 0.000000000000000000, 0.000000000000000000, 1.000000000000000000 ) ) ;
#3109=AXIS2_PLACEMENT_3D ( 'NONE', #43235, #2791, #6342 ) ;
#3110=ADVANCED_FACE ( 'NONE', ( #34304 ), #52335, .T. ) ;
#3111=CIRCLE ( 'NONE', #37946, 0.5000000000000006661 ) ;
#3113=DIRECTION ( 'NONE',  ( 0.000000000000000000, 1.000000000000000000, 0.000000000000000000 ) ) ;
#3116=ORIENTED_EDGE ( 'NONE', *, *, #36821, .F. ) ;
#3117=DIRECTION ( 'NONE',  ( 0.000000000000000000, 0.000000000000000000, 1.000000000000000000 ) ) ;
#3118=ORIENTED_EDGE ( 'NONE', *, *, #22608, .T. ) ;
#3120=CARTESIAN_POINT ( 'NONE',  ( 2.933193322904608991, -3.500000000000000000, -1.912021129721755530 ) ) ;
#3125=ADVANCED_FACE ( 'NONE', ( #57045 ), #28857, .T. ) ;
#3128=CARTESIAN_POINT ( 'NONE',  ( 7.345153731672205311, -55.57158755757197355, -8.188331488387625257 ) ) ;
#3129=ORIENTED_EDGE ( 'NONE', *, *, #50351, .F. ) ;
#3131=AXIS2_PLACEMENT_3D ( 'NONE', #44299, #4148, #22444 ) ;
#3132=DIRECTION ( 'NONE',  ( -0.9903465037206092836, -0.1386138613861012392, 0.000000000000000000 ) ) ;
#3134=CARTESIAN_POINT ( 'NONE',  ( 9.723199429438999175, -17.52306056078000296, -7.958735708418001487 ) ) ;
#3136=B_SPLINE_CURVE_WITH_KNOTS ( 'NONE', 3,
 ( #20333, #25043, #11488, #38328, #56351, #29460, #7044, #38621, #17933, #17633, #34753, #35622, #58073, #12899, #58371, #48648, #44795, #52780, #39191, #48085, #53650, #13190, #31184, #26471, #7901, #40057 ),
 .UNSPECIFIED., .F., .F.,
 ( 4, 2, 2, 2, 2, 2, 2, 2, 2, 2, 2, 2, 4 ),
 ( 0.000000000000000000, 0.06249999999999995837, 0.1249999999999999167, 0.2499999999999998335, 0.3749999999999998335, 0.4374999999999998890, 0.4999999999999998890, 0.6249999999999998890, 0.6874999999999998890, 0.7499999999999997780, 0.8749999999999998890, 0.9374999999999998890, 1.000000000000000000 ),
 .UNSPECIFIED. ) ;
#3137=CARTESIAN_POINT ( 'NONE',  ( 2.468869335794306785, -79.03645833334485360, 11.59083142015582624 ) ) ;
#3141=CARTESIAN_POINT ( 'NONE',  ( -10.12290050124000018, -18.75000000007999645, 7.648026767085999822 ) ) ;
#3144=CARTESIAN_POINT ( 'NONE',  ( 1.506700327918974347, -2.937474389527924945, 2.893236496711840910 ) ) ;
#3146=AXIS2_PLACEMENT_3D ( 'NONE', #850, #10562, #24125 ) ;
#3150=CARTESIAN_POINT ( 'NONE',  ( -3.268529449828999844, -2.290807261823000207, -1.950076325099000085 ) ) ;
#3151=CARTESIAN_POINT ( 'NONE',  ( 10.53003223724000037, -18.67547470641000018, 7.612971414716000140 ) ) ;
#3153=CARTESIAN_POINT ( 'NONE',  ( -8.588902834722000890, -61.93240111547999760, -9.317946123669999636 ) ) ;
#3156=CARTESIAN_POINT ( 'NONE',  ( 14.00000000000000000, -72.89999999999999147, -1.714505518806294638E-15 ) ) ;
#3157=CARTESIAN_POINT ( 'NONE',  ( 5.865988621150640190E-14, -72.89999999999999147, 14.00000000000097877 ) ) ;
#3159=EDGE_CURVE ( 'NONE', #57766, #22110, #11891, .T. ) ;
#3160=CARTESIAN_POINT ( 'NONE',  ( 13.49939038839240979, -32.88214388149999934, 0.1282931867975413143 ) ) ;
#3161=CARTESIAN_POINT ( 'NONE',  ( 6.640280624951000021, -75.91133535973999358, 10.42739536823000002 ) ) ;
#3162=ORIENTED_EDGE ( 'NONE', *, *, #13222, .F. ) ;
#3164=CARTESIAN_POINT ( 'NONE',  ( 0.000000000000000000, -32.88214388149999934, 0.000000000000000000 ) ) ;
#3165=CARTESIAN_POINT ( 'NONE',  ( 12.68703394093999925, -60.55066116444000102, 1.889962945498999902 ) ) ;
#3166=CARTESIAN_POINT ( 'NONE',  ( -12.50000327350000084, -79.18030127599000423, -1.860978320792999963 ) ) ;
#3167=DIRECTION ( 'NONE',  ( 0.000000000000000000, 1.000000000000000000, 0.000000000000000000 ) ) ;
#3173=CARTESIAN_POINT ( 'NONE',  ( -1.750000000000000000, -55.55000000278000272, -12.50000000000000000 ) ) ;
#3176=ORIENTED_EDGE ( 'NONE', *, *, #12093, .F. ) ;
#3177=EDGE_CURVE ( 'NONE', #41516, #19523, #44190, .T. ) ;
#3180=CARTESIAN_POINT ( 'NONE',  ( 12.82904109059999875, -55.47547726255000100, 2.062673488410000200 ) ) ;
#3182=ORIENTED_EDGE ( 'NONE', *, *, #23349, .F. ) ;
#3184=ORIENTED_EDGE ( 'NONE', *, *, #42622, .T. ) ;
#3186=TOROIDAL_SURFACE ( 'NONE', #6970, 13.50000000000000000, 0.5000000000000000000 ) ;
#3187=ADVANCED_FACE ( 'NONE', ( #38453 ), #56470, .F. ) ;
#3189=CARTESIAN_POINT ( 'NONE',  ( 1.704789469356775555, -60.50346161385093069, 12.53199752969997682 ) ) ;
#3191=EDGE_CURVE ( 'NONE', #46715, #42403, #24151, .T. ) ;
#3192=VERTEX_POINT ( 'NONE', #49648 ) ;
#3193=ORIENTED_EDGE ( 'NONE', *, *, #24448, .T. ) ;
#3194=CARTESIAN_POINT ( 'NONE',  ( -5.950798862880000151, -78.96531715013686892, 10.72320280238000123 ) ) ;
#3196=CARTESIAN_POINT ( 'NONE',  ( 9.966229686695001533, -55.13098097352000337, 7.657726530227999540 ) ) ;
#3197=CARTESIAN_POINT ( 'NONE',  ( 10.12290050255000118, -55.55000002206000431, 7.648026768392999664 ) ) ;
#3203=CARTESIAN_POINT ( 'NONE',  ( -3.151328970204000157, -76.05239898940999410, -11.89977497056000111 ) ) ;
#3204=EDGE_CURVE ( 'NONE', #44781, #13102, #48768, .T. ) ;
#3210=CARTESIAN_POINT ( 'NONE',  ( -7.553727747500123435, -60.48581381149021752, -7.997114030232342685 ) ) ;
#3213=CIRCLE ( 'NONE', #6031, 12.80000000000000071 ) ;
#3217=DIRECTION ( 'NONE',  ( 0.000000000000000000, 1.000000000000000000, 0.000000000000000000 ) ) ;
#3218=CLOSED_SHELL ( 'NONE', ( #8338, #40918, #18041, #43680, #15503, #48520, #15837, #43302, #5850, #23792, #36669, #13142, #53101, #45053, #3292, #4458, #3125, #12505, #11156, #53920, #48834, #529, #4367, #48637, #10478, #44201, #20250, #22544, #23612, #55524, #14497, #22097, #40205, #6910, #26633, #45845, #55223, #32970, #5936, #17479, #54884, #25957, #53064, #23359, #20414, #14717, #10200, #34037, #4557, #13972, #11603, #5920, #32233, #55487, #36421, #21309, #55816, #17575, #57832, #5765, #20027, #23374, #51918, #11364, #35979, #16319, #26875, #24105, #48964, #16030, #55403, #6379, #44115, #16915, #17400, #12301, #45690, #57367, #39943, #47183, #5732, #49551, #24219, #14028, #21451, #38622, #16932, #9387, #25711, #35017, #3110, #22286, #39114, #40170, #54572, #4210, #14617, #33146, #28674, #14531, #41565, #54667, #26515, #53296, #47340, #14802, #38501, #34398, #9443, #23619, #34283, #5043, #21299, #3488, #24657, #40909, #16496, #50052, #46342, #31475, #49610, #19966, #20041, #44427, #19917, #45559, #43172, #56061, #6172, #34971, #56880, #4493, #704, #27577, #56678, #56236, #16762, #9524, #29584, #12397, #43910, #47705, #38748, #12469, #28572, #48984, #38225, #57923, #46201, #10248, #6593, #52537, #37276, #24351, #30854, #28816, #12799, #3833, #9251, #33556, #16417, #31589, #29512, #36010, #42726, #13174, #50139, #22479, #22366, #31327, #34072, #29550, #37015, #27182, #54613, #31761, #32022, #53354, #58332, #18641, #976, #57921, #38911, #37941, #4494, #7921, #10905, #22196, #21380, #25950, #31508, #41828, #26727, #10290, #39613, #37678, #9156, #50171, #17354, #43984, #52338, #32561, #43187, #6703, #8680, #5711, #23597, #26063, #21737, #21375, #45256, #7096, #41901, #42026, #18199, #48703, #20008, #57471, #15039, #34434, #17220, #37299, #29784, #20577, #4795, #33162, #52970, #43972, #6515, #55747, #2531, #56383, #34149, #13300, #34327, #12366, #42712, #7828, #40016, #7506, #1636, #7030, #56631, #9458, #34880, #29760, #32486, #32352, #57205, #39530, #57220, #11434, #13277, #17754, #15007, #677, #8818, #44149, #57296, #49376, #22836, #55436, #56300, #24366, #47504, #16791, #46220, #5696, #49282, #13404, #41914, #49111, #4984, #11670, #40943, #16398, #29948, #17303, #249, #7904, #42844, #46376, #33520, #17463, #32716, #6066, #38165, #35114, #52022, #39032, #10731, #21529, #50550, #12054, #18411, #2658, #55826, #8749, #28300, #56772, #3035, #30120, #32437, #39476, #10619, #6117, #5226, #48559, #21635, #30835, #41288, #20955, #33294, #57614, #24969, #52698, #47370, #12776, #52294, #31903, #17772, #32316, #8908, #49931, #28074, #10529, #20961, #46185, #46754, #46603, #14787, #36338, #43342, #32522, #25499, #14428, #9317, #10565, #43713, #41666, #44030, #54470, #47584, #6237, #49721, #930, #40642, #32630, #40426, #30725, #28641, #20095, #36507, #33215, #19504, #42534, #33486, #29493, #55353, #42691, #41039, #56966, #16986, #43793, #31487, #3900, #8530, #47067, #21152, #42762, #38068, #40623, #51827, #38884, #54738, #57959, #33949, #10606, #4159, #16066, #12635, #19120, #7452, #48127, #55578, #50908, #56659, #27421, #36784, #15917, #37451, #25706, #30617, #32857, #15239, #5434, #2382, #56781, #34369, #54620, #7974, #14285, #53499, #44730, #27643, #8568, #20114, #34730, #50697, #4301, #36166, #56803, #12298, #44576, #52372, #9303, #285, #6802, #6857, #22319, #5611, #52559, #32027, #52484, #29721, #14752, #1722, #1973, #2775, #28026, #8446, #22193, #20810, #16813, #54295, #3187, #37516, #43760, #10132, #9131, #40588, #15294, #21249, #34612, #33321, #8035, #32651, #15623, #51382, #18860, #9650, #26542, #52741, #50327, #13348, #41608, #11592, #18385, #56475, #23395, #2585, #13071, #10406, #46236, #47326, #23915, #53266, #54039, #31255, #13773, #40707, #27571, #13549, #41088, #44915, #19057, #28215, #5877, #9531, #3499, #5088, #32227, #35229, #24240, #40437, #39920, #55919, #7414, #52129, #24574, #57275, #46884, #38669, #19441 ) ) ;
#3219=CARTESIAN_POINT ( 'NONE',  ( 2.847026051941000002, -3.259547503149000214, -1.861134274785000153 ) ) ;
#3222=CARTESIAN_POINT ( 'NONE',  ( -11.50186437804589090, -76.18325783269531826, 2.401250034516278831 ) ) ;
#3223=CARTESIAN_POINT ( 'NONE',  ( -7.644092900773785004, -18.47619833611051021, 10.09634159701094447 ) ) ;
#3231=FACE_OUTER_BOUND ( 'NONE', #52360, .T. ) ;
#3234=FACE_OUTER_BOUND ( 'NONE', #57758, .T. ) ;
#3236=VERTEX_POINT ( 'NONE', #36341 ) ;
#3238=CARTESIAN_POINT ( 'NONE',  ( 2.028166799595999770, -0.9844610208691998432, -3.466423845304999585 ) ) ;
#3244=ORIENTED_EDGE ( 'NONE', *, *, #18460, .T. ) ;
#3245=EDGE_CURVE ( 'NONE', #41301, #16006, #14699, .T. ) ;
#3247=CARTESIAN_POINT ( 'NONE',  ( 10.12290050122000018, -55.54999999974999980, -7.648026767069000087 ) ) ;
#3248=CARTESIAN_POINT ( 'NONE',  ( 1.667961445601999992, -57.05199022587000002, -12.58338334673999981 ) ) ;
#3249=CARTESIAN_POINT ( 'NONE',  ( -12.87024489159000140, -59.58461666436000570, 2.062597265787999845 ) ) ;
#3250=FACE_BOUND ( 'NONE', #48402, .T. ) ;
#3251=AXIS2_PLACEMENT_3D ( 'NONE', #19727, #37724, #24446 ) ;
#3253=EDGE_LOOP ( 'NONE', ( #38606, #33928, #36721, #13284 ) ) ;
#3254=EDGE_CURVE ( 'NONE', #48866, #46129, #37337, .T. ) ;
#3261=CARTESIAN_POINT ( 'NONE',  ( 0.5222397222179528953, -53.63701780570490740, 12.70447686579673352 ) ) ;
#3262=CARTESIAN_POINT ( 'NONE',  ( 5.552077009241000560, -78.59443890784000075, 11.35743496097000005 ) ) ;
#3263=CARTESIAN_POINT ( 'NONE',  ( 14.00000000000000000, -32.90763690531000663, 1.352038286454999952E-05 ) ) ;
#3264=CARTESIAN_POINT ( 'NONE',  ( -11.79999999999999893, -23.15000000000000213, -0.5999999999999999778 ) ) ;
#3265=CARTESIAN_POINT ( 'NONE',  ( 10.14950121160999963, -22.75077027493999893, 7.674627477456000157 ) ) ;
#3268=ORIENTED_EDGE ( 'NONE', *, *, #49091, .T. ) ;
#3270=EDGE_LOOP ( 'NONE', ( #3974, #51258, #19150 ) ) ;
#3276=CARTESIAN_POINT ( 'NONE',  ( -8.838834764832000701, -55.54999999966999980, -8.838834764832000701 ) ) ;
#3277=CARTESIAN_POINT ( 'NONE',  ( -7.610717068332717439, -18.47984996834297888, 10.41172376763008245 ) ) ;
#3279=CARTESIAN_POINT ( 'NONE',  ( -12.83044039274999903, -18.69360374348000065, -2.062670899148999926 ) ) ;
#3286=VERTEX_POINT ( 'NONE', #54073 ) ;
#3291=CARTESIAN_POINT ( 'NONE',  ( -12.70451544424564361, -17.44534321915444863, 1.498804046748215546 ) ) ;
#3292=ADVANCED_FACE ( 'NONE', ( #12736 ), #42070, .F. ) ;
#3297=CARTESIAN_POINT ( 'NONE',  ( -1.933504092460999857, -55.39593152692000189, -12.70940235704999921 ) ) ;
#3298=CARTESIAN_POINT ( 'NONE',  ( 9.798996500078068550, -75.99648035482640296, 6.483966265465372913 ) ) ;
#3300=VERTEX_POINT ( 'NONE', #21601 ) ;
#3301=CARTESIAN_POINT ( 'NONE',  ( 11.00000000000000000, -18.25000000000000000, 1.016729233725000008E-14 ) ) ;
#3309=CARTESIAN_POINT ( 'NONE',  ( 5.947890417171738164, -78.53226363305368807, 10.13299647784000257 ) ) ;
#3310=DIRECTION ( 'NONE',  ( 0.000000000000000000, 1.000000000000000000, 0.000000000000000000 ) ) ;
#3317=CARTESIAN_POINT ( 'NONE',  ( 10.26699006316251683, -77.59166666666666856, 5.917523019358090330 ) ) ;
#3322=DIRECTION ( 'NONE',  ( 0.000000000000000000, -1.000000000000000000, 0.000000000000000000 ) ) ;
#3323=CIRCLE ( 'NONE', #36310, 8.800000000000000711 ) ;
#3324=DIRECTION ( 'NONE',  ( -0.7071067811865474617, 0.000000000000000000, 0.7071067811865474617 ) ) ;
#3325=VERTEX_POINT ( 'NONE', #27474 ) ;
#3328=CARTESIAN_POINT ( 'NONE',  ( -12.66313295592999921, -53.62196533848999991, 0.06049275240488000138 ) ) ;
#3331=CARTESIAN_POINT ( 'NONE',  ( 8.438902753042999194, -78.73739079806000518, -8.898539530003999332 ) ) ;
#3332=VERTEX_POINT ( 'NONE', #26312 ) ;
#3338=VERTEX_POINT ( 'NONE', #4474 ) ;
#3342=CARTESIAN_POINT ( 'NONE',  ( 9.000000000000000000, -0.5000000000000000000, 0.000000000000000000 ) ) ;
#3343=CARTESIAN_POINT ( 'NONE',  ( -12.59682790095999927, -60.18734115192999923, -1.801645751184999922 ) ) ;
#3345=CARTESIAN_POINT ( 'NONE',  ( 7.642147947518999729, -22.78485473281999774, 10.55910102242999926 ) ) ;
#3346=CARTESIAN_POINT ( 'NONE',  ( -12.57042253521000141, -15.89905023022000030, 0.000000000000000000 ) ) ;
#3347=CARTESIAN_POINT ( 'NONE',  ( 10.42531125072000009, -55.53514854654000032, 7.624341767124000135 ) ) ;
#3349=CARTESIAN_POINT ( 'NONE',  ( 12.43570956085999946, -17.12016029981999665, -0.4384071701242000518 ) ) ;
#3351=VERTEX_POINT ( 'NONE', #44326 ) ;
#3352=CARTESIAN_POINT ( 'NONE',  ( -9.101506735319000896, -53.91932813864999474, 8.485532457216999447 ) ) ;
#3354=CARTESIAN_POINT ( 'NONE',  ( -9.395773752832997872, -17.29509747843999889, -8.188237371225000061 ) ) ;
#3358=CARTESIAN_POINT ( 'NONE',  ( 7.601397897754999633, -55.55000000209000177, 10.07627163191000008 ) ) ;
#3360=CARTESIAN_POINT ( 'NONE',  ( 13.49939038839240979, -9.295797029142999435, 0.1282931867975413143 ) ) ;
#3362=CARTESIAN_POINT ( 'NONE',  ( 1.738970389193763122, -3.500000000000001332, 2.879943715822681494 ) ) ;
#3364=EDGE_CURVE ( 'NONE', #17621, #47646, #32872, .T. ) ;
#3367=LINE ( 'NONE', #52387, #6067 ) ;
#3368=AXIS2_PLACEMENT_3D ( 'NONE', #46810, #1934, #42068 ) ;
#3369=CARTESIAN_POINT ( 'NONE',  ( -12.83044039274999903, -23.30639625649999758, 2.062670899148999926 ) ) ;
#3370=CARTESIAN_POINT ( 'NONE',  ( 3.754188153876000467, -2.981688735460999773, 0.6259984742306999861 ) ) ;
#3371=B_SPLINE_CURVE_WITH_KNOTS ( 'NONE', 3,
 ( #42656, #12222, #29635, #2793, #33776, #56813 ),
 .UNSPECIFIED., .F., .F.,
 ( 4, 2, 4 ),
 ( 0.000000000000000000, 0.5000000000000000000, 1.000000000000000000 ),
 .UNSPECIFIED. ) ;
#3373=B_SPLINE_CURVE_WITH_KNOTS ( 'NONE', 3,
 ( #3872, #3019, #52325, #57893, #34577, #13007, #4168, #26579, #21589, #11879, #57319, #3586, #52610, #8013, #31007, #7444, #39596, #57034, #17450, #8302, #29857, #26010, #34864, #39880, #49045, #12727, #30720, #8591, #48755, #16593 ),
 .UNSPECIFIED., .F., .F.,
 ( 4, 2, 2, 2, 2, 2, 2, 2, 2, 2, 2, 2, 2, 2, 4 ),
 ( 0.000000000000000000, 0.1250000000000009714, 0.1875000000000014155, 0.2500000000000018874, 0.3125000000000023315, 0.3750000000000027200, 0.5000000000000035527, 0.5625000000000039968, 0.6250000000000045519, 0.6875000000000049960, 0.7500000000000054401, 0.8125000000000059952, 0.8437500000000055511, 0.8750000000000051070, 1.000000000000000000 ),
 .UNSPECIFIED. ) ;
#3374=CARTESIAN_POINT ( 'NONE',  ( -12.77302454164000167, -54.07764858523999862, 1.481891240072999993 ) ) ;
#3376=DIRECTION ( 'NONE',  ( 0.4045849535018030685, -0.8201353734597037759, -0.4045849535018030685 ) ) ;
#3379=FACE_OUTER_BOUND ( 'NONE', #15527, .T. ) ;
#3381=CARTESIAN_POINT ( 'NONE',  ( 3.719372377260759421, -76.80315702122973676, 11.49187281106599201 ) ) ;
#3382=CARTESIAN_POINT ( 'NONE',  ( 10.84983825364951748, -76.41841306282870505, -4.509958312123425905 ) ) ;
#3384=EDGE_CURVE ( 'NONE', #25767, #48350, #8947, .T. ) ;
#3388=CARTESIAN_POINT ( 'NONE',  ( -0.5095438350929912819, -3.488646560560789922, 3.221021376419205939 ) ) ;
#3396=ORIENTED_EDGE ( 'NONE', *, *, #15670, .F. ) ;
#3397=EDGE_CURVE ( 'NONE', #28402, #27979, #26025, .T. ) ;
#3398=CARTESIAN_POINT ( 'NONE',  ( -1.689459950960819912, -24.29188253903401318, 12.71013585610284302 ) ) ;
#3399=EDGE_CURVE ( 'NONE', #27850, #17621, #55481, .T. ) ;
#3400=ORIENTED_EDGE ( 'NONE', *, *, #47283, .T. ) ;
#3401=ORIENTED_EDGE ( 'NONE', *, *, #32773, .T. ) ;
#3407=ORIENTED_EDGE ( 'NONE', *, *, #19575, .F. ) ;
#3408=CARTESIAN_POINT ( 'NONE',  ( -9.428374488006999954, -78.94967853533998436, 7.989839463457000690 ) ) ;
#3412=CARTESIAN_POINT ( 'NONE',  ( -7.601397897754999633, -60.04999999966999980, -9.369164850722000892 ) ) ;
#3413=CIRCLE ( 'NONE', #16609, 12.90000000000000036 ) ;
#3420=CARTESIAN_POINT ( 'NONE',  ( -3.226165562315000290, -77.90040178014000105, 12.71052925661000010 ) ) ;
#3426=CARTESIAN_POINT ( 'NONE',  ( -2.327681217703248873, -3.038872842925070650, 2.267910747349583200 ) ) ;
#3428=CARTESIAN_POINT ( 'NONE',  ( 0.8338927958961740439, -24.80053577746324223, -12.50366901602911796 ) ) ;
#3430=CARTESIAN_POINT ( 'NONE',  ( -1.568660613942000071, -1.873862256653000102, -3.467930652269000102 ) ) ;
#3432=EDGE_CURVE ( 'NONE', #44710, #32490, #947, .T. ) ;
#3433=CARTESIAN_POINT ( 'NONE',  ( 10.42531124905999995, -23.26485148473999942, 7.624341765453999997 ) ) ;
#3434=CARTESIAN_POINT ( 'NONE',  ( 12.50000000000000000, -55.55000000278000272, -1.750000000000000000 ) ) ;
#3436=CARTESIAN_POINT ( 'NONE',  ( -12.66235371498999918, -16.86260492134000089, -0.4957155363045999685 ) ) ;
#3437=DIRECTION ( 'NONE',  ( 0.000000000000000000, 0.000000000000000000, 1.000000000000000000 ) ) ;
#3439=CARTESIAN_POINT ( 'NONE',  ( 1.931736162947051527, -23.76670395715774120, -12.72978979890034523 ) ) ;
#3440=CARTESIAN_POINT ( 'NONE',  ( -10.36185853650999888, -76.12736320551000802, -6.742090815642000301 ) ) ;
#3441=ORIENTED_EDGE ( 'NONE', *, *, #3177, .F. ) ;
#3443=CARTESIAN_POINT ( 'NONE',  ( 12.46165725309000116, -60.47155322489999918, 1.631637378451999965 ) ) ;
#3444=CARTESIAN_POINT ( 'NONE',  ( -1.667917367065999912, -23.28056535155999995, -12.49306764015999960 ) ) ;
#3456=CARTESIAN_POINT ( 'NONE',  ( 12.92177931905999877, -58.55736537918999574, 2.062503053667999797 ) ) ;
#3460=AXIS2_PLACEMENT_3D ( 'NONE', #18296, #31549, #3827 ) ;
#3461=ORIENTED_EDGE ( 'NONE', *, *, #48168, .F. ) ;
#3462=VERTEX_POINT ( 'NONE', #55522 ) ;
#3463=CARTESIAN_POINT ( 'NONE',  ( -2.061613410425999771, -18.79429985524000202, 12.83797036855999885 ) ) ;
#3464=DIRECTION ( 'NONE',  ( -1.000000000000000000, 0.000000000000000000, 0.000000000000000000 ) ) ;
#3467=CARTESIAN_POINT ( 'NONE',  ( 10.98964036629034347, -18.48475764895797724, 0.4777763868204561448 ) ) ;
#3470=B_SPLINE_CURVE_WITH_KNOTS ( 'NONE', 3,
 ( #5061, #50819, #1812, #10362, #5345, #37504 ),
 .UNSPECIFIED., .F., .F.,
 ( 4, 1, 1, 4 ),
 ( 0.000000000000000000, 0.3333333311575783497, 0.6666666623152567306, 0.9999999934728349693 ),
 .UNSPECIFIED. ) ;
#3472=FACE_OUTER_BOUND ( 'NONE', #5779, .T. ) ;
#3473=EDGE_CURVE ( 'NONE', #22042, #6883, #33066, .T. ) ;
#3476=CARTESIAN_POINT ( 'NONE',  ( 12.70395504303439260, -61.40679290091602383, -1.447100708809422986 ) ) ;
#3478=CARTESIAN_POINT ( 'NONE',  ( -10.14950121160999963, -22.75077027493999893, -7.674627477456000157 ) ) ;
#3479=CARTESIAN_POINT ( 'NONE',  ( -8.596763593952999827, -25.13532396123000012, 9.310159863706001460 ) ) ;
#3480=AXIS2_PLACEMENT_3D ( 'NONE', #7195, #33469, #55927 ) ;
#3483=CARTESIAN_POINT ( 'NONE',  ( -12.77302454167999990, -17.27764858556999883, 1.481891240072999993 ) ) ;
#3486=CARTESIAN_POINT ( 'NONE',  ( -8.190817883596533733, -60.03019609282340951, -7.342377162853142458 ) ) ;
#3488=ADVANCED_FACE ( 'NONE', ( #51112 ), #15374, .T. ) ;
#3489=CARTESIAN_POINT ( 'NONE',  ( 4.117077995765999532, -1.540283069271000116, -0.2120472831400999902 ) ) ;
#3491=AXIS2_PLACEMENT_3D ( 'NONE', #28886, #10613, #55775 ) ;
#3494=CARTESIAN_POINT ( 'NONE',  ( 1.980532758766000212, -59.56256650660999696, -12.80088938804999898 ) ) ;
#3495=CARTESIAN_POINT ( 'NONE',  ( -7.954951288349001004, -23.44678171330999916, -9.722718241315000398 ) ) ;
#3496=CARTESIAN_POINT ( 'NONE',  ( -3.535607672357000020, -2.959660817501999830, 0.3961643838024999642 ) ) ;
#3499=ADVANCED_FACE ( 'NONE', ( #36635 ), #15672, .F. ) ;
#3500=CARTESIAN_POINT ( 'NONE',  ( -7.719682335140538143, -75.80000000000002558, 9.059469227681002934 ) ) ;
#3504=ORIENTED_EDGE ( 'NONE', *, *, #19789, .T. ) ;
#3505=CARTESIAN_POINT ( 'NONE',  ( -10.18589234708000113, -23.28917565320000094, -7.641012386039999882 ) ) ;
#3509=B_SPLINE_CURVE_WITH_KNOTS ( 'NONE', 3,
 ( #32368, #37689, #22948, #6103, #14084, #54542 ),
 .UNSPECIFIED., .F., .F.,
 ( 4, 1, 1, 4 ),
 ( 0.000000000000000000, 0.3333333333333000081, 0.6666666666667000474, 1.000000000000000000 ),
 .UNSPECIFIED. ) ;
#3510=DIRECTION ( 'NONE',  ( 0.000000000000000000, -1.000000000000000000, 0.000000000000000000 ) ) ;
#3512=CARTESIAN_POINT ( 'NONE',  ( 0.5847238537393000257, -1.182588905188999950, -3.489934961497000110 ) ) ;
#3514=CARTESIAN_POINT ( 'NONE',  ( 12.43646324844999995, -24.92048514568000073, -0.1256879863178999857 ) ) ;
#3518=CARTESIAN_POINT ( 'NONE',  ( -12.70556836324529293, -53.57227722633783173, 0.2641978056810228570 ) ) ;
#3520=CARTESIAN_POINT ( 'NONE',  ( 0.6679678761999167103, -1.742764817395623389, -3.205531000182274770 ) ) ;
#3524=FACE_OUTER_BOUND ( 'NONE', #15954, .T. ) ;
#3525=CARTESIAN_POINT ( 'NONE',  ( 8.583677311528019160, -61.77185920727337276, -9.102132575249884283 ) ) ;
#3526=CARTESIAN_POINT ( 'NONE',  ( -8.485281374238999419, -55.64999999967000122, 8.485281374238999419 ) ) ;
#3527=VECTOR ( 'NONE', #6675, 999.9999999999998863 ) ;
#3528=CARTESIAN_POINT ( 'NONE',  ( -12.49306764019000049, -60.08056535122999975, 1.667917367065999912 ) ) ;
#3529=CARTESIAN_POINT ( 'NONE',  ( -7.646966891740999195, -55.60358255701000019, -10.19019756604999927 ) ) ;
#3532=CONICAL_SURFACE ( 'NONE', #5437, 0.6999999997695030007, 0.7853981633972997312 ) ;
#3533=ORIENTED_EDGE ( 'NONE', *, *, #47407, .F. ) ;
#3535=CARTESIAN_POINT ( 'NONE',  ( -10.07627163191000008, -55.55000000209000177, 7.601397897754999633 ) ) ;
#3539=CARTESIAN_POINT ( 'NONE',  ( -2.099388381696000023E-14, -0.04999999937965000224, -12.74999999937999995 ) ) ;
#3540=AXIS2_PLACEMENT_3D ( 'NONE', #26513, #31527, #39809 ) ;
#3541=DIRECTION ( 'NONE',  ( -4.025425605489000457E-14, 1.534883903844000000E-11, -1.000000000000000000 ) ) ;
#3542=CARTESIAN_POINT ( 'NONE',  ( 12.30436613475999863, -78.39634877618999553, -3.523071432600000108 ) ) ;
#3544=CARTESIAN_POINT ( 'NONE',  ( -7.714303428875997959, -26.30294702886003222, 12.53545825868000385 ) ) ;
#3546=CARTESIAN_POINT ( 'NONE',  ( 8.838834764832000701, -60.04999999966999980, -8.838834764832000701 ) ) ;
#3549=VERTEX_POINT ( 'NONE', #25662 ) ;
#3553=DIRECTION ( 'NONE',  ( 0.000000000000000000, 0.000000000000000000, -1.000000000000000000 ) ) ;
#3556=CARTESIAN_POINT ( 'NONE',  ( -0.09454008427527169078, -3.226439081450838131, 3.519011153166962114 ) ) ;
#3557=CARTESIAN_POINT ( 'NONE',  ( -7.770365054039128694, -17.76417299472041122, 10.20675369723943859 ) ) ;
#3558=DIRECTION ( 'NONE',  ( 0.7071067811865475727, 0.000000000000000000, 0.7071067811865475727 ) ) ;
#3562=CARTESIAN_POINT ( 'NONE',  ( 10.18589226631999978, -23.28917723430000208, -7.641012305222999679 ) ) ;
#3569=CARTESIAN_POINT ( 'NONE',  ( 7.648026766753000416, -60.05000000550000294, -10.12290050090999927 ) ) ;
#3576=CARTESIAN_POINT ( 'NONE',  ( -0.9887300587134000285, -53.86589942198000358, -12.65963207085999898 ) ) ;
#3577=CARTESIAN_POINT ( 'NONE',  ( 9.282381572011505710, -76.00223643008524732, 7.204816828411842344 ) ) ;
#3580=CARTESIAN_POINT ( 'NONE',  ( 13.99999999996999911, -5.900000000026970781, -3.874887541704999824E-10 ) ) ;
#3586=CARTESIAN_POINT ( 'NONE',  ( -0.5135400119346991143, -16.82131466139585640, 12.70453250098583986 ) ) ;
#3588=DIRECTION ( 'NONE',  ( -0.7071067811865475727, 0.000000000000000000, 0.7071067811865475727 ) ) ;
#3595=CARTESIAN_POINT ( 'NONE',  ( -11.75000000000000000, -77.79999999999999716, 1.702919296826999607E-14 ) ) ;
#3597=CARTESIAN_POINT ( 'NONE',  ( 12.76303204525000012, -60.06485147653999945, 1.980584515753000208 ) ) ;
#3599=B_SPLINE_SURFACE_WITH_KNOTS ( 'NONE', 3, 3, ( 
 ( #35579, #34708, #27317, #31736 ),
 ( #14032, #45349, #55064, #9326 ),
 ( #54495, #10492, #9616, #41781 ),
 ( #4899, #5470, #50944, #32030 ),
 ( #22606, #32312, #37343, #36184 ),
 ( #22897, #19349, #55359, #40910 ),
 ( #4608, #1354, #50655, #46233 ),
 ( #9910, #214, #45646, #14902 ) ),
 .UNSPECIFIED., .F., .F., .F.,
 ( 4, 1, 1, 1, 1, 4 ),
 ( 4, 4 ),
 ( -0.01200407345746999990, 0.000000000000000000, 0.3333333333333000081, 0.6666666666667000474, 1.000000000000000000, 1.011997855551999947 ),
 ( -0.3559705542741999906, 1.355970554273999928 ),
 .UNSPECIFIED. ) ;
#3601=CARTESIAN_POINT ( 'NONE',  ( -12.50000000000000000, -60.04999999966999980, 0.000000000000000000 ) ) ;
#3602=CARTESIAN_POINT ( 'NONE',  ( -12.70556836352000118, -62.02772277195000328, -2.424224025342999716E-09 ) ) ;
#3603=CARTESIAN_POINT ( 'NONE',  ( 10.26699006316251683, -76.09166666666665435, 5.917523019358090330 ) ) ;
#3604=ORIENTED_EDGE ( 'NONE', *, *, #54172, .F. ) ;
#3605=ORIENTED_EDGE ( 'NONE', *, *, #6294, .F. ) ;
#3624=CIRCLE ( 'NONE', #44175, 0.6000000000000008660 ) ;
#3627=B_SPLINE_CURVE_WITH_KNOTS ( 'NONE', 3,
 ( #43968, #12938, #30936, #57822, #39808, #8231, #48124, #21805, #26511, #11809 ),
 .UNSPECIFIED., .F., .F.,
 ( 4, 2, 2, 2, 4 ),
 ( 0.000000000000000000, 0.2500000000000000000, 0.5000000000000000000, 0.7500000000000000000, 1.000000000000000000 ),
 .UNSPECIFIED. ) ;
#3629=CARTESIAN_POINT ( 'NONE',  ( 12.43421868118999818, -17.56340276631999942, -1.197355605037999871 ) ) ;
#3630=EDGE_CURVE ( 'NONE', #43983, #23504, #20253, .T. ) ;
#3631=FACE_OUTER_BOUND ( 'NONE', #54569, .T. ) ;
#3634=EDGE_CURVE ( 'NONE', #55158, #3325, #7092, .T. ) ;
#3638=CARTESIAN_POINT ( 'NONE',  ( -8.227509542990000924, -17.17460508872999725, -9.516261809269000338 ) ) ;
#3639=CARTESIAN_POINT ( 'NONE',  ( 7.627487525433000570, -60.09778754156999980, 10.35845608626999947 ) ) ;
#3640=CARTESIAN_POINT ( 'NONE',  ( -1.200170490671999879, -17.56594298002000087, -12.43444080551000042 ) ) ;
#3642=CARTESIAN_POINT ( 'NONE',  ( 10.42272502862000039, -58.55453807205000061, -7.691893942725999800 ) ) ;
#3645=CARTESIAN_POINT ( 'NONE',  ( 2.598917237794080570, -1.802083333333333259, 1.997276839918479485 ) ) ;
#3647=ORIENTED_EDGE ( 'NONE', *, *, #40726, .T. ) ;
#3648=LINE ( 'NONE', #58256, #35752 ) ;
#3649=CARTESIAN_POINT ( 'NONE',  ( 1.484804496640999893, -54.08130846584000295, 12.77261165604999960 ) ) ;
#3650=CARTESIAN_POINT ( 'NONE',  ( -12.49306752634999995, -18.71943307332999851, 1.667917367010000040 ) ) ;
#3651=EDGE_CURVE ( 'NONE', #50383, #32447, #39253, .T. ) ;
#3652=CARTESIAN_POINT ( 'NONE',  ( -0.9552977345487000393, -2.613729981583999606, 3.684183631831999595 ) ) ;
#3655=DIRECTION ( 'NONE',  ( 0.000000000000000000, -1.000000000000000000, 0.000000000000000000 ) ) ;
#3656=CARTESIAN_POINT ( 'NONE',  ( 0.000000000000000000, -3.749999999256000027, 0.000000000000000000 ) ) ;
#3657=CARTESIAN_POINT ( 'NONE',  ( -1.933504092458000034, -60.20406847242999504, 12.70940235709999833 ) ) ;
#3658=DIRECTION ( 'NONE',  ( 1.000000000000000000, 0.000000000000000000, 0.000000000000000000 ) ) ;
#3661=DIRECTION ( 'NONE',  ( 0.000000000000000000, 0.000000000000000000, -1.000000000000000000 ) ) ;
#3662=CARTESIAN_POINT ( 'NONE',  ( -1.206665456719130836, -77.07001001640816185, -11.96363559127014398 ) ) ;
#3668=CARTESIAN_POINT ( 'NONE',  ( 10.12290050255000118, -55.55000002206000431, 7.648026768392999664 ) ) ;
#3670=CARTESIAN_POINT ( 'NONE',  ( 2.598917237794088564, -2.697916666666666519, -1.997276839918468605 ) ) ;
#3673=CARTESIAN_POINT ( 'NONE',  ( -9.355955347629251406, -16.82516908807116351, -8.610895743724782392 ) ) ;
#3677=CARTESIAN_POINT ( 'NONE',  ( -10.98362417419999915, -23.15000000000000213, -0.5999999999999999778 ) ) ;
#3679=DIRECTION ( 'NONE',  ( 0.000000000000000000, 0.000000000000000000, 1.000000000000000000 ) ) ;
#3681=DIRECTION ( 'NONE',  ( -1.000000000000000000, 0.000000000000000000, 0.000000000000000000 ) ) ;
#3683=EDGE_CURVE ( 'NONE', #48012, #44548, #2386, .T. ) ;
#3690=CARTESIAN_POINT ( 'NONE',  ( -10.34744176347000000, -78.37400547832000086, 6.482158579691000178 ) ) ;
#3692=ORIENTED_EDGE ( 'NONE', *, *, #12384, .F. ) ;
#3694=DIRECTION ( 'NONE',  ( 1.000000000000000000, 0.000000000000000000, 0.000000000000000000 ) ) ;
#3697=DIRECTION ( 'NONE',  ( 0.7026410690473250398, 0.1122098755728047209, 0.7026410690473250398 ) ) ;
#3698=VECTOR ( 'NONE', #44379, 1000.000000000000000 ) ;
#3701=CARTESIAN_POINT ( 'NONE',  ( -9.359366689070000689, -77.56737393437001060, -9.185202947203000790 ) ) ;
#3702=CARTESIAN_POINT ( 'NONE',  ( 11.52003294054999927, -77.52814994903998524, 5.205193576094000463 ) ) ;
#3707=CARTESIAN_POINT ( 'NONE',  ( -10.35747158360999975, -55.48415522678000400, 7.626500902197000720 ) ) ;
#3708=CARTESIAN_POINT ( 'NONE',  ( -0.3986185775606674309, -2.985056446498978833, 3.227758659026054300 ) ) ;
#3711=CARTESIAN_POINT ( 'NONE',  ( -0.9356112518355850227, -24.74107830238661876, -12.50329130247234133 ) ) ;
#3713=CARTESIAN_POINT ( 'NONE',  ( 2.113064247614999669, -3.454503108079999940, -3.165785623842000351 ) ) ;
#3716=CARTESIAN_POINT ( 'NONE',  ( -8.643979526187999696, -62.05953772878000052, -9.422807787405000468 ) ) ;
#3718=EDGE_CURVE ( 'NONE', #24905, #21333, #5308, .T. ) ;
#3720=CARTESIAN_POINT ( 'NONE',  ( -12.54983130239999944, -16.94901607458999848, -0.1356732392833999989 ) ) ;
#3721=EDGE_CURVE ( 'NONE', #3462, #50691, #23060, .T. ) ;
#3722=CARTESIAN_POINT ( 'NONE',  ( -10.59876350475000173, -77.50274337785998569, 7.550195564144000393 ) ) ;
#3723=DIRECTION ( 'NONE',  ( 0.9999999999999694689, -2.469236814435925861E-07, -1.232399280382962518E-12 ) ) ;
#3724=CARTESIAN_POINT ( 'NONE',  ( 1.318114156690387784, -24.73572477191089902, -12.70261578162881655 ) ) ;
#3725=CARTESIAN_POINT ( 'NONE',  ( 0.7846939639768999442, -76.45140497417000347, 12.33726696821999802 ) ) ;
#3728=CARTESIAN_POINT ( 'NONE',  ( 8.485281374238999419, -18.75000000000000000, 8.485281374238999419 ) ) ;
#3729=CARTESIAN_POINT ( 'NONE',  ( -10.98964036629029195, -18.48475764895765039, -0.4777763868216057808 ) ) ;
#3738=EDGE_CURVE ( 'NONE', #21348, #27676, #1532, .T. ) ;
#3740=ORIENTED_EDGE ( 'NONE', *, *, #55612, .T. ) ;
#3743=CARTESIAN_POINT ( 'NONE',  ( -7.997114030203776203, -55.11418618783218903, -7.553727747530986747 ) ) ;
#3746=CIRCLE ( 'NONE', #19776, 0.5000000000000006661 ) ;
#3749=EDGE_CURVE ( 'NONE', #52954, #37470, #40635, .T. ) ;
#3750=AXIS2_PLACEMENT_3D ( 'NONE', #2464, #29587, #47929 ) ;
#3754=ORIENTED_EDGE ( 'NONE', *, *, #55399, .F. ) ;
#3755=CARTESIAN_POINT ( 'NONE',  ( 10.98362417419999915, -18.84999999999999787, 0.5999999999999999778 ) ) ;
#3759=CARTESIAN_POINT ( 'NONE',  ( 7.986982684638000762, -54.07364722701999682, 10.07612755991999975 ) ) ;
#3760=CARTESIAN_POINT ( 'NONE',  ( -0.5392637480170889841, -18.58467666638265925, 10.98678411023718482 ) ) ;
#3763=CARTESIAN_POINT ( 'NONE',  ( 7.718368845781999887, -58.54800977479000323, -10.07722254367000048 ) ) ;
#3765=VECTOR ( 'NONE', #24119, 1000.000000000000000 ) ;
#3770=CARTESIAN_POINT ( 'NONE',  ( 10.48774103546000092, -20.24527981753999839, -7.686941364807000632 ) ) ;
#3777=CARTESIAN_POINT ( 'NONE',  ( 7.714303428875997959, -15.69705297113999443, -12.53545825868000385 ) ) ;
#3780=CIRCLE ( 'NONE', #19821, 0.5000000000000006661 ) ;
#3782=CARTESIAN_POINT ( 'NONE',  ( -1.513302041219688123E-14, -80.75000000002938805, 13.94999999997000018 ) ) ;
#3783=VECTOR ( 'NONE', #20875, 1000.000000000000000 ) ;
#3785=CARTESIAN_POINT ( 'NONE',  ( 0.000000000000000000, -65.72928575305999743, 0.000000000000000000 ) ) ;
#3789=ORIENTED_EDGE ( 'NONE', *, *, #43267, .T. ) ;
#3793=DIRECTION ( 'NONE',  ( -0.7071067811865475727, 0.000000000000000000, -0.7071067811865475727 ) ) ;
#3795=CARTESIAN_POINT ( 'NONE',  ( -2.173628335086999819, -1.116741823149000057, -2.792292937636999817 ) ) ;
#3797=DIRECTION ( 'NONE',  ( -1.000000000000000000, 0.000000000000000000, 0.000000000000000000 ) ) ;
#3798=CARTESIAN_POINT ( 'NONE',  ( -1.799490225533999732, -59.57152778012000027, 12.64500484464999808 ) ) ;
#3803=CARTESIAN_POINT ( 'NONE',  ( -12.50679926050217006, -17.69581646372544981, 1.424414840279750072 ) ) ;
#3804=CARTESIAN_POINT ( 'NONE',  ( -10.53003223722000037, -55.47547470607999998, -7.612971414697999428 ) ) ;
#3805=EDGE_CURVE ( 'NONE', #41659, #29156, #12575, .T. ) ;
#3807=ORIENTED_EDGE ( 'NONE', *, *, #12414, .T. ) ;
#3813=EDGE_LOOP ( 'NONE', ( #29288, #38677, #38533, #27172 ) ) ;
#3814=CARTESIAN_POINT ( 'NONE',  ( -12.69619287811999797, -58.55083378327000077, 1.799475295154000065 ) ) ;
#3815=CARTESIAN_POINT ( 'NONE',  ( -9.395773752806999113, -54.09509747810999869, -8.188237371196001035 ) ) ;
#3818=EDGE_LOOP ( 'NONE', ( #44014, #30984, #21174, #55691, #31758 ) ) ;
#3822=VECTOR ( 'NONE', #39882, 1000.000000000000000 ) ;
#3825=AXIS2_PLACEMENT_3D ( 'NONE', #22605, #40616, #213 ) ;
#3827=DIRECTION ( 'NONE',  ( 0.000000000000000000, -1.000000000000000000, 0.000000000000000000 ) ) ;
#3828=CARTESIAN_POINT ( 'NONE',  ( -9.650487694675000228, -78.53128649030999497, 7.043610823269999877 ) ) ;
#3830=CARTESIAN_POINT ( 'NONE',  ( 13.13047446164998711, -19.21421830981000767, -0.8260994316375004365 ) ) ;
#3833=ADVANCED_FACE ( 'NONE', ( #6991 ), #43303, .F. ) ;
#3834=B_SPLINE_CURVE_WITH_KNOTS ( 'NONE', 3,
 ( #38076, #37785, #55211, #14757, #32755, #55509, #51096, #6198, #50802, #10347, #33350, #7075, #8223, #17083, #7647, #34787, #35358, #35065 ),
 .UNSPECIFIED., .F., .F.,
 ( 4, 2, 2, 2, 2, 2, 2, 2, 4 ),
 ( 0.000000000000000000, 0.1249999999999999722, 0.2499999999999999445, 0.3749999999999998890, 0.4999999999999998890, 0.6249999999999998890, 0.7499999999999997780, 0.8749999999999998890, 1.000000000000000000 ),
 .UNSPECIFIED. ) ;
#3836=CARTESIAN_POINT ( 'NONE',  ( 9.697390092220967261, -17.02767731352027525, 8.266602378556456188 ) ) ;
#3839=CARTESIAN_POINT ( 'NONE',  ( 12.02702378446000075, -75.75855317818999879, -1.341316611471999876 ) ) ;
#3842=CARTESIAN_POINT ( 'NONE',  ( -1.820508558488653783, -3.431062509705810726, -3.014547121651218298 ) ) ;
#3843=CARTESIAN_POINT ( 'NONE',  ( -9.073547343531414455, -16.77191135192954619, 8.894853367293087842 ) ) ;
#3851=ORIENTED_EDGE ( 'NONE', *, *, #7318, .T. ) ;
#3854=DIRECTION ( 'NONE',  ( 1.205798306211979422E-11, 1.868136817095964273E-07, -0.9999999999999824585 ) ) ;
#3862=CARTESIAN_POINT ( 'NONE',  ( -1.056237665594999875, -53.75133986268999564, -12.77256098193999989 ) ) ;
#3863=CARTESIAN_POINT ( 'NONE',  ( 11.52879444111039753, -75.96520208080863767, 2.268419725861221981 ) ) ;
#3865=ORIENTED_EDGE ( 'NONE', *, *, #30390, .T. ) ;
#3868=CARTESIAN_POINT ( 'NONE',  ( -2.750680930259973511, -78.80596977890112953, -11.46145582561345044 ) ) ;
#3872=CARTESIAN_POINT ( 'NONE',  ( -1.980584515756000030, -18.73514849905999924, 12.76303204340999997 ) ) ;
#3884=CARTESIAN_POINT ( 'NONE',  ( 9.502921960400678714, -17.25907999996281816, -8.179400289337134922 ) ) ;
#3887=CARTESIAN_POINT ( 'NONE',  ( -12.54976804508999955, -25.04775476228000031, -0.05637402076006000490 ) ) ;
#3891=VERTEX_POINT ( 'NONE', #7282 ) ;
#3892=CARTESIAN_POINT ( 'NONE',  ( 6.688645397968000950, -78.88109438844000465, 10.27915892414000076 ) ) ;
#3893=ORIENTED_EDGE ( 'NONE', *, *, #57288, .F. ) ;
#3894=CARTESIAN_POINT ( 'NONE',  ( 7.618386461942000309, -23.22712559346000205, 10.53495196323000016 ) ) ;
#3900=ADVANCED_FACE ( 'NONE', ( #38281 ), #30571, .T. ) ;
#3904=TOROIDAL_SURFACE ( 'NONE', #52017, 13.50000000000000000, 0.5000000000000000000 ) ;
#3909=CARTESIAN_POINT ( 'NONE',  ( 6.215989686684999960, -76.16613641031999293, 11.19887415192999924 ) ) ;
#3910=CARTESIAN_POINT ( 'NONE',  ( 2.880779477859606974, -2.210505338566499667, -1.557632211155396185 ) ) ;
#3911=CARTESIAN_POINT ( 'NONE',  ( 7.712209501855907590, -54.73822238195494805, -10.27335463208971866 ) ) ;
#3913=CARTESIAN_POINT ( 'NONE',  ( 12.43652237962999862, -17.07935153061999856, -0.1283967009857999997 ) ) ;
#3914=CARTESIAN_POINT ( 'NONE',  ( -9.992017125381000398, -24.16084087012999859, -7.762968460669999793 ) ) ;
#3918=CARTESIAN_POINT ( 'NONE',  ( -8.252512830309999714, -53.86594982524999864, 9.650910120403001002 ) ) ;
#3921=CARTESIAN_POINT ( 'NONE',  ( -12.70455691847952906, -61.36014620562671951, 1.489817752284223085 ) ) ;
#3922=CARTESIAN_POINT ( 'NONE',  ( 7.654537165450999936, -55.51943464808999806, 10.01332852686999964 ) ) ;
#3923=CARTESIAN_POINT ( 'NONE',  ( -1.484804496640999893, -17.28130846616999605, -12.77261165608999960 ) ) ;
#3924=CARTESIAN_POINT ( 'NONE',  ( -1.247385798842000071, -54.32277743483000165, 12.50301438874000048 ) ) ;
#3926=FACE_OUTER_BOUND ( 'NONE', #11696, .T. ) ;
#3931=CARTESIAN_POINT ( 'NONE',  ( 13.49939038839240979, -46.09579702914000165, 0.1282931867975413143 ) ) ;
#3932=DIRECTION ( 'NONE',  ( 0.000000000000000000, 0.000000000000000000, -1.000000000000000000 ) ) ;
#3933=CARTESIAN_POINT ( 'NONE',  ( 7.686941364959000822, -21.75472017805000036, -10.48774103561000182 ) ) ;
#3934=CARTESIAN_POINT ( 'NONE',  ( 1.455189730649000035, -1.703650774374000143, -3.167229696986999965 ) ) ;
#3939=CARTESIAN_POINT ( 'NONE',  ( -7.958776492183998741, -24.47699850274999989, 9.723157982400998378 ) ) ;
#3940=CARTESIAN_POINT ( 'NONE',  ( 12.54977952618000003, -16.95167110035999869, -0.03756586072996000170 ) ) ;
#3943=CARTESIAN_POINT ( 'NONE',  ( 11.94498200941940347, -77.21677916375155348, 2.095992703329072171 ) ) ;
#3944=B_SPLINE_CURVE_WITH_KNOTS ( 'NONE', 3,
 ( #39115, #57121, #16687, #12252, #26681, #9281, #39976, #57990, #40576, #18437 ),
 .UNSPECIFIED., .F., .F.,
 ( 4, 2, 2, 2, 4 ),
 ( 0.000000000000000000, 0.2500000000000000555, 0.5000000000000003331, 0.7500000000000003331, 1.000000000000000000 ),
 .UNSPECIFIED. ) ;
#3951=CARTESIAN_POINT ( 'NONE',  ( -12.82202361519000000, -60.22627773000999696, 2.066043355638000012 ) ) ;
#3954=CARTESIAN_POINT ( 'NONE',  ( 7.561997864713030815, -75.80000000000001137, 9.323372221969927764 ) ) ;
#3955=VERTEX_POINT ( 'NONE', #22303 ) ;
#3958=DIRECTION ( 'NONE',  ( -1.000000000000000000, 0.000000000000000000, 0.000000000000000000 ) ) ;
#3960=LINE ( 'NONE', #21963, #22410 ) ;
#3965=ORIENTED_EDGE ( 'NONE', *, *, #54374, .T. ) ;
#3967=VERTEX_POINT ( 'NONE', #31441 ) ;
#3968=AXIS2_PLACEMENT_3D ( 'NONE', #18638, #45211, #14481 ) ;
#3974=ORIENTED_EDGE ( 'NONE', *, *, #11053, .T. ) ;
#3975=DIRECTION ( 'NONE',  ( 1.000000000000000000, 0.000000000000000000, 0.000000000000000000 ) ) ;
#3976=CARTESIAN_POINT ( 'NONE',  ( 10.90767474025000006, -79.29456715226000085, 5.809805964757000396 ) ) ;
#3979=ORIENTED_EDGE ( 'NONE', *, *, #12974, .T. ) ;
#3980=CARTESIAN_POINT ( 'NONE',  ( 12.85144117164000122, -58.55472016995999951, -1.980464439859999981 ) ) ;
#3982=B_SPLINE_CURVE_WITH_KNOTS ( 'NONE', 3,
 ( #56228, #51228, #29626, #34052, #6039, #29339 ),
 .UNSPECIFIED., .F., .F.,
 ( 4, 1, 1, 4 ),
 ( 0.000000000000000000, 0.3333333311588953518, 0.6666666623178907347, 0.9999999934767860310 ),
 .UNSPECIFIED. ) ;
#3987=CARTESIAN_POINT ( 'NONE',  ( 11.98112765039999950, -78.28893426687999124, 5.330601325896000553 ) ) ;
#3988=CARTESIAN_POINT ( 'NONE',  ( -12.59654320151999940, -76.75108497556999509, -1.064070293361000008 ) ) ;
#3992=AXIS2_PLACEMENT_3D ( 'NONE', #18534, #27370, #28237 ) ;
#3993=CARTESIAN_POINT ( 'NONE',  ( -10.53101998745000145, -55.49360374314999689, 7.613962827161000035 ) ) ;
#3994=CARTESIAN_POINT ( 'NONE',  ( -0.7135609970306604488, -2.993047182741839229, 3.178329152650583023 ) ) ;
#3996=FACE_OUTER_BOUND ( 'NONE', #48852, .T. ) ;
#3998=CARTESIAN_POINT ( 'NONE',  ( 1.432628882339999965, -2.403710179781999745, -3.526139092948999743 ) ) ;
#4000=VERTEX_POINT ( 'NONE', #22604 ) ;
#4001=CARTESIAN_POINT ( 'NONE',  ( 0.5392637480170930919, -23.41532333362685847, 10.98678411023718304 ) ) ;
#4005=CARTESIAN_POINT ( 'NONE',  ( 5.647598101448999763, -77.82194253125999239, 11.72364604052000203 ) ) ;
#4006=EDGE_CURVE ( 'NONE', #11264, #30476, #40318, .T. ) ;
#4007=CARTESIAN_POINT ( 'NONE',  ( -10.21026636381520625, -61.05606635916441149, -7.764233071732244085 ) ) ;
#4008=CARTESIAN_POINT ( 'NONE',  ( 10.03847181070773331, -18.20634590497699179, 7.678636148852304721 ) ) ;
#4010=DIRECTION ( 'NONE',  ( 0.000000000000000000, 0.000000000000000000, 1.000000000000000000 ) ) ;
#4016=CARTESIAN_POINT ( 'NONE',  ( -1.799490220168999954, -59.57129148919000272, -12.64502302236999931 ) ) ;
#4024=VERTEX_POINT ( 'NONE', #21720 ) ;
#4026=CARTESIAN_POINT ( 'NONE',  ( 0.000000000000000000, -0.2000000000000000111, 0.000000000000000000 ) ) ;
#4029=EDGE_CURVE ( 'NONE', #22857, #41402, #6281, .T. ) ;
#4031=ORIENTED_EDGE ( 'NONE', *, *, #34935, .T. ) ;
#4032=VERTEX_POINT ( 'NONE', #212 ) ;
#4035=CARTESIAN_POINT ( 'NONE',  ( -1.184050902616055501, -1.449062058922204965, -3.841969317884664559 ) ) ;
#4036=B_SPLINE_SURFACE_WITH_KNOTS ( 'NONE', 3, 3, ( 
 ( #40112, #48696, #58125, #17687 ),
 ( #44848, #8240, #4402, #17988 ),
 ( #45152, #4704, #22701, #57254 ),
 ( #54590, #36857, #51046, #27990 ),
 ( #46039, #15002, #36569, #37441 ),
 ( #879, #27412, #5563, #14129 ),
 ( #50166, #45744, #32999, #19153 ),
 ( #23286, #41296, #27701, #18865 ) ),
 .UNSPECIFIED., .F., .F., .F.,
 ( 4, 1, 1, 1, 1, 4 ),
 ( 4, 4 ),
 ( -0.01200407347462999902, 0.000000000000000000, 0.3333333333333000081, 0.6666666666667000474, 1.000000000000000000, 1.011997855551999947 ),
 ( -0.3559705542741999906, 1.355970554273999928 ),
 .UNSPECIFIED. ) ;
#4038=CARTESIAN_POINT ( 'NONE',  ( 8.838834764832000701, -60.04999999966999980, 8.838834764832000701 ) ) ;
#4043=VECTOR ( 'NONE', #9762, 1000.000000000000000 ) ;
#4045=CARTESIAN_POINT ( 'NONE',  ( -7.642160924884000117, -19.21538333566000034, -10.55911395187000146 ) ) ;
#4046=DIRECTION ( 'NONE',  ( 0.9999999923520045408, 0.000000000000000000, 0.0001236769620553006580 ) ) ;
#4047=AXIS2_PLACEMENT_3D ( 'NONE', #20871, #33573, #34141 ) ;
#4048=CARTESIAN_POINT ( 'NONE',  ( 11.75000000000000355, -76.54297251775334132, -1.037641870170386005 ) ) ;
#4050=DIRECTION ( 'NONE',  ( 0.000000000000000000, 1.000000000000000000, 0.000000000000000000 ) ) ;
#4051=CARTESIAN_POINT ( 'NONE',  ( -9.835223439032999337, -24.08138927656000305, 7.760980897158999525 ) ) ;
#4056=CARTESIAN_POINT ( 'NONE',  ( 12.76303204294999993, -23.26485150694999859, -1.980584515756000030 ) ) ;
#4057=CARTESIAN_POINT ( 'NONE',  ( 1.044910384896000188, -25.05526494194999643, 12.77260826199000121 ) ) ;
#4060=CARTESIAN_POINT ( 'NONE',  ( 2.583538554219000360, -1.367443126209999971, 2.539878903945000044 ) ) ;
#4064=FACE_OUTER_BOUND ( 'NONE', #50399, .T. ) ;
#4065=AXIS2_PLACEMENT_3D ( 'NONE', #53827, #9246, #13362 ) ;
#4066=CARTESIAN_POINT ( 'NONE',  ( -12.51072239526000196, -15.69705297114000331, 0.7871079366006996647 ) ) ;
#4068=EDGE_CURVE ( 'NONE', #26175, #36059, #53606, .T. ) ;
#4070=CYLINDRICAL_SURFACE ( 'NONE', #37281, 1.750000000000001332 ) ;
#4071=DIRECTION ( 'NONE',  ( -0.7071067811865474617, 0.000000000000000000, 0.7071067811865474617 ) ) ;
#4078=CIRCLE ( 'NONE', #22929, 14.00000000000000000 ) ;
#4084=CARTESIAN_POINT ( 'NONE',  ( -10.36222489920000100, -60.02120223818999989, 7.631889817968999346 ) ) ;
#4085=CARTESIAN_POINT ( 'NONE',  ( -12.50000000000000000, -28.92928575306000383, 0.000000000000000000 ) ) ;
#4088=DIRECTION ( 'NONE',  ( 0.000000000000000000, 0.000000000000000000, -1.000000000000000000 ) ) ;
#4089=FACE_OUTER_BOUND ( 'NONE', #55085, .T. ) ;
#4092=CARTESIAN_POINT ( 'NONE',  ( -12.65372179309999900, -57.04935286341999756, 1.750000000000000000 ) ) ;
#4093=CARTESIAN_POINT ( 'NONE',  ( -12.52133763471513639, -18.07246868480434898, 1.618901767043031681 ) ) ;
#4095=CARTESIAN_POINT ( 'NONE',  ( -10.07722254367000048, -58.54800977479000323, -7.718368845781999887 ) ) ;
#4100=CARTESIAN_POINT ( 'NONE',  ( -3.044724405606854756, -77.80247681429408146, -11.37341351363359543 ) ) ;
#4101=CARTESIAN_POINT ( 'NONE',  ( -2.598917237794085455, -1.052083333333333481, -1.997276839918474600 ) ) ;
#4102=VERTEX_POINT ( 'NONE', #22007 ) ;
#4103=ORIENTED_EDGE ( 'NONE', *, *, #33823, .T. ) ;
#4104=CARTESIAN_POINT ( 'NONE',  ( -12.58338334669999981, -58.54800977479000323, 1.667961445601999992 ) ) ;
#4105=CARTESIAN_POINT ( 'NONE',  ( -7.636247231009999581, -55.03676232846999739, -10.30460520059999929 ) ) ;
#4110=EDGE_CURVE ( 'NONE', #37084, #11057, #57183, .T. ) ;
#4113=EDGE_CURVE ( 'NONE', #46129, #20252, #495, .T. ) ;
#4114=ORIENTED_EDGE ( 'NONE', *, *, #9647, .F. ) ;
#4118=CARTESIAN_POINT ( 'NONE',  ( 11.88773275212999891, -76.77906641171999524, 5.537155082298999886 ) ) ;
#4122=CIRCLE ( 'NONE', #44680, 1.250000000000000000 ) ;
#4126=VERTEX_POINT ( 'NONE', #9031 ) ;
#4129=CARTESIAN_POINT ( 'NONE',  ( -6.282410744257000523, -75.93495447697000600, 10.58616248715999930 ) ) ;
#4134=CARTESIAN_POINT ( 'NONE',  ( -2.913600672515707757, -2.800140272586570500, 2.082966609014084813 ) ) ;
#4136=CARTESIAN_POINT ( 'NONE',  ( 12.50385602700769994, -54.01562691795769666, -0.8579623876370696678 ) ) ;
#4141=CARTESIAN_POINT ( 'NONE',  ( 10.21381326473999884, -19.22870851082999977, -7.668949790020999302 ) ) ;
#4144=DIRECTION ( 'NONE',  ( -1.000000000000000000, 0.000000000000000000, 0.000000000000000000 ) ) ;
#4145=ORIENTED_EDGE ( 'NONE', *, *, #53630, .T. ) ;
#4148=DIRECTION ( 'NONE',  ( 0.000000000000000000, 0.000000000000000000, -1.000000000000000000 ) ) ;
#4155=CARTESIAN_POINT ( 'NONE',  ( -9.689272046653734094, -24.97888144173617775, -8.274769670417640555 ) ) ;
#4156=CARTESIAN_POINT ( 'NONE',  ( -10.07627163191000008, -18.75000000310999937, -7.601397897754999633 ) ) ;
#4159=ADVANCED_FACE ( 'NONE', ( #10788 ), #27888, .T. ) ;
#4161=CARTESIAN_POINT ( 'NONE',  ( -1.638273008393710262, -2.184753700216213179, -2.842570767342633697 ) ) ;
#4162=CARTESIAN_POINT ( 'NONE',  ( -11.30034656532730430, -78.72488567633864420, -3.687091655504522336 ) ) ;
#4163=AXIS2_PLACEMENT_3D ( 'NONE', #10976, #52562, #47288 ) ;
#4168=CARTESIAN_POINT ( 'NONE',  ( -1.495357591770747341, -17.44123662637707994, 12.70444646759436047 ) ) ;
#4170=CARTESIAN_POINT ( 'NONE',  ( 3.916804611567557437, -78.54668480355715587, 11.07851578385000302 ) ) ;
#4171=CYLINDRICAL_SURFACE ( 'NONE', #18263, 1.750000000000001332 ) ;
#4172=ORIENTED_EDGE ( 'NONE', *, *, #30759, .T. ) ;
#4173=AXIS2_PLACEMENT_3D ( 'NONE', #54775, #9614, #45644 ) ;
#4176=CARTESIAN_POINT ( 'NONE',  ( -13.99936781018472232, -46.09579702914000165, -0.1330447863085613691 ) ) ;
#4180=DIRECTION ( 'NONE',  ( 0.4045849533085069116, -0.8201353736504155556, -0.4045849533085069116 ) ) ;
#4183=VERTEX_POINT ( 'NONE', #19347 ) ;
#4184=CARTESIAN_POINT ( 'NONE',  ( 8.385806979700950237, -17.11189753004608605, -9.298530586708613654 ) ) ;
#4185=DIRECTION ( 'NONE',  ( 1.000000000000000000, 0.000000000000000000, 0.000000000000000000 ) ) ;
#4187=DIRECTION ( 'NONE',  ( 0.9999433559010179051, 0.000000000000000000, 0.01064354214585019887 ) ) ;
#4189=ORIENTED_EDGE ( 'NONE', *, *, #57105, .F. ) ;
#4193=CARTESIAN_POINT ( 'NONE',  ( 0.000000000000000000, -2.660000000000000142, 0.000000000000000000 ) ) ;
#4194=EDGE_LOOP ( 'NONE', ( #3504, #51425, #48433, #50870 ) ) ;
#4197=LINE ( 'NONE', #20828, #56099 ) ;
#4199=CARTESIAN_POINT ( 'NONE',  ( -12.50483465194470689, -24.86452578687041637, -0.6958747604665329600 ) ) ;
#4203=EDGE_LOOP ( 'NONE', ( #19819, #10461, #32782, #18036, #32710 ) ) ;
#4206=DIRECTION ( 'NONE',  ( 1.000000000000000000, 0.000000000000000000, 0.000000000000000000 ) ) ;
#4209=CARTESIAN_POINT ( 'NONE',  ( 3.541185312415000119, -75.59580845059001319, 11.43528872558000131 ) ) ;
#4210=ADVANCED_FACE ( 'NONE', ( #46525 ), #37342, .F. ) ;
#4214=CARTESIAN_POINT ( 'NONE',  ( 12.54981748964999966, -16.95163512371999914, 0.03767836620435999206 ) ) ;
#4215=CIRCLE ( 'NONE', #44759, 1.749999999999998002 ) ;
#4216=LINE ( 'NONE', #36089, #13049 ) ;
#4221=CARTESIAN_POINT ( 'NONE',  ( -9.788022091682998749, -17.47120090402999892, -7.956349397064001572 ) ) ;
#4222=CARTESIAN_POINT ( 'NONE',  ( 11.75000000000000178, -78.53958333333331154, -1.538071403319980268 ) ) ;
#4223=FACE_OUTER_BOUND ( 'NONE', #40712, .T. ) ;
#4224=CARTESIAN_POINT ( 'NONE',  ( -10.07627163191000008, -55.55000000278000272, -7.601397897754999633 ) ) ;
#4227=DIRECTION ( 'NONE',  ( 0.000000000000000000, -1.000000000000000000, 0.000000000000000000 ) ) ;
#4229=CARTESIAN_POINT ( 'NONE',  ( -0.4254240051736287720, -1.885416666666666519, 3.249999999999998224 ) ) ;
#4232=CARTESIAN_POINT ( 'NONE',  ( -0.8525066185231022775, -1.497527708407747626, 3.168802892732555776 ) ) ;
#4234=CARTESIAN_POINT ( 'NONE',  ( -0.4356486348728999536, -53.91935044157000334, 12.43591427117000059 ) ) ;
#4235=CARTESIAN_POINT ( 'NONE',  ( 8.838834764832000701, -18.75000000000000000, 8.838834764832000701 ) ) ;
#4236=CARTESIAN_POINT ( 'NONE',  ( 1.220124496691999960, -2.455504995393999579, -3.773911729633000256 ) ) ;
#4239=CARTESIAN_POINT ( 'NONE',  ( -0.006333666751042999442, -62.13262644267000212, 12.77652491961000081 ) ) ;
#4240=CARTESIAN_POINT ( 'NONE',  ( 12.77651065923999951, -16.69103388611000227, -0.04307580168118999714 ) ) ;
#4243=CARTESIAN_POINT ( 'NONE',  ( -12.99999999992999911, -5.999999999934908956, -2.526613301470000081E-09 ) ) ;
#4244=EDGE_CURVE ( 'NONE', #9459, #3462, #18783, .T. ) ;
#4245=FACE_OUTER_BOUND ( 'NONE', #56485, .T. ) ;
#4246=CARTESIAN_POINT ( 'NONE',  ( -3.644841321323999850, -78.56852404215999286, 11.22553106161999992 ) ) ;
#4248=AXIS2_PLACEMENT_3D ( 'NONE', #49786, #4010, #31448 ) ;
#4252=CARTESIAN_POINT ( 'NONE',  ( 1.308715794682547395, -61.54404499166074061, 12.70256747360829408 ) ) ;
#4254=DIRECTION ( 'NONE',  ( -0.7071067811865475727, 0.000000000000000000, 0.7071067811865475727 ) ) ;
#4262=CARTESIAN_POINT ( 'NONE',  ( 7.342331066867000544, -55.64999999967000122, 8.190859204290999784 ) ) ;
#4266=EDGE_CURVE ( 'NONE', #48292, #52197, #13602, .T. ) ;
#4267=VERTEX_POINT ( 'NONE', #36756 ) ;
#4268=DIRECTION ( 'NONE',  ( 0.000000000000000000, 0.000000000000000000, -1.000000000000000000 ) ) ;
#4269=ORIENTED_EDGE ( 'NONE', *, *, #56979, .T. ) ;
#4270=DIRECTION ( 'NONE',  ( 0.000000000000000000, 0.000000000000000000, 1.000000000000000000 ) ) ;
#4273=CARTESIAN_POINT ( 'NONE',  ( 1.890224871707000043, -23.74789248015000354, -12.68696160873999901 ) ) ;
#4276=EDGE_LOOP ( 'NONE', ( #39331, #12187, #50106, #11266 ) ) ;
#4278=CARTESIAN_POINT ( 'NONE',  ( -5.507598458736999270, -79.00630127599001185, -10.89743148201000089 ) ) ;
#4280=ORIENTED_EDGE ( 'NONE', *, *, #19550, .F. ) ;
#4286=DIRECTION ( 'NONE',  ( -0.9903465037221068634, -0.1386138613754009652, 0.000000000000000000 ) ) ;
#4292=CARTESIAN_POINT ( 'NONE',  ( -12.76303204517000012, -18.73514852243999940, 1.980584515753000208 ) ) ;
#4293=CARTESIAN_POINT ( 'NONE',  ( 1.998746230246073452, -76.83803665960124363, -11.64838672263795338 ) ) ;
#4297=CARTESIAN_POINT ( 'NONE',  ( 3.383845406481000406, -2.460161638760999914, -1.742318191517000070 ) ) ;
#4299=ORIENTED_EDGE ( 'NONE', *, *, #54449, .F. ) ;
#4300=CARTESIAN_POINT ( 'NONE',  ( 0.000000000000000000, 4.040000000000000036, 0.000000000000000000 ) ) ;
#4301=ADVANCED_FACE ( 'NONE', ( #14316 ), #50359, .F. ) ;
#4306=CARTESIAN_POINT ( 'NONE',  ( 12.51033564907000084, -78.21047501799000656, -3.582046052171000028 ) ) ;
#4307=CARTESIAN_POINT ( 'NONE',  ( -7.712213536754459753, -60.86179137581871146, -10.27334987168057090 ) ) ;
#4308=CARTESIAN_POINT ( 'NONE',  ( 12.80900240953000058, -21.75365779208000205, -1.930989144707000005 ) ) ;
#4311=EDGE_CURVE ( 'NONE', #469, #55491, #13171, .T. ) ;
#4313=CARTESIAN_POINT ( 'NONE',  ( 7.626500777237000150, -18.68415268018999953, -10.35747145892000098 ) ) ;
#4316=CARTESIAN_POINT ( 'NONE',  ( -3.616527695712999702, -1.863176978014000174, -0.5438149879621999583 ) ) ;
#4317=CARTESIAN_POINT ( 'NONE',  ( -2.062597299672999540, -56.01514526721999943, -12.87022657272000004 ) ) ;
#4320=ORIENTED_EDGE ( 'NONE', *, *, #20420, .F. ) ;
#4326=FACE_OUTER_BOUND ( 'NONE', #27734, .T. ) ;
#4328=CARTESIAN_POINT ( 'NONE',  ( 12.50000000000000000, -18.75000000000000000, 1.250000000000000000 ) ) ;
#4332=EDGE_LOOP ( 'NONE', ( #25034, #22262, #43485, #12254 ) ) ;
#4334=ORIENTED_EDGE ( 'NONE', *, *, #851, .T. ) ;
#4335=CARTESIAN_POINT ( 'NONE',  ( 7.398464061244442114, -60.25160423312497215, 8.140250184783569765 ) ) ;
#4336=B_SPLINE_SURFACE_WITH_KNOTS ( 'NONE', 3, 3, ( 
 ( #16440, #25862, #12010, #21146, #39155, #25574, #30575, #12292, #43307, #8154, #57737, #30283, #7863, #44173, #26153, #3722, #39729, #17296, #16728, #34128, #35284, #43891, #11439, #56592, #29989, #16151, #29419, #6997, #48043, #47472, #25000, #43020, #7285, #7576, #2577 ),
 ( #11727, #25287, #34709, #43594, #2864, #20860, #38862, #40619, #41196, #40911, #58033, #501, #22898, #36186, #13148, #215, #785, #22607, #18191, #4609, #31444, #4900, #32031, #23191, #45647, #54203, #12857, #17894, #13738, #31142, #53314, #31737, #50074, #49781, #17593 ),
 ( #53913, #9327, #45057, #13445, #18478, #9617, #27318, #45350, #27605, #36469, #35580, #8437, #18765, #54496, #30858, #14034, #5187, #48896, #35884, #26433, #49182, #44454, #4005, #22010, #40018, #53609, #8733, #26726, #44754, #4306, #49485, #27021, #22306, #40321, #58330 ),
 ( #9034, #19061, #50361, #2227, #46528, #24650, #37636, #47111, #42078, #19937, #6641, #32313, #11088, #41486, #42660, #29067, #36758, #28478, #37048, #1648, #14903, #32901, #10791, #27892, #23767, #45939, #5471, #50945, #55950, #10493, #6346, #54777, #55360, #6052, #55065 ) ),
 .UNSPECIFIED., .F., .F., .F.,
 ( 4, 4 ),
 ( 4, 1, 1, 1, 1, 1, 1, 1, 1, 1, 1, 1, 1, 1, 1, 1, 1, 1, 1, 1, 1, 1, 1, 1, 1, 1, 1, 1, 1, 1, 1, 1, 4 ),
 ( -0.02000000000002000178, 1.020000000000000018 ),
 ( -0.02000000000000000042, 0.01250000000000000069, 0.04499999999999999833, 0.07749999999999999944, 0.1100000000000000006, 0.1424999999999999878, 0.1749999999999999889, 0.2074999999999999900, 0.2399999999999999911, 0.2725000000000000200, 0.3049999999999999933, 0.3375000000000000222, 0.3699999999999999956, 0.4025000000000000244, 0.4349999999999999978, 0.4675000000000000266, 0.5000000000000000000, 0.5324999999999999734, 0.5649999999999999467, 0.5975000000000000311, 0.6300000000000000044, 0.6624999999999999778, 0.6949999999999999512, 0.7275000000000000355, 0.7600000000000000089, 0.7924999999999999822, 0.8249999999999999556, 0.8575000000000000400, 0.8900000000000000133, 0.9224999999999999867, 0.9549999999999999600, 0.9875000000000000444, 1.020000000000000018 ),
 .UNSPECIFIED. ) ;
#4337=DIRECTION ( 'NONE',  ( -1.000000000000000000, 0.000000000000000000, 0.000000000000000000 ) ) ;
#4341=ORIENTED_EDGE ( 'NONE', *, *, #21619, .T. ) ;
#4344=EDGE_CURVE ( 'NONE', #18184, #30606, #22055, .T. ) ;
#4345=CARTESIAN_POINT ( 'NONE',  ( 10.36222501928999939, -55.57880030132999849, 7.631889976297999922 ) ) ;
#4346=CARTESIAN_POINT ( 'NONE',  ( -7.627487525415999947, -23.29778754190000001, -10.35845608625999859 ) ) ;
#4348=DIRECTION ( 'NONE',  ( 0.000000000000000000, 0.000000000000000000, -1.000000000000000000 ) ) ;
#4349=CARTESIAN_POINT ( 'NONE',  ( 7.705119999435999567, -57.04828923575999511, -10.24996238029999951 ) ) ;
#4350=CARTESIAN_POINT ( 'NONE',  ( -10.12290050124000018, -23.24999999991999644, -7.648026767085999822 ) ) ;
#4351=CARTESIAN_POINT ( 'NONE',  ( -10.18127202938000053, -23.38645218951999993, 7.633406483298000644 ) ) ;
#4352=CARTESIAN_POINT ( 'NONE',  ( 10.42531124903999995, -55.53514851492000304, -7.624341765436000173 ) ) ;
#4357=CARTESIAN_POINT ( 'NONE',  ( -12.66316398248999953, -16.82133896655000171, -0.04044089952540000366 ) ) ;
#4358=CARTESIAN_POINT ( 'NONE',  ( 7.919595949288999570, -59.94999999969000015, 8.768124086712999699 ) ) ;
#4363=CARTESIAN_POINT ( 'NONE',  ( 2.370180320845999944, -1.873872700496999943, 2.739986503352000113 ) ) ;
#4367=ADVANCED_FACE ( 'NONE', ( #25794 ), #41891, .T. ) ;
#4368=CARTESIAN_POINT ( 'NONE',  ( 12.79895559718999998, -60.60469146232000526, -2.015913954445999856 ) ) ;
#4369=CYLINDRICAL_SURFACE ( 'NONE', #57062, 0.5999999999999999778 ) ;
#4372=AXIS2_PLACEMENT_3D ( 'NONE', #14606, #28175, #46228 ) ;
#4375=FACE_OUTER_BOUND ( 'NONE', #24167, .T. ) ;
#4383=EDGE_CURVE ( 'NONE', #56919, #35878, #42731, .T. ) ;
#4384=AXIS2_PLACEMENT_3D ( 'NONE', #30778, #12780, #49696 ) ;
#4388=CARTESIAN_POINT ( 'NONE',  ( -9.835223439052001027, -60.88138927622999574, 7.760980897183999971 ) ) ;
#4390=CARTESIAN_POINT ( 'NONE',  ( -1.842588707444517082, -76.41257734936500867, -11.67485934150305305 ) ) ;
#4391=CARTESIAN_POINT ( 'NONE',  ( 12.57354097141999993, -23.72384125742000194, -1.757953070309000054 ) ) ;
#4393=ORIENTED_EDGE ( 'NONE', *, *, #48882, .T. ) ;
#4396=CARTESIAN_POINT ( 'NONE',  ( -0.1371744130071849144, -1.722991222295529257, -3.270659802130597704 ) ) ;
#4398=CARTESIAN_POINT ( 'NONE',  ( -12.53241208775000004, -56.03537109808000594, -1.667936697358999965 ) ) ;
#4399=ORIENTED_EDGE ( 'NONE', *, *, #36754, .T. ) ;
#4401=CARTESIAN_POINT ( 'NONE',  ( 5.891586754291419759, -77.86430406625845535, -10.19928502571758244 ) ) ;
#4402=CARTESIAN_POINT ( 'NONE',  ( -1.799501877793999949, -23.28917723430000208, 12.60552511010000032 ) ) ;
#4404=CARTESIAN_POINT ( 'NONE',  ( -7.762982794220000038, -54.63910040255000666, -9.991998894170999179 ) ) ;
#4415=EDGE_CURVE ( 'NONE', #6738, #33527, #3371, .T. ) ;
#4417=CARTESIAN_POINT ( 'NONE',  ( -1.332847799107999887, -78.19825864453000008, -12.88744032790000027 ) ) ;
#4418=VECTOR ( 'NONE', #25494, 999.9999999999998863 ) ;
#4420=CARTESIAN_POINT ( 'NONE',  ( -8.031347306244652984, -78.38283164370827194, 9.096189540893634629 ) ) ;
#4424=VECTOR ( 'NONE', #56506, 1000.000000000000114 ) ;
#4426=ORIENTED_EDGE ( 'NONE', *, *, #39795, .F. ) ;
#4427=LINE ( 'NONE', #5299, #30646 ) ;
#4428=CARTESIAN_POINT ( 'NONE',  ( 10.69843650790000034, -76.34317683517998887, 6.089250768039999429 ) ) ;
#4431=CARTESIAN_POINT ( 'NONE',  ( -3.472969013104772795, -2.868348082004792410, -0.8615918643323726700 ) ) ;
#4433=CARTESIAN_POINT ( 'NONE',  ( -1.750000000000000000, -21.75064714178000003, 12.65372179279999898 ) ) ;
#4434=FACE_OUTER_BOUND ( 'NONE', #31026, .T. ) ;
#4436=CARTESIAN_POINT ( 'NONE',  ( 11.02852943141175857, -76.76673008103259122, -4.905271118666760799 ) ) ;
#4439=ORIENTED_EDGE ( 'NONE', *, *, #23257, .T. ) ;
#4443=DIRECTION ( 'NONE',  ( 0.000000000000000000, -1.000000000000000000, 0.000000000000000000 ) ) ;
#4450=CARTESIAN_POINT ( 'NONE',  ( -0.5506765233279999894, -53.54045707723000191, -12.77514798307000099 ) ) ;
#4451=CARTESIAN_POINT ( 'NONE',  ( 4.974995203995084658, -76.03968481403192925, 10.64665306664898026 ) ) ;
#4453=DIRECTION ( 'NONE',  ( -0.7071067811865475727, 0.000000000000000000, 0.7071067811865475727 ) ) ;
#4456=FACE_OUTER_BOUND ( 'NONE', #1970, .T. ) ;
#4458=ADVANCED_FACE ( 'NONE', ( #11085 ), #23972, .F. ) ;
#4459=CARTESIAN_POINT ( 'NONE',  ( -6.410916551769402005, -76.27903085470401834, -9.847934956580132848 ) ) ;
#4461=EDGE_CURVE ( 'NONE', #3236, #26282, #28686, .T. ) ;
#4464=DIRECTION ( 'NONE',  ( 0.000000000000000000, 1.000000000000000000, 0.000000000000000000 ) ) ;
#4466=ORIENTED_EDGE ( 'NONE', *, *, #36578, .F. ) ;
#4467=CIRCLE ( 'NONE', #3480, 0.5999999999999999778 ) ;
#4470=CARTESIAN_POINT ( 'NONE',  ( 0.000000000000000000, -23.25000000000000000, -12.50000000000000000 ) ) ;
#4471=CARTESIAN_POINT ( 'NONE',  ( -0.01108750193282677897, -76.32470312858129091, -11.74984001957459867 ) ) ;
#4474=CARTESIAN_POINT ( 'NONE',  ( 13.89999999999999858, -6.000000000000000000, 0.000000000000000000 ) ) ;
#4475=CIRCLE ( 'NONE', #52553, 8.800000000000000711 ) ;
#4476=CARTESIAN_POINT ( 'NONE',  ( -10.98768939184211568, -23.45050660130693032, 0.5207199486336721028 ) ) ;
#4478=EDGE_CURVE ( 'NONE', #23873, #31323, #3367, .T. ) ;
#4479=AXIS2_PLACEMENT_3D ( 'NONE', #18060, #36053, #4480 ) ;
#4480=DIRECTION ( 'NONE',  ( -0.7071067811865970887, 0.000000000000000000, 0.7071067811864981678 ) ) ;
#4481=B_SPLINE_CURVE_WITH_KNOTS ( 'NONE', 3,
 ( #52848, #44866, #4420, #57556, #23232, #17117, #827, #55398, #28222, #47154, #42122, #14945, #47444, #51573, #38260, #6093, #50986, #6683, #24692, #10537, #41823, #15833, #5801, #10241, #55107, #2270, #28520, #56283, #6972, #51860, #46860, #24102, #46569, #14652, #1987 ),
 .UNSPECIFIED., .F., .F.,
 ( 4, 1, 1, 1, 1, 1, 1, 1, 1, 1, 1, 1, 1, 1, 1, 1, 1, 1, 1, 1, 1, 1, 1, 1, 1, 1, 1, 1, 1, 1, 1, 1, 4 ),
 ( 0.000000000000000000, 0.01250068083058953131, 0.04500063614458217620, 0.07750059145855550669, 0.1100005467725481551, 0.1425005020865408034, 0.1750004574005334379, 0.2075004127145260724, 0.2400003680285573704, 0.2725003233423954896, 0.3050002786564267598, 0.3375002339704580856, 0.3700001892844893003, 0.4025001445985205706, 0.4350000999123587730, 0.4675000552263899878, 0.5000000105404213135, 0.5324999658544524728, 0.5649999211682906752, 0.5974998764823219455, 0.6299998317963532157, 0.6624997871103845970, 0.6949997424244157562, 0.7274996977382539587, 0.7599996530522852289, 0.7924996083663163882, 0.8249995636803477694, 0.8574995189941858609, 0.8899994743082172421, 0.9224994296222484014, 0.9549993849362796716, 0.9874993402501176520, 1.000000000000000000 ),
 .UNSPECIFIED. ) ;
#4482=CARTESIAN_POINT ( 'NONE',  ( -12.50000000000000000, -54.11762331445000029, -1.005384021965999963 ) ) ;
#4484=CARTESIAN_POINT ( 'NONE',  ( -12.66314513616999982, -25.17864743362000013, -0.04033065750139999683 ) ) ;
#4485=EDGE_LOOP ( 'NONE', ( #3054, #55026, #18370 ) ) ;
#4486=VERTEX_POINT ( 'NONE', #47107 ) ;
#4489=EDGE_LOOP ( 'NONE', ( #53032, #31030, #48854, #29672 ) ) ;
#4492=CARTESIAN_POINT ( 'NONE',  ( 10.07616267220999973, -24.72631139030000114, 7.986947465007999014 ) ) ;
#4493=ADVANCED_FACE ( 'NONE', ( #2223 ), #46977, .F. ) ;
#4494=ADVANCED_FACE ( 'NONE', ( #39659 ), #30787, .F. ) ;
#4500=ORIENTED_EDGE ( 'NONE', *, *, #43545, .T. ) ;
#4505=CARTESIAN_POINT ( 'NONE',  ( 12.08658817094000071, -76.05461784646999490, -4.238831966694000641 ) ) ;
#4507=CARTESIAN_POINT ( 'NONE',  ( 10.41144070831380120, -55.27453159746022493, -7.610433246081189651 ) ) ;
#4509=CARTESIAN_POINT ( 'NONE',  ( 12.54673671099000032, -17.17796527435999820, -0.9173654211231000444 ) ) ;
#4510=CYLINDRICAL_SURFACE ( 'NONE', #28008, 1.750000000000000000 ) ;
#4511=AXIS2_PLACEMENT_3D ( 'NONE', #58207, #22482, #21889 ) ;
#4512=CARTESIAN_POINT ( 'NONE',  ( -11.51097801420635491, -76.68374859038704017, 2.357506540188898825 ) ) ;
#4514=EDGE_LOOP ( 'NONE', ( #8553, #135, #23406, #48612, #13860, #9789 ) ) ;
#4519=CARTESIAN_POINT ( 'NONE',  ( -10.53559655343999957, -18.79430958026000198, 7.620036381602000475 ) ) ;
#4520=CARTESIAN_POINT ( 'NONE',  ( 11.44417895085271475, -78.52916666666665435, -3.075537641221520069 ) ) ;
#4522=AXIS2_PLACEMENT_3D ( 'NONE', #40999, #46032, #1446 ) ;
#4525=CARTESIAN_POINT ( 'NONE',  ( 10.04115011118999945, -59.56486430393999854, -7.682331425190000118 ) ) ;
#4528=CARTESIAN_POINT ( 'NONE',  ( -3.250000000000000000, -2.000000000000000000, 0.000000000000000000 ) ) ;
#4530=ORIENTED_EDGE ( 'NONE', *, *, #49929, .F. ) ;
#4532=CARTESIAN_POINT ( 'NONE',  ( 0.006333666751320000086, -53.46737355666999747, 12.77652491951000080 ) ) ;
#4534=CARTESIAN_POINT ( 'NONE',  ( -3.866967310333000007, -2.823463749271000189, -0.8818601717001000040 ) ) ;
#4536=CARTESIAN_POINT ( 'NONE',  ( 0.8506806241676642122, -1.645833333333333037, -3.165411199172024848 ) ) ;
#4538=CARTESIAN_POINT ( 'NONE',  ( -1.995901252186330854, -2.028574367018873836, 2.598485926919212652 ) ) ;
#4539=FACE_OUTER_BOUND ( 'NONE', #11687, .T. ) ;
#4542=CARTESIAN_POINT ( 'NONE',  ( 11.69170080689889701, -76.72310112267754789, 3.011422183730339874 ) ) ;
#4543=CARTESIAN_POINT ( 'NONE',  ( -1.762986776941000144, -79.36934499803000165, -12.35752141779000013 ) ) ;
#4544=B_SPLINE_SURFACE_WITH_KNOTS ( 'NONE', 3, 3, ( 
 ( #25701, #8275, #12133, #16567 ),
 ( #21846, #43730, #3562, #49019 ),
 ( #12982, #30697, #34837, #20990 ),
 ( #30121, #39853, #21275, #26278 ),
 ( #38995, #44011, #16856, #52867 ),
 ( #12422, #21565, #4141, #57869 ),
 ( #17422, #44292, #57573, #34550 ),
 ( #22139, #39571, #17137, #25985 ) ),
 .UNSPECIFIED., .F., .F., .F.,
 ( 4, 1, 1, 1, 1, 4 ),
 ( 4, 4 ),
 ( -0.01200407347462999902, 0.000000000000000000, 0.3333333333333000081, 0.6666666666667000474, 1.000000000000000000, 1.011997855551999947 ),
 ( -0.3559705542741999906, 1.355970554273999928 ),
 .UNSPECIFIED. ) ;
#4548=CARTESIAN_POINT ( 'NONE',  ( -1.318114156651510216, -61.53572477165713650, 12.70261578166483929 ) ) ;
#4550=CARTESIAN_POINT ( 'NONE',  ( -12.54983138332999815, -61.85098386317000063, 0.1356331847737999863 ) ) ;
#4552=DIRECTION ( 'NONE',  ( 0.000000000000000000, -0.7071067811866525998, -0.7071067811864425456 ) ) ;
#4554=AXIS2_PLACEMENT_3D ( 'NONE', #46213, #50636, #19039 ) ;
#4557=ADVANCED_FACE ( 'NONE', ( #9545 ), #11222, .F. ) ;
#4558=CYLINDRICAL_SURFACE ( 'NONE', #42555, 12.50000000000000000 ) ;
#4562=ORIENTED_EDGE ( 'NONE', *, *, #18886, .F. ) ;
#4565=ORIENTED_EDGE ( 'NONE', *, *, #49843, .F. ) ;
#4566=CARTESIAN_POINT ( 'NONE',  ( -1.758095523367999791, -18.27708336119999899, 12.57362173515999970 ) ) ;
#4568=AXIS2_PLACEMENT_3D ( 'NONE', #15408, #1848, #11568 ) ;
#4569=CARTESIAN_POINT ( 'NONE',  ( 10.26699006316253637, -77.50833333333329733, -5.917523019358050362 ) ) ;
#4570=EDGE_CURVE ( 'NONE', #20424, #56848, #43795, .T. ) ;
#4571=CARTESIAN_POINT ( 'NONE',  ( 1.930009203935999951, -23.20099032317000365, -12.72537718777000038 ) ) ;
#4574=CARTESIAN_POINT ( 'NONE',  ( 12.70556836343000029, -53.57227722738999631, -1.774194422348999890E-09 ) ) ;
#4575=CARTESIAN_POINT ( 'NONE',  ( -12.20786306117000031, -78.92007912177000151, -0.2360786541355999746 ) ) ;
#4578=DIRECTION ( 'NONE',  ( 0.000000000000000000, -1.000000000000000000, 0.000000000000000000 ) ) ;
#4579=CARTESIAN_POINT ( 'NONE',  ( -1.750000000001000089, -18.75000001325000198, -12.56594318051000059 ) ) ;
#4585=CARTESIAN_POINT ( 'NONE',  ( -1.332847799107999887, -78.03533949426000049, -12.88744032790000027 ) ) ;
#4587=EDGE_CURVE ( 'NONE', #18023, #822, #32139, .T. ) ;
#4595=DIRECTION ( 'NONE',  ( 0.7071067811865475727, 0.000000000000000000, -0.7071067811865475727 ) ) ;
#4596=CARTESIAN_POINT ( 'NONE',  ( 10.13881649148000008, -76.90783510652001098, -5.938594122520999719 ) ) ;
#4597=CARTESIAN_POINT ( 'NONE',  ( -13.49939038839240979, -9.295797029142999435, -0.1282931867975413143 ) ) ;
#4599=VECTOR ( 'NONE', #30627, 1000.000000000000000 ) ;
#4602=CARTESIAN_POINT ( 'NONE',  ( 1.781953555039999859, -2.981106643931000111, -3.363141973650999983 ) ) ;
#4605=DIRECTION ( 'NONE',  ( 0.000000000000000000, -1.000000000000000000, 0.000000000000000000 ) ) ;
#4608=CARTESIAN_POINT ( 'NONE',  ( 2.062670899148999926, -60.10639625617000092, 12.83044039277999993 ) ) ;
#4609=CARTESIAN_POINT ( 'NONE',  ( 7.349802007153999561, -77.69009527504000800, -10.73869877321999944 ) ) ;
#4612=CARTESIAN_POINT ( 'NONE',  ( 12.49306764015999960, -23.28056535155999995, -1.667917367065999912 ) ) ;
#4613=ORIENTED_EDGE ( 'NONE', *, *, #33823, .F. ) ;
#4614=DIRECTION ( 'NONE',  ( 0.000000000000000000, 1.000000000000000000, 0.000000000000000000 ) ) ;
#4615=CARTESIAN_POINT ( 'NONE',  ( 8.813906587775187873, -53.78989792558270722, -8.872948314069059705 ) ) ;
#4620=CARTESIAN_POINT ( 'NONE',  ( 2.627446458840999810, -1.670251425905000087, 3.037392460054000320 ) ) ;
#4621=CARTESIAN_POINT ( 'NONE',  ( -1.931087888049999979, -60.11584477251999203, -12.71658889743999943 ) ) ;
#4625=CARTESIAN_POINT ( 'NONE',  ( 0.000000000000000000, 4.040000000000000036, 0.000000000000000000 ) ) ;
#4628=VERTEX_POINT ( 'NONE', #6485 ) ;
#4629=DIRECTION ( 'NONE',  ( 0.000000000000000000, 1.000000000000000000, 0.000000000000000000 ) ) ;
#4632=ORIENTED_EDGE ( 'NONE', *, *, #42622, .F. ) ;
#4634=ORIENTED_EDGE ( 'NONE', *, *, #8150, .F. ) ;
#4635=VERTEX_POINT ( 'NONE', #7068 ) ;
#4636=CARTESIAN_POINT ( 'NONE',  ( -3.249653326647542251, -2.606879814458876066, -0.2573833159217454591 ) ) ;
#4637=AXIS2_PLACEMENT_3D ( 'NONE', #4300, #41192, #17889 ) ;
#4638=EDGE_CURVE ( 'NONE', #15196, #6738, #29388, .T. ) ;
#4640=CARTESIAN_POINT ( 'NONE',  ( 2.303718438183066208, -1.521409140963204676, -3.294797006952866258 ) ) ;
#4646=AXIS2_PLACEMENT_3D ( 'NONE', #43309, #2866, #12295 ) ;
#4649=VECTOR ( 'NONE', #40281, 1000.000000000000114 ) ;
#4650=CARTESIAN_POINT ( 'NONE',  ( -7.654537085030000299, -23.28056692670000061, -10.01332844637000008 ) ) ;
#4651=DIRECTION ( 'NONE',  ( 0.000000000000000000, -1.000000000000000000, 0.000000000000000000 ) ) ;
#4652=LINE ( 'NONE', #58075, #37418 ) ;
#4657=CARTESIAN_POINT ( 'NONE',  ( -10.47840054245999930, -23.78693148451999662, 7.622763498569999463 ) ) ;
#4659=CARTESIAN_POINT ( 'NONE',  ( -9.396085398178650294, -76.74791666666666856, 7.220923959705211281 ) ) ;
#4663=DIRECTION ( 'NONE',  ( -0.7071067811865475727, 0.000000000000000000, -0.7071067811865475727 ) ) ;
#4664=CARTESIAN_POINT ( 'NONE',  ( 0.5045596072230998930, -25.13528913037999857, 12.66210649709999991 ) ) ;
#4667=CARTESIAN_POINT ( 'NONE',  ( 2.081885476966999882, -0.9615064129436999840, -3.558236660806000096 ) ) ;
#4672=DIRECTION ( 'NONE',  ( 0.000000000000000000, 1.000000000000000000, 0.000000000000000000 ) ) ;
#4681=ORIENTED_EDGE ( 'NONE', *, *, #7435, .F. ) ;
#4684=DIRECTION ( 'NONE',  ( 1.000000000000000000, 0.000000000000000000, 0.000000000000000000 ) ) ;
#4686=CARTESIAN_POINT ( 'NONE',  ( -10.18949719147000010, -60.01529250184999853, 7.645392405676999736 ) ) ;
#4688=VECTOR ( 'NONE', #2380, 999.9999999999998863 ) ;
#4689=CARTESIAN_POINT ( 'NONE',  ( -10.33814977949000102, -77.20682288379001079, 7.275158806450000348 ) ) ;
#4691=CARTESIAN_POINT ( 'NONE',  ( 12.59651352881000008, -23.39056208384000257, -1.801710201210000140 ) ) ;
#4692=DIRECTION ( 'NONE',  ( -0.7592504785508227272, -0.04890181650118147205, 0.6489586451872195738 ) ) ;
#4694=CARTESIAN_POINT ( 'NONE',  ( 0.000000000000000000, -0.09999999995300053179, 0.000000000000000000 ) ) ;
#4700=B_SPLINE_CURVE_WITH_KNOTS ( 'NONE', 3,
 ( #48001, #26107, #52128, #2534, #29376, #16974, #29662, #21682, #7243, #25248, #7823, #47423, #57695, #2821, #20816, #21393, #20537, #52986, #43852, #34670, #12537, #38823, #39687, #3398, #38534, #17251, #48567, #48285, #6953, #24958 ),
 .UNSPECIFIED., .F., .F.,
 ( 4, 2, 2, 2, 2, 2, 2, 2, 2, 2, 2, 2, 2, 2, 4 ),
 ( 0.000000000000000000, 0.1249999999999988343, 0.1874999999999990286, 0.2499999999999992228, 0.3124999999999993894, 0.3749999999999996114, 0.5000000000000005551, 0.5625000000000009992, 0.6250000000000014433, 0.6875000000000019984, 0.7500000000000025535, 0.8125000000000031086, 0.8437500000000033307, 0.8750000000000035527, 1.000000000000000000 ),
 .UNSPECIFIED. ) ;
#4701=CARTESIAN_POINT ( 'NONE',  ( 10.98753362943493883, -23.45184359403916829, 0.5244447725534562288 ) ) ;
#4704=CARTESIAN_POINT ( 'NONE',  ( -1.931043762602999925, -22.77819125662999866, 12.75761570867000039 ) ) ;
#4705=ORIENTED_EDGE ( 'NONE', *, *, #19301, .T. ) ;
#4706=CARTESIAN_POINT ( 'NONE',  ( -7.633088938737000007, -55.40992532391999958, -10.18115029110999892 ) ) ;
#4709=EDGE_LOOP ( 'NONE', ( #33523, #24387, #15603, #32761 ) ) ;
#4717=CARTESIAN_POINT ( 'NONE',  ( -13.07317008567999927, -77.50062674423000431, -1.028553310913000063 ) ) ;
#4726=CARTESIAN_POINT ( 'NONE',  ( -1.476182556144000069, -76.43656575806998887, 12.22114576030999977 ) ) ;
#4728=B_SPLINE_SURFACE_WITH_KNOTS ( 'NONE', 3, 3, ( 
 ( #9036, #27023, #22012, #58035 ),
 ( #49185, #17595, #49784, #53611 ),
 ( #13150, #45355, #53316, #30861 ),
 ( #18481, #40621, #31144, #8736 ),
 ( #26729, #4308, #22308, #40323 ),
 ( #58334, #35886, #53916, #13448 ),
 ( #31446, #49488, #45059, #4612 ),
 ( #218, #18194, #13741, #36188 ) ),
 .UNSPECIFIED., .F., .F., .F.,
 ( 4, 1, 1, 1, 1, 4 ),
 ( 4, 4 ),
 ( -0.01200407345745999922, 0.000000000000000000, 0.3333333333333000081, 0.6666666666667000474, 1.000000000000000000, 1.011997855551999947 ),
 ( -0.3559705542741000150, 1.355970554273999928 ),
 .UNSPECIFIED. ) ;
#4729=CIRCLE ( 'NONE', #15084, 14.00000000000000000 ) ;
#4735=CARTESIAN_POINT ( 'NONE',  ( 12.02803943743313475, -76.79341500456992264, -1.008114833370821417 ) ) ;
#4737=ORIENTED_EDGE ( 'NONE', *, *, #37279, .T. ) ;
#4744=DIRECTION ( 'NONE',  ( 0.000000000000000000, -1.000000000000000000, 0.000000000000000000 ) ) ;
#4745=CARTESIAN_POINT ( 'NONE',  ( 0.01248279339869594502, -76.07459138074202087, 11.74977687581417918 ) ) ;
#4747=LINE ( 'NONE', #27161, #40774 ) ;
#4748=ORIENTED_EDGE ( 'NONE', *, *, #15022, .T. ) ;
#4751=CIRCLE ( 'NONE', #48129, 1.750000000000000000 ) ;
#4753=CARTESIAN_POINT ( 'NONE',  ( -0.8338927958969792886, -17.19946422253764950, -12.50366901602889058 ) ) ;
#4755=DIRECTION ( 'NONE',  ( -1.000000000000000000, 0.000000000000000000, 0.000000000000000000 ) ) ;
#4757=ORIENTED_EDGE ( 'NONE', *, *, #13222, .T. ) ;
#4760=CARTESIAN_POINT ( 'NONE',  ( 12.74331394910317705, -18.47353206583634844, 1.980611464662580756 ) ) ;
#4769=AXIS2_PLACEMENT_3D ( 'NONE', #10364, #45813, #36054 ) ;
#4770=CARTESIAN_POINT ( 'NONE',  ( 11.00000000000000000, -74.59999999999999432, 0.000000000000000000 ) ) ;
#4773=CARTESIAN_POINT ( 'NONE',  ( 12.50000000000000000, -18.75000000000000000, 0.000000000000000000 ) ) ;
#4774=ORIENTED_EDGE ( 'NONE', *, *, #10261, .F. ) ;
#4777=EDGE_CURVE ( 'NONE', #308, #37604, #44874, .T. ) ;
#4780=ORIENTED_EDGE ( 'NONE', *, *, #35176, .T. ) ;
#4783=CARTESIAN_POINT ( 'NONE',  ( 7.364280830341206396, -55.45989902438520858, -8.171144579308812439 ) ) ;
#4787=DIRECTION ( 'NONE',  ( 0.000000000000000000, 0.000000000000000000, -1.000000000000000000 ) ) ;
#4790=CARTESIAN_POINT ( 'NONE',  ( -10.98754182310630334, -18.54785535411248176, 0.5242772304794532934 ) ) ;
#4791=AXIS2_PLACEMENT_3D ( 'NONE', #45431, #35659, #40698 ) ;
#4795=ADVANCED_FACE ( 'NONE', ( #4064 ), #4369, .F. ) ;
#4798=CARTESIAN_POINT ( 'NONE',  ( -9.820549435267999172, -76.56333523746999958, -8.704928227648998984 ) ) ;
#4803=DIRECTION ( 'NONE',  ( 0.000000000000000000, 0.000000000000000000, 1.000000000000000000 ) ) ;
#4806=EDGE_LOOP ( 'NONE', ( #34896, #44549, #17753, #49884 ) ) ;
#4808=AXIS2_PLACEMENT_3D ( 'NONE', #22983, #13230, #40700 ) ;
#4813=AXIS2_PLACEMENT_3D ( 'NONE', #50698, #23518, #5800 ) ;
#4818=CARTESIAN_POINT ( 'NONE',  ( 10.01234990230000044, -60.09849137196000157, -7.653559502293999728 ) ) ;
#4823=ORIENTED_EDGE ( 'NONE', *, *, #19680, .T. ) ;
#4824=CARTESIAN_POINT ( 'NONE',  ( -0.5390150933986999071, -53.53739108314999839, 12.77520260999999913 ) ) ;
#4826=CARTESIAN_POINT ( 'NONE',  ( -10.03846658012971993, -23.79367507167474471, 7.678639819101479524 ) ) ;
#4832=CARTESIAN_POINT ( 'NONE',  ( 12.49830607528000037, -18.79028586434999681, 1.666977523253999838 ) ) ;
#4837=EDGE_CURVE ( 'NONE', #58165, #22857, #26490, .T. ) ;
#4838=CARTESIAN_POINT ( 'NONE',  ( 10.35398565885000011, -55.39211376237999929, -7.619387877908000206 ) ) ;
#4839=AXIS2_PLACEMENT_3D ( 'NONE', #37144, #13239, #18859 ) ;
#4845=B_SPLINE_CURVE_WITH_KNOTS ( 'NONE', 3,
 ( #6542, #29830, #7125, #20703 ),
 .UNSPECIFIED., .F., .F.,
 ( 4, 4 ),
 ( 0.000000000000000000, 1.000000000000000000 ),
 .UNSPECIFIED. ) ;
#4846=CARTESIAN_POINT ( 'NONE',  ( -12.49989425042000235, -59.99225390429000271, 1.666425739590000177 ) ) ;
#4855=CARTESIAN_POINT ( 'NONE',  ( 7.666647577131698199, -55.04957415510976659, 7.889735440111296683 ) ) ;
#4856=ORIENTED_EDGE ( 'NONE', *, *, #5762, .T. ) ;
#4860=ORIENTED_EDGE ( 'NONE', *, *, #29990, .T. ) ;
#4861=ORIENTED_EDGE ( 'NONE', *, *, #41988, .T. ) ;
#4863=CARTESIAN_POINT ( 'NONE',  ( 7.601397897754999633, -18.75000000310999937, -10.07627163191000008 ) ) ;
#4865=CARTESIAN_POINT ( 'NONE',  ( 1.930638663166000191, -23.22122063288999883, -12.72375916873000001 ) ) ;
#4867=CARTESIAN_POINT ( 'NONE',  ( 10.07627163191000008, -60.04999999725999515, 7.601397897754999633 ) ) ;
#4868=CARTESIAN_POINT ( 'NONE',  ( -9.202058689291000348, -78.77551683587999776, 7.798053816622000589 ) ) ;
#4869=EDGE_CURVE ( 'NONE', #23631, #24315, #29322, .T. ) ;
#4872=CARTESIAN_POINT ( 'NONE',  ( 14.00000000000000000, -32.88214388149999934, -1.168362945876000107E-11 ) ) ;
#4877=FACE_OUTER_BOUND ( 'NONE', #6668, .T. ) ;
#4879=CARTESIAN_POINT ( 'NONE',  ( -9.299140214181999653, -77.97983485329999098, -9.021566674317000434 ) ) ;
#4882=LINE ( 'NONE', #50054, #49179 ) ;
#4885=FACE_OUTER_BOUND ( 'NONE', #38599, .T. ) ;
#4886=CARTESIAN_POINT ( 'NONE',  ( 3.237146527450594391, -2.859107922686362269, 0.3631461997434258793 ) ) ;
#4889=EDGE_CURVE ( 'NONE', #12183, #35168, #21594, .T. ) ;
#4892=CARTESIAN_POINT ( 'NONE',  ( -2.707053224964000027, -2.755300808012999703, 2.675433656965999774 ) ) ;
#4894=VERTEX_POINT ( 'NONE', #41264 ) ;
#4896=CARTESIAN_POINT ( 'NONE',  ( -0.3135214471519903734, -18.31418618814238997, -10.99610567419574636 ) ) ;
#4898=DIRECTION ( 'NONE',  ( 0.000000000000000000, -1.000000000000000000, 0.000000000000000000 ) ) ;
#4899=CARTESIAN_POINT ( 'NONE',  ( 2.062503053667999797, -57.04263462147999775, 12.92177931909999877 ) ) ;
#4900=CARTESIAN_POINT ( 'NONE',  ( 11.85869973992999959, -77.80110455695999860, 5.358216250391999225 ) ) ;
#4902=CARTESIAN_POINT ( 'NONE',  ( -9.433548213809427097, -61.92797454580141192, -8.532643227302681765 ) ) ;
#4903=CARTESIAN_POINT ( 'NONE',  ( -9.328742748748998892, -76.43633340635999218, 8.338699562703999035 ) ) ;
#4905=EDGE_CURVE ( 'NONE', #2252, #55921, #13688, .T. ) ;
#4909=CARTESIAN_POINT ( 'NONE',  ( 7.641012386039999882, -23.28917565320000094, -10.18589234708000113 ) ) ;
#4912=CARTESIAN_POINT ( 'NONE',  ( -0.7824435345810000220, -1.707931841279000107, 3.939770163431000061 ) ) ;
#4913=CARTESIAN_POINT ( 'NONE',  ( -2.062670899148999926, -60.10639625617000092, -12.83044039277999993 ) ) ;
#4915=ORIENTED_EDGE ( 'NONE', *, *, #16294, .F. ) ;
#4918=ORIENTED_EDGE ( 'NONE', *, *, #37753, .F. ) ;
#4922=ORIENTED_EDGE ( 'NONE', *, *, #8142, .F. ) ;
#4927=DIRECTION ( 'NONE',  ( 0.7071067811864976127, -3.445410891335986341E-11, -0.7071067811865975328 ) ) ;
#4930=ORIENTED_EDGE ( 'NONE', *, *, #34287, .T. ) ;
#4931=FACE_OUTER_BOUND ( 'NONE', #27034, .T. ) ;
#4932=EDGE_LOOP ( 'NONE', ( #43859, #51912, #38368, #16701 ) ) ;
#4937=CARTESIAN_POINT ( 'NONE',  ( -7.641012305222999679, -23.28917723430000208, -10.18589226631999978 ) ) ;
#4938=CARTESIAN_POINT ( 'NONE',  ( 1.250000000000000000, -55.54999999966999980, 12.50000000000000000 ) ) ;
#4939=AXIS2_PLACEMENT_3D ( 'NONE', #51721, #20984, #6827 ) ;
#4940=LINE ( 'NONE', #41240, #26122 ) ;
#4941=FACE_OUTER_BOUND ( 'NONE', #50756, .T. ) ;
#4946=CARTESIAN_POINT ( 'NONE',  ( -11.75000000000000711, -76.78958333333332575, 1.538071403319954955 ) ) ;
#4948=VECTOR ( 'NONE', #11174, 1000.000000000000000 ) ;
#4949=CARTESIAN_POINT ( 'NONE',  ( -12.83677071377000090, -18.77261389757000032, 2.062839858857999698 ) ) ;
#4951=FACE_OUTER_BOUND ( 'NONE', #14127, .T. ) ;
#4952=CARTESIAN_POINT ( 'NONE',  ( 1.576170184332999824, -24.16086967216000048, 12.55466896104999996 ) ) ;
#4955=CARTESIAN_POINT ( 'NONE',  ( 1.913681202397000014, -1.135668112399999874, -3.270751771314000411 ) ) ;
#4957=CARTESIAN_POINT ( 'NONE',  ( -1.798944584243999945, -23.21533228280000216, -12.61116915999999932 ) ) ;
#4958=CARTESIAN_POINT ( 'NONE',  ( 12.77651065753999937, -62.10896598063000340, 0.04308629978602999955 ) ) ;
#4959=CYLINDRICAL_SURFACE ( 'NONE', #32801, 0.5000000000000006661 ) ;
#4961=CARTESIAN_POINT ( 'NONE',  ( 0.000000000000000000, -49.87071424677999687, 0.000000000000000000 ) ) ;
#4962=CARTESIAN_POINT ( 'NONE',  ( -1.980532734072999901, -56.03767313155999830, 12.80090744964999949 ) ) ;
#4968=DIRECTION ( 'NONE',  ( 0.000000000000000000, -1.000000000000000000, 0.000000000000000000 ) ) ;
#4971=CARTESIAN_POINT ( 'NONE',  ( 12.66322081666000088, -53.61838367289999496, -0.1487102037790999920 ) ) ;
#4972=CARTESIAN_POINT ( 'NONE',  ( -10.98362417419999915, -23.15000000000000213, 0.5999999999999999778 ) ) ;
#4975=CARTESIAN_POINT ( 'NONE',  ( -11.53944584717811317, -76.31731959221001205, -2.557081017239585918 ) ) ;
#4981=CARTESIAN_POINT ( 'NONE',  ( 11.74913005080746409, -75.94346313125201675, -0.9228039449030241981 ) ) ;
#4982=EDGE_CURVE ( 'NONE', #34855, #20949, #36827, .T. ) ;
#4984=ADVANCED_FACE ( 'NONE', ( #14383 ), #54243, .T. ) ;
#4988=LINE ( 'NONE', #597, #34625 ) ;
#4989=VERTEX_POINT ( 'NONE', #23538 ) ;
#4994=SURFACE_STYLE_USAGE ( .BOTH. , #45451 ) ;
#4998=DIRECTION ( 'NONE',  ( 0.7071067811865475727, 0.000000000000000000, -0.7071067811865475727 ) ) ;
#5000=ORIENTED_EDGE ( 'NONE', *, *, #39795, .T. ) ;
#5005=DIRECTION ( 'NONE',  ( -0.5721800012450894979, -0.8201280669353838704, 0.000000000000000000 ) ) ;
#5011=CARTESIAN_POINT ( 'NONE',  ( 12.02702378446000075, -75.79321984486000474, -1.341316611471999876 ) ) ;
#5014=CARTESIAN_POINT ( 'NONE',  ( 3.520806411577878325, -2.101010226048630081, 0.07559986181835516572 ) ) ;
#5015=CARTESIAN_POINT ( 'NONE',  ( 7.974014308154000474, -61.43100890296999950, -9.929675091768999096 ) ) ;
#5016=CARTESIAN_POINT ( 'NONE',  ( -11.38660623898999980, -79.08227941497999325, -4.554589311945999697 ) ) ;
#5018=CARTESIAN_POINT ( 'NONE',  ( 12.70259395227655475, -17.26112126508259337, -1.314575638817670145 ) ) ;
#5021=CARTESIAN_POINT ( 'NONE',  ( 5.203459128634499997, -77.38937829694961579, 10.83448682463159507 ) ) ;
#5022=CARTESIAN_POINT ( 'NONE',  ( 1.859746058491110965, -75.81538667321693481, 12.00664290235934217 ) ) ;
#5023=VECTOR ( 'NONE', #19324, 1000.000000000000000 ) ;
#5027=CARTESIAN_POINT ( 'NONE',  ( -11.75000000000000000, -77.79999999999999716, 1.702919296826999607E-14 ) ) ;
#5034=CARTESIAN_POINT ( 'NONE',  ( 4.701268039995720294, -76.04171589382065122, 10.76872600201126673 ) ) ;
#5040=CARTESIAN_POINT ( 'NONE',  ( 6.153863461931999623, -76.21665917695410997, -10.66140155521000032 ) ) ;
#5043=ADVANCED_FACE ( 'NONE', ( #40975 ), #4959, .F. ) ;
#5045=CARTESIAN_POINT ( 'NONE',  ( -5.692170641448433877, -76.28460817517897397, -10.28117217690509655 ) ) ;
#5047=CARTESIAN_POINT ( 'NONE',  ( 0.000000000000000000, -9.295797029142999435, 0.000000000000000000 ) ) ;
#5050=CARTESIAN_POINT ( 'NONE',  ( 7.606021555073000151, -18.57841460072999951, -10.52692944505000128 ) ) ;
#5053=CARTESIAN_POINT ( 'NONE',  ( 12.72924182832020534, -18.22450359986278201, 1.930521792012820370 ) ) ;
#5054=CARTESIAN_POINT ( 'NONE',  ( 12.50659830419106910, -53.82653389278990375, 0.3508388549139770940 ) ) ;
#5057=CARTESIAN_POINT ( 'NONE',  ( 12.56594317991999965, -60.04999999381999487, 1.750000000001000089 ) ) ;
#5058=EDGE_CURVE ( 'NONE', #47851, #17898, #47722, .T. ) ;
#5061=CARTESIAN_POINT ( 'NONE',  ( 14.00000000000000000, -9.295797029142999435, 0.000000000000000000 ) ) ;
#5062=B_SPLINE_CURVE_WITH_KNOTS ( 'NONE', 3,
 ( #9572, #49134, #9278, #26677, #40572, #27556, #5143, #54451, #36424, #4855, #44709, #18434, #35833, #23142, #26971, #39973, #31097, #4262 ),
 .UNSPECIFIED., .F., .F.,
 ( 4, 2, 2, 2, 2, 2, 2, 2, 4 ),
 ( 0.000000000000000000, 0.06250000000000328904, 0.1250000000000065781, 0.2500000000000031641, 0.5000000000000028866, 0.7500000000000025535, 0.8125000000000018874, 0.8750000000000012212, 1.000000000000000000 ),
 .UNSPECIFIED. ) ;
#5064=DIRECTION ( 'NONE',  ( 0.000000000000000000, 0.000000000000000000, -1.000000000000000000 ) ) ;
#5066=B_SPLINE_CURVE_WITH_KNOTS ( 'NONE', 3,
 ( #5900, #10345, #11226, #23910, #1500, #55506, #33046, #24209, #20082, #51093, #28624, #46669, #42227, #29205, #1792, #19788 ),
 .UNSPECIFIED., .F., .F.,
 ( 4, 2, 2, 2, 2, 2, 2, 4 ),
 ( 0.000000000000000000, 0.2500000000000000555, 0.3750000000000001110, 0.5000000000000001110, 0.6250000000000001110, 0.6875000000000001110, 0.7500000000000002220, 1.000000000000000000 ),
 .UNSPECIFIED. ) ;
#5067=CARTESIAN_POINT ( 'NONE',  ( -12.66319951811000166, -25.18148258132000095, 0.1455783832297000147 ) ) ;
#5069=ORIENTED_EDGE ( 'NONE', *, *, #23221, .T. ) ;
#5071=DIRECTION ( 'NONE',  ( 0.7071067811865475727, 0.000000000000000000, -0.7071067811865475727 ) ) ;
#5074=CARTESIAN_POINT ( 'NONE',  ( 7.606021324597999289, -23.42158946275000275, 10.52692925327000140 ) ) ;
#5077=CARTESIAN_POINT ( 'NONE',  ( 10.35398566683000077, -60.20788276206999967, 7.619388279096000360 ) ) ;
#5078=CARTESIAN_POINT ( 'NONE',  ( -13.49939038839240979, -32.88214388149999934, -0.1282931867975413143 ) ) ;
#5083=CARTESIAN_POINT ( 'NONE',  ( 7.850076762419817555, -61.11471440997013360, -9.837736659315822862 ) ) ;
#5087=CARTESIAN_POINT ( 'NONE',  ( 0.000000000000000000, -0.09999999858571000100, 0.000000000000000000 ) ) ;
#5088=ADVANCED_FACE ( 'NONE', ( #14673 ), #28088, .F. ) ;
#5090=CARTESIAN_POINT ( 'NONE',  ( 6.292427835922000057, -76.25321726005000755, 11.33658693087999936 ) ) ;
#5093=CARTESIAN_POINT ( 'NONE',  ( 14.00000000000000000, -32.88214388149999934, 0.000000000000000000 ) ) ;
#5095=CARTESIAN_POINT ( 'NONE',  ( -7.758655887903000092, -24.15078616243999932, -9.996711280983999970 ) ) ;
#5096=AXIS2_PLACEMENT_3D ( 'NONE', #4938, #4651, #50405 ) ;
#5099=ORIENTED_EDGE ( 'NONE', *, *, #5439, .T. ) ;
#5104=CARTESIAN_POINT ( 'NONE',  ( 2.598917237794081014, -3.302083333333333925, 1.997276839918480373 ) ) ;
#5106=CYLINDRICAL_SURFACE ( 'NONE', #25065, 0.5000000000000004441 ) ;
#5114=B_SPLINE_CURVE_WITH_KNOTS ( 'NONE', 3,
 ( #13152, #12862, #9624, #31146, #9333, #45061 ),
 .UNSPECIFIED., .F., .F.,
 ( 4, 1, 1, 4 ),
 ( 0.000000000000000000, 0.3333333311589000147, 0.6666666623179000606, 0.9999999934768000198 ),
 .UNSPECIFIED. ) ;
#5119=CARTESIAN_POINT ( 'NONE',  ( -2.536595847992999975, -3.375401880086999817, -3.049063006156000011 ) ) ;
#5126=DIRECTION ( 'NONE',  ( 0.000000000000000000, 0.000000000000000000, 1.000000000000000000 ) ) ;
#5127=FACE_OUTER_BOUND ( 'NONE', #23722, .T. ) ;
#5129=CARTESIAN_POINT ( 'NONE',  ( 9.029856014839001688, -53.46737842902999915, -9.038878718651000455 ) ) ;
#5134=CARTESIAN_POINT ( 'NONE',  ( -0.8898229089110474277, -61.82324531153690828, 12.70296869049124311 ) ) ;
#5136=CARTESIAN_POINT ( 'NONE',  ( -12.43641409355999983, -61.71801033862000452, -0.03481937293210000256 ) ) ;
#5138=DIRECTION ( 'NONE',  ( 0.7071067811865475727, 0.000000000000000000, 0.7071067811865475727 ) ) ;
#5141=CARTESIAN_POINT ( 'NONE',  ( -0.8338927961505636643, -61.60053577702783656, 12.50366901606069447 ) ) ;
#5143=CARTESIAN_POINT ( 'NONE',  ( 8.111636311586917003, -55.28385402669261595, 7.429974109814975414 ) ) ;
#5145=ORIENTED_EDGE ( 'NONE', *, *, #32666, .T. ) ;
#5147=ORIENTED_EDGE ( 'NONE', *, *, #55170, .T. ) ;
#5148=ORIENTED_EDGE ( 'NONE', *, *, #14702, .T. ) ;
#5149=DIRECTION ( 'NONE',  ( -1.000000000000000000, 0.000000000000000000, 0.000000000000000000 ) ) ;
#5151=CARTESIAN_POINT ( 'NONE',  ( 1.750000000000000000, -57.04935285922000077, 12.65372179284000076 ) ) ;
#5154=LINE ( 'NONE', #23155, #35243 ) ;
#5155=CARTESIAN_POINT ( 'NONE',  ( 9.995119889681001624, -79.03418329856999947, -6.751676457494999894 ) ) ;
#5160=EDGE_CURVE ( 'NONE', #29817, #45005, #45317, .T. ) ;
#5161=CARTESIAN_POINT ( 'NONE',  ( 0.8898229090076987813, -61.82324531144395507, -12.70296869049792932 ) ) ;
#5165=CARTESIAN_POINT ( 'NONE',  ( -10.55245342185999924, -77.36928380272000538, 7.517205849611000801 ) ) ;
#5166=EDGE_CURVE ( 'NONE', #39794, #27203, #45020, .T. ) ;
#5169=FACE_OUTER_BOUND ( 'NONE', #24018, .T. ) ;
#5173=FACE_OUTER_BOUND ( 'NONE', #51889, .T. ) ;
#5177=CARTESIAN_POINT ( 'NONE',  ( -8.485281374238999419, 0.000000000000000000, 8.485281374238999419 ) ) ;
#5181=CARTESIAN_POINT ( 'NONE',  ( -0.1610657711543910797, -18.25053022707189854, -10.99997582743960223 ) ) ;
#5183=CIRCLE ( 'NONE', #19305, 5.000000000000000000 ) ;
#5187=CARTESIAN_POINT ( 'NONE',  ( -12.97295173694999981, -77.48891468547999750, -1.020668466325000079 ) ) ;
#5189=CARTESIAN_POINT ( 'NONE',  ( -8.266617305365361545, -61.77234527411153664, -9.697375114849947408 ) ) ;
#5190=CARTESIAN_POINT ( 'NONE',  ( 10.12290050256999940, -18.75000002239000096, 7.648026768411000376 ) ) ;
#5191=ORIENTED_EDGE ( 'NONE', *, *, #55612, .F. ) ;
#5193=CARTESIAN_POINT ( 'NONE',  ( -9.621717086601071500, -24.62064477554104869, -8.060172378189184528 ) ) ;
#5195=EDGE_CURVE ( 'NONE', #47936, #891, #39400, .T. ) ;
#5197=CARTESIAN_POINT ( 'NONE',  ( 7.718346056127999510, -20.25111654322000021, -10.07719973196000041 ) ) ;
#5201=CARTESIAN_POINT ( 'NONE',  ( -3.249661007175000282, -0.6980864414130000251, 2.357191814219000037 ) ) ;
#5202=CARTESIAN_POINT ( 'NONE',  ( -2.062502994258999856, -58.55648180022999583, -12.92181194095999963 ) ) ;
#5204=VERTEX_POINT ( 'NONE', #26402 ) ;
#5214=EDGE_LOOP ( 'NONE', ( #2152, #51199, #1850, #46746, #43398 ) ) ;
#5215=CARTESIAN_POINT ( 'NONE',  ( -2.748921057787184541, -2.646192902617848564, -1.734975443660489169 ) ) ;
#5216=EDGE_CURVE ( 'NONE', #52133, #469, #10006, .T. ) ;
#5226=ADVANCED_FACE ( 'NONE', ( #35550 ), #6312, .F. ) ;
#5227=DIRECTION ( 'NONE',  ( 1.000000000000000000, 0.000000000000000000, 0.000000000000000000 ) ) ;
#5229=CARTESIAN_POINT ( 'NONE',  ( -9.298485322487321625, -24.88812323703229268, 8.385852789306289523 ) ) ;
#5237=CARTESIAN_POINT ( 'NONE',  ( -12.01673236380376686, -77.95062490049402015, 0.3580987964395272449 ) ) ;
#5241=CARTESIAN_POINT ( 'NONE',  ( 1.750000000001000089, -18.74999999009000007, -12.56594317857000043 ) ) ;
#5242=CARTESIAN_POINT ( 'NONE',  ( -2.065394024360999836, -23.42161432646000208, 12.82193048528000112 ) ) ;
#5245=CARTESIAN_POINT ( 'NONE',  ( -0.1136598462024999839, -0.8462797842361000633, 3.300476129822000004 ) ) ;
#5248=CARTESIAN_POINT ( 'NONE',  ( 10.59551070212999946, -58.55648180022999583, 7.678690995210999404 ) ) ;
#5250=CARTESIAN_POINT ( 'NONE',  ( -7.624341764906000130, -55.53514850498000044, -10.42531124851000079 ) ) ;
#5251=CARTESIAN_POINT ( 'NONE',  ( 2.866048672220999904, -2.746200577026000289, -1.983677989232000227 ) ) ;
#5253=DIRECTION ( 'NONE',  ( 1.674928520677000026E-10, 1.000000000000000000, -2.004067147595000089E-09 ) ) ;
#5254=DIRECTION ( 'NONE',  ( 0.000000000000000000, 1.000000000000000000, 0.000000000000000000 ) ) ;
#5262=FACE_BOUND ( 'NONE', #43467, .T. ) ;
#5264=CARTESIAN_POINT ( 'NONE',  ( 12.43647099676999979, -53.88193128055999637, 0.03491583288326000067 ) ) ;
#5265=CARTESIAN_POINT ( 'NONE',  ( -1.335477334469999862E-14, -72.70000000000000284, 0.000000000000000000 ) ) ;
#5266=CARTESIAN_POINT ( 'NONE',  ( 11.48986902082000050, -77.53985072955998703, 5.271442771914999881 ) ) ;
#5267=CARTESIAN_POINT ( 'NONE',  ( -8.556275607134224970, -76.36061857273500664, -8.153994206733470307 ) ) ;
#5269=EDGE_LOOP ( 'NONE', ( #13481, #29954, #12026, #28950 ) ) ;
#5271=CARTESIAN_POINT ( 'NONE',  ( 0.5135400118779288592, -53.62131466105113020, -12.70453250094157660 ) ) ;
#5273=CARTESIAN_POINT ( 'NONE',  ( 2.749590660225081251, -75.84330483478258600, -11.46114634323648396 ) ) ;
#5275=CARTESIAN_POINT ( 'NONE',  ( -12.00000000000000000, -18.75000000000000000, 1.250000000000000000 ) ) ;
#5276=CARTESIAN_POINT ( 'NONE',  ( -13.94827586207000003, -33.10361340872000113, -8.082385102019000922E-06 ) ) ;
#5278=CARTESIAN_POINT ( 'NONE',  ( 8.274772994052357333, -61.77888614391775235, -9.689268730118849149 ) ) ;
#5281=EDGE_CURVE ( 'NONE', #58211, #26037, #1041, .T. ) ;
#5283=EDGE_CURVE ( 'NONE', #44413, #56422, #1324, .T. ) ;
#5289=ORIENTED_EDGE ( 'NONE', *, *, #4889, .T. ) ;
#5291=DIRECTION ( 'NONE',  ( 0.000000000000000000, 0.000000000000000000, -1.000000000000000000 ) ) ;
#5292=CARTESIAN_POINT ( 'NONE',  ( 10.42531124905999995, -18.73514851523999880, -7.624341765453999997 ) ) ;
#5293=CARTESIAN_POINT ( 'NONE',  ( 1.930860503546800500, -18.22582494088415928, -12.72930866331970279 ) ) ;
#5295=EDGE_CURVE ( 'NONE', #14174, #22264, #22535, .T. ) ;
#5299=CARTESIAN_POINT ( 'NONE',  ( -1.750000000000000000, -18.75000000240999753, 12.50000000000000000 ) ) ;
#5300=CARTESIAN_POINT ( 'NONE',  ( 9.754023262367999436, -76.21512124563000157, -7.509630405475999915 ) ) ;
#5303=CARTESIAN_POINT ( 'NONE',  ( 3.490340410772612145, -2.109536202225938073, 0.4540853053036469911 ) ) ;
#5304=CARTESIAN_POINT ( 'NONE',  ( 10.12290050124000018, -18.75000000007999645, -7.648026767085999822 ) ) ;
#5305=CARTESIAN_POINT ( 'NONE',  ( -7.421655993048999811, -78.44405766871000196, 9.763070719336001346 ) ) ;
#5308=CIRCLE ( 'NONE', #25073, 0.5000000000000000000 ) ;
#5309=CARTESIAN_POINT ( 'NONE',  ( -10.18496935386999880, -57.04935285362000030, -7.710095619715000126 ) ) ;
#5313=CARTESIAN_POINT ( 'NONE',  ( -11.97720891572606128, -77.06026423996446795, -1.545522828243951929 ) ) ;
#5315=AXIS2_PLACEMENT_3D ( 'NONE', #56725, #2418, #16283 ) ;
#5316=ORIENTED_EDGE ( 'NONE', *, *, #38954, .F. ) ;
#5319=CARTESIAN_POINT ( 'NONE',  ( -1.750000000001000089, -59.55077028460999600, -12.60356226396000068 ) ) ;
#5325=CARTESIAN_POINT ( 'NONE',  ( 0.1978932475499107502, -76.07339481969196981, 11.74839477131042820 ) ) ;
#5328=ORIENTED_EDGE ( 'NONE', *, *, #23650, .T. ) ;
#5334=DIRECTION ( 'NONE',  ( 0.000000000000000000, -1.000000000000000000, 0.000000000000000000 ) ) ;
#5335=CARTESIAN_POINT ( 'NONE',  ( 8.790679651960999763, -17.06186536190000069, -8.797972003296999688 ) ) ;
#5339=CARTESIAN_POINT ( 'NONE',  ( 12.70455814331302768, -54.23992875941878822, 1.489882837217631595 ) ) ;
#5345=CARTESIAN_POINT ( 'NONE',  ( 13.89248035986000041, -9.608407476587998985, 2.632528379384000019E-05 ) ) ;
#5352=ORIENTED_EDGE ( 'NONE', *, *, #56248, .F. ) ;
#5353=AXIS2_PLACEMENT_3D ( 'NONE', #19626, #10193, #28173 ) ;
#5357=CIRCLE ( 'NONE', #35509, 13.86363636363999952 ) ;
#5358=ORIENTED_EDGE ( 'NONE', *, *, #49358, .T. ) ;
#5359=CARTESIAN_POINT ( 'NONE',  ( -1.750000000001000089, -23.24999998674999802, 12.56594318051000059 ) ) ;
#5361=CARTESIAN_POINT ( 'NONE',  ( 8.220407391966000787, -61.61950084198999633, 9.523310056136001123 ) ) ;
#5363=EDGE_CURVE ( 'NONE', #25542, #22170, #32865, .T. ) ;
#5367=ORIENTED_EDGE ( 'NONE', *, *, #37753, .T. ) ;
#5372=DIRECTION ( 'NONE',  ( 0.000000000000000000, -1.000000000000000000, 0.000000000000000000 ) ) ;
#5374=CARTESIAN_POINT ( 'NONE',  ( -10.03847181070773331, -18.20634590497699179, -7.678636148852304721 ) ) ;
#5379=CARTESIAN_POINT ( 'NONE',  ( -7.634438871657000192, -23.74781730700000182, -10.30764054782000017 ) ) ;
#5381=CARTESIAN_POINT ( 'NONE',  ( 12.71658872082999814, -55.48415267986000288, -1.931087888240000217 ) ) ;
#5383=ORIENTED_EDGE ( 'NONE', *, *, #1617, .F. ) ;
#5384=B_SPLINE_CURVE_WITH_KNOTS ( 'NONE', 3,
 ( #54333, #4436, #45185, #4735, #58160, #13873, #31567, #31867, #32157, #17726, #49909, #40451, #54037, #35714, #32445, #26855, #53743, #23320, #49616, #50196, #13576, #14159, #5313, #8863, #22733, #44886, #27732, #13279, #40744, #50489, #18896, #913, #9163, #9456, #36887, #23025, #31271, #14450, #49313, #22436, #10043, #337, #18317, #45478, #46069, #28024, #43, #5591, #23604, #41037, #18019, #5021, #36308, #27442, #628, #18611, #19770, #51662, #20346, #11499, #33901, #11210, #10625, #24774, #42209, #19186, #6765, #29473, #47528, #1775, #15337, #15037, #37766, #24483, #33328, #55787, #47236, #38343, #20067, #38055, #56365, #51077, #37181, #56078, #6180, #29188, #37468, #55194, #15915, #7057, #19475, #42787, #24192, #51365, #41616, #51943, #33618, #10329, #50784, #10920, #41911, #15624, #1196, #14737, #32736, #28901, #28309, #6472, #55489, #46360, #2351, #46947, #5885, #42498, #33031, #23892, #46653, #1484, #28607, #2066, #52792, #12631, #7628, #20915, #35339, #17065, #21776, #30044, #38918 ),
 .UNSPECIFIED., .F., .F.,
 ( 4, 2, 2, 2, 2, 2, 1, 2, 2, 2, 2, 2, 2, 2, 2, 2, 2, 1, 2, 2, 1, 1, 2, 2, 1, 2, 2, 1, 2, 2, 2, 2, 2, 2, 2, 1, 2, 2, 2, 2, 2, 2, 2, 1, 2, 2, 1, 2, 2, 1, 1, 2, 2, 1, 2, 2, 2, 2, 2, 2, 2, 2, 2, 2, 1, 2, 2, 2, 2, 2, 4 ),
 ( 0.000000000000000000, 0.01562500000000000000, 0.03125000000000000000, 0.04687500000000000000, 0.06250000000000000000, 0.07812500000000000000, 0.09375000000000000000, 0.1093750000000000000, 0.1250000000000000000, 0.1406250000000000000, 0.1562500000000000000, 0.1718750000000000278, 0.1875000000000000555, 0.2031250000000000833, 0.2187500000000001110, 0.2343750000000001388, 0.2421875000000001388, 0.2500000000000001665, 0.2656250000000001665, 0.2734375000000001665, 0.2812500000000001665, 0.2968750000000001665, 0.3046875000000001665, 0.3125000000000001665, 0.3281250000000001665, 0.3359375000000001665, 0.3437500000000001665, 0.3593750000000001665, 0.3671875000000001665, 0.3750000000000001665, 0.3906250000000001665, 0.4062500000000001665, 0.4218750000000001665, 0.4375000000000001665, 0.4687500000000001665, 0.5000000000000001110, 0.5312500000000001110, 0.5625000000000001110, 0.5781250000000001110, 0.5937500000000001110, 0.6093750000000001110, 0.6250000000000001110, 0.6328125000000001110, 0.6406250000000001110, 0.6562500000000001110, 0.6640625000000001110, 0.6718750000000001110, 0.6875000000000001110, 0.6953125000000001110, 0.7031250000000001110, 0.7187500000000001110, 0.7265625000000001110, 0.7343750000000001110, 0.7500000000000001110, 0.7578125000000001110, 0.7656250000000001110, 0.7812500000000001110, 0.7968750000000001110, 0.8125000000000001110, 0.8281250000000001110, 0.8437500000000001110, 0.8593750000000001110, 0.8750000000000001110, 0.8906250000000001110, 0.9062500000000001110, 0.9218750000000001110, 0.9375000000000001110, 0.9531250000000001110, 0.9687500000000001110, 0.9843750000000001110, 1.000000000000000000 ),
 .UNSPECIFIED. ) ;
#5385=DIRECTION ( 'NONE',  ( -0.7071067811865475727, 0.000000000000000000, -0.7071067811865475727 ) ) ;
#5388=AXIS2_PLACEMENT_3D ( 'NONE', #12129, #52578, #58376 ) ;
#5389=DIRECTION ( 'NONE',  ( -0.7071067811865475727, 0.000000000000000000, -0.7071067811865475727 ) ) ;
#5390=CARTESIAN_POINT ( 'NONE',  ( -1.250000000000000000, -60.04999999966999980, -12.00000000000000000 ) ) ;
#5391=CARTESIAN_POINT ( 'NONE',  ( 3.518011427261086954, -3.002431050661036327, 0.1098636256542055017 ) ) ;
#5395=CARTESIAN_POINT ( 'NONE',  ( 0.000000000000000000, -60.04999999966999980, 12.00000000000000000 ) ) ;
#5397=CIRCLE ( 'NONE', #42995, 1.750000000000000000 ) ;
#5398=ORIENTED_EDGE ( 'NONE', *, *, #10186, .F. ) ;
#5400=CARTESIAN_POINT ( 'NONE',  ( -3.388689987348999733, -2.762137290292000280, 2.061041899425999802 ) ) ;
#5403=CARTESIAN_POINT ( 'NONE',  ( 9.038948602518001252, -25.33262223864999640, -9.029786144013998594 ) ) ;
#5405=EDGE_CURVE ( 'NONE', #56093, #1567, #54741, .T. ) ;
#5407=LINE ( 'NONE', #1576, #14491 ) ;
#5410=CARTESIAN_POINT ( 'NONE',  ( 1.250000000000000000, -23.44678171330999916, -12.50000000000000000 ) ) ;
#5416=DIRECTION ( 'NONE',  ( 0.000000000000000000, -1.000000000000000000, 0.000000000000000000 ) ) ;
#5418=DIRECTION ( 'NONE',  ( -0.6489586469534679436, -0.04890178980860759861, 0.7592504787603620020 ) ) ;
#5419=CARTESIAN_POINT ( 'NONE',  ( 12.50409217853026078, -54.27871355468435866, -1.233808106764433532 ) ) ;
#5420=VERTEX_POINT ( 'NONE', #37308 ) ;
#5427=VERTEX_POINT ( 'NONE', #55324 ) ;
#5429=VERTEX_POINT ( 'NONE', #37602 ) ;
#5430=CARTESIAN_POINT ( 'NONE',  ( -1.669849926071999890, -18.62771399582999976, 12.48404299553000030 ) ) ;
#5434=ADVANCED_FACE ( 'NONE', ( #14868 ), #55618, .F. ) ;
#5437=AXIS2_PLACEMENT_3D ( 'NONE', #11614, #2466, #21320 ) ;
#5438=ORIENTED_EDGE ( 'NONE', *, *, #51508, .F. ) ;
#5439=EDGE_CURVE ( 'NONE', #35786, #46363, #9585, .T. ) ;
#5440=ORIENTED_EDGE ( 'NONE', *, *, #37309, .T. ) ;
#5445=CARTESIAN_POINT ( 'NONE',  ( 1.722320550013656915, -61.03663688784501318, -12.71171904440563161 ) ) ;
#5447=CIRCLE ( 'NONE', #39369, 13.94827586206999825 ) ;
#5448=B_SPLINE_CURVE_WITH_KNOTS ( 'NONE', 3,
 ( #12344, #48657, #43935, #35934, #13500, #4056 ),
 .UNSPECIFIED., .F., .F.,
 ( 4, 1, 1, 4 ),
 ( 0.000000000000000000, 0.3333333333333000081, 0.6666666666667000474, 1.000000000000000000 ),
 .UNSPECIFIED. ) ;
#5449=CARTESIAN_POINT ( 'NONE',  ( 10.36597333715451263, -60.57522428980394125, 7.635925938732074592 ) ) ;
#5451=CARTESIAN_POINT ( 'NONE',  ( 11.66345872527999994, -77.61523079875999542, 5.269998857220999255 ) ) ;
#5453=CARTESIAN_POINT ( 'NONE',  ( -12.58335110161999815, -21.74888345808999901, -1.667961430005999945 ) ) ;
#5454=EDGE_CURVE ( 'NONE', #52467, #34093, #5154, .T. ) ;
#5455=CARTESIAN_POINT ( 'NONE',  ( 0.1120494588183876261, -76.57414459540065366, 11.74947323293256574 ) ) ;
#5459=FACE_OUTER_BOUND ( 'NONE', #37962, .T. ) ;
#5463=PLANE ( 'NONE',  #45815 ) ;
#5464=CARTESIAN_POINT ( 'NONE',  ( 3.383845406481000406, -2.529494972095000183, -1.742318191517000070 ) ) ;
#5467=CARTESIAN_POINT ( 'NONE',  ( -11.75000000000000000, -78.79999999999999716, 1.318041981624000073E-14 ) ) ;
#5468=CARTESIAN_POINT ( 'NONE',  ( 8.838834764832000701, -60.04999999966999980, -8.838834764832000701 ) ) ;
#5469=DIRECTION ( 'NONE',  ( 0.7071067811865475727, 0.000000000000000000, 0.7071067811865475727 ) ) ;
#5470=CARTESIAN_POINT ( 'NONE',  ( 1.930989179114000143, -57.04546192861999998, 12.80896991328000034 ) ) ;
#5471=CARTESIAN_POINT ( 'NONE',  ( -9.339950055924999717, -78.00929442844000050, -9.061158367717998985 ) ) ;
#5474=CARTESIAN_POINT ( 'NONE',  ( 9.729416038176543324, -78.49535593849341808, 6.585780853366507870 ) ) ;
#5475=DIRECTION ( 'NONE',  ( 0.7071067811864970576, -3.534294796762985261E-08, 0.7071067811865970887 ) ) ;
#5478=LINE ( 'NONE', #1081, #15371 ) ;
#5481=DIRECTION ( 'NONE',  ( 0.000000000000000000, -1.000000000000000000, 0.000000000000000000 ) ) ;
#5489=ORIENTED_EDGE ( 'NONE', *, *, #8464, .T. ) ;
#5492=ORIENTED_EDGE ( 'NONE', *, *, #41895, .T. ) ;
#5493=CARTESIAN_POINT ( 'NONE',  ( 0.000000000000000000, -0.1000000007601000024, 0.000000000000000000 ) ) ;
#5494=ORIENTED_EDGE ( 'NONE', *, *, #52565, .F. ) ;
#5495=EDGE_LOOP ( 'NONE', ( #15599, #35180, #19449, #12572 ) ) ;
#5496=CARTESIAN_POINT ( 'NONE',  ( -3.066878322771222631, -2.627509113554599374, -1.087878959322058581 ) ) ;
#5497=ORIENTED_EDGE ( 'NONE', *, *, #3738, .F. ) ;
#5500=B_SPLINE_SURFACE_WITH_KNOTS ( 'NONE', 3, 3, ( 
 ( #15776, #46808, #20217, #25208 ),
 ( #33768, #10780, #7206, #52091 ),
 ( #47385, #47095, #38206, #42362 ),
 ( #43227, #42066, #19924, #55939 ),
 ( #42942, #11076, #20783, #15489 ),
 ( #38784, #33479, #42649, #19625 ),
 ( #15191, #56802, #16362, #34342 ),
 ( #28758, #1635, #37622, #55641 ),
 ( #33182, #57375, #21069, #39075 ),
 ( #31062, #43514, #58245, #48524 ),
 ( #30495, #12213, #35794, #22221 ),
 ( #3923, #57950, #57655, #3640 ),
 ( #8068, #8354, #26065, #16648 ),
 ( #17504, #40233, #17807, #8650 ),
 ( #52947, #34632, #11932, #52660 ),
 ( #47962, #44670, #48810, #49100 ),
 ( #21643, #26636, #29909, #44371 ) ),
 .UNSPECIFIED., .F., .F., .F.,
 ( 4, 1, 1, 1, 1, 1, 1, 1, 1, 1, 1, 1, 1, 1, 4 ),
 ( 4, 4 ),
 ( -0.01011408452870000106, 0.000000000000000000, 0.08333333333333001192, 0.1666666666667000196, 0.2500000000000000000, 0.3333333333333000081, 0.4166666666666999919, 0.5000000000000000000, 0.5833333333333000637, 0.6666666666667000474, 0.7500000000000000000, 0.8333333333333000637, 0.9166666666667000474, 1.000000000000000000, 1.010362559107000013 ),
 ( -0.3559705546268999710, 1.357612419602000076 ),
 .UNSPECIFIED. ) ;
#5508=CARTESIAN_POINT ( 'NONE',  ( -12.50728313516488832, -17.00024825485232682, 0.1773838730325038027 ) ) ;
#5509=CARTESIAN_POINT ( 'NONE',  ( -12.51072239526000196, -15.69705297114000331, -0.7871079366006996647 ) ) ;
#5515=CARTESIAN_POINT ( 'NONE',  ( -0.5392637480173118059, -23.41532333361683982, -10.98678411023716883 ) ) ;
#5519=CARTESIAN_POINT ( 'NONE',  ( -0.7823459921530014904, -78.33311419357939087, 12.04988513590113897 ) ) ;
#5522=CARTESIAN_POINT ( 'NONE',  ( -12.78037507862999966, -17.70670131430000183, 1.812742845510000089 ) ) ;
#5526=CARTESIAN_POINT ( 'NONE',  ( 1.247385801072999900, -24.47722256257999973, 12.50301438876999960 ) ) ;
#5527=CARTESIAN_POINT ( 'NONE',  ( 10.01234990226999955, -55.50150862742999891, 7.653559502261000347 ) ) ;
#5530=PLANE ( 'NONE',  #3146 ) ;
#5531=CARTESIAN_POINT ( 'NONE',  ( 12.46165725306000027, -23.67155322522999938, 1.631637378453000053 ) ) ;
#5533=DIRECTION ( 'NONE',  ( -4.529352715887982601E-09, -0.9999999999999983347, 5.940771866771979903E-08 ) ) ;
#5536=CARTESIAN_POINT ( 'NONE',  ( -1.980584515756000030, -23.26485150094000076, -12.76303204340999997 ) ) ;
#5537=CARTESIAN_POINT ( 'NONE',  ( 8.455103393227000552, -75.85439764561999709, -8.811608351744000700 ) ) ;
#5538=ORIENTED_EDGE ( 'NONE', *, *, #6928, .T. ) ;
#5542=CARTESIAN_POINT ( 'NONE',  ( 10.04568514500116372, -54.24913840229667983, 7.921286339673507371 ) ) ;
#5546=CARTESIAN_POINT ( 'NONE',  ( -3.693777716050999693, -1.773066864578999979, 1.600481400925999997 ) ) ;
#5548=CARTESIAN_POINT ( 'NONE',  ( -1.931087888049999979, -55.48415522678000400, 12.71658889739000031 ) ) ;
#5550=EDGE_CURVE ( 'NONE', #32631, #53612, #22841, .T. ) ;
#5552=CARTESIAN_POINT ( 'NONE',  ( -1.782734487936610934, -54.67754631409817279, -12.71547286922772457 ) ) ;
#5554=VECTOR ( 'NONE', #35121, 1000.000000000000000 ) ;
#5559=LINE ( 'NONE', #41581, #18050 ) ;
#5560=ORIENTED_EDGE ( 'NONE', *, *, #43215, .T. ) ;
#5563=CARTESIAN_POINT ( 'NONE',  ( -1.799490220168999954, -19.22870851082999977, 12.64502302238000020 ) ) ;
#5565=CIRCLE ( 'NONE', #7473, 0.6000000000000008660 ) ;
#5570=CARTESIAN_POINT ( 'NONE',  ( 12.78015286808999917, -54.49674784847999831, 1.806262579044999983 ) ) ;
#5571=FACE_OUTER_BOUND ( 'NONE', #42476, .T. ) ;
#5572=CARTESIAN_POINT ( 'NONE',  ( -12.54715528150999937, -24.53180535391000205, -1.292252957172000061 ) ) ;
#5576=CARTESIAN_POINT ( 'NONE',  ( -7.648026766753000416, -60.05000000550000294, 10.12290050090999927 ) ) ;
#5577=CARTESIAN_POINT ( 'NONE',  ( -1.276771495430000038E-14, -69.50420297070000686, 0.000000000000000000 ) ) ;
#5580=CARTESIAN_POINT ( 'NONE',  ( 8.485281374238999419, -23.25000000000000000, -8.485281374238999419 ) ) ;
#5581=ORIENTED_EDGE ( 'NONE', *, *, #5283, .T. ) ;
#5582=CARTESIAN_POINT ( 'NONE',  ( 10.69843650790000034, -76.30851016852000157, 6.089250768039999429 ) ) ;
#5583=CARTESIAN_POINT ( 'NONE',  ( -2.692194317453766139, -1.904912773971035422, -2.265922085054583146 ) ) ;
#5584=TOROIDAL_SURFACE ( 'NONE', #17842, 13.50000000000000000, 0.5000000000000000000 ) ;
#5586=CARTESIAN_POINT ( 'NONE',  ( -10.61911868076999887, -78.55902054102001841, -6.134606423928000041 ) ) ;
#5590=CARTESIAN_POINT ( 'NONE',  ( 3.249343497640856615, -2.845515713985523831, -0.2278308301013699799 ) ) ;
#5591=CARTESIAN_POINT ( 'NONE',  ( 10.49839420453927197, -77.34045593712866662, 5.848571948716326574 ) ) ;
#5595=B_SPLINE_CURVE_WITH_KNOTS ( 'NONE', 3,
 ( #28308, #41910, #46652, #36886, #37180, #54898, #14449, #1483 ),
 .UNSPECIFIED., .F., .F.,
 ( 4, 2, 2, 4 ),
 ( 0.000000000000000000, 0.5000000000000009992, 0.7500000000000004441, 1.000000000000000000 ),
 .UNSPECIFIED. ) ;
#5600=CARTESIAN_POINT ( 'NONE',  ( 2.151784307624999837, -2.466290364169000604, -3.217165252942999931 ) ) ;
#5601=AXIS2_PLACEMENT_3D ( 'NONE', #36146, #40871, #4270 ) ;
#5605=CARTESIAN_POINT ( 'NONE',  ( 5.917544427059681311, -76.03248552931820825, 10.15932382542081669 ) ) ;
#5606=B_SPLINE_CURVE_WITH_KNOTS ( 'NONE', 3,
 ( #32112, #51027, #14688, #28559, #54284, #50153, #14400, #6133 ),
 .UNSPECIFIED., .F., .F.,
 ( 4, 2, 2, 4 ),
 ( 0.000000000000000000, 0.4999999999999977796, 0.7499999999999988898, 1.000000000000000000 ),
 .UNSPECIFIED. ) ;
#5609=ORIENTED_EDGE ( 'NONE', *, *, #876, .F. ) ;
#5611=ADVANCED_FACE ( 'NONE', ( #43711 ), #57682, .F. ) ;
#5613=CARTESIAN_POINT ( 'NONE',  ( 12.56594317991999965, -60.04999999381999487, 1.750000000001000089 ) ) ;
#5617=CARTESIAN_POINT ( 'NONE',  ( 0.000000000000000000, -63.73717104351998586, 0.000000000000000000 ) ) ;
#5618=CARTESIAN_POINT ( 'NONE',  ( 7.645391692608000334, -18.78469634161999835, -10.18949678827999961 ) ) ;
#5619=CARTESIAN_POINT ( 'NONE',  ( 9.019406119853890402, -17.00707871055414344, 8.666949039025178436 ) ) ;
#5625=CARTESIAN_POINT ( 'NONE',  ( 7.723332765951321122, -77.77272290370588337, 9.278744632980441054 ) ) ;
#5626=EDGE_CURVE ( 'NONE', #54609, #44143, #16839, .T. ) ;
#5627=CARTESIAN_POINT ( 'NONE',  ( 12.54435915808562108, -60.32412882177209212, 1.733925320397567305 ) ) ;
#5628=DIRECTION ( 'NONE',  ( 0.000000000000000000, 1.000000000000000000, 0.000000000000000000 ) ) ;
#5633=DIRECTION ( 'NONE',  ( -0.7071067811865475727, 0.000000000000000000, 0.7071067811865475727 ) ) ;
#5635=CARTESIAN_POINT ( 'NONE',  ( -12.50386483995777809, -61.58505343581191482, 0.8574420495993835267 ) ) ;
#5646=CARTESIAN_POINT ( 'NONE',  ( 7.657745562928999661, -60.46920625093000012, 9.966193613345000202 ) ) ;
#5650=B_SPLINE_CURVE_WITH_KNOTS ( 'NONE', 3,
 ( #13598, #18632, #50511, #934, #13894, #31888 ),
 .UNSPECIFIED., .F., .F.,
 ( 4, 2, 4 ),
 ( 0.000000000000000000, 0.5000000000000001110, 1.000000000000000000 ),
 .UNSPECIFIED. ) ;
#5651=ORIENTED_EDGE ( 'NONE', *, *, #51191, .F. ) ;
#5652=CARTESIAN_POINT ( 'NONE',  ( 0.000000000000000000, -39.30476017083000073, 0.000000000000000000 ) ) ;
#5653=ORIENTED_EDGE ( 'NONE', *, *, #41879, .F. ) ;
#5657=CARTESIAN_POINT ( 'NONE',  ( -7.954951288349001004, -23.25000000000000000, -9.722718241315000398 ) ) ;
#5659=CARTESIAN_POINT ( 'NONE',  ( 1.063278045107967973, -2.151263346416249167, -3.097506788382764498 ) ) ;
#5664=CARTESIAN_POINT ( 'NONE',  ( 12.70228857843095227, -61.62190589586192857, 1.213561371183882187 ) ) ;
#5667=AXIS2_PLACEMENT_3D ( 'NONE', #4193, #57917, #35464 ) ;
#5668=ORIENTED_EDGE ( 'NONE', *, *, #16533, .T. ) ;
#5669=CARTESIAN_POINT ( 'NONE',  ( 0.6999999999999999556, -21.00000000000000000, -11.90000000000000036 ) ) ;
#5673=CARTESIAN_POINT ( 'NONE',  ( 0.4254240051736068451, -3.364583333333333481, 3.250000000000001776 ) ) ;
#5674=LINE ( 'NONE', #36386, #44044 ) ;
#5675=CARTESIAN_POINT ( 'NONE',  ( -1.344596514747811611, -3.156225089547542328, 3.253962609497633718 ) ) ;
#5681=CARTESIAN_POINT ( 'NONE',  ( 2.083499196047589042, -0.8606770703554429414, -2.709727116747193687 ) ) ;
#5683=ORIENTED_EDGE ( 'NONE', *, *, #5166, .T. ) ;
#5684=B_SPLINE_CURVE_WITH_KNOTS ( 'NONE', 3,
 ( #28235, #46286, #35116, #553, #45405, #45106, #53150, #36230, #12697, #36812, #14087, #30692, #9080, #4659, #13786, #31786, #4946, #49830 ),
 .UNSPECIFIED., .F., .F.,
 ( 4, 2, 2, 2, 2, 2, 2, 2, 4 ),
 ( 0.000000000000000000, 0.1250000000000000833, 0.2500000000000001665, 0.3750000000000001110, 0.5000000000000001110, 0.6250000000000001110, 0.7500000000000000000, 0.8750000000000000000, 1.000000000000000000 ),
 .UNSPECIFIED. ) ;
#5689=CARTESIAN_POINT ( 'NONE',  ( 7.659225027811000786, -23.68266641665999828, -9.963489011784998794 ) ) ;
#5692=CARTESIAN_POINT ( 'NONE',  ( -7.764220096216667422, -54.54399029303478841, -10.21028322253899923 ) ) ;
#5696=ADVANCED_FACE ( 'NONE', ( #38261 ), #12463, .F. ) ;
#5697=CARTESIAN_POINT ( 'NONE',  ( 10.36221646771999971, -55.57876216348000042, -7.631895822728999690 ) ) ;
#5698=CARTESIAN_POINT ( 'NONE',  ( -12.76303204513999923, -55.53514852210999919, 1.980584515753000208 ) ) ;
#5708=EDGE_LOOP ( 'NONE', ( #19589, #23469, #13835 ) ) ;
#5709=CARTESIAN_POINT ( 'NONE',  ( 13.97864847851000114, -45.76668425569999954, 0.0001086640162475999876 ) ) ;
#5711=ADVANCED_FACE ( 'NONE', ( #4877 ), #49761, .F. ) ;
#5713=CARTESIAN_POINT ( 'NONE',  ( 0.000000000000000000, 4.040000000000000036, 0.000000000000000000 ) ) ;
#5714=ORIENTED_EDGE ( 'NONE', *, *, #4110, .F. ) ;
#5717=B_SPLINE_CURVE_WITH_KNOTS ( 'NONE', 3,
 ( #56424, #11557, #42558, #56135, #15974, #33966 ),
 .UNSPECIFIED., .F., .F.,
 ( 4, 2, 4 ),
 ( 0.000000000000000000, 0.5000000000000000000, 1.000000000000000000 ),
 .UNSPECIFIED. ) ;
#5718=EDGE_LOOP ( 'NONE', ( #56477, #25652, #27852, #49998 ) ) ;
#5720=CARTESIAN_POINT ( 'NONE',  ( -0.5045596072232000351, -16.86471086961999788, 12.66210649709999991 ) ) ;
#5722=PRODUCT_CONTEXT ( 'NONE', #14927, 'mechanical' ) ;
#5726=ORIENTED_EDGE ( 'NONE', *, *, #52089, .F. ) ;
#5727=ORIENTED_EDGE ( 'NONE', *, *, #33780, .T. ) ;
#5729=AXIS2_PLACEMENT_3D ( 'NONE', #44908, #46091, #36039 ) ;
#5732=ADVANCED_FACE ( 'NONE', ( #53586, #40883 ), #40596, .F. ) ;
#5733=CARTESIAN_POINT ( 'NONE',  ( -1.308715794653438680, -61.54404499166313514, -12.70256747361121796 ) ) ;
#5736=DIRECTION ( 'NONE',  ( -1.000000000000000000, 0.000000000000000000, 0.000000000000000000 ) ) ;
#5737=CARTESIAN_POINT ( 'NONE',  ( -10.18589226631999978, -23.28917723430000208, 7.641012305222999679 ) ) ;
#5741=CARTESIAN_POINT ( 'NONE',  ( -9.160327239603146765, -76.64595974771152953, 7.362753168639923018 ) ) ;
#5747=LINE ( 'NONE', #18753, #48561 ) ;
#5750=CARTESIAN_POINT ( 'NONE',  ( 9.708203932494999577, -79.25000000000000000, 7.053423027515000499 ) ) ;
#5751=CARTESIAN_POINT ( 'NONE',  ( 1.432628882339999965, -2.473043513114999925, -3.526139092948999743 ) ) ;
#5754=CARTESIAN_POINT ( 'NONE',  ( -11.74999999999999645, -78.80833333333335133, -1.230457122656147373 ) ) ;
#5755=CARTESIAN_POINT ( 'NONE',  ( -0.5245219981418175470, -18.54839576653561650, -10.98753021428655963 ) ) ;
#5759=CARTESIAN_POINT ( 'NONE',  ( 1.750000000000000000, -20.25022860793999868, -12.65375411744000012 ) ) ;
#5762=EDGE_CURVE ( 'NONE', #56208, #800, #6321, .T. ) ;
#5763=FACE_OUTER_BOUND ( 'NONE', #43493, .T. ) ;
#5765=ADVANCED_FACE ( 'NONE', ( #37611 ), #28477, .T. ) ;
#5767=FACE_OUTER_BOUND ( 'NONE', #25602, .T. ) ;
#5771=FACE_OUTER_BOUND ( 'NONE', #47647, .T. ) ;
#5773=CARTESIAN_POINT ( 'NONE',  ( -1.750000000001000089, -18.75000001325000198, -12.56594318051000059 ) ) ;
#5775=CARTESIAN_POINT ( 'NONE',  ( -9.722718241315000398, -18.75000000000000000, 7.954951288349001004 ) ) ;
#5779=EDGE_LOOP ( 'NONE', ( #25005, #32198, #38244, #35085, #57341, #43560 ) ) ;
#5780=ORIENTED_EDGE ( 'NONE', *, *, #30745, .T. ) ;
#5783=EDGE_CURVE ( 'NONE', #8187, #26499, #56773, .T. ) ;
#5785=VERTEX_POINT ( 'NONE', #55334 ) ;
#5793=ORIENTED_EDGE ( 'NONE', *, *, #3738, .T. ) ;
#5794=DIRECTION ( 'NONE',  ( 0.000000000000000000, -1.000000000000000000, 0.000000000000000000 ) ) ;
#5795=CARTESIAN_POINT ( 'NONE',  ( -7.642147947524999374, -56.01514526721999943, 10.55910102243999837 ) ) ;
#5796=ORIENTED_EDGE ( 'NONE', *, *, #40776, .T. ) ;
#5800=DIRECTION ( 'NONE',  ( -0.7071067811865475727, 0.000000000000000000, -0.7071067811865475727 ) ) ;
#5801=CARTESIAN_POINT ( 'NONE',  ( -12.26179901070890566, -78.95175067907904065, -0.2371216807744343236 ) ) ;
#5804=DIRECTION ( 'NONE',  ( 0.000000000000000000, -1.000000000000000000, 0.000000000000000000 ) ) ;
#5805=CARTESIAN_POINT ( 'NONE',  ( -7.691893942725999800, -58.55453807205000061, -10.42272502862000039 ) ) ;
#5810=CARTESIAN_POINT ( 'NONE',  ( 0.6454797250853000490, -61.68806512111272156, -12.50471521371631312 ) ) ;
#5815=CARTESIAN_POINT ( 'NONE',  ( -12.72558083409999874, -18.79866855842000106, 1.930284430576000076 ) ) ;
#5820=FACE_OUTER_BOUND ( 'NONE', #57311, .T. ) ;
#5821=FACE_OUTER_BOUND ( 'NONE', #35757, .T. ) ;
#5822=CARTESIAN_POINT ( 'NONE',  ( -1.798336774608999988, -23.19644498052000259, -12.61277771566000006 ) ) ;
#5823=DIRECTION ( 'NONE',  ( 0.000000000000000000, 0.000000000000000000, -1.000000000000000000 ) ) ;
#5824=CARTESIAN_POINT ( 'NONE',  ( -1.898295385589999995, -2.623547659066999937, -2.923300871422000125 ) ) ;
#5825=CARTESIAN_POINT ( 'NONE',  ( 12.54673765596000123, -24.82199238237999950, 0.9174244429638999110 ) ) ;
#5827=DIRECTION ( 'NONE',  ( 0.000000000000000000, 0.000000000000000000, -1.000000000000000000 ) ) ;
#5828=CARTESIAN_POINT ( 'NONE',  ( 1.758095523364999968, -60.52291663846999370, 12.57362173518999882 ) ) ;
#5829=CARTESIAN_POINT ( 'NONE',  ( -1.495357591793033514, -24.55876337360558281, -12.70444646759402119 ) ) ;
#5830=CARTESIAN_POINT ( 'NONE',  ( -4.573833614540000703, -76.66157131458999174, 11.16101939607000126 ) ) ;
#5837=DIRECTION ( 'NONE',  ( 0.000000000000000000, 0.000000000000000000, 1.000000000000000000 ) ) ;
#5842=DIRECTION ( 'NONE',  ( -0.7071067811865475727, 0.000000000000000000, 0.7071067811865475727 ) ) ;
#5845=CARTESIAN_POINT ( 'NONE',  ( -1.741532119305578830, -0.7916666666665673757, 3.009437940290339064 ) ) ;
#5848=ORIENTED_EDGE ( 'NONE', *, *, #55863, .F. ) ;
#5850=ADVANCED_FACE ( 'NONE', ( #1917 ), #14879, .F. ) ;
#5852=EDGE_LOOP ( 'NONE', ( #33994, #24458, #41513, #38254 ) ) ;
#5855=CARTESIAN_POINT ( 'NONE',  ( 8.894916816534065518, -62.02809132899625411, -9.073484344827472015 ) ) ;
#5857=ORIENTED_EDGE ( 'NONE', *, *, #49509, .T. ) ;
#5858=ORIENTED_EDGE ( 'NONE', *, *, #29337, .T. ) ;
#5859=CARTESIAN_POINT ( 'NONE',  ( -10.53562613913000057, -55.59442116235999976, -7.620013630307000518 ) ) ;
#5861=ORIENTED_EDGE ( 'NONE', *, *, #18056, .T. ) ;
#5862=CARTESIAN_POINT ( 'NONE',  ( 12.43410192427999839, -54.35868879854000113, 1.192687910178000132 ) ) ;
#5863=CARTESIAN_POINT ( 'NONE',  ( 8.803747447820532201, -25.21568152340251601, -9.164340453613974091 ) ) ;
#5864=EDGE_LOOP ( 'NONE', ( #27262, #37310, #20014 ) ) ;
#5865=CARTESIAN_POINT ( 'NONE',  ( -12.48409101788000086, -23.36970703835000052, -1.669510252625999946 ) ) ;
#5866=CARTESIAN_POINT ( 'NONE',  ( 8.666912951388480835, -24.99291380871280310, 9.019442093124220960 ) ) ;
#5867=PLANE ( 'NONE',  #33836 ) ;
#5869=FACE_OUTER_BOUND ( 'NONE', #30671, .T. ) ;
#5870=CARTESIAN_POINT ( 'NONE',  ( 8.130813118010999929, -17.31476110167000115, -9.546856411651999608 ) ) ;
#5872=CARTESIAN_POINT ( 'NONE',  ( -12.70228549161442544, -17.17187149261430079, -1.205357499388056475 ) ) ;
#5874=CARTESIAN_POINT ( 'NONE',  ( 10.36746145411186149, -18.23400545010334284, 7.635225828759837796 ) ) ;
#5876=CARTESIAN_POINT ( 'NONE',  ( -3.151328970204000157, -76.12173232274999179, -11.89977497056000111 ) ) ;
#5877=ADVANCED_FACE ( 'NONE', ( #45623 ), #27547, .F. ) ;
#5879=CARTESIAN_POINT ( 'NONE',  ( 7.760939450761999758, -61.03085356300000086, -10.15321588361999972 ) ) ;
#5880=CARTESIAN_POINT ( 'NONE',  ( 4.750030159171999777, -78.63931674665001026, -11.30647155123999958 ) ) ;
#5882=CARTESIAN_POINT ( 'NONE',  ( -10.14948852603999896, -56.04899164556000102, -7.674614791885000287 ) ) ;
#5883=ADVANCED_FACE ( 'NONE', ( #10468 ), #14318, .F. ) ;
#5884=CARTESIAN_POINT ( 'NONE',  ( 12.50385649908071173, -24.78436723039533263, 0.8579675316851195221 ) ) ;
#5885=CARTESIAN_POINT ( 'NONE',  ( 9.134039069024126434, -78.24329585021101252, -7.883706473441567830 ) ) ;
#5886=DIRECTION ( 'NONE',  ( 0.000000000000000000, -1.000000000000000000, 0.000000000000000000 ) ) ;
#5887=VERTEX_POINT ( 'NONE', #32582 ) ;
#5888=LINE ( 'NONE', #23896, #496 ) ;
#5891=AXIS2_PLACEMENT_3D ( 'NONE', #45702, #41839, #36815 ) ;
#5893=CARTESIAN_POINT ( 'NONE',  ( 2.011257834211999995, -2.625894741107999586, 3.306836841438999919 ) ) ;
#5896=CARTESIAN_POINT ( 'NONE',  ( -10.84963681563615800, -76.16850844397271203, 4.510596736791835148 ) ) ;
#5900=CARTESIAN_POINT ( 'NONE',  ( 12.70556836347999941, -25.22772277227999993, 2.424222353299999887E-09 ) ) ;
#5901=AXIS2_PLACEMENT_3D ( 'NONE', #56671, #53384, #2659 ) ;
#5902=CARTESIAN_POINT ( 'NONE',  ( 11.71941206009442205, -79.16681733756954031, 2.493429747108907968 ) ) ;
#5903=EDGE_CURVE ( 'NONE', #3955, #31290, #3045, .T. ) ;
#5904=CARTESIAN_POINT ( 'NONE',  ( 3.250000000000000444, -2.260416666666666075, 0.4254240051736248862 ) ) ;
#5909=CARTESIAN_POINT ( 'NONE',  ( 9.516265623875000301, -17.17460635740999919, -8.227505979428000771 ) ) ;
#5910=CARTESIAN_POINT ( 'NONE',  ( 13.13047446164998711, -59.58578169018999660, 0.8260994316375004365 ) ) ;
#5914=CARTESIAN_POINT ( 'NONE',  ( 12.70228549161202380, -17.17187149263573431, 1.205357499442098357 ) ) ;
#5915=CARTESIAN_POINT ( 'NONE',  ( 12.50240633875000107, -54.11762602111000575, 1.005381409374000112 ) ) ;
#5917=CARTESIAN_POINT ( 'NONE',  ( -9.191912067484826920, -77.89725430145915652, 7.750011545041279426 ) ) ;
#5920=ADVANCED_FACE ( 'NONE', ( #55926 ), #23743, .F. ) ;
#5923=CARTESIAN_POINT ( 'NONE',  ( -3.453171399369999950, -1.763032031398999999, -0.5706200895263999762 ) ) ;
#5926=CARTESIAN_POINT ( 'NONE',  ( 1.980464439859999981, -21.75472017459999918, 12.85144117154000121 ) ) ;
#5928=B_SPLINE_CURVE_WITH_KNOTS ( 'NONE', 3,
 ( #46361, #41329, #18897, #36888, #23605, #19187 ),
 .UNSPECIFIED., .F., .F.,
 ( 4, 2, 4 ),
 ( 0.000000000000000000, 0.5000000000000000000, 1.000000000000000000 ),
 .UNSPECIFIED. ) ;
#5929=CARTESIAN_POINT ( 'NONE',  ( -12.50240681836000078, -61.48234730679999416, 1.005418944265999981 ) ) ;
#5930=VERTEX_POINT ( 'NONE', #19326 ) ;
#5931=EDGE_LOOP ( 'NONE', ( #45682, #29591, #161, #5653 ) ) ;
#5934=EDGE_LOOP ( 'NONE', ( #36366, #42448, #44872, #50823 ) ) ;
#5936=ADVANCED_FACE ( 'NONE', ( #51215 ), #10767, .F. ) ;
#5939=CARTESIAN_POINT ( 'NONE',  ( 7.633478499842999199, -60.00098177563999968, 10.36292345936000103 ) ) ;
#5944=EDGE_LOOP ( 'NONE', ( #49107, #34783, #6236, #11329, #6594 ) ) ;
#5945=CARTESIAN_POINT ( 'NONE',  ( -8.620921567869039848, -25.16528830419391838, 9.346042574068809117 ) ) ;
#5946=ORIENTED_EDGE ( 'NONE', *, *, #2953, .T. ) ;
#5953=FACE_OUTER_BOUND ( 'NONE', #21749, .T. ) ;
#5959=CARTESIAN_POINT ( 'NONE',  ( 12.71536556660652728, -60.92544729019407157, 1.781281568951020411 ) ) ;
#5969=CARTESIAN_POINT ( 'NONE',  ( 2.908337012396843946, -3.047664591510003795, 1.983095937705898537 ) ) ;
#5974=CARTESIAN_POINT ( 'NONE',  ( 0.8930464934706795477, -0.8411458150437891579, -3.319805051666669726 ) ) ;
#5978=CARTESIAN_POINT ( 'NONE',  ( -2.015551294784000191, -60.60347704811000824, -12.79857978897999971 ) ) ;
#5982=CARTESIAN_POINT ( 'NONE',  ( 7.765022563360999719, -24.09093562100999719, -9.830785949113998612 ) ) ;
#5984=DIRECTION ( 'NONE',  ( -0.7071067811865474617, 0.000000000000000000, -0.7071067811865474617 ) ) ;
#5985=CYLINDRICAL_SURFACE ( 'NONE', #28649, 1.750000000000001332 ) ;
#5989=CARTESIAN_POINT ( 'NONE',  ( 10.47513558171999826, -54.99636614397000045, -7.624778817986999968 ) ) ;
#5990=B_SPLINE_CURVE_WITH_KNOTS ( 'NONE', 3,
 ( #24471, #28003, #46052, #23301, #15320, #5576 ),
 .UNSPECIFIED., .F., .F.,
 ( 4, 1, 1, 4 ),
 ( 0.000000000000000000, 0.3333333333333000081, 0.6666666666667000474, 1.000000000000000000 ),
 .UNSPECIFIED. ) ;
#5994=CARTESIAN_POINT ( 'NONE',  ( -10.42531125074000009, -18.73514854687000053, -7.624341767140999870 ) ) ;
#5999=VECTOR ( 'NONE', #55637, 1000.000000000000000 ) ;
#6002=CIRCLE ( 'NONE', #47503, 1.750000000000001332 ) ;
#6005=FACE_OUTER_BOUND ( 'NONE', #29861, .T. ) ;
#6006=ORIENTED_EDGE ( 'NONE', *, *, #25191, .F. ) ;
#6007=EDGE_LOOP ( 'NONE', ( #41524, #49854, #14002, #10084, #38176, #29632, #12360 ) ) ;
#6009=ORIENTED_EDGE ( 'NONE', *, *, #32194, .F. ) ;
#6011=CYLINDRICAL_SURFACE ( 'NONE', #47197, 1.750000000000001332 ) ;
#6019=ORIENTED_EDGE ( 'NONE', *, *, #28429, .T. ) ;
#6020=EDGE_LOOP ( 'NONE', ( #53272, #45084, #32049 ) ) ;
#6022=CARTESIAN_POINT ( 'NONE',  ( -12.70395504299446188, -24.60679290123326268, 1.447100708826857263 ) ) ;
#6023=DIRECTION ( 'NONE',  ( 0.000000000000000000, 1.000000000000000000, 0.000000000000000000 ) ) ;
#6024=FACE_OUTER_BOUND ( 'NONE', #26761, .T. ) ;
#6027=CARTESIAN_POINT ( 'NONE',  ( -10.01234990228999955, -23.29849137228000444, 7.653559502275999016 ) ) ;
#6029=EDGE_CURVE ( 'NONE', #36474, #35786, #56796, .T. ) ;
#6031=AXIS2_PLACEMENT_3D ( 'NONE', #34867, #3310, #30443 ) ;
#6037=CARTESIAN_POINT ( 'NONE',  ( -7.619389775686000732, -18.59213701582999789, -10.35398629635000134 ) ) ;
#6039=CARTESIAN_POINT ( 'NONE',  ( 13.89248034750000116, -32.39159251014999796, 2.632538495369999938E-05 ) ) ;
#6045=VERTEX_POINT ( 'NONE', #29613 ) ;
#6046=CARTESIAN_POINT ( 'NONE',  ( -2.895491044260078528, -3.500000000000000000, -1.620397986153582437 ) ) ;
#6050=CARTESIAN_POINT ( 'NONE',  ( 12.43641409355999983, -61.71801033862000452, 0.03481937293210000256 ) ) ;
#6052=CARTESIAN_POINT ( 'NONE',  ( -8.048032176077001054, -78.37932536818000528, 9.328081102756000220 ) ) ;
#6057=CIRCLE ( 'NONE', #46628, 0.5000000000000000000 ) ;
#6060=CARTESIAN_POINT ( 'NONE',  ( -12.00000000000000000, -18.75000000000000000, 0.000000000000000000 ) ) ;
#6062=CARTESIAN_POINT ( 'NONE',  ( -3.250000000000001776, -2.989583333333332593, 0.4254240051736045136 ) ) ;
#6064=CARTESIAN_POINT ( 'NONE',  ( -7.648026768036999989, -60.04999998387000204, -10.12290050219000115 ) ) ;
#6066=ADVANCED_FACE ( 'NONE', ( #11063 ), #7752, .T. ) ;
#6067=VECTOR ( 'NONE', #25506, 1000.000000000000000 ) ;
#6072=ORIENTED_EDGE ( 'NONE', *, *, #10519, .F. ) ;
#6074=AXIS2_PLACEMENT_3D ( 'NONE', #30668, #26251, #8839 ) ;
#6076=CARTESIAN_POINT ( 'NONE',  ( 3.250000000000000000, -2.750000000000000000, 0.000000000000000000 ) ) ;
#6077=VERTEX_POINT ( 'NONE', #3346 ) ;
#6079=ORIENTED_EDGE ( 'NONE', *, *, #20325, .T. ) ;
#6080=ORIENTED_EDGE ( 'NONE', *, *, #6297, .F. ) ;
#6085=EDGE_LOOP ( 'NONE', ( #13756, #45817, #13416 ) ) ;
#6087=CARTESIAN_POINT ( 'NONE',  ( -7.642160924878999673, -59.58461666436000570, 10.55911395187000146 ) ) ;
#6089=CARTESIAN_POINT ( 'NONE',  ( 1.749899258077703301, -18.61283151237005740, 12.55433901290730603 ) ) ;
#6092=DIRECTION ( 'NONE',  ( 0.000000000000000000, -1.000000000000000000, 0.000000000000000000 ) ) ;
#6093=CARTESIAN_POINT ( 'NONE',  ( 9.889722810339758752, -78.75056565254401164, 7.252677050776306089 ) ) ;
#6099=CIRCLE ( 'NONE', #29644, 14.00000000000000355 ) ;
#6100=CARTESIAN_POINT ( 'NONE',  ( -7.655542440085000067, -59.57819125629999490, -10.38645071868999992 ) ) ;
#6102=CARTESIAN_POINT ( 'NONE',  ( 3.194637145771936027, -76.55251996074613885, 11.30859510570057402 ) ) ;
#6103=CARTESIAN_POINT ( 'NONE',  ( 1.980464439859999981, -20.24527982672000093, -12.85144117157999943 ) ) ;
#6107=CARTESIAN_POINT ( 'NONE',  ( -3.137524286708853971, -3.080320021855812662, 0.8496376415343023236 ) ) ;
#6112=CARTESIAN_POINT ( 'NONE',  ( -7.159979337456084281, -76.27258029778182902, -9.317074303591205364 ) ) ;
#6114=DIRECTION ( 'NONE',  ( -0.7071067811865474617, 0.000000000000000000, 0.7071067811865474617 ) ) ;
#6115=CIRCLE ( 'NONE', #57027, 14.00000000000000000 ) ;
#6116=CARTESIAN_POINT ( 'NONE',  ( 0.2218469911736734856, -3.500000000000000888, 3.293143398893245699 ) ) ;
#6117=ADVANCED_FACE ( 'NONE', ( #12202 ), #11918, .F. ) ;
#6118=CARTESIAN_POINT ( 'NONE',  ( 10.53101990617999917, -55.49360215019999742, 7.613962745591999592 ) ) ;
#6122=CARTESIAN_POINT ( 'NONE',  ( 12.77651047016999897, -25.30895689136000115, -0.04321256188106999824 ) ) ;
#6124=DIRECTION ( 'NONE',  ( 0.000000000000000000, 0.000000000000000000, -1.000000000000000000 ) ) ;
#6126=CARTESIAN_POINT ( 'NONE',  ( 11.65748953279999967, -76.39446726005000698, -3.638198820018999857 ) ) ;
#6127=ORIENTED_EDGE ( 'NONE', *, *, #51212, .T. ) ;
#6132=CARTESIAN_POINT ( 'NONE',  ( 1.025029370886000101E-14, -0.2000000000000005107, 0.000000000000000000 ) ) ;
#6133=CARTESIAN_POINT ( 'NONE',  ( 10.12290050253000118, -23.24999997822999731, -7.648026768374000639 ) ) ;
#6138=EDGE_CURVE ( 'NONE', #56909, #1239, #29045, .T. ) ;
#6139=ORIENTED_EDGE ( 'NONE', *, *, #28890, .T. ) ;
#6140=CARTESIAN_POINT ( 'NONE',  ( 0.000000000000000000, -55.54999999966999980, -12.00000000000000000 ) ) ;
#6141=DIRECTION ( 'NONE',  ( 4.529347781562982494E-09, -0.9999999999999983347, -5.940771729776980447E-08 ) ) ;
#6146=VECTOR ( 'NONE', #19354, 1000.000000000000114 ) ;
#6150=AXIS2_PLACEMENT_3D ( 'NONE', #13127, #16420, #58011 ) ;
#6151=CARTESIAN_POINT ( 'NONE',  ( 9.697372265369082811, -61.77233735005967219, -8.266620275728030265 ) ) ;
#6152=EDGE_LOOP ( 'NONE', ( #45299, #47353, #24603 ) ) ;
#6153=EDGE_CURVE ( 'NONE', #49275, #27979, #47954, .T. ) ;
#6154=VERTEX_POINT ( 'NONE', #38194 ) ;
#6156=AXIS2_PLACEMENT_3D ( 'NONE', #18102, #40232, #41408 ) ;
#6160=CARTESIAN_POINT ( 'NONE',  ( 12.65989785476000051, -53.85665906507999523, 0.9744897697748999832 ) ) ;
#6161=CARTESIAN_POINT ( 'NONE',  ( 7.610436523679670273, -23.52540704710936126, -10.41144397132592836 ) ) ;
#6163=CARTESIAN_POINT ( 'NONE',  ( -12.61277705613999878, -23.19666672528000007, -1.798399175679999740 ) ) ;
#6166=CARTESIAN_POINT ( 'NONE',  ( 1.980584515756000030, -18.73514849905999924, -12.76303204340999997 ) ) ;
#6169=DIRECTION ( 'NONE',  ( -0.7026410690473250398, 0.1122098755728047209, 0.7026410690473250398 ) ) ;
#6172=ADVANCED_FACE ( 'NONE', ( #25774 ), #53011, .F. ) ;
#6173=CARTESIAN_POINT ( 'NONE',  ( 5.894077591580000330, -76.68206586006000691, -10.80721126921000064 ) ) ;
#6174=CARTESIAN_POINT ( 'NONE',  ( 0.3280756968000912988, -1.981646559566586419, -3.506079728219933411 ) ) ;
#6175=CARTESIAN_POINT ( 'NONE',  ( -13.86363625866319715, -9.638971321655001034, -0.001706075946107427034 ) ) ;
#6176=CARTESIAN_POINT ( 'NONE',  ( -12.10179013622999911, -78.53027982294000253, -1.986401539992999954 ) ) ;
#6178=CARTESIAN_POINT ( 'NONE',  ( 12.76303204517000012, -18.73514852243999940, -1.980584515753000208 ) ) ;
#6179=CARTESIAN_POINT ( 'NONE',  ( 3.160362247288924564, -2.832624405079319452, -0.7606606948156037218 ) ) ;
#6180=CARTESIAN_POINT ( 'NONE',  ( 2.319020911157693821, -77.90973430596969251, 11.89852370548304172 ) ) ;
#6183=ORIENTED_EDGE ( 'NONE', *, *, #48931, .T. ) ;
#6186=CARTESIAN_POINT ( 'NONE',  ( 10.21026636380264740, -24.25606635949579371, 7.764233071689755405 ) ) ;
#6188=CARTESIAN_POINT ( 'NONE',  ( 3.108770384767000294, -3.085385803691999662, -2.032239610727000212 ) ) ;
#6191=CARTESIAN_POINT ( 'NONE',  ( -7.980753701116782395, -76.13439855002184231, 8.624097217009085270 ) ) ;
#6192=CARTESIAN_POINT ( 'NONE',  ( 10.28236248476030390, -76.80731616818275143, -6.022669235425634149 ) ) ;
#6196=CARTESIAN_POINT ( 'NONE',  ( 10.04991969245749672, -76.75384563621365430, -6.584037273805950718 ) ) ;
#6198=CARTESIAN_POINT ( 'NONE',  ( -3.075537641221531615, -76.90416666666666856, -11.44417895085270942 ) ) ;
#6200=CYLINDRICAL_SURFACE ( 'NONE', #20452, 0.5000000000000006661 ) ;
#6202=CARTESIAN_POINT ( 'NONE',  ( 10.52682159591000044, -18.57432398260000284, -7.605688676868000542 ) ) ;
#6203=CARTESIAN_POINT ( 'NONE',  ( 0.000000000000000000, -63.10294702885996543, -12.53545825868000207 ) ) ;
#6209=CARTESIAN_POINT ( 'NONE',  ( -11.89252178239981994, -77.93728225073550675, 2.372833624312832956 ) ) ;
#6212=CARTESIAN_POINT ( 'NONE',  ( -12.50000000000000000, -54.11762331445000029, -1.005384021965999963 ) ) ;
#6213=CARTESIAN_POINT ( 'NONE',  ( 2.113064247614999669, -3.419836441412999584, -3.165785623842000351 ) ) ;
#6214=EDGE_CURVE ( 'NONE', #40639, #56888, #21802, .T. ) ;
#6219=VECTOR ( 'NONE', #18548, 1000.000000000000000 ) ;
#6220=DIRECTION ( 'NONE',  ( 0.7071067811865475727, 0.000000000000000000, 0.7071067811865475727 ) ) ;
#6221=ORIENTED_EDGE ( 'NONE', *, *, #49369, .T. ) ;
#6226=CARTESIAN_POINT ( 'NONE',  ( 7.620037552712999762, -18.79433113555000290, 10.53559761427999852 ) ) ;
#6227=CIRCLE ( 'NONE', #50588, 14.00000000000000000 ) ;
#6229=CARTESIAN_POINT ( 'NONE',  ( 6.497627649074000367, -78.57347311384999955, 9.985601457511998902 ) ) ;
#6230=CARTESIAN_POINT ( 'NONE',  ( 10.18948929999999997, -60.01532694310999716, 7.645397820753000673 ) ) ;
#6236=ORIENTED_EDGE ( 'NONE', *, *, #6888, .F. ) ;
#6237=ADVANCED_FACE ( 'NONE', ( #5953 ), #28085, .F. ) ;
#6246=LINE ( 'NONE', #47014, #56474 ) ;
#6247=CARTESIAN_POINT ( 'NONE',  ( -7.619712170649999727, -23.40404510063000032, -10.35409959310000083 ) ) ;
#6251=EDGE_LOOP ( 'NONE', ( #44053, #35015, #49209, #17164, #46921 ) ) ;
#6253=CARTESIAN_POINT ( 'NONE',  ( 7.919595949288999570, -55.64999999965999677, -8.768124086712999699 ) ) ;
#6257=CARTESIAN_POINT ( 'NONE',  ( -9.929695104603000644, -17.36901065046999904, 7.973993995755001229 ) ) ;
#6259=CARTESIAN_POINT ( 'NONE',  ( -2.356642558701290024, -3.183365214057053194, 2.616017292610900657 ) ) ;
#6264=FACE_OUTER_BOUND ( 'NONE', #44535, .T. ) ;
#6268=CARTESIAN_POINT ( 'NONE',  ( -1.886823409074000146, -60.56319684329000097, -12.68610076208999971 ) ) ;
#6272=CARTESIAN_POINT ( 'NONE',  ( 7.986976573804001056, -24.72634345633999686, -10.07613380457000041 ) ) ;
#6275=DIRECTION ( 'NONE',  ( 0.000000000000000000, 0.000000000000000000, -1.000000000000000000 ) ) ;
#6280=CARTESIAN_POINT ( 'NONE',  ( -7.686918321215999939, -57.04439829094999936, 10.48771805383000100 ) ) ;
#6281=CIRCLE ( 'NONE', #58100, 10.40000000000000036 ) ;
#6282=VECTOR ( 'NONE', #14181, 1000.000000000000000 ) ;
#6283=CARTESIAN_POINT ( 'NONE',  ( 7.758650587924000419, -54.64922688096000059, -9.996717134825001239 ) ) ;
#6284=CIRCLE ( 'NONE', #11028, 11.00000000000000000 ) ;
#6292=ORIENTED_EDGE ( 'NONE', *, *, #36664, .T. ) ;
#6293=CARTESIAN_POINT ( 'NONE',  ( -7.601397897754999633, -18.75000000000000000, 9.369164850722000892 ) ) ;
#6294=EDGE_CURVE ( 'NONE', #822, #39513, #52765, .T. ) ;
#6297=EDGE_CURVE ( 'NONE', #47034, #33163, #19060, .T. ) ;
#6302=ORIENTED_EDGE ( 'NONE', *, *, #8905, .F. ) ;
#6304=ORIENTED_EDGE ( 'NONE', *, *, #15217, .F. ) ;
#6305=ORIENTED_EDGE ( 'NONE', *, *, #40249, .T. ) ;
#6306=CARTESIAN_POINT ( 'NONE',  ( -1.288488638074000159, -17.46435060632000003, 12.54709296483000003 ) ) ;
#6309=FACE_OUTER_BOUND ( 'NONE', #54453, .T. ) ;
#6312=CYLINDRICAL_SURFACE ( 'NONE', #30696, 11.75000000000000000 ) ;
#6313=EDGE_LOOP ( 'NONE', ( #57135, #7382, #12668, #33373, #9623, #7992, #52043 ) ) ;
#6314=ORIENTED_EDGE ( 'NONE', *, *, #18893, .T. ) ;
#6316=DIRECTION ( 'NONE',  ( 0.000000000000000000, 1.000000000000000000, 0.000000000000000000 ) ) ;
#6318=AXIS2_PLACEMENT_3D ( 'NONE', #31785, #31488, #35930 ) ;
#6319=CARTESIAN_POINT ( 'NONE',  ( 1.003693376153260264, -61.76223992066808677, -12.70247752669052232 ) ) ;
#6321=LINE ( 'NONE', #1621, #30356 ) ;
#6323=AXIS2_PLACEMENT_3D ( 'NONE', #56364, #33617, #24481 ) ;
#6326=FACE_OUTER_BOUND ( 'NONE', #32501, .T. ) ;
#6327=AXIS2_PLACEMENT_3D ( 'NONE', #56218, #56795, #6618 ) ;
#6329=CONICAL_SURFACE ( 'NONE', #58199, 8.899999998586000771, 0.7853981633972997312 ) ;
#6330=CARTESIAN_POINT ( 'NONE',  ( -10.47513558171999826, -54.99636614397000045, 7.624778817986999968 ) ) ;
#6332=CARTESIAN_POINT ( 'NONE',  ( -1.750000000001000089, -18.75000001325000198, -12.56594318051000059 ) ) ;
#6336=LINE ( 'NONE', #56229, #18558 ) ;
#6337=FACE_OUTER_BOUND ( 'NONE', #52329, .T. ) ;
#6339=CARTESIAN_POINT ( 'NONE',  ( 1.388126973326925473, -1.594193359475267524, 3.339128716332707469 ) ) ;
#6340=EDGE_LOOP ( 'NONE', ( #49186, #39748, #38658, #23948 ) ) ;
#6341=CARTESIAN_POINT ( 'NONE',  ( -0.2306306439467533664, -3.500000000000000000, -3.452531048248814294 ) ) ;
#6342=DIRECTION ( 'NONE',  ( 0.000000000000000000, 0.000000000000000000, -1.000000000000000000 ) ) ;
#6343=CARTESIAN_POINT ( 'NONE',  ( 3.077551880085030778, -77.55205857829017191, 11.44362783114953253 ) ) ;
#6346=CARTESIAN_POINT ( 'NONE',  ( 11.88928085110999966, -78.23131299228001012, 5.289737169833999886 ) ) ;
#6350=DIRECTION ( 'NONE',  ( -0.9999999999995751176, 0.000000000000000000, -9.217554819261769351E-07 ) ) ;
#6351=EDGE_CURVE ( 'NONE', #13102, #43717, #11559, .T. ) ;
#6358=LINE ( 'NONE', #41795, #37424 ) ;
#6363=EDGE_LOOP ( 'NONE', ( #7478, #53760, #28858 ) ) ;
#6364=VERTEX_POINT ( 'NONE', #23087 ) ;
#6367=DIRECTION ( 'NONE',  ( 0.000000000000000000, 0.000000000000000000, 1.000000000000000000 ) ) ;
#6368=LINE ( 'NONE', #42975, #35981 ) ;
#6369=VECTOR ( 'NONE', #6442, 1000.000000000000000 ) ;
#6372=VECTOR ( 'NONE', #38567, 1000.000000000000000 ) ;
#6375=AXIS2_PLACEMENT_3D ( 'NONE', #48406, #7943, #18279 ) ;
#6379=ADVANCED_FACE ( 'NONE', ( #29827 ), #49261, .T. ) ;
#6381=CARTESIAN_POINT ( 'NONE',  ( -10.48771805367000098, -57.04439828530000511, -7.686918321054999836 ) ) ;
#6382=DIRECTION ( 'NONE',  ( 0.000000000000000000, -1.000000000000000000, 3.788556036780999566E-11 ) ) ;
#6387=CARTESIAN_POINT ( 'NONE',  ( -12.50239399164999909, -17.31640749886000208, 1.003653729363000124 ) ) ;
#6392=CYLINDRICAL_SURFACE ( 'NONE', #1454, 14.00000000000000000 ) ;
#6395=CARTESIAN_POINT ( 'NONE',  ( 8.313499432590312210, -76.51190516819144705, 8.303026597870685421 ) ) ;
#6403=CARTESIAN_POINT ( 'NONE',  ( -13.63885489310999510, -59.58578169018998949, 7.254376133916000668 ) ) ;
#6406=CARTESIAN_POINT ( 'NONE',  ( 10.35747145892000098, -18.68415268018999953, 7.626500777237000150 ) ) ;
#6407=B_SPLINE_SURFACE_WITH_KNOTS ( 'NONE', 3, 3, ( 
 ( #21197, #39198, #31194, #49234 ),
 ( #26776, #4357, #44806, #22359 ),
 ( #17942, #58380, #48093, #7624 ),
 ( #43648, #57213, #16780, #21488 ),
 ( #34762, #52788, #12343, #7910 ),
 ( #3483, #39495, #14663, #40965 ),
 ( #5522, #41543, #45408, #36526 ),
 ( #35933, #9084, #53962, #32374 ),
 ( #27070, #23530, #50415, #13790 ),
 ( #4949, #19113, #54548, #13499 ),
 ( #23821, #5815, #14089, #9670 ) ),
 .UNSPECIFIED., .F., .F., .F.,
 ( 4, 1, 1, 1, 1, 1, 1, 1, 4 ),
 ( 4, 4 ),
 ( -0.01994574723509000280, 0.000000000000000000, 0.1666666666667000196, 0.3333333333333000081, 0.5000000000000000000, 0.6666666666667000474, 0.8333333333333000637, 1.000000000000000000, 1.020511277925000071 ),
 ( -0.3582002740325999635, 1.358574366096999997 ),
 .UNSPECIFIED. ) ;
#6408=CARTESIAN_POINT ( 'NONE',  ( -9.992017125402000488, -60.96084086979999483, -7.762968460695000239 ) ) ;
#6410=AXIS2_PLACEMENT_3D ( 'NONE', #4773, #22184, #44333 ) ;
#6412=CARTESIAN_POINT ( 'NONE',  ( 12.50686284812396210, -54.49510763085826426, 1.423064270604161630 ) ) ;
#6413=B_SPLINE_CURVE_WITH_KNOTS ( 'NONE', 3,
 ( #33206, #42091, #52405, #6944, #57404, #34081, #20807, #21383, #34659, #24948 ),
 .UNSPECIFIED., .F., .F.,
 ( 4, 2, 2, 2, 4 ),
 ( 0.000000000000000000, 0.1249999656550738053, 0.2499999313101476106, 0.3749998969652214020, 0.4999998626202952212 ),
 .UNSPECIFIED. ) ;
#6414=CARTESIAN_POINT ( 'NONE',  ( 12.77562710766000009, -25.26233677660999888, 0.5428386295906000303 ) ) ;
#6418=CARTESIAN_POINT ( 'NONE',  ( 6.478953145441000316, -76.08549705920000861, 10.17405887424000177 ) ) ;
#6419=ORIENTED_EDGE ( 'NONE', *, *, #51017, .F. ) ;
#6425=CARTESIAN_POINT ( 'NONE',  ( 12.54715396797999993, -54.26815137240999576, -1.292200816717000045 ) ) ;
#6428=FACE_OUTER_BOUND ( 'NONE', #15461, .T. ) ;
#6431=CARTESIAN_POINT ( 'NONE',  ( -7.919595949288999570, -59.94999999040999938, 9.050966798898000931 ) ) ;
#6434=ORIENTED_EDGE ( 'NONE', *, *, #55014, .F. ) ;
#6437=CARTESIAN_POINT ( 'NONE',  ( 12.83044027763000017, -60.10639784916000394, 2.062670899361999766 ) ) ;
#6439=ORIENTED_EDGE ( 'NONE', *, *, #36346, .F. ) ;
#6442=DIRECTION ( 'NONE',  ( -1.776356839400000238E-14, -1.000000000000000000, 3.019806626979999679E-13 ) ) ;
#6443=ORIENTED_EDGE ( 'NONE', *, *, #49719, .F. ) ;
#6450=CARTESIAN_POINT ( 'NONE',  ( -3.163647801558190586, -2.580206749503648922, 0.8517472837491544269 ) ) ;
#6452=EDGE_LOOP ( 'NONE', ( #14409, #27788, #21595 ) ) ;
#6453=CARTESIAN_POINT ( 'NONE',  ( -12.77562710766000009, -25.26233677660999888, -0.5428386295906000303 ) ) ;
#6456=LINE ( 'NONE', #46930, #44004 ) ;
#6457=CARTESIAN_POINT ( 'NONE',  ( -1.583004792629327806, -17.54790758840184139, -12.70616254410899515 ) ) ;
#6463=CARTESIAN_POINT ( 'NONE',  ( 12.17088485526999975, -75.74463960549999797, 1.845041276493999849 ) ) ;
#6466=DIRECTION ( 'NONE',  ( -1.000000000000000000, 0.000000000000000000, 0.000000000000000000 ) ) ;
#6467=CARTESIAN_POINT ( 'NONE',  ( 9.788011744299998540, -61.32881292732000134, -7.956359616248999345 ) ) ;
#6468=CARTESIAN_POINT ( 'NONE',  ( 11.93255069029000026, -79.17946444151000662, -2.830763026309000008 ) ) ;
#6471=CARTESIAN_POINT ( 'NONE',  ( 1.614622833403325686, -2.767753323799579501, -2.821287581134315658 ) ) ;
#6472=CARTESIAN_POINT ( 'NONE',  ( 0.9078743877195619705, -78.18103102862099263, -12.03646258193789897 ) ) ;
#6474=B_SPLINE_SURFACE_WITH_KNOTS ( 'NONE', 3, 3, ( 
 ( #12840, #34402, #30556, #48587, #44434, #35562, #17273, #35263, #53588, #53294, #16709, #29971, #48022, #44154, #25554, #39709, #34691, #3701, #48302, #12273, #30262, #57716, #25843, #3420, #21704, #30840, #48874, #21419, #8415, #26413, #3987, #21989, #39998, #17573, #31122 ),
 ( #45033, #9302, #18456, #31423, #23454, #193, #45329, #45916, #767, #49466, #41466, #14298, #9889, #9596, #14011, #5165, #36447, #18744, #54476, #26999, #27292, #27869, #32584, #50633, #19036, #53891, #4879, #4585, #46211, #22585, #18168, #58311, #55043, #40598, #54753 ),
 ( #14592, #10182, #32008, #28160, #27582, #9013, #22876, #36161, #50338, #17873, #49763, #31715, #54181, #1052, #40885, #35863, #23165, #477, #50050, #13718, #32292, #5451, #22285, #45625, #41174, #13422, #36737, #37029, #40302, #21705, #21421, #22586, #12559, #40599, #36162 ),
 ( #30557, #44156, #35563, #58013, #17574, #26135, #49161, #3988, #21990, #58312, #16997, #12841, #17274, #53589, #48588, #54182, #57436, #13719, #39999, #39710, #44435, #3702, #49764, #31716, #13128, #31124, #8134, #53007, #8714, #30841, #53295, #26414, #43871, #48875, #40303 ) ),
 .UNSPECIFIED., .F., .F., .F.,
 ( 4, 4 ),
 ( 4, 1, 1, 1, 1, 1, 1, 1, 1, 1, 1, 1, 1, 1, 1, 1, 1, 1, 1, 1, 1, 1, 1, 1, 1, 1, 1, 1, 1, 1, 1, 1, 4 ),
 ( -0.3708084972812999980, 1.370808497280999960 ),
 ( -0.02000000000000000042, 0.01250000000000000069, 0.04499999999999999833, 0.07749999999999999944, 0.1100000000000000006, 0.1424999999999999878, 0.1749999999999999889, 0.2074999999999999900, 0.2399999999999999911, 0.2725000000000000200, 0.3049999999999999933, 0.3375000000000000222, 0.3699999999999999956, 0.4025000000000000244, 0.4349999999999999978, 0.4675000000000000266, 0.5000000000000000000, 0.5324999999999999734, 0.5649999999999999467, 0.5975000000000000311, 0.6300000000000000044, 0.6624999999999999778, 0.6949999999999999512, 0.7275000000000000355, 0.7600000000000000089, 0.7924999999999999822, 0.8249999999999999556, 0.8575000000000000400, 0.8900000000000000133, 0.9224999999999999867, 0.9549999999999999600, 0.9875000000000000444, 1.020000000000000018 ),
 .UNSPECIFIED. ) ;
#6480=CARTESIAN_POINT ( 'NONE',  ( 1.179839603460000053, -3.032184344713000357, -3.521708340803999970 ) ) ;
#6483=AXIS2_PLACEMENT_3D ( 'NONE', #22006, #27599, #9612 ) ;
#6484=CARTESIAN_POINT ( 'NONE',  ( -10.85510852219592337, -76.16860941111713146, 4.497416836951729557 ) ) ;
#6485=CARTESIAN_POINT ( 'NONE',  ( -13.86363636363000218, -32.36102867817999851, -1.277888278874999896E-05 ) ) ;
#6487=CARTESIAN_POINT ( 'NONE',  ( 0.000000000000000000, -32.88214388149999934, 0.000000000000000000 ) ) ;
#6488=VERTEX_POINT ( 'NONE', #7123 ) ;
#6491=B_SPLINE_CURVE_WITH_KNOTS ( 'NONE', 3,
 ( #47026, #19552, #1560, #33410, #28688, #15417, #23400, #41699, #14240, #11000, #55273, #28985, #46441, #9829, #46151, #45858, #46739, #54696, #1275, #51448, #19852, #23974, #54983, #6259, #10123, #5675, #6556, #37550, #28394, #19268, #37259, #23686, #14819, #5969, #24564, #24274, #5391, #42292, #1857, #41992, #32817, #41410, #55567, #992, #18688, #15116, #33114, #50279, #37847, #51155, #36970, #10710, #28101, #55867, #50863, #36679, #708, #18978, #14532, #10409, #32525, #50568, #2145, #25429, #43163, #16297, #20431, #34562, #52594, #42581, #15999, #52025, #38133, #21001, #7136, #12145, #38426, #56156, #39293, #30426, #56444, #15705, #16868, #29268, #2428, #52309, #34274, #11865, #42871, #7426, #48458, #20716, #33986, #2720, #11578, #8001, #52879, #29842, #47894, #6845, #11288, #43444, #3005, #38716, #39007, #56737, #47316, #29557, #48181, #12433, #20146 ),
 .UNSPECIFIED., .F., .F.,
 ( 4, 2, 2, 2, 2, 2, 1, 2, 2, 2, 2, 2, 2, 2, 2, 2, 2, 2, 2, 2, 2, 2, 2, 2, 2, 2, 2, 2, 1, 2, 2, 2, 2, 2, 2, 2, 2, 2, 2, 2, 2, 2, 2, 2, 2, 2, 2, 2, 2, 2, 1, 2, 2, 2, 2, 2, 4 ),
 ( 0.000000000000000000, 0.01562500000000000347, 0.03125000000000000694, 0.04687500000000000000, 0.06250000000000000000, 0.07812499999999998612, 0.09374999999999997224, 0.1093749999999999722, 0.1249999999999999584, 0.1406249999999999445, 0.1562499999999999167, 0.1718749999999998890, 0.1874999999999998612, 0.2031249999999998890, 0.2187499999999998890, 0.2343749999999998890, 0.2499999999999998890, 0.2656249999999998890, 0.2812499999999998890, 0.2968749999999998890, 0.3124999999999998890, 0.3281249999999998890, 0.3437499999999998890, 0.3593749999999998890, 0.3749999999999998890, 0.4062499999999999445, 0.4374999999999999445, 0.4687499999999999445, 0.4999999999999999445, 0.5312499999999998890, 0.5624999999999998890, 0.5937499999999998890, 0.6249999999999998890, 0.6406249999999998890, 0.6562499999999998890, 0.6718749999999998890, 0.6874999999999998890, 0.7031249999999998890, 0.7187499999999998890, 0.7343749999999998890, 0.7499999999999998890, 0.7656250000000000000, 0.7812500000000000000, 0.7968750000000000000, 0.8125000000000000000, 0.8281250000000000000, 0.8437500000000000000, 0.8593750000000000000, 0.8750000000000000000, 0.8906250000000000000, 0.9062500000000000000, 0.9218750000000000000, 0.9375000000000000000, 0.9531250000000000000, 0.9687500000000000000, 0.9843750000000000000, 1.000000000000000000 ),
 .UNSPECIFIED. ) ;
#6492=CARTESIAN_POINT ( 'NONE',  ( -2.098469896607999926E-14, 0.000000000000000000, 0.000000000000000000 ) ) ;
#6493=CARTESIAN_POINT ( 'NONE',  ( -7.658900562732000594, -60.00940503048000352, 10.01676248783999945 ) ) ;
#6496=CARTESIAN_POINT ( 'NONE',  ( 3.248132008022913020, -3.329261903070285022, -0.8492709327984924172 ) ) ;
#6497=CARTESIAN_POINT ( 'NONE',  ( 8.060167320302427996, -17.37936585541044821, 9.621722526392044728 ) ) ;
#6498=ORIENTED_EDGE ( 'NONE', *, *, #17624, .T. ) ;
#6500=CARTESIAN_POINT ( 'NONE',  ( 7.655984445824144835, -23.70337239446406841, -10.06694410249365568 ) ) ;
#6501=AXIS2_PLACEMENT_3D ( 'NONE', #46049, #9725, #45460 ) ;
#6504=CARTESIAN_POINT ( 'NONE',  ( 1.173556370041068053, -77.58592580708349828, -12.24706281916396655 ) ) ;
#6508=LINE ( 'NONE', #20099, #21910 ) ;
#6510=CARTESIAN_POINT ( 'NONE',  ( -7.648026768019999366, -23.24999998419999869, -10.12290050217000115 ) ) ;
#6514=ORIENTED_EDGE ( 'NONE', *, *, #28980, .T. ) ;
#6515=ADVANCED_FACE ( 'NONE', ( #43147 ), #11275, .T. ) ;
#6520=ORIENTED_EDGE ( 'NONE', *, *, #40836, .T. ) ;
#6521=CARTESIAN_POINT ( 'NONE',  ( 8.878349648294999952, -16.93036913510000119, 8.870329531829000302 ) ) ;
#6524=CARTESIAN_POINT ( 'NONE',  ( 11.61968134756000026, -78.60307252743000106, 3.235820271459000086 ) ) ;
#6526=CARTESIAN_POINT ( 'NONE',  ( 10.14948852604999985, -19.24899164588000389, 7.674614791898999755 ) ) ;
#6528=ORIENTED_EDGE ( 'NONE', *, *, #28761, .T. ) ;
#6529=DIRECTION ( 'NONE',  ( -1.000000000000000000, 0.000000000000000000, 0.000000000000000000 ) ) ;
#6535=B_SPLINE_CURVE_WITH_KNOTS ( 'NONE', 3,
 ( #25853, #53015, #3711, #53305, #35272, #43882, #20568, #48035, #3428, #38853 ),
 .UNSPECIFIED., .F., .F.,
 ( 4, 2, 2, 2, 4 ),
 ( 0.000000000000000000, 0.2500000000000000000, 0.5000000000000000000, 0.7500000000000000000, 1.000000000000000000 ),
 .UNSPECIFIED. ) ;
#6538=CARTESIAN_POINT ( 'NONE',  ( -10.11462645681450034, -18.61287635839325461, -7.639895286233333138 ) ) ;
#6539=TOROIDAL_SURFACE ( 'NONE', #43333, 1.250000000000000000, 0.5000000000000000000 ) ;
#6540=CARTESIAN_POINT ( 'NONE',  ( 17.50000000000000000, -57.79999999999999716, 0.000000000000000000 ) ) ;
#6542=CARTESIAN_POINT ( 'NONE',  ( -5.869402599192000025, -78.46567021303999923, 10.46661899222999992 ) ) ;
#6544=CARTESIAN_POINT ( 'NONE',  ( 7.674614791501999989, -59.55100836074000625, 10.14948852566000070 ) ) ;
#6553=CARTESIAN_POINT ( 'NONE',  ( -8.478741751137999216, -17.12187496603999648, 9.108230428607001272 ) ) ;
#6554=EDGE_CURVE ( 'NONE', #34267, #8613, #40787, .T. ) ;
#6556=CARTESIAN_POINT ( 'NONE',  ( -0.5809223153592418809, -3.138131673207912087, 3.474841036571488129 ) ) ;
#6566=CARTESIAN_POINT ( 'NONE',  ( -1.576170184330999868, -60.96086967183000382, -12.55466896108000086 ) ) ;
#6570=CARTESIAN_POINT ( 'NONE',  ( 10.08161778466999969, -24.71855282893000094, -7.981584069265998949 ) ) ;
#6573=CARTESIAN_POINT ( 'NONE',  ( 6.306936360652213303, -78.52899687234631187, 9.913378331859004078 ) ) ;
#6574=FACE_OUTER_BOUND ( 'NONE', #23980, .T. ) ;
#6578=CARTESIAN_POINT ( 'NONE',  ( 7.622784390041999814, -55.01288991740999990, -10.47836615824999917 ) ) ;
#6580=EDGE_CURVE ( 'NONE', #33154, #37266, #11848, .T. ) ;
#6581=DIRECTION ( 'NONE',  ( 0.000000000000000000, -1.000000000000000000, 0.000000000000000000 ) ) ;
#6582=CARTESIAN_POINT ( 'NONE',  ( -7.634645133843775078, -23.47584427336687440, 10.10912661253024503 ) ) ;
#6584=AXIS2_PLACEMENT_3D ( 'NONE', #27253, #53552, #17532 ) ;
#6587=CONICAL_SURFACE ( 'NONE', #39566, 13.94999999937999924, 0.7853981633972997312 ) ;
#6588=CARTESIAN_POINT ( 'NONE',  ( -9.433537730344784933, -53.67202052640185883, 8.532653828180887245 ) ) ;
#6589=ORIENTED_EDGE ( 'NONE', *, *, #8047, .T. ) ;
#6593=ADVANCED_FACE ( 'NONE', ( #51723 ), #29541, .F. ) ;
#6594=ORIENTED_EDGE ( 'NONE', *, *, #25162, .F. ) ;
#6596=EDGE_CURVE ( 'NONE', #34348, #12597, #57058, .T. ) ;
#6597=EDGE_LOOP ( 'NONE', ( #57057, #23113, #45745, #17773 ) ) ;
#6599=CARTESIAN_POINT ( 'NONE',  ( 1.666727925315000025, -18.80825518223999993, 12.50018462903999961 ) ) ;
#6600=CARTESIAN_POINT ( 'NONE',  ( 12.69999999929000012, 7.140943757287000156E-10, 6.699859664396000284E-09 ) ) ;
#6601=CARTESIAN_POINT ( 'NONE',  ( -12.99510751537000353, -52.49705297113997204, -6.911973076623003642 ) ) ;
#6608=B_SPLINE_CURVE_WITH_KNOTS ( 'NONE', 3,
 ( #57726, #7276, #48313, #25278, #43010, #21429 ),
 .UNSPECIFIED., .F., .F.,
 ( 4, 1, 1, 4 ),
 ( 0.000000000000000000, 0.3333333333333000081, 0.6666666666667000474, 0.9999998688569219363 ),
 .UNSPECIFIED. ) ;
#6610=CARTESIAN_POINT ( 'NONE',  ( -12.70619440579224246, -24.46151788317378006, 1.571771935825063915 ) ) ;
#6612=CARTESIAN_POINT ( 'NONE',  ( -12.43571054531000186, -61.67980566386000163, -0.4385525234350999835 ) ) ;
#6618=DIRECTION ( 'NONE',  ( 0.000000000000000000, 1.000000000000000000, 0.000000000000000000 ) ) ;
#6619=B_SPLINE_CURVE_WITH_KNOTS ( 'NONE', 3,
 ( #7895, #31177, #25896, #8468, #3467, #53059, #17044, #35027, #48642, #3755 ),
 .UNSPECIFIED., .F., .F.,
 ( 4, 2, 2, 2, 4 ),
 ( 0.000000000000000000, 0.5000000000000001110, 0.6250000000000000000, 0.7500000000000000000, 1.000000000000000000 ),
 .UNSPECIFIED. ) ;
#6620=CARTESIAN_POINT ( 'NONE',  ( 7.067261237832259013, -79.23437499043450316, -9.724484250782996497 ) ) ;
#6621=CARTESIAN_POINT ( 'NONE',  ( -10.19019671030999952, -55.60356357307000508, 7.646965722228999951 ) ) ;
#6624=CARTESIAN_POINT ( 'NONE',  ( 1.799502287691000069, -18.69283319134000010, -12.60413670420000010 ) ) ;
#6625=EDGE_CURVE ( 'NONE', #47968, #27284, #53988, .T. ) ;
#6626=VECTOR ( 'NONE', #31313, 1000.000000000000000 ) ;
#6627=VECTOR ( 'NONE', #7890, 1000.000000000000000 ) ;
#6634=CARTESIAN_POINT ( 'NONE',  ( -2.888768896543007614, -1.298725683607843351, -2.022024471902001519 ) ) ;
#6637=CARTESIAN_POINT ( 'NONE',  ( -1.560639837747103131, -3.499999999999999556, -3.021350444604665508 ) ) ;
#6638=DIRECTION ( 'NONE',  ( 0.000000000000000000, -1.000000000000000000, 0.000000000000000000 ) ) ;
#6641=CARTESIAN_POINT ( 'NONE',  ( 7.411516475408999050, -77.12122017304999133, -10.69619859711000132 ) ) ;
#6651=CARTESIAN_POINT ( 'NONE',  ( 17.50000000000000000, -21.00000000000000000, 0.000000000000000000 ) ) ;
#6653=DIRECTION ( 'NONE',  ( -0.7071067811865475727, 0.000000000000000000, 0.7071067811865475727 ) ) ;
#6655=CYLINDRICAL_SURFACE ( 'NONE', #11732, 3.250000000000000000 ) ;
#6656=CYLINDRICAL_SURFACE ( 'NONE', #49233, 0.5000000000000006661 ) ;
#6660=DIRECTION ( 'NONE',  ( 0.4045602622694902117, 0.8201597334573811349, -0.4045602622694902117 ) ) ;
#6661=CARTESIAN_POINT ( 'NONE',  ( 7.655983890243021506, -18.29663439994899221, 10.06694524887558551 ) ) ;
#6662=EDGE_LOOP ( 'NONE', ( #12706, #4613, #36143 ) ) ;
#6663=EDGE_CURVE ( 'NONE', #45005, #9948, #21086, .T. ) ;
#6667=EDGE_LOOP ( 'NONE', ( #42072, #30105, #57122, #15532 ) ) ;
#6668=EDGE_LOOP ( 'NONE', ( #12088, #1901, #6221 ) ) ;
#6670=CARTESIAN_POINT ( 'NONE',  ( -1.750000000000000000, -60.04999999725999515, -12.50000000000000000 ) ) ;
#6671=ORIENTED_EDGE ( 'NONE', *, *, #29229, .F. ) ;
#6674=EDGE_LOOP ( 'NONE', ( #10672, #25130, #14230, #3182 ) ) ;
#6675=DIRECTION ( 'NONE',  ( 0.7071067811814920612, -1.249158819818986152E-07, -0.7071067811915919821 ) ) ;
#6677=CARTESIAN_POINT ( 'NONE',  ( -3.104418684490000135, -2.089115405599000219, -1.389370826391999936 ) ) ;
#6679=CARTESIAN_POINT ( 'NONE',  ( 0.000000000000000000, -23.25000000000000000, 12.00000000000000000 ) ) ;
#6682=DIRECTION ( 'NONE',  ( -0.5000000000000744960, -0.7071067811864422126, 0.5000000000000744960 ) ) ;
#6683=CARTESIAN_POINT ( 'NONE',  ( 2.624903909527706247, -78.80804708869507635, 11.97989236737772778 ) ) ;
#6691=CARTESIAN_POINT ( 'NONE',  ( 5.333565260656944140, -76.53737489142297079, 10.47213728794457310 ) ) ;
#6695=DIRECTION ( 'NONE',  ( 0.000000000000000000, 0.000000000000000000, -1.000000000000000000 ) ) ;
#6702=CYLINDRICAL_SURFACE ( 'NONE', #588, 0.5000000000000004441 ) ;
#6703=ADVANCED_FACE ( 'NONE', ( #34832 ), #1707, .F. ) ;
#6704=CARTESIAN_POINT ( 'NONE',  ( -10.07616267223999884, -61.52631138996999738, -7.986947465035998839 ) ) ;
#6707=CARTESIAN_POINT ( 'NONE',  ( 12.50240633875000107, -54.11762602111000575, 1.005381409374000112 ) ) ;
#6708=CARTESIAN_POINT ( 'NONE',  ( 12.44210192979000063, -24.08432059816999882, 1.464837683472000052 ) ) ;
#6709=VECTOR ( 'NONE', #44029, 1000.000000000000114 ) ;
#6711=CARTESIAN_POINT ( 'NONE',  ( -3.783525742921558521, -78.29734542223856408, -11.14657560477560061 ) ) ;
#6713=CARTESIAN_POINT ( 'NONE',  ( -5.681140472451000178, -76.84159451939000007, -10.64016158193000017 ) ) ;
#6714=VERTEX_POINT ( 'NONE', #49904 ) ;
#6717=CARTESIAN_POINT ( 'NONE',  ( 0.000000000000000000, -3.500000000000000000, 0.000000000000000000 ) ) ;
#6719=CARTESIAN_POINT ( 'NONE',  ( 7.764220096253753312, -54.54399029293954726, 10.21028322249942022 ) ) ;
#6721=CARTESIAN_POINT ( 'NONE',  ( 12.48408657656000109, -55.43026141536999774, -1.669508654504999967 ) ) ;
#6723=CARTESIAN_POINT ( 'NONE',  ( -7.342331066867000544, -59.94999999967000548, -8.190859204290999784 ) ) ;
#6724=DIRECTION ( 'NONE',  ( 0.000000000000000000, -1.000000000000000000, 0.000000000000000000 ) ) ;
#6727=CARTESIAN_POINT ( 'NONE',  ( -2.299491490204544242, -0.8333333333332290094, 2.552553896037383474 ) ) ;
#6729=VERTEX_POINT ( 'NONE', #14730 ) ;
#6732=CARTESIAN_POINT ( 'NONE',  ( 12.49306752636999995, -60.08056692637000396, 1.667917367010000040 ) ) ;
#6733=CARTESIAN_POINT ( 'NONE',  ( 3.250000000000000000, -3.250000000000000000, 0.000000000000000000 ) ) ;
#6734=ORIENTED_EDGE ( 'NONE', *, *, #25417, .F. ) ;
#6735=AXIS2_PLACEMENT_3D ( 'NONE', #43548, #3113, #39682 ) ;
#6738=VERTEX_POINT ( 'NONE', #5304 ) ;
#6743=CARTESIAN_POINT ( 'NONE',  ( -12.70228857838970704, -24.82190589609123776, -1.213561371311159487 ) ) ;
#6751=EDGE_CURVE ( 'NONE', #39806, #40044, #57765, .T. ) ;
#6752=CARTESIAN_POINT ( 'NONE',  ( 9.850513605848957965, -54.49492088415036761, 7.836738268828630893 ) ) ;
#6756=LINE ( 'NONE', #24766, #32846 ) ;
#6758=CARTESIAN_POINT ( 'NONE',  ( -7.765022563360999719, -24.09093562100999719, 9.830785949113998612 ) ) ;
#6760=CARTESIAN_POINT ( 'NONE',  ( 10.52693147742000157, -60.22153431716999705, -7.606024891127000309 ) ) ;
#6761=CARTESIAN_POINT ( 'NONE',  ( -7.421655993048999811, -78.37472433538000871, 9.763070719336001346 ) ) ;
#6763=DIRECTION ( 'NONE',  ( -1.000000000000000000, 0.000000000000000000, 0.000000000000000000 ) ) ;
#6765=CARTESIAN_POINT ( 'NONE',  ( 1.173085220040108290, -77.68291245588305571, -12.24193935082051965 ) ) ;
#6768=ORIENTED_EDGE ( 'NONE', *, *, #4068, .F. ) ;
#6771=CARTESIAN_POINT ( 'NONE',  ( 2.062312494845999655, -23.22715659892999795, 12.83634740209000036 ) ) ;
#6773=CARTESIAN_POINT ( 'NONE',  ( 2.064858460238000237, -2.553371213896999947, -3.087201104211000136 ) ) ;
#6777=CARTESIAN_POINT ( 'NONE',  ( -9.885937566445212710, -76.15396054158379968, 6.353414232468484357 ) ) ;
#6781=ORIENTED_EDGE ( 'NONE', *, *, #52656, .T. ) ;
#6782=CARTESIAN_POINT ( 'NONE',  ( 1.328206530128999807, -76.68360379137467930, -12.23810562210000086 ) ) ;
#6785=PLANE ( 'NONE',  #37248 ) ;
#6786=CARTESIAN_POINT ( 'NONE',  ( -9.523353692561999040, -61.61947015589999666, 8.220363114712000652 ) ) ;
#6787=AXIS2_PLACEMENT_3D ( 'NONE', #33468, #37318, #50919 ) ;
#6790=DIRECTION ( 'NONE',  ( 0.000000000000000000, -1.000000000000000000, 0.000000000000000000 ) ) ;
#6791=DIRECTION ( 'NONE',  ( 0.000000000000000000, 1.000000000000000000, 0.000000000000000000 ) ) ;
#6796=LINE ( 'NONE', #24803, #4688 ) ;
#6801=CARTESIAN_POINT ( 'NONE',  ( 1.799490220168999954, -56.02870851050000311, -12.64502302235999842 ) ) ;
#6802=ADVANCED_FACE ( 'NONE', ( #10324 ), #24323, .F. ) ;
#6804=PLANE ( 'NONE',  #24587 ) ;
#6811=ORIENTED_EDGE ( 'NONE', *, *, #26192, .T. ) ;
#6812=CARTESIAN_POINT ( 'NONE',  ( 8.227509542990000924, -17.17460508872999725, 9.516261809269000338 ) ) ;
#6813=CARTESIAN_POINT ( 'NONE',  ( 10.26699006316253637, -76.00833333333331154, -5.917523019358050362 ) ) ;
#6814=CARTESIAN_POINT ( 'NONE',  ( -3.799640087458000082, -78.34354736923999951, -11.29133014407999980 ) ) ;
#6816=DIRECTION ( 'NONE',  ( -0.7071067811865475727, 0.000000000000000000, -0.7071067811865475727 ) ) ;
#6819=ORIENTED_EDGE ( 'NONE', *, *, #3245, .T. ) ;
#6820=CARTESIAN_POINT ( 'NONE',  ( 10.70099950850357118, -78.08451462771667195, 4.958828595142525941 ) ) ;
#6821=EDGE_LOOP ( 'NONE', ( #24831, #13161, #44726, #3605 ) ) ;
#6823=LINE ( 'NONE', #56715, #45582 ) ;
#6824=CIRCLE ( 'NONE', #32298, 5.000000000000000888 ) ;
#6827=DIRECTION ( 'NONE',  ( 0.000000000000000000, 0.000000000000000000, 1.000000000000000000 ) ) ;
#6830=CARTESIAN_POINT ( 'NONE',  ( -7.641012386039999882, -23.28917565320000094, 10.18589234708000113 ) ) ;
#6837=EDGE_CURVE ( 'NONE', #1677, #18184, #39801, .T. ) ;
#6842=CARTESIAN_POINT ( 'NONE',  ( -8.284626357352999904, -16.95139346842000094, 9.778502130864000108 ) ) ;
#6843=AXIS2_PLACEMENT_3D ( 'NONE', #25951, #30658, #12381 ) ;
#6845=CARTESIAN_POINT ( 'NONE',  ( 1.407444721559201417, -1.907779362115657573, -3.228803909804078831 ) ) ;
#6848=CARTESIAN_POINT ( 'NONE',  ( 2.015551294784000191, -54.99652295122999845, -12.79857978891999970 ) ) ;
#6850=CARTESIAN_POINT ( 'NONE',  ( -13.99999999961999819, -72.70000000038000110, 1.691901337660000028E-09 ) ) ;
#6853=ORIENTED_EDGE ( 'NONE', *, *, #666, .T. ) ;
#6855=CARTESIAN_POINT ( 'NONE',  ( 10.98465012826175169, -18.69514063119935088, -0.5809631169955021823 ) ) ;
#6856=CARTESIAN_POINT ( 'NONE',  ( 0.005928781627365999583, -62.00113050230000056, -12.66336824422999996 ) ) ;
#6857=ADVANCED_FACE ( 'NONE', ( #24478 ), #11495, .F. ) ;
#6858=CARTESIAN_POINT ( 'NONE',  ( -7.664266801483091918, -55.05053022673563135, 7.892048199458214341 ) ) ;
#6861=CARTESIAN_POINT ( 'NONE',  ( 10.15831671671000080, -24.21991983044000207, -7.756223511073000232 ) ) ;
#6863=CARTESIAN_POINT ( 'NONE',  ( -10.03846658019334193, -60.59367507117082852, 7.678639819092132335 ) ) ;
#6865=CARTESIAN_POINT ( 'NONE',  ( -10.41172477450676581, -60.32013115014467530, 7.610718073431628206 ) ) ;
#6866=ORIENTED_EDGE ( 'NONE', *, *, #37206, .T. ) ;
#6873=AXIS2_PLACEMENT_3D ( 'NONE', #34481, #38640, #20071 ) ;
#6876=CARTESIAN_POINT ( 'NONE',  ( -7.864797288573664780, -54.34877151149995456, 10.10445166985919840 ) ) ;
#6877=VERTEX_POINT ( 'NONE', #6175 ) ;
#6878=CARTESIAN_POINT ( 'NONE',  ( 1.667961445601999992, -21.74800977511999989, 12.58338334669999981 ) ) ;
#6881=CARTESIAN_POINT ( 'NONE',  ( -12.48375848564000101, -23.37270426058999817, 1.669543623995999981 ) ) ;
#6882=ORIENTED_EDGE ( 'NONE', *, *, #41832, .F. ) ;
#6883=VERTEX_POINT ( 'NONE', #33322 ) ;
#6884=CARTESIAN_POINT ( 'NONE',  ( -12.57354471034999932, -55.07622323954000620, -1.757967544833999973 ) ) ;
#6885=ORIENTED_EDGE ( 'NONE', *, *, #5216, .T. ) ;
#6887=ORIENTED_EDGE ( 'NONE', *, *, #42765, .F. ) ;
#6888=EDGE_CURVE ( 'NONE', #47936, #37628, #29468, .T. ) ;
#6890=VECTOR ( 'NONE', #35642, 1000.000000000000114 ) ;
#6894=AXIS2_PLACEMENT_3D ( 'NONE', #10576, #50739, #55442 ) ;
#6897=ORIENTED_EDGE ( 'NONE', *, *, #3634, .F. ) ;
#6900=DIRECTION ( 'NONE',  ( -0.7071067811865475727, 0.000000000000000000, 0.7071067811865475727 ) ) ;
#6901=CARTESIAN_POINT ( 'NONE',  ( -12.49997170193999985, -59.99201514515999634, -1.666513530428000101 ) ) ;
#6903=CARTESIAN_POINT ( 'NONE',  ( 7.626500902215000544, -18.68415522710999710, 10.35747158362999976 ) ) ;
#6906=CARTESIAN_POINT ( 'NONE',  ( 2.997885520263000370, -78.88962101269000016, -11.53013814508000046 ) ) ;
#6908=EDGE_CURVE ( 'NONE', #29025, #20424, #10631, .T. ) ;
#6910=ADVANCED_FACE ( 'NONE', ( #1770 ), #56817, .F. ) ;
#6911=CARTESIAN_POINT ( 'NONE',  ( -9.963464501270999918, -55.11723479348000154, 7.659241807016999637 ) ) ;
#6915=CARTESIAN_POINT ( 'NONE',  ( 1.667916687244999974, -23.29849137228000444, -12.49168433579000137 ) ) ;
#6918=CARTESIAN_POINT ( 'NONE',  ( -2.897260861154202338, -1.143336016975180058, -1.695352622819430444 ) ) ;
#6920=CARTESIAN_POINT ( 'NONE',  ( 10.12290050122000018, -55.54999999974999980, -7.648026767069000087 ) ) ;
#6921=CARTESIAN_POINT ( 'NONE',  ( 3.450547804646586059, -1.024362841730831697, 1.065430366115255323 ) ) ;
#6922=ORIENTED_EDGE ( 'NONE', *, *, #31610, .T. ) ;
#6923=FACE_OUTER_BOUND ( 'NONE', #43058, .T. ) ;
#6924=DIRECTION ( 'NONE',  ( 0.000000000000000000, 0.000000000000000000, 1.000000000000000000 ) ) ;
#6926=CARTESIAN_POINT ( 'NONE',  ( -12.50240681836000078, -61.48234730679999416, 1.005418944265999981 ) ) ;
#6928=EDGE_CURVE ( 'NONE', #25833, #52807, #55782, .T. ) ;
#6933=DIRECTION ( 'NONE',  ( 0.000000000000000000, 1.000000000000000000, 0.000000000000000000 ) ) ;
#6934=VECTOR ( 'NONE', #11012, 1000.000000000000000 ) ;
#6937=DIRECTION ( 'NONE',  ( 0.000000000000000000, 1.000000000000000000, 0.000000000000000000 ) ) ;
#6939=CARTESIAN_POINT ( 'NONE',  ( 8.325345585179579899, -76.38763475635133204, -8.291621564338084838 ) ) ;
#6942=CARTESIAN_POINT ( 'NONE',  ( -7.601397897754999633, -60.04999999657000131, -10.07627163191000008 ) ) ;
#6944=CARTESIAN_POINT ( 'NONE',  ( -3.035171633316387396, -0.7760416592923815582, -1.750338234017642769 ) ) ;
#6947=FACE_OUTER_BOUND ( 'NONE', #5495, .T. ) ;
#6948=ORIENTED_EDGE ( 'NONE', *, *, #56456, .T. ) ;
#6952=ORIENTED_EDGE ( 'NONE', *, *, #18774, .F. ) ;
#6953=CARTESIAN_POINT ( 'NONE',  ( -1.980610890452893624, -23.52073889483701308, 12.74374574607051258 ) ) ;
#6957=CARTESIAN_POINT ( 'NONE',  ( 8.090910852014772559, -60.34721902436125873, 7.452378523310778213 ) ) ;
#6958=CARTESIAN_POINT ( 'NONE',  ( 3.075537641221555596, -77.44583333333332575, -11.44417895085270587 ) ) ;
#6962=ORIENTED_EDGE ( 'NONE', *, *, #10266, .F. ) ;
#6966=ORIENTED_EDGE ( 'NONE', *, *, #48934, .F. ) ;
#6967=FACE_OUTER_BOUND ( 'NONE', #1031, .T. ) ;
#6970=AXIS2_PLACEMENT_3D ( 'NONE', #40309, #49168, #14306 ) ;
#6972=CARTESIAN_POINT ( 'NONE',  ( 7.081266003839625789, -79.12419498753402536, -10.01317160224411396 ) ) ;
#6979=EDGE_CURVE ( 'NONE', #9420, #469, #43679, .T. ) ;
#6991=FACE_OUTER_BOUND ( 'NONE', #13601, .T. ) ;
#6992=AXIS2_PLACEMENT_3D ( 'NONE', #42842, #38397, #25682 ) ;
#6995=CARTESIAN_POINT ( 'NONE',  ( 12.56594317819999951, -55.54999998572999687, 1.750000000000000000 ) ) ;
#6997=CARTESIAN_POINT ( 'NONE',  ( -1.338697082642999803, -78.16879906939999501, -12.94399764267999942 ) ) ;
#7000=CARTESIAN_POINT ( 'NONE',  ( -9.397239103731438448, -78.25099886579246800, -7.223445203516699387 ) ) ;
#7001=DIRECTION ( 'NONE',  ( 1.000000000000000000, 0.000000000000000000, 0.000000000000000000 ) ) ;
#7002=CARTESIAN_POINT ( 'NONE',  ( 9.309741638652999640, -76.86252759254999489, -7.903174005480999575 ) ) ;
#7005=LINE ( 'NONE', #34716, #8819 ) ;
#7007=LINE ( 'NONE', #25298, #37784 ) ;
#7008=CARTESIAN_POINT ( 'NONE',  ( 12.57433760364000008, -55.08878254084000048, -1.760777649351999985 ) ) ;
#7011=CARTESIAN_POINT ( 'NONE',  ( 12.50000000000000000, -18.75000000000000000, 0.000000000000000000 ) ) ;
#7017=CARTESIAN_POINT ( 'NONE',  ( -12.76303204513999923, -55.53514852210999919, 1.980584515753000208 ) ) ;
#7020=FACE_OUTER_BOUND ( 'NONE', #27551, .T. ) ;
#7022=EDGE_LOOP ( 'NONE', ( #26265, #5726, #1030, #44200 ) ) ;
#7025=EDGE_LOOP ( 'NONE', ( #31826, #55152, #4856, #55174 ) ) ;
#7026=ORIENTED_EDGE ( 'NONE', *, *, #28599, .F. ) ;
#7027=EDGE_CURVE ( 'NONE', #51275, #41447, #9697, .T. ) ;
#7030=ADVANCED_FACE ( 'NONE', ( #40372 ), #6407, .F. ) ;
#7033=CIRCLE ( 'NONE', #9908, 12.50000000000000000 ) ;
#7034=ORIENTED_EDGE ( 'NONE', *, *, #56303, .T. ) ;
#7035=CARTESIAN_POINT ( 'NONE',  ( 2.840278559734812802, -2.392921495863389758, 1.635260199181394647 ) ) ;
#7037=ORIENTED_EDGE ( 'NONE', *, *, #28006, .T. ) ;
#7040=CARTESIAN_POINT ( 'NONE',  ( -8.485281374238999419, -55.54999999966999980, 8.485281374238999419 ) ) ;
#7041=CARTESIAN_POINT ( 'NONE',  ( 12.60356226362999976, -59.55077028856999988, -1.750000000000000000 ) ) ;
#7042=CARTESIAN_POINT ( 'NONE',  ( 10.09635500651664053, -55.27627834093870973, 7.644087038098070330 ) ) ;
#7044=CARTESIAN_POINT ( 'NONE',  ( -9.396809191439480458, -77.25090611101180116, -7.223167806601616725 ) ) ;
#7047=CARTESIAN_POINT ( 'NONE',  ( 12.72923908220964506, -60.57554307125821680, -1.930512971242454912 ) ) ;
#7050=FACE_OUTER_BOUND ( 'NONE', #36791, .T. ) ;
#7053=CARTESIAN_POINT ( 'NONE',  ( 0.000000000000000000, -0.2000000000000000111, 0.000000000000000000 ) ) ;
#7054=CARTESIAN_POINT ( 'NONE',  ( -5.531768889155999958, -79.07042751779999890, -10.94525552207000096 ) ) ;
#7055=CARTESIAN_POINT ( 'NONE',  ( 0.000000000000000000, -23.15000000000000213, -12.00000000000000000 ) ) ;
#7056=FACE_OUTER_BOUND ( 'NONE', #56495, .T. ) ;
#7057=CARTESIAN_POINT ( 'NONE',  ( -5.578716042954554588, -77.96310415304682806, 10.76391831645009134 ) ) ;
#7058=FACE_OUTER_BOUND ( 'NONE', #20764, .T. ) ;
#7059=ORIENTED_EDGE ( 'NONE', *, *, #19782, .T. ) ;
#7061=CARTESIAN_POINT ( 'NONE',  ( 12.49989425042000235, -59.99225390429000271, -1.666425739590000177 ) ) ;
#7062=CARTESIAN_POINT ( 'NONE',  ( 1.930628539545000022, -23.22124444086000139, 12.72375828104000028 ) ) ;
#7064=CARTESIAN_POINT ( 'NONE',  ( 3.543471834705000045, -3.225668112400000176, 0.3182372728196999900 ) ) ;
#7067=CARTESIAN_POINT ( 'NONE',  ( -8.307785421988745256, -76.13749769528703837, 8.309209506187553274 ) ) ;
#7068=CARTESIAN_POINT ( 'NONE',  ( -12.50239399164999909, -17.31640749886000208, 1.003653729363000124 ) ) ;
#7071=ORIENTED_EDGE ( 'NONE', *, *, #15660, .F. ) ;
#7072=CARTESIAN_POINT ( 'NONE',  ( -7.685416442687997396, -76.62134450945413278, -9.616126112745993382 ) ) ;
#7073=AXIS2_PLACEMENT_3D ( 'NONE', #48613, #39454, #12016 ) ;
#7075=CARTESIAN_POINT ( 'NONE',  ( 5.917523019358082337, -76.96666666666665435, -10.26699006316252394 ) ) ;
#7076=CARTESIAN_POINT ( 'NONE',  ( -8.485538010685999666, -61.68067982404999583, 9.101501073510000595 ) ) ;
#7081=CARTESIAN_POINT ( 'NONE',  ( -12.74331394907106407, -55.27353206545080155, -1.980611464663724286 ) ) ;
#7082=ORIENTED_EDGE ( 'NONE', *, *, #32773, .F. ) ;
#7083=CARTESIAN_POINT ( 'NONE',  ( -9.722718241315000398, -60.24678171298000251, 7.954951288349001004 ) ) ;
#7086=EDGE_CURVE ( 'NONE', #9942, #51555, #30271, .T. ) ;
#7087=AXIS2_PLACEMENT_3D ( 'NONE', #1216, #24502, #15357 ) ;
#7092=LINE ( 'NONE', #39241, #19439 ) ;
#7093=CARTESIAN_POINT ( 'NONE',  ( 12.50657368826004046, -61.77245458960354796, 0.3553454088956558010 ) ) ;
#7096=ADVANCED_FACE ( 'NONE', ( #55120 ), #1414, .T. ) ;
#7097=CARTESIAN_POINT ( 'NONE',  ( 12.70451544420807188, -54.24534321882928367, -1.498804046740677798 ) ) ;
#7098=ORIENTED_EDGE ( 'NONE', *, *, #7725, .F. ) ;
#7099=EDGE_LOOP ( 'NONE', ( #58304, #46547, #15012, #51467 ) ) ;
#7102=EDGE_LOOP ( 'NONE', ( #23494, #6520, #297, #10236 ) ) ;
#7103=CARTESIAN_POINT ( 'NONE',  ( 7.646966891758999907, -18.80358255734000039, 10.19019756605999838 ) ) ;
#7107=CARTESIAN_POINT ( 'NONE',  ( 12.17287523535000027, -77.98388785726000094, -3.409737174454000375 ) ) ;
#7108=CARTESIAN_POINT ( 'NONE',  ( 0.000000000000000000, -0.6500000000000000222, 0.000000000000000000 ) ) ;
#7110=CYLINDRICAL_SURFACE ( 'NONE', #15308, 3.250000000000000000 ) ;
#7112=EDGE_CURVE ( 'NONE', #54154, #2738, #556, .T. ) ;
#7113=CIRCLE ( 'NONE', #36347, 12.57042253521000141 ) ;
#7114=ORIENTED_EDGE ( 'NONE', *, *, #53523, .T. ) ;
#7115=CARTESIAN_POINT ( 'NONE',  ( 7.970415440577865773, -54.27707676769661305, -9.713035532171977238 ) ) ;
#7119=TOROIDAL_SURFACE ( 'NONE', #31573, 17.50000000000000000, 5.000000000000000000 ) ;
#7123=CARTESIAN_POINT ( 'NONE',  ( -1.980584515752000119, -18.73514853375999678, -12.76303204602000108 ) ) ;
#7125=CARTESIAN_POINT ( 'NONE',  ( -5.866053559275163032, -78.39900354637602220, 10.46067059907391439 ) ) ;
#7127=CARTESIAN_POINT ( 'NONE',  ( 7.624341764943999955, -60.06485149430999826, -10.42531124854999902 ) ) ;
#7129=ORIENTED_EDGE ( 'NONE', *, *, #21214, .T. ) ;
#7134=CARTESIAN_POINT ( 'NONE',  ( -8.188285776315000319, -17.29506253989999820, 9.395726099566001466 ) ) ;
#7136=CARTESIAN_POINT ( 'NONE',  ( -3.488853381481115346, -2.260600980737770271, -0.4651628758941012132 ) ) ;
#7141=CARTESIAN_POINT ( 'NONE',  ( 0.000000000000000000, -9.295797029142999435, 0.000000000000000000 ) ) ;
#7143=ORIENTED_EDGE ( 'NONE', *, *, #53765, .F. ) ;
#7144=CARTESIAN_POINT ( 'NONE',  ( 0.000000000000000000, -49.87071424677999687, 0.000000000000000000 ) ) ;
#7146=CARTESIAN_POINT ( 'NONE',  ( 1.484804496640999893, -61.51869153350000374, -12.77261165612999960 ) ) ;
#7150=CARTESIAN_POINT ( 'NONE',  ( 10.53495260691999924, -23.22711197486000145, -7.618387230241999930 ) ) ;
#7152=B_SPLINE_CURVE_WITH_KNOTS ( 'NONE', 3,
 ( #3677, #26104, #21391, #39684, #19739, #15302, #16685, #42177, #48283, #11969 ),
 .UNSPECIFIED., .F., .F.,
 ( 4, 2, 2, 2, 4 ),
 ( 0.000000000000000000, 0.1249999999999990563, 0.2499999999999981126, 0.4999999999999962252, 1.000000000000000000 ),
 .UNSPECIFIED. ) ;
#7154=FACE_OUTER_BOUND ( 'NONE', #55515, .T. ) ;
#7155=CARTESIAN_POINT ( 'NONE',  ( -8.274772994298601247, -61.77888614401855705, 9.689268729882146047 ) ) ;
#7157=DIRECTION ( 'NONE',  ( 0.7071067811865475727, 0.000000000000000000, 0.7071067811865475727 ) ) ;
#7161=CARTESIAN_POINT ( 'NONE',  ( -6.007496854199997571, -79.17708331421573575, -10.42139454737465343 ) ) ;
#7162=CARTESIAN_POINT ( 'NONE',  ( 11.44417895085270054, -77.57083333333332575, 3.075537641221564922 ) ) ;
#7163=CARTESIAN_POINT ( 'NONE',  ( -10.14950121160999963, -56.04922972508000356, 7.674627477461999803 ) ) ;
#7166=AXIS2_PLACEMENT_3D ( 'NONE', #44967, #54695, #40531 ) ;
#7167=CARTESIAN_POINT ( 'NONE',  ( -7.610717068315568490, -55.27984996805254525, 10.41172376761247875 ) ) ;
#7168=ORIENTED_EDGE ( 'NONE', *, *, #55708, .F. ) ;
#7169=AXIS2_PLACEMENT_3D ( 'NONE', #43190, #81, #45218 ) ;
#7171=EDGE_CURVE ( 'NONE', #21680, #6877, #48348, .T. ) ;
#7173=DIRECTION ( 'NONE',  ( -0.7071067811865475727, 0.000000000000000000, -0.7071067811865475727 ) ) ;
#7175=EDGE_LOOP ( 'NONE', ( #41734, #12118, #25595, #5848 ) ) ;
#7176=CARTESIAN_POINT ( 'NONE',  ( -12.43410192427999839, -54.35868879854000113, -1.192687910178000132 ) ) ;
#7179=DIRECTION ( 'NONE',  ( 0.7071067811865475727, 0.000000000000000000, -0.7071067811865475727 ) ) ;
#7182=CARTESIAN_POINT ( 'NONE',  ( -7.764010764070559567, -60.92280919712734288, 9.931043767944283118 ) ) ;
#7188=ORIENTED_EDGE ( 'NONE', *, *, #37559, .F. ) ;
#7191=CARTESIAN_POINT ( 'NONE',  ( -12.83838776462000020, -60.00596988455000513, -2.062170466182000172 ) ) ;
#7193=CARTESIAN_POINT ( 'NONE',  ( 7.642160924884000117, -19.21538333566000034, 10.55911395187000146 ) ) ;
#7194=CARTESIAN_POINT ( 'NONE',  ( 7.610716808859600668, -60.32015489444223988, 10.41172350879423014 ) ) ;
#7195=CARTESIAN_POINT ( 'NONE',  ( 0.000000000000000000, -23.15000000000000213, 11.79999999999999893 ) ) ;
#7197=DIRECTION ( 'NONE',  ( 1.000000000000000000, 0.000000000000000000, 0.000000000000000000 ) ) ;
#7199=CARTESIAN_POINT ( 'NONE',  ( -10.30457855490000085, -55.03665569380999756, 7.636266480997000450 ) ) ;
#7201=CARTESIAN_POINT ( 'NONE',  ( 1.568318300085000120E-14, 6.776263578034402713E-18, -12.89999999999698588 ) ) ;
#7203=CARTESIAN_POINT ( 'NONE',  ( 1.667917367010000040, -23.28056692670000061, -12.49306752634999995 ) ) ;
#7204=CIRCLE ( 'NONE', #12835, 12.25000000000000000 ) ;
#7206=CARTESIAN_POINT ( 'NONE',  ( 1.798944584243999945, -18.78466771720000139, -12.61116915999999932 ) ) ;
#7208=CARTESIAN_POINT ( 'NONE',  ( -3.448863046786000197, -1.886744131007000114, -1.608907009436000068 ) ) ;
#7209=VECTOR ( 'NONE', #49480, 1000.000000000000000 ) ;
#7210=CARTESIAN_POINT ( 'NONE',  ( 2.227269615981378070, -0.9293910887734395665, -2.735979432117919607 ) ) ;
#7214=CARTESIAN_POINT ( 'NONE',  ( 0.000000000000000000, -23.15000000000000213, -11.79999999999999893 ) ) ;
#7215=CARTESIAN_POINT ( 'NONE',  ( -1.821913034590999979E-14, -80.69999999923000189, 0.000000000000000000 ) ) ;
#7217=CIRCLE ( 'NONE', #24194, 14.00000000000000533 ) ;
#7218=CARTESIAN_POINT ( 'NONE',  ( 2.383426421432000009, -3.359465166820999826, 2.543613531316000209 ) ) ;
#7220=CARTESIAN_POINT ( 'NONE',  ( -12.43359548531999970, -54.09290601346000216, 0.8500179128028999553 ) ) ;
#7222=CARTESIAN_POINT ( 'NONE',  ( 1.929975092515999968, -60.00107256231000008, 12.72537404212999768 ) ) ;
#7227=CARTESIAN_POINT ( 'NONE',  ( 9.371262623183563178, -76.39810623049203286, -7.089854323050989393 ) ) ;
#7229=DIRECTION ( 'NONE',  ( 0.000000000000000000, 1.000000000000000000, 0.000000000000000000 ) ) ;
#7239=CARTESIAN_POINT ( 'NONE',  ( 8.485281374238999419, -23.25000000000000000, -8.485281374238999419 ) ) ;
#7243=CARTESIAN_POINT ( 'NONE',  ( 1.208267226973974706, -24.82590682147949934, 12.70228502423902484 ) ) ;
#7245=VECTOR ( 'NONE', #42889, 1000.000000000000114 ) ;
#7246=ORIENTED_EDGE ( 'NONE', *, *, #15787, .T. ) ;
#7247=DIRECTION ( 'NONE',  ( 0.7071067811865475727, 0.000000000000000000, -0.7071067811865475727 ) ) ;
#7249=VECTOR ( 'NONE', #47267, 1000.000000000000000 ) ;
#7252=ORIENTED_EDGE ( 'NONE', *, *, #32267, .T. ) ;
#7253=CARTESIAN_POINT ( 'NONE',  ( -7.478989599426999924, -78.43234560996998539, 9.838492168967000850 ) ) ;
#7254=EDGE_CURVE ( 'NONE', #43183, #6714, #6824, .T. ) ;
#7255=CIRCLE ( 'NONE', #41178, 12.50000000000000000 ) ;
#7256=VERTEX_POINT ( 'NONE', #24560 ) ;
#7258=ORIENTED_EDGE ( 'NONE', *, *, #19301, .F. ) ;
#7259=CYLINDRICAL_SURFACE ( 'NONE', #29009, 1.750000000000000000 ) ;
#7264=CARTESIAN_POINT ( 'NONE',  ( -8.838834764832000701, -18.75000000000000000, -8.838834764832000701 ) ) ;
#7268=CARTESIAN_POINT ( 'NONE',  ( 12.76303204522000101, -23.26485147686999966, 1.980584515753000208 ) ) ;
#7272=DIRECTION ( 'NONE',  ( 0.000000000000000000, -1.000000000000000000, 0.000000000000000000 ) ) ;
#7273=CARTESIAN_POINT ( 'NONE',  ( 1.980744519413613292, -2.923166175690931290, 2.579508073329230378 ) ) ;
#7276=CARTESIAN_POINT ( 'NONE',  ( -14.00000000000000000, -32.90763690531000663, -1.352038286243999979E-05 ) ) ;
#7277=CARTESIAN_POINT ( 'NONE',  ( -8.096452064242996016, -56.01421830980998351, 13.15643568217000769 ) ) ;
#7279=CARTESIAN_POINT ( 'NONE',  ( -11.55907703490496985, -76.21507827338332675, -2.244914986486493902 ) ) ;
#7280=CARTESIAN_POINT ( 'NONE',  ( 10.24998526315000014, -21.75083378359999742, 7.705142895586000407 ) ) ;
#7281=CARTESIAN_POINT ( 'NONE',  ( -7.753906807064999462, -61.08933445950000163, -10.31979621052999896 ) ) ;
#7282=CARTESIAN_POINT ( 'NONE',  ( -11.00000000000000000, -4.000000000000000000, 0.000000000000000000 ) ) ;
#7283=CARTESIAN_POINT ( 'NONE',  ( 3.799999999999999822, 0.000000000000000000, 0.000000000000000000 ) ) ;
#7285=CARTESIAN_POINT ( 'NONE',  ( -3.129814719915999799, -78.44632227421000437, 12.62985940900000159 ) ) ;
#7286=AXIS2_PLACEMENT_3D ( 'NONE', #52156, #7272, #25273 ) ;
#7288=CARTESIAN_POINT ( 'NONE',  ( 10.06692847398457857, -23.70343452287690056, 7.655995225931332193 ) ) ;
#7289=CARTESIAN_POINT ( 'NONE',  ( 8.768124086712999699, -59.94999999969000015, -7.919595949288999570 ) ) ;
#7290=CARTESIAN_POINT ( 'NONE',  ( -10.00409279782000027, -76.63142817898000203, -7.262369351941000417 ) ) ;
#7294=AXIS2_PLACEMENT_3D ( 'NONE', #48241, #30487, #29331 ) ;
#7295=CARTESIAN_POINT ( 'NONE',  ( -10.99069764842704622, -18.45457471225823554, -0.4531388007107930438 ) ) ;
#7296=CARTESIAN_POINT ( 'NONE',  ( -9.943915246433000732, -78.72146835062000036, -7.799333767171999554 ) ) ;
#7297=DIRECTION ( 'NONE',  ( -0.7071067811865475727, 0.000000000000000000, 0.7071067811865475727 ) ) ;
#7302=ORIENTED_EDGE ( 'NONE', *, *, #1337, .T. ) ;
#7303=DIRECTION ( 'NONE',  ( -0.7071067811865475727, 0.000000000000000000, 0.7071067811865475727 ) ) ;
#7304=CIRCLE ( 'NONE', #57270, 0.5000000000000006661 ) ;
#7307=VERTEX_POINT ( 'NONE', #39289 ) ;
#7308=CARTESIAN_POINT ( 'NONE',  ( -10.06692847420048054, -60.50343452148293721, -7.655995225848112540 ) ) ;
#7310=ORIENTED_EDGE ( 'NONE', *, *, #18821, .T. ) ;
#7312=EDGE_LOOP ( 'NONE', ( #57709, #34099, #53274, #27921, #9871, #25868 ) ) ;
#7317=VERTEX_POINT ( 'NONE', #7421 ) ;
#7318=EDGE_CURVE ( 'NONE', #13397, #30070, #2140, .T. ) ;
#7319=ORIENTED_EDGE ( 'NONE', *, *, #21880, .F. ) ;
#7321=EDGE_CURVE ( 'NONE', #27203, #18938, #48596, .T. ) ;
#7324=CARTESIAN_POINT ( 'NONE',  ( 12.56594317825999951, -60.05000001354000005, -1.750000000000000000 ) ) ;
#7329=CIRCLE ( 'NONE', #50720, 1.750000000000002220 ) ;
#7332=CARTESIAN_POINT ( 'NONE',  ( -7.624757096123999212, -23.80351363819999833, 10.47516529248999895 ) ) ;
#7335=EDGE_CURVE ( 'NONE', #56888, #36961, #32251, .T. ) ;
#7336=CARTESIAN_POINT ( 'NONE',  ( 10.19022265129000004, -59.99634105610000034, -7.646946115762000673 ) ) ;
#7338=CARTESIAN_POINT ( 'NONE',  ( 12.16303714866999997, -79.24287182625000980, 1.568404430622000190 ) ) ;
#7340=CARTESIAN_POINT ( 'NONE',  ( -7.345153731672117381, -60.02841244177280089, -8.188331488387708745 ) ) ;
#7341=CARTESIAN_POINT ( 'NONE',  ( 11.75000000000000000, -77.95000000000000284, 2.316376715183999699E-14 ) ) ;
#7348=CARTESIAN_POINT ( 'NONE',  ( 0.1941442403254999838, -3.685159174984999897, -3.395596365263000127 ) ) ;
#7349=EDGE_CURVE ( 'NONE', #32986, #28865, #20712, .T. ) ;
#7352=CARTESIAN_POINT ( 'NONE',  ( -10.29258502670653996, -75.80000000000002558, 5.813495078707884289 ) ) ;
#7355=CARTESIAN_POINT ( 'NONE',  ( -7.651160336694000641, -22.76232686216999923, 10.45205658994000153 ) ) ;
#7357=EDGE_CURVE ( 'NONE', #587, #54702, #38711, .T. ) ;
#7358=CARTESIAN_POINT ( 'NONE',  ( -10.07722254365999959, -21.74800977511999989, -7.718368845776000242 ) ) ;
#7362=CARTESIAN_POINT ( 'NONE',  ( -8.227501432806000992, -61.62538814575999879, 9.516269855012000178 ) ) ;
#7363=CARTESIAN_POINT ( 'NONE',  ( 0.008285467789246998838, -1.006281426753999897, 3.701232203711000146 ) ) ;
#7365=FACE_OUTER_BOUND ( 'NONE', #3818, .T. ) ;
#7371=B_SPLINE_SURFACE_WITH_KNOTS ( 'NONE', 3, 3, ( 
 ( #53107, #13530, #57527, #44837 ),
 ( #22087, #31522, #48684, #8228 ),
 ( #31226, #18793, #3798, #21800 ),
 ( #49571, #22392, #9118, #39805 ),
 ( #27104, #49265, #58114, #8816 ),
 ( #57818, #45141, #296, #17377 ),
 ( #35364, #53389, #17676, #26808 ),
 ( #40403, #5548, #55446, #19434 ) ),
 .UNSPECIFIED., .F., .F., .F.,
 ( 4, 1, 1, 1, 1, 4 ),
 ( 4, 4 ),
 ( -0.01200407347464999865, 0.000000000000000000, 0.3333333333333000081, 0.6666666666667000474, 1.000000000000000000, 1.011997855551999947 ),
 ( -0.3559705542741999906, 1.355970554273999928 ),
 .UNSPECIFIED. ) ;
#7372=CARTESIAN_POINT ( 'NONE',  ( 11.75000000000000000, -76.05000000000001137, 0.000000000000000000 ) ) ;
#7374=VERTEX_POINT ( 'NONE', #42577 ) ;
#7381=VERTEX_POINT ( 'NONE', #16573 ) ;
#7382=ORIENTED_EDGE ( 'NONE', *, *, #25049, .F. ) ;
#7387=CARTESIAN_POINT ( 'NONE',  ( 8.541162059891000524, -16.99199348450000002, 9.205819316576999256 ) ) ;
#7389=CARTESIAN_POINT ( 'NONE',  ( -3.075537641221531615, -75.90416666666669698, -11.44417895085270942 ) ) ;
#7390=CARTESIAN_POINT ( 'NONE',  ( 5.621201030502000151, -78.50735805811000034, 11.49883638144000031 ) ) ;
#7391=DIRECTION ( 'NONE',  ( 0.000000000000000000, -1.000000000000000000, 0.000000000000000000 ) ) ;
#7392=FACE_OUTER_BOUND ( 'NONE', #38607, .T. ) ;
#7398=CARTESIAN_POINT ( 'NONE',  ( 11.75000000000000000, -78.04999999999999716, 0.000000000000000000 ) ) ;
#7406=CARTESIAN_POINT ( 'NONE',  ( -7.836764916109927093, -61.10511429613131895, -9.850487231183631565 ) ) ;
#7412=CARTESIAN_POINT ( 'NONE',  ( -7.626500902217000721, -23.31584477285000290, 10.35747158362999976 ) ) ;
#7414=ADVANCED_FACE ( 'NONE', ( #344 ), #22148, .T. ) ;
#7415=CARTESIAN_POINT ( 'NONE',  ( -9.723174505940001211, -24.47697504200000296, -7.958760297012999807 ) ) ;
#7421=CARTESIAN_POINT ( 'NONE',  ( -13.86363636363000218, -69.16102867818000277, -1.277888281761000050E-05 ) ) ;
#7426=CARTESIAN_POINT ( 'NONE',  ( 2.780473330202828386, -2.052526692832529420, 2.160620055192048472 ) ) ;
#7431=DIRECTION ( 'NONE',  ( 0.7071067811865475727, 0.000000000000000000, 0.7071067811865475727 ) ) ;
#7432=CARTESIAN_POINT ( 'NONE',  ( 11.74991234329036516, -75.95242683881967594, 0.3799060071047825060 ) ) ;
#7435=EDGE_CURVE ( 'NONE', #24723, #43107, #21697, .T. ) ;
#7437=CARTESIAN_POINT ( 'NONE',  ( 3.077479315212850342, -77.05195087253886754, 11.44416613010283434 ) ) ;
#7439=SHAPE_REPRESENTATION ( 'Body', ( #43526 ), #53938 ) ;
#7443=CARTESIAN_POINT ( 'NONE',  ( 10.30767511322000018, -23.74763733895999707, -7.634418707049000830 ) ) ;
#7444=CARTESIAN_POINT ( 'NONE',  ( 0.5222397221428117797, -16.83701780599038145, 12.70447686583918134 ) ) ;
#7446=CARTESIAN_POINT ( 'NONE',  ( 4.341671546774118262, -78.54407962236030016, 10.92272608737802386 ) ) ;
#7447=CARTESIAN_POINT ( 'NONE',  ( -9.355938762769532957, -61.97483710998693596, 8.610912454485829315 ) ) ;
#7448=EDGE_LOOP ( 'NONE', ( #36752, #54014, #50101, #42790 ) ) ;
#7452=ADVANCED_FACE ( 'NONE', ( #49322 ), #44593, .F. ) ;
#7454=AXIS2_PLACEMENT_3D ( 'NONE', #32283, #15166, #51207 ) ;
#7455=CARTESIAN_POINT ( 'NONE',  ( -12.83044027763000017, -60.10639784916000394, -2.062670899361999766 ) ) ;
#7456=CARTESIAN_POINT ( 'NONE',  ( 5.917523019358037040, -77.63333333333329733, 10.26699006316254525 ) ) ;
#7460=AXIS2_PLACEMENT_3D ( 'NONE', #2005, #19410, #33555 ) ;
#7461=CARTESIAN_POINT ( 'NONE',  ( 1.931087888049999979, -23.31584477285000290, 12.71658889741999943 ) ) ;
#7463=CARTESIAN_POINT ( 'NONE',  ( -11.44417895085272008, -76.27916666666668277, 3.075537641221497420 ) ) ;
#7466=CARTESIAN_POINT ( 'NONE',  ( -12.59651451715000015, -55.40944962329000134, -1.801708894189000043 ) ) ;
#7467=AXIS2_PLACEMENT_3D ( 'NONE', #15873, #2877, #57177 ) ;
#7468=EDGE_CURVE ( 'NONE', #47045, #37124, #26864, .T. ) ;
#7473=AXIS2_PLACEMENT_3D ( 'NONE', #33166, #6900, #24332 ) ;
#7478=ORIENTED_EDGE ( 'NONE', *, *, #34032, .T. ) ;
#7481=CARTESIAN_POINT ( 'NONE',  ( 1.250000000000000000, -18.75000000000000000, 12.00000000000000000 ) ) ;
#7483=CARTESIAN_POINT ( 'NONE',  ( 7.653559626094000201, -18.70151115557999688, 10.01235002622999914 ) ) ;
#7484=EDGE_CURVE ( 'NONE', #23569, #56133, #54045, .T. ) ;
#7485=CARTESIAN_POINT ( 'NONE',  ( -1.821913034590999979E-14, -80.69999999923000189, -12.14999999923000118 ) ) ;
#7491=CARTESIAN_POINT ( 'NONE',  ( -7.969034948568999077, -54.17623147781999648, 9.934750886883000121 ) ) ;
#7494=CARTESIAN_POINT ( 'NONE',  ( -9.835237363972000324, -17.91864156569999977, -7.760968332719999196 ) ) ;
#7495=CARTESIAN_POINT ( 'NONE',  ( 7.640030139773000606, -60.10716934574000447, 10.18491068061999982 ) ) ;
#7496=DIRECTION ( 'NONE',  ( 1.000000000000000000, 0.000000000000000000, 0.000000000000000000 ) ) ;
#7497=VECTOR ( 'NONE', #20508, 1000.000000000000000 ) ;
#7504=EDGE_LOOP ( 'NONE', ( #10162, #13412, #18112, #21835, #32229 ) ) ;
#7506=ADVANCED_FACE ( 'NONE', ( #45190 ), #31575, .F. ) ;
#7507=CARTESIAN_POINT ( 'NONE',  ( -12.50686498859634455, -61.10484291343429675, 1.423095205018104936 ) ) ;
#7509=CARTESIAN_POINT ( 'NONE',  ( -0.06818180916829999494, -3.594953325257000287, 3.804809017442000396 ) ) ;
#7511=AXIS2_PLACEMENT_3D ( 'NONE', #51242, #32610, #55362 ) ;
#7512=CARTESIAN_POINT ( 'NONE',  ( -12.59682398755999877, -55.41262488626999527, 1.801644812721000077 ) ) ;
#7516=CARTESIAN_POINT ( 'NONE',  ( 12.50000000000000000, -55.55000000209000177, 1.750000000000000000 ) ) ;
#7521=CARTESIAN_POINT ( 'NONE',  ( 9.763034649155766687, -76.40254628798982139, -6.537437777648473336 ) ) ;
#7526=CARTESIAN_POINT ( 'NONE',  ( 0.4254240051736215000, -2.635416666666666963, -3.250000000000000000 ) ) ;
#7534=ORIENTED_EDGE ( 'NONE', *, *, #4383, .T. ) ;
#7535=CARTESIAN_POINT ( 'NONE',  ( 0.000000000000000000, -60.04999999966999980, -12.50000000000000000 ) ) ;
#7537=ORIENTED_EDGE ( 'NONE', *, *, #851, .F. ) ;
#7538=EDGE_LOOP ( 'NONE', ( #22415, #14478, #37446, #32918 ) ) ;
#7539=DIRECTION ( 'NONE',  ( 0.000000000000000000, -1.000000000000000000, 0.000000000000000000 ) ) ;
#7540=ORIENTED_EDGE ( 'NONE', *, *, #14271, .T. ) ;
#7549=B_SPLINE_CURVE_WITH_KNOTS ( 'NONE', 3,
 ( #14485, #18642, #45216, #23351, #13903, #5627, #9487, #5057 ),
 .UNSPECIFIED., .F., .F.,
 ( 4, 2, 2, 4 ),
 ( 0.000000000000000000, 0.4999999999999946709, 0.7499999999999973355, 1.000000000000000000 ),
 .UNSPECIFIED. ) ;
#7556=CARTESIAN_POINT ( 'NONE',  ( 4.812343589168453839, -79.02604166667481422, 10.81843774669307656 ) ) ;
#7557=LINE ( 'NONE', #7268, #24058 ) ;
#7562=CARTESIAN_POINT ( 'NONE',  ( 2.295137415993966368, -2.913156379416062869, 2.300548530246512513 ) ) ;
#7565=LINE ( 'NONE', #12568, #36409 ) ;
#7567=CARTESIAN_POINT ( 'NONE',  ( -2.422546195149999804, -2.212571010530000049, 2.935532677474999907 ) ) ;
#7568=CARTESIAN_POINT ( 'NONE',  ( 10.07719973196000041, -20.25111654322000021, 7.718346056127999510 ) ) ;
#7569=CARTESIAN_POINT ( 'NONE',  ( -9.310177428715999071, -61.93531023604000296, -8.596745825462999591 ) ) ;
#7576=CARTESIAN_POINT ( 'NONE',  ( -8.048032176077001054, -78.48332536818000449, 9.328081102756000220 ) ) ;
#7579=CARTESIAN_POINT ( 'NONE',  ( -1.112866131775000156, -76.11229163771001538, -12.46277982123999983 ) ) ;
#7584=CARTESIAN_POINT ( 'NONE',  ( -10.99606201159948426, -18.31532548059006515, -0.3145367810785520413 ) ) ;
#7585=CARTESIAN_POINT ( 'NONE',  ( -10.99674072140000014, -79.21640068957000835, 5.906003873140000415 ) ) ;
#7594=AXIS2_PLACEMENT_3D ( 'NONE', #35454, #26317, #57909 ) ;
#7596=ORIENTED_EDGE ( 'NONE', *, *, #8442, .F. ) ;
#7597=CARTESIAN_POINT ( 'NONE',  ( -10.42531124903999995, -55.53514851492000304, 7.624341765436000173 ) ) ;
#7599=EDGE_LOOP ( 'NONE', ( #53940, #25822, #46612, #21624, #36862 ) ) ;
#7601=VERTEX_POINT ( 'NONE', #35129 ) ;
#7604=CARTESIAN_POINT ( 'NONE',  ( 9.393673072993333761, -77.99939921257045228, 7.217662729535765820 ) ) ;
#7606=ORIENTED_EDGE ( 'NONE', *, *, #24294, .F. ) ;
#7607=CARTESIAN_POINT ( 'NONE',  ( 12.77656766269999977, -53.48801851230000182, 0.1555695072194999973 ) ) ;
#7608=VECTOR ( 'NONE', #54577, 1000.000000000000000 ) ;
#7610=CARTESIAN_POINT ( 'NONE',  ( -3.911342194028000208, -78.64916925129686831, -11.62327352135999980 ) ) ;
#7612=EDGE_CURVE ( 'NONE', #35427, #18065, #53161, .T. ) ;
#7613=CARTESIAN_POINT ( 'NONE',  ( 10.30768118222999874, -55.05239703883000146, 7.634415485482000108 ) ) ;
#7614=CARTESIAN_POINT ( 'NONE',  ( 9.164374456839587069, -16.78432317405038532, -8.803712804485032350 ) ) ;
#7616=DIRECTION ( 'NONE',  ( 0.7026410690473252618, -0.1122098755728027641, 0.7026410690473252618 ) ) ;
#7619=LINE ( 'NONE', #30035, #47309 ) ;
#7620=CARTESIAN_POINT ( 'NONE',  ( -7.645398488021999839, -23.21531609142999741, 10.18948971874999998 ) ) ;
#7622=AXIS2_PLACEMENT_3D ( 'NONE', #58071, #9071, #27356 ) ;
#7624=CARTESIAN_POINT ( 'NONE',  ( -12.43652237962999862, -17.07935153061999856, 0.1283967009857999997 ) ) ;
#7625=CARTESIAN_POINT ( 'NONE',  ( 2.624826629463999694, -78.84050177318998465, 11.97953966613999910 ) ) ;
#7628=CARTESIAN_POINT ( 'NONE',  ( 4.518722420425526742, -78.39451041693787658, 11.19879261494060962 ) ) ;
#7629=DIRECTION ( 'NONE',  ( 0.000000000000000000, 0.000000000000000000, 1.000000000000000000 ) ) ;
#7634=CARTESIAN_POINT ( 'NONE',  ( 1.749722766158907650, -23.47588992887090953, 12.54673760678561223 ) ) ;
#7635=CARTESIAN_POINT ( 'NONE',  ( 2.469846707035999955, -3.365950421107999802, 2.338639843265999829 ) ) ;
#7642=ORIENTED_EDGE ( 'NONE', *, *, #20193, .T. ) ;
#7643=CARTESIAN_POINT ( 'NONE',  ( -10.24998526315000014, -21.75083378359999742, -7.705142895586000407 ) ) ;
#7647=CARTESIAN_POINT ( 'NONE',  ( 10.26699006316253637, -77.00833333333331154, -5.917523019358050362 ) ) ;
#7648=CARTESIAN_POINT ( 'NONE',  ( -7.647735717269999789, -60.52294882350999927, 10.13404777204000062 ) ) ;
#7649=CARTESIAN_POINT ( 'NONE',  ( -3.017608268723000364, -1.664752247162999854, -1.341678642855000048 ) ) ;
#7651=CARTESIAN_POINT ( 'NONE',  ( 2.426647618366999603E-14, -5.949999999936560258, 0.000000000000000000 ) ) ;
#7653=ORIENTED_EDGE ( 'NONE', *, *, #11118, .T. ) ;
#7655=FACE_OUTER_BOUND ( 'NONE', #9544, .T. ) ;
#7657=CARTESIAN_POINT ( 'NONE',  ( 1.750000000001000089, -60.04999998641999781, -12.56594318054000148 ) ) ;
#7658=CARTESIAN_POINT ( 'NONE',  ( -10.07719973194999952, -57.05111654290000445, -7.718346056122999954 ) ) ;
#7662=AXIS2_PLACEMENT_3D ( 'NONE', #13776, #31180, #41235 ) ;
#7664=CARTESIAN_POINT ( 'NONE',  ( 1.799475304559999822, -58.55171076491000548, -12.69616050744000013 ) ) ;
#7668=CARTESIAN_POINT ( 'NONE',  ( 12.76303204513999923, -55.53514852210999919, -1.980584515753000208 ) ) ;
#7673=ORIENTED_EDGE ( 'NONE', *, *, #56889, .F. ) ;
#7674=CARTESIAN_POINT ( 'NONE',  ( 12.50686284816651472, -17.69510763146307397, 1.423064270789805574 ) ) ;
#7677=CARTESIAN_POINT ( 'NONE',  ( 1.583004792641895531, -54.34790758811762146, 12.70616254407479140 ) ) ;
#7678=CARTESIAN_POINT ( 'NONE',  ( 7.379132703266000348, -77.25467974817999561, -10.64946278274999969 ) ) ;
#7681=PLANE ( 'NONE',  #4163 ) ;
#7685=VERTEX_POINT ( 'NONE', #1781 ) ;
#7698=CARTESIAN_POINT ( 'NONE',  ( -12.56594317819999951, -55.54999998572999687, -1.750000000000000000 ) ) ;
#7701=CARTESIAN_POINT ( 'NONE',  ( 7.674627477108999507, -56.04922971914000129, 10.14950121126000049 ) ) ;
#7709=DIRECTION ( 'NONE',  ( 4.134220892123999815E-14, -1.534448722697999916E-11, -1.000000000000000000 ) ) ;
#7712=AXIS2_PLACEMENT_3D ( 'NONE', #20314, #10588, #2606 ) ;
#7718=CARTESIAN_POINT ( 'NONE',  ( 11.75000000000000000, -75.95000000000000284, 0.000000000000000000 ) ) ;
#7722=FACE_OUTER_BOUND ( 'NONE', #39453, .T. ) ;
#7723=DIRECTION ( 'NONE',  ( 2.678932014865000134E-11, 1.000000000000000000, -2.678911359553000079E-11 ) ) ;
#7724=FACE_OUTER_BOUND ( 'NONE', #54888, .T. ) ;
#7725=EDGE_CURVE ( 'NONE', #41082, #52202, #23178, .T. ) ;
#7728=EDGE_CURVE ( 'NONE', #21905, #17178, #22925, .T. ) ;
#7733=ORIENTED_EDGE ( 'NONE', *, *, #27870, .T. ) ;
#7737=B_SPLINE_SURFACE_WITH_KNOTS ( 'NONE', 3, 3, ( 
 ( #1692, #14655, #1404, #19986 ),
 ( #24109, #832, #41241, #46280 ),
 ( #28226, #6100, #23236, #37095 ),
 ( #18813, #5805, #51286, #10245 ),
 ( #42424, #50705, #19395, #32365 ),
 ( #1993, #37387, #55406, #54823 ),
 ( #14951, #55111, #1116, #32653 ),
 ( #32948, #46574, #50991, #10541 ) ),
 .UNSPECIFIED., .F., .F., .F.,
 ( 4, 1, 1, 1, 1, 4 ),
 ( 4, 4 ),
 ( -0.01200407347462000007, 0.000000000000000000, 0.3333333333333000081, 0.6666666666667000474, 1.000000000000000000, 1.011997855551999947 ),
 ( -0.3559705542741999906, 1.355970554273999928 ),
 .UNSPECIFIED. ) ;
#7742=CARTESIAN_POINT ( 'NONE',  ( -7.651147547619999933, -59.56256650291999222, -10.45204383579000051 ) ) ;
#7745=EDGE_CURVE ( 'NONE', #26499, #41659, #45575, .T. ) ;
#7746=DIRECTION ( 'NONE',  ( 0.000000000000000000, -1.000000000000000000, 0.000000000000000000 ) ) ;
#7747=DIRECTION ( 'NONE',  ( 0.9957542233908819318, -0.04890176544946910064, -0.07798810124080861328 ) ) ;
#7748=CARTESIAN_POINT ( 'NONE',  ( -12.78015149457000099, -24.30330660695999967, 1.806228889758999978 ) ) ;
#7751=CARTESIAN_POINT ( 'NONE',  ( -12.43646312217999927, -53.87951485525000095, -0.1257251053154000153 ) ) ;
#7752=TOROIDAL_SURFACE ( 'NONE', #37925, 13.50000000000000000, 0.5000000000000000000 ) ;
#7754=CARTESIAN_POINT ( 'NONE',  ( 4.750030159171999777, -78.70865007999000795, -11.30647155123999958 ) ) ;
#7756=DIRECTION ( 'NONE',  ( 0.000000000000000000, -1.000000000000000000, 0.000000000000000000 ) ) ;
#7759=EDGE_CURVE ( 'NONE', #52628, #15626, #50587, .T. ) ;
#7762=CIRCLE ( 'NONE', #19102, 0.6000000000000008660 ) ;
#7764=ORIENTED_EDGE ( 'NONE', *, *, #20729, .F. ) ;
#7765=ORIENTED_EDGE ( 'NONE', *, *, #15022, .F. ) ;
#7769=CARTESIAN_POINT ( 'NONE',  ( -12.43422056534000042, -61.23655741401000085, -1.197404442626999854 ) ) ;
#7771=AXIS2_PLACEMENT_3D ( 'NONE', #37943, #51257, #11392 ) ;
#7772=CARTESIAN_POINT ( 'NONE',  ( 7.864802647436849092, -61.25123893485678650, 10.10444599044500968 ) ) ;
#7773=CARTESIAN_POINT ( 'NONE',  ( 7.730439324398687972, -54.67809618926516890, -10.25198230927261456 ) ) ;
#7775=VECTOR ( 'NONE', #34773, 1000.000000000000000 ) ;
#7776=B_SPLINE_CURVE_WITH_KNOTS ( 'NONE', 3,
 ( #29404, #32955, #10548, #1411, #46871, #38562, #24986, #5810, #23817, #28531 ),
 .UNSPECIFIED., .F., .F.,
 ( 4, 2, 2, 2, 4 ),
 ( 0.000000000000000000, 0.2500000000000000000, 0.5000000000000000000, 0.7500000000000000000, 1.000000000000000000 ),
 .UNSPECIFIED. ) ;
#7777=CARTESIAN_POINT ( 'NONE',  ( 12.49996905250000090, -18.80797343466000271, -1.666511841114999948 ) ) ;
#7778=CARTESIAN_POINT ( 'NONE',  ( 1.980464483675000054, -57.04439829357999514, 12.85140862645999782 ) ) ;
#7780=EDGE_LOOP ( 'NONE', ( #11686, #22782, #55447, #10302, #41579, #6952, #36267 ) ) ;
#7781=CARTESIAN_POINT ( 'NONE',  ( -9.205836503685999261, -53.79200673903999785, 8.541144771039000716 ) ) ;
#7783=CARTESIAN_POINT ( 'NONE',  ( -9.996785040898998886, -17.84937852891999910, -7.758588586541999454 ) ) ;
#7784=CARTESIAN_POINT ( 'NONE',  ( 7.626500902197000720, -55.48415522678000400, 10.35747158360999975 ) ) ;
#7785=CARTESIAN_POINT ( 'NONE',  ( 7.919595949288999570, -57.79999999967000690, 8.909545442949999838 ) ) ;
#7786=CARTESIAN_POINT ( 'NONE',  ( 2.600548699141073783, -1.299417036785829094, -1.998661137613467975 ) ) ;
#7789=CARTESIAN_POINT ( 'NONE',  ( -10.12290050124000018, -18.75000000007999645, 7.648026767085999822 ) ) ;
#7790=CARTESIAN_POINT ( 'NONE',  ( -3.500000000146000101, -0.7499999998540000101, 2.054632350152999929E-08 ) ) ;
#7794=CARTESIAN_POINT ( 'NONE',  ( -12.80896991329000123, -20.24546192895000019, 1.930989179114000143 ) ) ;
#7795=CARTESIAN_POINT ( 'NONE',  ( 2.257397718401000120, -3.043015194441000215, 3.064303898428999862 ) ) ;
#7797=VECTOR ( 'NONE', #23245, 1000.000000000000000 ) ;
#7798=CARTESIAN_POINT ( 'NONE',  ( -12.43652237957999951, -53.87935153028999480, 0.1283967009859000308 ) ) ;
#7800=CARTESIAN_POINT ( 'NONE',  ( 0.4356486348705999601, -61.68064955776999625, 12.43591427125000060 ) ) ;
#7803=DIRECTION ( 'NONE',  ( 1.000000000000000000, 0.000000000000000000, 0.000000000000000000 ) ) ;
#7806=CARTESIAN_POINT ( 'NONE',  ( 10.84423179882955779, -76.41830951051049681, -4.523413806819045924 ) ) ;
#7810=CARTESIAN_POINT ( 'NONE',  ( 7.601397897754999633, -18.75000000310999937, -10.07627163191000008 ) ) ;
#7814=CARTESIAN_POINT ( 'NONE',  ( -1.624989163556999772E-14, -74.69999999881999031, 0.000000000000000000 ) ) ;
#7816=AXIS2_PLACEMENT_3D ( 'NONE', #20649, #33636, #41928 ) ;
#7818=CIRCLE ( 'NONE', #4047, 14.00000000000000000 ) ;
#7823=CARTESIAN_POINT ( 'NONE',  ( 0.8804656547800843169, -25.02803394706689843, 12.70299681151785265 ) ) ;
#7826=CARTESIAN_POINT ( 'NONE',  ( -2.598917237794094337, -1.447916666666666297, 1.997276839918461722 ) ) ;
#7827=DIRECTION ( 'NONE',  ( -0.9999999999999994449, -3.428898372811998503E-08, 7.236136581007996102E-12 ) ) ;
#7828=ADVANCED_FACE ( 'NONE', ( #20921 ), #16213, .F. ) ;
#7832=CARTESIAN_POINT ( 'NONE',  ( 2.645103879840000172, -78.86345638110998379, 12.07208373076000107 ) ) ;
#7833=CARTESIAN_POINT ( 'NONE',  ( 7.664266801488738068, -55.05053022673565266, -7.892048199452570856 ) ) ;
#7834=ORIENTED_EDGE ( 'NONE', *, *, #45921, .T. ) ;
#7835=CARTESIAN_POINT ( 'NONE',  ( 10.07627163191000008, -18.75000000240999753, -7.601397897754999633 ) ) ;
#7836=CONICAL_SURFACE ( 'NONE', #6873, 0.6999999997695000031, 0.7853981633972997312 ) ;
#7841=CARTESIAN_POINT ( 'NONE',  ( 8.786918763555123135, -79.00520833333479231, 7.904998819390135267 ) ) ;
#7846=B_SPLINE_CURVE_WITH_KNOTS ( 'NONE', 3,
 ( #35925, #45397, #53955, #54246, #4048, #31781 ),
 .UNSPECIFIED., .F., .F.,
 ( 4, 2, 4 ),
 ( 0.000000000000000000, 0.5000000000000000000, 1.000000000000000000 ),
 .UNSPECIFIED. ) ;
#7850=CARTESIAN_POINT ( 'NONE',  ( 0.8973824584412640748, -2.954159113890376887, 3.123983622971040486 ) ) ;
#7855=CARTESIAN_POINT ( 'NONE',  ( 2.234646451474000095, -2.607731223386999808, 3.080979982494000069 ) ) ;
#7857=AXIS2_PLACEMENT_3D ( 'NONE', #56679, #16235, #2666 ) ;
#7858=CARTESIAN_POINT ( 'NONE',  ( -9.643350356198000739, -61.74034317005999384, -8.260133465614998727 ) ) ;
#7860=B_SPLINE_CURVE_WITH_KNOTS ( 'NONE', 3,
 ( #24355, #34347, #25502, #2788, #24641, #29916, #15195, #56809, #6339, #46813, #51812, #55943, #16366, #34058, #43520, #33186, #42367, #20787, #33483, #3081, #37627, #51523, #47684, #6634, #55645, #38211, #51232, #1936, #19928, #11081, #29061, #52096, #47390, #11654, #47103, #6921, #56232, #43231, #42653, #29631, #7210, #15782, #33773, #11368, #42946, #2502, #49106, #16941, #16654, #17814, #7790 ),
 .UNSPECIFIED., .F., .F.,
 ( 4, 2, 2, 2, 2, 2, 2, 2, 2, 1, 2, 2, 2, 2, 2, 2, 2, 2, 2, 2, 2, 2, 1, 2, 1, 2, 4 ),
 ( 0.000000000000000000, 0.03125000000000002776, 0.06250000000000005551, 0.1250000000000000555, 0.1875000000000000833, 0.2500000000000000555, 0.2812500000000000555, 0.3125000000000000555, 0.3437500000000000000, 0.3750000000000000555, 0.4062500000000000555, 0.4375000000000000555, 0.4687500000000000000, 0.5000000000000000000, 0.5312500000000000000, 0.5625000000000000000, 0.6250000000000000000, 0.6874999999999998890, 0.7499999999999998890, 0.7812499999999998890, 0.8124999999999998890, 0.8437500000000000000, 0.8750000000000000000, 0.9062500000000000000, 0.9375000000000000000, 0.9687500000000001110, 1.000000000000000000 ),
 .UNSPECIFIED. ) ;
#7862=CARTESIAN_POINT ( 'NONE',  ( -12.54977952618000003, -16.95167110035999869, 0.03756586072994999581 ) ) ;
#7863=CARTESIAN_POINT ( 'NONE',  ( 11.82764905900999963, -77.33622945496999534, 5.426413045081000419 ) ) ;
#7866=CARTESIAN_POINT ( 'NONE',  ( -4.147314951225999913, -75.89626379192999650, 11.80504683188000037 ) ) ;
#7867=ORIENTED_EDGE ( 'NONE', *, *, #35084, .F. ) ;
#7876=ORIENTED_EDGE ( 'NONE', *, *, #35176, .F. ) ;
#7880=ORIENTED_EDGE ( 'NONE', *, *, #40054, .T. ) ;
#7883=CARTESIAN_POINT ( 'NONE',  ( 12.80900240956999880, -57.04634220890999785, 1.930989144707000005 ) ) ;
#7887=ORIENTED_EDGE ( 'NONE', *, *, #35949, .F. ) ;
#7890=DIRECTION ( 'NONE',  ( -0.9957542233430538570, 0.04890176636660768794, -0.07798810127639639600 ) ) ;
#7893=CARTESIAN_POINT ( 'NONE',  ( -1.779454691337655659, -0.7645432949399240119, 3.096242983992194553 ) ) ;
#7894=ORIENTED_EDGE ( 'NONE', *, *, #8905, .T. ) ;
#7895=CARTESIAN_POINT ( 'NONE',  ( 11.00000000000000000, -18.25000000000000000, 1.016729233725000008E-14 ) ) ;
#7896=VERTEX_POINT ( 'NONE', #11215 ) ;
#7897=CARTESIAN_POINT ( 'NONE',  ( 8.939244305430717574, -79.24132811518457231, -8.111072825249147300 ) ) ;
#7899=CARTESIAN_POINT ( 'NONE',  ( 12.65372179309999900, -57.04935286341999756, -1.750000000000000000 ) ) ;
#7901=CARTESIAN_POINT ( 'NONE',  ( 11.74935832213735587, -77.44163738188349555, -0.7696680151942836279 ) ) ;
#7903=CARTESIAN_POINT ( 'NONE',  ( 12.70722176278216686, -61.21036110583639100, -1.610175936231609484 ) ) ;
#7904=ADVANCED_FACE ( 'NONE', ( #38922 ), #51223, .T. ) ;
#7906=DIRECTION ( 'NONE',  ( 0.000000000000000000, 1.000000000000000000, 0.000000000000000000 ) ) ;
#7907=CARTESIAN_POINT ( 'NONE',  ( 11.88049207238000093, -76.17691755325998315, -3.223263369271999856 ) ) ;
#7910=CARTESIAN_POINT ( 'NONE',  ( -12.43359548536000148, -17.29290601378000147, 0.8500179128024000219 ) ) ;
#7912=DIRECTION ( 'NONE',  ( 0.000000000000000000, 1.000000000000000000, 0.000000000000000000 ) ) ;
#7914=CARTESIAN_POINT ( 'NONE',  ( 11.75000000000000000, -76.45000000000000284, 0.000000000000000000 ) ) ;
#7915=CARTESIAN_POINT ( 'NONE',  ( -1.980584515752000119, -23.26485146623999967, 12.76303204602000108 ) ) ;
#7919=DIRECTION ( 'NONE',  ( 0.000000000000000000, 0.000000000000000000, 1.000000000000000000 ) ) ;
#7921=ADVANCED_FACE ( 'NONE', ( #43656 ), #7836, .F. ) ;
#7922=CARTESIAN_POINT ( 'NONE',  ( 0.5109974968053999644, -3.332071030359000208, 3.520844556087999955 ) ) ;
#7925=CARTESIAN_POINT ( 'NONE',  ( -6.183644282731068920, -75.80000000000002558, 10.16304460950663113 ) ) ;
#7929=ORIENTED_EDGE ( 'NONE', *, *, #19590, .F. ) ;
#7930=CARTESIAN_POINT ( 'NONE',  ( -10.59551070212000035, -21.75648180056000314, -7.678690995204998870 ) ) ;
#7935=CARTESIAN_POINT ( 'NONE',  ( -3.850958688833999943, -1.225056440563999871, -0.3160333990881999955 ) ) ;
#7937=CARTESIAN_POINT ( 'NONE',  ( 12.77568181202000019, -25.26511628633999962, -0.5294980821347999855 ) ) ;
#7943=DIRECTION ( 'NONE',  ( -1.000000000000000000, 0.000000000000000000, 0.000000000000000000 ) ) ;
#7944=CARTESIAN_POINT ( 'NONE',  ( -10.59548767699999949, -57.04263462147999775, -7.678667886061999681 ) ) ;
#7946=AXIS2_PLACEMENT_3D ( 'NONE', #48584, #26130, #8411 ) ;
#7949=CARTESIAN_POINT ( 'NONE',  ( 5.208980231641255010, -77.85915179526145380, -10.56064782346102682 ) ) ;
#7950=CARTESIAN_POINT ( 'NONE',  ( -1.997276839918471714, -1.072916666666666963, -2.598917237794086788 ) ) ;
#7951=CARTESIAN_POINT ( 'NONE',  ( -12.49168451100999988, -60.09848884406000025, 1.667916687331000070 ) ) ;
#7952=CARTESIAN_POINT ( 'NONE',  ( -9.422860735104000796, -53.54048607621999878, -8.643926020445999114 ) ) ;
#7958=ORIENTED_EDGE ( 'NONE', *, *, #44295, .T. ) ;
#7960=DIRECTION ( 'NONE',  ( 1.000000000000000000, 0.000000000000000000, 0.000000000000000000 ) ) ;
#7961=EDGE_CURVE ( 'NONE', #28651, #49809, #33906, .T. ) ;
#7965=CYLINDRICAL_SURFACE ( 'NONE', #31966, 12.50000000000000000 ) ;
#7966=CARTESIAN_POINT ( 'NONE',  ( -0.5999999999999999778, -23.15000000000999947, 11.79999999999999893 ) ) ;
#7967=CARTESIAN_POINT ( 'NONE',  ( -3.078285613438000112, -78.56286269907000985, 12.42192206172999924 ) ) ;
#7970=CARTESIAN_POINT ( 'NONE',  ( -12.51072239526000196, -26.30294702885999669, -0.7871079366006996647 ) ) ;
#7974=ADVANCED_FACE ( 'NONE', ( #51370 ), #28907, .T. ) ;
#7979=DIRECTION ( 'NONE',  ( 0.000000000000000000, -1.000000000000000000, 0.000000000000000000 ) ) ;
#7982=DIRECTION ( 'NONE',  ( 0.9999476293090542312, 0.000000000000000000, 0.01023418971888952027 ) ) ;
#7983=CARTESIAN_POINT ( 'NONE',  ( 12.83044027760000105, -23.30639784948999704, 2.062670899361999766 ) ) ;
#7990=CIRCLE ( 'NONE', #42906, 0.8000000000000011546 ) ;
#7992=ORIENTED_EDGE ( 'NONE', *, *, #44758, .F. ) ;
#7994=VECTOR ( 'NONE', #31577, 1000.000000000000114 ) ;
#7998=CARTESIAN_POINT ( 'NONE',  ( -12.70259395227543209, -17.26112126506535915, 1.314575638808931579 ) ) ;
#7999=B_SPLINE_CURVE_WITH_KNOTS ( 'NONE', 3,
 ( #8268, #44005, #49827, #30687, #48725, #27363 ),
 .UNSPECIFIED., .F., .F.,
 ( 4, 1, 1, 4 ),
 ( 0.000000000000000000, 0.3333333333333000081, 0.6666666666667000474, 1.000000000000000000 ),
 .UNSPECIFIED. ) ;
#8001=CARTESIAN_POINT ( 'NONE',  ( 3.290942002251577403, -1.971106319304349208, -1.249796515420581455 ) ) ;
#8003=CARTESIAN_POINT ( 'NONE',  ( -1.798954018885000172, -55.58469026579999905, -12.61117007300000026 ) ) ;
#8004=CARTESIAN_POINT ( 'NONE',  ( 9.770175552643170391, -75.99682500216157166, 6.527251886581928453 ) ) ;
#8006=ORIENTED_EDGE ( 'NONE', *, *, #27932, .T. ) ;
#8007=DIRECTION ( 'NONE',  ( 0.000000000000000000, 1.000000000000000000, 0.000000000000000000 ) ) ;
#8008=CARTESIAN_POINT ( 'NONE',  ( -11.74590880730695908, -77.18882810128452832, 1.536480942173005682 ) ) ;
#8009=CIRCLE ( 'NONE', #7087, 13.86363636363999952 ) ;
#8010=CARTESIAN_POINT ( 'NONE',  ( -8.335659130299518438, -78.76230910829006859, -8.330744675050686610 ) ) ;
#8011=DIRECTION ( 'NONE',  ( 0.000000000000000000, 0.000000000000000000, -1.000000000000000000 ) ) ;
#8013=CARTESIAN_POINT ( 'NONE',  ( 0.1380878922962947286, -16.77265597675712172, 12.70555840932531488 ) ) ;
#8016=CARTESIAN_POINT ( 'NONE',  ( -7.764217752296561414, -61.05600304933474121, 10.21028588418797867 ) ) ;
#8017=VERTEX_POINT ( 'NONE', #25062 ) ;
#8018=EDGE_CURVE ( 'NONE', #54902, #11044, #44575, .T. ) ;
#8028=DIRECTION ( 'NONE',  ( 1.000000000000000000, 0.000000000000000000, 0.000000000000000000 ) ) ;
#8029=CARTESIAN_POINT ( 'NONE',  ( -12.70556836333273409, -62.02772277294080538, -0.2642470009393159125 ) ) ;
#8030=AXIS2_PLACEMENT_3D ( 'NONE', #11092, #47118, #14907 ) ;
#8031=CARTESIAN_POINT ( 'NONE',  ( -5.917523019358107206, -76.21666666666666856, 10.26699006316250795 ) ) ;
#8032=ORIENTED_EDGE ( 'NONE', *, *, #47268, .T. ) ;
#8033=ORIENTED_EDGE ( 'NONE', *, *, #31603, .T. ) ;
#8034=CARTESIAN_POINT ( 'NONE',  ( -12.77297374709000088, -54.07184670079000455, -1.476174539902000094 ) ) ;
#8035=ADVANCED_FACE ( 'NONE', ( #51668 ), #9635, .F. ) ;
#8036=CONICAL_SURFACE ( 'NONE', #15596, 12.14999999923000118, 0.7853981633972997312 ) ;
#8037=ORIENTED_EDGE ( 'NONE', *, *, #13088, .T. ) ;
#8038=CARTESIAN_POINT ( 'NONE',  ( -3.911342194028000208, -78.65116864382999040, -11.62327352135999980 ) ) ;
#8039=ORIENTED_EDGE ( 'NONE', *, *, #6580, .T. ) ;
#8047=EDGE_CURVE ( 'NONE', #28865, #32105, #31493, .T. ) ;
#8055=CARTESIAN_POINT ( 'NONE',  ( 7.640030139755999983, -23.30716934606000024, 10.18491068059999805 ) ) ;
#8059=DIRECTION ( 'NONE',  ( -0.7071067811865475727, 0.000000000000000000, 0.7071067811865475727 ) ) ;
#8064=CARTESIAN_POINT ( 'NONE',  ( -12.50000000000000000, -60.24678171298000251, -1.250000000000000000 ) ) ;
#8066=CARTESIAN_POINT ( 'NONE',  ( -9.966229686710001090, -18.33098097385000003, -7.657726530248999630 ) ) ;
#8068=CARTESIAN_POINT ( 'NONE',  ( -1.814305421036000121, -17.71058030669000161, -12.78003582253000125 ) ) ;
#8069=EDGE_CURVE ( 'NONE', #11901, #48636, #19407, .T. ) ;
#8070=DIRECTION ( 'NONE',  ( -1.893719483827980309E-11, 1.538483568841980365E-07, 0.9999999999999882316 ) ) ;
#8071=CARTESIAN_POINT ( 'NONE',  ( 10.18589226633000067, -60.08917723397000543, -7.641012305240000302 ) ) ;
#8074=CARTESIAN_POINT ( 'NONE',  ( 0.000000000000000000, -28.92928575306000383, 0.000000000000000000 ) ) ;
#8077=CARTESIAN_POINT ( 'NONE',  ( 11.90000000000000036, -21.00000000000000000, 0.6999999999999999556 ) ) ;
#8078=CARTESIAN_POINT ( 'NONE',  ( 1.798368564629000188, -55.60363242921000193, 12.61278090839000043 ) ) ;
#8080=CARTESIAN_POINT ( 'NONE',  ( -12.58338334669999981, -21.74800977511999989, 1.667961445601999992 ) ) ;
#8081=CARTESIAN_POINT ( 'NONE',  ( -2.870258726797999760, -3.078587262672000335, 2.247988175434000091 ) ) ;
#8084=CARTESIAN_POINT ( 'NONE',  ( -12.48408657656000109, -55.43026141536999774, 1.669508654504999967 ) ) ;
#8086=CARTESIAN_POINT ( 'NONE',  ( -3.248580004278440292, -2.091064288162170381, 0.4260749490998382294 ) ) ;
#8087=CARTESIAN_POINT ( 'NONE',  ( 0.8506806241676642122, -3.145833333333332593, -3.165411199172024848 ) ) ;
#8088=AXIS2_PLACEMENT_3D ( 'NONE', #55352, #14312, #45342 ) ;
#8091=CARTESIAN_POINT ( 'NONE',  ( 1.750000000001000089, -55.55000001292999912, 12.56594318049000059 ) ) ;
#8092=EDGE_CURVE ( 'NONE', #21405, #38037, #48382, .T. ) ;
#8094=CARTESIAN_POINT ( 'NONE',  ( 10.74237452437923501, -76.41648142056769188, -4.760415518113283007 ) ) ;
#8097=DIRECTION ( 'NONE',  ( 0.000000000000000000, -1.000000000000000000, 0.000000000000000000 ) ) ;
#8100=CARTESIAN_POINT ( 'NONE',  ( 0.2548462785871886682, -3.469750342128967269, 3.250954444181449965 ) ) ;
#8102=CARTESIAN_POINT ( 'NONE',  ( -12.50000000000000000, -39.49523982883999906, 0.000000000000000000 ) ) ;
#8103=CARTESIAN_POINT ( 'NONE',  ( -8.274781782264163610, -17.02110650125764479, -9.689260013727274412 ) ) ;
#8104=ORIENTED_EDGE ( 'NONE', *, *, #14095, .T. ) ;
#8109=ORIENTED_EDGE ( 'NONE', *, *, #49807, .T. ) ;
#8112=CARTESIAN_POINT ( 'NONE',  ( 0.000000000000000000, -39.30476017083000073, 0.000000000000000000 ) ) ;
#8113=ORIENTED_EDGE ( 'NONE', *, *, #890, .T. ) ;
#8114=DIRECTION ( 'NONE',  ( -0.7071067811865475727, 0.000000000000000000, 0.7071067811865475727 ) ) ;
#8119=ORIENTED_EDGE ( 'NONE', *, *, #49214, .T. ) ;
#8121=CARTESIAN_POINT ( 'NONE',  ( -5.924797529000001006, -78.83385696754000094, 10.67634899623000067 ) ) ;
#8124=CARTESIAN_POINT ( 'NONE',  ( 12.76303204513999923, -55.53514852210999919, -1.980584515753000208 ) ) ;
#8127=AXIS2_PLACEMENT_3D ( 'NONE', #3785, #21786, #57803 ) ;
#8129=CARTESIAN_POINT ( 'NONE',  ( -1.004305231718999991, -1.000000000000000000, 3.090933677959000203 ) ) ;
#8133=CARTESIAN_POINT ( 'NONE',  ( -1.235365865572026101, -79.05208333334985582, 11.80208333293604461 ) ) ;
#8134=CARTESIAN_POINT ( 'NONE',  ( -9.073214995490001655, -77.80567315384000437, -8.802385182600000135 ) ) ;
#8139=CARTESIAN_POINT ( 'NONE',  ( -10.42274798266000069, -57.04634220890999785, 7.691916945423999508 ) ) ;
#8140=CARTESIAN_POINT ( 'NONE',  ( -1.250993231609307310, -3.007667436560337304, 2.998783452090319823 ) ) ;
#8142=EDGE_CURVE ( 'NONE', #14039, #54879, #2687, .T. ) ;
#8143=FACE_OUTER_BOUND ( 'NONE', #48287, .T. ) ;
#8146=CARTESIAN_POINT ( 'NONE',  ( -2.809159726167000048, -3.376266856787000226, -2.568020482856000264 ) ) ;
#8148=EDGE_LOOP ( 'NONE', ( #9860, #36928, #2033, #31364 ) ) ;
#8149=CARTESIAN_POINT ( 'NONE',  ( -7.657745562929999750, -60.46920625093000012, -9.966193613345000202 ) ) ;
#8150=EDGE_CURVE ( 'NONE', #46551, #52925, #52142, .T. ) ;
#8153=CARTESIAN_POINT ( 'NONE',  ( -12.79895942954000176, -18.19538174383999873, -2.015930660725000045 ) ) ;
#8154=CARTESIAN_POINT ( 'NONE',  ( -1.189541931187000134, -77.16971553208000500, -12.95855809378999979 ) ) ;
#8156=CARTESIAN_POINT ( 'NONE',  ( 12.79999999996999982, -0.1000000000339999751, -4.310453117238000074E-10 ) ) ;
#8157=CARTESIAN_POINT ( 'NONE',  ( -4.630778388809000390, -76.57449046486000555, 11.29997541932999994 ) ) ;
#8159=EDGE_CURVE ( 'NONE', #33091, #39794, #54028, .T. ) ;
#8177=DIRECTION ( 'NONE',  ( 1.000000000000000000, 0.000000000000000000, 0.000000000000000000 ) ) ;
#8180=VERTEX_POINT ( 'NONE', #47388 ) ;
#8181=VECTOR ( 'NONE', #27637, 1000.000000000000000 ) ;
#8182=ORIENTED_EDGE ( 'NONE', *, *, #46535, .T. ) ;
#8184=CARTESIAN_POINT ( 'NONE',  ( -0.7706254096772040540, -78.07838742812036514, 11.74774115849858980 ) ) ;
#8185=DIRECTION ( 'NONE',  ( -1.000000000000000000, 0.000000000000000000, 0.000000000000000000 ) ) ;
#8186=EDGE_LOOP ( 'NONE', ( #17095, #26057, #46268, #26463 ) ) ;
#8187=VERTEX_POINT ( 'NONE', #47101 ) ;
#8188=CARTESIAN_POINT ( 'NONE',  ( -5.869402599192000025, -78.46567021303999923, 10.46661899222999992 ) ) ;
#8190=CARTESIAN_POINT ( 'NONE',  ( 7.631896578914999729, -55.57877526445999905, 10.36221705163000095 ) ) ;
#8191=CARTESIAN_POINT ( 'NONE',  ( -0.4764073897351723819, -18.48308356130623054, 10.98970030907993589 ) ) ;
#8196=CARTESIAN_POINT ( 'NONE',  ( -9.422842877294000274, -25.25952027282999879, 8.643944052295999825 ) ) ;
#8197=VECTOR ( 'NONE', #44952, 1000.000000000000000 ) ;
#8201=CYLINDRICAL_SURFACE ( 'NONE', #1910, 0.5000000000000004441 ) ;
#8203=CARTESIAN_POINT ( 'NONE',  ( -8.107762507645800198, -60.31691643837310579, -7.434020715870987672 ) ) ;
#8206=CIRCLE ( 'NONE', #44046, 14.00000000000000000 ) ;
#8209=CARTESIAN_POINT ( 'NONE',  ( 1.980464483675000054, -58.55560170709000545, -12.85140862643000048 ) ) ;
#8210=CARTESIAN_POINT ( 'NONE',  ( 8.096452064242996016, -22.78578169018999944, -13.15643568217000769 ) ) ;
#8212=CARTESIAN_POINT ( 'NONE',  ( -8.485281374238999419, -55.54999999966999980, -8.485281374238999419 ) ) ;
#8214=CARTESIAN_POINT ( 'NONE',  ( -11.51299102148243136, -76.18361529713614289, 2.346991155758191283 ) ) ;
#8219=EDGE_CURVE ( 'NONE', #54533, #57635, #15383, .T. ) ;
#8223=CARTESIAN_POINT ( 'NONE',  ( 7.220923959705269013, -76.97708333333335418, -9.396085398178609438 ) ) ;
#8225=CARTESIAN_POINT ( 'NONE',  ( 2.260467989216000007, -0.8087401806307999985, -2.930715944272999973 ) ) ;
#8227=CARTESIAN_POINT ( 'NONE',  ( 12.54983138327999903, -25.05098386350000084, -0.1356331847737999863 ) ) ;
#8228=CARTESIAN_POINT ( 'NONE',  ( -1.667917367010000040, -60.08056692637000396, 12.49306752636999995 ) ) ;
#8231=CARTESIAN_POINT ( 'NONE',  ( 8.872958366908434868, -25.01010144684876835, -8.813896668998575379 ) ) ;
#8232=DIRECTION ( 'NONE',  ( -2.011981753536000215E-11, -1.000000000000000000, 1.337054718097999961E-10 ) ) ;
#8236=B_SPLINE_CURVE_WITH_KNOTS ( 'NONE', 3,
 ( #47195, #37138, #32696, #10001, #56036, #10286, #6727, #5845, #23851, #46905 ),
 .UNSPECIFIED., .F., .F.,
 ( 4, 2, 2, 2, 4 ),
 ( 0.000000000000000000, 0.2500000000000000555, 0.5000000000000000000, 0.7500000000000000000, 1.000000000000000000 ),
 .UNSPECIFIED. ) ;
#8238=CARTESIAN_POINT ( 'NONE',  ( 0.000000000000000000, 4.040000000000000036, 0.000000000000000000 ) ) ;
#8239=CARTESIAN_POINT ( 'NONE',  ( 3.074415043147969318, -77.84369498227056283, -11.43808899272451463 ) ) ;
#8240=CARTESIAN_POINT ( 'NONE',  ( -1.931086388578000079, -23.29778754190000001, 12.71798269385000069 ) ) ;
#8242=VECTOR ( 'NONE', #2829, 1000.000000000000000 ) ;
#8243=CARTESIAN_POINT ( 'NONE',  ( -10.08162962779999994, -54.08146287347000225, -7.981572332307999673 ) ) ;
#8245=ORIENTED_EDGE ( 'NONE', *, *, #37396, .T. ) ;
#8249=CYLINDRICAL_SURFACE ( 'NONE', #15481, 1.750000000000000000 ) ;
#8252=EDGE_LOOP ( 'NONE', ( #14003, #22409, #40423, #58053 ) ) ;
#8253=EDGE_CURVE ( 'NONE', #29038, #56208, #56230, .T. ) ;
#8255=DIRECTION ( 'NONE',  ( -1.000000000000000000, 0.000000000000000000, 0.000000000000000000 ) ) ;
#8258=CARTESIAN_POINT ( 'NONE',  ( 7.406580528771000260, -77.66714066711000442, -10.82165712228000132 ) ) ;
#8260=CARTESIAN_POINT ( 'NONE',  ( 12.51072239526000196, -26.30294702885999669, -0.7871079366006996647 ) ) ;
#8262=DIRECTION ( 'NONE',  ( -0.07798810297684731496, 0.04890180918263831167, -0.9957542211071653826 ) ) ;
#8264=CARTESIAN_POINT ( 'NONE',  ( 7.635939924825046354, -18.22474192286703598, 10.36595855977228453 ) ) ;
#8266=CARTESIAN_POINT ( 'NONE',  ( 6.153863461931999623, -76.21865827134000426, -10.66140155521000032 ) ) ;
#8268=CARTESIAN_POINT ( 'NONE',  ( -12.56594317989000054, -23.24999999414999863, -1.750000000001000089 ) ) ;
#8270=CARTESIAN_POINT ( 'NONE',  ( 1.978728478177648853, -3.021815653195938367, -2.910175349659095634 ) ) ;
#8271=CARTESIAN_POINT ( 'NONE',  ( 12.69616050742999924, -21.75171076523999858, 1.799475304559999822 ) ) ;
#8273=CARTESIAN_POINT ( 'NONE',  ( -8.813891479790338934, -61.81010130340408892, -8.872963529899354995 ) ) ;
#8275=CARTESIAN_POINT ( 'NONE',  ( 10.35747145892000098, -23.31584731985000047, -7.626500777234999973 ) ) ;
#8278=B_SPLINE_SURFACE_WITH_KNOTS ( 'NONE', 3, 3, ( 
 ( #3463, #41156, #749, #40870 ),
 ( #461, #45898, #18441, #36431 ),
 ( #54458, #18728, #36722, #5430 ),
 ( #54736, #57194, #4566, #21469 ),
 ( #35843, #53872, #13405, #24320 ),
 ( #55318, #24020, #6306, #15160 ),
 ( #29030, #20187, #1902, #19896 ),
 ( #37888, #5720, #37010, #47360 ),
 ( #11332, #42335, #33744, #28731 ),
 ( #51780, #19019, #56200, #10166 ),
 ( #33156, #55613, #51200, #23730 ),
 ( #24609, #55910, #38179, #55027 ),
 ( #10754, #23439, #46782, #10452 ),
 ( #32567, #42624, #1318, #46486 ),
 ( #15463, #50615, #2188, #33454 ),
 ( #51491, #11049, #47070, #19596 ),
 ( #37596, #28141, #28439, #6599 ) ),
 .UNSPECIFIED., .F., .F., .F.,
 ( 4, 1, 1, 1, 1, 1, 1, 1, 1, 1, 1, 1, 1, 1, 4 ),
 ( 4, 4 ),
 ( -0.01011408452870000106, 0.000000000000000000, 0.08333333333333001192, 0.1666666666667000196, 0.2500000000000000000, 0.3333333333333000081, 0.4166666666666999919, 0.5000000000000000000, 0.5833333333333000637, 0.6666666666667000474, 0.7500000000000000000, 0.8333333333333000637, 0.9166666666667000474, 1.000000000000000000, 1.010362559107000013 ),
 ( -0.3559705546267999954, 1.357612419600999987 ),
 .UNSPECIFIED. ) ;
#8280=VERTEX_POINT ( 'NONE', #42944 ) ;
#8286=CARTESIAN_POINT ( 'NONE',  ( -12.50000000000000000, -55.54999999966999980, 1.250000000000000000 ) ) ;
#8289=CARTESIAN_POINT ( 'NONE',  ( -10.36597333712761326, -23.77522429014145544, -7.635925938716360051 ) ) ;
#8290=CARTESIAN_POINT ( 'NONE',  ( 11.67550463150810991, -75.95899070002479903, 1.336096097494961832 ) ) ;
#8292=EDGE_LOOP ( 'NONE', ( #20254, #42892, #11249, #48989 ) ) ;
#8295=CARTESIAN_POINT ( 'NONE',  ( -5.913247735470008593, -77.11512497811247613, 10.26344855921360733 ) ) ;
#8302=CARTESIAN_POINT ( 'NONE',  ( 1.217390015642536349, -17.18106975072029741, 12.70229597940824107 ) ) ;
#8311=EDGE_CURVE ( 'NONE', #19156, #46351, #47484, .T. ) ;
#8314=CARTESIAN_POINT ( 'NONE',  ( 10.99071003982047579, -23.54576790506894923, -0.4528411669651079552 ) ) ;
#8317=CARTESIAN_POINT ( 'NONE',  ( 8.813906588475214576, -16.98989792586488434, -8.872948313418005384 ) ) ;
#8319=CARTESIAN_POINT ( 'NONE',  ( -10.07627163191000008, -23.24999999758999536, -7.601397897754999633 ) ) ;
#8321=ORIENTED_EDGE ( 'NONE', *, *, #48454, .T. ) ;
#8324=EDGE_LOOP ( 'NONE', ( #39747, #43908, #40648, #2977 ) ) ;
#8325=FACE_OUTER_BOUND ( 'NONE', #28064, .T. ) ;
#8327=CARTESIAN_POINT ( 'NONE',  ( 9.029867227896000159, -25.33262194290999858, 9.038867509618000895 ) ) ;
#8329=CIRCLE ( 'NONE', #4554, 1.750000000000000222 ) ;
#8333=ORIENTED_EDGE ( 'NONE', *, *, #53277, .F. ) ;
#8334=VERTEX_POINT ( 'NONE', #53234 ) ;
#8336=DIRECTION ( 'NONE',  ( 0.000000000000000000, -1.000000000000000000, 0.000000000000000000 ) ) ;
#8338=ADVANCED_FACE ( 'NONE', ( #40236 ), #29520, .F. ) ;
#8340=CARTESIAN_POINT ( 'NONE',  ( 6.585972550682999582, -76.08593941427999141, -11.16860520736000062 ) ) ;
#8343=CARTESIAN_POINT ( 'NONE',  ( 7.792421629638690561, -54.50899070338012820, -10.18245656324170412 ) ) ;
#8345=DIRECTION ( 'NONE',  ( 0.000000000000000000, 1.000000000000000000, 0.000000000000000000 ) ) ;
#8348=ORIENTED_EDGE ( 'NONE', *, *, #5405, .F. ) ;
#8350=CARTESIAN_POINT ( 'NONE',  ( -7.620012214408999895, -55.59439747889000216, 10.53562508622999871 ) ) ;
#8351=CARTESIAN_POINT ( 'NONE',  ( 1.001315001700999963, -54.11477588220000001, 12.50000000000000000 ) ) ;
#8352=CARTESIAN_POINT ( 'NONE',  ( -12.70722176278296267, -61.21036110582522127, 1.610175936235292760 ) ) ;
#8354=CARTESIAN_POINT ( 'NONE',  ( -1.698401934077000019, -17.77985954096000043, -12.66748707612999958 ) ) ;
#8355=DIRECTION ( 'NONE',  ( 0.0001178721535688749143, 0.000000000000000000, -0.9999999930530777403 ) ) ;
#8359=CARTESIAN_POINT ( 'NONE',  ( 0.000000000000000000, 4.040000000000000036, 0.000000000000000000 ) ) ;
#8362=CARTESIAN_POINT ( 'NONE',  ( 12.00000000000000000, -18.84999999999999787, 0.000000000000000000 ) ) ;
#8364=CARTESIAN_POINT ( 'NONE',  ( 3.500567196895000510, -2.403996213896999912, 1.018756774997999992 ) ) ;
#8367=CARTESIAN_POINT ( 'NONE',  ( 3.250000000000000444, -1.739583333333333037, -0.4254240051736113415 ) ) ;
#8368=FACE_OUTER_BOUND ( 'NONE', #40784, .T. ) ;
#8369=CARTESIAN_POINT ( 'NONE',  ( -1.632307027704000157, -60.46927189524000568, 12.46200249215000078 ) ) ;
#8370=CARTESIAN_POINT ( 'NONE',  ( 12.77656766273999978, -16.68801851262999847, 0.1555695072196000006 ) ) ;
#8374=CARTESIAN_POINT ( 'NONE',  ( -8.714384359252477452, -76.89210801961958452, 8.361740495897693748 ) ) ;
#8375=EDGE_CURVE ( 'NONE', #27205, #37084, #44625, .T. ) ;
#8380=CYLINDRICAL_SURFACE ( 'NONE', #57640, 0.5000000000000004441 ) ;
#8381=CARTESIAN_POINT ( 'NONE',  ( -2.839805762151337731, -2.541666666666666519, -1.636761686205423949 ) ) ;
#8383=CARTESIAN_POINT ( 'NONE',  ( -12.50409240825461765, -24.52129362382453337, -1.233800929768802401 ) ) ;
#8384=CARTESIAN_POINT ( 'NONE',  ( -8.894932048719153883, -16.77190732483956737, -9.073469156704689453 ) ) ;
#8385=CIRCLE ( 'NONE', #6501, 4.999999999999996447 ) ;
#8386=EDGE_LOOP ( 'NONE', ( #57549, #46961, #36867, #2539 ) ) ;
#8387=B_SPLINE_CURVE_WITH_KNOTS ( 'NONE', 3,
 ( #24498, #38931, #29768, #10935, #7355, #34199 ),
 .UNSPECIFIED., .F., .F.,
 ( 4, 1, 1, 4 ),
 ( 0.000000000000000000, 0.3333333333333000081, 0.6666666666667000474, 1.000000000000000000 ),
 .UNSPECIFIED. ) ;
#8388=CARTESIAN_POINT ( 'NONE',  ( 8.583665413911145237, -53.82814424961789257, 9.102144265363879327 ) ) ;
#8389=DIRECTION ( 'NONE',  ( 0.000000000000000000, -1.000000000000000000, 0.000000000000000000 ) ) ;
#8392=ORIENTED_EDGE ( 'NONE', *, *, #46302, .F. ) ;
#8396=CARTESIAN_POINT ( 'NONE',  ( -12.50745077490000057, -24.99994448286999926, -2.662114616045000020E-09 ) ) ;
#8398=DIRECTION ( 'NONE',  ( 0.000000000000000000, -1.000000000000000000, 0.000000000000000000 ) ) ;
#8401=CARTESIAN_POINT ( 'NONE',  ( 1.484804496640999893, -24.71869153383000040, -12.77261165608999960 ) ) ;
#8406=CARTESIAN_POINT ( 'NONE',  ( 0.4517264908803999557, -78.63353063649999797, -12.35021147003999964 ) ) ;
#8408=CARTESIAN_POINT ( 'NONE',  ( 0.000000000000000000, -45.91785611817000046, 0.000000000000000000 ) ) ;
#8411=DIRECTION ( 'NONE',  ( 1.000000000000000000, 0.000000000000000000, 0.000000000000000000 ) ) ;
#8412=VECTOR ( 'NONE', #16989, 1000.000000000000227 ) ;
#8413=CARTESIAN_POINT ( 'NONE',  ( 12.00000000000000000, -23.25000000000000000, 0.000000000000000000 ) ) ;
#8415=CARTESIAN_POINT ( 'NONE',  ( 7.344138154013000630, -78.17792498495001041, -10.86413439232000044 ) ) ;
#8416=EDGE_CURVE ( 'NONE', #31547, #27322, #11644, .T. ) ;
#8417=CARTESIAN_POINT ( 'NONE',  ( -1.001315001699999874, -54.11477588220000001, -12.50000000000000000 ) ) ;
#8421=CIRCLE ( 'NONE', #31974, 0.5000000000000004441 ) ;
#8422=CARTESIAN_POINT ( 'NONE',  ( -10.35845608626999947, -60.09778754156999980, 7.627487525433000570 ) ) ;
#8423=CARTESIAN_POINT ( 'NONE',  ( 0.4879870162820874047, -2.964277948476393920, 3.219086890419578406 ) ) ;
#8425=AXIS2_PLACEMENT_3D ( 'NONE', #38537, #7247, #48571 ) ;
#8430=CARTESIAN_POINT ( 'NONE',  ( -3.593558748265999636, -1.745109825020999983, 0.1459214154804999997 ) ) ;
#8432=ORIENTED_EDGE ( 'NONE', *, *, #13062, .F. ) ;
#8437=CARTESIAN_POINT ( 'NONE',  ( 12.55073801092999908, -77.21139148068000679, -3.437763296274999991 ) ) ;
#8442=EDGE_CURVE ( 'NONE', #27322, #15167, #30780, .T. ) ;
#8444=CARTESIAN_POINT ( 'NONE',  ( -1.930989144707000005, -21.75365779208000205, -12.80900240953000058 ) ) ;
#8446=ADVANCED_FACE ( 'NONE', ( #44374, #3926 ), #35497, .T. ) ;
#8448=CARTESIAN_POINT ( 'NONE',  ( -2.062597265787999845, -59.58461666436000570, -12.87024489159000140 ) ) ;
#8450=ORIENTED_EDGE ( 'NONE', *, *, #45774, .T. ) ;
#8455=ORIENTED_EDGE ( 'NONE', *, *, #38169, .T. ) ;
#8456=CARTESIAN_POINT ( 'NONE',  ( -7.666647577134583003, -55.04957415510975949, -7.889735440108408326 ) ) ;
#8458=ORIENTED_EDGE ( 'NONE', *, *, #26849, .T. ) ;
#8460=AXIS2_PLACEMENT_3D ( 'NONE', #52403, #52974, #25811 ) ;
#8461=EDGE_LOOP ( 'NONE', ( #35980, #240, #9526, #11616 ) ) ;
#8463=CIRCLE ( 'NONE', #9414, 12.50000000000000000 ) ;
#8464=EDGE_CURVE ( 'NONE', #50392, #50856, #46444, .T. ) ;
#8466=CARTESIAN_POINT ( 'NONE',  ( 12.04999999926000243, -79.29999999926000953, 5.384918141074000180E-09 ) ) ;
#8468=CARTESIAN_POINT ( 'NONE',  ( 10.99069764842708175, -18.45457471225845580, 0.4531388007100142223 ) ) ;
#8472=CARTESIAN_POINT ( 'NONE',  ( 0.000000000000000000, 0.000000000000000000, 12.00000000000000000 ) ) ;
#8473=B_SPLINE_CURVE_WITH_KNOTS ( 'NONE', 3,
 ( #46128, #31923, #23376, #9509, #5083, #685 ),
 .UNSPECIFIED., .F., .F.,
 ( 4, 2, 4 ),
 ( 0.000000000000000000, 0.5000000000000000000, 1.000000000000000000 ),
 .UNSPECIFIED. ) ;
#8477=CARTESIAN_POINT ( 'NONE',  ( -1.247385798842000071, -54.32277743483000165, 12.50301438874000048 ) ) ;
#8478=CARTESIAN_POINT ( 'NONE',  ( 7.705142895592000052, -58.55083378327000077, -10.24998526315000014 ) ) ;
#8483=B_SPLINE_CURVE_WITH_KNOTS ( 'NONE', 3,
 ( #41813, #817, #14067, #13770, #1388, #55389 ),
 .UNSPECIFIED., .F., .F.,
 ( 4, 1, 1, 4 ),
 ( 0.000000000000000000, 0.3333333333333000081, 0.6666666666667000474, 1.000000000000000000 ),
 .UNSPECIFIED. ) ;
#8487=FACE_OUTER_BOUND ( 'NONE', #37661, .T. ) ;
#8488=CARTESIAN_POINT ( 'NONE',  ( -1.798954018882000128, -23.21530973387000074, 12.61117007302000026 ) ) ;
#8489=LINE ( 'NONE', #53079, #1623 ) ;
#8490=CARTESIAN_POINT ( 'NONE',  ( -1.067023211856000131, -1.656831454374000145, -3.462241726570000289 ) ) ;
#8493=CARTESIAN_POINT ( 'NONE',  ( 12.54983138332999815, -61.85098386317000063, -0.1356331847737999863 ) ) ;
#8494=DIRECTION ( 'NONE',  ( -1.000000000000000000, 0.000000000000000000, 0.000000000000000000 ) ) ;
#8495=FACE_OUTER_BOUND ( 'NONE', #24395, .T. ) ;
#8497=CIRCLE ( 'NONE', #7594, 12.57042253521000141 ) ;
#8508=CARTESIAN_POINT ( 'NONE',  ( -14.00000000000000000, -72.39999999999999147, 0.000000000000000000 ) ) ;
#8511=CARTESIAN_POINT ( 'NONE',  ( -3.238788824226999985, -1.555722370088000073, -0.4869776969663000554 ) ) ;
#8513=CARTESIAN_POINT ( 'NONE',  ( 12.65989858207000118, -24.94344101132999825, -0.9743214026256000748 ) ) ;
#8515=ORIENTED_EDGE ( 'NONE', *, *, #57030, .F. ) ;
#8518=CARTESIAN_POINT ( 'NONE',  ( 0.000000000000000000, -0.1000000063292999924, 0.000000000000000000 ) ) ;
#8523=VERTEX_POINT ( 'NONE', #29845 ) ;
#8525=DIRECTION ( 'NONE',  ( 0.000000000000000000, -1.000000000000000000, 0.000000000000000000 ) ) ;
#8526=CARTESIAN_POINT ( 'NONE',  ( 8.179414027362144068, -61.54093020446555329, -9.502908391260222132 ) ) ;
#8529=ORIENTED_EDGE ( 'NONE', *, *, #41895, .F. ) ;
#8530=ADVANCED_FACE ( 'NONE', ( #19855 ), #19763, .F. ) ;
#8531=CARTESIAN_POINT ( 'NONE',  ( -12.49306752631999906, -55.51943307300000185, 1.667917367010000040 ) ) ;
#8532=CARTESIAN_POINT ( 'NONE',  ( -7.758899961864000439, -54.49918178063000340, -10.31442855571999928 ) ) ;
#8534=ORIENTED_EDGE ( 'NONE', *, *, #51594, .T. ) ;
#8535=EDGE_LOOP ( 'NONE', ( #48493, #5793, #106, #38544 ) ) ;
#8537=DIRECTION ( 'NONE',  ( 1.000000000000000000, 0.000000000000000000, 0.000000000000000000 ) ) ;
#8538=AXIS2_PLACEMENT_3D ( 'NONE', #45799, #5334, #18917 ) ;
#8540=ORIENTED_EDGE ( 'NONE', *, *, #48777, .T. ) ;
#8541=CARTESIAN_POINT ( 'NONE',  ( 10.53495272788999948, -18.77289072628000355, 7.618387390369000478 ) ) ;
#8542=AXIS2_PLACEMENT_3D ( 'NONE', #57312, #52888, #20725 ) ;
#8545=CARTESIAN_POINT ( 'NONE',  ( -3.259705057564000530, -77.47669831202999546, 12.53941704951999903 ) ) ;
#8547=CARTESIAN_POINT ( 'NONE',  ( -13.13047446164998711, -19.21421830981000767, -0.8260994316375004365 ) ) ;
#8552=DIRECTION ( 'NONE',  ( 0.7071067811865474617, 0.000000000000000000, 0.7071067811865474617 ) ) ;
#8553=ORIENTED_EDGE ( 'NONE', *, *, #15749, .T. ) ;
#8555=CARTESIAN_POINT ( 'NONE',  ( -1.771468677314999907, -75.90382483601000274, 12.18184739844999953 ) ) ;
#8558=CARTESIAN_POINT ( 'NONE',  ( -1.263607411038969008, -2.945081867600211734, -3.286951345324313767 ) ) ;
#8559=CARTESIAN_POINT ( 'NONE',  ( -8.792808668242045655, -16.77303577624769559, 9.175550543643495871 ) ) ;
#8565=FACE_OUTER_BOUND ( 'NONE', #48626, .T. ) ;
#8568=ADVANCED_FACE ( 'NONE', ( #33413 ), #43430, .F. ) ;
#8571=ORIENTED_EDGE ( 'NONE', *, *, #14100, .F. ) ;
#8572=B_SPLINE_CURVE_WITH_KNOTS ( 'NONE', 3,
 ( #3924, #45267, #31063, #39934, #17505, #44671, #35495, #53525, #8651, #27811 ),
 .UNSPECIFIED., .F., .F.,
 ( 4, 2, 2, 2, 4 ),
 ( 0.000000000000000000, 0.2500000000000000000, 0.5000000000000000000, 0.7500000000000000000, 1.000000000000000000 ),
 .UNSPECIFIED. ) ;
#8574=DIRECTION ( 'NONE',  ( -0.7026410690473250398, -0.1122098755728047209, 0.7026410690473250398 ) ) ;
#8576=LINE ( 'NONE', #22149, #33339 ) ;
#8581=CARTESIAN_POINT ( 'NONE',  ( -2.062323307449999810, -55.57286846775000555, -12.83634826441000065 ) ) ;
#8582=CARTESIAN_POINT ( 'NONE',  ( 11.64020011326665660, -75.96092683841732196, 1.623265142550421203 ) ) ;
#8591=CARTESIAN_POINT ( 'NONE',  ( 1.931736162947209179, -18.23329604289370209, 12.72978979890546292 ) ) ;
#8592=EDGE_CURVE ( 'NONE', #26124, #23569, #39296, .T. ) ;
#8594=CARTESIAN_POINT ( 'NONE',  ( 2.069888253764102792, -78.55744420716430909, 11.57512296172573052 ) ) ;
#8601=DIRECTION ( 'NONE',  ( 0.000000000000000000, 0.000000000000000000, -1.000000000000000000 ) ) ;
#8603=CARTESIAN_POINT ( 'NONE',  ( 12.50386483995752052, -61.58505343581200719, -0.8574420495986169177 ) ) ;
#8604=CARTESIAN_POINT ( 'NONE',  ( -10.99607952893977370, -23.68503250286043027, 0.3139933498860824068 ) ) ;
#8610=CARTESIAN_POINT ( 'NONE',  ( -12.71536556660682926, -60.92544729011922300, -1.781281569003885679 ) ) ;
#8611=CARTESIAN_POINT ( 'NONE',  ( -12.77651065749000026, -25.30896598096000005, -0.04308629978602999955 ) ) ;
#8613=VERTEX_POINT ( 'NONE', #44306 ) ;
#8614=CIRCLE ( 'NONE', #47293, 1.250000000000000444 ) ;
#8616=VERTEX_POINT ( 'NONE', #44601 ) ;
#8617=CARTESIAN_POINT ( 'NONE',  ( -10.61911868076999887, -78.59368720767999150, -6.134606423928000041 ) ) ;
#8618=ORIENTED_EDGE ( 'NONE', *, *, #8716, .F. ) ;
#8619=CARTESIAN_POINT ( 'NONE',  ( 7.646092217281999837, -23.70851177913000285, 10.13691708057999996 ) ) ;
#8622=EDGE_CURVE ( 'NONE', #53336, #43546, #35813, .T. ) ;
#8623=CARTESIAN_POINT ( 'NONE',  ( -12.50657368821661208, -24.97245458995920586, -0.3553454087125454408 ) ) ;
#8626=ORIENTED_EDGE ( 'NONE', *, *, #50416, .T. ) ;
#8628=ORIENTED_EDGE ( 'NONE', *, *, #41760, .T. ) ;
#8632=AXIS2_PLACEMENT_3D ( 'NONE', #49205, #53936, #17916 ) ;
#8634=CARTESIAN_POINT ( 'NONE',  ( -13.11938987471999951, -76.50757595554999568, -0.3223533933333999624 ) ) ;
#8636=CARTESIAN_POINT ( 'NONE',  ( 12.85140862673999784, -58.55560170131000319, 1.980464483675000054 ) ) ;
#8639=FACE_OUTER_BOUND ( 'NONE', #56775, .T. ) ;
#8641=EDGE_CURVE ( 'NONE', #38246, #19156, #10564, .T. ) ;
#8643=ORIENTED_EDGE ( 'NONE', *, *, #54821, .F. ) ;
#8645=CARTESIAN_POINT ( 'NONE',  ( -8.643969996042999426, -53.54046576124999746, 9.422817222679000793 ) ) ;
#8648=CARTESIAN_POINT ( 'NONE',  ( -8.260145278149000347, -17.05964900975000020, -9.643338479001000607 ) ) ;
#8650=CARTESIAN_POINT ( 'NONE',  ( -1.632307027708999936, -18.33072810443000122, -12.46200249212000166 ) ) ;
#8651=CARTESIAN_POINT ( 'NONE',  ( 0.8338927956426691601, -53.99946422210107499, 12.50366901599831060 ) ) ;
#8653=CARTESIAN_POINT ( 'NONE',  ( 0.000000000000000000, 0.000000000000000000, 0.000000000000000000 ) ) ;
#8658=CARTESIAN_POINT ( 'NONE',  ( -0.4268555006395731710, -1.487093160906469036, 3.249579827604153870 ) ) ;
#8659=CARTESIAN_POINT ( 'NONE',  ( 0.005119011380280999966, -53.86186137778000216, 12.43705489340000092 ) ) ;
#8660=CARTESIAN_POINT ( 'NONE',  ( -12.71798280855999863, -23.29778595484999926, 1.931086388455000025 ) ) ;
#8661=CARTESIAN_POINT ( 'NONE',  ( -1.440490910816999870, -2.210199159476000208, 3.695416286417999796 ) ) ;
#8663=CARTESIAN_POINT ( 'NONE',  ( -1.374053708643000007E-14, -74.80000000000001137, 0.000000000000000000 ) ) ;
#8664=DIRECTION ( 'NONE',  ( 0.000000000000000000, -1.000000000000000000, 0.000000000000000000 ) ) ;
#8666=CARTESIAN_POINT ( 'NONE',  ( -1.056237665594999875, -61.84866013665000395, 12.77256098201999990 ) ) ;
#8667=CARTESIAN_POINT ( 'NONE',  ( 12.66314509270999977, -16.82135249322999826, -0.04032083120557000688 ) ) ;
#8669=CYLINDRICAL_SURFACE ( 'NONE', #16948, 0.5000000000000006661 ) ;
#8670=CARTESIAN_POINT ( 'NONE',  ( 10.81498442169830909, -77.23901691334977215, 5.255458039015602267 ) ) ;
#8671=CARTESIAN_POINT ( 'NONE',  ( -10.56602462368999973, -78.44534377886000698, 7.483748555556999804 ) ) ;
#8676=CARTESIAN_POINT ( 'NONE',  ( 12.50745077490000057, -24.99994448286999926, 2.662071812989000278E-09 ) ) ;
#8678=CARTESIAN_POINT ( 'NONE',  ( -12.77656765298000074, -62.11198129881000085, 0.1555235816857000186 ) ) ;
#8680=ADVANCED_FACE ( 'NONE', ( #28547 ), #53341, .F. ) ;
#8681=CARTESIAN_POINT ( 'NONE',  ( -12.55433072264035843, -23.38725213725906471, -1.749897784985361637 ) ) ;
#8683=CARTESIAN_POINT ( 'NONE',  ( 9.546815223802999739, -54.11472046612000497, 8.130854305859999798 ) ) ;
#8688=VERTEX_POINT ( 'NONE', #3157 ) ;
#8691=DIRECTION ( 'NONE',  ( -1.000000000000000000, 0.000000000000000000, 0.000000000000000000 ) ) ;
#8692=ORIENTED_EDGE ( 'NONE', *, *, #33961, .F. ) ;
#8701=ORIENTED_EDGE ( 'NONE', *, *, #51494, .F. ) ;
#8703=CARTESIAN_POINT ( 'NONE',  ( -11.33685376752999829, -78.94881983984001295, -4.534688555742999228 ) ) ;
#8704=VERTEX_POINT ( 'NONE', #17013 ) ;
#8705=EDGE_CURVE ( 'NONE', #50911, #28385, #16812, .T. ) ;
#8706=ORIENTED_EDGE ( 'NONE', *, *, #25996, .T. ) ;
#8707=CYLINDRICAL_SURFACE ( 'NONE', #20700, 0.5000000000000004441 ) ;
#8708=LINE ( 'NONE', #53582, #8412 ) ;
#8711=CARTESIAN_POINT ( 'NONE',  ( 0.000000000000000000, 0.000000000000000000, 0.000000000000000000 ) ) ;
#8713=CARTESIAN_POINT ( 'NONE',  ( -11.86979166781643968, -79.11979166670496966, 1.243547081883744188 ) ) ;
#8714=CARTESIAN_POINT ( 'NONE',  ( 7.079708506942000490, -77.91668243576999942, -10.47296538612000028 ) ) ;
#8716=EDGE_CURVE ( 'NONE', #28402, #4126, #52453, .T. ) ;
#8717=DIRECTION ( 'NONE',  ( 0.000000000000000000, -1.000000000000000000, 0.000000000000000000 ) ) ;
#8720=CARTESIAN_POINT ( 'NONE',  ( -4.310712596281979891, -76.79473241825421326, -11.00476471888044827 ) ) ;
#8725=CARTESIAN_POINT ( 'NONE',  ( 3.171758640500000226, -3.567406026038999922, 1.479846994257000059 ) ) ;
#8728=CARTESIAN_POINT ( 'NONE',  ( -0.3135214471687461368, -23.68581381185224544, 10.99610567419509977 ) ) ;
#8732=CARTESIAN_POINT ( 'NONE',  ( -12.43640296266999989, -17.08252466130999991, 0.05222744260230000046 ) ) ;
#8733=CARTESIAN_POINT ( 'NONE',  ( -9.339950055924999717, -78.04396109509998780, -9.061158367717998985 ) ) ;
#8736=CARTESIAN_POINT ( 'NONE',  ( 12.58335110166999904, -20.25111654322000021, -1.667961430005999945 ) ) ;
#8738=AXIS2_PLACEMENT_3D ( 'NONE', #3495, #3217, #20353 ) ;
#8739=CARTESIAN_POINT ( 'NONE',  ( -8.251802458333543200, -24.80055625133827846, -9.431055090843393884 ) ) ;
#8742=CARTESIAN_POINT ( 'NONE',  ( 7.612971414716000140, -18.67547470641000018, -10.53003223724000037 ) ) ;
#8745=CARTESIAN_POINT ( 'NONE',  ( -3.754890333716000228, -1.311529764407000087, -1.424957469106999941 ) ) ;
#8749=ADVANCED_FACE ( 'NONE', ( #12578 ), #4336, .F. ) ;
#8753=ORIENTED_EDGE ( 'NONE', *, *, #5454, .F. ) ;
#8754=VERTEX_POINT ( 'NONE', #37344 ) ;
#8756=DIRECTION ( 'NONE',  ( 0.000000000000000000, -1.000000000000000000, 0.000000000000000000 ) ) ;
#8762=CARTESIAN_POINT ( 'NONE',  ( 7.429974109838866525, -60.31614597266855782, 8.111636311564803137 ) ) ;
#8763=AXIS2_PLACEMENT_3D ( 'NONE', #15891, #5071, #41081 ) ;
#8765=CARTESIAN_POINT ( 'NONE',  ( -0.4621935165842904203, -1.232020812799707432, 3.993632164156191600 ) ) ;
#8769=EDGE_CURVE ( 'NONE', #11225, #6077, #47940, .T. ) ;
#8772=CARTESIAN_POINT ( 'NONE',  ( 10.01752115540999988, -55.60828330164999755, 7.660412752583999563 ) ) ;
#8773=CARTESIAN_POINT ( 'NONE',  ( -7.653559626094000201, -18.70151115557999688, -10.01235002622999914 ) ) ;
#8776=CARTESIAN_POINT ( 'NONE',  ( 13.86363636363000218, -46.43897132165000130, 1.277887489249999988E-05 ) ) ;
#8778=EDGE_CURVE ( 'NONE', #8841, #56133, #33610, .T. ) ;
#8779=FACE_OUTER_BOUND ( 'NONE', #32211, .T. ) ;
#8780=CARTESIAN_POINT ( 'NONE',  ( -9.395758989562999375, -24.70491532583000449, 8.188252216825999241 ) ) ;
#8781=EDGE_CURVE ( 'NONE', #39540, #3332, #1943, .T. ) ;
#8787=CARTESIAN_POINT ( 'NONE',  ( 1.758095523367999791, -23.72291663880000101, 12.57362173515999970 ) ) ;
#8789=DIRECTION ( 'NONE',  ( 0.7071067811865475727, 0.000000000000000000, 0.7071067811865475727 ) ) ;
#8790=CARTESIAN_POINT ( 'NONE',  ( -3.114032450773999816, -1.916752247163000078, -1.479365640781999947 ) ) ;
#8794=CARTESIAN_POINT ( 'NONE',  ( -1.980584515752000119, -18.73514853375999678, -12.76303204602000108 ) ) ;
#8799=EDGE_CURVE ( 'NONE', #46040, #42021, #30769, .T. ) ;
#8800=CARTESIAN_POINT ( 'NONE',  ( -11.75000000000000000, -76.70000000000000284, 1.487410190129999909E-14 ) ) ;
#8805=VECTOR ( 'NONE', #39272, 1000.000000000000000 ) ;
#8813=CARTESIAN_POINT ( 'NONE',  ( 3.901255009783000105, -1.575525618456000032, 0.9967003545521999630 ) ) ;
#8814=CARTESIAN_POINT ( 'NONE',  ( 13.86301033151605289, -9.638971321655001034, 0.1317488955328472711 ) ) ;
#8815=CARTESIAN_POINT ( 'NONE',  ( 12.77306367228999839, -25.05881314456000197, -1.040970605966999862 ) ) ;
#8816=CARTESIAN_POINT ( 'NONE',  ( -1.667961445601999992, -57.05199022587000002, 12.58338334673999981 ) ) ;
#8818=ADVANCED_FACE ( 'NONE', ( #1355 ), #40650, .F. ) ;
#8819=VECTOR ( 'NONE', #11164, 1000.000000000000000 ) ;
#8820=CARTESIAN_POINT ( 'NONE',  ( -12.72966282067487143, -55.03110224943692685, 1.931329623869216583 ) ) ;
#8824=AXIS2_PLACEMENT_3D ( 'NONE', #1011, #24588, #38155 ) ;
#8829=CARTESIAN_POINT ( 'NONE',  ( -7.223926682746276917, -77.77156318831207216, -9.395512816074530704 ) ) ;
#8830=CARTESIAN_POINT ( 'NONE',  ( -1.423904377294301637, -54.49487194733364959, -12.50677628652253759 ) ) ;
#8832=ORIENTED_EDGE ( 'NONE', *, *, #5160, .F. ) ;
#8833=CARTESIAN_POINT ( 'NONE',  ( -9.650965486062000664, -53.86598967493999623, -8.252456811976999873 ) ) ;
#8839=DIRECTION ( 'NONE',  ( 0.7071067811865474617, 0.000000000000000000, -0.7071067811865474617 ) ) ;
#8841=VERTEX_POINT ( 'NONE', #34929 ) ;
#8843=CARTESIAN_POINT ( 'NONE',  ( -12.00000000000000000, 0.000000000000000000, 0.000000000000000000 ) ) ;
#8845=CARTESIAN_POINT ( 'NONE',  ( 7.468771752218000159, -77.16759889844999520, -10.77882862479000003 ) ) ;
#8847=CARTESIAN_POINT ( 'NONE',  ( 8.096452064242996016, -19.21421830981000056, 13.15643568217000769 ) ) ;
#8849=VECTOR ( 'NONE', #24893, 1000.000000000000227 ) ;
#8853=ORIENTED_EDGE ( 'NONE', *, *, #2118, .F. ) ;
#8855=CARTESIAN_POINT ( 'NONE',  ( 3.295079792876999925, -76.40543611710999983, 11.86077433336000020 ) ) ;
#8857=CARTESIAN_POINT ( 'NONE',  ( 3.574643530366263366, -2.595516844331640538, -0.1804099968710304036 ) ) ;
#8858=CARTESIAN_POINT ( 'NONE',  ( 0.000000000000000000, -33.10361340872000113, 0.000000000000000000 ) ) ;
#8859=CARTESIAN_POINT ( 'NONE',  ( -1.750000000000000000, -20.25022860793999868, 12.65375411744000012 ) ) ;
#8863=CARTESIAN_POINT ( 'NONE',  ( -11.72115528760076941, -77.06915921447735229, -2.879779154500307747 ) ) ;
#8866=B_SPLINE_CURVE_WITH_KNOTS ( 'NONE', 3,
 ( #31390, #14267, #42320, #28423 ),
 .UNSPECIFIED., .F., .F.,
 ( 4, 4 ),
 ( 0.000000000000000000, 1.000000000000000000 ),
 .UNSPECIFIED. ) ;
#8867=VERTEX_POINT ( 'NONE', #52672 ) ;
#8870=DIRECTION ( 'NONE',  ( -1.000000000000000000, 0.000000000000000000, 0.000000000000000000 ) ) ;
#8875=CARTESIAN_POINT ( 'NONE',  ( -1.669724228661999987, -55.43102323432999867, -12.48434610065999983 ) ) ;
#8877=CARTESIAN_POINT ( 'NONE',  ( 9.132460868846187907, -76.00377128848815289, 7.392938176916904247 ) ) ;
#8879=PLANE ( 'NONE',  #15322 ) ;
#8880=ORIENTED_EDGE ( 'NONE', *, *, #25689, .F. ) ;
#8882=DIRECTION ( 'NONE',  ( 0.000000000000000000, 0.000000000000000000, 1.000000000000000000 ) ) ;
#8884=AXIS2_PLACEMENT_3D ( 'NONE', #26539, #13264, #25967 ) ;
#8887=CARTESIAN_POINT ( 'NONE',  ( 12.50000000000000000, -23.25000000000000000, 0.000000000000000000 ) ) ;
#8889=DIRECTION ( 'NONE',  ( 1.000000000000000000, 0.000000000000000000, 0.000000000000000000 ) ) ;
#8891=EDGE_LOOP ( 'NONE', ( #41025, #58290 ) ) ;
#8892=AXIS2_PLACEMENT_3D ( 'NONE', #51816, #20790, #39378 ) ;
#8901=CARTESIAN_POINT ( 'NONE',  ( 11.00000000000000000, -23.75000000000000000, -1.203259120426999909E-14 ) ) ;
#8904=DIRECTION ( 'NONE',  ( -0.7592504785508700227, 0.04890181650103809369, -0.6489586451871750539 ) ) ;
#8905=EDGE_CURVE ( 'NONE', #47045, #37071, #54429, .T. ) ;
#8906=CARTESIAN_POINT ( 'NONE',  ( -1.733997378035443404, -60.32383216727247088, 12.54437956615585215 ) ) ;
#8907=DIRECTION ( 'NONE',  ( -1.000000000000000000, 0.000000000000000000, 0.000000000000000000 ) ) ;
#8908=ADVANCED_FACE ( 'NONE', ( #17519, #21939 ), #49114, .T. ) ;
#8910=ORIENTED_EDGE ( 'NONE', *, *, #41494, .F. ) ;
#8911=ORIENTED_EDGE ( 'NONE', *, *, #49590, .T. ) ;
#8917=CARTESIAN_POINT ( 'NONE',  ( 8.188293269161999177, -24.70494400568999893, 9.395718629078000816 ) ) ;
#8918=CARTESIAN_POINT ( 'NONE',  ( 8.190817883596546167, -55.56980390652893220, -7.342377162853135353 ) ) ;
#8920=CARTESIAN_POINT ( 'NONE',  ( -12.50385649908071706, -24.78436723039500222, -0.8579675316857384715 ) ) ;
#8924=EDGE_LOOP ( 'NONE', ( #19516, #2942, #26613, #33056, #25546, #41373, #3441, #36490, #37557, #9500, #53282 ) ) ;
#8928=AXIS2_PLACEMENT_3D ( 'NONE', #43277, #36358, #27198 ) ;
#8929=LINE ( 'NONE', #3342, #42248 ) ;
#8931=CARTESIAN_POINT ( 'NONE',  ( 6.425964501063000434, -75.91177771482000480, -10.89726081251999901 ) ) ;
#8933=CARTESIAN_POINT ( 'NONE',  ( 12.85144117167999944, -57.04527983067000463, 1.980464439859999981 ) ) ;
#8935=CARTESIAN_POINT ( 'NONE',  ( 12.66316398248999953, -16.82133896655000171, 0.04044089952542000155 ) ) ;
#8937=CARTESIAN_POINT ( 'NONE',  ( -9.643350356168998161, -24.94034317039000115, -8.260133465584999612 ) ) ;
#8947=B_SPLINE_CURVE_WITH_KNOTS ( 'NONE', 3,
 ( #49055, #8603, #23639, #32189, #14192, #10666 ),
 .UNSPECIFIED., .F., .F.,
 ( 4, 2, 4 ),
 ( 0.000000000000000000, 0.5000000000000000000, 1.000000000000000000 ),
 .UNSPECIFIED. ) ;
#8949=DIRECTION ( 'NONE',  ( 0.000000000000000000, 0.000000000000000000, 1.000000000000000000 ) ) ;
#8950=CARTESIAN_POINT ( 'NONE',  ( -9.369164850722000892, -23.25000000000000000, 7.601397897754999633 ) ) ;
#8952=CARTESIAN_POINT ( 'NONE',  ( 10.53003236230999917, -55.47547726255000100, -7.612971540256999958 ) ) ;
#8957=ORIENTED_EDGE ( 'NONE', *, *, #17131, .T. ) ;
#8959=CARTESIAN_POINT ( 'NONE',  ( 1.667269374601999976, -55.59060116482999803, 12.49858097728999873 ) ) ;
#8960=CARTESIAN_POINT ( 'NONE',  ( -1.930628539543000066, -60.02124444054000207, -12.72375828107000117 ) ) ;
#8961=CARTESIAN_POINT ( 'NONE',  ( -3.553300626444999555, -1.714275249885000019, 0.2100116894659999900 ) ) ;
#8963=CARTESIAN_POINT ( 'NONE',  ( 1.636761686205427058, -1.666666666666666519, -2.839805762151336399 ) ) ;
#8965=CYLINDRICAL_SURFACE ( 'NONE', #55330, 1.750000000000000000 ) ;
#8966=CARTESIAN_POINT ( 'NONE',  ( 12.54902617719999824, -16.99030198144999915, 0.4617931494614999632 ) ) ;
#8967=B_SPLINE_SURFACE_WITH_KNOTS ( 'NONE', 3, 3, ( 
 ( #2298, #14976, #50732, #32974, #42735, #29134, #56021, #38287, #6418, #51602, #19421, #32678, #42447, #20013, #23837, #55135, #14392, #51019, #37996, #46599, #15570, #33564, #2015, #47181, #5830, #46889, #19129, #14680, #19712, #6713, #10272, #32390, #50434, #37412, #15276 ),
 ( #1432, #9984, #33269, #27964, #5537, #23546, #51310, #10869, #41560, #28840, #28253, #24431, #1142, #10569, #46307, #41853, #55433, #55732, #28551, #6126, #24132, #42150, #1720, #53031, #8157, #25291, #48611, #47476, #43310, #2582, #52456, #30287, #7002, #2867, #47755 ),
 ( #20584, #26157, #34713, #43599, #21150, #57164, #52744, #25578, #3161, #25004, #57456, #48326, #43894, #16157, #3440, #29424, #39158, #20865, #25867, #43025, #38581, #21441, #44177, #3725, #12581, #34999, #16732, #39452, #7290, #56597, #34133, #33850, #30579, #52175, #12014 ),
 ( #21726, #11730, #56310, #15864, #51888, #17017, #11444, #29709, #12296, #38867, #7866, #56887, #16443, #34426, #29994, #48046, #7579, #27321, #9331, #35584, #35286, #36473, #26435, #54499, #50077, #4903, #17897, #12860, #44756, #48899, #9622, #57740, #14038, #22610, #40914 ) ),
 .UNSPECIFIED., .F., .F., .F.,
 ( 4, 4 ),
 ( 4, 1, 1, 1, 1, 1, 1, 1, 1, 1, 1, 1, 1, 1, 1, 1, 1, 1, 1, 1, 1, 1, 1, 1, 1, 1, 1, 1, 1, 1, 1, 1, 4 ),
 ( -0.3708084972814000291, 1.370808497280999960 ),
 ( 0.3383484129489999770, 0.3594304488109000273, 0.3805124846727999666, 0.4015945205347000169, 0.4226765563966999872, 0.4437585922585999820, 0.4648406281204999768, 0.4859226639823999716, 0.5070046998442999664, 0.5280867357063000478, 0.5491687715681999871, 0.5702508074300999263, 0.5913328432919999766, 0.6124148791539000269, 0.6334969150158999973, 0.6545789508778000476, 0.6756609867396999869, 0.6967430226016000372, 0.7178250584634999765, 0.7389070943254999468, 0.7599891301873999971, 0.7810711660493000474, 0.8021532019111999867, 0.8232352377731000370, 0.8443172736351000074, 0.8653993094969999467, 0.8864813453588999970, 0.9075633812208000473, 0.9286454170826999865, 0.9497274529446999569, 0.9708094888066000072, 0.9918915246685000575, 1.012973560530000094 ),
 .UNSPECIFIED. ) ;
#8972=CARTESIAN_POINT ( 'NONE',  ( 2.552428662871000231, -79.02735696754000116, 12.37732342135999986 ) ) ;
#8979=DIRECTION ( 'NONE',  ( -0.4045837981831721941, 0.8201365133289436615, -0.4045837981831721941 ) ) ;
#8988=DIRECTION ( 'NONE',  ( -9.217554797286021519E-07, 2.297153352953660798E-20, 0.9999999999995752287 ) ) ;
#8989=ORIENTED_EDGE ( 'NONE', *, *, #14095, .F. ) ;
#8990=ORIENTED_EDGE ( 'NONE', *, *, #25417, .T. ) ;
#8993=ORIENTED_EDGE ( 'NONE', *, *, #29375, .F. ) ;
#8994=DIRECTION ( 'NONE',  ( -1.000000000000000000, 0.000000000000000000, 0.000000000000000000 ) ) ;
#8995=EDGE_LOOP ( 'NONE', ( #40634, #35600, #49217 ) ) ;
#9002=CARTESIAN_POINT ( 'NONE',  ( 12.02473175675000050, -79.23708571609999751, -2.852631171805999788 ) ) ;
#9006=CARTESIAN_POINT ( 'NONE',  ( -12.56594317823000040, -18.74999998606000062, -1.750000000000000000 ) ) ;
#9007=EDGE_CURVE ( 'NONE', #21517, #17310, #47759, .T. ) ;
#9013=CARTESIAN_POINT ( 'NONE',  ( -3.291354266399999950, -76.72715654337000046, 12.36836470155000001 ) ) ;
#9021=CARTESIAN_POINT ( 'NONE',  ( -10.53101990622000095, -60.10639784916000394, 7.613962745625999062 ) ) ;
#9022=CARTESIAN_POINT ( 'NONE',  ( 8.665496919457343239, -76.89000174921478958, -8.038609273865034766 ) ) ;
#9025=CYLINDRICAL_SURFACE ( 'NONE', #44928, 12.05000000000000071 ) ;
#9027=CARTESIAN_POINT ( 'NONE',  ( -0.8385792221450999451, -2.959321851618000210, -3.712528424878000166 ) ) ;
#9029=ORIENTED_EDGE ( 'NONE', *, *, #26192, .F. ) ;
#9030=LINE ( 'NONE', #31440, #14021 ) ;
#9031=CARTESIAN_POINT ( 'NONE',  ( 12.05000000000000071, -80.60000000000000853, 0.000000000000000000 ) ) ;
#9033=CARTESIAN_POINT ( 'NONE',  ( -12.78015286811999829, -17.69674784880999852, -1.806262579046000072 ) ) ;
#9034=CARTESIAN_POINT ( 'NONE',  ( 6.891227191158999510, -76.62167840439001054, -9.824000600561999974 ) ) ;
#9035=CARTESIAN_POINT ( 'NONE',  ( -7.864802647442891370, -61.25123893484760629, -10.10444599044162572 ) ) ;
#9036=CARTESIAN_POINT ( 'NONE',  ( 12.82904091339000097, -18.67547470641000018, -2.062673488738000049 ) ) ;
#9037=ORIENTED_EDGE ( 'NONE', *, *, #37431, .T. ) ;
#9039=CARTESIAN_POINT ( 'NONE',  ( 1.750000000000000000, -60.04999999657000131, -12.50000000000000000 ) ) ;
#9040=EDGE_CURVE ( 'NONE', #6883, #23569, #25316, .T. ) ;
#9042=DIRECTION ( 'NONE',  ( 1.000000000000000000, 0.000000000000000000, 0.000000000000000000 ) ) ;
#9045=CARTESIAN_POINT ( 'NONE',  ( -3.616527695712999702, -1.793843644679999905, -0.5438149879621999583 ) ) ;
#9046=CARTESIAN_POINT ( 'NONE',  ( -1.667917367065999912, -60.08056535122999975, -12.49306764019000049 ) ) ;
#9053=EDGE_LOOP ( 'NONE', ( #30138, #58350, #20958, #54673 ) ) ;
#9054=DIRECTION ( 'NONE',  ( 0.000000000000000000, -1.000000000000000000, 0.000000000000000000 ) ) ;
#9055=DIRECTION ( 'NONE',  ( 0.000000000000000000, 1.000000000000000000, 0.000000000000000000 ) ) ;
#9056=CONICAL_SURFACE ( 'NONE', #29755, 0.6999999997694995590, 0.7853981633972997312 ) ;
#9058=LINE ( 'NONE', #27339, #44455 ) ;
#9061=ORIENTED_EDGE ( 'NONE', *, *, #55984, .F. ) ;
#9062=AXIS2_PLACEMENT_3D ( 'NONE', #24927, #29344, #20506 ) ;
#9064=CARTESIAN_POINT ( 'NONE',  ( -2.569810659366867256, -2.654058635901579866, -1.999144479470090330 ) ) ;
#9071=DIRECTION ( 'NONE',  ( -0.7071067811865475727, 0.000000000000000000, 0.7071067811865475727 ) ) ;
#9072=CARTESIAN_POINT ( 'NONE',  ( 0.5962167095188423138, -18.77158755789457345, 10.98383273456533615 ) ) ;
#9074=CARTESIAN_POINT ( 'NONE',  ( 5.917523019358037040, -78.63333333333332575, 10.26699006316254525 ) ) ;
#9077=CARTESIAN_POINT ( 'NONE',  ( -9.317978910659999059, -25.13238463018999980, 8.588869595444998950 ) ) ;
#9080=CARTESIAN_POINT ( 'NONE',  ( -7.220923959705292994, -76.72708333333335418, 9.396085398178589898 ) ) ;
#9084=CARTESIAN_POINT ( 'NONE',  ( -12.68702648026999924, -18.24922088193000036, 1.889939500033999797 ) ) ;
#9085=CARTESIAN_POINT ( 'NONE',  ( -8.343860018000999190, -55.64999999967000122, -8.343860018000999190 ) ) ;
#9086=CARTESIAN_POINT ( 'NONE',  ( 1.460729357738999923, -24.09091243202000143, 12.44211643240000065 ) ) ;
#9089=CARTESIAN_POINT ( 'NONE',  ( -0.4548042850443000384, -1.265628508794999885, 3.929784724312000321 ) ) ;
#9094=CARTESIAN_POINT ( 'NONE',  ( 0.000000000000000000, -19.21421830981000767, -13.15643568216998638 ) ) ;
#9099=DIRECTION ( 'NONE',  ( -0.07798810159604820103, 0.04890177472414890258, 0.9957542229075772022 ) ) ;
#9102=ORIENTED_EDGE ( 'NONE', *, *, #31239, .F. ) ;
#9103=AXIS2_PLACEMENT_3D ( 'NONE', #38701, #16280, #47304 ) ;
#9108=EDGE_CURVE ( 'NONE', #29606, #30887, #2684, .T. ) ;
#9109=CARTESIAN_POINT ( 'NONE',  ( 12.57042253521000141, -52.69905023022000279, 0.000000000000000000 ) ) ;
#9115=CARTESIAN_POINT ( 'NONE',  ( -0.6832218802960999815, -0.9170547980460999060, -3.968530914128000298 ) ) ;
#9116=CARTESIAN_POINT ( 'NONE',  ( -7.612366974783192575, -76.36927836883999987, -9.041534318350693766 ) ) ;
#9117=CARTESIAN_POINT ( 'NONE',  ( 12.00000000000000000, -18.75000000000000000, 1.250000000000000000 ) ) ;
#9118=CARTESIAN_POINT ( 'NONE',  ( -1.799475304559999822, -58.55171076491000548, 12.69616050744000013 ) ) ;
#9119=ORIENTED_EDGE ( 'NONE', *, *, #39959, .F. ) ;
#9120=CARTESIAN_POINT ( 'NONE',  ( -1.003693376013180982, -53.83776007857952095, -12.70247752660270812 ) ) ;
#9125=CARTESIAN_POINT ( 'NONE',  ( -12.49306764013999960, -55.51943464808999806, -1.667917367065999912 ) ) ;
#9126=EDGE_CURVE ( 'NONE', #18438, #42771, #53596, .T. ) ;
#9127=LINE ( 'NONE', #19149, #51059 ) ;
#9130=LINE ( 'NONE', #31537, #46894 ) ;
#9131=ADVANCED_FACE ( 'NONE', ( #23411 ), #23222, .F. ) ;
#9132=ORIENTED_EDGE ( 'NONE', *, *, #2786, .F. ) ;
#9133=CARTESIAN_POINT ( 'NONE',  ( -10.31988039472999930, -54.51085245502000021, -7.753829094159000235 ) ) ;
#9135=ORIENTED_EDGE ( 'NONE', *, *, #18932, .F. ) ;
#9144=CARTESIAN_POINT ( 'NONE',  ( 7.317687889309999250, -77.75422151684000482, -10.69177725920999933 ) ) ;
#9153=CARTESIAN_POINT ( 'NONE',  ( 11.88049207238000093, -76.28091755325999657, -3.223263369271999856 ) ) ;
#9156=ADVANCED_FACE ( 'NONE', ( #34002 ), #11595, .F. ) ;
#9157=CARTESIAN_POINT ( 'NONE',  ( -3.404284203830477917, -3.328750795578371502, 0.8991780458718586777 ) ) ;
#9159=CARTESIAN_POINT ( 'NONE',  ( -9.050966798898000931, -55.65000000893999754, 7.919595949288999570 ) ) ;
#9161=EDGE_CURVE ( 'NONE', #40041, #25888, #32867, .T. ) ;
#9163=CARTESIAN_POINT ( 'NONE',  ( 0.1322711626442740762, -77.17589890863403923, -12.01631470786458422 ) ) ;
#9165=CARTESIAN_POINT ( 'NONE',  ( 0.000000000000000000, 4.040000000000000036, 0.000000000000000000 ) ) ;
#9175=CARTESIAN_POINT ( 'NONE',  ( 9.085506314616404566, -76.00424330776989734, 7.450508573089704711 ) ) ;
#9177=DIRECTION ( 'NONE',  ( 1.000000000000000000, 0.000000000000000000, 0.000000000000000000 ) ) ;
#9178=ORIENTED_EDGE ( 'NONE', *, *, #45523, .F. ) ;
#9179=CARTESIAN_POINT ( 'NONE',  ( -11.91862232003999544, -76.02988133117466418, 3.079279237876998199 ) ) ;
#9184=DIRECTION ( 'NONE',  ( -1.893382764135975334E-11, -1.538485725003980272E-07, -0.9999999999999882316 ) ) ;
#9189=CARTESIAN_POINT ( 'NONE',  ( 12.70305331329204535, -53.76853698820474392, 0.8727610012071782553 ) ) ;
#9196=CARTESIAN_POINT ( 'NONE',  ( 0.000000000000000000, -45.91785611817000046, 0.000000000000000000 ) ) ;
#9197=VECTOR ( 'NONE', #8664, 1000.000000000000000 ) ;
#9200=CARTESIAN_POINT ( 'NONE',  ( -2.098469896607999926E-14, 0.000000000000000000, 0.000000000000000000 ) ) ;
#9201=CARTESIAN_POINT ( 'NONE',  ( 12.69999999999999929, 0.000000000000000000, 0.000000000000000000 ) ) ;
#9205=ORIENTED_EDGE ( 'NONE', *, *, #17715, .F. ) ;
#9208=CARTESIAN_POINT ( 'NONE',  ( 7.658894224177999810, -23.20939395863999977, 10.01676912201999947 ) ) ;
#9211=CARTESIAN_POINT ( 'NONE',  ( 7.429974109822146566, -55.28385402668686055, -8.111636311580273428 ) ) ;
#9213=EDGE_CURVE ( 'NONE', #25746, #56911, #52782, .T. ) ;
#9218=ORIENTED_EDGE ( 'NONE', *, *, #57744, .F. ) ;
#9219=CARTESIAN_POINT ( 'NONE',  ( -11.00000000000000000, -18.25000000000000000, 0.000000000000000000 ) ) ;
#9220=ORIENTED_EDGE ( 'NONE', *, *, #45118, .T. ) ;
#9225=CARTESIAN_POINT ( 'NONE',  ( -9.803620017999000069, -75.77582143684999494, 8.243458997453000592 ) ) ;
#9228=DIRECTION ( 'NONE',  ( 0.000000000000000000, 0.000000000000000000, 1.000000000000000000 ) ) ;
#9229=EDGE_CURVE ( 'NONE', #32213, #1567, #6756, .T. ) ;
#9231=CARTESIAN_POINT ( 'NONE',  ( -10.00831380745999866, -23.37230364585000331, -7.646786653130999589 ) ) ;
#9232=CIRCLE ( 'NONE', #54503, 12.57042253521000141 ) ;
#9234=ORIENTED_EDGE ( 'NONE', *, *, #44386, .T. ) ;
#9238=B_SPLINE_CURVE_WITH_KNOTS ( 'NONE', 3,
 ( #10970, #39256, #25964, #33955, #52273, #24822, #21542, #7389, #39548, #56982, #20396, #56702, #38394, #57271, #6813, #11827, #43988, #30388 ),
 .UNSPECIFIED., .F., .F.,
 ( 4, 2, 2, 2, 2, 2, 2, 2, 4 ),
 ( 0.000000000000000000, 0.1249999999999999722, 0.2499999999999999445, 0.3749999999999998890, 0.4999999999999998890, 0.6249999999999998890, 0.7499999999999997780, 0.8749999999999998890, 1.000000000000000000 ),
 .UNSPECIFIED. ) ;
#9240=CARTESIAN_POINT ( 'NONE',  ( -12.70457892003044620, -61.97873330296432215, 0.5105076821750260674 ) ) ;
#9244=CARTESIAN_POINT ( 'NONE',  ( 26.49999981590656262, -39.30476017083000073, 0.003123612069575185893 ) ) ;
#9246=DIRECTION ( 'NONE',  ( 0.000000000000000000, 1.000000000000000000, 0.000000000000000000 ) ) ;
#9248=CYLINDRICAL_SURFACE ( 'NONE', #23354, 12.05000000000000071 ) ;
#9251=ADVANCED_FACE ( 'NONE', ( #42778 ), #52213, .F. ) ;
#9252=CARTESIAN_POINT ( 'NONE',  ( 1.814305421036000121, -54.51058030636000495, 12.78003582248999948 ) ) ;
#9253=CARTESIAN_POINT ( 'NONE',  ( -2.062312494845999655, -60.02715659860000130, -12.83634740211000036 ) ) ;
#9254=CARTESIAN_POINT ( 'NONE',  ( -3.585353612862000272, -2.245771227706999884, -1.277122609306000189 ) ) ;
#9257=CARTESIAN_POINT ( 'NONE',  ( -0.4254240051736147277, -1.614583333333333259, -3.250000000000000888 ) ) ;
#9258=DIRECTION ( 'NONE',  ( 0.7071067811865473507, -1.433669009702094715E-08, 0.7071067811865473507 ) ) ;
#9260=CARTESIAN_POINT ( 'NONE',  ( 7.648026766753000416, -60.05000000550000294, -10.12290050090999927 ) ) ;
#9263=CARTESIAN_POINT ( 'NONE',  ( 9.643342484248000446, -53.85965044121000034, -8.260141428653000162 ) ) ;
#9270=CARTESIAN_POINT ( 'NONE',  ( -12.66736977985000046, -61.03307288738999858, 1.690635117038999935 ) ) ;
#9272=CARTESIAN_POINT ( 'NONE',  ( 12.56594317823000040, -23.25000001387000026, -1.750000000000000000 ) ) ;
#9274=AXIS2_PLACEMENT_3D ( 'NONE', #1626, #19331, #50053 ) ;
#9278=CARTESIAN_POINT ( 'NONE',  ( 8.188331488387602164, -55.57158755757197355, 7.345153731672233732 ) ) ;
#9281=CARTESIAN_POINT ( 'NONE',  ( -3.046994021028059052, -0.7499999999999998890, 1.760728177967239461 ) ) ;
#9283=CARTESIAN_POINT ( 'NONE',  ( 1.733997378016492341, -55.27616783188641136, 12.54437956609226035 ) ) ;
#9284=ORIENTED_EDGE ( 'NONE', *, *, #356, .F. ) ;
#9287=( GEOMETRIC_REPRESENTATION_CONTEXT ( 3 ) GLOBAL_UNCERTAINTY_ASSIGNED_CONTEXT ( ( #11271 ) ) GLOBAL_UNIT_ASSIGNED_CONTEXT ( ( #20137, #52585, #47603 ) ) REPRESENTATION_CONTEXT ( 'NONE', 'WORKASPACE' ) );
#9289=CARTESIAN_POINT ( 'NONE',  ( -1.818468715484000065E-14, -79.21250000010999770, -11.96250000010999948 ) ) ;
#9290=B_SPLINE_CURVE_WITH_KNOTS ( 'NONE', 3,
 ( #37561, #28698, #4162, #12441, #39876, #8010, #35430, #53460, #57888, #3868, #30715, #30142, #44311, #49040, #34285, #48191, #30434, #58182, #35143, #17156, #26298, #13003, #52890 ),
 .UNSPECIFIED., .F., .F.,
 ( 4, 2, 2, 1, 2, 2, 2, 2, 2, 2, 2, 4 ),
 ( 0.000000000000000000, 0.1250000000000001388, 0.1875000000000001388, 0.2500000000000001665, 0.3125000000000001665, 0.3750000000000001665, 0.5000000000000001110, 0.6250000000000001110, 0.6875000000000001110, 0.7500000000000000000, 0.8750000000000001110, 1.000000000000000000 ),
 .UNSPECIFIED. ) ;
#9294=CARTESIAN_POINT ( 'NONE',  ( -1.726904517088999835, -78.63095455000001266, 11.78767162433000060 ) ) ;
#9296=ORIENTED_EDGE ( 'NONE', *, *, #27766, .T. ) ;
#9297=CARTESIAN_POINT ( 'NONE',  ( -3.248553649406136667, -1.606043880758631248, -0.1773244309825293408 ) ) ;
#9301=CARTESIAN_POINT ( 'NONE',  ( -10.59548767697000038, -21.75736537952000305, 7.678667886032999768 ) ) ;
#9302=CARTESIAN_POINT ( 'NONE',  ( 9.135190432272999317, -76.61072037624001041, -8.185884657762999339 ) ) ;
#9303=ADVANCED_FACE ( 'NONE', ( #4941 ), #31795, .F. ) ;
#9307=FACE_OUTER_BOUND ( 'NONE', #22114, .T. ) ;
#9310=CARTESIAN_POINT ( 'NONE',  ( -10.18491080491000034, -55.49283319101999723, 7.640030264136999705 ) ) ;
#9311=CARTESIAN_POINT ( 'NONE',  ( 3.099784061626695841, -2.875628255113011456, 1.008047939721263608 ) ) ;
#9314=AXIS2_PLACEMENT_3D ( 'NONE', #50422, #42724, #24714 ) ;
#9317=ADVANCED_FACE ( 'NONE', ( #19685 ), #7737, .F. ) ;
#9320=CARTESIAN_POINT ( 'NONE',  ( 0.000000000000000000, -15.06282895647999887, 0.000000000000000000 ) ) ;
#9325=CARTESIAN_POINT ( 'NONE',  ( -7.247844507162001015, -18.75000000000000000, -9.722718241315000398 ) ) ;
#9326=CARTESIAN_POINT ( 'NONE',  ( 1.667917367010000040, -55.51943307300000185, 12.49306752631999906 ) ) ;
#9327=CARTESIAN_POINT ( 'NONE',  ( 9.175280770439000477, -76.67484661803999302, -8.221808909867000636 ) ) ;
#9329=AXIS2_PLACEMENT_3D ( 'NONE', #29321, #56210, #29608 ) ;
#9331=CARTESIAN_POINT ( 'NONE',  ( 9.112744727833000269, -76.18430091963000450, -8.574219231229999849 ) ) ;
#9333=CARTESIAN_POINT ( 'NONE',  ( -13.89248034750000116, -69.19159251015000223, -2.632538496651000052E-05 ) ) ;
#9335=B_SPLINE_CURVE_WITH_KNOTS ( 'NONE', 3,
 ( #53520, #48807, #13061, #52376, #11929, #8352, #44368, #3921, #31060, #49097, #29907, #41113, #27225, #9240, #54114, #990 ),
 .UNSPECIFIED., .F., .F.,
 ( 4, 2, 2, 2, 2, 2, 2, 4 ),
 ( 0.000000000000000000, 0.2499999999999955591, 0.3749999999999933387, 0.4374999999999921729, 0.4999999999999910072, 0.6249999999999932276, 0.7499999999999954481, 1.000000000000000000 ),
 .UNSPECIFIED. ) ;
#9337=CARTESIAN_POINT ( 'NONE',  ( -7.648026768024999811, -18.75000001589999954, 10.12290050218000026 ) ) ;
#9340=CARTESIAN_POINT ( 'NONE',  ( 3.981113306789000106, -1.022141436244000001, -0.5296481109823999445 ) ) ;
#9346=CARTESIAN_POINT ( 'NONE',  ( 11.75000000000000000, -77.45000000000000284, 1.043320980279999928E-14 ) ) ;
#9347=ORIENTED_EDGE ( 'NONE', *, *, #57788, .T. ) ;
#9348=ORIENTED_EDGE ( 'NONE', *, *, #32148, .T. ) ;
#9352=EDGE_LOOP ( 'NONE', ( #36280, #42103, #12251, #20693 ) ) ;
#9357=CARTESIAN_POINT ( 'NONE',  ( 1.048127130988076861, -2.751564908735101067, -3.083268915589403303 ) ) ;
#9366=LINE ( 'NONE', #18809, #48202 ) ;
#9367=CARTESIAN_POINT ( 'NONE',  ( -7.718368845809999712, -20.25199022618999933, -10.07722254369999959 ) ) ;
#9370=CARTESIAN_POINT ( 'NONE',  ( -1.538071403320043551, -78.68541666666666856, 11.74999999999999467 ) ) ;
#9374=EDGE_CURVE ( 'NONE', #31775, #13118, #8329, .T. ) ;
#9375=CARTESIAN_POINT ( 'NONE',  ( -9.650948395506999233, -24.93402498662999989, 8.252474012539000370 ) ) ;
#9376=CARTESIAN_POINT ( 'NONE',  ( -14.00000000000000000, -9.295797029142999435, 0.000000000000000000 ) ) ;
#9381=CARTESIAN_POINT ( 'NONE',  ( -1.750000000001000089, -56.04922971509999741, 12.60356226394999979 ) ) ;
#9382=DIRECTION ( 'NONE',  ( -0.7071067811865475727, 0.000000000000000000, 0.7071067811865475727 ) ) ;
#9383=CARTESIAN_POINT ( 'NONE',  ( -1.484804496640999893, -24.71869153383000040, 12.77261165608999960 ) ) ;
#9384=CARTESIAN_POINT ( 'NONE',  ( 10.12290050256999940, -18.75000002239000096, 7.648026768411000376 ) ) ;
#9385=CARTESIAN_POINT ( 'NONE',  ( 2.479132830488999684, -1.786791850769000156, 2.865938273056999996 ) ) ;
#9387=ADVANCED_FACE ( 'NONE', ( #6326 ), #47009, .F. ) ;
#9392=CARTESIAN_POINT ( 'NONE',  ( -10.18491080493000212, -23.30716680861999990, -7.640030264156999706 ) ) ;
#9395=VECTOR ( 'NONE', #1714, 1000.000000000000114 ) ;
#9396=CARTESIAN_POINT ( 'NONE',  ( -13.79999999999999893, 0.000000000000000000, 0.000000000000000000 ) ) ;
#9402=CARTESIAN_POINT ( 'NONE',  ( -14.00000000000000000, -0.2000000000000005107, 0.000000000000000000 ) ) ;
#9405=FACE_OUTER_BOUND ( 'NONE', #25675, .T. ) ;
#9408=CARTESIAN_POINT ( 'NONE',  ( 2.850509184763999837, -1.027515194441000146, 2.608524172722999968 ) ) ;
#9409=CARTESIAN_POINT ( 'NONE',  ( 7.958776490642000212, -61.27699850017000216, -9.723157983989999309 ) ) ;
#9410=CARTESIAN_POINT ( 'NONE',  ( -8.872958366221523008, -61.81010144656713123, 8.813896669733001232 ) ) ;
#9412=ORIENTED_EDGE ( 'NONE', *, *, #16899, .T. ) ;
#9413=DIRECTION ( 'NONE',  ( 0.7071067811865475727, 0.000000000000000000, -0.7071067811865475727 ) ) ;
#9414=AXIS2_PLACEMENT_3D ( 'NONE', #19290, #27833, #42015 ) ;
#9415=LINE ( 'NONE', #41286, #42985 ) ;
#9418=CARTESIAN_POINT ( 'NONE',  ( -12.50485633186319490, -17.13407854666478514, -0.6924329881533773934 ) ) ;
#9419=CARTESIAN_POINT ( 'NONE',  ( 11.00000000000000000, -23.75000000000000000, -1.203259120426999909E-14 ) ) ;
#9420=VERTEX_POINT ( 'NONE', #479 ) ;
#9422=CARTESIAN_POINT ( 'NONE',  ( 10.18248259422395385, -61.09095036164143266, -7.792398156856013891 ) ) ;
#9426=CARTESIAN_POINT ( 'NONE',  ( -13.86363636363000218, -9.638971321655001034, -1.277887488715999925E-05 ) ) ;
#9427=FILL_AREA_STYLE_COLOUR ( '', #24685 ) ;
#9429=ORIENTED_EDGE ( 'NONE', *, *, #40075, .T. ) ;
#9431=CYLINDRICAL_SURFACE ( 'NONE', #40935, 1.750000000000001332 ) ;
#9432=VECTOR ( 'NONE', #45998, 1000.000000000000000 ) ;
#9436=CARTESIAN_POINT ( 'NONE',  ( 11.98112765039999950, -78.27769171769000423, 5.330601325896000553 ) ) ;
#9440=CARTESIAN_POINT ( 'NONE',  ( 11.75000000000000000, -78.04999999999999716, 0.000000000000000000 ) ) ;
#9441=ORIENTED_EDGE ( 'NONE', *, *, #23257, .F. ) ;
#9442=FACE_OUTER_BOUND ( 'NONE', #58115, .T. ) ;
#9443=ADVANCED_FACE ( 'NONE', ( #23456 ), #49821, .F. ) ;
#9444=CARTESIAN_POINT ( 'NONE',  ( 11.05577208806000122, -76.76861526166000260, -4.921212746988999243 ) ) ;
#9446=AXIS2_PLACEMENT_3D ( 'NONE', #34014, #33728, #34874 ) ;
#9447=B_SPLINE_SURFACE_WITH_KNOTS ( 'NONE', 3, 3, ( 
 ( #22541, #144, #17523, #21942 ),
 ( #58263, #22239, #31375, #4832 ),
 ( #57968, #45579, #18122, #26369 ),
 ( #23122, #53541, #437, #17825 ),
 ( #13673, #54134, #724, #18413 ),
 ( #35812, #49418, #18701, #13081 ),
 ( #53247, #50007, #36404, #54432 ),
 ( #49716, #48828, #8966, #30796 ),
 ( #8370, #45284, #31964, #44388 ),
 ( #4240, #8667, #3940, #35513 ),
 ( #26653, #40252, #26951, #44984 ) ),
 .UNSPECIFIED., .F., .F., .F.,
 ( 4, 1, 1, 1, 1, 1, 1, 1, 4 ),
 ( 4, 4 ),
 ( -0.02001211456244999728, 0.000000000000000000, 0.1666666666667000196, 0.3333333333333000081, 0.5000000000000000000, 0.6666666666667000474, 0.8333333333333000637, 1.000000000000000000, 1.020273719995999917 ),
 ( -0.3582002740325999635, 1.358863140973999961 ),
 .UNSPECIFIED. ) ;
#9449=CARTESIAN_POINT ( 'NONE',  ( 2.836926435089343723, -3.149705295855155018, 2.084417755536846606 ) ) ;
#9450=AXIS2_PLACEMENT_3D ( 'NONE', #12323, #22568, #50322 ) ;
#9451=CARTESIAN_POINT ( 'NONE',  ( 8.292771711479000274, -61.85529938492000213, -9.770424367394999976 ) ) ;
#9452=CARTESIAN_POINT ( 'NONE',  ( -4.802691730569000228, -78.42489718999000559, 11.09149278351999968 ) ) ;
#9453=LINE ( 'NONE', #9159, #51768 ) ;
#9456=CARTESIAN_POINT ( 'NONE',  ( 2.148140615799914777, -77.18924137040484368, -11.93000460038572719 ) ) ;
#9457=DIRECTION ( 'NONE',  ( 0.7071067811865475727, 0.000000000000000000, -0.7071067811865475727 ) ) ;
#9458=ADVANCED_FACE ( 'NONE', ( #41468 ), #21402, .F. ) ;
#9459=VERTEX_POINT ( 'NONE', #48729 ) ;
#9461=CARTESIAN_POINT ( 'NONE',  ( -11.75000000000000355, -77.81041666666666856, -1.538071403320004249 ) ) ;
#9468=CARTESIAN_POINT ( 'NONE',  ( 4.515762143495796188, -76.04307832163055991, 10.84725862635628602 ) ) ;
#9471=VERTEX_POINT ( 'NONE', #52864 ) ;
#9472=CARTESIAN_POINT ( 'NONE',  ( 7.568503529865000523, -76.37230738176410227, 9.708412483427999007 ) ) ;
#9483=FACE_BOUND ( 'NONE', #35414, .T. ) ;
#9487=CARTESIAN_POINT ( 'NONE',  ( 12.55433072267388894, -60.18725213688288989, 1.749897784984624005 ) ) ;
#9489=PLANE ( 'NONE',  #20495 ) ;
#9492=DIRECTION ( 'NONE',  ( 0.000000000000000000, 1.000000000000000000, 0.000000000000000000 ) ) ;
#9493=EDGE_CURVE ( 'NONE', #39575, #3891, #24364, .T. ) ;
#9494=CARTESIAN_POINT ( 'NONE',  ( 8.838834764832000701, -23.25000000000000000, 8.838834764832000701 ) ) ;
#9495=CARTESIAN_POINT ( 'NONE',  ( -12.43646324844999995, -24.92048514568000073, 0.1256879863178999857 ) ) ;
#9496=ORIENTED_EDGE ( 'NONE', *, *, #14112, .T. ) ;
#9497=ORIENTED_EDGE ( 'NONE', *, *, #7745, .F. ) ;
#9500=ORIENTED_EDGE ( 'NONE', *, *, #46706, .F. ) ;
#9502=CARTESIAN_POINT ( 'NONE',  ( 9.992017125381000398, -24.16084087012999859, 7.762968460669999793 ) ) ;
#9503=CARTESIAN_POINT ( 'NONE',  ( 8.188293269190999979, -61.50494400535999517, 9.395718629102999486 ) ) ;
#9507=LINE ( 'NONE', #50252, #42203 ) ;
#9508=VERTEX_POINT ( 'NONE', #7698 ) ;
#9509=CARTESIAN_POINT ( 'NONE',  ( 7.764010764072387438, -60.92280919713373777, -9.931043767944542466 ) ) ;
#9510=AXIS2_PLACEMENT_3D ( 'NONE', #13168, #9055, #40345 ) ;
#9515=CARTESIAN_POINT ( 'NONE',  ( 0.000000000000000000, -32.88214388149999934, 0.000000000000000000 ) ) ;
#9517=CARTESIAN_POINT ( 'NONE',  ( -10.11336291351999961, -76.36473582389999137, 8.113742140220999488 ) ) ;
#9520=LINE ( 'NONE', #31051, #54456 ) ;
#9522=CARTESIAN_POINT ( 'NONE',  ( 12.70249480710770662, -61.76498603277217825, 0.9989402949278443078 ) ) ;
#9523=CARTESIAN_POINT ( 'NONE',  ( -8.111636311560200596, -60.31614597267139999, 7.429974109843835883 ) ) ;
#9524=ADVANCED_FACE ( 'NONE', ( #52579 ), #34547, .F. ) ;
#9526=ORIENTED_EDGE ( 'NONE', *, *, #1459, .F. ) ;
#9528=AXIS2_PLACEMENT_3D ( 'NONE', #24732, #55445, #46902 ) ;
#9531=ADVANCED_FACE ( 'NONE', ( #30693 ), #34834, .F. ) ;
#9533=FACE_OUTER_BOUND ( 'NONE', #7312, .T. ) ;
#9535=CARTESIAN_POINT ( 'NONE',  ( -9.396085398178614767, -78.35208333333332575, -7.220923959705254802 ) ) ;
#9544=EDGE_LOOP ( 'NONE', ( #31909, #53058, #49252, #32266 ) ) ;
#9545=FACE_OUTER_BOUND ( 'NONE', #7025, .T. ) ;
#9547=CARTESIAN_POINT ( 'NONE',  ( -1.269242897982000073, -1.816486014851000030, -3.588396222942000335 ) ) ;
#9557=CARTESIAN_POINT ( 'NONE',  ( 9.205836503685999261, -53.79200673903999785, -8.541144771039000716 ) ) ;
#9561=CARTESIAN_POINT ( 'NONE',  ( 0.2584144823669621838, -62.02845396880400841, 12.70558781493838296 ) ) ;
#9565=FACE_OUTER_BOUND ( 'NONE', #43200, .T. ) ;
#9567=VERTEX_POINT ( 'NONE', #26274 ) ;
#9568=EDGE_CURVE ( 'NONE', #35685, #14936, #50795, .T. ) ;
#9572=CARTESIAN_POINT ( 'NONE',  ( 8.190859204290999784, -55.64999999967000122, 7.342331066867000544 ) ) ;
#9580=CARTESIAN_POINT ( 'NONE',  ( 12.00000000000000000, -23.15000000000000213, 0.000000000000000000 ) ) ;
#9583=CARTESIAN_POINT ( 'NONE',  ( 1.814305421036000121, -24.28941969330999839, -12.78003582253000125 ) ) ;
#9585=LINE ( 'NONE', #27569, #32883 ) ;
#9586=CARTESIAN_POINT ( 'NONE',  ( -1.269878056453999982, -78.86088029460999849, -11.84562412616999971 ) ) ;
#9587=ORIENTED_EDGE ( 'NONE', *, *, #24546, .T. ) ;
#9589=CARTESIAN_POINT ( 'NONE',  ( -7.624341766647000362, -18.73514853758999976, 10.42531125024999916 ) ) ;
#9594=CARTESIAN_POINT ( 'NONE',  ( -1.164828128805999992E-14, -72.75000000040999737, 0.000000000000000000 ) ) ;
#9596=CARTESIAN_POINT ( 'NONE',  ( 5.555615362064000529, -77.25827452080000057, 11.70460571637999969 ) ) ;
#9598=CARTESIAN_POINT ( 'NONE',  ( -12.64500484462999985, -22.77152778045000048, -1.799490225533999732 ) ) ;
#9604=LINE ( 'NONE', #27590, #5999 ) ;
#9608=DIRECTION ( 'NONE',  ( 0.000000000000000000, -1.000000000000000000, 0.000000000000000000 ) ) ;
#9611=ORIENTED_EDGE ( 'NONE', *, *, #15089, .T. ) ;
#9612=DIRECTION ( 'NONE',  ( 0.000000000000000000, -1.000000000000000000, 0.000000000000000000 ) ) ;
#9614=DIRECTION ( 'NONE',  ( 0.000000000000000000, -1.000000000000000000, 0.000000000000000000 ) ) ;
#9616=CARTESIAN_POINT ( 'NONE',  ( 1.799490225533999732, -56.02847221959000024, 12.64500484464000074 ) ) ;
#9617=CARTESIAN_POINT ( 'NONE',  ( -3.346450045594000056, -76.87836363489999769, 12.57540552286999791 ) ) ;
#9622=CARTESIAN_POINT ( 'NONE',  ( -0.4750644714246999856, -76.61635661117000495, -12.50333200011000123 ) ) ;
#9623=ORIENTED_EDGE ( 'NONE', *, *, #42368, .F. ) ;
#9624=CARTESIAN_POINT ( 'NONE',  ( -13.98934701301999972, -69.37813015403000350, -1.420884291397000047E-05 ) ) ;
#9627=CARTESIAN_POINT ( 'NONE',  ( 7.601397897754999633, -60.04999999657000131, 10.07627163191000008 ) ) ;
#9630=CARTESIAN_POINT ( 'NONE',  ( 2.627446458840999810, -1.566251425905000216, 3.037392460054000320 ) ) ;
#9631=CARTESIAN_POINT ( 'NONE',  ( -1.799501877793999949, -55.51082276539999327, -12.60552511008000032 ) ) ;
#9632=CARTESIAN_POINT ( 'NONE',  ( -8.485281374238999419, -18.75000000000000000, -8.485281374238999419 ) ) ;
#9633=ORIENTED_EDGE ( 'NONE', *, *, #33398, .T. ) ;
#9635=B_SPLINE_SURFACE_WITH_KNOTS ( 'NONE', 3, 3, ( 
 ( #11504, #29193, #2356, #47240 ),
 ( #6771, #7062, #24780, #43086 ),
 ( #2644, #56657, #53964, #13501 ),
 ( #35337, #40967, #8787, #49836 ),
 ( #17644, #45704, #4952, #9086 ),
 ( #36528, #31793, #22361, #49236 ),
 ( #4057, #40675, #13201, #22956 ),
 ( #50130, #4664, #27072, #22664 ),
 ( #13792, #9672, #35935, #265 ),
 ( #558, #22061, #18536, #45410 ),
 ( #35634, #18246, #23247, #45112 ),
 ( #9383, #36236, #48943, #54551 ),
 ( #54259, #53362, #40375, #27372 ),
 ( #17348, #14091, #32090, #27662 ),
 ( #5242, #41255, #12910, #30909 ),
 ( #49540, #53662, #8488, #26483 ),
 ( #26778, #44808, #44507, #40068 ) ),
 .UNSPECIFIED., .F., .F., .F.,
 ( 4, 1, 1, 1, 1, 1, 1, 1, 1, 1, 1, 1, 1, 1, 4 ),
 ( 4, 4 ),
 ( -0.01011408452870000106, 0.000000000000000000, 0.08333333333333001192, 0.1666666666667000196, 0.2500000000000000000, 0.3333333333333000081, 0.4166666666666999919, 0.5000000000000000000, 0.5833333333333000637, 0.6666666666667000474, 0.7500000000000000000, 0.8333333333333000637, 0.9166666666667000474, 1.000000000000000000, 1.010362559107000013 ),
 ( -0.3559705546268999710, 1.357612419602000076 ),
 .UNSPECIFIED. ) ;
#9638=EDGE_LOOP ( 'NONE', ( #5946, #9712, #31842, #53865 ) ) ;
#9639=EDGE_CURVE ( 'NONE', #2137, #23895, #20987, .T. ) ;
#9642=EDGE_LOOP ( 'NONE', ( #23737, #38757, #50605, #8701, #16690, #25886 ) ) ;
#9644=ORIENTED_EDGE ( 'NONE', *, *, #36687, .T. ) ;
#9646=CARTESIAN_POINT ( 'NONE',  ( 0.3737964730420059167, -2.734503530802450122, -3.231708774972011700 ) ) ;
#9647=EDGE_CURVE ( 'NONE', #33154, #53225, #56722, .T. ) ;
#9650=ADVANCED_FACE ( 'NONE', ( #39849 ), #37532, .F. ) ;
#9652=CARTESIAN_POINT ( 'NONE',  ( -9.431004454403218773, -53.99940410528813572, -8.251853356944486961 ) ) ;
#9653=ORIENTED_EDGE ( 'NONE', *, *, #39686, .F. ) ;
#9655=AXIS2_PLACEMENT_3D ( 'NONE', #3546, #21549, #12686 ) ;
#9657=DIRECTION ( 'NONE',  ( 0.000000000000000000, 0.000000000000000000, 1.000000000000000000 ) ) ;
#9660=CARTESIAN_POINT ( 'NONE',  ( -3.075537641221584018, -78.69583333333332575, 11.44417895085269876 ) ) ;
#9665=FACE_OUTER_BOUND ( 'NONE', #5718, .T. ) ;
#9669=AXIS2_PLACEMENT_3D ( 'NONE', #9928, #44772, #13754 ) ;
#9670=CARTESIAN_POINT ( 'NONE',  ( -12.49996905250000090, -18.80797343466000271, 1.666511841114999948 ) ) ;
#9671=CARTESIAN_POINT ( 'NONE',  ( -8.909545442950999927, -55.64999999967000122, 8.061017305527000687 ) ) ;
#9672=CARTESIAN_POINT ( 'NONE',  ( -0.005928781627502999370, -25.20113050262999721, 12.66336824419000173 ) ) ;
#9673=CARTESIAN_POINT ( 'NONE',  ( 10.44683666574804093, -79.24999999999998579, -6.036782287597141305 ) ) ;
#9675=VECTOR ( 'NONE', #12796, 1000.000000000000114 ) ;
#9676=CARTESIAN_POINT ( 'NONE',  ( 3.756388134018000091, -1.208015194441000251, -0.4997506290278999619 ) ) ;
#9677=CARTESIAN_POINT ( 'NONE',  ( -8.130811096542000627, -24.68523690389000080, -9.546858433121998999 ) ) ;
#9678=CARTESIAN_POINT ( 'NONE',  ( 10.07719973194999952, -57.05111654290000445, 7.718346056121999865 ) ) ;
#9680=CARTESIAN_POINT ( 'NONE',  ( 0.000000000000000000, -0.1000000063292999924, 0.000000000000000000 ) ) ;
#9685=CARTESIAN_POINT ( 'NONE',  ( 7.651147547606000465, -22.76256650325000308, 10.45204383577999963 ) ) ;
#9689=VERTEX_POINT ( 'NONE', #57001 ) ;
#9693=DIRECTION ( 'NONE',  ( 0.000000000000000000, -1.000000000000000000, 2.131628207279999907E-13 ) ) ;
#9695=CARTESIAN_POINT ( 'NONE',  ( 10.13881649148000008, -76.50783510652000530, -5.938594122520999719 ) ) ;
#9697=CIRCLE ( 'NONE', #33235, 13.94827586206999825 ) ;
#9698=CARTESIAN_POINT ( 'NONE',  ( -12.60246356036999948, -77.76186929341000109, -0.9915196953554998860 ) ) ;
#9699=CARTESIAN_POINT ( 'NONE',  ( -11.75000000000000000, -76.30000000000001137, 1.487410190129999909E-14 ) ) ;
#9702=CARTESIAN_POINT ( 'NONE',  ( -0.1380878923252624457, -53.57265597643803545, -12.70555840928063773 ) ) ;
#9704=CARTESIAN_POINT ( 'NONE',  ( 11.75000000000000000, -75.95000000000000284, 0.000000000000000000 ) ) ;
#9705=EDGE_CURVE ( 'NONE', #53225, #30862, #50579, .T. ) ;
#9706=VECTOR ( 'NONE', #37760, 1000.000000000000000 ) ;
#9707=CARTESIAN_POINT ( 'NONE',  ( 0.000000000000000000, -23.25000000000000000, 12.50000000000000000 ) ) ;
#9708=VERTEX_POINT ( 'NONE', #40144 ) ;
#9710=CARTESIAN_POINT ( 'NONE',  ( 8.121699804378911480, -61.63626205718931317, -9.841121124288225275 ) ) ;
#9711=ORIENTED_EDGE ( 'NONE', *, *, #38780, .T. ) ;
#9712=ORIENTED_EDGE ( 'NONE', *, *, #31298, .T. ) ;
#9713=AXIS2_PLACEMENT_3D ( 'NONE', #49549, #31804, #26212 ) ;
#9714=CARTESIAN_POINT ( 'NONE',  ( -10.18949731070000020, -55.58470987670000341, -7.645392562244000878 ) ) ;
#9715=AXIS2_PLACEMENT_3D ( 'NONE', #20302, #30001, #38297 ) ;
#9716=( NAMED_UNIT ( * ) PLANE_ANGLE_UNIT ( ) SI_UNIT ( $, .RADIAN. ) );
#9719=ORIENTED_EDGE ( 'NONE', *, *, #44033, .T. ) ;
#9720=DIRECTION ( 'NONE',  ( 0.7071067811865475727, 0.000000000000000000, -0.7071067811865475727 ) ) ;
#9725=DIRECTION ( 'NONE',  ( -9.217554813251081680E-07, 2.920569602132825499E-20, 0.9999999999995752287 ) ) ;
#9727=CARTESIAN_POINT ( 'NONE',  ( 1.779623408250214922, -17.86369130974330233, -12.71471627657038361 ) ) ;
#9730=DIRECTION ( 'NONE',  ( 0.7071067811865475727, 0.000000000000000000, -0.7071067811865475727 ) ) ;
#9733=CARTESIAN_POINT ( 'NONE',  ( -1.476182556144000069, -76.36723242473999562, 12.22114576030999977 ) ) ;
#9736=EDGE_CURVE ( 'NONE', #58179, #5420, #9453, .T. ) ;
#9737=CARTESIAN_POINT ( 'NONE',  ( 2.772699504624841715, -2.152166083112415418, 2.171300326618198273 ) ) ;
#9738=CARTESIAN_POINT ( 'NONE',  ( 8.596763593984000806, -61.93532396089999992, -9.310159863737000663 ) ) ;
#9739=CARTESIAN_POINT ( 'NONE',  ( -5.531768889155999958, -79.10509418445998620, -10.94525552207000096 ) ) ;
#9744=CARTESIAN_POINT ( 'NONE',  ( -9.722718241315000398, -18.75000000000000000, 7.247844507162001015 ) ) ;
#9745=CARTESIAN_POINT ( 'NONE',  ( -1.880557995764754908, -76.56599386863840095, -12.89133805120253307 ) ) ;
#9747=B_SPLINE_SURFACE_WITH_KNOTS ( 'NONE', 3, 3, ( 
 ( #50049, #32583, #23164, #6027 ),
 ( #32291, #1622, #5737, #10181 ),
 ( #28159, #23744, #41758, #1333 ),
 ( #9301, #27581, #22875, #40884 ),
 ( #476, #19328, #45624, #41172 ),
 ( #766, #36736, #51506, #29897 ),
 ( #43503, #38486, #56214, #38195 ),
 ( #34043, #24913, #47955, #24340 ) ),
 .UNSPECIFIED., .F., .F., .F.,
 ( 4, 1, 1, 1, 1, 4 ),
 ( 4, 4 ),
 ( -0.01200407347463999970, 0.000000000000000000, 0.3333333333333000081, 0.6666666666667000474, 1.000000000000000000, 1.011997855551999947 ),
 ( -0.3559705542741000150, 1.355970554273999928 ),
 .UNSPECIFIED. ) ;
#9749=DIRECTION ( 'NONE',  ( -0.9999999999999994449, -3.428898374088997947E-08, 7.236136583703995822E-12 ) ) ;
#9754=AXIS2_PLACEMENT_3D ( 'NONE', #52178, #57459, #25871 ) ;
#9757=CARTESIAN_POINT ( 'NONE',  ( 6.329451544447319833, -76.02924920104398154, 9.917131221196935797 ) ) ;
#9760=VERTEX_POINT ( 'NONE', #54896 ) ;
#9762=DIRECTION ( 'NONE',  ( 1.894056205636980548E-11, -1.538484108169980264E-07, 0.9999999999999882316 ) ) ;
#9767=LINE ( 'NONE', #27755, #48194 ) ;
#9768=CARTESIAN_POINT ( 'NONE',  ( 10.01749678875999905, -18.80819056997000160, -7.660430392568000180 ) ) ;
#9769=CARTESIAN_POINT ( 'NONE',  ( 10.07627163191000008, -23.24999999688999708, -7.601397897754999633 ) ) ;
#9772=FACE_BOUND ( 'NONE', #4332, .T. ) ;
#9782=CARTESIAN_POINT ( 'NONE',  ( 0.000000000000000000, -23.25000000000000000, -12.00000000000000000 ) ) ;
#9785=AXIS2_PLACEMENT_3D ( 'NONE', #15647, #6790, #38656 ) ;
#9787=ORIENTED_EDGE ( 'NONE', *, *, #19680, .F. ) ;
#9789=ORIENTED_EDGE ( 'NONE', *, *, #38831, .T. ) ;
#9793=ORIENTED_EDGE ( 'NONE', *, *, #43829, .T. ) ;
#9798=CARTESIAN_POINT ( 'NONE',  ( 7.619712170668999640, -60.20404510030000012, 10.35409959312000083 ) ) ;
#9799=DIRECTION ( 'NONE',  ( 0.000000000000000000, 0.000000000000000000, 1.000000000000000000 ) ) ;
#9804=DIRECTION ( 'NONE',  ( 0.07798810297639352518, 0.04890180917562222257, 0.9957542211075455230 ) ) ;
#9815=CARTESIAN_POINT ( 'NONE',  ( -8.643979526155998627, -25.25953772911000073, -9.422807787372999400 ) ) ;
#9824=CARTESIAN_POINT ( 'NONE',  ( -9.963464501286001251, -18.31723479381000175, 7.659241807038999816 ) ) ;
#9825=AXIS2_PLACEMENT_3D ( 'NONE', #7215, #6638, #56523 ) ;
#9827=CARTESIAN_POINT ( 'NONE',  ( -1.538071403319991814, -78.41458333333333997, -11.75000000000000355 ) ) ;
#9828=CARTESIAN_POINT ( 'NONE',  ( -1.480597980168999888E-14, -80.60000000000000853, 0.000000000000000000 ) ) ;
#9829=CARTESIAN_POINT ( 'NONE',  ( -2.278169229989186029, -3.319065836604013775, -2.686266703802629330 ) ) ;
#9839=CARTESIAN_POINT ( 'NONE',  ( -9.713032445540607185, -24.52293762691879309, 7.970418356296339546 ) ) ;
#9844=DIRECTION ( 'NONE',  ( 0.8090169943751300830, 0.000000000000000000, -0.5877852522922218936 ) ) ;
#9846=CARTESIAN_POINT ( 'NONE',  ( -0.5999999999999999778, -18.84999999999999787, 10.98362417419999915 ) ) ;
#9849=CARTESIAN_POINT ( 'NONE',  ( -10.42531125074000009, -18.73514854687000053, -7.624341767140999870 ) ) ;
#9850=CARTESIAN_POINT ( 'NONE',  ( 8.588893914397997875, -53.66760216274000328, -9.317954957978999531 ) ) ;
#9852=EDGE_CURVE ( 'NONE', #20675, #46623, #53078, .T. ) ;
#9855=DIRECTION ( 'NONE',  ( 0.000000000000000000, -3.446666965303000135E-11, 1.000000000000000000 ) ) ;
#9860=ORIENTED_EDGE ( 'NONE', *, *, #2316, .T. ) ;
#9863=AXIS2_PLACEMENT_3D ( 'NONE', #42550, #15966, #56127 ) ;
#9867=EDGE_LOOP ( 'NONE', ( #21392, #34868, #57918, #10046 ) ) ;
#9869=EDGE_CURVE ( 'NONE', #22759, #36944, #11497, .T. ) ;
#9870=ORIENTED_EDGE ( 'NONE', *, *, #20391, .F. ) ;
#9871=ORIENTED_EDGE ( 'NONE', *, *, #14552, .F. ) ;
#9878=DIRECTION ( 'NONE',  ( -4.762495317921000031E-11, -1.000000000000000000, 4.762546956201999894E-11 ) ) ;
#9881=DIRECTION ( 'NONE',  ( 0.000000000000000000, -1.000000000000000000, 0.000000000000000000 ) ) ;
#9882=CARTESIAN_POINT ( 'NONE',  ( -1.618935784642295816, -18.07248831326895910, -12.52134385800258087 ) ) ;
#9884=CARTESIAN_POINT ( 'NONE',  ( 0.000000000000000000, -49.87071424677999687, 0.000000000000000000 ) ) ;
#9886=EDGE_CURVE ( 'NONE', #52710, #37882, #42321, .T. ) ;
#9889=CARTESIAN_POINT ( 'NONE',  ( 11.77596950146999966, -77.20276987983000083, 5.402702954953999992 ) ) ;
#9891=CARTESIAN_POINT ( 'NONE',  ( -12.75761570867000039, -22.77819125662999866, -1.931043762602999925 ) ) ;
#9896=CARTESIAN_POINT ( 'NONE',  ( 2.926762049849723102, -2.887065986493968062, 1.411820854762963595 ) ) ;
#9901=CARTESIAN_POINT ( 'NONE',  ( -10.98362417419999915, -18.84999999999999787, -0.5999999999999999778 ) ) ;
#9903=EDGE_CURVE ( 'NONE', #34968, #38188, #28172, .T. ) ;
#9905=CARTESIAN_POINT ( 'NONE',  ( -10.79468190471742695, -78.83333333333331439, -4.801183948429945225 ) ) ;
#9907=CARTESIAN_POINT ( 'NONE',  ( 9.722718241315000398, -55.54999999966999980, -7.247844507162001015 ) ) ;
#9908=AXIS2_PLACEMENT_3D ( 'NONE', #46733, #986, #14813 ) ;
#9909=AXIS2_PLACEMENT_3D ( 'NONE', #15387, #12113, #38106 ) ;
#9910=CARTESIAN_POINT ( 'NONE',  ( 2.062673488410000200, -60.12452273675999947, 12.82904109066000053 ) ) ;
#9911=CARTESIAN_POINT ( 'NONE',  ( 7.601397897754999633, -18.75000000000000000, -9.369164850722000892 ) ) ;
#9914=CARTESIAN_POINT ( 'NONE',  ( 9.263181489341201669, -78.50004972168174788, 7.234445444280653170 ) ) ;
#9922=CARTESIAN_POINT ( 'NONE',  ( 2.301364338783000285, -1.490890595155999865, -3.291430154679999998 ) ) ;
#9928=CARTESIAN_POINT ( 'NONE',  ( 12.00000000000000000, -23.15000000000000213, 0.000000000000000000 ) ) ;
#9930=ORIENTED_EDGE ( 'NONE', *, *, #15670, .T. ) ;
#9931=ORIENTED_EDGE ( 'NONE', *, *, #43956, .F. ) ;
#9935=ORIENTED_EDGE ( 'NONE', *, *, #18549, .F. ) ;
#9940=EDGE_LOOP ( 'NONE', ( #57767, #16641, #43922, #13184 ) ) ;
#9941=CARTESIAN_POINT ( 'NONE',  ( -1.063988671825434995, -2.699566373942746456, -3.070960408435446709 ) ) ;
#9942=VERTEX_POINT ( 'NONE', #25339 ) ;
#9944=DIRECTION ( 'NONE',  ( -0.9999999999995751176, 0.000000000000000000, -9.217549100139771309E-07 ) ) ;
#9945=VECTOR ( 'NONE', #20799, 1000.000000000000114 ) ;
#9948=VERTEX_POINT ( 'NONE', #43355 ) ;
#9952=FACE_BOUND ( 'NONE', #19670, .T. ) ;
#9955=CARTESIAN_POINT ( 'NONE',  ( -1.821913034590999979E-14, -80.69999999923000189, 0.000000000000000000 ) ) ;
#9956=EDGE_CURVE ( 'NONE', #25888, #23504, #44800, .T. ) ;
#9963=CARTESIAN_POINT ( 'NONE',  ( -5.600965982043615732, -78.03957589888349844, -10.69184727915017064 ) ) ;
#9970=CARTESIAN_POINT ( 'NONE',  ( 9.708203932502000200, -79.25000000000000000, -7.053423027506000587 ) ) ;
#9972=EDGE_CURVE ( 'NONE', #37820, #14569, #39249, .T. ) ;
#9973=DIRECTION ( 'NONE',  ( -0.7071067811865475727, 0.000000000000000000, -0.7071067811865475727 ) ) ;
#9978=FACE_OUTER_BOUND ( 'NONE', #748, .T. ) ;
#9979=CARTESIAN_POINT ( 'NONE',  ( -0.9212224518321000533, -53.98045898127999465, -12.54670315977999984 ) ) ;
#9981=CARTESIAN_POINT ( 'NONE',  ( 7.686941364994000381, -20.24527982330999976, 10.48774103564000093 ) ) ;
#9982=CARTESIAN_POINT ( 'NONE',  ( 10.12290050126000196, -60.04999999958999979, 7.648026767103999646 ) ) ;
#9984=CARTESIAN_POINT ( 'NONE',  ( -5.115276909939000305, -75.75838526971999443, -10.78423561930000041 ) ) ;
#9985=ORIENTED_EDGE ( 'NONE', *, *, #30091, .F. ) ;
#9992=CARTESIAN_POINT ( 'NONE',  ( -10.07627163191000008, -55.55000000278000272, -7.601397897754999633 ) ) ;
#9994=CARTESIAN_POINT ( 'NONE',  ( 12.50000000000000000, -23.24999999758999536, -1.750000000000000000 ) ) ;
#9995=CARTESIAN_POINT ( 'NONE',  ( -12.56594317825999951, -60.05000001354000005, 1.750000000000000000 ) ) ;
#9996=CARTESIAN_POINT ( 'NONE',  ( 6.694424008027000106, -76.92929967898000143, -9.543441777632999390 ) ) ;
#10001=CARTESIAN_POINT ( 'NONE',  ( -3.062995278220659756, -0.9166666666665526098, 1.359963116106802650 ) ) ;
#10002=CARTESIAN_POINT ( 'NONE',  ( 1.980584515756000030, -55.53514849873000259, -12.76303204337999908 ) ) ;
#10006=CIRCLE ( 'NONE', #50541, 1.750000000000000000 ) ;
#10007=CARTESIAN_POINT ( 'NONE',  ( -12.92181194098999875, -57.04351820043999766, -2.062502994258999856 ) ) ;
#10016=B_SPLINE_CURVE_WITH_KNOTS ( 'NONE', 3,
 ( #54264, #28543, #36533, #55423, #14671, #847, #28242, #10262, #41845, #54557, #50135, #45712, #32966, #37111, #27953, #272 ),
 .UNSPECIFIED., .F., .F.,
 ( 4, 2, 2, 2, 2, 2, 2, 4 ),
 ( 0.000000000000000000, 0.2499999999999996669, 0.3750000000000010547, 0.4375000000000017764, 0.5000000000000025535, 0.6250000000000015543, 0.7500000000000006661, 1.000000000000000000 ),
 .UNSPECIFIED. ) ;
#10018=VERTEX_POINT ( 'NONE', #1846 ) ;
#10019=CARTESIAN_POINT ( 'NONE',  ( 0.000000000000000000, -5.899999999999999467, 0.000000000000000000 ) ) ;
#10023=CARTESIAN_POINT ( 'NONE',  ( 0.000000000000000000, -0.5000000000000000000, 0.000000000000000000 ) ) ;
#10025=CARTESIAN_POINT ( 'NONE',  ( -0.2678032734925760439, -16.78567224710776529, -12.70526550769186258 ) ) ;
#10032=CARTESIAN_POINT ( 'NONE',  ( 1.328206530128999807, -76.65093621910000365, -12.23810562210000086 ) ) ;
#10033=CIRCLE ( 'NONE', #4372, 1.750000000000000000 ) ;
#10034=CARTESIAN_POINT ( 'NONE',  ( 2.521648037650194407, -2.160692059289706979, 2.456016280877232560 ) ) ;
#10035=CARTESIAN_POINT ( 'NONE',  ( 12.58338334675000070, -20.25199022618999933, 1.667961445601999992 ) ) ;
#10036=CARTESIAN_POINT ( 'NONE',  ( 4.750030159171999777, -78.67398341331998779, -11.30647155123999958 ) ) ;
#10039=CARTESIAN_POINT ( 'NONE',  ( -3.451066577810062874, -1.796365364732098957, -0.5702761658243397092 ) ) ;
#10040=VECTOR ( 'NONE', #26302, 1000.000000000000000 ) ;
#10042=CARTESIAN_POINT ( 'NONE',  ( 12.50000000000000000, -24.68359816828999698, 1.003641515614000168 ) ) ;
#10043=CARTESIAN_POINT ( 'NONE',  ( 11.37043047323898293, -77.27374362828227561, -3.893187843879513110 ) ) ;
#10046=ORIENTED_EDGE ( 'NONE', *, *, #45514, .T. ) ;
#10051=CARTESIAN_POINT ( 'NONE',  ( 0.2209175225483000216, -3.423916625800000002, -3.863862947105999979 ) ) ;
#10054=CARTESIAN_POINT ( 'NONE',  ( 8.883745460416154316, -76.00626841134847211, 7.692327491078800428 ) ) ;
#10058=CARTESIAN_POINT ( 'NONE',  ( 7.836763323858055408, -17.69488832272547185, -9.850488778970140302 ) ) ;
#10060=CARTESIAN_POINT ( 'NONE',  ( 9.708203932494999577, -79.25000000000000000, 7.053423027515000499 ) ) ;
#10065=CARTESIAN_POINT ( 'NONE',  ( 1.980584515756000030, -23.26485150094000076, 12.76303204340999997 ) ) ;
#10066=CARTESIAN_POINT ( 'NONE',  ( 7.633403241821000051, -18.61350283651999860, -10.18127013549000104 ) ) ;
#10067=CARTESIAN_POINT ( 'NONE',  ( -5.827740701927429434, -78.31867367200482022, 10.39237278454248958 ) ) ;
#10068=ORIENTED_EDGE ( 'NONE', *, *, #28273, .F. ) ;
#10070=LINE ( 'NONE', #22762, #22004 ) ;
#10075=DIRECTION ( 'NONE',  ( 0.000000000000000000, -1.000000000000000000, 0.000000000000000000 ) ) ;
#10076=DIRECTION ( 'NONE',  ( 0.000000000000000000, -0.7071067811866525998, -0.7071067811864425456 ) ) ;
#10077=EDGE_CURVE ( 'NONE', #24848, #40579, #6246, .T. ) ;
#10083=DIRECTION ( 'NONE',  ( 0.7071067811865474617, 0.000000000000000000, -0.7071067811865474617 ) ) ;
#10084=ORIENTED_EDGE ( 'NONE', *, *, #3384, .F. ) ;
#10085=AXIS2_PLACEMENT_3D ( 'NONE', #58247, #49991, #54414 ) ;
#10086=VERTEX_POINT ( 'NONE', #37833 ) ;
#10089=AXIS2_PLACEMENT_3D ( 'NONE', #30674, #27426, #49596 ) ;
#10093=CARTESIAN_POINT ( 'NONE',  ( 8.284635637516000628, -61.84861451525000575, 9.778492910201000754 ) ) ;
#10098=CARTESIAN_POINT ( 'NONE',  ( -10.41172477448170497, -23.52013115057688353, 7.610718073406644635 ) ) ;
#10105=CARTESIAN_POINT ( 'NONE',  ( 0.6677177572643692161, -2.141389681057874306, -3.206128740696444268 ) ) ;
#10109=EDGE_CURVE ( 'NONE', #46363, #49572, #10310, .T. ) ;
#10110=CARTESIAN_POINT ( 'NONE',  ( -7.646944885436999684, -23.19635956544000166, -10.19022188674999896 ) ) ;
#10111=CARTESIAN_POINT ( 'NONE',  ( 12.87024489159000140, -59.58461666436000570, -2.062597265787999845 ) ) ;
#10119=LINE ( 'NONE', #54980, #57009 ) ;
#10120=VECTOR ( 'NONE', #47455, 1000.000000000000114 ) ;
#10122=DIRECTION ( 'NONE',  ( 0.000000000000000000, 1.000000000000000000, 0.000000000000000000 ) ) ;
#10123=CARTESIAN_POINT ( 'NONE',  ( -1.707856248730948989, -3.165271797717385205, 3.077356143116399601 ) ) ;
#10126=DIRECTION ( 'NONE',  ( -0.6562721000522208081, 0.7545243075561237633, 7.878854448478247525E-10 ) ) ;
#10128=DIRECTION ( 'NONE',  ( 0.000000000000000000, -1.000000000000000000, 0.000000000000000000 ) ) ;
#10130=EDGE_LOOP ( 'NONE', ( #11461, #46846, #31032 ) ) ;
#10132=ADVANCED_FACE ( 'NONE', ( #11854 ), #4544, .F. ) ;
#10137=AXIS2_PLACEMENT_3D ( 'NONE', #15203, #28773, #1944 ) ;
#10138=CARTESIAN_POINT ( 'NONE',  ( 9.778543098479998363, -25.04857981702999936, -8.284584910395000890 ) ) ;
#10140=CARTESIAN_POINT ( 'NONE',  ( 2.598748023862139878, -1.903594524732164617, 1.996140164127287786 ) ) ;
#10141=CARTESIAN_POINT ( 'NONE',  ( -9.697390092234948966, -53.82767731322027771, -8.266602378481318070 ) ) ;
#10143=CARTESIAN_POINT ( 'NONE',  ( 7.954951288349001004, -18.75000000000000000, 9.722718241315000398 ) ) ;
#10144=CARTESIAN_POINT ( 'NONE',  ( -11.40747292386999945, -78.95515814038999736, 6.126595231985000112 ) ) ;
#10148=CARTESIAN_POINT ( 'NONE',  ( -7.850076763451487416, -24.31471441246267062, 9.837736658179169424 ) ) ;
#10150=CARTESIAN_POINT ( 'NONE',  ( -12.54976804513999866, -61.84775476195000010, -0.05637402076004000007 ) ) ;
#10152=LINE ( 'NONE', #45593, #22107 ) ;
#10155=CARTESIAN_POINT ( 'NONE',  ( 13.99609303072000088, -45.84137733102999590, 3.303213538507999633E-05 ) ) ;
#10156=DIRECTION ( 'NONE',  ( 0.000000000000000000, 0.000000000000000000, 1.000000000000000000 ) ) ;
#10159=ORIENTED_EDGE ( 'NONE', *, *, #54449, .T. ) ;
#10160=ORIENTED_EDGE ( 'NONE', *, *, #1337, .F. ) ;
#10162=ORIENTED_EDGE ( 'NONE', *, *, #33398, .F. ) ;
#10163=AXIS2_PLACEMENT_3D ( 'NONE', #54967, #41396, #36374 ) ;
#10165=EDGE_CURVE ( 'NONE', #38582, #10018, #53440, .T. ) ;
#10166=CARTESIAN_POINT ( 'NONE',  ( 0.4450739772391999471, -17.12186785197999939, 12.43586747594999942 ) ) ;
#10172=AXIS2_PLACEMENT_3D ( 'NONE', #5713, #15457, #28431 ) ;
#10173=ORIENTED_EDGE ( 'NONE', *, *, #15089, .F. ) ;
#10177=DIRECTION ( 'NONE',  ( -1.205798305761979436E-11, -1.868137355152963707E-07, -0.9999999999999824585 ) ) ;
#10178=CARTESIAN_POINT ( 'NONE',  ( 1.689459950995380044, -61.09188253861194084, -12.71013585614447194 ) ) ;
#10180=DIRECTION ( 'NONE',  ( -1.000000000000000000, 0.000000000000000000, 0.000000000000000000 ) ) ;
#10181=CARTESIAN_POINT ( 'NONE',  ( -10.01332844637000008, -23.28056692670000061, 7.654537085030000299 ) ) ;
#10182=CARTESIAN_POINT ( 'NONE',  ( 9.024219425886000678, -76.52363952651001000, -8.086445476350000661 ) ) ;
#10186=EDGE_CURVE ( 'NONE', #2185, #52707, #38552, .T. ) ;
#10190=DIRECTION ( 'NONE',  ( 1.000000000000000000, 0.000000000000000000, 0.000000000000000000 ) ) ;
#10193=DIRECTION ( 'NONE',  ( 0.000000000000000000, -1.000000000000000000, 0.000000000000000000 ) ) ;
#10194=CARTESIAN_POINT ( 'NONE',  ( -1.980584515752000119, -23.26485146623999967, 12.76303204602000108 ) ) ;
#10197=CARTESIAN_POINT ( 'NONE',  ( -2.169990332168064473, -3.499999999999999112, -2.587771324678439733 ) ) ;
#10198=CARTESIAN_POINT ( 'NONE',  ( 0.5999381870721750554, -18.76980390685249844, -10.98362755083787334 ) ) ;
#10200=ADVANCED_FACE ( 'NONE', ( #8565 ), #53154, .F. ) ;
#10202=CARTESIAN_POINT ( 'NONE',  ( 12.54435570283317780, -18.47582218226679274, -1.733918077769244448 ) ) ;
#10205=CARTESIAN_POINT ( 'NONE',  ( 0.000000000000000000, -46.43897132165000130, 0.000000000000000000 ) ) ;
#10208=CARTESIAN_POINT ( 'NONE',  ( -1.247385801055000076, -17.52277743740000204, 12.50301438876999960 ) ) ;
#10211=CARTESIAN_POINT ( 'NONE',  ( -1.997276839918484148, -2.927083333333333481, 2.598917237794077018 ) ) ;
#10215=CARTESIAN_POINT ( 'NONE',  ( 11.79999999988000070, -23.14999999478999726, -0.5999999998848000171 ) ) ;
#10222=FACE_OUTER_BOUND ( 'NONE', #41055, .T. ) ;
#10223=CARTESIAN_POINT ( 'NONE',  ( 0.000000000000000000, 4.040000000000000036, 0.000000000000000000 ) ) ;
#10224=EDGE_LOOP ( 'NONE', ( #9102, #12811, #5581, #31731 ) ) ;
#10226=ORIENTED_EDGE ( 'NONE', *, *, #37737, .F. ) ;
#10229=ORIENTED_EDGE ( 'NONE', *, *, #10230, .T. ) ;
#10230=EDGE_CURVE ( 'NONE', #44757, #47059, #34955, .T. ) ;
#10232=CARTESIAN_POINT ( 'NONE',  ( 10.42531124908000173, -60.06485148440999922, 7.624341765471999821 ) ) ;
#10233=B_SPLINE_SURFACE_WITH_KNOTS ( 'NONE', 3, 3, ( 
 ( #52633, #12190, #20757, #30749 ),
 ( #52066, #38758, #29882, #11620 ),
 ( #25760, #29596, #56776, #47652 ),
 ( #36647, #26604, #18363, #31324 ),
 ( #23070, #26327, #9502, #17477 ),
 ( #4492, #49071, #49958, #45234 ),
 ( #35766, #57919, #35466, #44935 ),
 ( #21897, #54665, #26907, #48783 ),
 ( #8327, #53493, #36355, #49367 ),
 ( #676, #40791, #27488, #53795 ),
 ( #54384, #13921, #58214, #8917 ),
 ( #18072, #36066, #97, #22490 ),
 ( #45530, #18660, #41084, #54086 ),
 ( #13329, #13624, #8619, #44341 ),
 ( #5074, #49665, #13035, #31914 ),
 ( #3894, #31622, #40501, #9208 ),
 ( #385, #14206, #39905, #22191 ) ),
 .UNSPECIFIED., .F., .F., .F.,
 ( 4, 1, 1, 1, 1, 1, 1, 1, 1, 1, 1, 1, 1, 1, 4 ),
 ( 4, 4 ),
 ( -0.01011400514350000064, 0.000000000000000000, 0.08333333333333001192, 0.1666666666667000196, 0.2500000000000000000, 0.3333333333333000081, 0.4166666666666999919, 0.5000000000000000000, 0.5833333333333000637, 0.6666666666667000474, 0.7500000000000000000, 0.8333333333333000637, 0.9166666666667000474, 1.000000000000000000, 1.010365328128000062 ),
 ( -0.3559705546945999832, 1.357612395619000045 ),
 .UNSPECIFIED. ) ;
#10236=ORIENTED_EDGE ( 'NONE', *, *, #2040, .F. ) ;
#10237=FACE_OUTER_BOUND ( 'NONE', #39176, .T. ) ;
#10241=CARTESIAN_POINT ( 'NONE',  ( -11.38694148309949128, -78.98049139715394062, -4.554723408025081355 ) ) ;
#10242=AXIS2_PLACEMENT_3D ( 'NONE', #43428, #53436, #12698 ) ;
#10244=CARTESIAN_POINT ( 'NONE',  ( -8.768124086712999699, -59.94999999969000015, 7.919595949288999570 ) ) ;
#10245=CARTESIAN_POINT ( 'NONE',  ( -7.718346056099999686, -58.54888345776999614, -10.07719973192999952 ) ) ;
#10247=CARTESIAN_POINT ( 'NONE',  ( -0.5999381870721927079, -23.23019609315233325, -10.98362755083787690 ) ) ;
#10248=ADVANCED_FACE ( 'NONE', ( #45776 ), #36012, .F. ) ;
#10259=CARTESIAN_POINT ( 'NONE',  ( -9.929702205026998740, -61.43097880247000120, -7.973987073312001073 ) ) ;
#10260=CARTESIAN_POINT ( 'NONE',  ( 1.247385798810000113, -54.32277743478999810, -12.50301438874000048 ) ) ;
#10261=EDGE_CURVE ( 'NONE', #17264, #18726, #50831, .T. ) ;
#10262=CARTESIAN_POINT ( 'NONE',  ( 12.70455691843822343, -24.56014620597932918, -1.489817752280619967 ) ) ;
#10263=FACE_OUTER_BOUND ( 'NONE', #33903, .T. ) ;
#10264=CARTESIAN_POINT ( 'NONE',  ( 7.651147547618999845, -56.03743349692000209, -10.45204383579000051 ) ) ;
#10265=CARTESIAN_POINT ( 'NONE',  ( -1.541016483300999829, -2.132935987229999775, -3.126416733747999999 ) ) ;
#10266=EDGE_CURVE ( 'NONE', #822, #26684, #5384, .T. ) ;
#10267=CARTESIAN_POINT ( 'NONE',  ( 12.82230166703000052, -23.42260938006999993, 2.065916748305000272 ) ) ;
#10269=LINE ( 'NONE', #32101, #40134 ) ;
#10270=CARTESIAN_POINT ( 'NONE',  ( 1.798944584240000255, -60.01533228248000285, 12.61116916001999932 ) ) ;
#10272=CARTESIAN_POINT ( 'NONE',  ( -0.4579595194372000355, -76.87759916035999197, -12.05314280177999997 ) ) ;
#10279=CARTESIAN_POINT ( 'NONE',  ( -7.247844507162001015, -23.25000000000000000, 9.722718241315000398 ) ) ;
#10285=VERTEX_POINT ( 'NONE', #43652 ) ;
#10286=CARTESIAN_POINT ( 'NONE',  ( -2.539546420801134019, -0.8541666666665600482, 2.281950960269295337 ) ) ;
#10287=CARTESIAN_POINT ( 'NONE',  ( 0.8804656548135700866, -53.77196605261325857, -12.70299681147314708 ) ) ;
#10289=AXIS2_PLACEMENT_3D ( 'NONE', #7055, #43077, #16207 ) ;
#10290=ADVANCED_FACE ( 'NONE', ( #38634 ), #35046, .F. ) ;
#10291=CARTESIAN_POINT ( 'NONE',  ( 10.04953137661648199, -75.90590377007603706, -6.156255326924525484 ) ) ;
#10292=ORIENTED_EDGE ( 'NONE', *, *, #18627, .T. ) ;
#10295=LINE ( 'NONE', #28573, #24706 ) ;
#10299=LINE ( 'NONE', #22995, #18643 ) ;
#10300=AXIS2_PLACEMENT_3D ( 'NONE', #18490, #54512, #50088 ) ;
#10302=ORIENTED_EDGE ( 'NONE', *, *, #2462, .F. ) ;
#10303=CONICAL_SURFACE ( 'NONE', #56488, 0.6999999997695030007, 0.7853981633972997312 ) ;
#10304=DIRECTION ( 'NONE',  ( -0.07798810159117737506, -0.04890177459366838036, -0.9957542229143666601 ) ) ;
#10305=EDGE_CURVE ( 'NONE', #37146, #11113, #39153, .T. ) ;
#10307=EDGE_LOOP ( 'NONE', ( #14275, #22933, #20182, #48286 ) ) ;
#10308=FACE_OUTER_BOUND ( 'NONE', #31752, .T. ) ;
#10309=CARTESIAN_POINT ( 'NONE',  ( 11.79999999988000070, -23.14999999478999726, -0.5999999998848000171 ) ) ;
#10310=B_SPLINE_CURVE_WITH_KNOTS ( 'NONE', 3,
 ( #15406, #6544, #24553, #42568, #7701, #48732 ),
 .UNSPECIFIED., .F., .F.,
 ( 4, 1, 1, 4 ),
 ( 0.000000000000000000, 0.3333333333333000081, 0.6666666666667000474, 1.000000000000000000 ),
 .UNSPECIFIED. ) ;
#10315=CARTESIAN_POINT ( 'NONE',  ( 8.768124086549999419, -59.94999999446000771, 7.919595949288999570 ) ) ;
#10317=CARTESIAN_POINT ( 'NONE',  ( -12.71466563516724158, -17.86210710701672610, -1.778810201854685857 ) ) ;
#10319=CARTESIAN_POINT ( 'NONE',  ( 10.27342224349336419, -17.93842478175138311, 7.712153330322453648 ) ) ;
#10321=CARTESIAN_POINT ( 'NONE',  ( 11.88049207238000093, -76.24625088658999061, -3.223263369271999856 ) ) ;
#10322=CARTESIAN_POINT ( 'NONE',  ( -2.150973351021207236, -1.921964726325504413, -2.785944457644208949 ) ) ;
#10324=FACE_OUTER_BOUND ( 'NONE', #14467, .T. ) ;
#10325=CARTESIAN_POINT ( 'NONE',  ( 11.81418954875000082, -78.78894628561999980, 3.289986436736999753 ) ) ;
#10327=CARTESIAN_POINT ( 'NONE',  ( 12.74365836114991346, -18.47810168886552162, -1.980611005600054986 ) ) ;
#10328=CARTESIAN_POINT ( 'NONE',  ( 2.557969438714201349, -2.797342906287011655, -2.007748672213171215 ) ) ;
#10329=CARTESIAN_POINT ( 'NONE',  ( -11.97917456330697838, -78.05650138543988703, -0.9813211398764013493 ) ) ;
#10333=CARTESIAN_POINT ( 'NONE',  ( -5.917523019358058356, -77.88333333333329733, -10.26699006316253282 ) ) ;
#10334=DIRECTION ( 'NONE',  ( 0.7071067811865475727, 0.000000000000000000, -0.7071067811865475727 ) ) ;
#10337=CARTESIAN_POINT ( 'NONE',  ( -1.859685218087000047, -3.298191639609999726, 3.214968926965999785 ) ) ;
#10341=CARTESIAN_POINT ( 'NONE',  ( -10.76168635603615975, -76.16692037179028318, 4.717286685116878431 ) ) ;
#10345=CARTESIAN_POINT ( 'NONE',  ( 12.70556836328846373, -25.22772277325712764, 0.2642470010264758584 ) ) ;
#10346=CARTESIAN_POINT ( 'NONE',  ( 10.98648384835751024, -79.20851479812272089, 4.884329123650943849 ) ) ;
#10347=CARTESIAN_POINT ( 'NONE',  ( 1.538071403320016461, -76.93541666666665435, -11.74999999999999822 ) ) ;
#10351=CARTESIAN_POINT ( 'NONE',  ( 8.284626357352999904, -16.95139346842000094, -9.778502130864000108 ) ) ;
#10352=DIRECTION ( 'NONE',  ( 0.000000000000000000, -1.000000000000000000, 0.000000000000000000 ) ) ;
#10357=CARTESIAN_POINT ( 'NONE',  ( 12.01773220436371403, -77.71045720483247976, 1.122334885944337168 ) ) ;
#10362=CARTESIAN_POINT ( 'NONE',  ( 13.94241847916999966, -9.539970597796999741, 4.312626734329999762E-05 ) ) ;
#10364=CARTESIAN_POINT ( 'NONE',  ( -8.485281374238999419, -59.94999999967000548, -8.485281374238999419 ) ) ;
#10366=EDGE_CURVE ( 'NONE', #40915, #38307, #30019, .T. ) ;
#10368=VERTEX_POINT ( 'NONE', #7914 ) ;
#10372=AXIS2_PLACEMENT_3D ( 'NONE', #37794, #46974, #25085 ) ;
#10373=EDGE_LOOP ( 'NONE', ( #20121, #30454, #15825 ) ) ;
#10376=CIRCLE ( 'NONE', #30163, 12.69999999999999929 ) ;
#10378=EDGE_CURVE ( 'NONE', #50691, #54307, #53080, .T. ) ;
#10379=CARTESIAN_POINT ( 'NONE',  ( 7.620012114232000755, -60.00560398617000146, 10.53562503196000044 ) ) ;
#10384=EDGE_LOOP ( 'NONE', ( #11326, #5352, #56207, #24960, #24094, #17497 ) ) ;
#10385=CARTESIAN_POINT ( 'NONE',  ( -7.610436523679670273, -23.52540704710936126, 10.41144397132592836 ) ) ;
#10389=CARTESIAN_POINT ( 'NONE',  ( 8.485281374238999419, -55.64999999967000122, 8.485281374238999419 ) ) ;
#10397=CARTESIAN_POINT ( 'NONE',  ( -8.478749451758998745, -24.87812788920000173, -9.108222796172999125 ) ) ;
#10398=CARTESIAN_POINT ( 'NONE',  ( 12.75761570867999950, -56.02180874340999850, -1.931043762602999925 ) ) ;
#10400=CIRCLE ( 'NONE', #21681, 12.50000000000000000 ) ;
#10406=ADVANCED_FACE ( 'NONE', ( #25916 ), #12519, .F. ) ;
#10407=CARTESIAN_POINT ( 'NONE',  ( -7.981651535810999398, -17.28135615487000010, 10.08154952397000059 ) ) ;
#10409=CARTESIAN_POINT ( 'NONE',  ( 3.582811860122647296, -2.504862101322317347, 0.2337939847196791321 ) ) ;
#10414=CARTESIAN_POINT ( 'NONE',  ( 1.710992592906253718, -0.8541666519182247175, -2.966907352992771862 ) ) ;
#10417=CARTESIAN_POINT ( 'NONE',  ( 0.9212224518285999642, -61.61954101805999784, -12.54670315985999984 ) ) ;
#10422=CARTESIAN_POINT ( 'NONE',  ( 7.618394338636999663, -23.22713821270000167, -10.53494418059000104 ) ) ;
#10430=CARTESIAN_POINT ( 'NONE',  ( 4.750168553339000788, -78.64926952346999656, -12.04580866360999991 ) ) ;
#10434=CARTESIAN_POINT ( 'NONE',  ( 7.919595949288999570, -55.64999999964999233, -9.050966799188000067 ) ) ;
#10436=CARTESIAN_POINT ( 'NONE',  ( -13.86363636363000218, -32.36102867817999851, -1.277888278874999896E-05 ) ) ;
#10437=ORIENTED_EDGE ( 'NONE', *, *, #24128, .T. ) ;
#10441=EDGE_CURVE ( 'NONE', #37950, #237, #24403, .T. ) ;
#10444=FACE_OUTER_BOUND ( 'NONE', #54942, .T. ) ;
#10447=AXIS2_PLACEMENT_3D ( 'NONE', #10711, #28689, #51449 ) ;
#10448=EDGE_CURVE ( 'NONE', #42344, #15053, #34222, .T. ) ;
#10452=CARTESIAN_POINT ( 'NONE',  ( 1.466594960159999905, -17.91841800947999985, 12.44238958332999800 ) ) ;
#10459=EDGE_CURVE ( 'NONE', #35553, #32105, #10558, .T. ) ;
#10460=ORIENTED_EDGE ( 'NONE', *, *, #41760, .F. ) ;
#10461=ORIENTED_EDGE ( 'NONE', *, *, #24334, .T. ) ;
#10463=AXIS2_PLACEMENT_3D ( 'NONE', #2532, #39403, #16394 ) ;
#10466=CARTESIAN_POINT ( 'NONE',  ( 1.001315002179999913, -17.31477588286000113, 12.50000000000000000 ) ) ;
#10468=FACE_OUTER_BOUND ( 'NONE', #35664, .T. ) ;
#10470=DIRECTION ( 'NONE',  ( 0.000000000000000000, 1.000000000000000000, 0.000000000000000000 ) ) ;
#10473=CARTESIAN_POINT ( 'NONE',  ( -8.293363313813765458, -76.63724320113942667, 8.323509784614648410 ) ) ;
#10478=ADVANCED_FACE ( 'NONE', ( #55420 ), #37582, .F. ) ;
#10479=CARTESIAN_POINT ( 'NONE',  ( -7.633502222236000279, -18.79895684643999942, -10.36289759016999845 ) ) ;
#10480=DIRECTION ( 'NONE',  ( 0.000000000000000000, 0.000000000000000000, 1.000000000000000000 ) ) ;
#10482=DIRECTION ( 'NONE',  ( -0.7592504788685878747, 0.04890177849880918831, 0.6489586476790899505 ) ) ;
#10484=DIRECTION ( 'NONE',  ( 0.000000000000000000, 1.000000000000000000, 6.735284179502000863E-11 ) ) ;
#10486=ORIENTED_EDGE ( 'NONE', *, *, #19517, .T. ) ;
#10487=CARTESIAN_POINT ( 'NONE',  ( -2.460715419380010260, -78.90833333333333144, -11.55514622821886839 ) ) ;
#10488=DIRECTION ( 'NONE',  ( 0.000000000000000000, 1.000000000000000000, 0.000000000000000000 ) ) ;
#10490=CARTESIAN_POINT ( 'NONE',  ( 12.43569926720000041, -61.68202092968000727, -0.4277578398253000236 ) ) ;
#10492=CARTESIAN_POINT ( 'NONE',  ( 1.931043762602999925, -56.02180874340999850, 12.75761570867999950 ) ) ;
#10493=CARTESIAN_POINT ( 'NONE',  ( 12.51033564907000084, -78.17580835132000061, -3.582046052171000028 ) ) ;
#10497=B_SPLINE_CURVE_WITH_KNOTS ( 'NONE', 3,
 ( #46580, #38270, #15844, #6107, #11424, #1698, #47456, #24114, #19992, #42133, #19692, #37692, #29117, #15258, #55711, #51292, #10848, #28822, #37979, #15553, #33546, #43582, #3426, #58020, #11999, #40004, #26140, #34983, #12566, #48594, #44161, #17002, #53013, #56868, #48880, #39717, #35270, #30563, #39435, #8140, #43878, #57724, #57442, #52439, #3994, #3708, #20846, #21711, #17581, #48030, #53303, #12279, #25274, #17280, #12846, #21996, #30845, #8423, #52728, #7850, #35568, #53594, #26420, #13134, #25851, #30269, #29977, #47740, #3144, #44442, #7273, #21427, #43293, #2849, #38850, #21132, #57151, #48311, #16427, #34410, #7562, #25562, #39141, #16716, #34698, #23176, #9896, #36170, #49472, #774, #36746, #40605, #13431, #41474, #9311, #54763, #4886, #32300, #50347 ),
 .UNSPECIFIED., .F., .F.,
 ( 4, 2, 2, 2, 1, 1, 1, 1, 2, 2, 2, 2, 2, 1, 1, 1, 1, 2, 2, 2, 2, 2, 1, 1, 1, 1, 2, 2, 2, 2, 2, 1, 1, 1, 2, 2, 2, 2, 1, 1, 1, 1, 2, 2, 2, 2, 2, 1, 1, 1, 2, 2, 2, 2, 2, 1, 1, 1, 2, 2, 2, 4 ),
 ( 0.000000000000000000, 0.06250000000000603684, 0.09375000000000904832, 0.1093750000000105194, 0.1171875000000112688, 0.1210937500000117129, 0.1230468750000119349, 0.1240234375000121014, 0.1245117187500121569, 0.1250000000000121847, 0.1875000000000133504, 0.2187500000000138500, 0.2343750000000139888, 0.2421875000000140443, 0.2460937500000140721, 0.2480468750000141831, 0.2490234375000141553, 0.2495117187500141276, 0.2500000000000140998, 0.3125000000000109912, 0.3437500000000094369, 0.3593750000000087153, 0.3671875000000083822, 0.3710937500000082157, 0.3730468750000080491, 0.3740234375000080491, 0.3745117187500080491, 0.3750000000000079936, 0.4375000000000078826, 0.4687500000000078826, 0.4843750000000078271, 0.4921875000000077716, 0.4960937500000077716, 0.4980468750000077716, 0.4990234375000077161, 0.5000000000000076605, 0.5625000000000073275, 0.5937500000000072164, 0.6093750000000069944, 0.6171875000000069944, 0.6210937500000068834, 0.6230468750000069944, 0.6240234375000069944, 0.6250000000000069944, 0.6875000000000058842, 0.7187500000000053291, 0.7343750000000051070, 0.7421875000000048850, 0.7460937500000047740, 0.7480468750000047740, 0.7490234375000047740, 0.7500000000000046629, 0.8125000000000039968, 0.8437500000000036637, 0.8593750000000035527, 0.8671875000000033307, 0.8710937500000033307, 0.8730468750000033307, 0.8740234375000032196, 0.8750000000000032196, 0.9375000000000016653, 1.000000000000000000 ),
 .UNSPECIFIED. ) ;
#10500=CARTESIAN_POINT ( 'NONE',  ( -2.690539317418799925, -76.30618315013305164, -11.43924176612597421 ) ) ;
#10506=CARTESIAN_POINT ( 'NONE',  ( -2.598917237794094337, -2.947916666666666519, 1.997276839918461722 ) ) ;
#10512=CIRCLE ( 'NONE', #30284, 8.500000000000000000 ) ;
#10515=EDGE_CURVE ( 'NONE', #25083, #44710, #42140, .T. ) ;
#10519=EDGE_CURVE ( 'NONE', #31399, #14569, #34738, .T. ) ;
#10524=ORIENTED_EDGE ( 'NONE', *, *, #10441, .T. ) ;
#10528=LINE ( 'NONE', #19671, #26154 ) ;
#10529=ADVANCED_FACE ( 'NONE', ( #5820 ), #14967, .F. ) ;
#10531=CARTESIAN_POINT ( 'NONE',  ( -7.654537085013999764, -55.51943307300000185, 10.01332844635999919 ) ) ;
#10536=FACE_OUTER_BOUND ( 'NONE', #37584, .T. ) ;
#10537=CARTESIAN_POINT ( 'NONE',  ( -5.950974066117157513, -78.86552852484902587, 10.72351851458284955 ) ) ;
#10541=CARTESIAN_POINT ( 'NONE',  ( -7.653559626076999578, -55.50151115525000023, -10.01235002620999914 ) ) ;
#10543=CARTESIAN_POINT ( 'NONE',  ( 4.934236507922636683, -76.54027943633899156, 10.66431010429060500 ) ) ;
#10546=VECTOR ( 'NONE', #25620, 1000.000000000000000 ) ;
#10548=CARTESIAN_POINT ( 'NONE',  ( -0.9356112540347810702, -61.54107830070422125, -12.50329130249530962 ) ) ;
#10550=AXIS2_PLACEMENT_3D ( 'NONE', #29373, #11109, #56260 ) ;
#10556=DIRECTION ( 'NONE',  ( -0.6489586469528950685, -0.04890178981570961203, 0.7592504787603941985 ) ) ;
#10558=LINE ( 'NONE', #28241, #36648 ) ;
#10559=CARTESIAN_POINT ( 'NONE',  ( -1.004305231718999991, -3.500000000000000000, 3.090933677959000203 ) ) ;
#10560=CARTESIAN_POINT ( 'NONE',  ( 7.648026766715999791, -55.54999999381000464, 10.12290050087000104 ) ) ;
#10562=DIRECTION ( 'NONE',  ( 1.000000000000000000, 0.000000000000000000, 0.000000000000000000 ) ) ;
#10564=LINE ( 'NONE', #37705, #9395 ) ;
#10565=ADVANCED_FACE ( 'NONE', ( #23826 ), #31381, .F. ) ;
#10568=CARTESIAN_POINT ( 'NONE',  ( -0.2584144827219213014, -25.22845396921143646, -12.70558781488152178 ) ) ;
#10569=CARTESIAN_POINT ( 'NONE',  ( -12.11766251513999926, -76.17843941428000676, -1.515192406448999884 ) ) ;
#10570=ORIENTED_EDGE ( 'NONE', *, *, #17371, .F. ) ;
#10574=CARTESIAN_POINT ( 'NONE',  ( 8.894932048652069767, -53.57190732449146253, 9.073469156702891780 ) ) ;
#10576=CARTESIAN_POINT ( 'NONE',  ( 8.485281374238999419, -23.25000000000000000, 8.485281374238999419 ) ) ;
#10581=ORIENTED_EDGE ( 'NONE', *, *, #11187, .F. ) ;
#10588=DIRECTION ( 'NONE',  ( 0.7071067811865475727, 0.000000000000000000, 0.7071067811865475727 ) ) ;
#10589=EDGE_LOOP ( 'NONE', ( #19300, #46272, #29880, #42923 ) ) ;
#10590=EDGE_CURVE ( 'NONE', #41082, #49440, #52736, .T. ) ;
#10593=DIRECTION ( 'NONE',  ( 0.000000000000000000, -1.000000000000000000, 0.000000000000000000 ) ) ;
#10594=ORIENTED_EDGE ( 'NONE', *, *, #16825, .F. ) ;
#10595=VERTEX_POINT ( 'NONE', #30276 ) ;
#10603=CARTESIAN_POINT ( 'NONE',  ( 8.620921567869039848, -25.16528830419391838, -9.346042574068809117 ) ) ;
#10606=ADVANCED_FACE ( 'NONE', ( #54196 ), #31915, .F. ) ;
#10609=AXIS2_PLACEMENT_3D ( 'NONE', #4625, #22625, #231 ) ;
#10610=CARTESIAN_POINT ( 'NONE',  ( 10.07627163191000008, -55.55000000209000177, -7.601397897754999633 ) ) ;
#10611=CARTESIAN_POINT ( 'NONE',  ( 0.2584144826998103217, -16.77154603077302752, -12.70558781487933153 ) ) ;
#10613=DIRECTION ( 'NONE',  ( 0.000000000000000000, 1.000000000000000000, 0.000000000000000000 ) ) ;
#10616=CARTESIAN_POINT ( 'NONE',  ( 7.331368884251999951, -75.80689888741999027, 9.888700222343000945 ) ) ;
#10619=ADVANCED_FACE ( 'NONE', ( #13438 ), #45642, .F. ) ;
#10620=CARTESIAN_POINT ( 'NONE',  ( 10.00844230538000090, -60.16891112520000462, -7.647097279411999793 ) ) ;
#10621=CARTESIAN_POINT ( 'NONE',  ( -12.02296678431999943, -78.50153910486000086, 2.418109797047000242 ) ) ;
#10623=CARTESIAN_POINT ( 'NONE',  ( 12.70451796517036236, -16.82354927384910326, -0.5205401191694412066 ) ) ;
#10624=CARTESIAN_POINT ( 'NONE',  ( 3.011380544091495359, -2.820368407733745197, -1.220682024450374659 ) ) ;
#10625=CARTESIAN_POINT ( 'NONE',  ( -12.21774757455541227, -77.54059286367716197, 1.402801556591745102 ) ) ;
#10630=CARTESIAN_POINT ( 'NONE',  ( -8.343860018000999190, -59.94999999967000548, 8.343860018000999190 ) ) ;
#10631=CIRCLE ( 'NONE', #45527, 4.999999999999996447 ) ;
#10633=CARTESIAN_POINT ( 'NONE',  ( 3.682706024758999774, -2.519491823149000442, -1.190799860096000140 ) ) ;
#10634=EDGE_CURVE ( 'NONE', #52467, #48012, #9030, .T. ) ;
#10637=CARTESIAN_POINT ( 'NONE',  ( -7.649652380981335043, -76.13136791021121041, 8.919978599461032331 ) ) ;
#10641=ORIENTED_EDGE ( 'NONE', *, *, #6214, .F. ) ;
#10645=B_SPLINE_CURVE_WITH_KNOTS ( 'NONE', 3,
 ( #39166, #57176, #16742, #25876, #43903, #54511 ),
 .UNSPECIFIED., .F., .F.,
 ( 4, 1, 1, 4 ),
 ( 0.000000000000000000, 0.3333333333333000081, 0.6666666666667000474, 1.000000000000000000 ),
 .UNSPECIFIED. ) ;
#10653=CARTESIAN_POINT ( 'NONE',  ( 8.870405106263998363, -16.93036971772000143, -8.878274241758997931 ) ) ;
#10655=EDGE_LOOP ( 'NONE', ( #12259, #41964, #41739, #4145, #42471, #14538, #52640, #55016, #28094, #16860, #40119, #22029 ) ) ;
#10657=AXIS2_PLACEMENT_3D ( 'NONE', #54057, #31587, #22457 ) ;
#10660=CARTESIAN_POINT ( 'NONE',  ( -13.95956770371999944, -45.71924237694000226, -5.182383547034000008E-05 ) ) ;
#10661=CARTESIAN_POINT ( 'NONE',  ( -10.35422612692059197, -77.91059695121818152, 6.109131574142480758 ) ) ;
#10662=B_SPLINE_SURFACE_WITH_KNOTS ( 'NONE', 3, 3, ( 
 ( #33932, #51970, #21230, #18205, #9630, #32041, #40631, #226, #31155, #39234, #27618, #53926, #53620, #27904, #50086, #45658, #5201, #54214, #18488 ),
 ( #36481, #9045, #35894, #23202, #49193, #27329, #58342, #41207, #8745, #36771, #49794, #13749, #9340, #54510, #512, #54789, #22619, #45363, #50375 ),
 ( #26736, #797, #18779, #4912, #22316, #22911, #9922, #31749, #40924, #13458, #14331, #14047, #32328, #3238, #58043, #17603, #35592, #27031, #13158 ),
 ( #44767, #4316, #40333, #17905, #4620, #31454, #49496, #45068, #36196, #46540, #19648, #23778, #37937, #55960, #45950, #19361, #55370, #41500, #24373 ) ),
 .UNSPECIFIED., .F., .F., .F.,
 ( 4, 4 ),
 ( 4, 1, 1, 1, 1, 1, 1, 1, 1, 1, 1, 1, 1, 1, 1, 1, 4 ),
 ( -0.02000000000000999936, 1.020000000000000018 ),
 ( -0.01116670151518999940, 0.02512507840917000204, 0.06141685833353999896, 0.09770863825790000734, 0.1340004181822999907, 0.1702921981065999846, 0.2065839780310000096, 0.2428757579554000068, 0.2791675378797000007, 0.3154593178041000257, 0.3517510977284000195, 0.3880428776527999890, 0.4243346575772000140, 0.4606264375015000079, 0.4969182174258999773, 0.5332099973503000578, 0.5695017772746000517 ),
 .UNSPECIFIED. ) ;
#10663=AXIS2_PLACEMENT_3D ( 'NONE', #13967, #22831, #13377 ) ;
#10666=CARTESIAN_POINT ( 'NONE',  ( 12.50745077494999968, -61.79994448255000350, 2.662030659623000237E-09 ) ) ;
#10667=FACE_OUTER_BOUND ( 'NONE', #8292, .T. ) ;
#10669=CARTESIAN_POINT ( 'NONE',  ( 1.980464483675000054, -20.24439829391000245, 12.85140862646999871 ) ) ;
#10672=ORIENTED_EDGE ( 'NONE', *, *, #51508, .T. ) ;
#10676=ORIENTED_EDGE ( 'NONE', *, *, #683, .F. ) ;
#10677=CARTESIAN_POINT ( 'NONE',  ( 9.788022091682998749, -17.47120090402999892, 7.956349397064001572 ) ) ;
#10679=CARTESIAN_POINT ( 'NONE',  ( -11.90254689395000121, -78.34440606474001356, -1.953697528535000005 ) ) ;
#10680=CARTESIAN_POINT ( 'NONE',  ( 8.533826143256000307, -61.80526450216999734, 9.213084459935000581 ) ) ;
#10683=AXIS2_PLACEMENT_3D ( 'NONE', #9884, #11061, #41755 ) ;
#10686=CARTESIAN_POINT ( 'NONE',  ( -9.697372265328400687, -24.97233735039882063, 8.266620275706634047 ) ) ;
#10687=ORIENTED_EDGE ( 'NONE', *, *, #46657, .F. ) ;
#10692=AXIS2_PLACEMENT_3D ( 'NONE', #33048, #2085, #20083 ) ;
#10695=CARTESIAN_POINT ( 'NONE',  ( 0.000000000000000000, -60.04999999966999980, -12.50000000000000000 ) ) ;
#10697=CIRCLE ( 'NONE', #30431, 1.749999999999999556 ) ;
#10700=CARTESIAN_POINT ( 'NONE',  ( 12.70556836352000118, -62.02772277195000328, 2.424222323408999617E-09 ) ) ;
#10701=CARTESIAN_POINT ( 'NONE',  ( 12.60552522438000089, -60.08917565288000162, -1.799501877759999813 ) ) ;
#10708=CARTESIAN_POINT ( 'NONE',  ( -7.634437838915999919, -18.25219468451000182, 10.30764259110000047 ) ) ;
#10710=CARTESIAN_POINT ( 'NONE',  ( -3.572991711198483245, -2.758169930076621146, -0.3534553494227741233 ) ) ;
#10711=CARTESIAN_POINT ( 'NONE',  ( 0.000000000000000000, -60.04999999966999980, -12.00000000000000000 ) ) ;
#10715=CARTESIAN_POINT ( 'NONE',  ( 2.700519054749793924, -0.8736979072298788340, -2.074293297084300214 ) ) ;
#10716=FACE_OUTER_BOUND ( 'NONE', #31227, .T. ) ;
#10717=ORIENTED_EDGE ( 'NONE', *, *, #20456, .T. ) ;
#10718=EDGE_CURVE ( 'NONE', #35763, #32105, #20857, .T. ) ;
#10720=CARTESIAN_POINT ( 'NONE',  ( 1.669724228651999987, -60.16897676502000536, -12.48434610070000161 ) ) ;
#10724=CARTESIAN_POINT ( 'NONE',  ( 7.605690822180000588, -23.42565082156999878, -10.52682217035000001 ) ) ;
#10727=CARTESIAN_POINT ( 'NONE',  ( -10.25203062048491987, -54.67822876342075489, -7.730397977250241581 ) ) ;
#10728=ORIENTED_EDGE ( 'NONE', *, *, #34778, .T. ) ;
#10731=ADVANCED_FACE ( 'NONE', ( #26722 ), #36464, .T. ) ;
#10733=CARTESIAN_POINT ( 'NONE',  ( 8.478741751108000102, -53.92187496570999627, -9.108230428579000559 ) ) ;
#10734=EDGE_CURVE ( 'NONE', #42913, #37628, #57432, .T. ) ;
#10742=CARTESIAN_POINT ( 'NONE',  ( -8.485281374238999419, -60.04999999966999980, 8.485281374238999419 ) ) ;
#10749=ORIENTED_EDGE ( 'NONE', *, *, #43021, .T. ) ;
#10752=ORIENTED_EDGE ( 'NONE', *, *, #497, .T. ) ;
#10754=CARTESIAN_POINT ( 'NONE',  ( 1.814305421036000121, -17.71058030669000161, 12.78003582253000125 ) ) ;
#10756=CARTESIAN_POINT ( 'NONE',  ( 0.000000000000000000, -39.30476017083000073, 0.000000000000000000 ) ) ;
#10761=ORIENTED_EDGE ( 'NONE', *, *, #27057, .T. ) ;
#10763=CARTESIAN_POINT ( 'NONE',  ( -12.70556836347999941, -25.22772277227999993, -2.424223956931999920E-09 ) ) ;
#10765=CARTESIAN_POINT ( 'NONE',  ( 1.782734487938277379, -60.92245368521658122, -12.71547286929869180 ) ) ;
#10767=CYLINDRICAL_SURFACE ( 'NONE', #47355, 0.5999999999999999778 ) ;
#10773=CARTESIAN_POINT ( 'NONE',  ( -5.863032908986463454, -76.61570338723420548, 10.21229380548447274 ) ) ;
#10774=CARTESIAN_POINT ( 'NONE',  ( 8.504267844457428893, -79.24218749521728000, -8.507439143850103136 ) ) ;
#10777=CARTESIAN_POINT ( 'NONE',  ( -1.750000000000000000, -20.24935285954000008, -12.65372179284999810 ) ) ;
#10778=CARTESIAN_POINT ( 'NONE',  ( 2.062502994258999856, -20.24351820077000141, -12.92181194099999963 ) ) ;
#10780=CARTESIAN_POINT ( 'NONE',  ( 1.930628539545000022, -18.77875555914000216, -12.72375828104000028 ) ) ;
#10782=CARTESIAN_POINT ( 'NONE',  ( -7.624341764943999955, -60.06485149430999826, 10.42531124854999902 ) ) ;
#10784=CARTESIAN_POINT ( 'NONE',  ( -14.00000000000000000, -69.50420297070000686, 0.000000000000000000 ) ) ;
#10785=CARTESIAN_POINT ( 'NONE',  ( 8.385799987749599893, -61.68809827201926055, 9.298537617308133107 ) ) ;
#10787=CARTESIAN_POINT ( 'NONE',  ( -8.485281374238999419, -23.25000000000000000, 8.485281374238999419 ) ) ;
#10788=FACE_OUTER_BOUND ( 'NONE', #4194, .T. ) ;
#10791=CARTESIAN_POINT ( 'NONE',  ( 5.647598101448999763, -77.78727586459000065, 11.72364604052000203 ) ) ;
#10801=CARTESIAN_POINT ( 'NONE',  ( -8.485281374238999419, -55.64999999967000122, -8.485281374238999419 ) ) ;
#10803=CARTESIAN_POINT ( 'NONE',  ( -3.206516299415000049, -1.613032031399000088, -0.5298615117031000299 ) ) ;
#10807=AXIS2_PLACEMENT_3D ( 'NONE', #8362, #26360, #3932 ) ;
#10809=DIRECTION ( 'NONE',  ( 0.7071067811865475727, 0.000000000000000000, 0.7071067811865475727 ) ) ;
#10811=ORIENTED_EDGE ( 'NONE', *, *, #51087, .F. ) ;
#10815=LINE ( 'NONE', #28794, #30319 ) ;
#10817=ORIENTED_EDGE ( 'NONE', *, *, #47097, .F. ) ;
#10820=EDGE_CURVE ( 'NONE', #18938, #2185, #13847, .T. ) ;
#10823=CARTESIAN_POINT ( 'NONE',  ( 8.137215171343381570, -60.25155696365702340, 7.401770473315491650 ) ) ;
#10824=ORIENTED_EDGE ( 'NONE', *, *, #7171, .T. ) ;
#10827=VERTEX_POINT ( 'NONE', #55945 ) ;
#10830=CARTESIAN_POINT ( 'NONE',  ( 2.568255498652000313, -2.248719782538000089, -2.230126530280999830 ) ) ;
#10835=PLANE ( 'NONE',  #15220 ) ;
#10843=CARTESIAN_POINT ( 'NONE',  ( 6.551839081868985559, -76.52774692925073907, 9.753635134337040213 ) ) ;
#10848=CARTESIAN_POINT ( 'NONE',  ( -2.723040898605983084, -3.054315476261060258, 1.788012656602580019 ) ) ;
#10854=CARTESIAN_POINT ( 'NONE',  ( 7.714303428875997959, -52.49705297113997204, 12.53545825868000385 ) ) ;
#10855=CARTESIAN_POINT ( 'NONE',  ( -11.65013480063129059, -76.21076195607875547, -1.612759596057231848 ) ) ;
#10857=CARTESIAN_POINT ( 'NONE',  ( -10.47513974136000137, -60.60361494148999384, -7.624776006180999488 ) ) ;
#10858=EDGE_CURVE ( 'NONE', #55619, #18438, #32135, .T. ) ;
#10859=CIRCLE ( 'NONE', #11768, 1.250000000000000444 ) ;
#10862=EDGE_CURVE ( 'NONE', #16112, #52194, #43457, .T. ) ;
#10863=CARTESIAN_POINT ( 'NONE',  ( 3.250000000000000000, -2.250000000000000000, 0.000000000000000000 ) ) ;
#10865=CARTESIAN_POINT ( 'NONE',  ( -8.792818914773597783, -25.22696626442860790, -9.175540344814811178 ) ) ;
#10869=CARTESIAN_POINT ( 'NONE',  ( 10.40273743810999996, -75.96241156850999232, 6.396609211732999789 ) ) ;
#10870=VERTEX_POINT ( 'NONE', #29918 ) ;
#10876=CARTESIAN_POINT ( 'NONE',  ( 12.43421868114999995, -54.36340276600000010, -1.197355605038999959 ) ) ;
#10879=DIRECTION ( 'NONE',  ( 0.000000000000000000, -1.000000000000000000, 0.000000000000000000 ) ) ;
#10888=ORIENTED_EDGE ( 'NONE', *, *, #55553, .F. ) ;
#10891=CIRCLE ( 'NONE', #43876, 0.5000000000000001110 ) ;
#10892=CARTESIAN_POINT ( 'NONE',  ( 8.768124086712999699, -59.94999999967000548, -7.919595949288999570 ) ) ;
#10893=ORIENTED_EDGE ( 'NONE', *, *, #56086, .F. ) ;
#10900=CARTESIAN_POINT ( 'NONE',  ( 12.66235371494999917, -53.66260492101000068, 0.4957155363043999619 ) ) ;
#10903=CARTESIAN_POINT ( 'NONE',  ( -12.66315196848000113, -25.17802884708999756, 0.06065366946595000114 ) ) ;
#10905=ADVANCED_FACE ( 'NONE', ( #6923 ), #56235, .T. ) ;
#10909=PLANE ( 'NONE',  #26862 ) ;
#10913=CARTESIAN_POINT ( 'NONE',  ( -10.62397638184999948, -76.02480637415999354, -6.218250916117999516 ) ) ;
#10914=CARTESIAN_POINT ( 'NONE',  ( -0.5999999999999999778, -23.15000000000000213, 11.79999999999999893 ) ) ;
#10915=CARTESIAN_POINT ( 'NONE',  ( 9.523353692561999040, -61.61947015589999666, -8.220363114712000652 ) ) ;
#10916=CARTESIAN_POINT ( 'NONE',  ( 11.81418954875000082, -78.75427961895999829, 3.289986436736999753 ) ) ;
#10919=CARTESIAN_POINT ( 'NONE',  ( 3.134197176858777301, -2.830045019308922605, -0.8619150459417437293 ) ) ;
#10920=CARTESIAN_POINT ( 'NONE',  ( -11.51192706679896816, -78.07429133446665048, -3.621052222003904308 ) ) ;
#10921=FACE_OUTER_BOUND ( 'NONE', #48985, .T. ) ;
#10922=AXIS2_PLACEMENT_3D ( 'NONE', #38067, #11508, #56088 ) ;
#10924=DIRECTION ( 'NONE',  ( 1.000000000000000000, 0.000000000000000000, 0.000000000000000000 ) ) ;
#10926=DIRECTION ( 'NONE',  ( -2.273758747900730032E-11, -6.364523519691810633E-20, 1.000000000000000000 ) ) ;
#10927=DIRECTION ( 'NONE',  ( -2.678934596778999979E-11, 1.000000000000000000, 2.678911359553000079E-11 ) ) ;
#10929=CARTESIAN_POINT ( 'NONE',  ( -0.3056021915128999678, -2.413088905188999878, -3.858359142670999997 ) ) ;
#10932=CARTESIAN_POINT ( 'NONE',  ( -10.84377968468480979, -76.16840065501064316, 4.524662071590493717 ) ) ;
#10935=CARTESIAN_POINT ( 'NONE',  ( -7.686941364959000822, -21.75472017805000036, 10.48774103561000182 ) ) ;
#10936=ORIENTED_EDGE ( 'NONE', *, *, #36282, .F. ) ;
#10937=CARTESIAN_POINT ( 'NONE',  ( -12.22985280536000019, -76.55908522753409784, -1.402219185754999486 ) ) ;
#10938=CARTESIAN_POINT ( 'NONE',  ( 11.85356139282347954, -79.10427114674126869, -1.243530160672429163 ) ) ;
#10940=CARTESIAN_POINT ( 'NONE',  ( -0.8506806241676722058, -2.395833333333332149, 3.165411199172022627 ) ) ;
#10941=CARTESIAN_POINT ( 'NONE',  ( -7.636246406707999590, -60.56323123069000047, 10.30460653227000023 ) ) ;
#10942=EDGE_CURVE ( 'NONE', #19958, #15969, #12176, .T. ) ;
#10945=CARTESIAN_POINT ( 'NONE',  ( 10.00831378477999856, -18.62769332291999902, -7.646786280044999273 ) ) ;
#10946=CARTESIAN_POINT ( 'NONE',  ( 12.51072239526000196, -52.49705297114005020, 0.7871079366006996647 ) ) ;
#10948=DIRECTION ( 'NONE',  ( 1.000000000000000000, 0.000000000000000000, 0.000000000000000000 ) ) ;
#10951=CARTESIAN_POINT ( 'NONE',  ( 10.30793518295451960, -77.74603760418852971, 6.185760751847420913 ) ) ;
#10955=DIRECTION ( 'NONE',  ( 0.000000000000000000, 1.000000000000000000, 0.000000000000000000 ) ) ;
#10959=CARTESIAN_POINT ( 'NONE',  ( -12.60413652829999975, -55.49283065365000311, 1.799502287743000029 ) ) ;
#10961=CARTESIAN_POINT ( 'NONE',  ( 12.70299804973600466, -53.77411689947622619, -0.8844418155219602173 ) ) ;
#10962=ORIENTED_EDGE ( 'NONE', *, *, #54374, .F. ) ;
#10963=ORIENTED_EDGE ( 'NONE', *, *, #54936, .T. ) ;
#10966=VERTEX_POINT ( 'NONE', #56811 ) ;
#10967=CARTESIAN_POINT ( 'NONE',  ( 8.260145278149000347, -17.05964900975000020, 9.643338479001000607 ) ) ;
#10968=AXIS2_PLACEMENT_3D ( 'NONE', #36544, #5254, #17661 ) ;
#10970=CARTESIAN_POINT ( 'NONE',  ( -11.75000000000000000, -75.80000000000001137, -9.948686767780999254E-14 ) ) ;
#10971=AXIS2_PLACEMENT_3D ( 'NONE', #15070, #42246, #10075 ) ;
#10972=CARTESIAN_POINT ( 'NONE',  ( 9.726612558640999495, -78.63181324549999829, 7.133059342380000167 ) ) ;
#10973=AXIS2_PLACEMENT_3D ( 'NONE', #3656, #12794, #49416 ) ;
#10976=CARTESIAN_POINT ( 'NONE',  ( -12.00000000000000000, -23.15000000000000213, 0.5999999999999999778 ) ) ;
#10983=DIRECTION ( 'NONE',  ( 0.9903465037206092836, -0.1386138613861012392, 0.000000000000000000 ) ) ;
#10987=DIRECTION ( 'NONE',  ( -0.7071067811865475727, 0.000000000000000000, 0.7071067811865475727 ) ) ;
#10991=CARTESIAN_POINT ( 'NONE',  ( -7.342377162852876005, -60.03019609282243607, 8.190817883596773541 ) ) ;
#10998=CARTESIAN_POINT ( 'NONE',  ( -9.102137319215390932, -53.82814024814979348, 8.583672456483473212 ) ) ;
#11000=CARTESIAN_POINT ( 'NONE',  ( 0.3283580454435180429, -3.382392793792461383, -3.504945231587735410 ) ) ;
#11004=CARTESIAN_POINT ( 'NONE',  ( 2.061613410425999771, -55.59429985491999560, -12.83797036852999796 ) ) ;
#11006=CARTESIAN_POINT ( 'NONE',  ( 3.343750000583999960, -0.9062499994161000716, -3.925818329445000231E-08 ) ) ;
#11009=EDGE_LOOP ( 'NONE', ( #34006, #2112, #32056, #28151 ) ) ;
#11011=CARTESIAN_POINT ( 'NONE',  ( 1.761265949705000056, -60.50858218752999562, -12.57448205046000034 ) ) ;
#11012=DIRECTION ( 'NONE',  ( 0.000000000000000000, 0.7071067811866525998, -0.7071067811864425456 ) ) ;
#11016=CARTESIAN_POINT ( 'NONE',  ( 8.194866293440998817, -24.71043252651000088, -9.389192598794000588 ) ) ;
#11020=DIRECTION ( 'NONE',  ( -0.7071067811865475727, 0.000000000000000000, 0.7071067811865475727 ) ) ;
#11022=ORIENTED_EDGE ( 'NONE', *, *, #28354, .F. ) ;
#11027=CARTESIAN_POINT ( 'NONE',  ( 7.645391692591000599, -55.58469634128999814, -10.18949678826999872 ) ) ;
#11028=AXIS2_PLACEMENT_3D ( 'NONE', #51518, #46225, #41478 ) ;
#11031=CARTESIAN_POINT ( 'NONE',  ( 7.919595949288999570, -59.94999999969000015, 8.768124086712999699 ) ) ;
#11034=CARTESIAN_POINT ( 'NONE',  ( -7.954951288349001004, -55.54999999966999980, 9.722718241315000398 ) ) ;
#11037=CARTESIAN_POINT ( 'NONE',  ( -9.346058022005980348, -53.63471832377268100, 8.620905970535309493 ) ) ;
#11038=VERTEX_POINT ( 'NONE', #25792 ) ;
#11043=EDGE_LOOP ( 'NONE', ( #39927, #16626, #6127, #11751 ) ) ;
#11044=VERTEX_POINT ( 'NONE', #2790 ) ;
#11049=CARTESIAN_POINT ( 'NONE',  ( 1.930638663166000191, -18.77877936711000117, 12.72375916873000001 ) ) ;
#11050=CARTESIAN_POINT ( 'NONE',  ( -9.713030931734584428, -54.27705886621604492, -7.970419577022142654 ) ) ;
#11052=CARTESIAN_POINT ( 'NONE',  ( -7.634645133894798263, -60.27584427251471055, 10.10912661257252410 ) ) ;
#11053=EDGE_CURVE ( 'NONE', #34958, #26247, #57383, .T. ) ;
#11057=VERTEX_POINT ( 'NONE', #48532 ) ;
#11060=CIRCLE ( 'NONE', #25192, 13.86363636363999952 ) ;
#11061=DIRECTION ( 'NONE',  ( 0.000000000000000000, -1.000000000000000000, 0.000000000000000000 ) ) ;
#11063=FACE_OUTER_BOUND ( 'NONE', #8386, .T. ) ;
#11064=CARTESIAN_POINT ( 'NONE',  ( 1.750000000001000089, -22.75077028492999887, 12.60356226393999890 ) ) ;
#11071=CARTESIAN_POINT ( 'NONE',  ( -10.53559655342999868, -55.59430957992999822, 7.620036381585000740 ) ) ;
#11074=CARTESIAN_POINT ( 'NONE',  ( 2.062673488410000200, -18.67547726287999765, -12.82904109062999964 ) ) ;
#11076=CARTESIAN_POINT ( 'NONE',  ( 1.691611010928000036, -17.76917308770000048, -12.66722148969999928 ) ) ;
#11077=FACE_OUTER_BOUND ( 'NONE', #18584, .T. ) ;
#11081=CARTESIAN_POINT ( 'NONE',  ( -2.949966724422874886, -1.203753930650452109, 1.940841882792249118 ) ) ;
#11082=ORIENTED_EDGE ( 'NONE', *, *, #54019, .T. ) ;
#11083=CARTESIAN_POINT ( 'NONE',  ( 8.782705133632456196, -78.99166666666667425, -7.901937437512484230 ) ) ;
#11084=FACE_OUTER_BOUND ( 'NONE', #8535, .T. ) ;
#11085=FACE_OUTER_BOUND ( 'NONE', #37877, .T. ) ;
#11088=CARTESIAN_POINT ( 'NONE',  ( 11.82764905900999963, -77.23222945497001035, 5.426413045081000419 ) ) ;
#11092=CARTESIAN_POINT ( 'NONE',  ( 0.000000000000000000, 4.040000000000000036, 0.000000000000000000 ) ) ;
#11099=CARTESIAN_POINT ( 'NONE',  ( 7.850068286652203575, -54.48530314306970013, 9.837745659570314771 ) ) ;
#11105=EDGE_CURVE ( 'NONE', #26696, #6154, #38213, .T. ) ;
#11106=ORIENTED_EDGE ( 'NONE', *, *, #1459, .T. ) ;
#11108=CARTESIAN_POINT ( 'NONE',  ( 8.838834764832000701, -55.54999999966999980, 8.838834764832000701 ) ) ;
#11109=DIRECTION ( 'NONE',  ( 0.000000000000000000, 0.000000000000000000, -1.000000000000000000 ) ) ;
#11112=DIRECTION ( 'NONE',  ( 0.000000000000000000, 1.000000000000000000, 0.000000000000000000 ) ) ;
#11113=VERTEX_POINT ( 'NONE', #29347 ) ;
#11115=CIRCLE ( 'NONE', #4479, 0.5000000000000000000 ) ;
#11116=B_SPLINE_CURVE_WITH_KNOTS ( 'NONE', 3,
 ( #21395, #39979, #30819, #57992, #49741, #36142 ),
 .UNSPECIFIED., .F., .F.,
 ( 4, 2, 4 ),
 ( 0.000000000000000000, 0.5000000000000000000, 1.000000000000000000 ),
 .UNSPECIFIED. ) ;
#11117=CARTESIAN_POINT ( 'NONE',  ( -10.26699006316252749, -77.34166666666665435, -5.917523019358070790 ) ) ;
#11118=EDGE_CURVE ( 'NONE', #52418, #7381, #47392, .T. ) ;
#11122=CARTESIAN_POINT ( 'NONE',  ( -10.42531124908000173, -60.06485148440999922, -7.624341765471999821 ) ) ;
#11125=ORIENTED_EDGE ( 'NONE', *, *, #43215, .F. ) ;
#11126=CARTESIAN_POINT ( 'NONE',  ( 1.733997378023100833, -18.47616783230471071, 12.54437956612015981 ) ) ;
#11129=CARTESIAN_POINT ( 'NONE',  ( -12.50385602495247639, -17.21562718850158902, 0.8579628946858919303 ) ) ;
#11133=EDGE_CURVE ( 'NONE', #56405, #27707, #47985, .T. ) ;
#11136=EDGE_CURVE ( 'NONE', #3351, #56911, #53532, .T. ) ;
#11139=CARTESIAN_POINT ( 'NONE',  ( 8.595597484336256144, -76.50923340009842377, 8.012250707705186770 ) ) ;
#11143=CARTESIAN_POINT ( 'NONE',  ( -12.60354432329999952, -59.55100837068999908, -1.750000000001000089 ) ) ;
#11152=CARTESIAN_POINT ( 'NONE',  ( -10.31444895690999886, -61.10075144983999706, -7.758883253367000243 ) ) ;
#11155=CARTESIAN_POINT ( 'NONE',  ( 12.66316452095000145, -25.17866137669000182, -0.04044945982121000289 ) ) ;
#11156=ADVANCED_FACE ( 'NONE', ( #35803 ), #36697, .T. ) ;
#11158=CARTESIAN_POINT ( 'NONE',  ( -1.538085309883418406, -78.31279427438737173, -11.67755942590387797 ) ) ;
#11161=FACE_OUTER_BOUND ( 'NONE', #52999, .T. ) ;
#11162=EDGE_LOOP ( 'NONE', ( #7867, #9496, #47853 ) ) ;
#11164=DIRECTION ( 'NONE',  ( 0.000000000000000000, -1.000000000000000000, 0.000000000000000000 ) ) ;
#11168=CARTESIAN_POINT ( 'NONE',  ( 12.66761570926000147, -54.57632520071999949, -1.696752301450999978 ) ) ;
#11171=LINE ( 'NONE', #20305, #40666 ) ;
#11174=DIRECTION ( 'NONE',  ( 4.762495317921000031E-11, -1.000000000000000000, -4.762531464717999529E-11 ) ) ;
#11176=ORIENTED_EDGE ( 'NONE', *, *, #9161, .F. ) ;
#11178=CARTESIAN_POINT ( 'NONE',  ( 12.71798269388000158, -60.09778754156999980, 1.931086388578000079 ) ) ;
#11184=ORIENTED_EDGE ( 'NONE', *, *, #28599, .T. ) ;
#11185=AXIS2_PLACEMENT_3D ( 'NONE', #51219, #32879, #18459 ) ;
#11187=EDGE_CURVE ( 'NONE', #47194, #28878, #13073, .T. ) ;
#11190=VERTEX_POINT ( 'NONE', #39942 ) ;
#11191=CARTESIAN_POINT ( 'NONE',  ( -12.71536556657220451, -24.12544729046540581, -1.781281568994087072 ) ) ;
#11193=EDGE_CURVE ( 'NONE', #425, #47713, #905, .T. ) ;
#11195=CARTESIAN_POINT ( 'NONE',  ( -12.49837680049000177, -23.20957148803000081, -1.667051419334999895 ) ) ;
#11197=DIRECTION ( 'NONE',  ( 0.7071067811865475727, 0.000000000000000000, -0.7071067811865475727 ) ) ;
#11204=CARTESIAN_POINT ( 'NONE',  ( -6.282410744257000523, -75.86562114363999854, 10.58616248715999930 ) ) ;
#11206=DIRECTION ( 'NONE',  ( 0.000000000000000000, 1.000000000000000000, 0.000000000000000000 ) ) ;
#11207=CARTESIAN_POINT ( 'NONE',  ( -3.911342194028000208, -78.54716864382999120, -11.62327352135999980 ) ) ;
#11210=CARTESIAN_POINT ( 'NONE',  ( -11.56310788679330237, -77.52280291465159223, 4.163831652655801463 ) ) ;
#11212=ORIENTED_EDGE ( 'NONE', *, *, #23827, .F. ) ;
#11214=CARTESIAN_POINT ( 'NONE',  ( 9.396085398178630754, -77.99791666666665435, -7.220923959705230821 ) ) ;
#11215=CARTESIAN_POINT ( 'NONE',  ( 3.600000000000000089, -0.2000000000000000111, 0.000000000000000000 ) ) ;
#11216=CARTESIAN_POINT ( 'NONE',  ( -13.89999999999999858, -72.79999999999999716, 0.000000000000000000 ) ) ;
#11217=CARTESIAN_POINT ( 'NONE',  ( -0.4524135602540000356, -2.766177049815000011, 3.686430941907999692 ) ) ;
#11221=CARTESIAN_POINT ( 'NONE',  ( -5.657080530349652747, -76.11476686863957752, 10.31273069280180366 ) ) ;
#11222=PLANE ( 'NONE',  #36232 ) ;
#11225=VERTEX_POINT ( 'NONE', #40242 ) ;
#11226=CARTESIAN_POINT ( 'NONE',  ( 12.70451681027663859, -25.17641660208789389, 0.5206746370197306018 ) ) ;
#11229=CARTESIAN_POINT ( 'NONE',  ( -7.624757096145000190, -60.60351363786999457, 10.47516529250999895 ) ) ;
#11233=CARTESIAN_POINT ( 'NONE',  ( -1.480597980168999888E-14, -80.60000000000000853, 0.000000000000000000 ) ) ;
#11237=CYLINDRICAL_SURFACE ( 'NONE', #7857, 12.80000000000000071 ) ;
#11240=CARTESIAN_POINT ( 'NONE',  ( 0.000000000000000000, -18.84999999999999787, -12.00000000000000000 ) ) ;
#11243=CARTESIAN_POINT ( 'NONE',  ( 0.3664097462935664851, -53.82809982434488916, -12.50575740041013439 ) ) ;
#11244=CARTESIAN_POINT ( 'NONE',  ( 2.062670899148999926, -55.49360374314999689, -12.83044039271999992 ) ) ;
#11249=ORIENTED_EDGE ( 'NONE', *, *, #47769, .F. ) ;
#11250=ORIENTED_EDGE ( 'NONE', *, *, #38896, .T. ) ;
#11253=EDGE_CURVE ( 'NONE', #35254, #54663, #3648, .T. ) ;
#11255=CARTESIAN_POINT ( 'NONE',  ( 7.986982684666001475, -17.27364722735000058, 10.07612755993999976 ) ) ;
#11257=CARTESIAN_POINT ( 'NONE',  ( -1.779623408300066600, -54.66369130952792688, 12.71471627654026548 ) ) ;
#11258=CARTESIAN_POINT ( 'NONE',  ( 2.581611620594999934, -78.68929468166000163, 11.78230914923999961 ) ) ;
#11259=FACE_OUTER_BOUND ( 'NONE', #22332, .T. ) ;
#11261=FACE_OUTER_BOUND ( 'NONE', #18195, .T. ) ;
#11264=VERTEX_POINT ( 'NONE', #39658 ) ;
#11266=ORIENTED_EDGE ( 'NONE', *, *, #28555, .T. ) ;
#11271=UNCERTAINTY_MEASURE_WITH_UNIT (LENGTH_MEASURE( 1.000000000000000082E-05 ), #20137, 'distance_accuracy_value', 'NONE');
#11274=AXIS2_PLACEMENT_3D ( 'NONE', #37466, #28900, #1195 ) ;
#11275=PLANE ( 'NONE',  #52103 ) ;
#11277=CARTESIAN_POINT ( 'NONE',  ( -7.682331425195999763, -19.23513569609999863, 10.04115011120000034 ) ) ;
#11281=ORIENTED_EDGE ( 'NONE', *, *, #40043, .T. ) ;
#11283=DIRECTION ( 'NONE',  ( 0.7071067811865475727, 0.000000000000000000, -0.7071067811865475727 ) ) ;
#11286=CARTESIAN_POINT ( 'NONE',  ( -9.643342484277001248, -17.05965044154000054, 8.260141428683001052 ) ) ;
#11288=CARTESIAN_POINT ( 'NONE',  ( 0.6479767009551614665, -1.889685945776059972, -3.462595171283828321 ) ) ;
#11291=CARTESIAN_POINT ( 'NONE',  ( 1.801750019967000016, -55.40992573246000319, -12.59656967650999881 ) ) ;
#11296=ORIENTED_EDGE ( 'NONE', *, *, #44540, .T. ) ;
#11298=CARTESIAN_POINT ( 'NONE',  ( 2.061649843245999758, -60.00561307554999502, -12.83797346717000210 ) ) ;
#11299=CARTESIAN_POINT ( 'NONE',  ( -7.648026766733999615, -18.74999999413999774, -10.12290050089000104 ) ) ;
#11304=CARTESIAN_POINT ( 'NONE',  ( -12.50000000000000000, -54.11762331445000029, -1.005384021965999963 ) ) ;
#11305=CARTESIAN_POINT ( 'NONE',  ( 11.08108919492889655, -78.47635570878233580, 3.913470582576941137 ) ) ;
#11307=ORIENTED_EDGE ( 'NONE', *, *, #45794, .F. ) ;
#11308=EDGE_CURVE ( 'NONE', #38037, #17469, #43406, .T. ) ;
#11310=DIRECTION ( 'NONE',  ( 0.000000000000000000, 1.000000000000000000, 0.000000000000000000 ) ) ;
#11319=AXIS2_PLACEMENT_3D ( 'NONE', #44925, #57616, #49654 ) ;
#11322=CARTESIAN_POINT ( 'NONE',  ( 2.062670899148999926, -23.30639625649999758, 12.83044039274999903 ) ) ;
#11323=B_SPLINE_CURVE_WITH_KNOTS ( 'NONE', 3,
 ( #25800, #8086, #26084, #52964, #48265, #4538, #43827, #21659, #39952, #23413, #32249, #37273, #28409, #10140, #28116, #46456, #46166, #13966 ),
 .UNSPECIFIED., .F., .F.,
 ( 4, 2, 2, 2, 2, 2, 2, 2, 4 ),
 ( 0.000000000000000000, 0.1250000000000000000, 0.2500000000000000000, 0.3750000000000000000, 0.5000000000000000000, 0.6250000000000000000, 0.7500000000000000000, 0.8750000000000000000, 1.000000000000000000 ),
 .UNSPECIFIED. ) ;
#11324=CARTESIAN_POINT ( 'NONE',  ( -12.61112459819999998, -23.21565178569999688, 1.798929298655999931 ) ) ;
#11326=ORIENTED_EDGE ( 'NONE', *, *, #22856, .T. ) ;
#11327=CARTESIAN_POINT ( 'NONE',  ( -12.78015286808999917, -54.49674784847999831, -1.806262579044999983 ) ) ;
#11329=ORIENTED_EDGE ( 'NONE', *, *, #57711, .F. ) ;
#11331=ORIENTED_EDGE ( 'NONE', *, *, #22017, .F. ) ;
#11332=CARTESIAN_POINT ( 'NONE',  ( 0.006333666751159999601, -16.66737355700000123, 12.77652491955999992 ) ) ;
#11335=CARTESIAN_POINT ( 'NONE',  ( 7.601397897754999633, -55.54999999966999980, -9.369164850722000892 ) ) ;
#11342=ORIENTED_EDGE ( 'NONE', *, *, #44045, .T. ) ;
#11346=CARTESIAN_POINT ( 'NONE',  ( -12.66232158689999920, -61.93482640547999551, -0.5080765942054000783 ) ) ;
#11348=CARTESIAN_POINT ( 'NONE',  ( 7.613962745608000127, -23.30639784948999704, 10.53101990620000095 ) ) ;
#11349=DIRECTION ( 'NONE',  ( -0.9936845293270585300, -0.1122098755727947705, 0.000000000000000000 ) ) ;
#11353=CARTESIAN_POINT ( 'NONE',  ( -12.05000000000000071, -79.29999999999999716, 0.000000000000000000 ) ) ;
#11358=CARTESIAN_POINT ( 'NONE',  ( -7.646966891758999907, -18.80358255734000039, -10.19019756605999838 ) ) ;
#11359=AXIS2_PLACEMENT_3D ( 'NONE', #31427, #26707, #36451 ) ;
#11364=ADVANCED_FACE ( 'NONE', ( #56701 ), #7965, .T. ) ;
#11365=CARTESIAN_POINT ( 'NONE',  ( -0.8510563811109643773, -1.205768424899396285, -3.162557679667391319 ) ) ;
#11368=CARTESIAN_POINT ( 'NONE',  ( 0.07079953276963653341, -0.8766290037971383731, -3.580880310080847728 ) ) ;
#11370=DIRECTION ( 'NONE',  ( 0.000000000000000000, -1.000000000000000000, 0.000000000000000000 ) ) ;
#11371=CARTESIAN_POINT ( 'NONE',  ( -2.062312494845999655, -55.57284340075000273, 12.83634740207000036 ) ) ;
#11375=DIRECTION ( 'NONE',  ( -1.000000000000000000, 0.000000000000000000, 0.000000000000000000 ) ) ;
#11376=CARTESIAN_POINT ( 'NONE',  ( -3.250000000000001332, -3.010416666666667407, -0.4254240051736181139 ) ) ;
#11383=CIRCLE ( 'NONE', #4791, 12.50000000000000000 ) ;
#11384=CARTESIAN_POINT ( 'NONE',  ( 9.758188809318015799, -76.40248920481857908, -6.544674992857547835 ) ) ;
#11387=CARTESIAN_POINT ( 'NONE',  ( 3.250000000000000444, -2.760416666666666963, 0.4254240051736248862 ) ) ;
#11389=CARTESIAN_POINT ( 'NONE',  ( 3.165411199172027512, -2.729166666666666963, -0.8506806241676553304 ) ) ;
#11391=DIRECTION ( 'NONE',  ( 0.000000000000000000, 1.000000000000000000, 0.000000000000000000 ) ) ;
#11392=DIRECTION ( 'NONE',  ( -0.7071067811865475727, 0.000000000000000000, -0.7071067811865475727 ) ) ;
#11400=CIRCLE ( 'NONE', #45369, 12.90000000000000036 ) ;
#11402=CARTESIAN_POINT ( 'NONE',  ( -1.538071403319991814, -77.41458333333332575, -11.75000000000000355 ) ) ;
#11407=ORIENTED_EDGE ( 'NONE', *, *, #11911, .F. ) ;
#11409=VERTEX_POINT ( 'NONE', #57269 ) ;
#11410=CARTESIAN_POINT ( 'NONE',  ( 7.919595949288999570, -55.64999999964999233, -9.050966799188000067 ) ) ;
#11420=VECTOR ( 'NONE', #1376, 1000.000000000000000 ) ;
#11424=CARTESIAN_POINT ( 'NONE',  ( -3.110324816758189836, -3.077988516191772828, 0.9426514480803485085 ) ) ;
#11430=CARTESIAN_POINT ( 'NONE',  ( -13.13047446164998711, -59.58578169018999660, -0.8260994316375004365 ) ) ;
#11432=FACE_OUTER_BOUND ( 'NONE', #812, .T. ) ;
#11433=CARTESIAN_POINT ( 'NONE',  ( -7.646092217304000904, -60.50851177880000620, -10.13691708059000085 ) ) ;
#11434=ADVANCED_FACE ( 'NONE', ( #37086 ), #53414, .T. ) ;
#11438=CARTESIAN_POINT ( 'NONE',  ( -12.83675912440999944, -18.77244614031999959, -2.062833085520999976 ) ) ;
#11439=CARTESIAN_POINT ( 'NONE',  ( 5.647598101448999763, -77.89127586458999986, 11.72364604052000203 ) ) ;
#11442=CARTESIAN_POINT ( 'NONE',  ( -0.7700304397887851593, -78.31794389177034077, -11.75310685588702064 ) ) ;
#11443=CARTESIAN_POINT ( 'NONE',  ( -14.00000000000000000, -32.88214388149999934, 0.000000000000000000 ) ) ;
#11444=CARTESIAN_POINT ( 'NONE',  ( 12.45128148039999871, -75.75224522809000405, 1.234877051265000025 ) ) ;
#11449=CARTESIAN_POINT ( 'NONE',  ( 12.48409101790999998, -60.16970703802000031, 1.669510252625000080 ) ) ;
#11450=CARTESIAN_POINT ( 'NONE',  ( 10.72212007569999948, -79.38422702059999381, -4.932905528729000011 ) ) ;
#11451=CARTESIAN_POINT ( 'NONE',  ( 12.77302454164000167, -54.07764858523999862, -1.481891240072999993 ) ) ;
#11454=DIRECTION ( 'NONE',  ( 0.000000000000000000, 1.000000000000000000, 0.000000000000000000 ) ) ;
#11456=ORIENTED_EDGE ( 'NONE', *, *, #190, .F. ) ;
#11461=ORIENTED_EDGE ( 'NONE', *, *, #19575, .T. ) ;
#11465=EDGE_CURVE ( 'NONE', #43629, #43983, #57428, .T. ) ;
#11469=CIRCLE ( 'NONE', #6735, 0.5000000000000006661 ) ;
#11472=ORIENTED_EDGE ( 'NONE', *, *, #52390, .T. ) ;
#11480=EDGE_LOOP ( 'NONE', ( #41927, #20880, #46655, #15639 ) ) ;
#11481=AXIS2_PLACEMENT_3D ( 'NONE', #5580, #9730, #37172 ) ;
#11482=CARTESIAN_POINT ( 'NONE',  ( -9.356096982537000173, -78.99405786821630215, 7.928589704419000128 ) ) ;
#11485=CARTESIAN_POINT ( 'NONE',  ( 9.213130513665999999, -53.79475660653999824, 8.533779407502999348 ) ) ;
#11486=CARTESIAN_POINT ( 'NONE',  ( 10.10712711932128549, -17.53345760874380588, -7.860996423953121592 ) ) ;
#11488=CARTESIAN_POINT ( 'NONE',  ( -11.67560174948319052, -77.20966691730704667, -1.536251511391871771 ) ) ;
#11492=CARTESIAN_POINT ( 'NONE',  ( -7.631896413330000684, -23.22122715205999555, 10.36221694966999962 ) ) ;
#11495=CYLINDRICAL_SURFACE ( 'NONE', #34158, 1.750000000000001332 ) ;
#11496=CARTESIAN_POINT ( 'NONE',  ( 10.42531125068999920, -23.26485145404000221, -7.624341767093000044 ) ) ;
#11497=LINE ( 'NONE', #30332, #26272 ) ;
#11498=DIRECTION ( 'NONE',  ( 0.000000000000000000, 0.000000000000000000, -1.000000000000000000 ) ) ;
#11499=CARTESIAN_POINT ( 'NONE',  ( -8.501675986534307228, -77.48722301659734057, 8.566518206373759270 ) ) ;
#11504=CARTESIAN_POINT ( 'NONE',  ( 2.061613410425999771, -23.20570014476000154, 12.83797036855999885 ) ) ;
#11505=DIRECTION ( 'NONE',  ( 0.000000000000000000, 0.000000000000000000, 1.000000000000000000 ) ) ;
#11506=CARTESIAN_POINT ( 'NONE',  ( -2.528906407072000206, -2.906459358523000081, 2.502418873083000150 ) ) ;
#11508=DIRECTION ( 'NONE',  ( -2.582622310454000054E-11, 0.000000000000000000, 1.000000000000000000 ) ) ;
#11509=CARTESIAN_POINT ( 'NONE',  ( -9.578632711364354790, -76.15034707418256232, 6.805328245342409765 ) ) ;
#11513=VERTEX_POINT ( 'NONE', #53885 ) ;
#11514=EDGE_CURVE ( 'NONE', #12818, #6738, #13121, .T. ) ;
#11517=CARTESIAN_POINT ( 'NONE',  ( 9.050966799188000067, -59.94999999967000548, -7.919595949288999570 ) ) ;
#11518=CARTESIAN_POINT ( 'NONE',  ( -7.646788277353000041, -60.17228598344999568, 10.00831419132999933 ) ) ;
#11524=ORIENTED_EDGE ( 'NONE', *, *, #55298, .T. ) ;
#11525=CIRCLE ( 'NONE', #34115, 0.5000000000000006661 ) ;
#11532=CARTESIAN_POINT ( 'NONE',  ( 1.247385798810000113, -54.32277743478999810, -12.50301438874000048 ) ) ;
#11533=DIRECTION ( 'NONE',  ( 0.7071067811865475727, 0.000000000000000000, 0.7071067811865475727 ) ) ;
#11534=AXIS2_PLACEMENT_3D ( 'NONE', #38230, #1655, #55958 ) ;
#11535=CARTESIAN_POINT ( 'NONE',  ( 1.980532758766000212, -19.23743349341999931, 12.80088938805999987 ) ) ;
#11536=LINE ( 'NONE', #30082, #51859 ) ;
#11538=ORIENTED_EDGE ( 'NONE', *, *, #37347, .F. ) ;
#11539=EDGE_LOOP ( 'NONE', ( #5316, #28565, #50787, #19435 ) ) ;
#11540=B_SPLINE_CURVE_WITH_KNOTS ( 'NONE', 3,
 ( #21710, #40893, #49167, #484, #40308, #57723 ),
 .UNSPECIFIED., .F., .F.,
 ( 4, 1, 1, 4 ),
 ( 0.000000000000000000, 0.3333333333333000081, 0.6666666666667000474, 1.000000000000000000 ),
 .UNSPECIFIED. ) ;
#11543=EDGE_LOOP ( 'NONE', ( #53831, #28729, #34018, #45007 ) ) ;
#11545=CARTESIAN_POINT ( 'NONE',  ( 7.633088938756000807, -18.60992532424000245, 10.18115029113000070 ) ) ;
#11547=CARTESIAN_POINT ( 'NONE',  ( -1.980584515756000030, -55.53514849873000259, 12.76303204337999908 ) ) ;
#11548=CARTESIAN_POINT ( 'NONE',  ( -10.46686097783000058, -77.11974203406001038, 7.365735401690999495 ) ) ;
#11551=CARTESIAN_POINT ( 'NONE',  ( -8.768124086712999699, -55.64999999965999677, -7.919595949288999570 ) ) ;
#11553=ORIENTED_EDGE ( 'NONE', *, *, #53021, .T. ) ;
#11557=CARTESIAN_POINT ( 'NONE',  ( 12.54238283049872393, -60.32853599783607024, -1.749799162368461891 ) ) ;
#11559=CIRCLE ( 'NONE', #1203, 1.750000000000000000 ) ;
#11562=DIRECTION ( 'NONE',  ( -0.7071067811865475727, 0.000000000000000000, 0.7071067811865475727 ) ) ;
#11565=CARTESIAN_POINT ( 'NONE',  ( 0.000000000000000000, -51.86282895648000135, 0.000000000000000000 ) ) ;
#11567=CARTESIAN_POINT ( 'NONE',  ( -12.85140862679999962, -57.04439829966000275, 1.980464483675000054 ) ) ;
#11568=DIRECTION ( 'NONE',  ( -0.9999999930530777403, 0.000000000000000000, -0.0001178721535689973885 ) ) ;
#11573=DIRECTION ( 'NONE',  ( 0.7071067811704841999, -1.939412262328955489E-07, -0.7071067812025843002 ) ) ;
#11575=CARTESIAN_POINT ( 'NONE',  ( -9.830798712624998714, -17.90910918523000106, 7.765013391413999599 ) ) ;
#11576=AXIS2_PLACEMENT_3D ( 'NONE', #53397, #57538, #21525 ) ;
#11578=CARTESIAN_POINT ( 'NONE',  ( 3.487123655132066347, -1.989199735643871092, -0.4781024640137967463 ) ) ;
#11583=DIRECTION ( 'NONE',  ( -0.7071067811864980568, -0.7071067811865969777, 1.459343291646993799E-08 ) ) ;
#11584=DIRECTION ( 'NONE',  ( 0.7071067811865474617, 0.000000000000000000, -0.7071067811865474617 ) ) ;
#11586=VERTEX_POINT ( 'NONE', #48014 ) ;
#11587=AXIS2_PLACEMENT_3D ( 'NONE', #42512, #56379, #11793 ) ;
#11590=CARTESIAN_POINT ( 'NONE',  ( 11.75000000000000000, -76.95000000000000284, 0.000000000000000000 ) ) ;
#11592=ADVANCED_FACE ( 'NONE', ( #26126, #44146, #39993, #34969 ), #39703, .F. ) ;
#11595=CYLINDRICAL_SURFACE ( 'NONE', #26234, 1.750000000000000000 ) ;
#11599=CARTESIAN_POINT ( 'NONE',  ( -7.624341764943999955, -60.06485149430999826, 10.42531124854999902 ) ) ;
#11603=ADVANCED_FACE ( 'NONE', ( #44728 ), #48956, .F. ) ;
#11606=DIRECTION ( 'NONE',  ( 0.000000000000000000, 0.000000000000000000, -1.000000000000000000 ) ) ;
#11607=CARTESIAN_POINT ( 'NONE',  ( -9.050966799188000067, -55.64999999964999233, -7.919595949288999570 ) ) ;
#11608=VECTOR ( 'NONE', #10927, 1000.000000000000000 ) ;
#11613=CARTESIAN_POINT ( 'NONE',  ( 1.931086388578000079, -18.70221245812999911, 12.71798269385000069 ) ) ;
#11614=CARTESIAN_POINT ( 'NONE',  ( 8.414570695956999913, -55.64999999967000122, -8.414570695956999913 ) ) ;
#11616=ORIENTED_EDGE ( 'NONE', *, *, #24294, .T. ) ;
#11617=CARTESIAN_POINT ( 'NONE',  ( -12.48375942314000042, -55.42730665069999674, -1.669542353228000042 ) ) ;
#11618=VERTEX_POINT ( 'NONE', #39127 ) ;
#11619=ORIENTED_EDGE ( 'NONE', *, *, #43573, .T. ) ;
#11620=CARTESIAN_POINT ( 'NONE',  ( 10.01676216527999941, -23.20941515021999635, 7.658899892521000119 ) ) ;
#11621=TOROIDAL_SURFACE ( 'NONE', #10657, 1.250000000000000000, 0.5000000000000000000 ) ;
#11624=CARTESIAN_POINT ( 'NONE',  ( -12.99510751537000353, -63.10294702886003648, -6.911973076623003642 ) ) ;
#11626=CIRCLE ( 'NONE', #21046, 1.250000000000000000 ) ;
#11630=ORIENTED_EDGE ( 'NONE', *, *, #39977, .F. ) ;
#11631=ORIENTED_EDGE ( 'NONE', *, *, #56709, .F. ) ;
#11633=CARTESIAN_POINT ( 'NONE',  ( -12.70228545255361752, -24.82820680358864252, 1.205254117556738169 ) ) ;
#11634=EDGE_CURVE ( 'NONE', #55458, #36570, #8708, .T. ) ;
#11637=CARTESIAN_POINT ( 'NONE',  ( 7.655542440070999710, -22.77819125662999866, 10.38645071867999903 ) ) ;
#11638=CARTESIAN_POINT ( 'NONE',  ( 7.770369683913386893, -61.03583903303879765, 10.20674856006229980 ) ) ;
#11640=CARTESIAN_POINT ( 'NONE',  ( -8.838834764832000701, -60.04999999966999980, 8.838834764832000701 ) ) ;
#11644=CIRCLE ( 'NONE', #42402, 11.19999999999999929 ) ;
#11647=CARTESIAN_POINT ( 'NONE',  ( 1.931087888240000217, -23.31584731985000047, -12.71658872084999992 ) ) ;
#11652=CARTESIAN_POINT ( 'NONE',  ( 12.85144117169000033, -20.24527983099999773, 1.980464439859999981 ) ) ;
#11654=CARTESIAN_POINT ( 'NONE',  ( 1.657628819186623526, -1.087677343702487587, 3.213874994219929171 ) ) ;
#11656=CARTESIAN_POINT ( 'NONE',  ( -2.599125635968795311, -1.549700445914265368, 1.994837577964314601 ) ) ;
#11657=VECTOR ( 'NONE', #29249, 1000.000000000000000 ) ;
#11658=DIRECTION ( 'NONE',  ( 1.000000000000000000, 0.000000000000000000, 0.000000000000000000 ) ) ;
#11660=EDGE_CURVE ( 'NONE', #11586, #49814, #56515, .T. ) ;
#11663=FACE_OUTER_BOUND ( 'NONE', #1876, .T. ) ;
#11664=CARTESIAN_POINT ( 'NONE',  ( 2.839805762151339952, -3.208333333333332149, -1.636761686205418176 ) ) ;
#11666=CARTESIAN_POINT ( 'NONE',  ( 9.722718241315000398, -18.75000000000000000, -7.247844507162001015 ) ) ;
#11670=ADVANCED_FACE ( 'NONE', ( #12550 ), #5584, .T. ) ;
#11673=DIRECTION ( 'NONE',  ( 0.000000000000000000, 1.000000000000000000, 0.000000000000000000 ) ) ;
#11674=EDGE_CURVE ( 'NONE', #13177, #56405, #15549, .T. ) ;
#11685=CARTESIAN_POINT ( 'NONE',  ( 12.50659830422946683, -17.02653389314800947, 0.3508388550761127322 ) ) ;
#11686=ORIENTED_EDGE ( 'NONE', *, *, #7745, .T. ) ;
#11687=EDGE_LOOP ( 'NONE', ( #2353, #9119, #45671, #48474, #24208, #16971 ) ) ;
#11688=CARTESIAN_POINT ( 'NONE',  ( 3.500000000000000000, -3.500000000000000000, 1.049058100190999900E-13 ) ) ;
#11689=EDGE_CURVE ( 'NONE', #45142, #20811, #24016, .T. ) ;
#11691=AXIS2_PLACEMENT_3D ( 'NONE', #39900, #13619, #30744 ) ;
#11696=EDGE_LOOP ( 'NONE', ( #9135, #10962, #34295, #21801 ) ) ;
#11698=ORIENTED_EDGE ( 'NONE', *, *, #9568, .F. ) ;
#11703=AXIS2_PLACEMENT_3D ( 'NONE', #37329, #10190, #15188 ) ;
#11707=CARTESIAN_POINT ( 'NONE',  ( -7.342331066867000544, -55.64999999967000122, 8.190859204290999784 ) ) ;
#11718=DIRECTION ( 'NONE',  ( -1.000000000000000000, 0.000000000000000000, 0.000000000000000000 ) ) ;
#11720=LINE ( 'NONE', #29696, #45915 ) ;
#11721=CARTESIAN_POINT ( 'NONE',  ( 10.18589234708000113, -23.28917565320000094, 7.641012386039999882 ) ) ;
#11722=CARTESIAN_POINT ( 'NONE',  ( -7.634438871678000282, -60.54781730666999806, -10.30764054783999839 ) ) ;
#11727=CARTESIAN_POINT ( 'NONE',  ( 6.891227191158999510, -76.69101173772000379, -9.824000600561999974 ) ) ;
#11728=CARTESIAN_POINT ( 'NONE',  ( 10.12290050124000018, -23.24999999991999644, 7.648026767085999822 ) ) ;
#11729=DIRECTION ( 'NONE',  ( 0.009503199022040095811, 0.000000000000000000, -0.9999548435846228323 ) ) ;
#11730=CARTESIAN_POINT ( 'NONE',  ( -5.241082234444999877, -75.58422357026000782, -11.04946354059000058 ) ) ;
#11731=VERTEX_POINT ( 'NONE', #54467 ) ;
#11732=AXIS2_PLACEMENT_3D ( 'NONE', #37654, #42093, #1663 ) ;
#11733=CARTESIAN_POINT ( 'NONE',  ( 9.621742410812267110, -54.17938299883542896, -8.060146970871130634 ) ) ;
#11734=CARTESIAN_POINT ( 'NONE',  ( 12.66761950495000022, -61.02355206165999846, 1.696827901577000031 ) ) ;
#11735=CARTESIAN_POINT ( 'NONE',  ( 5.973326116064999525, -79.42032643418001214, -10.95954443647000076 ) ) ;
#11736=CARTESIAN_POINT ( 'NONE',  ( 12.49837451343999994, -55.59042109264999709, -1.667049596277000001 ) ) ;
#11741=DIRECTION ( 'NONE',  ( 0.000000000000000000, 1.000000000000000000, 0.000000000000000000 ) ) ;
#11745=VERTEX_POINT ( 'NONE', #22579 ) ;
#11749=ORIENTED_EDGE ( 'NONE', *, *, #44691, .F. ) ;
#11750=EDGE_LOOP ( 'NONE', ( #46632, #10159, #41888, #4562 ) ) ;
#11751=ORIENTED_EDGE ( 'NONE', *, *, #50035, .F. ) ;
#11752=EDGE_CURVE ( 'NONE', #50911, #22487, #31735, .T. ) ;
#11757=CIRCLE ( 'NONE', #23077, 1.750000000000001332 ) ;
#11758=ORIENTED_EDGE ( 'NONE', *, *, #49558, .T. ) ;
#11759=CARTESIAN_POINT ( 'NONE',  ( -12.70249480706781497, -24.96498603299993846, -0.9989402950542592974 ) ) ;
#11763=CARTESIAN_POINT ( 'NONE',  ( 10.08162962779999994, -54.08146287347000225, 7.981572332307999673 ) ) ;
#11768=AXIS2_PLACEMENT_3D ( 'NONE', #10742, #50893, #5138 ) ;
#11769=CARTESIAN_POINT ( 'NONE',  ( -12.70556836347999941, -16.77227722772000007, 1.774192816106000118E-09 ) ) ;
#11770=DIRECTION ( 'NONE',  ( -0.7071067811865475727, 0.000000000000000000, 0.7071067811865475727 ) ) ;
#11773=CARTESIAN_POINT ( 'NONE',  ( -9.662446363796000526, -76.39482503998999618, 7.627099640079999965 ) ) ;
#11776=DIRECTION ( 'NONE',  ( -1.000000000000000000, 0.000000000000000000, 0.000000000000000000 ) ) ;
#11777=CARTESIAN_POINT ( 'NONE',  ( -9.356096982537000173, -78.92672392741998522, 7.928589704419000128 ) ) ;
#11780=CARTESIAN_POINT ( 'NONE',  ( 12.56594317823000040, -23.25000001387000026, -1.750000000000000000 ) ) ;
#11781=LINE ( 'NONE', #7915, #21078 ) ;
#11784=CARTESIAN_POINT ( 'NONE',  ( -8.500000000000000000, -3.500000000000000000, 0.000000000000000000 ) ) ;
#11787=CARTESIAN_POINT ( 'NONE',  ( -3.382079042057999807, -1.966566916551000022, 0.09601839907216000447 ) ) ;
#11793=DIRECTION ( 'NONE',  ( 1.000000000000000000, 0.000000000000000000, 0.000000000000000000 ) ) ;
#11794=ORIENTED_EDGE ( 'NONE', *, *, #8705, .F. ) ;
#11800=CARTESIAN_POINT ( 'NONE',  ( 0.000000000000000000, -23.25000000000000000, 12.50000000000000000 ) ) ;
#11806=VERTEX_POINT ( 'NONE', #41166 ) ;
#11809=CARTESIAN_POINT ( 'NONE',  ( 9.546819346421999697, -24.68527546640000025, -8.130850183241999929 ) ) ;
#11810=AXIS2_PLACEMENT_3D ( 'NONE', #23624, #37487, #15643 ) ;
#11824=EDGE_LOOP ( 'NONE', ( #22276, #35072, #46194, #20974 ) ) ;
#11825=CARTESIAN_POINT ( 'NONE',  ( 7.948094694409999050, -17.55965255610999876, 9.636752590488001147 ) ) ;
#11827=CARTESIAN_POINT ( 'NONE',  ( 11.44417895085271475, -76.02916666666666856, -3.075537641221520069 ) ) ;
#11828=CARTESIAN_POINT ( 'NONE',  ( 7.289493654314999738, -77.34176059790999602, -10.52009694070999934 ) ) ;
#11829=DIRECTION ( 'NONE',  ( -0.7071067811865475727, 0.000000000000000000, 0.7071067811865475727 ) ) ;
#11830=CYLINDRICAL_SURFACE ( 'NONE', #30572, 11.75000000000000000 ) ;
#11834=VECTOR ( 'NONE', #48955, 1000.000000000000000 ) ;
#11836=ORIENTED_EDGE ( 'NONE', *, *, #21054, .F. ) ;
#11838=ORIENTED_EDGE ( 'NONE', *, *, #55187, .F. ) ;
#11844=FACE_OUTER_BOUND ( 'NONE', #10307, .T. ) ;
#11848=LINE ( 'NONE', #38118, #2173 ) ;
#11851=DIRECTION ( 'NONE',  ( 0.000000000000000000, 0.000000000000000000, 1.000000000000000000 ) ) ;
#11852=CARTESIAN_POINT ( 'NONE',  ( -7.624341764943999955, -60.06485149430999826, 10.42531124854999902 ) ) ;
#11854=FACE_OUTER_BOUND ( 'NONE', #7175, .T. ) ;
#11861=CARTESIAN_POINT ( 'NONE',  ( -9.369164850722000892, -55.54999999966999980, -7.601397897754999633 ) ) ;
#11863=CARTESIAN_POINT ( 'NONE',  ( 10.07627163191000008, -23.24999999688999708, -7.601397897754999633 ) ) ;
#11865=CARTESIAN_POINT ( 'NONE',  ( 1.898611045869317726, -2.079666817341920382, 2.965229623691935767 ) ) ;
#11868=DIRECTION ( 'NONE',  ( 0.7071067811865475727, 0.000000000000000000, -0.7071067811865475727 ) ) ;
#11873=CARTESIAN_POINT ( 'NONE',  ( 10.99609774599710654, -18.31447404871020268, -0.3135602106693130553 ) ) ;
#11879=CARTESIAN_POINT ( 'NONE',  ( -0.9935076046995571231, -17.03183812246616213, 12.70250268217020917 ) ) ;
#11880=EDGE_CURVE ( 'NONE', #43451, #17562, #47369, .T. ) ;
#11882=CARTESIAN_POINT ( 'NONE',  ( 11.73235549862695670, -78.45166484604632728, 0.7720932834806667477 ) ) ;
#11883=CARTESIAN_POINT ( 'NONE',  ( -10.27340958486083089, -60.86161210392388909, 7.712164009451874414 ) ) ;
#11888=AXIS2_PLACEMENT_3D ( 'NONE', #45420, #37119, #14677 ) ;
#11890=CARTESIAN_POINT ( 'NONE',  ( -12.60413652834999887, -60.10716934574000447, -1.799502287743000029 ) ) ;
#11891=LINE ( 'NONE', #16604, #34491 ) ;
#11895=CIRCLE ( 'NONE', #43946, 3.600000000000000089 ) ;
#11896=CARTESIAN_POINT ( 'NONE',  ( 1.931087888240000217, -18.68415268018999953, 12.71658872085999903 ) ) ;
#11897=CARTESIAN_POINT ( 'NONE',  ( -12.77297283014999962, -24.72822696531000020, 1.476112654659999857 ) ) ;
#11898=ORIENTED_EDGE ( 'NONE', *, *, #48016, .F. ) ;
#11899=ORIENTED_EDGE ( 'NONE', *, *, #10634, .T. ) ;
#11900=DIRECTION ( 'NONE',  ( 0.000000000000000000, 1.000000000000000000, 0.000000000000000000 ) ) ;
#11901=VERTEX_POINT ( 'NONE', #55923 ) ;
#11902=ORIENTED_EDGE ( 'NONE', *, *, #20588, .F. ) ;
#11910=ORIENTED_EDGE ( 'NONE', *, *, #43490, .F. ) ;
#11911=EDGE_CURVE ( 'NONE', #37664, #45201, #5565, .T. ) ;
#11912=EDGE_LOOP ( 'NONE', ( #26826, #37311, #37009 ) ) ;
#11914=CARTESIAN_POINT ( 'NONE',  ( -1.821913034590999979E-14, -80.69999999923000189, 0.000000000000000000 ) ) ;
#11915=FACE_OUTER_BOUND ( 'NONE', #56043, .T. ) ;
#11917=CARTESIAN_POINT ( 'NONE',  ( 7.626500777234999973, -23.31584731985000047, 10.35747145892000098 ) ) ;
#11918=CYLINDRICAL_SURFACE ( 'NONE', #20037, 11.75000000000000000 ) ;
#11919=CARTESIAN_POINT ( 'NONE',  ( 0.5999999999999999778, -18.84999999999999787, 10.98362417419999915 ) ) ;
#11921=CARTESIAN_POINT ( 'NONE',  ( -12.00000000000000000, -23.25000000000000000, 0.000000000000000000 ) ) ;
#11924=B_SPLINE_CURVE_WITH_KNOTS ( 'NONE', 3,
 ( #47053, #6582, #50305, #46766, #10148, #37285 ),
 .UNSPECIFIED., .F., .F.,
 ( 4, 2, 4 ),
 ( 0.000000000000000000, 0.5000000000000000000, 1.000000000000000000 ),
 .UNSPECIFIED. ) ;
#11926=CARTESIAN_POINT ( 'NONE',  ( -7.618386520025000053, -55.57287536619999457, 10.53495200518000097 ) ) ;
#11929=CARTESIAN_POINT ( 'NONE',  ( -12.71106812367899330, -61.05135172933366761, 1.717582538852624907 ) ) ;
#11930=CIRCLE ( 'NONE', #47768, 12.90000000000000036 ) ;
#11932=CARTESIAN_POINT ( 'NONE',  ( -1.801614160558000055, -18.61347738095000182, -12.59687422887999908 ) ) ;
#11936=CARTESIAN_POINT ( 'NONE',  ( -0.7994329013177036147, -3.500000000000000444, 3.166868224362918927 ) ) ;
#11939=ORIENTED_EDGE ( 'NONE', *, *, #37633, .T. ) ;
#11941=CARTESIAN_POINT ( 'NONE',  ( 11.79999999999999893, -18.84999999999999787, 0.000000000000000000 ) ) ;
#11942=CARTESIAN_POINT ( 'NONE',  ( -12.50745077490000057, -24.99994448286999926, -2.662114616045000020E-09 ) ) ;
#11945=CARTESIAN_POINT ( 'NONE',  ( -3.316243310697999824, -2.097363918999999743, 1.514716574117999981 ) ) ;
#11947=CARTESIAN_POINT ( 'NONE',  ( -12.54901566175999861, -53.79264670667999582, 0.4731578885121000555 ) ) ;
#11949=DIRECTION ( 'NONE',  ( 0.7071067811865475727, 0.000000000000000000, 0.7071067811865475727 ) ) ;
#11950=LINE ( 'NONE', #7516, #46177 ) ;
#11953=CARTESIAN_POINT ( 'NONE',  ( -0.07779856576520610689, -76.32427321278245813, -11.74963840653824576 ) ) ;
#11956=CARTESIAN_POINT ( 'NONE',  ( 7.710095619821999868, -21.75064714351000106, 10.18496935396999881 ) ) ;
#11959=B_SPLINE_CURVE_WITH_KNOTS ( 'NONE', 3,
 ( #8901, #44918, #48770, #8314, #82, #19510, #1518, #14773, #18931, #32772 ),
 .UNSPECIFIED., .F., .F.,
 ( 4, 2, 2, 2, 4 ),
 ( 0.000000000000000000, 0.5000000000000091038, 0.6250000000000093259, 0.7500000000000096589, 1.000000000000000000 ),
 .UNSPECIFIED. ) ;
#11960=CARTESIAN_POINT ( 'NONE',  ( 2.839805762151339952, -2.708333333333331705, -1.636761686205418176 ) ) ;
#11965=B_SPLINE_CURVE_WITH_KNOTS ( 'NONE', 3,
 ( #54931, #21946, #26956, #35518, #44987, #4542, #23350, #13380, #40255, #21664, #53846, #3381, #35818, #14483, #30516, #41361, #943, #8374, #44692, #22244, #53546, #16955, #43833, #58267, #39958, #44112, #32474, #50519, #21374, #17232, #34936, #3662, #17831, #52969, #39669, #57676, #35221, #13085, #31082, #53250, #12801, #30800, #44391, #49119, #3943, #57971, #8670, #26658, #51108, #37210, #24513, #46689, #41650, #24223, #20096, #32767, #33361, #1514, #46101, #42240, #1807, #42529, #14769, #37796, #19503, #19802, #6504, #38084, #55817, #2098, #55519, #41942, #55222, #56108, #10357, #28054, #15369, #15066, #10951, #51395, #5625, #37498, #33061, #23636, #28932, #46976, #1227, #19218, #50814, #28340, #46392, #5917, #23924, #10661, #28639, #6209, #5237, #50710, #40962, #37101, #27067, #54545, #23528, #41540, #9963, #50413, #18819, #259, #32371, #39568, #14371, #55118, #49534, #27944, #1122, #27367, #23242, #41249, #32084, #54830, #57569, #837, #18531, #22659, #45992, #5519, #21560, #54255, #19110 ),
 .UNSPECIFIED., .F., .F.,
 ( 4, 2, 2, 2, 2, 2, 1, 2, 2, 2, 2, 2, 2, 2, 2, 2, 2, 1, 2, 2, 1, 1, 2, 2, 1, 2, 2, 1, 2, 2, 2, 2, 2, 2, 2, 1, 2, 2, 2, 2, 2, 2, 2, 1, 2, 2, 1, 2, 2, 1, 1, 2, 2, 1, 2, 2, 2, 2, 2, 2, 2, 2, 2, 2, 1, 2, 2, 2, 2, 2, 4 ),
 ( 0.000000000000000000, 0.01562499999999993755, 0.03124999999999987510, 0.04687499999999981265, 0.06249999999999975020, 0.07812499999999969469, 0.09374999999999963918, 0.1093749999999995837, 0.1249999999999995282, 0.1406249999999994726, 0.1562499999999993894, 0.1718749999999993339, 0.1874999999999992784, 0.2031249999999992228, 0.2187499999999991396, 0.2343749999999990841, 0.2421874999999990563, 0.2499999999999990563, 0.2656249999999990008, 0.2734374999999989453, 0.2812499999999989453, 0.2968749999999989453, 0.3046874999999988898, 0.3124999999999988343, 0.3281249999999988343, 0.3359374999999988343, 0.3437499999999987788, 0.3593749999999987788, 0.3671874999999988343, 0.3749999999999988343, 0.3906249999999988343, 0.4062499999999988343, 0.4218749999999988343, 0.4374999999999987788, 0.4687499999999987788, 0.4999999999999987788, 0.5312499999999987788, 0.5624999999999987788, 0.5781249999999987788, 0.5937499999999988898, 0.6093749999999988898, 0.6249999999999988898, 0.6328124999999988898, 0.6406249999999988898, 0.6562499999999988898, 0.6640624999999988898, 0.6718749999999988898, 0.6874999999999988898, 0.6953124999999988898, 0.7031249999999988898, 0.7187499999999988898, 0.7265624999999990008, 0.7343749999999991118, 0.7499999999999991118, 0.7578124999999992228, 0.7656249999999992228, 0.7812499999999993339, 0.7968749999999993339, 0.8124999999999994449, 0.8281249999999994449, 0.8437499999999995559, 0.8593749999999995559, 0.8749999999999995559, 0.8906249999999996669, 0.9062499999999996669, 0.9218749999999997780, 0.9374999999999997780, 0.9531249999999998890, 0.9687499999999998890, 0.9843750000000000000, 1.000000000000000000 ),
 .UNSPECIFIED. ) ;
#11969=CARTESIAN_POINT ( 'NONE',  ( -11.00000000000000000, -23.75000000000000000, 0.000000000000000000 ) ) ;
#11970=ORIENTED_EDGE ( 'NONE', *, *, #32409, .T. ) ;
#11971=CARTESIAN_POINT ( 'NONE',  ( 12.50386430100449076, -17.21495444376988360, 0.8574445000318078325 ) ) ;
#11972=VERTEX_POINT ( 'NONE', #15473 ) ;
#11973=CIRCLE ( 'NONE', #15725, 11.19999999999999929 ) ;
#11981=CIRCLE ( 'NONE', #43121, 0.5000000000000006661 ) ;
#11983=ORIENTED_EDGE ( 'NONE', *, *, #57105, .T. ) ;
#11984=EDGE_CURVE ( 'NONE', #22563, #10870, #48034, .T. ) ;
#11987=AXIS2_PLACEMENT_3D ( 'NONE', #57683, #4254, #8979 ) ;
#11988=CARTESIAN_POINT ( 'NONE',  ( -12.50000000000000000, -60.04999999725999515, 1.750000000000000000 ) ) ;
#11993=CARTESIAN_POINT ( 'NONE',  ( -11.66766085128260677, -79.11458333336996418, 2.485230469016839194 ) ) ;
#11999=CARTESIAN_POINT ( 'NONE',  ( -2.304930700997001924, -3.038123778412107789, 2.290893979963799953 ) ) ;
#12004=CARTESIAN_POINT ( 'NONE',  ( -8.358306106603231811, -76.26144349183930160, -8.257935116388701147 ) ) ;
#12005=CARTESIAN_POINT ( 'NONE',  ( 12.00000000000000000, -55.54999999966999980, -1.250000000000000000 ) ) ;
#12006=CARTESIAN_POINT ( 'NONE',  ( -9.101516360845000264, -61.68066799025999813, -8.485522730771000610 ) ) ;
#12009=CARTESIAN_POINT ( 'NONE',  ( 12.50412681318975139, -54.28010473027887173, 1.235016000149061322 ) ) ;
#12010=CARTESIAN_POINT ( 'NONE',  ( 12.56884868898000107, -76.78118304535000505, -3.366471670097000324 ) ) ;
#12011=AXIS2_PLACEMENT_3D ( 'NONE', #12565, #17279, #35269 ) ;
#12013=CARTESIAN_POINT ( 'NONE',  ( 1.750000000001000089, -23.24999998674999802, -12.56594318051000059 ) ) ;
#12014=CARTESIAN_POINT ( 'NONE',  ( 11.57190666824999958, -76.81145138379000059, -2.972430358477000212 ) ) ;
#12016=DIRECTION ( 'NONE',  ( 0.000000000000000000, 0.8191944459061824002, -0.5735158758015881375 ) ) ;
#12018=CARTESIAN_POINT ( 'NONE',  ( 12.77657007944999989, -62.11210281297999813, 0.1589025507403999948 ) ) ;
#12019=CARTESIAN_POINT ( 'NONE',  ( 2.583815929080000018, -78.94027611781000076, 12.52952761449999919 ) ) ;
#12020=CARTESIAN_POINT ( 'NONE',  ( 12.82229880955999946, -55.37735182805000278, -2.065917129154000165 ) ) ;
#12022=AXIS2_PLACEMENT_3D ( 'NONE', #42957, #47112, #2511 ) ;
#12026=ORIENTED_EDGE ( 'NONE', *, *, #9639, .T. ) ;
#12029=CONICAL_SURFACE ( 'NONE', #43185, 12.84999999993999964, 0.7853981633972997312 ) ;
#12032=EDGE_CURVE ( 'NONE', #30887, #456, #38127, .T. ) ;
#12034=CARTESIAN_POINT ( 'NONE',  ( -10.12290050126000196, -60.04999999958999979, -7.648026767103999646 ) ) ;
#12036=ORIENTED_EDGE ( 'NONE', *, *, #21142, .T. ) ;
#12038=ORIENTED_EDGE ( 'NONE', *, *, #55014, .T. ) ;
#12041=CARTESIAN_POINT ( 'NONE',  ( -5.913030101731338917, -78.11524859537807686, 10.26283145188432044 ) ) ;
#12043=ORIENTED_EDGE ( 'NONE', *, *, #27695, .F. ) ;
#12044=ORIENTED_EDGE ( 'NONE', *, *, #21142, .F. ) ;
#12045=EDGE_CURVE ( 'NONE', #45320, #11731, #29121, .T. ) ;
#12048=CARTESIAN_POINT ( 'NONE',  ( 9.996785040876998707, -54.64937852858999889, 7.758588586516999008 ) ) ;
#12049=CYLINDRICAL_SURFACE ( 'NONE', #53431, 1.750000000000001332 ) ;
#12052=CARTESIAN_POINT ( 'NONE',  ( 12.70619440583160475, -61.26151788282474087, -1.571771935831642653 ) ) ;
#12054=ADVANCED_FACE ( 'NONE', ( #26047 ), #15943, .F. ) ;
#12056=CARTESIAN_POINT ( 'NONE',  ( 5.894077591580000330, -76.61273252672999945, -10.80721126921000064 ) ) ;
#12057=EDGE_CURVE ( 'NONE', #37150, #50613, #53648, .T. ) ;
#12061=CARTESIAN_POINT ( 'NONE',  ( 8.438902753042999194, -78.63339079806000598, -8.898539530003999332 ) ) ;
#12064=CARTESIAN_POINT ( 'NONE',  ( 12.50240681834000078, -24.68234730741999883, -1.005418943851999813 ) ) ;
#12065=DIRECTION ( 'NONE',  ( 0.000000000000000000, 1.000000000000000000, 0.000000000000000000 ) ) ;
#12069=LINE ( 'NONE', #43658, #7775 ) ;
#12070=CARTESIAN_POINT ( 'NONE',  ( -3.389826679555999700, -1.914953706142999978, -1.517104093797000175 ) ) ;
#12074=CARTESIAN_POINT ( 'NONE',  ( -11.74961884786346467, -76.19396137550481285, 0.7978361957832171836 ) ) ;
#12079=CARTESIAN_POINT ( 'NONE',  ( -10.01332844637000008, -18.71943307332999851, -7.654537085030999499 ) ) ;
#12083=CARTESIAN_POINT ( 'NONE',  ( -7.762981007074000850, -60.96089459184000248, 9.992000916374999875 ) ) ;
#12084=CARTESIAN_POINT ( 'NONE',  ( -1.626826133776999786E-14, -74.80000000000001137, 0.000000000000000000 ) ) ;
#12086=DIRECTION ( 'NONE',  ( 0.7071067811865475727, 0.000000000000000000, -0.7071067811865475727 ) ) ;
#12087=CARTESIAN_POINT ( 'NONE',  ( -12.71466563513548209, -54.66210710670594608, -1.778810201849397643 ) ) ;
#12088=ORIENTED_EDGE ( 'NONE', *, *, #10305, .F. ) ;
#12093=EDGE_CURVE ( 'NONE', #6883, #54081, #26289, .T. ) ;
#12094=CARTESIAN_POINT ( 'NONE',  ( -10.01235002625000092, -60.09848884406000025, -7.653559626114000203 ) ) ;
#12096=ORIENTED_EDGE ( 'NONE', *, *, #41105, .T. ) ;
#12099=CARTESIAN_POINT ( 'NONE',  ( 1.931086388455000025, -55.50221404479999876, -12.71798280852999952 ) ) ;
#12102=CARTESIAN_POINT ( 'NONE',  ( 12.70610308055456805, -54.34479009114169656, -1.580620443402273256 ) ) ;
#12110=DIRECTION ( 'NONE',  ( 0.000000000000000000, -1.000000000000000000, 0.000000000000000000 ) ) ;
#12111=CARTESIAN_POINT ( 'NONE',  ( 0.8898229089104329192, -53.77675468782315704, 12.70296869040592824 ) ) ;
#12112=CARTESIAN_POINT ( 'NONE',  ( -12.91020013338000005, -77.08816582529999550, -1.090565897604000023 ) ) ;
#12113=DIRECTION ( 'NONE',  ( 1.000000000000000000, 0.000000000000000000, 0.000000000000000000 ) ) ;
#12114=FACE_OUTER_BOUND ( 'NONE', #53515, .T. ) ;
#12118=ORIENTED_EDGE ( 'NONE', *, *, #4638, .T. ) ;
#12120=ORIENTED_EDGE ( 'NONE', *, *, #44213, .T. ) ;
#12126=CARTESIAN_POINT ( 'NONE',  ( -7.970414252720478210, -61.32292089011284730, -9.713036876910228656 ) ) ;
#12127=AXIS2_PLACEMENT_3D ( 'NONE', #41843, #24423, #46294 ) ;
#12129=CARTESIAN_POINT ( 'NONE',  ( 0.000000000000000000, -0.2000000000000000111, 0.000000000000000000 ) ) ;
#12131=CARTESIAN_POINT ( 'NONE',  ( -7.653559626096999580, -23.29848884437999956, 10.01235002622999914 ) ) ;
#12133=CARTESIAN_POINT ( 'NONE',  ( 10.18491068059999805, -23.30716934606000024, -7.640030139755999983 ) ) ;
#12144=AXIS2_PLACEMENT_3D ( 'NONE', #7040, #44145, #39421 ) ;
#12145=CARTESIAN_POINT ( 'NONE',  ( -3.506641315871922071, -2.242507564398121822, 0.3302723819864074595 ) ) ;
#12150=CARTESIAN_POINT ( 'NONE',  ( 7.624341766647000362, -18.73514853758999976, -10.42531125024999916 ) ) ;
#12151=CARTESIAN_POINT ( 'NONE',  ( 9.879208005528543168, -75.99548624166914124, 6.361455101744899032 ) ) ;
#12153=ORIENTED_EDGE ( 'NONE', *, *, #30745, .F. ) ;
#12155=DIRECTION ( 'NONE',  ( 0.000000000000000000, 0.000000000000000000, 1.000000000000000000 ) ) ;
#12160=CARTESIAN_POINT ( 'NONE',  ( 9.788011744275999959, -24.52881292764999799, -7.956359616222000497 ) ) ;
#12161=LINE ( 'NONE', #12444, #10040 ) ;
#12163=CARTESIAN_POINT ( 'NONE',  ( -8.768124086549999419, -59.94999999446000771, -7.919595949288999570 ) ) ;
#12164=CARTESIAN_POINT ( 'NONE',  ( 9.708203932494999577, -79.25000000000000000, 7.053423027515000499 ) ) ;
#12165=ORIENTED_EDGE ( 'NONE', *, *, #6351, .T. ) ;
#12169=EDGE_CURVE ( 'NONE', #50392, #56632, #27211, .T. ) ;
#12171=FACE_OUTER_BOUND ( 'NONE', #4932, .T. ) ;
#12172=CARTESIAN_POINT ( 'NONE',  ( 7.220923959705223716, -77.62291666666665435, 9.396085398178630754 ) ) ;
#12173=CARTESIAN_POINT ( 'NONE',  ( -10.12290050255000118, -60.04999997790999799, 7.648026768390999486 ) ) ;
#12176=CIRCLE ( 'NONE', #45180, 12.05000000000000071 ) ;
#12178=CARTESIAN_POINT ( 'NONE',  ( 8.666925696778452703, -17.00708316157502864, -9.019429295394159496 ) ) ;
#12179=CARTESIAN_POINT ( 'NONE',  ( 12.76303204522000101, -23.26485147686999966, 1.980584515753000208 ) ) ;
#12181=EDGE_CURVE ( 'NONE', #35471, #35553, #41969, .T. ) ;
#12182=CARTESIAN_POINT ( 'NONE',  ( -12.70926857199000004, -23.40841990708999987, 1.933876778424000076 ) ) ;
#12183=VERTEX_POINT ( 'NONE', #24833 ) ;
#12185=CARTESIAN_POINT ( 'NONE',  ( -12.61271781517999990, -55.60306329017999616, -1.798333084008999938 ) ) ;
#12186=CIRCLE ( 'NONE', #45191, 1.250000000000000000 ) ;
#12187=ORIENTED_EDGE ( 'NONE', *, *, #7468, .T. ) ;
#12190=CARTESIAN_POINT ( 'NONE',  ( 10.36289662401999934, -23.20106470441999846, 7.633500902327000404 ) ) ;
#12192=VECTOR ( 'NONE', #7539, 1000.000000000000000 ) ;
#12199=CARTESIAN_POINT ( 'NONE',  ( -12.46165725309000116, -60.47155322489999918, -1.631637378451999965 ) ) ;
#12201=CARTESIAN_POINT ( 'NONE',  ( 7.640030264154999529, -18.69283319134000010, 10.18491080493000212 ) ) ;
#12202=FACE_OUTER_BOUND ( 'NONE', #18693, .T. ) ;
#12203=CARTESIAN_POINT ( 'NONE',  ( 8.792808668394924254, -53.57303577587560994, -9.175550543417134719 ) ) ;
#12205=CARTESIAN_POINT ( 'NONE',  ( 12.43645963092999907, -17.08248289540999920, 0.05235777564064000161 ) ) ;
#12207=CARTESIAN_POINT ( 'NONE',  ( -9.767984832581378285, -76.65268247146492797, 6.530121237128238221 ) ) ;
#12209=CARTESIAN_POINT ( 'NONE',  ( -7.657744736598999680, -55.13080421771999795, 9.966195456739999514 ) ) ;
#12211=CARTESIAN_POINT ( 'NONE',  ( -8.541162059891000524, -16.99199348450000002, -9.205819316576999256 ) ) ;
#12212=CARTESIAN_POINT ( 'NONE',  ( 7.612971540256999958, -55.47547726255000100, 10.53003236230999917 ) ) ;
#12213=CARTESIAN_POINT ( 'NONE',  ( -0.9887300587125997797, -17.06589942230999668, -12.65963207090000076 ) ) ;
#12214=AXIS2_PLACEMENT_3D ( 'NONE', #52312, #11868, #1860 ) ;
#12215=DIRECTION ( 'NONE',  ( 0.000000000000000000, 1.000000000000000000, 0.000000000000000000 ) ) ;
#12218=CARTESIAN_POINT ( 'NONE',  ( 1.679092372047056303, -3.500000000000000444, 2.912269088518365301 ) ) ;
#12221=DIRECTION ( 'NONE',  ( -1.000000000000000000, 0.000000000000000000, 0.000000000000000000 ) ) ;
#12222=CARTESIAN_POINT ( 'NONE',  ( 10.10912542009492476, -18.52413588830737012, -7.634643956514229224 ) ) ;
#12223=CARTESIAN_POINT ( 'NONE',  ( -12.64502302235000109, -22.77129148951999937, 1.799490220168999954 ) ) ;
#12224=CARTESIAN_POINT ( 'NONE',  ( 3.399769613747000374, -1.852058083081000062, -1.316590098206999793 ) ) ;
#12230=AXIS2_PLACEMENT_3D ( 'NONE', #40569, #162, #22558 ) ;
#12232=DIRECTION ( 'NONE',  ( -1.000000000000000000, 0.000000000000000000, 0.000000000000000000 ) ) ;
#12233=EDGE_CURVE ( 'NONE', #54663, #25767, #5717, .T. ) ;
#12236=CARTESIAN_POINT ( 'NONE',  ( 8.150535938090355259, -76.38592193059849933, -8.463838335192644280 ) ) ;
#12240=CARTESIAN_POINT ( 'NONE',  ( 10.14950121161999874, -59.55077027461999961, 7.674627477469999626 ) ) ;
#12245=CARTESIAN_POINT ( 'NONE',  ( -9.697390092196839007, -17.02767731347392299, -8.266602378574265941 ) ) ;
#12247=CARTESIAN_POINT ( 'NONE',  ( -9.050966798898000931, -55.65000000893999754, 7.919595949288999570 ) ) ;
#12251=ORIENTED_EDGE ( 'NONE', *, *, #19969, .F. ) ;
#12252=CARTESIAN_POINT ( 'NONE',  ( -2.353768593183752866, -0.7500000000000000000, 2.616124937882430945 ) ) ;
#12253=VERTEX_POINT ( 'NONE', #55779 ) ;
#12254=ORIENTED_EDGE ( 'NONE', *, *, #31389, .T. ) ;
#12256=ORIENTED_EDGE ( 'NONE', *, *, #42729, .T. ) ;
#12259=ORIENTED_EDGE ( 'NONE', *, *, #42011, .F. ) ;
#12260=CARTESIAN_POINT ( 'NONE',  ( -11.50369798034000013, -78.89133840368999984, 4.092992355904999435 ) ) ;
#12263=CARTESIAN_POINT ( 'NONE',  ( -7.653559626114000203, -60.09848884406000025, 10.01235002625000092 ) ) ;
#12265=CARTESIAN_POINT ( 'NONE',  ( -3.234167002596432638, -1.610214578096402116, -0.3547048605170013413 ) ) ;
#12273=CARTESIAN_POINT ( 'NONE',  ( 7.406580528771000260, -77.67838321630000564, -10.82165712228000132 ) ) ;
#12274=DIRECTION ( 'NONE',  ( -0.6489586469979856664, 0.04890178911501888437, -0.7592504787669837052 ) ) ;
#12276=DIRECTION ( 'NONE',  ( 0.7071067811865474617, 0.000000000000000000, -0.7071067811865474617 ) ) ;
#12278=FACE_OUTER_BOUND ( 'NONE', #24088, .T. ) ;
#12279=CARTESIAN_POINT ( 'NONE',  ( -0.02783871057799041163, -2.976126516332163963, 3.249638514261254940 ) ) ;
#12282=CARTESIAN_POINT ( 'NONE',  ( 8.343860018000999190, -60.54999999966955926, -8.343860018000999190 ) ) ;
#12285=CARTESIAN_POINT ( 'NONE',  ( -3.796701970596999764, -2.777085600324999959, 0.2667143827384000354 ) ) ;
#12287=DIRECTION ( 'NONE',  ( -0.9957542217969272969, 0.04890179605515140859, 0.07798810240143222439 ) ) ;
#12290=AXIS2_PLACEMENT_3D ( 'NONE', #31989, #27561, #41154 ) ;
#12292=CARTESIAN_POINT ( 'NONE',  ( -12.96685733093999993, -77.05870625016000020, -1.095351912296000041 ) ) ;
#12295=DIRECTION ( 'NONE',  ( -0.9999999999995751176, 0.000000000000000000, -9.217549100139771309E-07 ) ) ;
#12296=CARTESIAN_POINT ( 'NONE',  ( 6.720944364705999874, -75.82425451000999317, 10.55406361522000047 ) ) ;
#12298=ADVANCED_FACE ( 'NONE', ( #52216 ), #53413, .F. ) ;
#12299=CARTESIAN_POINT ( 'NONE',  ( -7.624341764906000130, -55.53514850498000044, -10.42531124851000079 ) ) ;
#12300=DIRECTION ( 'NONE',  ( 0.000000000000000000, -1.000000000000000000, 0.000000000000000000 ) ) ;
#12301=ADVANCED_FACE ( 'NONE', ( #15317, #45758 ), #5867, .F. ) ;
#12302=CARTESIAN_POINT ( 'NONE',  ( 12.49837680052000088, -60.00957148770000060, 1.667051419334000029 ) ) ;
#12303=CARTESIAN_POINT ( 'NONE',  ( 7.642147947538999730, -19.21514526754999963, -10.55910102244999926 ) ) ;
#12310=CIRCLE ( 'NONE', #45324, 13.89999999999999858 ) ;
#12315=CARTESIAN_POINT ( 'NONE',  ( -7.342377162853141570, -55.56980390652893931, -8.190817883596540838 ) ) ;
#12316=B_SPLINE_CURVE_WITH_KNOTS ( 'NONE', 3,
 ( #47585, #6526, #38398, #2119, #3265, #51420 ),
 .UNSPECIFIED., .F., .F.,
 ( 4, 1, 1, 4 ),
 ( 0.000000000000000000, 0.3333333333333000081, 0.6666666666667000474, 1.000000000000000000 ),
 .UNSPECIFIED. ) ;
#12319=EDGE_LOOP ( 'NONE', ( #37886, #6897, #5383, #55102 ) ) ;
#12320=ORIENTED_EDGE ( 'NONE', *, *, #32009, .F. ) ;
#12321=EDGE_LOOP ( 'NONE', ( #27916, #49290, #5609, #12926 ) ) ;
#12323=CARTESIAN_POINT ( 'NONE',  ( -1.250000000000000000, -60.04999999966999980, -12.50000000000000000 ) ) ;
#12324=FACE_OUTER_BOUND ( 'NONE', #6662, .T. ) ;
#12325=CARTESIAN_POINT ( 'NONE',  ( -3.303475362236280688, -1.803380025278898957, 2.022687598699045797 ) ) ;
#12326=ORIENTED_EDGE ( 'NONE', *, *, #37396, .F. ) ;
#12327=CARTESIAN_POINT ( 'NONE',  ( -12.70556836328846728, -25.22772277325712409, -0.2642470010205509867 ) ) ;
#12330=DIRECTION ( 'NONE',  ( 0.000000000000000000, 1.000000000000000000, 0.000000000000000000 ) ) ;
#12332=CARTESIAN_POINT ( 'NONE',  ( 9.038965287750000854, -53.46737759073999996, 9.029769469428000406 ) ) ;
#12334=CARTESIAN_POINT ( 'NONE',  ( -17.50000000000000000, -57.79999999999999716, 0.000000000000000000 ) ) ;
#12338=CARTESIAN_POINT ( 'NONE',  ( -7.646788277333999240, -23.37228598377000210, 10.00831419131999844 ) ) ;
#12341=EDGE_CURVE ( 'NONE', #7317, #39806, #8385, .T. ) ;
#12343=CARTESIAN_POINT ( 'NONE',  ( -12.54673671099000032, -17.17796527435999820, 0.9173654211231000444 ) ) ;
#12344=CARTESIAN_POINT ( 'NONE',  ( 12.76303204517000012, -18.73514852243999940, -1.980584515753000208 ) ) ;
#12347=CARTESIAN_POINT ( 'NONE',  ( 0.000000000000000000, -26.93717104351999936, 0.000000000000000000 ) ) ;
#12353=CARTESIAN_POINT ( 'NONE',  ( 1.080502472816999848, -3.206346044169000375, -3.225196509442000092 ) ) ;
#12355=CARTESIAN_POINT ( 'NONE',  ( 17.50000000000000000, -63.73717104351998586, 4.519614127395999927E-10 ) ) ;
#12360=ORIENTED_EDGE ( 'NONE', *, *, #15660, .T. ) ;
#12361=CARTESIAN_POINT ( 'NONE',  ( -10.21381326472000062, -22.77129148951999937, -7.668949790003000366 ) ) ;
#12364=B_SPLINE_CURVE_WITH_KNOTS ( 'NONE', 3,
 ( #6166, #32427, #5293, #9727, #1470, #38042, #51061, #2054, #55474, #1181, #23587, #895, #10611, #36871, #10025, #19459, #37455, #33014, #50473, #28593, #28294, #46638, #6457, #45760, #54882, #24176, #27715, #42192, #37165, #46346 ),
 .UNSPECIFIED., .F., .F.,
 ( 4, 2, 2, 2, 2, 2, 2, 2, 2, 2, 2, 2, 2, 2, 4 ),
 ( 0.000000000000000000, 0.1250000000000000000, 0.1875000000000000000, 0.2500000000000000000, 0.3125000000000000000, 0.3750000000000000000, 0.4999999999999999445, 0.5624999999999998890, 0.6249999999999998890, 0.6874999999999998890, 0.7499999999999998890, 0.8124999999999998890, 0.8437499999999998890, 0.8749999999999998890, 1.000000000000000000 ),
 .UNSPECIFIED. ) ;
#12366=ADVANCED_FACE ( 'NONE', ( #15018 ), #33012, .F. ) ;
#12369=CARTESIAN_POINT ( 'NONE',  ( 3.743655618246999772, -1.488444768727999801, 0.9564365499490000699 ) ) ;
#12371=CARTESIAN_POINT ( 'NONE',  ( -3.251382512355739163, -3.110731818665983361, -0.4248859449704894820 ) ) ;
#12376=CARTESIAN_POINT ( 'NONE',  ( -12.54435570283313162, -18.47582218226908424, 1.733918077769268873 ) ) ;
#12381=DIRECTION ( 'NONE',  ( 0.9999999999995751176, 0.000000000000000000, 9.217549097710770925E-07 ) ) ;
#12382=CARTESIAN_POINT ( 'NONE',  ( -0.6454797251710800987, -53.91193487831872488, -12.50471521364922545 ) ) ;
#12383=LINE ( 'NONE', #48413, #14829 ) ;
#12384=EDGE_CURVE ( 'NONE', #34267, #46987, #41393, .T. ) ;
#12386=CARTESIAN_POINT ( 'NONE',  ( -12.92177931909999877, -57.04263462147999775, 2.062503053667999797 ) ) ;
#12388=DIRECTION ( 'NONE',  ( 0.000000000000000000, -1.000000000000000000, 0.000000000000000000 ) ) ;
#12390=ORIENTED_EDGE ( 'NONE', *, *, #57484, .T. ) ;
#12395=DIRECTION ( 'NONE',  ( 0.000000000000000000, -1.000000000000000000, 0.000000000000000000 ) ) ;
#12397=ADVANCED_FACE ( 'NONE', ( #37163 ), #10303, .F. ) ;
#12398=FACE_OUTER_BOUND ( 'NONE', #23143, .T. ) ;
#12399=CARTESIAN_POINT ( 'NONE',  ( -7.915529793650001089, -78.59986579304998600, 9.174504061492999796 ) ) ;
#12401=CARTESIAN_POINT ( 'NONE',  ( 0.000000000000000000, -19.21421830981000767, 13.15643568216998638 ) ) ;
#12404=FACE_OUTER_BOUND ( 'NONE', #53194, .T. ) ;
#12414=EDGE_CURVE ( 'NONE', #16042, #35254, #45781, .T. ) ;
#12419=CARTESIAN_POINT ( 'NONE',  ( -7.718346056127999510, -20.25111654322000021, 10.07719973196000041 ) ) ;
#12422=CARTESIAN_POINT ( 'NONE',  ( 10.55911395187000146, -19.21538333566000034, -7.642160924884000117 ) ) ;
#12430=CARTESIAN_POINT ( 'NONE',  ( -12.70451796517048315, -16.82354927383735799, 0.5205401191410179429 ) ) ;
#12433=CARTESIAN_POINT ( 'NONE',  ( -3.386904097422250182, -1.772078739568806682, -0.9629521321246109489 ) ) ;
#12435=CARTESIAN_POINT ( 'NONE',  ( -0.005523896504025000050, -53.73036543741000060, -12.55021156877000088 ) ) ;
#12436=CARTESIAN_POINT ( 'NONE',  ( 9.655637611919594576, -75.99817351014564792, 6.698623033092742318 ) ) ;
#12439=CARTESIAN_POINT ( 'NONE',  ( -5.747123378374999980, -78.61567021304000491, 10.24856442990000005 ) ) ;
#12441=CARTESIAN_POINT ( 'NONE',  ( -10.04834954474590170, -78.74359739231434219, -6.156343130738470393 ) ) ;
#12444=CARTESIAN_POINT ( 'NONE',  ( 9.050966799188000067, -59.94999999969999749, -7.919595949288999570 ) ) ;
#12446=CARTESIAN_POINT ( 'NONE',  ( 0.7004007752496766992, -78.56662277740376510, 11.72745275690763833 ) ) ;
#12447=CARTESIAN_POINT ( 'NONE',  ( -10.36746145409134812, -55.03400544978683229, -7.635225828739184983 ) ) ;
#12454=CARTESIAN_POINT ( 'NONE',  ( -7.624341766656999475, -60.06485146221000093, -10.42531125026000005 ) ) ;
#12457=DIRECTION ( 'NONE',  ( -0.9999999999998321343, 0.000000000000000000, -5.794542750377190787E-07 ) ) ;
#12458=FACE_OUTER_BOUND ( 'NONE', #13760, .T. ) ;
#12460=EDGE_LOOP ( 'NONE', ( #42151, #11983, #15823, #56782 ) ) ;
#12462=FACE_BOUND ( 'NONE', #45528, .T. ) ;
#12463=TOROIDAL_SURFACE ( 'NONE', #13387, 17.50000000000000000, 5.000000000000000000 ) ;
#12464=EDGE_LOOP ( 'NONE', ( #8626, #20039, #15240, #17105, #23362, #24319, #39159 ) ) ;
#12469=ADVANCED_FACE ( 'NONE', ( #26125 ), #2335, .F. ) ;
#12475=ORIENTED_EDGE ( 'NONE', *, *, #10515, .F. ) ;
#12481=CIRCLE ( 'NONE', #7771, 0.5000000000000006661 ) ;
#12482=CARTESIAN_POINT ( 'NONE',  ( 3.673449851479000383, -75.85705099976999577, 11.86240085298999958 ) ) ;
#12487=AXIS2_PLACEMENT_3D ( 'NONE', #52885, #26873, #9177 ) ;
#12488=CARTESIAN_POINT ( 'NONE',  ( 12.66761570929000058, -17.77632520104999969, -1.696752301450999978 ) ) ;
#12490=CARTESIAN_POINT ( 'NONE',  ( -11.75000000000000000, -76.70000000000000284, 1.487410190129999909E-14 ) ) ;
#12491=ORIENTED_EDGE ( 'NONE', *, *, #39130, .T. ) ;
#12495=CARTESIAN_POINT ( 'NONE',  ( -10.18127254044999930, -18.61355771719999908, -7.633407132383000615 ) ) ;
#12496=CARTESIAN_POINT ( 'NONE',  ( 7.718368845804999268, -57.05199022587000002, 10.07722254368999870 ) ) ;
#12497=PLANE ( 'NONE',  #55336 ) ;
#12503=ORIENTED_EDGE ( 'NONE', *, *, #31416, .F. ) ;
#12505=ADVANCED_FACE ( 'NONE', ( #36155 ), #1803, .T. ) ;
#12506=CARTESIAN_POINT ( 'NONE',  ( -1.886823409076999969, -55.03680315604999151, 12.68610076202999792 ) ) ;
#12507=CARTESIAN_POINT ( 'NONE',  ( -12.00000000000000000, -23.25000000000000000, 0.000000000000000000 ) ) ;
#12508=CARTESIAN_POINT ( 'NONE',  ( -3.254128868261999763, -1.540113550428000133, 0.1923296600005000023 ) ) ;
#12511=CARTESIAN_POINT ( 'NONE',  ( -12.43421868114999995, -54.36340276600000010, 1.197355605038999959 ) ) ;
#12512=DIRECTION ( 'NONE',  ( 0.000000000000000000, 1.000000000000000000, 0.000000000000000000 ) ) ;
#12513=CARTESIAN_POINT ( 'NONE',  ( 0.9113424693931000409, -61.62535793526999583, 12.54674099561999867 ) ) ;
#12516=DIRECTION ( 'NONE',  ( 0.000000000000000000, 1.000000000000000000, 0.000000000000000000 ) ) ;
#12517=TOROIDAL_SURFACE ( 'NONE', #57768, 17.50000000000000000, 5.000000000000000000 ) ;
#12519=B_SPLINE_SURFACE_WITH_KNOTS ( 'NONE', 3, 3, ( 
 ( #39203, #57218, #57794, #34766, #43938, #3489, #21493, #39499, #40970, #58088, #53967, #17648, #35637, #4667, #27664, #45115, #36530, #18828, #27075 ),
 ( #8790, #32379, #36820, #36239, #54262, #31199, #53665, #40677, #13504, #35939, #9089, #26486, #31496, #22960, #49543, #18248, #269, #22666, #18539 ),
 ( #40378, #54554, #54837, #27374, #9385, #41258, #14094, #32093, #50133, #14380, #13795, #49239, #9676, #4955, #45708, #13205, #31796, #26781, #5245 ),
 ( #561, #49838, #44811, #45412, #4363, #23249, #844, #8490, #40071, #22364, #44510, #4060, #22064, #58385, #17948, #37700, #38280, #37988, #55125 ) ),
 .UNSPECIFIED., .F., .F., .F.,
 ( 4, 4 ),
 ( 4, 1, 1, 1, 1, 1, 1, 1, 1, 1, 1, 1, 1, 1, 1, 1, 4 ),
 ( -0.3708084972812999980, 1.370808497280999960 ),
 ( -0.01116670151518999940, 0.02512507840917000204, 0.06141685833353999896, 0.09770863825790000734, 0.1340004181822999907, 0.1702921981065999846, 0.2065839780310000096, 0.2428757579554000068, 0.2791675378797000007, 0.3154593178041000257, 0.3517510977284000195, 0.3880428776527999890, 0.4243346575772000140, 0.4606264375015000079, 0.4969182174258999773, 0.5332099973503000578, 0.5695017772746000517 ),
 .UNSPECIFIED. ) ;
#12520=CARTESIAN_POINT ( 'NONE',  ( 8.308415499261105452, -76.38746760283510184, -8.308548603794546850 ) ) ;
#12524=CARTESIAN_POINT ( 'NONE',  ( 0.000000000000000000, -3.500000000000000000, 0.000000000000000000 ) ) ;
#12529=AXIS2_PLACEMENT_3D ( 'NONE', #48392, #17080, #21215 ) ;
#12536=ORIENTED_EDGE ( 'NONE', *, *, #209, .T. ) ;
#12537=CARTESIAN_POINT ( 'NONE',  ( -1.318114156682550941, -24.73572477192366037, 12.70261578162813265 ) ) ;
#12539=ORIENTED_EDGE ( 'NONE', *, *, #33081, .T. ) ;
#12540=CARTESIAN_POINT ( 'NONE',  ( 3.169069393497101483, -3.500000000000000444, -1.511488537269458643 ) ) ;
#12547=CARTESIAN_POINT ( 'NONE',  ( -1.317308456444000075, -79.12212284379999971, -12.28806242769000079 ) ) ;
#12550=FACE_OUTER_BOUND ( 'NONE', #50622, .T. ) ;
#12551=VECTOR ( 'NONE', #13287, 1000.000000000000000 ) ;
#12554=CARTESIAN_POINT ( 'NONE',  ( 0.000000000000000000, 4.040000000000000036, 0.000000000000000000 ) ) ;
#12557=CARTESIAN_POINT ( 'NONE',  ( 5.921937764992279973, -79.02083333333980875, 10.24701051719076439 ) ) ;
#12559=CARTESIAN_POINT ( 'NONE',  ( -3.078285613438000112, -78.22578184934000944, 12.42192206172999924 ) ) ;
#12565=CARTESIAN_POINT ( 'NONE',  ( -8.485281374238999419, -55.64999999967000122, 8.485281374238999419 ) ) ;
#12566=CARTESIAN_POINT ( 'NONE',  ( -2.299428515032341025, -3.037945768799499291, 2.296401124946453542 ) ) ;
#12568=CARTESIAN_POINT ( 'NONE',  ( 12.00000000000000000, -23.25000000000000000, 1.250000000000000000 ) ) ;
#12570=CARTESIAN_POINT ( 'NONE',  ( -3.448863046786000197, -1.817410797673999934, -1.608907009436000068 ) ) ;
#12572=ORIENTED_EDGE ( 'NONE', *, *, #43359, .T. ) ;
#12573=CARTESIAN_POINT ( 'NONE',  ( -7.606021324617000090, -60.22158946241999899, -10.52692925329000140 ) ) ;
#12575=LINE ( 'NONE', #3434, #14733 ) ;
#12577=CARTESIAN_POINT ( 'NONE',  ( -12.43569863939999998, -17.11799904157000185, -0.4278707626186999957 ) ) ;
#12578=FACE_OUTER_BOUND ( 'NONE', #6821, .T. ) ;
#12580=CARTESIAN_POINT ( 'NONE',  ( 0.8898229089128317781, -25.02324531182464185, -12.70296869045280275 ) ) ;
#12581=CARTESIAN_POINT ( 'NONE',  ( -4.687723163076999100, -76.48740961512999093, 11.43893144258999861 ) ) ;
#12582=ORIENTED_EDGE ( 'NONE', *, *, #52968, .F. ) ;
#12584=DIRECTION ( 'NONE',  ( 1.000000000000000000, 0.000000000000000000, 0.000000000000000000 ) ) ;
#12585=CARTESIAN_POINT ( 'NONE',  ( -10.98362417419999915, -18.84999999999999787, -0.5999999999999999778 ) ) ;
#12586=CARTESIAN_POINT ( 'NONE',  ( 7.919595949288999570, -55.65000000893999754, 9.050966798898000931 ) ) ;
#12591=EDGE_CURVE ( 'NONE', #47034, #3351, #54174, .T. ) ;
#12592=ORIENTED_EDGE ( 'NONE', *, *, #50508, .T. ) ;
#12593=CARTESIAN_POINT ( 'NONE',  ( 0.000000000000000000, -45.69638659094999866, 0.000000000000000000 ) ) ;
#12596=VERTEX_POINT ( 'NONE', #13120 ) ;
#12597=VERTEX_POINT ( 'NONE', #9589 ) ;
#12600=CARTESIAN_POINT ( 'NONE',  ( -8.111636311582410386, -55.28385402668900639, -7.429974109819841743 ) ) ;
#12605=VERTEX_POINT ( 'NONE', #49755 ) ;
#12608=CARTESIAN_POINT ( 'NONE',  ( -9.344374848299676017, -78.14684388159851380, 7.168986247577478821 ) ) ;
#12615=CARTESIAN_POINT ( 'NONE',  ( 12.60354432324999863, -56.04899162853999428, -1.750000000000000000 ) ) ;
#12616=CARTESIAN_POINT ( 'NONE',  ( 0.3135214471491306609, -18.31418618813953358, 10.99610567419586182 ) ) ;
#12617=CARTESIAN_POINT ( 'NONE',  ( 8.838834764832000701, -55.54999999966999980, -8.838834764832000701 ) ) ;
#12618=EDGE_CURVE ( 'NONE', #23838, #38250, #45321, .T. ) ;
#12619=CARTESIAN_POINT ( 'NONE',  ( 12.70457892003493150, -61.97873330296430794, -0.5105076820992421327 ) ) ;
#12620=AXIS2_PLACEMENT_3D ( 'NONE', #13861, #31857, #49898 ) ;
#12623=EDGE_CURVE ( 'NONE', #30461, #47356, #58305, .T. ) ;
#12631=CARTESIAN_POINT ( 'NONE',  ( 6.874986978319857833, -78.37672046791054470, 9.923497271207523340 ) ) ;
#12634=B_SPLINE_SURFACE_WITH_KNOTS ( 'NONE', 3, 3, ( 
 ( #16409, #29961, #23944, #1533 ),
 ( #14502, #46710, #6230, #50539 ),
 ( #41668, #5077, #41380, #23072 ),
 ( #49962, #36939, #28661, #15087 ),
 ( #19526, #24246, #42262, #51127 ),
 ( #54950, #18661, #19824, #36649 ),
 ( #31917, #1828, #54668, #28363 ),
 ( #50833, #33083, #54385, #46410 ),
 ( #41086, #963, #678, #41960 ),
 ( #32493, #13922, #10680, #32786 ),
 ( #10093, #37519, #5361, #9503 ),
 ( #23655, #28072, #46122, #18946 ),
 ( #1248, #27490, #55537, #14209 ),
 ( #45531, #37228, #32206, #5646 ),
 ( #50247, #9798, #27781, #45826 ),
 ( #23369, #19236, #55245, #14791 ),
 ( #10379, #5939, #20686, #33672 ) ),
 .UNSPECIFIED., .F., .F., .F.,
 ( 4, 1, 1, 1, 1, 1, 1, 1, 1, 1, 1, 1, 1, 1, 4 ),
 ( 4, 4 ),
 ( -0.01011400514355999952, 0.000000000000000000, 0.08333333333333001192, 0.1666666666667000196, 0.2500000000000000000, 0.3333333333333000081, 0.4166666666666999919, 0.5000000000000000000, 0.5833333333333000637, 0.6666666666667000474, 0.7500000000000000000, 0.8333333333333000637, 0.9166666666667000474, 1.000000000000000000, 1.010365328128000062 ),
 ( -0.3559705546945999832, 1.357612395641000003 ),
 .UNSPECIFIED. ) ;
#12635=ADVANCED_FACE ( 'NONE', ( #49155 ), #8707, .F. ) ;
#12636=B_SPLINE_CURVE_WITH_KNOTS ( 'NONE', 3,
 ( #3668, #39674, #39394, #34370, #12240, #2811 ),
 .UNSPECIFIED., .F., .F.,
 ( 4, 1, 1, 4 ),
 ( 0.000000000000000000, 0.3333333333333000081, 0.6666666666667000474, 1.000000000000000000 ),
 .UNSPECIFIED. ) ;
#12639=CARTESIAN_POINT ( 'NONE',  ( 1.980532734072999901, -56.03767313155999830, -12.80090744964999949 ) ) ;
#12640=CARTESIAN_POINT ( 'NONE',  ( 0.000000000000000000, -22.78578169018998878, -13.15643568216998638 ) ) ;
#12642=CARTESIAN_POINT ( 'NONE',  ( -1.980532758766000212, -59.56256650660999696, 12.80088938804999898 ) ) ;
#12643=CARTESIAN_POINT ( 'NONE',  ( -10.06032152983862638, -75.80000000000001137, 6.218695677770802455 ) ) ;
#12652=CARTESIAN_POINT ( 'NONE',  ( -10.30767511324000019, -60.54763733864000130, 7.634418707071000121 ) ) ;
#12653=CARTESIAN_POINT ( 'NONE',  ( 0.6116024548114998849, -1.269669754918000049, -3.650360381117999431 ) ) ;
#12655=CARTESIAN_POINT ( 'NONE',  ( 12.54673349184999864, -24.82806887810999896, -0.9076721992841999542 ) ) ;
#12656=FACE_OUTER_BOUND ( 'NONE', #6363, .T. ) ;
#12660=CARTESIAN_POINT ( 'NONE',  ( -3.140976149987326327, -1.624123246795792008, -0.9279992776312928626 ) ) ;
#12661=CARTESIAN_POINT ( 'NONE',  ( -10.18589234709999936, -60.08917565288000162, -7.641012386057000505 ) ) ;
#12663=CIRCLE ( 'NONE', #9863, 0.5999999999999999778 ) ;
#12664=ORIENTED_EDGE ( 'NONE', *, *, #43490, .T. ) ;
#12665=CARTESIAN_POINT ( 'NONE',  ( 12.50000000000000000, -55.35321828636000419, -1.250000000000000000 ) ) ;
#12667=CARTESIAN_POINT ( 'NONE',  ( -2.839805762151337731, -1.041666666666666741, -1.636761686205423949 ) ) ;
#12668=ORIENTED_EDGE ( 'NONE', *, *, #3364, .F. ) ;
#12669=EDGE_CURVE ( 'NONE', #38673, #4989, #26990, .T. ) ;
#12670=CARTESIAN_POINT ( 'NONE',  ( 1.618935784558559021, -54.87248831271503491, 12.52134385796530047 ) ) ;
#12671=CARTESIAN_POINT ( 'NONE',  ( -7.633502222218000455, -55.59895684611999656, -10.36289759015999934 ) ) ;
#12672=AXIS2_PLACEMENT_3D ( 'NONE', #25170, #43193, #48485 ) ;
#12683=CARTESIAN_POINT ( 'NONE',  ( 12.32442898454999813, -77.89680700753000053, -3.452188809138999837 ) ) ;
#12686=DIRECTION ( 'NONE',  ( -0.7026410690473252618, 0.1122098755728027641, -0.7026410690473252618 ) ) ;
#12691=EDGE_CURVE ( 'NONE', #46623, #2183, #35916, .T. ) ;
#12696=CARTESIAN_POINT ( 'NONE',  ( 12.92177931904999966, -21.75736537952000305, 2.062503053667999797 ) ) ;
#12697=CARTESIAN_POINT ( 'NONE',  ( 1.538071403319964281, -76.66458333333332575, 11.75000000000000711 ) ) ;
#12698=DIRECTION ( 'NONE',  ( 1.000000000000000000, 0.000000000000000000, 0.000000000000000000 ) ) ;
#12701=CARTESIAN_POINT ( 'NONE',  ( -10.12290050124000018, -23.24999999991999644, -7.648026767085999822 ) ) ;
#12704=CARTESIAN_POINT ( 'NONE',  ( -0.5999999999999999778, -18.84999999999999787, 12.00000000000000000 ) ) ;
#12706=ORIENTED_EDGE ( 'NONE', *, *, #41494, .T. ) ;
#12710=CARTESIAN_POINT ( 'NONE',  ( 7.648026768008000076, -55.55000001556999933, -10.12290050216000026 ) ) ;
#12712=CARTESIAN_POINT ( 'NONE',  ( -12.90000000000000036, -5.899999999999999467, 0.000000000000000000 ) ) ;
#12716=CARTESIAN_POINT ( 'NONE',  ( -10.41144098943260055, -23.52546312060280798, -7.610433527965647649 ) ) ;
#12717=CARTESIAN_POINT ( 'NONE',  ( 9.776257737944273885, -75.99675307336229935, 6.518143555704688730 ) ) ;
#12721=CARTESIAN_POINT ( 'NONE',  ( 2.842273781882246109, -2.309665338011450242, -1.638569763671750668 ) ) ;
#12727=CARTESIAN_POINT ( 'NONE',  ( 1.782734487935019541, -17.87754631442412645, 12.71547286926183062 ) ) ;
#12729=CARTESIAN_POINT ( 'NONE',  ( 3.275141186877373656, -78.55044160814078680, 11.28318025823995541 ) ) ;
#12734=CARTESIAN_POINT ( 'NONE',  ( 8.907139034666096578, -75.80000000000001137, -7.900904588343065527 ) ) ;
#12736=FACE_OUTER_BOUND ( 'NONE', #36853, .T. ) ;
#12738=CARTESIAN_POINT ( 'NONE',  ( 11.75000000000000000, -76.95000000000000284, 0.000000000000000000 ) ) ;
#12740=DIRECTION ( 'NONE',  ( 0.000000000000000000, -1.000000000000000000, 0.000000000000000000 ) ) ;
#12742=DIRECTION ( 'NONE',  ( 0.000000000000000000, 1.000000000000000000, 0.000000000000000000 ) ) ;
#12743=AXIS2_PLACEMENT_3D ( 'NONE', #10205, #32905, #18772 ) ;
#12744=CARTESIAN_POINT ( 'NONE',  ( 0.000000000000000000, -26.93717104351999936, 0.000000000000000000 ) ) ;
#12745=ORIENTED_EDGE ( 'NONE', *, *, #19701, .F. ) ;
#12747=B_SPLINE_CURVE_WITH_KNOTS ( 'NONE', 3,
 ( #27566, #45610, #5151, #45900, #52354, #33746 ),
 .UNSPECIFIED., .F., .F.,
 ( 4, 1, 1, 4 ),
 ( 0.000000000000000000, 0.3333333333333000081, 0.6666666666667000474, 1.000000000000000000 ),
 .UNSPECIFIED. ) ;
#12748=FACE_OUTER_BOUND ( 'NONE', #56465, .T. ) ;
#12750=ORIENTED_EDGE ( 'NONE', *, *, #57349, .F. ) ;
#12751=CARTESIAN_POINT ( 'NONE',  ( -11.89999999977000122, -23.15000000000000213, 0.000000000000000000 ) ) ;
#12752=ORIENTED_EDGE ( 'NONE', *, *, #15032, .T. ) ;
#12753=FACE_OUTER_BOUND ( 'NONE', #38141, .T. ) ;
#12763=LINE ( 'NONE', #44654, #50299 ) ;
#12765=CARTESIAN_POINT ( 'NONE',  ( 6.505968525872999564, -75.99885856455000521, -11.03293300994000070 ) ) ;
#12769=CARTESIAN_POINT ( 'NONE',  ( 12.48408657659000021, -18.63026141570000149, -1.669508654504000100 ) ) ;
#12770=CARTESIAN_POINT ( 'NONE',  ( -9.770427757044000572, -25.05529868456000386, -8.292768371742001321 ) ) ;
#12771=CARTESIAN_POINT ( 'NONE',  ( -11.52337632743963347, -76.68415288553248388, 2.295937825998684012 ) ) ;
#12773=ORIENTED_EDGE ( 'NONE', *, *, #4266, .T. ) ;
#12775=DIRECTION ( 'NONE',  ( 1.000000000000000000, 0.000000000000000000, 0.000000000000000000 ) ) ;
#12776=ADVANCED_FACE ( 'NONE', ( #30685 ), #13973, .F. ) ;
#12778=CARTESIAN_POINT ( 'NONE',  ( -10.36222501930000028, -18.77880030165999869, -7.631889976314999657 ) ) ;
#12779=CARTESIAN_POINT ( 'NONE',  ( 7.612971414731999786, -60.12452529330000317, 10.53003223724999948 ) ) ;
#12780=DIRECTION ( 'NONE',  ( 0.000000000000000000, 1.000000000000000000, 0.000000000000000000 ) ) ;
#12784=CARTESIAN_POINT ( 'NONE',  ( 7.601397897754999633, -23.24999999688999708, 10.07627163191000008 ) ) ;
#12788=CARTESIAN_POINT ( 'NONE',  ( 1.295048492664000017, -54.27106480841000291, 12.54716442233000073 ) ) ;
#12789=VECTOR ( 'NONE', #46517, 1000.000000000000114 ) ;
#12790=CARTESIAN_POINT ( 'NONE',  ( -12.60552522436000089, -23.28917565320000094, 1.799501877760999902 ) ) ;
#12791=CARTESIAN_POINT ( 'NONE',  ( -3.114903485943000039, -2.587975590836000261, 1.894521665057000037 ) ) ;
#12794=DIRECTION ( 'NONE',  ( 0.000000000000000000, -1.000000000000000000, 0.000000000000000000 ) ) ;
#12795=CARTESIAN_POINT ( 'NONE',  ( -0.4450739772378000114, -61.67813214767999597, 12.43586747599000120 ) ) ;
#12796=DIRECTION ( 'NONE',  ( -0.7071067811864970576, -3.534300182982984496E-08, -0.7071067811865970887 ) ) ;
#12799=ADVANCED_FACE ( 'NONE', ( #7050 ), #26185, .F. ) ;
#12801=CARTESIAN_POINT ( 'NONE',  ( 11.37518297042895909, -77.17675121447568642, -3.894839749335730517 ) ) ;
#12807=CARTESIAN_POINT ( 'NONE',  ( -12.77297283019000140, -61.52822696498000710, 1.476112654660999723 ) ) ;
#12809=FACE_OUTER_BOUND ( 'NONE', #6597, .T. ) ;
#12810=CARTESIAN_POINT ( 'NONE',  ( 11.99999999999998757, -75.80000000000001137, 1.262728147666866585 ) ) ;
#12811=ORIENTED_EDGE ( 'NONE', *, *, #52089, .T. ) ;
#12817=ORIENTED_EDGE ( 'NONE', *, *, #23827, .T. ) ;
#12818=VERTEX_POINT ( 'NONE', #27365 ) ;
#12820=ORIENTED_EDGE ( 'NONE', *, *, #1310, .T. ) ;
#12825=CARTESIAN_POINT ( 'NONE',  ( 0.5506765233278000382, -25.25954292244000143, -12.77514798311000099 ) ) ;
#12830=CARTESIAN_POINT ( 'NONE',  ( -11.64344076419000018, -78.97841925342000025, 4.142712554322000251 ) ) ;
#12835=AXIS2_PLACEMENT_3D ( 'NONE', #27089, #27962, #58098 ) ;
#12839=VECTOR ( 'NONE', #9258, 1000.000000000000227 ) ;
#12840=CARTESIAN_POINT ( 'NONE',  ( 6.944463141141999252, -76.67929967898000143, -9.899892744310998083 ) ) ;
#12841=CARTESIAN_POINT ( 'NONE',  ( 12.19230762942000013, -76.97310353941999495, -3.339585897562999950 ) ) ;
#12846=CARTESIAN_POINT ( 'NONE',  ( -0.003892519155869273318, -2.975579981115140438, 3.249707649575004798 ) ) ;
#12848=CARTESIAN_POINT ( 'NONE',  ( -13.89999999999999858, -6.000000000000000000, 0.000000000000000000 ) ) ;
#12850=CARTESIAN_POINT ( 'NONE',  ( 1.781953555039999859, -2.946439977264000198, -3.363141973650999983 ) ) ;
#12852=ORIENTED_EDGE ( 'NONE', *, *, #22643, .F. ) ;
#12856=CARTESIAN_POINT ( 'NONE',  ( -12.44180763926000033, -17.90743932638000047, -1.459474665415000150 ) ) ;
#12857=CARTESIAN_POINT ( 'NONE',  ( -9.339950055924999717, -78.07862776177000796, -9.061158367717998985 ) ) ;
#12860=CARTESIAN_POINT ( 'NONE',  ( -12.32022177036999899, -76.50834268828999996, -2.184374125126999910 ) ) ;
#12861=ORIENTED_EDGE ( 'NONE', *, *, #45866, .F. ) ;
#12862=CARTESIAN_POINT ( 'NONE',  ( -14.00000000000000000, -69.46217755556000384, -5.544640309915999038E-06 ) ) ;
#12866=CARTESIAN_POINT ( 'NONE',  ( -1.799475304559999822, -20.24828923609000242, -12.69616050747999836 ) ) ;
#12877=VECTOR ( 'NONE', #10556, 1000.000000000000227 ) ;
#12878=ORIENTED_EDGE ( 'NONE', *, *, #43410, .F. ) ;
#12881=CARTESIAN_POINT ( 'NONE',  ( -7.353725627631181538, -55.49344856148322691, -8.180687091746209560 ) ) ;
#12883=VECTOR ( 'NONE', #40533, 1000.000000000000114 ) ;
#12888=CARTESIAN_POINT ( 'NONE',  ( -11.74632961396963182, -78.18897092989068653, 1.536354035319362099 ) ) ;
#12889=CARTESIAN_POINT ( 'NONE',  ( -3.315446055502797140, -0.8053565017603924181, 2.002980581032114404 ) ) ;
#12897=CARTESIAN_POINT ( 'NONE',  ( 10.36292447788999915, -55.59904187545999577, 7.633480004398999874 ) ) ;
#12898=CARTESIAN_POINT ( 'NONE',  ( -7.641012386038000592, -18.71082434677000350, -10.18589234708000113 ) ) ;
#12899=CARTESIAN_POINT ( 'NONE',  ( 1.535709645332969941, -77.33338449841629370, -11.74782911498686389 ) ) ;
#12901=CARTESIAN_POINT ( 'NONE',  ( 7.668949790015999746, -59.57129148919000272, -10.21381326473999884 ) ) ;
#12903=CARTESIAN_POINT ( 'NONE',  ( -10.53562597589000127, -23.20558297624999966, 7.620013358880999732 ) ) ;
#12910=CARTESIAN_POINT ( 'NONE',  ( -1.801614160558000055, -23.38652261905000174, 12.59687422887999908 ) ) ;
#12915=CIRCLE ( 'NONE', #32721, 1.750000000000000000 ) ;
#12918=TOROIDAL_SURFACE ( 'NONE', #56321, 17.50000000000000000, 5.000000000000000000 ) ;
#12919=FACE_BOUND ( 'NONE', #53627, .T. ) ;
#12923=LINE ( 'NONE', #57230, #42064 ) ;
#12926=ORIENTED_EDGE ( 'NONE', *, *, #56821, .F. ) ;
#12927=CARTESIAN_POINT ( 'NONE',  ( -10.04116292115999975, -22.76462890193000277, -7.682344222570999470 ) ) ;
#12931=CARTESIAN_POINT ( 'NONE',  ( -10.53495260694000102, -60.02711197453000125, 7.618387230260000642 ) ) ;
#12932=CARTESIAN_POINT ( 'NONE',  ( 2.610509270830999817, -0.8533534949847000339, 2.388898296653999775 ) ) ;
#12934=CARTESIAN_POINT ( 'NONE',  ( 12.68624828429000040, -23.76426636002999970, -1.886933512377000133 ) ) ;
#12935=CARTESIAN_POINT ( 'NONE',  ( -7.958763982144999360, -54.32301960774000094, -9.723170657514000226 ) ) ;
#12937=CARTESIAN_POINT ( 'NONE',  ( -12.71005124793994945, -54.50500926678794400, 1.687536500513815874 ) ) ;
#12938=CARTESIAN_POINT ( 'NONE',  ( 8.060180467146665251, -24.62064870852272236, -9.621709426102265539 ) ) ;
#12939=DIRECTION ( 'NONE',  ( 0.000000000000000000, 0.000000000000000000, -1.000000000000000000 ) ) ;
#12940=EDGE_CURVE ( 'NONE', #41885, #20895, #24647, .T. ) ;
#12941=CARTESIAN_POINT ( 'NONE',  ( -10.53101998748999968, -60.10639625617000092, -7.613962827198000660 ) ) ;
#12943=ORIENTED_EDGE ( 'NONE', *, *, #3683, .F. ) ;
#12944=EDGE_CURVE ( 'NONE', #43269, #40118, #3509, .T. ) ;
#12946=CARTESIAN_POINT ( 'NONE',  ( 0.000000000000000000, -0.5000000000000000000, 0.000000000000000000 ) ) ;
#12948=VERTEX_POINT ( 'NONE', #41537 ) ;
#12950=CARTESIAN_POINT ( 'NONE',  ( -9.108265402946999600, -53.92189187171000242, -8.478706101031999509 ) ) ;
#12952=EDGE_LOOP ( 'NONE', ( #50094, #29300, #12390, #10594 ) ) ;
#12957=DIRECTION ( 'NONE',  ( 0.7071067811865475727, 0.000000000000000000, -0.7071067811865475727 ) ) ;
#12959=EDGE_LOOP ( 'NONE', ( #8119, #54866, #14494, #13323 ) ) ;
#12960=CARTESIAN_POINT ( 'NONE',  ( 10.01676960212000012, -18.79061945240999876, 7.658895148207999881 ) ) ;
#12963=CARTESIAN_POINT ( 'NONE',  ( -1.349038754591999956, -78.11117779481000412, -13.04399231589999886 ) ) ;
#12968=B_SPLINE_CURVE_WITH_KNOTS ( 'NONE', 3,
 ( #16475, #57198, #6450, #38321, #16188, #29168, #47214, #20047, #24465, #43338, #34166, #38898, #42477, #52203, #7035, #16766, #34744, #34456 ),
 .UNSPECIFIED., .F., .F.,
 ( 4, 2, 2, 2, 2, 2, 2, 2, 4 ),
 ( 0.000000000000000000, 0.1250000000000000000, 0.2499999999999999722, 0.3749999999999999445, 0.4999999999999999445, 0.6250000000000000000, 0.7500000000000000000, 0.8750000000000000000, 1.000000000000000000 ),
 .UNSPECIFIED. ) ;
#12969=CARTESIAN_POINT ( 'NONE',  ( 10.18249594443127393, -17.70907903273885964, 7.792385963404970362 ) ) ;
#12972=CARTESIAN_POINT ( 'NONE',  ( 7.331368884251999951, -75.87623222076001639, 9.888700222343000945 ) ) ;
#12974=EDGE_CURVE ( 'NONE', #50856, #45467, #56333, .T. ) ;
#12976=CARTESIAN_POINT ( 'NONE',  ( 0.2195004960192260823, -2.979185772309488556, -3.512406260861363982 ) ) ;
#12978=DIRECTION ( 'NONE',  ( -1.000000000000000000, 0.000000000000000000, 0.000000000000000000 ) ) ;
#12982=CARTESIAN_POINT ( 'NONE',  ( 10.55910102242999926, -22.78485473281999774, -7.642147947518999729 ) ) ;
#12987=ORIENTED_EDGE ( 'NONE', *, *, #49558, .F. ) ;
#12994=EDGE_CURVE ( 'NONE', #37470, #43983, #5595, .T. ) ;
#12998=CARTESIAN_POINT ( 'NONE',  ( -1.761265949711000145, -55.09141781180999686, -12.57448205041000122 ) ) ;
#12999=CARTESIAN_POINT ( 'NONE',  ( 10.35033528849731077, -75.98912452525786421, 5.575283253277660833 ) ) ;
#13001=ORIENTED_EDGE ( 'NONE', *, *, #44045, .F. ) ;
#13003=CARTESIAN_POINT ( 'NONE',  ( 10.58663230755379558, -78.98684970000721250, 5.411474183400683202 ) ) ;
#13007=CARTESIAN_POINT ( 'NONE',  ( -1.575772165385731283, -17.53845457198085711, 12.70597445617638144 ) ) ;
#13009=CARTESIAN_POINT ( 'NONE',  ( -0.8690907654282591377, -78.57852448961540404, 11.75728093043408151 ) ) ;
#13010=CARTESIAN_POINT ( 'NONE',  ( -1.247385803317999864, -61.27722255996999934, -12.50301438880000049 ) ) ;
#13011=B_SPLINE_CURVE_WITH_KNOTS ( 'NONE', 3,
 ( #28258, #27971, #46896, #6719, #24438, #32687, #47187, #2020, #46021, #51316, #10574, #42157, #46312, #56027, #15576, #5542, #41860, #19428, #23552, #33571, #24138, #15867, #38295, #33853 ),
 .UNSPECIFIED., .F., .F.,
 ( 4, 2, 2, 2, 2, 2, 2, 2, 2, 2, 2, 4 ),
 ( 0.000000000000000000, 0.1249999999999965028, 0.2499999999999930056, 0.3749999999999895084, 0.4374999999999880096, 0.4999999999999865663, 0.6249999999999841238, 0.7499999999999817923, 0.8124999999999819034, 0.8437499999999832356, 0.8749999999999845679, 1.000000000000000000 ),
 .UNSPECIFIED. ) ;
#13012=VERTEX_POINT ( 'NONE', #32444 ) ;
#13015=CIRCLE ( 'NONE', #15862, 1.250000000000000000 ) ;
#13019=EDGE_CURVE ( 'NONE', #44485, #4989, #14077, .T. ) ;
#13020=CARTESIAN_POINT ( 'NONE',  ( -12.50385602492088566, -54.01562718794550477, 0.8579628942656060131 ) ) ;
#13021=CARTESIAN_POINT ( 'NONE',  ( -11.00000000000000000, -23.75000000000000000, 0.000000000000000000 ) ) ;
#13023=CARTESIAN_POINT ( 'NONE',  ( 1.980584515756000030, -23.26485150094000076, 12.76303204340999997 ) ) ;
#13024=CARTESIAN_POINT ( 'NONE',  ( 9.723199429438999175, -17.52306056078000296, -7.958735708418001487 ) ) ;
#13026=CARTESIAN_POINT ( 'NONE',  ( -12.43641409351999982, -24.91801033895000117, -0.03481937293212000045 ) ) ;
#13027=EDGE_LOOP ( 'NONE', ( #20539, #32778, #18496, #41457 ) ) ;
#13028=EDGE_CURVE ( 'NONE', #4183, #51185, #14798, .T. ) ;
#13029=VERTEX_POINT ( 'NONE', #35910 ) ;
#13034=ORIENTED_EDGE ( 'NONE', *, *, #52799, .T. ) ;
#13035=CARTESIAN_POINT ( 'NONE',  ( 7.633403016703000254, -23.38650073851000144, 10.18126993294000115 ) ) ;
#13037=VECTOR ( 'NONE', #21657, 1000.000000000000000 ) ;
#13042=ORIENTED_EDGE ( 'NONE', *, *, #6979, .F. ) ;
#13043=ORIENTED_EDGE ( 'NONE', *, *, #19051, .F. ) ;
#13048=CARTESIAN_POINT ( 'NONE',  ( -9.584819989847998656, -76.38917353800999877, -8.495977810255999074 ) ) ;
#13049=VECTOR ( 'NONE', #57648, 1000.000000000000000 ) ;
#13051=CARTESIAN_POINT ( 'NONE',  ( 7.635226873531286707, -55.03391307102463514, -10.36745167320620808 ) ) ;
#13053=CARTESIAN_POINT ( 'NONE',  ( 12.77302454167999990, -17.27764858556999883, -1.481891240072999993 ) ) ;
#13054=CARTESIAN_POINT ( 'NONE',  ( -9.310177428684999867, -25.13531023636999961, -8.596745825432000387 ) ) ;
#13061=CARTESIAN_POINT ( 'NONE',  ( -12.72923908220886524, -60.57554307127314530, 1.930512971237506870 ) ) ;
#13062=EDGE_CURVE ( 'NONE', #42403, #3300, #241, .T. ) ;
#13063=CARTESIAN_POINT ( 'NONE',  ( 7.640030264136999705, -55.49283319101999723, 10.18491080491000034 ) ) ;
#13065=CARTESIAN_POINT ( 'NONE',  ( -1.250000000000000000, -23.44678171330999916, 12.50000000000000000 ) ) ;
#13069=CARTESIAN_POINT ( 'NONE',  ( 3.165411199172025292, -1.770833333333333481, 0.8506806241676674318 ) ) ;
#13071=ADVANCED_FACE ( 'NONE', ( #36213 ), #24460, .F. ) ;
#13072=VERTEX_POINT ( 'NONE', #54231 ) ;
#13073=LINE ( 'NONE', #26359, #3698 ) ;
#13074=CARTESIAN_POINT ( 'NONE',  ( 0.9887300587132999974, -53.86589942198000358, 12.65963207085999898 ) ) ;
#13075=DIRECTION ( 'NONE',  ( 0.000000000000000000, 0.000000000000000000, 1.000000000000000000 ) ) ;
#13076=CARTESIAN_POINT ( 'NONE',  ( 3.356323744093999917, -1.913384542061000060, 1.423708999316999790 ) ) ;
#13080=CARTESIAN_POINT ( 'NONE',  ( -0.005523896503676999775, -61.86963456192999899, 12.55021156886000000 ) ) ;
#13081=CARTESIAN_POINT ( 'NONE',  ( 12.43410192431999839, -17.55868879885999689, 1.192687910177000044 ) ) ;
#13085=CARTESIAN_POINT ( 'NONE',  ( 7.575978808960503130, -77.13227571528085491, -9.335878689481054593 ) ) ;
#13086=CARTESIAN_POINT ( 'NONE',  ( 10.59026995113000069, -79.47130787033000843, -4.872245490990999350 ) ) ;
#13088=EDGE_CURVE ( 'NONE', #26901, #29384, #26708, .T. ) ;
#13091=CARTESIAN_POINT ( 'NONE',  ( 1.495357591765385630, -61.35876337328488717, 12.70444646763499108 ) ) ;
#13095=CARTESIAN_POINT ( 'NONE',  ( 0.000000000000000000, -0.09999999995300053179, -13.89999999994999946 ) ) ;
#13102=VERTEX_POINT ( 'NONE', #6670 ) ;
#13103=EDGE_CURVE ( 'NONE', #38250, #22857, #48074, .T. ) ;
#13117=CARTESIAN_POINT ( 'NONE',  ( -11.97043380835999926, -78.40274619638999809, 2.407544143317999819 ) ) ;
#13118=VERTEX_POINT ( 'NONE', #19967 ) ;
#13120=CARTESIAN_POINT ( 'NONE',  ( 7.919595949288999570, -55.65000000488999632, 8.768124086549999419 ) ) ;
#13121=LINE ( 'NONE', #7835, #43324 ) ;
#13124=EDGE_CURVE ( 'NONE', #36059, #38869, #2824, .T. ) ;
#13127=CARTESIAN_POINT ( 'NONE',  ( -12.50000000000000000, -23.25000000000000000, 0.000000000000000000 ) ) ;
#13128=CARTESIAN_POINT ( 'NONE',  ( -10.25367346088999909, -77.69466387191998535, 7.393739220494000008 ) ) ;
#13132=CIRCLE ( 'NONE', #53690, 13.89999999999999858 ) ;
#13133=CARTESIAN_POINT ( 'NONE',  ( -10.59551070214999946, -57.04351820043999766, 7.678690995233999672 ) ) ;
#13134=CARTESIAN_POINT ( 'NONE',  ( 1.208728522240711367, -2.945855492842563095, 3.016110857596538963 ) ) ;
#13140=CARTESIAN_POINT ( 'NONE',  ( -3.593558748265999636, -1.779776491687000028, 0.1459214154804999997 ) ) ;
#13142=ADVANCED_FACE ( 'NONE', ( #25538 ), #923, .F. ) ;
#13143=EDGE_LOOP ( 'NONE', ( #492, #52001, #40928, #3965 ) ) ;
#13147=CARTESIAN_POINT ( 'NONE',  ( -12.54705919859000041, -17.46307476627999833, -1.287183453418999868 ) ) ;
#13148=CARTESIAN_POINT ( 'NONE',  ( -3.274010471232999819, -77.41257207022999864, 12.59444704299999884 ) ) ;
#13150=CARTESIAN_POINT ( 'NONE',  ( 12.87022657274000004, -19.21514526754999963, -2.062597299672999540 ) ) ;
#13152=CARTESIAN_POINT ( 'NONE',  ( -14.00000000000000000, -69.50420297070000686, 0.000000000000000000 ) ) ;
#13153=CARTESIAN_POINT ( 'NONE',  ( -5.869402599192000025, -78.36567021304000491, 10.46661899222999992 ) ) ;
#13155=DIRECTION ( 'NONE',  ( 1.000000000000000000, 0.000000000000000000, 0.000000000000000000 ) ) ;
#13158=CARTESIAN_POINT ( 'NONE',  ( -0.1204595238885999980, -0.6950726927052999216, 3.497926457646999943 ) ) ;
#13159=CARTESIAN_POINT ( 'NONE',  ( 12.00000000000000000, -60.04999999966999980, 1.250000000000000000 ) ) ;
#13161=ORIENTED_EDGE ( 'NONE', *, *, #24328, .T. ) ;
#13163=PLANE ( 'NONE',  #41741 ) ;
#13168=CARTESIAN_POINT ( 'NONE',  ( 0.000000000000000000, -33.10361340872000113, 0.000000000000000000 ) ) ;
#13169=CARTESIAN_POINT ( 'NONE',  ( 9.050966798898000931, -55.65000000893999754, -7.919595949288999570 ) ) ;
#13171=B_SPLINE_CURVE_WITH_KNOTS ( 'NONE', 3,
 ( #56238, #25216, #34062, #39085, #30212, #11942 ),
 .UNSPECIFIED., .F., .F.,
 ( 4, 2, 4 ),
 ( 0.000000000000000000, 0.5000000000000000000, 1.000000000000000000 ),
 .UNSPECIFIED. ) ;
#13174=ADVANCED_FACE ( 'NONE', ( #21111 ), #6539, .F. ) ;
#13175=ORIENTED_EDGE ( 'NONE', *, *, #52470, .T. ) ;
#13176=B_SPLINE_SURFACE_WITH_KNOTS ( 'NONE', 3, 3, ( 
 ( #49795, #54790, #27032, #23203 ),
 ( #26737, #26443, #9631, #44768 ),
 ( #4317, #22317, #22912, #44465 ),
 ( #40334, #35895, #27619, #53927 ),
 ( #5202, #45364, #41208, #32329 ),
 ( #8448, #31455, #4016, #22022 ),
 ( #4913, #58044, #49497, #9046 ),
 ( #45069, #4621, #22620, #40632 ) ),
 .UNSPECIFIED., .F., .F., .F.,
 ( 4, 1, 1, 1, 1, 4 ),
 ( 4, 4 ),
 ( -0.01200407345746999990, 0.000000000000000000, 0.3333333333333000081, 0.6666666666667000474, 1.000000000000000000, 1.011997855551999947 ),
 ( -0.3559705542741999906, 1.355970554273999928 ),
 .UNSPECIFIED. ) ;
#13177=VERTEX_POINT ( 'NONE', #56552 ) ;
#13178=AXIS2_PLACEMENT_3D ( 'NONE', #46400, #5633, #37217 ) ;
#13179=CARTESIAN_POINT ( 'NONE',  ( 7.345153731672220410, -60.02841244177673730, 8.188331488387616375 ) ) ;
#13183=CARTESIAN_POINT ( 'NONE',  ( -12.00000000000000000, -23.25000000000000000, -1.250000000000000000 ) ) ;
#13184=ORIENTED_EDGE ( 'NONE', *, *, #27381, .F. ) ;
#13187=DIRECTION ( 'NONE',  ( 0.7071067811865474617, 0.7071067811865474617, 6.623688493237445538E-09 ) ) ;
#13188=EDGE_CURVE ( 'NONE', #25114, #16112, #42953, .T. ) ;
#13190=CARTESIAN_POINT ( 'NONE',  ( 11.15465700714716135, -77.42101778503236176, -3.785658037966275202 ) ) ;
#13192=CARTESIAN_POINT ( 'NONE',  ( -1.532229593853648764, -54.67701036647127211, 12.51228690871742977 ) ) ;
#13193=CARTESIAN_POINT ( 'NONE',  ( 7.613962827198000660, -60.10639625617000092, -10.53101998748999968 ) ) ;
#13195=CARTESIAN_POINT ( 'NONE',  ( 0.5962167095188528609, -23.22841244210244938, -10.98383273456533260 ) ) ;
#13199=CARTESIAN_POINT ( 'NONE',  ( 0.000000000000000000, -33.10361340872000113, 0.000000000000000000 ) ) ;
#13201=CARTESIAN_POINT ( 'NONE',  ( 0.9113424693944999211, -24.82535793559999959, 12.54674099557999867 ) ) ;
#13204=ADVANCED_FACE ( 'NONE', ( #24961, #30822 ), #48288, .F. ) ;
#13205=CARTESIAN_POINT ( 'NONE',  ( -3.640412412913000217, -0.9909739483179998976, -1.054207720119999969 ) ) ;
#13208=CARTESIAN_POINT ( 'NONE',  ( 1.980584515752000119, -60.06485146591000301, -12.76303204605000197 ) ) ;
#13211=AXIS2_PLACEMENT_3D ( 'NONE', #40306, #58314, #45038 ) ;
#13214=AXIS2_PLACEMENT_3D ( 'NONE', #53030, #39732, #7001 ) ;
#13219=ORIENTED_EDGE ( 'NONE', *, *, #57288, .T. ) ;
#13222=EDGE_CURVE ( 'NONE', #17310, #18079, #40091, .T. ) ;
#13224=CARTESIAN_POINT ( 'NONE',  ( -9.723174505940001211, -24.47697504200000296, -7.958760297012999807 ) ) ;
#13227=CARTESIAN_POINT ( 'NONE',  ( -12.85140862673999784, -58.55560170131000319, -1.980464483675000054 ) ) ;
#13229=CARTESIAN_POINT ( 'NONE',  ( -3.688842081945000295, -1.137975590836000084, -0.3027291113864000183 ) ) ;
#13230=DIRECTION ( 'NONE',  ( -0.7071067811865475727, 0.000000000000000000, -0.7071067811865475727 ) ) ;
#13231=CARTESIAN_POINT ( 'NONE',  ( 12.43410103865999972, -24.44137177768999791, -1.192638008239000014 ) ) ;
#13232=DIRECTION ( 'NONE',  ( 0.000000000000000000, 0.000000000000000000, 1.000000000000000000 ) ) ;
#13234=CARTESIAN_POINT ( 'NONE',  ( -12.76303204513999923, -55.53514852210999919, 1.980584515753000208 ) ) ;
#13236=CARTESIAN_POINT ( 'NONE',  ( -3.003066045103267800, -1.634010044345757695, -1.313579205990373699 ) ) ;
#13237=CARTESIAN_POINT ( 'NONE',  ( -10.21380041493999968, -56.02847221959000024, -7.668936932630000314 ) ) ;
#13239=DIRECTION ( 'NONE',  ( 0.000000000000000000, -1.000000000000000000, 0.000000000000000000 ) ) ;
#13240=ORIENTED_EDGE ( 'NONE', *, *, #34746, .T. ) ;
#13244=DIRECTION ( 'NONE',  ( -0.7071067811865474617, 0.000000000000000000, -0.7071067811865474617 ) ) ;
#13247=CARTESIAN_POINT ( 'NONE',  ( -8.485548443509001615, -53.91931586703000079, -9.101490738433000161 ) ) ;
#13251=ORIENTED_EDGE ( 'NONE', *, *, #23281, .T. ) ;
#13253=CARTESIAN_POINT ( 'NONE',  ( -12.50000000000000000, -23.25000000000000000, 0.000000000000000000 ) ) ;
#13254=CIRCLE ( 'NONE', #43496, 12.05000000000000071 ) ;
#13256=ORIENTED_EDGE ( 'NONE', *, *, #19101, .F. ) ;
#13258=CIRCLE ( 'NONE', #20820, 14.00000000000000000 ) ;
#13261=CARTESIAN_POINT ( 'NONE',  ( -10.72428337452000058, -76.94558033460998558, 7.546888592172999566 ) ) ;
#13264=DIRECTION ( 'NONE',  ( -1.000000000000000000, 0.000000000000000000, 0.000000000000000000 ) ) ;
#13268=CARTESIAN_POINT ( 'NONE',  ( -8.838834764832000701, -23.25000000000000000, 8.838834764832000701 ) ) ;
#13270=DIRECTION ( 'NONE',  ( -1.206135027324979392E-11, 1.868136817095964273E-07, 0.9999999999999824585 ) ) ;
#13271=CARTESIAN_POINT ( 'NONE',  ( 12.17088485526999975, -75.81397293882999122, 1.845041276493999849 ) ) ;
#13272=CARTESIAN_POINT ( 'NONE',  ( 2.969846905577856688, -2.646672701395195837, 1.998772415440041472 ) ) ;
#13273=CARTESIAN_POINT ( 'NONE',  ( -7.864797288620628990, -17.54877151179043793, 10.10445166986456123 ) ) ;
#13277=ADVANCED_FACE ( 'NONE', ( #53873, #18149 ), #18729, .T. ) ;
#13279=CARTESIAN_POINT ( 'NONE',  ( -7.393247292513355440, -77.12252906155467258, -9.541960917511291385 ) ) ;
#13284=ORIENTED_EDGE ( 'NONE', *, *, #34756, .F. ) ;
#13287=DIRECTION ( 'NONE',  ( 0.000000000000000000, 0.7071067811866525998, -0.7071067811864425456 ) ) ;
#13293=CARTESIAN_POINT ( 'NONE',  ( 1.194090706002000069, -54.35968341064000242, -12.43436538485999954 ) ) ;
#13294=CARTESIAN_POINT ( 'NONE',  ( 4.630631704076160204, -76.04223606416009318, 10.79891528241036092 ) ) ;
#13296=PLANE ( 'NONE',  #41746 ) ;
#13299=CARTESIAN_POINT ( 'NONE',  ( -9.344545319423653851, -77.14671203089999096, 7.168886721853569455 ) ) ;
#13300=ADVANCED_FACE ( 'NONE', ( #750 ), #22595, .F. ) ;
#13304=DIRECTION ( 'NONE',  ( 0.7071067811865475727, 0.000000000000000000, -0.7071067811865475727 ) ) ;
#13306=CARTESIAN_POINT ( 'NONE',  ( -12.76303204294000082, -18.73514849292999784, -1.980584515756000030 ) ) ;
#13307=FACE_OUTER_BOUND ( 'NONE', #43789, .T. ) ;
#13308=EDGE_LOOP ( 'NONE', ( #39232, #44263, #53500, #49879 ) ) ;
#13311=CARTESIAN_POINT ( 'NONE',  ( 11.07590168690624921, -75.80000000000001137, -4.579409602955339054 ) ) ;
#13314=CARTESIAN_POINT ( 'NONE',  ( -12.00000000000000000, -18.84999999999999787, 0.000000000000000000 ) ) ;
#13315=CARTESIAN_POINT ( 'NONE',  ( -10.98449824368628569, -23.30634943317874885, 0.5845455749771404363 ) ) ;
#13318=DIRECTION ( 'NONE',  ( 0.000000000000000000, 1.000000000000000000, 0.000000000000000000 ) ) ;
#13320=CARTESIAN_POINT ( 'NONE',  ( -12.76303204525000012, -60.06485147653999945, -1.980584515753000208 ) ) ;
#13321=CARTESIAN_POINT ( 'NONE',  ( 10.20000000000000107, -0.5000000000000000000, 0.000000000000000000 ) ) ;
#13323=ORIENTED_EDGE ( 'NONE', *, *, #46847, .T. ) ;
#13327=DIRECTION ( 'NONE',  ( 0.000000000000000000, 0.000000000000000000, -1.000000000000000000 ) ) ;
#13329=CARTESIAN_POINT ( 'NONE',  ( 7.622785526030999570, -23.78712283485999990, 10.47836401506999948 ) ) ;
#13331=CARTESIAN_POINT ( 'NONE',  ( 7.995796640821898116, -55.11315380194076141, -7.555116226629998266 ) ) ;
#13342=CIRCLE ( 'NONE', #46388, 0.5000000000000004441 ) ;
#13344=CARTESIAN_POINT ( 'NONE',  ( -2.166618510580000212, -76.03018013234999728, -12.78353179556000008 ) ) ;
#13346=CARTESIAN_POINT ( 'NONE',  ( 12.76303204525000012, -60.06485147653999945, 1.980584515753000208 ) ) ;
#13348=ADVANCED_FACE ( 'NONE', ( #18442 ), #46181, .F. ) ;
#13350=CARTESIAN_POINT ( 'NONE',  ( -11.03440961815829624, -76.67173248339075542, 4.064493473767709197 ) ) ;
#13358=CARTESIAN_POINT ( 'NONE',  ( -10.36221646773000060, -18.77876216379999974, 7.631895822745999425 ) ) ;
#13360=CARTESIAN_POINT ( 'NONE',  ( -17.50000000000000000, -49.87071424677999687, -2.007252870860999804E-13 ) ) ;
#13361=FACE_OUTER_BOUND ( 'NONE', #56048, .T. ) ;
#13362=DIRECTION ( 'NONE',  ( 0.000000000000000000, 0.000000000000000000, -1.000000000000000000 ) ) ;
#13367=CARTESIAN_POINT ( 'NONE',  ( 3.250000000000000000, -1.350000000000000089, 0.000000000000000000 ) ) ;
#13368=CARTESIAN_POINT ( 'NONE',  ( 2.019183793707000074, -55.01279722724000010, 12.79944116701999768 ) ) ;
#13371=CARTESIAN_POINT ( 'NONE',  ( 1.478503027591000052, -2.061791850768999623, 3.507110283440000309 ) ) ;
#13376=CARTESIAN_POINT ( 'NONE',  ( -1.801614160555000010, -60.18652261871999798, 12.59687422890000086 ) ) ;
#13377=DIRECTION ( 'NONE',  ( 0.9999999999995751176, 0.000000000000000000, 9.217549102787771002E-07 ) ) ;
#13380=CARTESIAN_POINT ( 'NONE',  ( 10.05509635955887582, -76.74978642219571157, 6.690173733955245616 ) ) ;
#13381=CARTESIAN_POINT ( 'NONE',  ( 9.549799293660999666, -79.45431405828000493, -7.133803361836999812 ) ) ;
#13383=CARTESIAN_POINT ( 'NONE',  ( -12.79999999971638225, -2.899999999995986233, -2.660989632711285603E-09 ) ) ;
#13386=DIRECTION ( 'NONE',  ( 0.000000000000000000, 0.000000000000000000, 1.000000000000000000 ) ) ;
#13387=AXIS2_PLACEMENT_3D ( 'NONE', #39131, #57433, #56284 ) ;
#13390=CARTESIAN_POINT ( 'NONE',  ( -12.52785920744742043, -23.79405666946010456, -1.668536824485600256 ) ) ;
#13392=CARTESIAN_POINT ( 'NONE',  ( 12.55432891850757748, -55.41272687720891099, -1.749897736046111651 ) ) ;
#13394=CARTESIAN_POINT ( 'NONE',  ( -0.6454797250855089930, -61.68806512111238760, 12.50471521371613726 ) ) ;
#13397=VERTEX_POINT ( 'NONE', #4863 ) ;
#13401=VERTEX_POINT ( 'NONE', #31405 ) ;
#13404=ADVANCED_FACE ( 'NONE', ( #13703 ), #1842, .T. ) ;
#13405=CARTESIAN_POINT ( 'NONE',  ( -1.576170184333999913, -17.83913032783999952, 12.55466896104999996 ) ) ;
#13407=DIRECTION ( 'NONE',  ( 0.000000000000000000, 0.1122098755727947705, 0.9936845293270585300 ) ) ;
#13412=ORIENTED_EDGE ( 'NONE', *, *, #24328, .F. ) ;
#13414=CARTESIAN_POINT ( 'NONE',  ( -1.769904851686999958, -78.80511624945999927, 12.08118746087999895 ) ) ;
#13415=ORIENTED_EDGE ( 'NONE', *, *, #42011, .T. ) ;
#13416=ORIENTED_EDGE ( 'NONE', *, *, #2631, .F. ) ;
#13422=CARTESIAN_POINT ( 'NONE',  ( -12.76493461869000079, -77.83724936260999527, -0.9303755367166000045 ) ) ;
#13429=AXIS2_PLACEMENT_3D ( 'NONE', #38410, #47302, #24840 ) ;
#13431=CARTESIAN_POINT ( 'NONE',  ( 2.999869787185454495, -2.882451689260415506, 1.248622406629191106 ) ) ;
#13435=CARTESIAN_POINT ( 'NONE',  ( -3.750250575282000121, -2.234355802843000394, 0.6493866540274000343 ) ) ;
#13438=FACE_OUTER_BOUND ( 'NONE', #17389, .T. ) ;
#13439=AXIS2_PLACEMENT_3D ( 'NONE', #49256, #4684, #40695 ) ;
#13441=EDGE_CURVE ( 'NONE', #41589, #15410, #36432, .T. ) ;
#13443=CARTESIAN_POINT ( 'NONE',  ( -12.49830607528000037, -18.79028586434999681, -1.666977523253999838 ) ) ;
#13445=CARTESIAN_POINT ( 'NONE',  ( 11.79660191402999914, -76.76735435298000709, 5.494707494196000575 ) ) ;
#13446=CIRCLE ( 'NONE', #45544, 12.90000000000000036 ) ;
#13447=CARTESIAN_POINT ( 'NONE',  ( -9.689272046837857033, -61.77888144139958371, -8.274769670276990396 ) ) ;
#13448=CARTESIAN_POINT ( 'NONE',  ( 12.53241208773999915, -22.76462890193000277, -1.667936697358999965 ) ) ;
#13450=ORIENTED_EDGE ( 'NONE', *, *, #25850, .T. ) ;
#13458=CARTESIAN_POINT ( 'NONE',  ( -3.431352783032999731, -1.273849349033000067, 2.086989923523999924 ) ) ;
#13459=LINE ( 'NONE', #13159, #27468 ) ;
#13461=ORIENTED_EDGE ( 'NONE', *, *, #48543, .F. ) ;
#13466=EDGE_LOOP ( 'NONE', ( #51702, #29797, #6734, #30595 ) ) ;
#13473=ORIENTED_EDGE ( 'NONE', *, *, #31603, .F. ) ;
#13474=EDGE_CURVE ( 'NONE', #21405, #23950, #28732, .T. ) ;
#13475=CARTESIAN_POINT ( 'NONE',  ( -2.152895537798944048, -2.668002774646853759, -2.435455713980514858 ) ) ;
#13477=CONICAL_SURFACE ( 'NONE', #49316, 0.6999999997695030007, 0.7853981633972997312 ) ;
#13481=ORIENTED_EDGE ( 'NONE', *, *, #50184, .F. ) ;
#13483=B_SPLINE_CURVE_WITH_KNOTS ( 'NONE', 3,
 ( #30900, #22651, #40363, #49528, #13780, #18237, #9074, #32075, #23235, #9370, #9660, #54822, #22049, #49226, #35623, #53651, #36224, #58372 ),
 .UNSPECIFIED., .F., .F.,
 ( 4, 2, 2, 2, 2, 2, 2, 2, 4 ),
 ( 0.000000000000000000, 0.1250000000000000833, 0.2500000000000001665, 0.3750000000000001110, 0.5000000000000001110, 0.6250000000000001110, 0.7500000000000000000, 0.8750000000000000000, 1.000000000000000000 ),
 .UNSPECIFIED. ) ;
#13487=VECTOR ( 'NONE', #27324, 1000.000000000000000 ) ;
#13488=CARTESIAN_POINT ( 'NONE',  ( 10.35410226329999794, -55.39601732791000188, 7.619716344056000068 ) ) ;
#13491=LINE ( 'NONE', #14080, #36494 ) ;
#13495=CARTESIAN_POINT ( 'NONE',  ( -10.31986335554000078, -24.28918510737999981, 7.753844818030001029 ) ) ;
#13499=CARTESIAN_POINT ( 'NONE',  ( -12.49837451347000084, -18.79042109296999641, 1.667049596275999912 ) ) ;
#13500=CARTESIAN_POINT ( 'NONE',  ( 12.80090744918999945, -22.76232687447999936, -1.980532734072999901 ) ) ;
#13501=CARTESIAN_POINT ( 'NONE',  ( 1.669849926071999890, -23.37228600417000024, 12.48404299553000030 ) ) ;
#13504=CARTESIAN_POINT ( 'NONE',  ( -3.698639260106999949, -1.410322672877000194, -1.403610537410000081 ) ) ;
#13514=DIRECTION ( 'NONE',  ( -0.9999433559010179051, 0.000000000000000000, -0.01064354214585019887 ) ) ;
#13520=AXIS2_PLACEMENT_3D ( 'NONE', #26782, #18249, #36240 ) ;
#13523=DIRECTION ( 'NONE',  ( 0.7071067811865474617, 0.000000000000000000, 0.7071067811865474617 ) ) ;
#13525=CARTESIAN_POINT ( 'NONE',  ( -10.31986335556999990, -61.08918510704999960, 7.753844818055000587 ) ) ;
#13527=CARTESIAN_POINT ( 'NONE',  ( -1.321087349134000055, -1.707219782537999997, 3.804044948481000166 ) ) ;
#13529=CARTESIAN_POINT ( 'NONE',  ( 12.70926857199000004, -23.40841990708999987, -1.933876778424000076 ) ) ;
#13530=CARTESIAN_POINT ( 'NONE',  ( -1.931087888240000217, -60.11584731951999316, 12.71658872087999903 ) ) ;
#13531=ORIENTED_EDGE ( 'NONE', *, *, #19550, .T. ) ;
#13532=VECTOR ( 'NONE', #31576, 1000.000000000000114 ) ;
#13534=CARTESIAN_POINT ( 'NONE',  ( 12.50240633877000107, -17.31762602171999887, 1.005381409788000058 ) ) ;
#13537=CIRCLE ( 'NONE', #26720, 3.799999999999999822 ) ;
#13539=EDGE_CURVE ( 'NONE', #49809, #9708, #32859, .T. ) ;
#13541=CARTESIAN_POINT ( 'NONE',  ( 10.98384481689545389, -23.22882187213949123, 0.5959944459582935394 ) ) ;
#13542=ORIENTED_EDGE ( 'NONE', *, *, #2689, .F. ) ;
#13544=CARTESIAN_POINT ( 'NONE',  ( -3.783546124412332290, -77.79732454329705149, -11.14641671793737210 ) ) ;
#13546=ORIENTED_EDGE ( 'NONE', *, *, #48168, .T. ) ;
#13547=ORIENTED_EDGE ( 'NONE', *, *, #6138, .F. ) ;
#13548=CARTESIAN_POINT ( 'NONE',  ( -9.966229686695001533, -55.13098097352000337, -7.657726530227999540 ) ) ;
#13549=ADVANCED_FACE ( 'NONE', ( #1037 ), #28440, .F. ) ;
#13558=CARTESIAN_POINT ( 'NONE',  ( -3.299302781710000243, -77.38961746229999505, 12.69174137596000129 ) ) ;
#13566=ORIENTED_EDGE ( 'NONE', *, *, #22014, .F. ) ;
#13568=CARTESIAN_POINT ( 'NONE',  ( -10.77133038182000035, -76.59221396288000960, -5.959359258312999508 ) ) ;
#13571=CARTESIAN_POINT ( 'NONE',  ( -2.416613568816377011, -3.414010557351236486, -2.560321170370766009 ) ) ;
#13572=CARTESIAN_POINT ( 'NONE',  ( 12.50483450296212773, -53.93545441819600939, -0.6958183767277665854 ) ) ;
#13574=CARTESIAN_POINT ( 'NONE',  ( -8.251802458177941446, -61.60055625090545561, -9.431055091043617722 ) ) ;
#13576=CARTESIAN_POINT ( 'NONE',  ( -11.80802719753318719, -77.03357931642592860, 2.478256143328310124 ) ) ;
#13578=DIRECTION ( 'NONE',  ( 0.7071067811865475727, 0.000000000000000000, 0.7071067811865475727 ) ) ;
#13582=CARTESIAN_POINT ( 'NONE',  ( 1.750000000000000000, -18.75000000240999753, -12.50000000000000000 ) ) ;
#13583=CARTESIAN_POINT ( 'NONE',  ( -10.07627163191000008, -23.24999999758999536, -7.601397897754999633 ) ) ;
#13586=FACE_OUTER_BOUND ( 'NONE', #13308, .T. ) ;
#13587=CARTESIAN_POINT ( 'NONE',  ( 7.775008698615757829, -76.01703051611190176, 8.841530247503397888 ) ) ;
#13589=FACE_OUTER_BOUND ( 'NONE', #26874, .T. ) ;
#13590=ORIENTED_EDGE ( 'NONE', *, *, #36608, .T. ) ;
#13592=CARTESIAN_POINT ( 'NONE',  ( -9.844172144369998989, -75.99875169021464671, 7.391061701651998384 ) ) ;
#13595=CARTESIAN_POINT ( 'NONE',  ( 13.99936781018472232, -9.295797029142999435, 0.1330447863085613691 ) ) ;
#13597=DIRECTION ( 'NONE',  ( -0.9999548435846228323, 0.000000000000000000, -0.009503199022040218977 ) ) ;
#13598=CARTESIAN_POINT ( 'NONE',  ( 12.50745077490000057, -17.00005551713000074, -2.011911479242000131E-09 ) ) ;
#13599=DIRECTION ( 'NONE',  ( 1.000000000000000000, 0.000000000000000000, 0.000000000000000000 ) ) ;
#13600=CYLINDRICAL_SURFACE ( 'NONE', #20168, 14.00000000000000000 ) ;
#13601=EDGE_LOOP ( 'NONE', ( #22498, #25672, #40788 ) ) ;
#13602=CIRCLE ( 'NONE', #4173, 0.5000000000000006661 ) ;
#13607=EDGE_CURVE ( 'NONE', #55326, #12605, #30986, .T. ) ;
#13610=B_SPLINE_CURVE_WITH_KNOTS ( 'NONE', 3,
 ( #41990, #28685, #33408, #51446, #10998, #47023, #42579, #20144, #15703, #21575 ),
 .UNSPECIFIED., .F., .F.,
 ( 4, 2, 2, 2, 4 ),
 ( 0.000000000000000000, 0.2500000000000000000, 0.5000000000000000000, 0.7500000000000000000, 1.000000000000000000 ),
 .UNSPECIFIED. ) ;
#13612=CARTESIAN_POINT ( 'NONE',  ( -1.818468715484000065E-14, -79.21250000010999770, 0.000000000000000000 ) ) ;
#13613=CARTESIAN_POINT ( 'NONE',  ( 8.768124086712999699, -55.64999999965999677, 7.919595949288999570 ) ) ;
#13619=DIRECTION ( 'NONE',  ( -0.7071067811865475727, 0.000000000000000000, 0.7071067811865475727 ) ) ;
#13621=ORIENTED_EDGE ( 'NONE', *, *, #10858, .T. ) ;
#13622=CARTESIAN_POINT ( 'NONE',  ( -7.601397897754999633, -18.75000000000000000, 9.369164850722000892 ) ) ;
#13623=VERTEX_POINT ( 'NONE', #50616 ) ;
#13624=CARTESIAN_POINT ( 'NONE',  ( 7.634438871657000192, -23.74781730700000182, 10.30764054782999928 ) ) ;
#13628=CARTESIAN_POINT ( 'NONE',  ( -10.48771805366000009, -21.75560171527000008, 7.686918321049000191 ) ) ;
#13629=B_SPLINE_CURVE_WITH_KNOTS ( 'NONE', 3,
 ( #27400, #40994, #22984, #585, #49866, #9410, #45434, #54288, #13826, #31824 ),
 .UNSPECIFIED., .F., .F.,
 ( 4, 2, 2, 2, 4 ),
 ( 0.000000000000000000, 0.2500000000000000000, 0.5000000000000000000, 0.7500000000000000000, 1.000000000000000000 ),
 .UNSPECIFIED. ) ;
#13636=ORIENTED_EDGE ( 'NONE', *, *, #18821, .F. ) ;
#13639=CIRCLE ( 'NONE', #8928, 12.80000000000000071 ) ;
#13642=CARTESIAN_POINT ( 'NONE',  ( -12.96193297681999823, -76.42049510581999527, -0.3184845575242999938 ) ) ;
#13647=CARTESIAN_POINT ( 'NONE',  ( -10.01676216527999941, -23.20941515021999635, -7.658899892521000119 ) ) ;
#13655=EDGE_CURVE ( 'NONE', #47936, #48492, #8463, .T. ) ;
#13656=FACE_OUTER_BOUND ( 'NONE', #2470, .T. ) ;
#13660=CARTESIAN_POINT ( 'NONE',  ( 0.000000000000000000, -5.899999999999999467, 0.000000000000000000 ) ) ;
#13662=CARTESIAN_POINT ( 'NONE',  ( 1.997276839918466829, -1.822916666666666741, 2.598917237794090784 ) ) ;
#13664=VERTEX_POINT ( 'NONE', #5698 ) ;
#13665=CARTESIAN_POINT ( 'NONE',  ( 1.801614160562000189, -55.41347738061999451, 12.59687422885999908 ) ) ;
#13667=CARTESIAN_POINT ( 'NONE',  ( 1.170835004517000177, -2.368424145665999792, -3.621456637410000123 ) ) ;
#13669=LINE ( 'NONE', #43892, #31393 ) ;
#13672=CARTESIAN_POINT ( 'NONE',  ( -1.666727925310000025, -59.99174481743000342, 12.50018462905999961 ) ) ;
#13673=CARTESIAN_POINT ( 'NONE',  ( 12.78015286811999829, -17.69674784880999852, 1.806262579046000072 ) ) ;
#13676=CARTESIAN_POINT ( 'NONE',  ( 9.929695104576000020, -54.16901065014000238, -7.973993995727001405 ) ) ;
#13677=VECTOR ( 'NONE', #32321, 1000.000000000000114 ) ;
#13682=CARTESIAN_POINT ( 'NONE',  ( -1.583004792665463345, -61.25209241118189141, 12.70616254415227786 ) ) ;
#13684=CARTESIAN_POINT ( 'NONE',  ( -12.43646324850000084, -61.72048514535000407, 0.1256879863178999857 ) ) ;
#13685=DIRECTION ( 'NONE',  ( 0.9999999999998321343, 0.000000000000000000, 5.794540611356191117E-07 ) ) ;
#13688=CIRCLE ( 'NONE', #46724, 8.800000000000000711 ) ;
#13692=CARTESIAN_POINT ( 'NONE',  ( -1.250000000000000000, -55.54999999966999980, -12.00000000000000000 ) ) ;
#13694=CARTESIAN_POINT ( 'NONE',  ( -11.00000000000000000, -4.000000000000000000, 0.000000000000000000 ) ) ;
#13696=ORIENTED_EDGE ( 'NONE', *, *, #1472, .T. ) ;
#13700=DIRECTION ( 'NONE',  ( 0.000000000000000000, 0.000000000000000000, -1.000000000000000000 ) ) ;
#13703=FACE_OUTER_BOUND ( 'NONE', #58068, .T. ) ;
#13705=CARTESIAN_POINT ( 'NONE',  ( 1.669724228656999987, -23.36897676534000112, -12.48434610067999984 ) ) ;
#13709=CARTESIAN_POINT ( 'NONE',  ( 9.607004209881999657, -78.54473239578000232, 7.045343969285000618 ) ) ;
#13710=EDGE_CURVE ( 'NONE', #25542, #48463, #4729, .T. ) ;
#13711=ORIENTED_EDGE ( 'NONE', *, *, #23098, .T. ) ;
#13713=CARTESIAN_POINT ( 'NONE',  ( -3.250000000000000000, -1.600000000000000089, 0.000000000000000000 ) ) ;
#13714=CARTESIAN_POINT ( 'NONE',  ( -1.718598679931974349, -61.04962933016155802, -12.71111582771588999 ) ) ;
#13718=CARTESIAN_POINT ( 'NONE',  ( 7.228795249850000104, -77.50422151684000482, -10.56189739613000000 ) ) ;
#13719=CARTESIAN_POINT ( 'NONE',  ( -9.022377653937999398, -77.30613138518998539, -8.854484771337999049 ) ) ;
#13720=TOROIDAL_SURFACE ( 'NONE', #3368, 17.50000000000000000, 5.000000000000000000 ) ;
#13723=B_SPLINE_CURVE_WITH_KNOTS ( 'NONE', 3,
 ( #17492, #4507, #53219, #49385, #39355, #57363, #52649, #58230, #52936, #40519, #34620, #12203, #21913, #39636, #35187, #17795, #35479, #8343, #48237, #7773, #3911, #13051, #44357, #26622 ),
 .UNSPECIFIED., .F., .F.,
 ( 4, 2, 2, 2, 2, 2, 2, 2, 2, 2, 2, 4 ),
 ( 0.000000000000000000, 0.1250000000000002776, 0.2500000000000005551, 0.3750000000000008327, 0.4375000000000006106, 0.5000000000000004441, 0.6249999999999993339, 0.7499999999999983347, 0.8124999999999977796, 0.8437499999999975575, 0.8749999999999972244, 1.000000000000000000 ),
 .UNSPECIFIED. ) ;
#13727=CARTESIAN_POINT ( 'NONE',  ( 9.492740219875408059, -76.89866259748522737, -7.042134608814008878 ) ) ;
#13730=DIRECTION ( 'NONE',  ( -5.794542751833290187E-07, -4.446058653751146425E-20, 0.9999999999998322453 ) ) ;
#13733=EDGE_LOOP ( 'NONE', ( #31465, #25213, #5683, #53201 ) ) ;
#13734=CARTESIAN_POINT ( 'NONE',  ( 0.5847500590559170375, -23.30655143818054498, 10.98448857562229897 ) ) ;
#13738=CARTESIAN_POINT ( 'NONE',  ( 7.287838312904000304, -78.18963704368999856, -10.78085041437000058 ) ) ;
#13741=CARTESIAN_POINT ( 'NONE',  ( 12.60413670420000010, -23.30716680861999990, -1.799502287691000069 ) ) ;
#13743=FACE_OUTER_BOUND ( 'NONE', #30017, .T. ) ;
#13744=DIRECTION ( 'NONE',  ( 0.7071067811865475727, 0.000000000000000000, 0.7071067811865475727 ) ) ;
#13749=CARTESIAN_POINT ( 'NONE',  ( 2.863963203921999767, -1.094488518283999845, 2.815564610575000071 ) ) ;
#13751=FACE_OUTER_BOUND ( 'NONE', #49619, .T. ) ;
#13752=ORIENTED_EDGE ( 'NONE', *, *, #6351, .F. ) ;
#13754=DIRECTION ( 'NONE',  ( 0.000000000000000000, 0.000000000000000000, -1.000000000000000000 ) ) ;
#13756=ORIENTED_EDGE ( 'NONE', *, *, #29377, .F. ) ;
#13758=CARTESIAN_POINT ( 'NONE',  ( 8.190859204290999784, -55.64999999967000122, 7.342331066867000544 ) ) ;
#13760=EDGE_LOOP ( 'NONE', ( #33462, #6139, #28585, #23503 ) ) ;
#13764=CIRCLE ( 'NONE', #21315, 1.250000000000000000 ) ;
#13765=ORIENTED_EDGE ( 'NONE', *, *, #11053, .F. ) ;
#13766=CARTESIAN_POINT ( 'NONE',  ( 0.5319755900005730398, -2.738347930379791517, -3.208410176395029012 ) ) ;
#13767=AXIS2_PLACEMENT_3D ( 'NONE', #14486, #5628, #18645 ) ;
#13769=CARTESIAN_POINT ( 'NONE',  ( 10.07627163191000008, -55.55000000209000177, -7.601397897754999633 ) ) ;
#13770=CARTESIAN_POINT ( 'NONE',  ( -12.85144117169000033, -20.24527983099999773, -1.980464439859999981 ) ) ;
#13773=ADVANCED_FACE ( 'NONE', ( #14341, #4326 ), #17913, .T. ) ;
#13774=ORIENTED_EDGE ( 'NONE', *, *, #29568, .F. ) ;
#13776=CARTESIAN_POINT ( 'NONE',  ( 0.000000000000000000, -55.54999999966999980, -12.50000000000000000 ) ) ;
#13777=DIRECTION ( 'NONE',  ( 0.000000000000000000, 0.000000000000000000, -1.000000000000000000 ) ) ;
#13778=CARTESIAN_POINT ( 'NONE',  ( -0.5200379331666001859, -18.54844303602364164, 10.98772212209854438 ) ) ;
#13779=DIRECTION ( 'NONE',  ( 0.7071067811864980568, 1.533578360404995178E-11, -0.7071067811865969777 ) ) ;
#13780=CARTESIAN_POINT ( 'NONE',  ( 9.396085398178598780, -78.60208333333329733, 7.220923959705271677 ) ) ;
#13784=CARTESIAN_POINT ( 'NONE',  ( -8.958641849965999882, -25.20112647804999995, 8.950065109822000764 ) ) ;
#13786=CARTESIAN_POINT ( 'NONE',  ( -10.26699006316255591, -76.75833333333331154, 5.917523019358029934 ) ) ;
#13790=CARTESIAN_POINT ( 'NONE',  ( -12.48408657659000021, -18.63026141570000149, 1.669508654504000100 ) ) ;
#13791=CARTESIAN_POINT ( 'NONE',  ( 12.51072239526000196, -63.10294702885996543, -0.7871079366006996647 ) ) ;
#13792=CARTESIAN_POINT ( 'NONE',  ( -0.006333666751184999569, -25.33262644299999877, 12.77652491955999992 ) ) ;
#13793=DIRECTION ( 'NONE',  ( 1.894056206342980493E-11, -1.538486802511980436E-07, 0.9999999999999882316 ) ) ;
#13795=CARTESIAN_POINT ( 'NONE',  ( -0.4356580584946000423, -1.352709358523000116, 3.764349720514999831 ) ) ;
#13797=CARTESIAN_POINT ( 'NONE',  ( 10.53003223722000037, -55.47547470607999998, 7.612971414697999428 ) ) ;
#13799=CARTESIAN_POINT ( 'NONE',  ( 12.78015149461000100, -61.10330660662999946, -1.806228889759999845 ) ) ;
#13800=CARTESIAN_POINT ( 'NONE',  ( 7.624341766629000539, -55.53514853726999689, -10.42531125022999916 ) ) ;
#13801=CARTESIAN_POINT ( 'NONE',  ( -10.01235002622999914, -23.29848884437999956, -7.653559626096999580 ) ) ;
#13813=EDGE_CURVE ( 'NONE', #20471, #40525, #55591, .T. ) ;
#13818=CARTESIAN_POINT ( 'NONE',  ( -1.980584515756000030, -60.06485150062000145, -12.76303204342999997 ) ) ;
#13823=AXIS2_PLACEMENT_3D ( 'NONE', #14720, #2053, #45759 ) ;
#13824=CARTESIAN_POINT ( 'NONE',  ( 4.011554133421999957, -1.048748962127999951, -0.3473264786097000067 ) ) ;
#13825=CARTESIAN_POINT ( 'NONE',  ( 5.629119960535821754, -76.46453612599496807, -10.39280916107768959 ) ) ;
#13826=CARTESIAN_POINT ( 'NONE',  ( -9.431008682118280362, -61.60059307736693057, 8.251849285865670680 ) ) ;
#13829=CARTESIAN_POINT ( 'NONE',  ( -0.2678032735318023327, -53.58567224679264029, -12.70526550764705753 ) ) ;
#13833=CARTESIAN_POINT ( 'NONE',  ( -12.60413670417000098, -55.49283319101999723, -1.799502287691000069 ) ) ;
#13835=ORIENTED_EDGE ( 'NONE', *, *, #55067, .T. ) ;
#13836=EDGE_CURVE ( 'NONE', #23858, #378, #37725, .T. ) ;
#13838=CARTESIAN_POINT ( 'NONE',  ( 10.36745710150462330, -60.56601929499611714, -7.635228183650348832 ) ) ;
#13841=CARTESIAN_POINT ( 'NONE',  ( 8.414570695956999913, -60.64999999943950826, 8.414570695956999913 ) ) ;
#13846=CARTESIAN_POINT ( 'NONE',  ( 8.121699804427876757, -24.83626205760389993, -9.841121124182388158 ) ) ;
#13847=B_SPLINE_CURVE_WITH_KNOTS ( 'NONE', 3,
 ( #18761, #15197, #42073, #32309, #28765, #51234, #55061, #10785, #28177, #42370 ),
 .UNSPECIFIED., .F., .F.,
 ( 4, 2, 2, 2, 4 ),
 ( 0.000000000000000000, 0.2500000000000000000, 0.5000000000000000000, 0.7500000000000000000, 1.000000000000000000 ),
 .UNSPECIFIED. ) ;
#13854=CARTESIAN_POINT ( 'NONE',  ( -8.012867221502000703, -78.51278494331999980, 9.287323121044000374 ) ) ;
#13859=CARTESIAN_POINT ( 'NONE',  ( 10.42531125074000009, -18.73514854687000053, 7.624341767140999870 ) ) ;
#13860=ORIENTED_EDGE ( 'NONE', *, *, #2135, .F. ) ;
#13861=CARTESIAN_POINT ( 'NONE',  ( 0.000000000000000000, -23.25000000000000000, 12.00000000000000000 ) ) ;
#13864=VECTOR ( 'NONE', #39891, 1000.000000000000114 ) ;
#13866=CARTESIAN_POINT ( 'NONE',  ( -3.469432447681296328, -3.362854700287415621, -0.6005825324968658840 ) ) ;
#13868=CARTESIAN_POINT ( 'NONE',  ( 7.961052042476000068, -61.33567434991999789, -9.783216378940000624 ) ) ;
#13869=CARTESIAN_POINT ( 'NONE',  ( -11.55418265775999842, -79.02479797882000412, 4.110954701505000308 ) ) ;
#13871=CARTESIAN_POINT ( 'NONE',  ( -12.76303204291999904, -55.53514849259999409, -1.980584515756000030 ) ) ;
#13873=CARTESIAN_POINT ( 'NONE',  ( 11.68679759850510358, -76.82009992810888832, 3.010188169988853524 ) ) ;
#13877=DIRECTION ( 'NONE',  ( 0.000000000000000000, 0.000000000000000000, 1.000000000000000000 ) ) ;
#13878=CARTESIAN_POINT ( 'NONE',  ( 7.635227771886311743, -23.76609606960563070, 10.36745004610104637 ) ) ;
#13885=CARTESIAN_POINT ( 'NONE',  ( 2.844842352609428637, -76.05516034136756787, 11.40062995561528680 ) ) ;
#13888=VERTEX_POINT ( 'NONE', #26673 ) ;
#13890=CARTESIAN_POINT ( 'NONE',  ( 10.69843650790000034, -76.34117774079464880, 6.089250768039999429 ) ) ;
#13893=CARTESIAN_POINT ( 'NONE',  ( -1.001315002179000047, -17.31477588286000113, -12.50000000000000000 ) ) ;
#13894=CARTESIAN_POINT ( 'NONE',  ( 12.50385602704033694, -17.21562691850715865, -0.8579623880475349962 ) ) ;
#13895=CARTESIAN_POINT ( 'NONE',  ( 7.601397897754999633, -60.04999999657000131, 10.07627163191000008 ) ) ;
#13900=CARTESIAN_POINT ( 'NONE',  ( 12.70556836324320926, -16.77227722580009228, 0.2598513551428152102 ) ) ;
#13903=CARTESIAN_POINT ( 'NONE',  ( 12.52785920748583059, -60.59405666895393239, 1.668536824535970631 ) ) ;
#13907=CIRCLE ( 'NONE', #17577, 10.20000000000000107 ) ;
#13909=VECTOR ( 'NONE', #27405, 1000.000000000000114 ) ;
#13914=CARTESIAN_POINT ( 'NONE',  ( -12.54705830248999909, -24.53699017355999956, 1.287129557046000183 ) ) ;
#13915=ORIENTED_EDGE ( 'NONE', *, *, #30353, .F. ) ;
#13919=ORIENTED_EDGE ( 'NONE', *, *, #44976, .T. ) ;
#13921=CARTESIAN_POINT ( 'NONE',  ( 8.252521514711000705, -24.93405767894999769, 9.650901483139000092 ) ) ;
#13922=CARTESIAN_POINT ( 'NONE',  ( 8.588902834722000890, -61.93240111547999760, 9.317946123669999636 ) ) ;
#13927=VERTEX_POINT ( 'NONE', #41442 ) ;
#13928=CARTESIAN_POINT ( 'NONE',  ( -8.894916816479799593, -25.22809132934175835, 9.073484344813371294 ) ) ;
#13929=EDGE_LOOP ( 'NONE', ( #49801, #58345, #8993, #55754 ) ) ;
#13934=CARTESIAN_POINT ( 'NONE',  ( -13.12320710921999911, -76.00574241823001387, -0.02004563557600999926 ) ) ;
#13935=EDGE_CURVE ( 'NONE', #16006, #45077, #43563, .T. ) ;
#13936=DIRECTION ( 'NONE',  ( -1.000000000000000000, 0.000000000000000000, 0.000000000000000000 ) ) ;
#13938=CARTESIAN_POINT ( 'NONE',  ( 7.648026766735999793, -23.25000000582000226, -10.12290050089000104 ) ) ;
#13940=CARTESIAN_POINT ( 'NONE',  ( -10.30458248778999852, -23.76332651811999952, -7.636263891322999875 ) ) ;
#13941=CARTESIAN_POINT ( 'NONE',  ( -8.190836719257360343, -59.98964892062407728, 7.342356150419296235 ) ) ;
#13947=CARTESIAN_POINT ( 'NONE',  ( -0.4254240051736286610, -3.385416666666666075, 3.249999999999997780 ) ) ;
#13948=DIRECTION ( 'NONE',  ( 0.000000000000000000, -1.000000000000000000, -9.096334742604000621E-12 ) ) ;
#13949=CIRCLE ( 'NONE', #23399, 14.00000000000000000 ) ;
#13950=CARTESIAN_POINT ( 'NONE',  ( 9.050966799188000067, -59.94999999969999749, -7.919595949288999570 ) ) ;
#13953=CARTESIAN_POINT ( 'NONE',  ( 12.70556836347999941, -25.22772277227999993, 2.424222353299999887E-09 ) ) ;
#13955=CARTESIAN_POINT ( 'NONE',  ( -1.001315002657000131, -61.48522411647999775, 12.50000000000000000 ) ) ;
#13958=EDGE_CURVE ( 'NONE', #525, #12605, #3039, .T. ) ;
#13961=DIRECTION ( 'NONE',  ( -0.4045849533089092009, -0.8201353736500186509, 0.4045849533089092009 ) ) ;
#13965=LINE ( 'NONE', #55287, #53379 ) ;
#13966=CARTESIAN_POINT ( 'NONE',  ( 3.250000000000000000, -1.850000000000000089, 0.000000000000000000 ) ) ;
#13967=CARTESIAN_POINT ( 'NONE',  ( 0.000000000000000000, -46.43897132165000130, 0.000000000000000000 ) ) ;
#13969=FACE_OUTER_BOUND ( 'NONE', #36285, .T. ) ;
#13970=EDGE_CURVE ( 'NONE', #35427, #46904, #56190, .T. ) ;
#13971=CARTESIAN_POINT ( 'NONE',  ( -5.483474447459000700, -78.90417670422999663, 11.73017812283000083 ) ) ;
#13972=ADVANCED_FACE ( 'NONE', ( #12458 ), #19189, .F. ) ;
#13973=B_SPLINE_SURFACE_WITH_KNOTS ( 'NONE', 3, 3, ( 
 ( #54322, #5011, #13271, #31262, #12972, #18601, #41027, #22428, #30, #17414, #39842, #26845, #58152, #22128, #53732, #8266, #40139, #9153, #17719, #4428, #44875, #8855, #4726, #36002, #26547, #31858, #618, #13568, #54026, #45469, #49899, #49606, #30970, #9444, #27137 ),
 ( #45176, #3839, #57857, #26267, #44280, #35398, #8555, #4129, #55185, #14727, #36879, #2060, #46938, #5876, #23885, #902, #5300, #10321, #41607, #5582, #37174, #54611, #23593, #51068, #1187, #46352, #28299, #50776, #46644, #19465, #10032, #6173, #24476, #55479, #37460 ),
 ( #15027, #15327, #6463, #41902, #10616, #32435, #54891, #42490, #24182, #28013, #1476, #10913, #50480, #33319, #28597, #32725, #23310, #33021, #46060, #42197, #19178, #1767, #9733, #41318, #19760, #37757, #55778, #51355, #28891, #36590, #14149, #32149, #18883, #50188, #27722 ),
 ( #45766, #14440, #20061, #51654, #38048, #16489, #43350, #11204, #48089, #34468, #56356, #30036, #47521, #3203, #20626, #56071, #43645, #7907, #48369, #38627, #52215, #51933, #56643, #2908, #11773, #16201, #25622, #16777, #56929, #52498, #34758, #12056, #2344, #33611, #43931 ) ),
 .UNSPECIFIED., .F., .F., .F.,
 ( 4, 4 ),
 ( 4, 1, 1, 1, 1, 1, 1, 1, 1, 1, 1, 1, 1, 1, 1, 1, 1, 1, 1, 1, 1, 1, 1, 1, 1, 1, 1, 1, 1, 1, 1, 1, 4 ),
 ( -0.02000000000003999967, 1.020000000000000018 ),
 ( 0.4279355161862000156, 0.4461630610136000374, 0.4643906058410000037, 0.4826181506684000255, 0.5008456954957999363, 0.5190732403232000136, 0.5373007851505999799, 0.5555283299780000572, 0.5737558748054000235, 0.5919834196327999898, 0.6102109644601999561, 0.6284385092876000334, 0.6466660541149999997, 0.6648935989424000770, 0.6831211437698000433, 0.7013486885972000096, 0.7195762334245999758, 0.7378037782519999421, 0.7560313230794000194, 0.7742588679067999857, 0.7924864127342000630, 0.8107139575616000293, 0.8289415023890001066, 0.8471690472163999619, 0.8653965920437999282, 0.8836241368712000055, 0.9018516816985999718, 0.9200792265260000491, 0.9383067713534000154, 0.9565343161808000927, 0.9747618610081999480, 0.9929894058356000253, 1.011216950662999992 ),
 .UNSPECIFIED. ) ;
#13977=CARTESIAN_POINT ( 'NONE',  ( 1.980611416589732610, -60.32597731768191096, 12.74335092666149194 ) ) ;
#13979=CARTESIAN_POINT ( 'NONE',  ( -12.54902678216000034, -61.80971938179000347, 0.4616712539285000028 ) ) ;
#13983=ORIENTED_EDGE ( 'NONE', *, *, #57496, .T. ) ;
#13985=CARTESIAN_POINT ( 'NONE',  ( 0.5668640744809375631, -61.71659694886578507, 12.50470739229114692 ) ) ;
#13987=DIRECTION ( 'NONE',  ( 0.000000000000000000, -1.000000000000000000, 0.000000000000000000 ) ) ;
#13988=ORIENTED_EDGE ( 'NONE', *, *, #38950, .F. ) ;
#13994=DIRECTION ( 'NONE',  ( 0.000000000000000000, -1.000000000000000000, 0.000000000000000000 ) ) ;
#13995=CIRCLE ( 'NONE', #52647, 14.00000000000000000 ) ;
#13997=CARTESIAN_POINT ( 'NONE',  ( 0.4450739772392999782, -24.87813214802000061, -12.43586747594999942 ) ) ;
#14000=CARTESIAN_POINT ( 'NONE',  ( -8.784324219567999137, -78.80339885845999959, -8.047797807107999191 ) ) ;
#14002=ORIENTED_EDGE ( 'NONE', *, *, #20260, .F. ) ;
#14003=ORIENTED_EDGE ( 'NONE', *, *, #14664, .T. ) ;
#14005=CARTESIAN_POINT ( 'NONE',  ( -1.668607604570410352, -18.20618368758860584, -12.52787843850897076 ) ) ;
#14011=CARTESIAN_POINT ( 'NONE',  ( -3.259705057564000530, -77.31377916175999587, 12.53941704951999903 ) ) ;
#14013=CARTESIAN_POINT ( 'NONE',  ( -12.60552511010000032, -23.28917723430000208, -1.799501877793999949 ) ) ;
#14014=PLANE ( 'NONE',  #27382 ) ;
#14018=CARTESIAN_POINT ( 'NONE',  ( -11.54010588699839168, -76.71678478382965238, -2.556919625331205204 ) ) ;
#14021=VECTOR ( 'NONE', #45344, 1000.000000000000114 ) ;
#14024=CARTESIAN_POINT ( 'NONE',  ( -2.422546195149999804, -2.247237677196999961, 2.935532677474999907 ) ) ;
#14028=ADVANCED_FACE ( 'NONE', ( #42904 ), #48489, .F. ) ;
#14030=DIRECTION ( 'NONE',  ( 0.000000000000000000, -1.000000000000000000, -1.398881011027999911E-13 ) ) ;
#14032=CARTESIAN_POINT ( 'NONE',  ( 2.062670899361999766, -55.49360215019999742, 12.83044027758000105 ) ) ;
#14034=CARTESIAN_POINT ( 'NONE',  ( -10.59876350475000173, -77.43341004451998799, 7.550195564144000393 ) ) ;
#14038=CARTESIAN_POINT ( 'NONE',  ( 9.538705796123998937, -76.68836589309999852, -8.097544982435998406 ) ) ;
#14039=VERTEX_POINT ( 'NONE', #12179 ) ;
#14040=CARTESIAN_POINT ( 'NONE',  ( -9.723174505940001211, -24.47697504200000296, -7.958760297012999807 ) ) ;
#14044=CARTESIAN_POINT ( 'NONE',  ( 7.627487606609999915, -23.29778595484999926, -10.35845616727999996 ) ) ;
#14047=CARTESIAN_POINT ( 'NONE',  ( 2.863963203921999767, -1.129155184950999979, 2.815564610575000071 ) ) ;
#14063=EDGE_LOOP ( 'NONE', ( #19007, #53052, #54625 ) ) ;
#14064=ORIENTED_EDGE ( 'NONE', *, *, #26142, .F. ) ;
#14065=CARTESIAN_POINT ( 'NONE',  ( -2.256754848263711644, -2.664732714192036500, -2.338051317333970758 ) ) ;
#14067=CARTESIAN_POINT ( 'NONE',  ( -12.85140862673999784, -21.75560170163999985, -1.980464483675000054 ) ) ;
#14075=ADVANCED_FACE ( 'NONE', ( #43479 ), #21034, .F. ) ;
#14077=CIRCLE ( 'NONE', #11274, 0.5000000000000006661 ) ;
#14079=CARTESIAN_POINT ( 'NONE',  ( 10.26699006316251683, -77.09166666666665435, 5.917523019358090330 ) ) ;
#14080=CARTESIAN_POINT ( 'NONE',  ( -0.7999999999999001243, -18.84999999997999964, -12.00000000000000000 ) ) ;
#14081=CARTESIAN_POINT ( 'NONE',  ( 7.653559502261000347, -55.50150862742999891, -10.01234990226999955 ) ) ;
#14083=CARTESIAN_POINT ( 'NONE',  ( 11.75000000000000000, -76.45000000000000284, 0.000000000000000000 ) ) ;
#14084=CARTESIAN_POINT ( 'NONE',  ( 1.980532734072999901, -19.23767313188999850, -12.80090744966999949 ) ) ;
#14087=CARTESIAN_POINT ( 'NONE',  ( -3.075537641221584018, -76.69583333333332575, 11.44417895085269876 ) ) ;
#14089=CARTESIAN_POINT ( 'NONE',  ( -12.61277494329999982, -18.80332099654000189, 1.798398135845000079 ) ) ;
#14090=CARTESIAN_POINT ( 'NONE',  ( 13.13047446164998711, -59.58578169018999660, -0.8260994316375004365 ) ) ;
#14091=CARTESIAN_POINT ( 'NONE',  ( -1.890224871707000043, -23.74789248015000354, 12.68696160873999901 ) ) ;
#14092=CARTESIAN_POINT ( 'NONE',  ( 12.00000000112311227, -79.25000000000001421, -1.256637052497524998 ) ) ;
#14094=CARTESIAN_POINT ( 'NONE',  ( 2.171457335693999902, -1.642097686686999847, -3.105636093276999965 ) ) ;
#14095=EDGE_CURVE ( 'NONE', #56909, #12948, #42213, .T. ) ;
#14097=CARTESIAN_POINT ( 'NONE',  ( 1.532229593839658177, -54.67701036644005086, -12.51228690871818117 ) ) ;
#14098=CARTESIAN_POINT ( 'NONE',  ( 10.24996238029999951, -57.04828923575999511, 7.705119999435999567 ) ) ;
#14099=CARTESIAN_POINT ( 'NONE',  ( -1.933650113856000052, -23.40786253026000097, -12.70909635754000000 ) ) ;
#14100=EDGE_CURVE ( 'NONE', #38037, #47780, #10376, .T. ) ;
#14102=CARTESIAN_POINT ( 'NONE',  ( 2.067335093441000193, -2.868853494984999752, 2.806303441592000070 ) ) ;
#14105=DIRECTION ( 'NONE',  ( 0.7071067811865969777, -1.534448722697995070E-11, -0.7071067811864980568 ) ) ;
#14108=VERTEX_POINT ( 'NONE', #21606 ) ;
#14112=EDGE_CURVE ( 'NONE', #52197, #39336, #56566, .T. ) ;
#14117=VECTOR ( 'NONE', #14557, 1000.000000000000000 ) ;
#14118=CARTESIAN_POINT ( 'NONE',  ( 5.420640129221999892, -77.59535537052001075, 11.42023903890000014 ) ) ;
#14124=DIRECTION ( 'NONE',  ( 0.000000000000000000, 0.000000000000000000, -1.000000000000000000 ) ) ;
#14127=EDGE_LOOP ( 'NONE', ( #5780, #11970, #30092, #12320, #18613, #6514, #8455, #14523, #3692, #21243, #35687, #15991 ) ) ;
#14129=CARTESIAN_POINT ( 'NONE',  ( -1.667936697358999965, -19.23537109840999904, 12.53241208775999915 ) ) ;
#14130=ORIENTED_EDGE ( 'NONE', *, *, #33717, .F. ) ;
#14131=LINE ( 'NONE', #27704, #1930 ) ;
#14134=CYLINDRICAL_SURFACE ( 'NONE', #57210, 1.750000000000001332 ) ;
#14140=EDGE_CURVE ( 'NONE', #4628, #29025, #25459, .T. ) ;
#14142=CARTESIAN_POINT ( 'NONE',  ( -10.68064082909000057, -77.44512210326000456, 7.608522161463999289 ) ) ;
#14143=CARTESIAN_POINT ( 'NONE',  ( -1.342463812738999916E-14, -80.75000000002938805, -13.94999999997000018 ) ) ;
#14144=B_SPLINE_CURVE_WITH_KNOTS ( 'NONE', 3,
 ( #36465, #28178, #41777, #54492, #41193, #782, #14315, #41483, #18762, #54773, #1069, #32310, #14609, #19056, #37045, #19346, #55946, #46817 ),
 .UNSPECIFIED., .F., .F.,
 ( 4, 2, 2, 2, 2, 2, 2, 2, 4 ),
 ( 0.000000000000000000, 0.06249999999999433786, 0.1249999999999886757, 0.2499999999999873435, 0.4999999999999846789, 0.7499999999999829026, 0.8124999999999845679, 0.8749999999999862332, 1.000000000000000000 ),
 .UNSPECIFIED. ) ;
#14149=CARTESIAN_POINT ( 'NONE',  ( 1.328206530128999807, -76.61626955243001191, -12.23810562210000086 ) ) ;
#14152=CARTESIAN_POINT ( 'NONE',  ( -1.304001331138744835, -2.254477797239900827, 3.271227269354120892 ) ) ;
#14154=CARTESIAN_POINT ( 'NONE',  ( 8.652376385632999600, -62.06264602932999708, -9.414489258850998965 ) ) ;
#14155=CARTESIAN_POINT ( 'NONE',  ( -9.356096982537000173, -78.99605726074999268, 7.928589704419000128 ) ) ;
#14157=CARTESIAN_POINT ( 'NONE',  ( 12.71162569433669276, -17.76025712763402709, -1.720540999442599972 ) ) ;
#14159=CARTESIAN_POINT ( 'NONE',  ( -12.01728813451669176, -77.04247429093877031, 1.133778321476297535 ) ) ;
#14160=CARTESIAN_POINT ( 'NONE',  ( 6.617191270873545861, -76.11991961324837064, -11.22154644849154081 ) ) ;
#14161=ORIENTED_EDGE ( 'NONE', *, *, #16105, .F. ) ;
#14165=DIRECTION ( 'NONE',  ( -1.000000000000000000, 0.000000000000000000, 0.000000000000000000 ) ) ;
#14171=CARTESIAN_POINT ( 'NONE',  ( 2.294676624047414126, -76.05915692578440712, 11.52361598551882516 ) ) ;
#14174=VERTEX_POINT ( 'NONE', #49357 ) ;
#14178=CIRCLE ( 'NONE', #42479, 1.250000000000000000 ) ;
#14180=EDGE_CURVE ( 'NONE', #41402, #38250, #22638, .T. ) ;
#14181=DIRECTION ( 'NONE',  ( 0.000000000000000000, -1.000000000000000000, 0.000000000000000000 ) ) ;
#14183=LINE ( 'NONE', #50512, #2909 ) ;
#14184=CARTESIAN_POINT ( 'NONE',  ( 9.830798712624998714, -17.90910918523000106, -7.765013391413999599 ) ) ;
#14185=CARTESIAN_POINT ( 'NONE',  ( 14.00000000000000000, -80.70000000000000284, -1.714505518806294638E-15 ) ) ;
#14186=ORIENTED_EDGE ( 'NONE', *, *, #56179, .T. ) ;
#14188=CARTESIAN_POINT ( 'NONE',  ( 12.70395600760365795, -17.39327811306810645, 1.447166682387068137 ) ) ;
#14192=CARTESIAN_POINT ( 'NONE',  ( 12.50728630775800809, -61.79975539279633523, -0.1757873579559299515 ) ) ;
#14193=DIRECTION ( 'NONE',  ( -1.000000000000000000, 0.000000000000000000, 0.000000000000000000 ) ) ;
#14194=CIRCLE ( 'NONE', #3825, 0.5000000000000004441 ) ;
#14196=CYLINDRICAL_SURFACE ( 'NONE', #47859, 1.750000000000000000 ) ;
#14199=CARTESIAN_POINT ( 'NONE',  ( 12.70451796513349763, -53.62354927360125600, -0.5205401192079295303 ) ) ;
#14201=VERTEX_POINT ( 'NONE', #58206 ) ;
#14204=ORIENTED_EDGE ( 'NONE', *, *, #50879, .F. ) ;
#14205=DIRECTION ( 'NONE',  ( 0.000000000000000000, -1.000000000000000000, 0.000000000000000000 ) ) ;
#14206=CARTESIAN_POINT ( 'NONE',  ( 7.633478499826000352, -23.20098177597000344, 10.36292345935000014 ) ) ;
#14208=EDGE_CURVE ( 'NONE', #18144, #20659, #19779, .T. ) ;
#14209=CARTESIAN_POINT ( 'NONE',  ( 7.761030428359000588, -60.88151201342000007, 9.835168816244998169 ) ) ;
#14214=EDGE_LOOP ( 'NONE', ( #15227, #51567, #51259 ) ) ;
#14220=CARTESIAN_POINT ( 'NONE',  ( -8.485281374238999419, -59.94999999967000548, 8.485281374238999419 ) ) ;
#14227=CARTESIAN_POINT ( 'NONE',  ( 1.667916687244999974, -60.09849137196000157, -12.49168433582000226 ) ) ;
#14230=ORIENTED_EDGE ( 'NONE', *, *, #10590, .F. ) ;
#14232=AXIS2_PLACEMENT_3D ( 'NONE', #52428, #25549, #3132 ) ;
#14236=CARTESIAN_POINT ( 'NONE',  ( -10.00831378477999856, -18.62769332291999902, 7.646786280044999273 ) ) ;
#14238=CARTESIAN_POINT ( 'NONE',  ( 1.538071403320016461, -78.43541666666665435, -11.74999999999999822 ) ) ;
#14240=CARTESIAN_POINT ( 'NONE',  ( 1.107543465625472345, -3.400486210132132481, -3.341007379328037707 ) ) ;
#14246=ORIENTED_EDGE ( 'NONE', *, *, #45154, .T. ) ;
#14248=CARTESIAN_POINT ( 'NONE',  ( -9.546819346421999697, -24.68527546640000025, 8.130850183241999929 ) ) ;
#14251=DIRECTION ( 'NONE',  ( 0.000000000000000000, 1.000000000000000000, 0.000000000000000000 ) ) ;
#14253=FACE_OUTER_BOUND ( 'NONE', #36729, .T. ) ;
#14258=CYLINDRICAL_SURFACE ( 'NONE', #50995, 0.5000000000000004441 ) ;
#14267=CARTESIAN_POINT ( 'NONE',  ( -5.787029044103459974, -78.56271173619120418, 10.31969192858259099 ) ) ;
#14271=EDGE_CURVE ( 'NONE', #31547, #9471, #11536, .T. ) ;
#14274=ORIENTED_EDGE ( 'NONE', *, *, #37862, .F. ) ;
#14275=ORIENTED_EDGE ( 'NONE', *, *, #34220, .T. ) ;
#14277=AXIS2_PLACEMENT_3D ( 'NONE', #31126, #16423, #12276 ) ;
#14283=CARTESIAN_POINT ( 'NONE',  ( 0.000000000000000000, -18.84999999999999787, 11.89999999977000122 ) ) ;
#14285=ADVANCED_FACE ( 'NONE', ( #3250, #56402 ), #20385, .T. ) ;
#14291=DIRECTION ( 'NONE',  ( -0.9999548435846228323, 0.000000000000000000, -0.009503199022040218977 ) ) ;
#14294=CARTESIAN_POINT ( 'NONE',  ( 12.50000000000000000, -23.25000000000000000, 0.000000000000000000 ) ) ;
#14298=CARTESIAN_POINT ( 'NONE',  ( 12.49589899905999957, -77.14726523887000553, -3.422742383397000321 ) ) ;
#14301=CARTESIAN_POINT ( 'NONE',  ( -1.004305231718999991, -3.500000000000000000, 3.090933677959000203 ) ) ;
#14302=CARTESIAN_POINT ( 'NONE',  ( -3.045010225283240501, -76.59478582781956391, 11.45375641726638705 ) ) ;
#14306=DIRECTION ( 'NONE',  ( -0.9999548435846228323, 0.000000000000000000, -0.009503199022040218977 ) ) ;
#14309=CARTESIAN_POINT ( 'NONE',  ( 0.000000000000000000, -4.000000000000000000, 0.000000000000000000 ) ) ;
#14311=CARTESIAN_POINT ( 'NONE',  ( -3.796701970596999764, -2.811752266991999871, 0.2667143827384000354 ) ) ;
#14312=DIRECTION ( 'NONE',  ( 0.000000000000000000, -1.000000000000000000, 0.000000000000000000 ) ) ;
#14313=ORIENTED_EDGE ( 'NONE', *, *, #9108, .T. ) ;
#14315=CARTESIAN_POINT ( 'NONE',  ( 8.111636311571439606, -60.31614597266276689, -7.429974109831698925 ) ) ;
#14316=FACE_OUTER_BOUND ( 'NONE', #41868, .T. ) ;
#14318=CONICAL_SURFACE ( 'NONE', #39762, 12.84999999993999964, 0.7853981633972997312 ) ;
#14319=CARTESIAN_POINT ( 'NONE',  ( 1.750000000001000089, -18.74999999009000007, -12.56594317857000043 ) ) ;
#14321=AXIS2_PLACEMENT_3D ( 'NONE', #57611, #54865, #45443 ) ;
#14323=CARTESIAN_POINT ( 'NONE',  ( 9.724573642157064768, -78.49540306821776880, 6.592917362395923853 ) ) ;
#14324=ORIENTED_EDGE ( 'NONE', *, *, #53342, .T. ) ;
#14325=LINE ( 'NONE', #29072, #43872 ) ;
#14329=CARTESIAN_POINT ( 'NONE',  ( 7.668949790003000366, -22.77129148951999937, -10.21381326472000062 ) ) ;
#14331=CARTESIAN_POINT ( 'NONE',  ( -0.4617212151683000032, -1.201502266992000134, 3.989551193614000013 ) ) ;
#14337=LINE ( 'NONE', #9346, #32278 ) ;
#14339=ORIENTED_EDGE ( 'NONE', *, *, #44361, .T. ) ;
#14341=FACE_BOUND ( 'NONE', #22309, .T. ) ;
#14344=ORIENTED_EDGE ( 'NONE', *, *, #33961, .T. ) ;
#14346=EDGE_LOOP ( 'NONE', ( #55920, #52345, #38832, #28574, #51789 ) ) ;
#14348=CARTESIAN_POINT ( 'NONE',  ( -3.220112201118367157, -2.612390273010157138, -0.4917168695184507277 ) ) ;
#14349=ORIENTED_EDGE ( 'NONE', *, *, #9108, .F. ) ;
#14360=DIRECTION ( 'NONE',  ( -1.000000000000000000, 0.000000000000000000, 0.000000000000000000 ) ) ;
#14362=LINE ( 'NONE', #10244, #49521 ) ;
#14363=TOROIDAL_SURFACE ( 'NONE', #2134, 1.250000000000000000, 0.5000000000000000000 ) ;
#14367=CARTESIAN_POINT ( 'NONE',  ( 3.747061555208543115, -76.54862165773606364, 11.14272879161189600 ) ) ;
#14369=DIRECTION ( 'NONE',  ( -0.7071067811865474617, 0.000000000000000000, -0.7071067811865474617 ) ) ;
#14371=CARTESIAN_POINT ( 'NONE',  ( 6.040704753788179282, -78.11963179743526098, -10.46256944259450883 ) ) ;
#14373=AXIS2_PLACEMENT_3D ( 'NONE', #51619, #32987, #2313 ) ;
#14374=CARTESIAN_POINT ( 'NONE',  ( -11.75000000000000000, -76.20000000000000284, -1.391479524197000231E-14 ) ) ;
#14379=VECTOR ( 'NONE', #23414, 1000.000000000000000 ) ;
#14380=CARTESIAN_POINT ( 'NONE',  ( -3.237660394099999728, -1.425056440564000049, 1.969183889131999932 ) ) ;
#14381=CARTESIAN_POINT ( 'NONE',  ( 10.38646360829999971, -59.57795407677000554, 7.655555357447999754 ) ) ;
#14382=CARTESIAN_POINT ( 'NONE',  ( -1.576170184332999824, -24.16086967216000048, -12.55466896104999996 ) ) ;
#14383=FACE_OUTER_BOUND ( 'NONE', #15158, .T. ) ;
#14384=CARTESIAN_POINT ( 'NONE',  ( -0.8748660084214999744, -2.439568282128000032, 3.373992119635000009 ) ) ;
#14385=CARTESIAN_POINT ( 'NONE',  ( -0.8537148449507000469, -54.09501854057999992, -12.43377424869000158 ) ) ;
#14389=CARTESIAN_POINT ( 'NONE',  ( 7.624341764923000753, -18.73514850530999709, 10.42531124853000080 ) ) ;
#14392=CARTESIAN_POINT ( 'NONE',  ( -1.072796787723000023, -76.37353418688999795, -12.01405072592999979 ) ) ;
#14393=ORIENTED_EDGE ( 'NONE', *, *, #18790, .T. ) ;
#14400=CARTESIAN_POINT ( 'NONE',  ( 10.11462613662204646, -23.38712935484991107, -7.639894945624773115 ) ) ;
#14401=CARTESIAN_POINT ( 'NONE',  ( -3.250000000000000000, -1.500000000000000000, 0.000000000000000000 ) ) ;
#14402=CARTESIAN_POINT ( 'NONE',  ( 3.373947135798999852, -1.509678536415000050, -2.197671934948000061 ) ) ;
#14405=VERTEX_POINT ( 'NONE', #43977 ) ;
#14406=CARTESIAN_POINT ( 'NONE',  ( -1.811016405462518852, -54.73826444593738216, -12.71771640060642206 ) ) ;
#14409=ORIENTED_EDGE ( 'NONE', *, *, #31239, .T. ) ;
#14410=AXIS2_PLACEMENT_3D ( 'NONE', #44784, #4337, #50104 ) ;
#14411=CYLINDRICAL_SURFACE ( 'NONE', #41583, 10.20000000000000107 ) ;
#14413=ORIENTED_EDGE ( 'NONE', *, *, #90, .F. ) ;
#14416=CARTESIAN_POINT ( 'NONE',  ( 7.958763982157000427, -54.32301960771999916, 9.723170657500999070 ) ) ;
#14420=CARTESIAN_POINT ( 'NONE',  ( 12.50386483992548570, -24.78505343634600777, -0.8574420492259948734 ) ) ;
#14423=PRESENTATION_STYLE_ASSIGNMENT (( #4994 ) ) ;
#14426=FACE_OUTER_BOUND ( 'NONE', #22515, .T. ) ;
#14427=LINE ( 'NONE', #18586, #20206 ) ;
#14428=ADVANCED_FACE ( 'NONE', ( #35983 ), #49813, .F. ) ;
#14429=CARTESIAN_POINT ( 'NONE',  ( -12.77302471391999994, -24.72230123305000049, -1.481949986259999852 ) ) ;
#14434=FACE_OUTER_BOUND ( 'NONE', #34841, .T. ) ;
#14435=EDGE_CURVE ( 'NONE', #11113, #50856, #1340, .T. ) ;
#14438=EDGE_LOOP ( 'NONE', ( #44258, #48580, #29276, #48914, #49489 ) ) ;
#14439=CARTESIAN_POINT ( 'NONE',  ( 0.000000000000000000, 4.040000000000000036, 0.000000000000000000 ) ) ;
#14440=CARTESIAN_POINT ( 'NONE',  ( 12.02702378446000075, -75.68921984486000554, -1.341316611471999876 ) ) ;
#14443=CARTESIAN_POINT ( 'NONE',  ( -2.546061316244721873, -2.288581701949032876, 2.429709843700893490 ) ) ;
#14445=CARTESIAN_POINT ( 'NONE',  ( -10.39285214024000048, -78.43813172011999768, 6.510605926401999533 ) ) ;
#14449=CARTESIAN_POINT ( 'NONE',  ( 10.11462613664634347, -60.18712935448241552, -7.639894945646048541 ) ) ;
#14450=CARTESIAN_POINT ( 'NONE',  ( 7.572826708286753750, -77.22926875571705807, -9.331956626295818680 ) ) ;
#14452=TOROIDAL_SURFACE ( 'NONE', #10683, 17.50000000000000000, 5.000000000000000000 ) ;
#14454=B_SPLINE_CURVE_WITH_KNOTS ( 'NONE', 3,
 ( #26765, #53351, #9072, #27059, #17052, #48932, #26470, #12616, #53952, #40056, #250, #30898, #8191, #13778, #3760, #49822, #27357, #36222 ),
 .UNSPECIFIED., .F., .F.,
 ( 4, 2, 2, 2, 2, 2, 2, 2, 4 ),
 ( 0.000000000000000000, 0.06250000000000160982, 0.1250000000000032196, 0.2500000000000014433, 0.4999999999999981126, 0.7499999999999947820, 0.8124999999999947820, 0.8749999999999948930, 1.000000000000000000 ),
 .UNSPECIFIED. ) ;
#14460=CARTESIAN_POINT ( 'NONE',  ( 7.644093100845071653, -23.52380578988460513, 10.09634101412665075 ) ) ;
#14464=CARTESIAN_POINT ( 'NONE',  ( 7.257927454905483522, -76.02152169444083540, 9.258411468306171344 ) ) ;
#14467=EDGE_LOOP ( 'NONE', ( #57382, #14858, #46854, #27186, #28, #35028 ) ) ;
#14469=LINE ( 'NONE', #54916, #4043 ) ;
#14471=DIRECTION ( 'NONE',  ( 0.000000000000000000, 1.000000000000000000, 0.000000000000000000 ) ) ;
#14475=CARTESIAN_POINT ( 'NONE',  ( 0.000000000000000000, -55.54999999966999980, 12.50000000000000000 ) ) ;
#14476=CARTESIAN_POINT ( 'NONE',  ( 8.252512830340000605, -17.06594982557999884, -9.650910120430999939 ) ) ;
#14477=CARTESIAN_POINT ( 'NONE',  ( -7.714303428875997959, -52.49705297113997204, -12.53545825868000385 ) ) ;
#14478=ORIENTED_EDGE ( 'NONE', *, *, #6294, .T. ) ;
#14481=DIRECTION ( 'NONE',  ( -0.9999463328794432337, 0.000000000000000000, 0.01036008498777044214 ) ) ;
#14482=DIRECTION ( 'NONE',  ( 0.000000000000000000, -3.446666965303000135E-11, -1.000000000000000000 ) ) ;
#14483=CARTESIAN_POINT ( 'NONE',  ( -1.629962280006342690, -76.83873742058555933, 11.96830011435914365 ) ) ;
#14485=CARTESIAN_POINT ( 'NONE',  ( 12.50000000000000000, -61.48359816765000119, 1.003641516062000250 ) ) ;
#14486=CARTESIAN_POINT ( 'NONE',  ( -1.823750004803999641E-14, -80.79999999999999716, 0.000000000000000000 ) ) ;
#14487=CARTESIAN_POINT ( 'NONE',  ( 10.45205659047000069, -22.76232685227000019, 7.651160337221999619 ) ) ;
#14491=VECTOR ( 'NONE', #1291, 1000.000000000000000 ) ;
#14492=CARTESIAN_POINT ( 'NONE',  ( 0.000000000000000000, -62.90094976977999863, 0.000000000000000000 ) ) ;
#14493=ORIENTED_EDGE ( 'NONE', *, *, #26277, .T. ) ;
#14494=ORIENTED_EDGE ( 'NONE', *, *, #38573, .T. ) ;
#14497=ADVANCED_FACE ( 'NONE', ( #46041 ), #6587, .T. ) ;
#14502=CARTESIAN_POINT ( 'NONE',  ( 10.53494356941000021, -60.02715052954999919, 7.618393677181999557 ) ) ;
#14506=CARTESIAN_POINT ( 'NONE',  ( 1.787953089535764484, -1.772425210045708521, -2.745890603803126329 ) ) ;
#14507=EDGE_CURVE ( 'NONE', #37067, #53695, #22998, .T. ) ;
#14510=ORIENTED_EDGE ( 'NONE', *, *, #10448, .F. ) ;
#14515=CARTESIAN_POINT ( 'NONE',  ( -9.850513606030963487, -17.69492088480771841, -7.836738268704446675 ) ) ;
#14516=CARTESIAN_POINT ( 'NONE',  ( -0.5440519240141012958, -2.111768684982749278, -3.229414189797041423 ) ) ;
#14520=CARTESIAN_POINT ( 'NONE',  ( -7.753906807039999904, -24.28933445982999828, -10.31979621049999807 ) ) ;
#14521=CARTESIAN_POINT ( 'NONE',  ( 12.60413652829999975, -55.49283065365000311, -1.799502287743000029 ) ) ;
#14523=ORIENTED_EDGE ( 'NONE', *, *, #25016, .F. ) ;
#14528=CARTESIAN_POINT ( 'NONE',  ( -9.992014434680999813, -17.83915351714000153, 7.762970980311999725 ) ) ;
#14529=CARTESIAN_POINT ( 'NONE',  ( 5.917523019358082337, -78.46666666666666856, -10.26699006316252394 ) ) ;
#14531=ADVANCED_FACE ( 'NONE', ( #1458 ), #49882, .F. ) ;
#14532=CARTESIAN_POINT ( 'NONE',  ( 3.127772079701002017, -2.541048934001464144, 1.756767877748572459 ) ) ;
#14533=CARTESIAN_POINT ( 'NONE',  ( 10.01235002620999914, -55.50151115525000023, -7.653559626076999578 ) ) ;
#14538=ORIENTED_EDGE ( 'NONE', *, *, #9493, .F. ) ;
#14541=CARTESIAN_POINT ( 'NONE',  ( -2.160078058180999960, -2.884790208251000188, -3.326435979223000050 ) ) ;
#14545=CARTESIAN_POINT ( 'NONE',  ( 7.619389973898000434, -23.40786254230999930, -10.35398617733999949 ) ) ;
#14548=CARTESIAN_POINT ( 'NONE',  ( -8.803761571499403971, -53.58431590319399618, -9.164326402776838520 ) ) ;
#14551=CARTESIAN_POINT ( 'NONE',  ( -10.45205659047000069, -22.76232685227000019, -7.651160337221999619 ) ) ;
#14552=EDGE_CURVE ( 'NONE', #12597, #37604, #14131, .T. ) ;
#14553=CARTESIAN_POINT ( 'NONE',  ( -10.18847629493000007, -78.54730665117000399, -7.991150893161999669 ) ) ;
#14557=DIRECTION ( 'NONE',  ( 0.000000000000000000, 1.000000000000000000, -3.788597347406000047E-11 ) ) ;
#14559=CARTESIAN_POINT ( 'NONE',  ( -13.89248034750000116, -32.39159251014999796, -2.632538494498000187E-05 ) ) ;
#14560=DIRECTION ( 'NONE',  ( -1.590618475122999970E-12, 1.000000000000000000, 3.446049153258000297E-10 ) ) ;
#14562=ORIENTED_EDGE ( 'NONE', *, *, #38137, .F. ) ;
#14564=DIRECTION ( 'NONE',  ( 1.000000000000000000, 0.000000000000000000, 0.000000000000000000 ) ) ;
#14566=CIRCLE ( 'NONE', #24012, 1.250000000000000000 ) ;
#14569=VERTEX_POINT ( 'NONE', #9426 ) ;
#14572=EDGE_LOOP ( 'NONE', ( #42540, #11296, #16521, #14782, #6072 ) ) ;
#14574=CARTESIAN_POINT ( 'NONE',  ( -10.03847181063980365, -55.00634590446541949, -7.678636148863311917 ) ) ;
#14578=AXIS2_PLACEMENT_3D ( 'NONE', #27550, #50603, #27841 ) ;
#14582=ORIENTED_EDGE ( 'NONE', *, *, #35938, .T. ) ;
#14588=CARTESIAN_POINT ( 'NONE',  ( 1.931736162949456714, -60.56670395682250074, -12.72978979893091100 ) ) ;
#14592=CARTESIAN_POINT ( 'NONE',  ( 6.777770385731999525, -76.50513797953000505, -9.662258766526001352 ) ) ;
#14594=CARTESIAN_POINT ( 'NONE',  ( -12.83044027760000105, -23.30639784948999704, -2.062670899361999766 ) ) ;
#14595=CARTESIAN_POINT ( 'NONE',  ( -8.645873396781713183, -76.64070860396672913, 7.966348362312300146 ) ) ;
#14599=CARTESIAN_POINT ( 'NONE',  ( -1.750000000001000089, -23.25000000990999993, -12.56594317857000043 ) ) ;
#14602=EDGE_CURVE ( 'NONE', #40041, #43983, #48351, .T. ) ;
#14605=CARTESIAN_POINT ( 'NONE',  ( 2.113064247614999669, -3.523836441412999676, -3.165785623842000351 ) ) ;
#14606=CARTESIAN_POINT ( 'NONE',  ( 0.000000000000000000, -60.04999999966999980, 12.50000000000000000 ) ) ;
#14607=EDGE_LOOP ( 'NONE', ( #47260, #34229, #50775 ) ) ;
#14608=CARTESIAN_POINT ( 'NONE',  ( 1.230457122658317193, -78.93333333333330870, -11.74999999999977263 ) ) ;
#14609=CARTESIAN_POINT ( 'NONE',  ( 7.434020715870190088, -60.31691643837059047, -8.107762507646533834 ) ) ;
#14610=CARTESIAN_POINT ( 'NONE',  ( 9.393805349124416892, -77.49942542969233727, 7.217729611353487229 ) ) ;
#14614=DIRECTION ( 'NONE',  ( 0.000000000000000000, 1.000000000000000000, 0.000000000000000000 ) ) ;
#14617=ADVANCED_FACE ( 'NONE', ( #31991 ), #45608, .F. ) ;
#14619=LINE ( 'NONE', #42664, #25932 ) ;
#14622=DIRECTION ( 'NONE',  ( 0.000000000000000000, 1.000000000000000000, 0.000000000000000000 ) ) ;
#14628=DIRECTION ( 'NONE',  ( -0.7071067811865474617, 0.000000000000000000, 0.7071067811865474617 ) ) ;
#14629=CARTESIAN_POINT ( 'NONE',  ( -12.80000000000000071, -6.000000000000000000, 0.000000000000000000 ) ) ;
#14632=ORIENTED_EDGE ( 'NONE', *, *, #35515, .T. ) ;
#14634=CARTESIAN_POINT ( 'NONE',  ( -12.50000000000000000, -61.48359816765000119, -1.003641516062000250 ) ) ;
#14635=FACE_OUTER_BOUND ( 'NONE', #34315, .T. ) ;
#14638=ORIENTED_EDGE ( 'NONE', *, *, #23512, .F. ) ;
#14642=CARTESIAN_POINT ( 'NONE',  ( 1.250000000000000000, -23.25000000000000000, -12.00000000000000000 ) ) ;
#14648=CIRCLE ( 'NONE', #35360, 12.57042253521000141 ) ;
#14652=CARTESIAN_POINT ( 'NONE',  ( 10.03482481951295391, -79.24652767382275442, 6.603860533736427563 ) ) ;
#14654=CARTESIAN_POINT ( 'NONE',  ( -9.431008681915484360, -24.80059307780060252, 8.251849286025537467 ) ) ;
#14655=CARTESIAN_POINT ( 'NONE',  ( -7.626500777253000685, -60.11584731951999316, -10.35747145894000099 ) ) ;
#14657=CARTESIAN_POINT ( 'NONE',  ( 4.510718562000938903, -76.54328005551209912, 10.84945785253482065 ) ) ;
#14663=CARTESIAN_POINT ( 'NONE',  ( -12.54715396801999994, -17.46815137273999952, 1.292200816715999956 ) ) ;
#14664=EDGE_CURVE ( 'NONE', #26037, #13102, #54712, .T. ) ;
#14667=DIRECTION ( 'NONE',  ( -0.7071067811864975017, -0.7071067811865974218, 1.156400220097994687E-08 ) ) ;
#14669=CARTESIAN_POINT ( 'NONE',  ( -9.963467980718000661, -60.48274967040000405, -7.659239661670000032 ) ) ;
#14671=CARTESIAN_POINT ( 'NONE',  ( 12.71106812363992766, -24.25135172970251674, -1.717582538846509799 ) ) ;
#14673=FACE_OUTER_BOUND ( 'NONE', #8324, .T. ) ;
#14674=CARTESIAN_POINT ( 'NONE',  ( 0.6744326473074000461, -2.684874118045999847, -3.419700858360999796 ) ) ;
#14675=CARTESIAN_POINT ( 'NONE',  ( 12.54980660768000078, -25.04777352165000082, -0.05651102257795000139 ) ) ;
#14677=DIRECTION ( 'NONE',  ( 1.000000000000000000, 0.000000000000000000, 0.000000000000000000 ) ) ;
#14680=CARTESIAN_POINT ( 'NONE',  ( -11.87662555441000123, -76.76958523746999674, -2.105724559057000178 ) ) ;
#14681=ORIENTED_EDGE ( 'NONE', *, *, #47821, .T. ) ;
#14682=EDGE_CURVE ( 'NONE', #34093, #8523, #34879, .T. ) ;
#14685=CARTESIAN_POINT ( 'NONE',  ( -7.648026766733999615, -18.74999999413999774, -10.12290050089000104 ) ) ;
#14686=CARTESIAN_POINT ( 'NONE',  ( 12.77649732931999971, -62.10828417218999675, -0.06479631635404999035 ) ) ;
#14688=CARTESIAN_POINT ( 'NONE',  ( 9.850507815892393992, -24.30508874547875919, -7.836744050302931974 ) ) ;
#14693=EDGE_LOOP ( 'NONE', ( #14246, #54042, #49956, #36203, #41297, #11281 ) ) ;
#14695=CARTESIAN_POINT ( 'NONE',  ( 0.2584144827513251697, -53.57154603042778263, -12.70558781483102884 ) ) ;
#14699=CIRCLE ( 'NONE', #20363, 14.00000000000000000 ) ;
#14702=EDGE_CURVE ( 'NONE', #245, #10285, #3780, .T. ) ;
#14707=CARTESIAN_POINT ( 'NONE',  ( 9.355938762769536510, -61.97483710998693596, -8.610912454485829315 ) ) ;
#14712=ORIENTED_EDGE ( 'NONE', *, *, #54184, .F. ) ;
#14713=CARTESIAN_POINT ( 'NONE',  ( 12.61271781517999990, -55.60306329017999616, 1.798333084008999938 ) ) ;
#14714=CARTESIAN_POINT ( 'NONE',  ( 8.532660243322236937, -25.12798380540222709, -9.433531203469305737 ) ) ;
#14715=VERTEX_POINT ( 'NONE', #22859 ) ;
#14716=CARTESIAN_POINT ( 'NONE',  ( -12.66316452095000145, -25.17866137669000182, 0.04044945982123000078 ) ) ;
#14717=ADVANCED_FACE ( 'NONE', ( #43917 ), #8278, .F. ) ;
#14719=DIRECTION ( 'NONE',  ( 0.000000000000000000, -1.000000000000000000, 0.000000000000000000 ) ) ;
#14720=CARTESIAN_POINT ( 'NONE',  ( 7.247844507162001015, -55.54999999966999980, 9.722718241315000398 ) ) ;
#14721=CARTESIAN_POINT ( 'NONE',  ( -1.750000000000000000, -18.75000000310999937, -12.50000000000000000 ) ) ;
#14727=CARTESIAN_POINT ( 'NONE',  ( -11.91862232004000077, -75.99721375889998853, 3.079279237876999531 ) ) ;
#14728=TOROIDAL_SURFACE ( 'NONE', #46806, 13.50000000000000000, 0.5000000000000000000 ) ;
#14729=CARTESIAN_POINT ( 'NONE',  ( -3.505468337749547914, -2.356789511367288092, -0.3314898072761500725 ) ) ;
#14730=CARTESIAN_POINT ( 'NONE',  ( -10.12290050255000118, -60.04999997790999799, 7.648026768390999486 ) ) ;
#14731=CARTESIAN_POINT ( 'NONE',  ( -3.911342194028000208, -78.58183531049999715, -11.62327352135999980 ) ) ;
#14733=VECTOR ( 'NONE', #29416, 1000.000000000000000 ) ;
#14737=CARTESIAN_POINT ( 'NONE',  ( -6.768773376071942849, -78.12766118154397077, -9.992519656028999719 ) ) ;
#14740=ORIENTED_EDGE ( 'NONE', *, *, #24334, .F. ) ;
#14743=CARTESIAN_POINT ( 'NONE',  ( 7.610716808838798642, -23.52015489479942190, 10.41172350877303820 ) ) ;
#14744=CARTESIAN_POINT ( 'NONE',  ( 11.75000000000000000, -77.04999999999999716, 0.000000000000000000 ) ) ;
#14745=CARTESIAN_POINT ( 'NONE',  ( 1.930008848924000153, -2.712975590836000261, 3.173250220514999942 ) ) ;
#14748=CARTESIAN_POINT ( 'NONE',  ( -9.758470251469047341, -76.15243675912641663, 6.544191908880855557 ) ) ;
#14749=CARTESIAN_POINT ( 'NONE',  ( -3.250000000000000000, -3.500000000000000000, -1.188926645705999921E-13 ) ) ;
#14752=ADVANCED_FACE ( 'NONE', ( #15747 ), #6011, .F. ) ;
#14753=CARTESIAN_POINT ( 'NONE',  ( 12.00000000000000000, -75.80000000000001137, -2.990830162875999918E-13 ) ) ;
#14755=CARTESIAN_POINT ( 'NONE',  ( 10.43010923569933368, -79.22936352839808194, 6.024574312383253805 ) ) ;
#14757=CARTESIAN_POINT ( 'NONE',  ( -10.26699006316252749, -76.84166666666664014, -5.917523019358070790 ) ) ;
#14761=LINE ( 'NONE', #54644, #15171 ) ;
#14762=CARTESIAN_POINT ( 'NONE',  ( 8.588893914429998944, -16.86760216306999993, -9.317954958010000510 ) ) ;
#14763=CARTESIAN_POINT ( 'NONE',  ( -12.50240681834000078, -24.68234730741999883, 1.005418943852999902 ) ) ;
#14764=VERTEX_POINT ( 'NONE', #39621 ) ;
#14766=CARTESIAN_POINT ( 'NONE',  ( 12.70556836347999941, -16.77227722772000007, -1.774194455291999869E-09 ) ) ;
#14769=CARTESIAN_POINT ( 'NONE',  ( -12.22285758008880308, -77.44360420965402625, 1.403409555567897149 ) ) ;
#14773=CARTESIAN_POINT ( 'NONE',  ( 10.98449824368628391, -23.30634943316888652, -0.5845455749771567566 ) ) ;
#14774=AXIS2_PLACEMENT_3D ( 'NONE', #45462, #40128, #5005 ) ;
#14776=CARTESIAN_POINT ( 'NONE',  ( -12.50412681318974251, -54.28010473027888594, -1.235016000149057325 ) ) ;
#14779=CARTESIAN_POINT ( 'NONE',  ( -1.164828128805999992E-14, -72.75000000040999737, 0.000000000000000000 ) ) ;
#14781=AXIS2_PLACEMENT_3D ( 'NONE', #46055, #58147, #6169 ) ;
#14782=ORIENTED_EDGE ( 'NONE', *, *, #49164, .F. ) ;
#14785=VECTOR ( 'NONE', #25892, 999.9999999999998863 ) ;
#14787=ADVANCED_FACE ( 'NONE', ( #12753 ), #39046, .F. ) ;
#14791=CARTESIAN_POINT ( 'NONE',  ( 7.658894224196000522, -60.00939395830999956, 10.01676912202999858 ) ) ;
#14798=B_SPLINE_CURVE_WITH_KNOTS ( 'NONE', 3,
 ( #15036, #5590, #55786, #6179, #10919, #18895, #50488, #33030, #41327, #10624, #50783, #24191, #28023, #33327, #19185, #10328, #15336, #42208, #46068, #51364, #1774, #23603, #19769, #37765, #46946, #6471, #55193, #24482, #911, #45085, #9357, #49810, #13766, #9646, #40942, #31470, #27634, #45971, #18506, #530, #32346, #36501, #36789, #9941, #27347, #32061, #53942, #58359, #27919, #45677, #49513, #45382, #50393, #13475, #54807, #14065, #18222, #44783, #22928, #9064, #5215, #54527, #58063, #23219, #17623, #26754, #41226, #40649, #27049, #5496, #50102, #14348, #4636, #17923 ),
 .UNSPECIFIED., .F., .F.,
 ( 4, 2, 2, 1, 1, 1, 2, 2, 2, 2, 1, 1, 2, 2, 2, 2, 2, 2, 2, 1, 1, 2, 2, 2, 2, 1, 1, 2, 2, 2, 2, 1, 1, 2, 2, 2, 2, 1, 1, 1, 2, 2, 2, 4 ),
 ( 0.000000000000000000, 0.06250000000000086042, 0.09375000000000129063, 0.1093750000000015266, 0.1171875000000015821, 0.1210937500000015543, 0.1230468750000015821, 0.1250000000000016098, 0.1875000000000031364, 0.2187500000000039135, 0.2343750000000043299, 0.2421875000000045519, 0.2460937500000047184, 0.2500000000000048850, 0.3125000000000050515, 0.3437500000000050515, 0.3593750000000051070, 0.3750000000000051625, 0.4375000000000052180, 0.4687500000000052736, 0.4843750000000052736, 0.4921875000000052736, 0.5000000000000052180, 0.5625000000000053291, 0.5937500000000054401, 0.6093750000000054401, 0.6171875000000054401, 0.6210937500000053291, 0.6250000000000052180, 0.6875000000000052180, 0.7187500000000053291, 0.7343750000000054401, 0.7421875000000054401, 0.7460937500000054401, 0.7500000000000053291, 0.8125000000000044409, 0.8437500000000039968, 0.8593750000000038858, 0.8671875000000037748, 0.8710937500000036637, 0.8730468750000036637, 0.8750000000000036637, 0.9375000000000018874, 1.000000000000000000 ),
 .UNSPECIFIED. ) ;
#14801=DIRECTION ( 'NONE',  ( 1.000000000000000000, 0.000000000000000000, 0.000000000000000000 ) ) ;
#14802=ADVANCED_FACE ( 'NONE', ( #34605 ), #10233, .F. ) ;
#14809=CARTESIAN_POINT ( 'NONE',  ( -7.756281347471999155, -24.22006031113999569, -10.15825374573999973 ) ) ;
#14810=CARTESIAN_POINT ( 'NONE',  ( 12.69616050746999925, -57.04828923575999511, -1.799475304559999822 ) ) ;
#14813=DIRECTION ( 'NONE',  ( 1.000000000000000000, 0.000000000000000000, 0.000000000000000000 ) ) ;
#14817=CARTESIAN_POINT ( 'NONE',  ( -1.750000000001000089, -18.74999999009000007, 12.56594317857000043 ) ) ;
#14819=CARTESIAN_POINT ( 'NONE',  ( 2.661529024748306327, -3.056711299679849336, 2.302964992746549200 ) ) ;
#14826=ORIENTED_EDGE ( 'NONE', *, *, #13813, .F. ) ;
#14827=EDGE_CURVE ( 'NONE', #32490, #40010, #27193, .T. ) ;
#14828=CARTESIAN_POINT ( 'NONE',  ( -1.929975092515999968, -60.00107256231000008, -12.72537404212999768 ) ) ;
#14829=VECTOR ( 'NONE', #21814, 1000.000000000000000 ) ;
#14834=VECTOR ( 'NONE', #51533, 1000.000000000000000 ) ;
#14835=DIRECTION ( 'NONE',  ( 0.000000000000000000, -1.000000000000000000, 0.000000000000000000 ) ) ;
#14838=DIRECTION ( 'NONE',  ( 0.9999999999995751176, 0.000000000000000000, 9.217549097710770925E-07 ) ) ;
#14842=CARTESIAN_POINT ( 'NONE',  ( 10.15323015671000029, -54.56919784871999468, -7.760928569184999404 ) ) ;
#14851=CARTESIAN_POINT ( 'NONE',  ( -1.980532734072999901, -22.76232686847000153, -12.80090744964000038 ) ) ;
#14857=ORIENTED_EDGE ( 'NONE', *, *, #34220, .F. ) ;
#14858=ORIENTED_EDGE ( 'NONE', *, *, #53886, .T. ) ;
#14860=ORIENTED_EDGE ( 'NONE', *, *, #52320, .T. ) ;
#14868=FACE_OUTER_BOUND ( 'NONE', #25606, .T. ) ;
#14869=VECTOR ( 'NONE', #45600, 1000.000000000000114 ) ;
#14871=ORIENTED_EDGE ( 'NONE', *, *, #55835, .T. ) ;
#14872=CARTESIAN_POINT ( 'NONE',  ( 12.60356226360999798, -56.04922971106000062, 1.750000000000000000 ) ) ;
#14876=CARTESIAN_POINT ( 'NONE',  ( 0.8338927958996298351, -17.19946422253883966, 12.50366901602930447 ) ) ;
#14878=AXIS2_PLACEMENT_3D ( 'NONE', #1891, #28719, #2176 ) ;
#14879=CYLINDRICAL_SURFACE ( 'NONE', #6787, 3.250000000000000000 ) ;
#14882=B_SPLINE_CURVE_WITH_KNOTS ( 'NONE', 3,
 ( #28040, #18910, #10058, #50211, #18626, #45793, #23040, #41632 ),
 .UNSPECIFIED., .F., .F.,
 ( 4, 2, 2, 4 ),
 ( 0.000000000000000000, 0.5000000000000000000, 0.7500000000000000000, 1.000000000000000000 ),
 .UNSPECIFIED. ) ;
#14890=FACE_OUTER_BOUND ( 'NONE', #9352, .T. ) ;
#14896=ORIENTED_EDGE ( 'NONE', *, *, #45220, .T. ) ;
#14897=CARTESIAN_POINT ( 'NONE',  ( -10.22919423418071005, -78.84166666666666856, -5.911015991358792299 ) ) ;
#14899=CARTESIAN_POINT ( 'NONE',  ( -3.785211018891809776, -77.59942841202766317, 11.15200902601148769 ) ) ;
#14902=CARTESIAN_POINT ( 'NONE',  ( 1.667916687331000070, -60.09848884406000025, 12.49168451100999988 ) ) ;
#14903=CARTESIAN_POINT ( 'NONE',  ( 12.53073434187000146, -77.67626658266999584, -3.509976885708000260 ) ) ;
#14907=DIRECTION ( 'NONE',  ( -1.000000000000000000, 0.000000000000000000, 0.000000000000000000 ) ) ;
#14909=EDGE_CURVE ( 'NONE', #3462, #19523, #53984, .T. ) ;
#14911=CARTESIAN_POINT ( 'NONE',  ( 12.50000000000000000, -15.06282895647999887, 0.000000000000000000 ) ) ;
#14915=CARTESIAN_POINT ( 'NONE',  ( 7.648026766715999791, -55.54999999381000464, 10.12290050087000104 ) ) ;
#14917=DIRECTION ( 'NONE',  ( 0.7071067811864973907, 0.7071067811865973107, -2.112640561316990679E-08 ) ) ;
#14919=CARTESIAN_POINT ( 'NONE',  ( 12.50745077485999879, -53.80005551680000053, -2.012158279073999839E-09 ) ) ;
#14920=CARTESIAN_POINT ( 'NONE',  ( -7.624341764923000753, -18.73514850530999709, -10.42531124853000080 ) ) ;
#14921=CIRCLE ( 'NONE', #50811, 11.00000000000000000 ) ;
#14925=DIRECTION ( 'NONE',  ( -1.000000000000000000, 0.000000000000000000, 0.000000000000000000 ) ) ;
#14927=APPLICATION_CONTEXT ( 'automotive_design' ) ;
#14931=DIRECTION ( 'NONE',  ( 1.000000000000000000, 0.000000000000000000, 0.000000000000000000 ) ) ;
#14935=CARTESIAN_POINT ( 'NONE',  ( 10.48774103543000180, -58.55472018357999531, 7.686941364784000363 ) ) ;
#14936=VERTEX_POINT ( 'NONE', #32979 ) ;
#14938=CARTESIAN_POINT ( 'NONE',  ( -7.626500777218999438, -55.48415267986000288, 10.35747145890000098 ) ) ;
#14939=EDGE_LOOP ( 'NONE', ( #50041, #23064, #50974, #54735, #4280 ) ) ;
#14945=CARTESIAN_POINT ( 'NONE',  ( 8.439151210957692939, -78.63560278023904004, -8.898801520529000086 ) ) ;
#14951=CARTESIAN_POINT ( 'NONE',  ( -7.613962827161000035, -55.49360374314999689, -10.53101998745000145 ) ) ;
#14953=CARTESIAN_POINT ( 'NONE',  ( 6.541589835834063393, -76.52783443949311959, 9.760510139220190950 ) ) ;
#14965=CARTESIAN_POINT ( 'NONE',  ( 12.76303204513999923, -55.53514852210999919, -1.980584515753000208 ) ) ;
#14967=CYLINDRICAL_SURFACE ( 'NONE', #47057, 0.6000000000000008660 ) ;
#14971=CARTESIAN_POINT ( 'NONE',  ( 13.63885489310999510, -22.78578169018999944, -7.254376133916000668 ) ) ;
#14973=CARTESIAN_POINT ( 'NONE',  ( 12.77649732927999970, -25.30828417252000051, -0.06479631635390999123 ) ) ;
#14975=CARTESIAN_POINT ( 'NONE',  ( -0.9935076046663652294, -24.96816187757334049, -12.70250268216760681 ) ) ;
#14976=CARTESIAN_POINT ( 'NONE',  ( -5.052374247686000075, -75.84546611944999484, -10.65162165865999988 ) ) ;
#14981=CARTESIAN_POINT ( 'NONE',  ( 12.77651047021000075, -62.10895689102999739, -0.04321256188117000158 ) ) ;
#14984=AXIS2_PLACEMENT_3D ( 'NONE', #36435, #467, #55033 ) ;
#14987=DIRECTION ( 'NONE',  ( -1.000000000000000000, 0.000000000000000000, 0.000000000000000000 ) ) ;
#14988=DIRECTION ( 'NONE',  ( 0.7071067811864981678, 0.000000000000000000, -0.7071067811865970887 ) ) ;
#14989=ORIENTED_EDGE ( 'NONE', *, *, #12169, .T. ) ;
#14991=PLANE ( 'NONE',  #14373 ) ;
#14995=ORIENTED_EDGE ( 'NONE', *, *, #45102, .F. ) ;
#14997=B_SPLINE_CURVE_WITH_KNOTS ( 'NONE', 3,
 ( #56543, #12810, #30809, #57115, #25816, #26382, #44402, #43260, #3954, #38528, #21387, #16104, #34663 ),
 .UNSPECIFIED., .F., .F.,
 ( 4, 2, 2, 1, 2, 2, 4 ),
 ( 0.000000000000000000, 0.2499999999999998890, 0.4999999999999997780, 0.6249999999999997780, 0.6874999999999995559, 0.7499999999999995559, 1.000000000000000000 ),
 .UNSPECIFIED. ) ;
#15002=CARTESIAN_POINT ( 'NONE',  ( -1.930989144707000005, -20.24634220924000161, 12.80900240957999969 ) ) ;
#15003=VECTOR ( 'NONE', #47116, 1000.000000000000114 ) ;
#15004=ORIENTED_EDGE ( 'NONE', *, *, #32148, .F. ) ;
#15007=ADVANCED_FACE ( 'NONE', ( #42452 ), #1437, .F. ) ;
#15009=EDGE_CURVE ( 'NONE', #23097, #49897, #55140, .T. ) ;
#15012=ORIENTED_EDGE ( 'NONE', *, *, #52048, .T. ) ;
#15013=CARTESIAN_POINT ( 'NONE',  ( -8.130813118348999780, -54.11476110100999648, 9.546856411314999846 ) ) ;
#15014=CARTESIAN_POINT ( 'NONE',  ( 10.04567131160781557, -24.55088387374295067, -7.921299640536786590 ) ) ;
#15015=ORIENTED_EDGE ( 'NONE', *, *, #47427, .T. ) ;
#15016=DIRECTION ( 'NONE',  ( 0.000000000000000000, 0.000000000000000000, -1.000000000000000000 ) ) ;
#15018=FACE_OUTER_BOUND ( 'NONE', #5708, .T. ) ;
#15022=EDGE_CURVE ( 'NONE', #15410, #18144, #27088, .T. ) ;
#15027=CARTESIAN_POINT ( 'NONE',  ( 11.65396969189999865, -75.71350996453999471, -2.860942225950000140 ) ) ;
#15029=AXIS2_PLACEMENT_3D ( 'NONE', #31070, #44099, #22531 ) ;
#15030=CARTESIAN_POINT ( 'NONE',  ( 7.619389973917000347, -60.20786254198000620, -10.35398617735999949 ) ) ;
#15031=CARTESIAN_POINT ( 'NONE',  ( -12.26143800982999998, -79.05353869690000579, -0.2371146996492999870 ) ) ;
#15032=EDGE_CURVE ( 'NONE', #470, #48419, #13011, .T. ) ;
#15036=CARTESIAN_POINT ( 'NONE',  ( 3.250000000000000000, -2.850000000000000089, 0.000000000000000000 ) ) ;
#15037=CARTESIAN_POINT ( 'NONE',  ( 10.79003353078767091, -77.76296722650485549, -5.409130585825370652 ) ) ;
#15039=ADVANCED_FACE ( 'NONE', ( #1149 ), #21947, .F. ) ;
#15042=CARTESIAN_POINT ( 'NONE',  ( 1.538071403320016461, -77.93541666666664014, -11.74999999999999822 ) ) ;
#15044=CIRCLE ( 'NONE', #42374, 14.00000000000000000 ) ;
#15046=CARTESIAN_POINT ( 'NONE',  ( 2.922428402108999901, -1.987477233353000194, -2.537670070524999932 ) ) ;
#15049=CARTESIAN_POINT ( 'NONE',  ( -8.776627003607282873, -76.14201958266359327, 7.813090293080676041 ) ) ;
#15053=VERTEX_POINT ( 'NONE', #43029 ) ;
#15060=CARTESIAN_POINT ( 'NONE',  ( 10.53494359615000064, -18.77285042833999995, -7.618393753193999807 ) ) ;
#15061=CARTESIAN_POINT ( 'NONE',  ( 8.583665412795216554, -17.02814425026380718, 9.102144266516488003 ) ) ;
#15066=CARTESIAN_POINT ( 'NONE',  ( 10.93488396298730336, -77.73714250434947814, 5.001126911209347270 ) ) ;
#15070=CARTESIAN_POINT ( 'NONE',  ( 8.485281374238999419, 0.000000000000000000, 8.485281374238999419 ) ) ;
#15071=CARTESIAN_POINT ( 'NONE',  ( 10.48774103543000180, -21.75472018390999907, 7.686941364778000718 ) ) ;
#15073=CARTESIAN_POINT ( 'NONE',  ( 0.000000000000000000, 4.040000000000000036, 0.000000000000000000 ) ) ;
#15076=ORIENTED_EDGE ( 'NONE', *, *, #11752, .T. ) ;
#15077=EDGE_LOOP ( 'NONE', ( #35463, #43436, #19085, #51123 ) ) ;
#15078=B_SPLINE_CURVE_WITH_KNOTS ( 'NONE', 3,
 ( #22934, #23511, #31773, #55101, #18803, #45977, #40947, #32935, #9652, #54812 ),
 .UNSPECIFIED., .F., .F.,
 ( 4, 2, 2, 2, 4 ),
 ( 0.000000000000000000, 0.2500000000000000000, 0.5000000000000000000, 0.7500000000000000000, 1.000000000000000000 ),
 .UNSPECIFIED. ) ;
#15083=CARTESIAN_POINT ( 'NONE',  ( 9.038965287783000235, -16.66737759107000372, 9.029769469460999787 ) ) ;
#15084=AXIS2_PLACEMENT_3D ( 'NONE', #32338, #4629, #36204 ) ;
#15086=CARTESIAN_POINT ( 'NONE',  ( 8.852327248605000420, -79.13956593151999641, 7.934268801159999107 ) ) ;
#15087=CARTESIAN_POINT ( 'NONE',  ( 9.963467980718000661, -60.48274967040000405, 7.659239661670000032 ) ) ;
#15089=EDGE_CURVE ( 'NONE', #46308, #36059, #55270, .T. ) ;
#15093=CARTESIAN_POINT ( 'NONE',  ( -10.04567131160781557, -24.55088387374295067, 7.921299640536786590 ) ) ;
#15094=ORIENTED_EDGE ( 'NONE', *, *, #26526, .T. ) ;
#15097=CYLINDRICAL_SURFACE ( 'NONE', #25326, 0.6000000000000008660 ) ;
#15099=CARTESIAN_POINT ( 'NONE',  ( 10.24474360436999909, -76.45078410675000669, -6.192822469190000234 ) ) ;
#15100=DIRECTION ( 'NONE',  ( 1.000000000000000000, 0.000000000000000000, 0.000000000000000000 ) ) ;
#15103=CARTESIAN_POINT ( 'NONE',  ( 12.72966770608134546, -60.56881200341882021, 1.931346186347591809 ) ) ;
#15105=CARTESIAN_POINT ( 'NONE',  ( 12.80900240954000147, -58.55365779174999830, -1.930989144707000005 ) ) ;
#15107=AXIS2_PLACEMENT_3D ( 'NONE', #22566, #3681, #40578 ) ;
#15108=ORIENTED_EDGE ( 'NONE', *, *, #36357, .F. ) ;
#15110=DIRECTION ( 'NONE',  ( 0.7071067811865474617, 0.000000000000000000, 0.7071067811865474617 ) ) ;
#15113=CARTESIAN_POINT ( 'NONE',  ( -7.633478597825000378, -18.79901960220000134, 10.36292351978000070 ) ) ;
#15114=B_SPLINE_CURVE_WITH_KNOTS ( 'NONE', 3,
 ( #8188, #56920, #34168, #16477, #20615, #44207, #30609, #48080, #7610, #43059, #47511, #52489, #43340, #47790, #20897, #15897, #2897, #30316, #34458, #3194, #11482, #26189, #39185, #52205, #48357, #20328, #57200, #16768, #53061, #7897, #35029 ),
 .UNSPECIFIED., .F., .F.,
 ( 4, 1, 1, 1, 1, 1, 1, 1, 1, 1, 1, 1, 1, 1, 1, 1, 1, 1, 1, 1, 1, 1, 1, 1, 1, 1, 1, 1, 4 ),
 ( 0.000000000000000000, 0.01409448528475833011, 0.05073813331262903153, 0.08738178134047794310, 0.1240254293683486497, 0.1606690773962193564, 0.1973127254240683026, 0.2339563734519607419, 0.2706000214798749970, 0.3072436695075715374, 0.3438873175354857925, 0.3805309655634000476, 0.4171746135913142473, 0.4538182616192285579, 0.4904619096469250983, 0.5271055576748392424, 0.5637492057027536640, 0.6003928537306677526, 0.6370365017583644596, 0.6736801497862785482, 0.7103237978141928588, 0.7469674458421071694, 0.7836110938698035433, 0.8202547418977179650, 0.8568983899256321646, 0.8935420379535463642, 0.9301856859814607859, 0.9668293340091570487, 1.000000000000000000 ),
 .UNSPECIFIED. ) ;
#15116=CARTESIAN_POINT ( 'NONE',  ( 0.4318235569510932015, -2.884823844453682895, -3.492932053398966730 ) ) ;
#15117=CARTESIAN_POINT ( 'NONE',  ( -10.12290050122000018, -55.54999999974999980, 7.648026767069000087 ) ) ;
#15123=VERTEX_POINT ( 'NONE', #19357 ) ;
#15125=CARTESIAN_POINT ( 'NONE',  ( -1.539858032099693741, -77.08353792532550131, 11.67459080161200546 ) ) ;
#15126=CARTESIAN_POINT ( 'NONE',  ( 0.9887300587116000239, -61.73410057736000311, -12.65963207093999898 ) ) ;
#15127=CARTESIAN_POINT ( 'NONE',  ( -7.648026768019999366, -23.24999998419999869, -10.12290050217000115 ) ) ;
#15134=CARTESIAN_POINT ( 'NONE',  ( 0.000000000000000000, 0.000000000000000000, 0.000000000000000000 ) ) ;
#15139=CARTESIAN_POINT ( 'NONE',  ( 7.761025538834000592, -54.71850014388999739, -9.835174270505000038 ) ) ;
#15145=CARTESIAN_POINT ( 'NONE',  ( -14.00000000000000000, -32.66217755555999958, -5.544640309346000075E-06 ) ) ;
#15148=CARTESIAN_POINT ( 'NONE',  ( -8.266608573639034674, -53.82766203646255576, 9.697383820226121998 ) ) ;
#15155=ORIENTED_EDGE ( 'NONE', *, *, #33060, .T. ) ;
#15156=CONICAL_SURFACE ( 'NONE', #46282, 8.749999999256001360, 0.7853981633972997312 ) ;
#15158=EDGE_LOOP ( 'NONE', ( #36297, #37811, #35251, #3129 ) ) ;
#15159=EDGE_LOOP ( 'NONE', ( #19154, #40715, #26181, #51705 ) ) ;
#15160=CARTESIAN_POINT ( 'NONE',  ( -1.194090705999000024, -17.55968341096999552, 12.43436538489999954 ) ) ;
#15164=EDGE_CURVE ( 'NONE', #55842, #17140, #11115, .T. ) ;
#15166=DIRECTION ( 'NONE',  ( 0.000000000000000000, 0.000000000000000000, -1.000000000000000000 ) ) ;
#15167=VERTEX_POINT ( 'NONE', #4770 ) ;
#15170=CARTESIAN_POINT ( 'NONE',  ( 12.56594317819999951, -55.54999998572999687, 1.750000000000000000 ) ) ;
#15171=VECTOR ( 'NONE', #36331, 1000.000000000000000 ) ;
#15172=CARTESIAN_POINT ( 'NONE',  ( -12.70556836322084848, -25.22772277445464795, 0.2597962961080404476 ) ) ;
#15173=CARTESIAN_POINT ( 'NONE',  ( -7.601397897754999633, -60.04999999966999980, -9.369164850722000892 ) ) ;
#15174=CARTESIAN_POINT ( 'NONE',  ( -0.9935076046646102998, -61.76816187723938611, -12.70250268221170309 ) ) ;
#15183=EDGE_CURVE ( 'NONE', #24970, #55907, #5447, .T. ) ;
#15184=CARTESIAN_POINT ( 'NONE',  ( 0.01555524843309799218, -76.57477272176625149, 11.74989434732423099 ) ) ;
#15185=CARTESIAN_POINT ( 'NONE',  ( 12.50745077494999968, -61.79994448255000350, 2.662030659623000237E-09 ) ) ;
#15188=DIRECTION ( 'NONE',  ( 0.000000000000000000, -0.1122098755727947705, 0.9936845293270585300 ) ) ;
#15189=CARTESIAN_POINT ( 'NONE',  ( 1.667917367065999912, -18.71943464842000182, -12.49306764015999960 ) ) ;
#15191=CARTESIAN_POINT ( 'NONE',  ( 1.044910384896000188, -16.94473505805000002, -12.77260826199000121 ) ) ;
#15192=LINE ( 'NONE', #33480, #16661 ) ;
#15193=CARTESIAN_POINT ( 'NONE',  ( 0.000000000000000000, -23.84999999976950136, 11.89999999977000122 ) ) ;
#15194=CARTESIAN_POINT ( 'NONE',  ( 3.190249742999000215, -2.056098507945999465, -2.075671974272999876 ) ) ;
#15195=CARTESIAN_POINT ( 'NONE',  ( -1.416116075149735476, -1.657507861446844588, 3.334501019042391157 ) ) ;
#15196=VERTEX_POINT ( 'NONE', #22180 ) ;
#15197=CARTESIAN_POINT ( 'NONE',  ( 9.621717088333529233, -61.42064477329430616, 8.060172376500883473 ) ) ;
#15202=CARTESIAN_POINT ( 'NONE',  ( 1.750000000001000089, -19.24922971542000028, -12.60356226396999979 ) ) ;
#15203=CARTESIAN_POINT ( 'NONE',  ( 7.954951288349001004, -23.44678171330999916, 9.722718241315000398 ) ) ;
#15205=CARTESIAN_POINT ( 'NONE',  ( 5.939680743703000668E-14, -6.000000000000000000, 0.000000000000000000 ) ) ;
#15206=DIRECTION ( 'NONE',  ( 0.000000000000000000, -1.000000000000000000, 0.000000000000000000 ) ) ;
#15210=AXIS2_PLACEMENT_3D ( 'NONE', #15385, #34236, #55534 ) ;
#15217=EDGE_CURVE ( 'NONE', #55158, #31908, #18648, .T. ) ;
#15220=AXIS2_PLACEMENT_3D ( 'NONE', #27933, #6092, #41822 ) ;
#15221=DIRECTION ( 'NONE',  ( -0.9999999999999694689, -2.469236275681924191E-07, 1.232399280382961306E-12 ) ) ;
#15222=ORIENTED_EDGE ( 'NONE', *, *, #23189, .F. ) ;
#15226=LINE ( 'NONE', #1377, #32218 ) ;
#15227=ORIENTED_EDGE ( 'NONE', *, *, #42254, .F. ) ;
#15231=VERTEX_POINT ( 'NONE', #35753 ) ;
#15238=CARTESIAN_POINT ( 'NONE',  ( -1.287989364273000037, -2.461525618456000153, 3.148088515452999836 ) ) ;
#15239=ADVANCED_FACE ( 'NONE', ( #54656 ), #14196, .F. ) ;
#15240=ORIENTED_EDGE ( 'NONE', *, *, #12974, .F. ) ;
#15244=CARTESIAN_POINT ( 'NONE',  ( -12.50483450108329642, -17.13545459011075422, 0.6958188036703752966 ) ) ;
#15247=FACE_OUTER_BOUND ( 'NONE', #51277, .T. ) ;
#15251=EDGE_CURVE ( 'NONE', #52629, #800, #53482, .T. ) ;
#15253=CARTESIAN_POINT ( 'NONE',  ( 6.622872397097998132, -76.52713920344137932, 9.705607225355446843 ) ) ;
#15254=CARTESIAN_POINT ( 'NONE',  ( 0.4820079653409431453, -23.51614597298007681, -10.98957811953319563 ) ) ;
#15256=ADVANCED_FACE ( 'NONE', ( #44921 ), #12029, .F. ) ;
#15258=CARTESIAN_POINT ( 'NONE',  ( -3.002690198994237392, -3.070074872230420748, 1.241492466252928750 ) ) ;
#15264=CARTESIAN_POINT ( 'NONE',  ( -8.852458463678310352, -76.25659527127551485, -7.727683512292325752 ) ) ;
#15269=CARTESIAN_POINT ( 'NONE',  ( -8.768124086712999699, -59.94999999969000015, 7.919595949288999570 ) ) ;
#15271=CARTESIAN_POINT ( 'NONE',  ( -9.164385193226218362, -25.21567483134532139, -8.803702036953628962 ) ) ;
#15273=CARTESIAN_POINT ( 'NONE',  ( 0.000000000000000000, -55.54999999966999980, -12.50000000000000000 ) ) ;
#15276=CARTESIAN_POINT ( 'NONE',  ( 11.29076395134999977, -76.98561308323999697, -2.900214329540999891 ) ) ;
#15277=EDGE_LOOP ( 'NONE', ( #29947, #4705, #50447, #42397, #20038 ) ) ;
#15281=CARTESIAN_POINT ( 'NONE',  ( -12.00000000000000000, -55.54999999966999980, 0.000000000000000000 ) ) ;
#15283=CARTESIAN_POINT ( 'NONE',  ( 12.46164872704999915, -55.12834420008999814, -1.631615798669999950 ) ) ;
#15294=ADVANCED_FACE ( 'NONE', ( #41597 ), #58269, .F. ) ;
#15297=CARTESIAN_POINT ( 'NONE',  ( 12.60413652834999887, -60.10716934574000447, 1.799502287743000029 ) ) ;
#15299=ORIENTED_EDGE ( 'NONE', *, *, #44940, .F. ) ;
#15302=CARTESIAN_POINT ( 'NONE',  ( -10.98753362943491929, -23.45184359403960528, -0.5244447725538564642 ) ) ;
#15303=VECTOR ( 'NONE', #47085, 1000.000000000000000 ) ;
#15308=AXIS2_PLACEMENT_3D ( 'NONE', #38975, #25111, #34530 ) ;
#15312=CARTESIAN_POINT ( 'NONE',  ( 12.83675912438999944, -55.57244613998999938, 2.062833085520999976 ) ) ;
#15314=ORIENTED_EDGE ( 'NONE', *, *, #31742, .T. ) ;
#15315=CARTESIAN_POINT ( 'NONE',  ( -12.43652404745000162, -24.92065244538000002, -0.1284256373645999982 ) ) ;
#15317=FACE_BOUND ( 'NONE', #22109, .T. ) ;
#15318=VECTOR ( 'NONE', #36130, 999.9999999999998863 ) ;
#15320=CARTESIAN_POINT ( 'NONE',  ( -7.674627477118999508, -59.55077028051999832, 10.14950121126999960 ) ) ;
#15322=AXIS2_PLACEMENT_3D ( 'NONE', #22454, #4453, #30711 ) ;
#15325=EDGE_CURVE ( 'NONE', #3325, #21397, #51658, .T. ) ;
#15327=CARTESIAN_POINT ( 'NONE',  ( 12.02702378446000075, -75.72388651151999284, -1.341316611471999876 ) ) ;
#15332=DIRECTION ( 'NONE',  ( -0.7071067811865474617, 0.000000000000000000, -0.7071067811865474617 ) ) ;
#15333=CARTESIAN_POINT ( 'NONE',  ( 7.081057523560999378, -79.12198300536000772, -10.01287680343000019 ) ) ;
#15335=CARTESIAN_POINT ( 'NONE',  ( -7.664266801483791802, -60.54946977258678231, -7.892048199457517121 ) ) ;
#15336=CARTESIAN_POINT ( 'NONE',  ( 2.461679710009094801, -2.793789481889469961, -2.122462569764226092 ) ) ;
#15337=CARTESIAN_POINT ( 'NONE',  ( 10.10840608942275942, -77.75407225199086270, -6.586910062449264913 ) ) ;
#15342=CARTESIAN_POINT ( 'NONE',  ( 0.5999999999999999778, -23.15000000000999947, -11.79999999999999893 ) ) ;
#15343=VECTOR ( 'NONE', #47232, 1000.000000000000000 ) ;
#15345=FACE_OUTER_BOUND ( 'NONE', #37666, .T. ) ;
#15348=EDGE_CURVE ( 'NONE', #17469, #11901, #1676, .T. ) ;
#15349=CARTESIAN_POINT ( 'NONE',  ( -6.183423720564950266, -76.11889232786028003, 10.01094227326205122 ) ) ;
#15353=ORIENTED_EDGE ( 'NONE', *, *, #51262, .F. ) ;
#15355=CIRCLE ( 'NONE', #8763, 1.250000000000000444 ) ;
#15357=DIRECTION ( 'NONE',  ( 0.9999999999995751176, 0.000000000000000000, 9.217549102787771002E-07 ) ) ;
#15359=FACE_OUTER_BOUND ( 'NONE', #28680, .T. ) ;
#15361=CARTESIAN_POINT ( 'NONE',  ( 8.478741751137999216, -17.12187496603999648, -9.108230428607001272 ) ) ;
#15363=ORIENTED_EDGE ( 'NONE', *, *, #13935, .F. ) ;
#15369=CARTESIAN_POINT ( 'NONE',  ( 11.19652597747931289, -77.73269495442998789, 4.381814868441350264 ) ) ;
#15370=EDGE_CURVE ( 'NONE', #26684, #47937, #15114, .T. ) ;
#15371=VECTOR ( 'NONE', #19069, 1000.000000000000227 ) ;
#15374=PLANE ( 'NONE',  #10971 ) ;
#15376=FACE_OUTER_BOUND ( 'NONE', #40415, .T. ) ;
#15378=CARTESIAN_POINT ( 'NONE',  ( 12.70556836343000029, -53.57227722738999631, -1.774194422348999890E-09 ) ) ;
#15379=ORIENTED_EDGE ( 'NONE', *, *, #50576, .F. ) ;
#15383=CIRCLE ( 'NONE', #56854, 0.5000000000000004441 ) ;
#15384=ORIENTED_EDGE ( 'NONE', *, *, #15749, .F. ) ;
#15385=CARTESIAN_POINT ( 'NONE',  ( -1.392423410630999929E-14, -75.80000000000001137, 0.000000000000000000 ) ) ;
#15386=CARTESIAN_POINT ( 'NONE',  ( -10.09604776472000154, -78.19984377886000004, 6.324672719602999926 ) ) ;
#15387=CARTESIAN_POINT ( 'NONE',  ( 12.50000000000000000, -60.04999999966999980, 0.000000000000000000 ) ) ;
#15388=DIRECTION ( 'NONE',  ( -1.000000000000000000, 0.000000000000000000, 0.000000000000000000 ) ) ;
#15390=AXIS2_PLACEMENT_3D ( 'NONE', #44003, #21266, #3553 ) ;
#15392=EDGE_LOOP ( 'NONE', ( #28797, #37580, #28725 ) ) ;
#15393=CARTESIAN_POINT ( 'NONE',  ( 12.00000000000000000, -23.25000000000000000, 1.250000000000000000 ) ) ;
#15401=CARTESIAN_POINT ( 'NONE',  ( 11.08637824332000044, -76.46937053406000473, -3.603444353441000114 ) ) ;
#15406=CARTESIAN_POINT ( 'NONE',  ( 7.648026768036999989, -60.04999998387000204, 10.12290050219000115 ) ) ;
#15408=CARTESIAN_POINT ( 'NONE',  ( 0.000000000000000000, -39.30476017083000073, 0.000000000000000000 ) ) ;
#15410=VERTEX_POINT ( 'NONE', #29453 ) ;
#15415=CARTESIAN_POINT ( 'NONE',  ( -7.619712398446999657, -18.59595871862000038, 10.35409979026999849 ) ) ;
#15417=CARTESIAN_POINT ( 'NONE',  ( 2.464672433998302381, -3.436673042811343670, -2.513837925488545455 ) ) ;
#15425=ORIENTED_EDGE ( 'NONE', *, *, #30633, .F. ) ;
#15427=CARTESIAN_POINT ( 'NONE',  ( -1.044910384896000188, -61.85526494161999977, -12.77260826204000033 ) ) ;
#15428=LINE ( 'NONE', #51459, #6934 ) ;
#15431=CARTESIAN_POINT ( 'NONE',  ( 7.647735717248999698, -23.72294882383999948, -10.13404777202000062 ) ) ;
#15433=CARTESIAN_POINT ( 'NONE',  ( -10.09635298639777723, -60.32373519955906715, 7.644087781989489905 ) ) ;
#15434=CARTESIAN_POINT ( 'NONE',  ( 9.000350940039702152, -78.50278833705510806, 7.564101958034004980 ) ) ;
#15435=CARTESIAN_POINT ( 'NONE',  ( -8.274781782374516226, -53.82110650087535220, -9.689260013561808549 ) ) ;
#15436=VERTEX_POINT ( 'NONE', #45092 ) ;
#15438=CARTESIAN_POINT ( 'NONE',  ( -7.624341766629000539, -55.53514853726999689, 10.42531125022999916 ) ) ;
#15440=AXIS2_PLACEMENT_3D ( 'NONE', #16807, #52816, #28925 ) ;
#15441=CARTESIAN_POINT ( 'NONE',  ( 7.618386520025000053, -55.57287536619999457, -10.53495200518000097 ) ) ;
#15446=CARTESIAN_POINT ( 'NONE',  ( -13.98934701301999972, -32.57813015402999923, -1.420884290613999911E-05 ) ) ;
#15448=CARTESIAN_POINT ( 'NONE',  ( -1.980464483675000054, -20.24439829391000245, -12.85140862646999871 ) ) ;
#15449=VECTOR ( 'NONE', #54046, 1000.000000000000000 ) ;
#15452=ORIENTED_EDGE ( 'NONE', *, *, #4244, .F. ) ;
#15457=DIRECTION ( 'NONE',  ( 0.000000000000000000, -1.000000000000000000, 0.000000000000000000 ) ) ;
#15461=EDGE_LOOP ( 'NONE', ( #34734, #36508, #48221, #37369 ) ) ;
#15462=ORIENTED_EDGE ( 'NONE', *, *, #17570, .F. ) ;
#15463=CARTESIAN_POINT ( 'NONE',  ( 2.065394024360999836, -18.57838567354000148, 12.82193048528000112 ) ) ;
#15466=CARTESIAN_POINT ( 'NONE',  ( -13.13047446164998711, -59.58578169018999660, 0.8260994316375004365 ) ) ;
#15473=CARTESIAN_POINT ( 'NONE',  ( 3.250000000000000000, -3.350000000000000089, 0.000000000000000000 ) ) ;
#15478=CARTESIAN_POINT ( 'NONE',  ( 1.750000000000000000, -20.24935285954000008, 12.65372179284999810 ) ) ;
#15481=AXIS2_PLACEMENT_3D ( 'NONE', #30953, #26531, #7960 ) ;
#15482=CARTESIAN_POINT ( 'NONE',  ( -8.278253510431028417, -76.63709233168063406, 8.338544273060703560 ) ) ;
#15483=CARTESIAN_POINT ( 'NONE',  ( 1.878467530605369307, -79.21093747608632896, -11.84982925898997230 ) ) ;
#15487=CARTESIAN_POINT ( 'NONE',  ( 1.667961445601999992, -20.25199022618999933, -12.58338334675000070 ) ) ;
#15488=CARTESIAN_POINT ( 'NONE',  ( -7.601397897754999633, -23.24999999688999708, -10.07627163191000008 ) ) ;
#15489=CARTESIAN_POINT ( 'NONE',  ( 1.460729357738999923, -17.90908756796999768, -12.44211643240000065 ) ) ;
#15491=DIRECTION ( 'NONE',  ( -0.7071067811865475727, 0.000000000000000000, 0.7071067811865475727 ) ) ;
#15500=CARTESIAN_POINT ( 'NONE',  ( -12.43645963087999995, -53.88248289507999544, -0.05235777564057000205 ) ) ;
#15502=CARTESIAN_POINT ( 'NONE',  ( -10.42531125074000009, -18.73514854687000053, -7.624341767140999870 ) ) ;
#15503=ADVANCED_FACE ( 'NONE', ( #10237 ), #38449, .T. ) ;
#15506=AXIS2_PLACEMENT_3D ( 'NONE', #43993, #44566, #21546 ) ;
#15507=EDGE_CURVE ( 'NONE', #8180, #36778, #27758, .T. ) ;
#15511=CARTESIAN_POINT ( 'NONE',  ( 2.598917237794081014, -2.802083333333333037, 1.997276839918480373 ) ) ;
#15518=B_SPLINE_CURVE_WITH_KNOTS ( 'NONE', 3,
 ( #20277, #11143, #37392, #55411, #33832, #24413 ),
 .UNSPECIFIED., .F., .F.,
 ( 4, 1, 1, 4 ),
 ( 0.000000000000000000, 0.3333333333333000081, 0.6666666666667000474, 1.000000000000000000 ),
 .UNSPECIFIED. ) ;
#15520=AXIS2_PLACEMENT_3D ( 'NONE', #50019, #24307, #23137 ) ;
#15524=EDGE_LOOP ( 'NONE', ( #32273, #53046, #3893, #16187 ) ) ;
#15526=ORIENTED_EDGE ( 'NONE', *, *, #6214, .T. ) ;
#15527=EDGE_LOOP ( 'NONE', ( #53116, #36720, #21076 ) ) ;
#15528=DIRECTION ( 'NONE',  ( 0.000000000000000000, 1.000000000000000000, 0.000000000000000000 ) ) ;
#15532=ORIENTED_EDGE ( 'NONE', *, *, #19037, .F. ) ;
#15534=CARTESIAN_POINT ( 'NONE',  ( -3.360781121377000247, -2.567928536415000185, -0.5239545519189000577 ) ) ;
#15536=CARTESIAN_POINT ( 'NONE',  ( -1.342463812738999916E-14, -80.75000000002938805, 0.000000000000000000 ) ) ;
#15539=CARTESIAN_POINT ( 'NONE',  ( 9.723199427898999048, -54.32306055827000080, -7.958735709912999390 ) ) ;
#15544=VECTOR ( 'NONE', #50857, 1000.000000000000114 ) ;
#15547=CARTESIAN_POINT ( 'NONE',  ( 2.370075440808774747, -76.55841085529293366, 11.50824778498618528 ) ) ;
#15549=B_SPLINE_CURVE_WITH_KNOTS ( 'NONE', 3,
 ( #52714, #12265, #9297, #13713 ),
 .UNSPECIFIED., .F., .F.,
 ( 4, 4 ),
 ( 0.000000000000000000, 1.000000000000000000 ),
 .UNSPECIFIED. ) ;
#15551=VECTOR ( 'NONE', #48456, 1000.000000000000000 ) ;
#15553=CARTESIAN_POINT ( 'NONE',  ( -2.396502291928098938, -3.041257940394757497, 2.195690585843919074 ) ) ;
#15559=CARTESIAN_POINT ( 'NONE',  ( 7.714303428875997959, -63.10294702886003648, 12.53545825868000385 ) ) ;
#15560=CARTESIAN_POINT ( 'NONE',  ( -6.558766225408620976, -76.27778056724990563, -9.749046883922389384 ) ) ;
#15561=CARTESIAN_POINT ( 'NONE',  ( 10.24996238031000040, -20.24828923609000242, 7.705119999441000012 ) ) ;
#15562=CARTESIAN_POINT ( 'NONE',  ( -10.18948929999999997, -60.01532694310999716, -7.645397820753000673 ) ) ;
#15568=CARTESIAN_POINT ( 'NONE',  ( 11.75000000000000000, -78.45000000000000284, 0.000000000000000000 ) ) ;
#15570=CARTESIAN_POINT ( 'NONE',  ( 11.92652830712999901, -76.51755275073999485, 1.801729816758000036 ) ) ;
#15574=EDGE_CURVE ( 'NONE', #21570, #15196, #18805, .T. ) ;
#15576=CARTESIAN_POINT ( 'NONE',  ( 9.848035040981065080, -53.97131634258318655, 8.114786739967440710 ) ) ;
#15578=LINE ( 'NONE', #55739, #38949 ) ;
#15581=DIRECTION ( 'NONE',  ( -0.7071067811865475727, 0.000000000000000000, 0.7071067811865475727 ) ) ;
#15586=EDGE_LOOP ( 'NONE', ( #4172, #41065, #6443, #55208 ) ) ;
#15589=CIRCLE ( 'NONE', #48589, 0.8000000000000000444 ) ;
#15592=ORIENTED_EDGE ( 'NONE', *, *, #90, .T. ) ;
#15596=AXIS2_PLACEMENT_3D ( 'NONE', #9955, #5804, #19394 ) ;
#15597=CARTESIAN_POINT ( 'NONE',  ( -11.75000000000000000, -78.70000000000000284, -1.701764645356999850E-14 ) ) ;
#15599=ORIENTED_EDGE ( 'NONE', *, *, #10261, .T. ) ;
#15603=ORIENTED_EDGE ( 'NONE', *, *, #51191, .T. ) ;
#15604=CARTESIAN_POINT ( 'NONE',  ( 12.77651065919999951, -53.49103388577999851, -0.04307580168117999125 ) ) ;
#15607=CARTESIAN_POINT ( 'NONE',  ( -12.59682790092999838, -23.38734115225999943, -1.801645751184999922 ) ) ;
#15609=LINE ( 'NONE', #33604, #20462 ) ;
#15611=DIRECTION ( 'NONE',  ( 0.000000000000000000, 0.000000000000000000, -1.000000000000000000 ) ) ;
#15612=CARTESIAN_POINT ( 'NONE',  ( -12.72924182832285567, -18.22450359994043723, -1.930521792048641716 ) ) ;
#15615=CARTESIAN_POINT ( 'NONE',  ( -7.986976573804001056, -24.72634345633999686, 10.07613380457000041 ) ) ;
#15617=EDGE_CURVE ( 'NONE', #48410, #57766, #33816, .T. ) ;
#15619=CARTESIAN_POINT ( 'NONE',  ( 10.01752098898000121, -59.99172009619000079, -7.660412494194000388 ) ) ;
#15620=CARTESIAN_POINT ( 'NONE',  ( -9.042566447131001439, -79.00702013305000548, -8.284387575507999202 ) ) ;
#15623=ADVANCED_FACE ( 'NONE', ( #6967 ), #7259, .F. ) ;
#15624=CARTESIAN_POINT ( 'NONE',  ( -9.679134854984988934, -78.10097625800554511, -7.212729867296981290 ) ) ;
#15626=VERTEX_POINT ( 'NONE', #25260 ) ;
#15629=CARTESIAN_POINT ( 'NONE',  ( 0.000000000000000000, -4.000000000000000000, 0.000000000000000000 ) ) ;
#15631=CARTESIAN_POINT ( 'NONE',  ( -2.222171105826999504, -3.370715166820999809, -3.169094681224999821 ) ) ;
#15635=CARTESIAN_POINT ( 'NONE',  ( -11.30495782231091972, -76.17783368164089097, 3.211150208059951883 ) ) ;
#15639=ORIENTED_EDGE ( 'NONE', *, *, #2118, .T. ) ;
#15642=EDGE_CURVE ( 'NONE', #7307, #41589, #51855, .T. ) ;
#15643=DIRECTION ( 'NONE',  ( 1.000000000000000000, 0.000000000000000000, 0.000000000000000000 ) ) ;
#15644=CARTESIAN_POINT ( 'NONE',  ( -9.650948395536001811, -61.73402498629999968, 8.252474012569001260 ) ) ;
#15647=CARTESIAN_POINT ( 'NONE',  ( 0.000000000000000000, 4.040000000000000036, 0.000000000000000000 ) ) ;
#15648=CARTESIAN_POINT ( 'NONE',  ( -12.70556836319933858, -53.57227722548667970, -0.2598513551041126690 ) ) ;
#15649=ORIENTED_EDGE ( 'NONE', *, *, #55472, .F. ) ;
#15651=DIRECTION ( 'NONE',  ( 0.000000000000000000, -1.000000000000000000, 0.000000000000000000 ) ) ;
#15658=DIRECTION ( 'NONE',  ( 0.000000000000000000, 1.000000000000000000, 0.000000000000000000 ) ) ;
#15660=EDGE_CURVE ( 'NONE', #13623, #40049, #49760, .T. ) ;
#15661=CARTESIAN_POINT ( 'NONE',  ( -12.71658872082999814, -55.48415267986000288, 1.931087888240000217 ) ) ;
#15663=CARTESIAN_POINT ( 'NONE',  ( 0.000000000000000000, 4.040000000000000036, 0.000000000000000000 ) ) ;
#15665=ORIENTED_EDGE ( 'NONE', *, *, #55298, .F. ) ;
#15668=ORIENTED_EDGE ( 'NONE', *, *, #54272, .T. ) ;
#15669=CARTESIAN_POINT ( 'NONE',  ( 9.108265402975000313, -17.12189187203999907, 8.478706101062000400 ) ) ;
#15670=EDGE_CURVE ( 'NONE', #21736, #54376, #9507, .T. ) ;
#15672=CONICAL_SURFACE ( 'NONE', #43953, 3.699999993671000187, 0.7853981633972997312 ) ;
#15673=CARTESIAN_POINT ( 'NONE',  ( -7.544476508856000407, -78.31480665116998807, -9.220210271162999405 ) ) ;
#15674=AXIS2_PLACEMENT_3D ( 'NONE', #18631, #28043, #23045 ) ;
#15675=LINE ( 'NONE', #34527, #2372 ) ;
#15676=CARTESIAN_POINT ( 'NONE',  ( -8.343860018000999190, -59.94999999967000548, -8.343860018000999190 ) ) ;
#15679=TOROIDAL_SURFACE ( 'NONE', #43044, 1.250000000000000000, 0.5000000000000000000 ) ;
#15680=ORIENTED_EDGE ( 'NONE', *, *, #11465, .F. ) ;
#15681=FACE_OUTER_BOUND ( 'NONE', #1103, .T. ) ;
#15682=ORIENTED_EDGE ( 'NONE', *, *, #29021, .F. ) ;
#15689=DIRECTION ( 'NONE',  ( 0.000000000000000000, 1.000000000000000000, 0.000000000000000000 ) ) ;
#15691=CARTESIAN_POINT ( 'NONE',  ( -7.655555357433999397, -22.77795407709999864, 10.38646360829000059 ) ) ;
#15692=EDGE_CURVE ( 'NONE', #20749, #13177, #1034, .T. ) ;
#15694=DIRECTION ( 'NONE',  ( 0.000000000000000000, 0.7071067811866525998, -0.7071067811864425456 ) ) ;
#15696=CARTESIAN_POINT ( 'NONE',  ( -12.57042253521000141, -62.90094976977999863, 0.000000000000000000 ) ) ;
#15699=LINE ( 'NONE', #37253, #15544 ) ;
#15703=CARTESIAN_POINT ( 'NONE',  ( -8.251806177847308632, -53.99944067039370310, 9.431051272634938698 ) ) ;
#15705=CARTESIAN_POINT ( 'NONE',  ( -1.543989697593808330, -2.161087190870070618, 3.163786432364460666 ) ) ;
#15708=CARTESIAN_POINT ( 'NONE',  ( 1.798944584246999989, -55.58466771687000119, -12.61116915997000021 ) ) ;
#15715=CARTESIAN_POINT ( 'NONE',  ( 1.933504092458000034, -60.20406847242999504, -12.70940235709999833 ) ) ;
#15716=CARTESIAN_POINT ( 'NONE',  ( -14.00000000000000000, -46.09579702914000165, 3.101240652847000040E-11 ) ) ;
#15719=CARTESIAN_POINT ( 'NONE',  ( 10.42531124903999995, -55.53514851492000304, -7.624341765436000173 ) ) ;
#15722=CARTESIAN_POINT ( 'NONE',  ( 5.971486360289516071, -78.53205027161877183, 10.11909832258768382 ) ) ;
#15724=EDGE_LOOP ( 'NONE', ( #8458, #52015, #46842, #57916 ) ) ;
#15725=AXIS2_PLACEMENT_3D ( 'NONE', #12084, #16517, #25363 ) ;
#15728=AXIS2_PLACEMENT_3D ( 'NONE', #9244, #8355, #40234 ) ;
#15730=DIRECTION ( 'NONE',  ( 0.000000000000000000, 0.000000000000000000, -1.000000000000000000 ) ) ;
#15738=CARTESIAN_POINT ( 'NONE',  ( 1.930989144707000005, -21.75365779208000205, 12.80900240953000058 ) ) ;
#15739=CARTESIAN_POINT ( 'NONE',  ( -1.980584515756000030, -55.53514849873000259, 12.76303204337999908 ) ) ;
#15741=ORIENTED_EDGE ( 'NONE', *, *, #6928, .F. ) ;
#15746=EDGE_LOOP ( 'NONE', ( #1937, #20307, #4426, #56340 ) ) ;
#15747=FACE_OUTER_BOUND ( 'NONE', #36153, .T. ) ;
#15749=EDGE_CURVE ( 'NONE', #49656, #34958, #7304, .T. ) ;
#15750=CARTESIAN_POINT ( 'NONE',  ( -7.958776490640000034, -61.27699850015999772, 9.723157983991999487 ) ) ;
#15758=VECTOR ( 'NONE', #49160, 1000.000000000000000 ) ;
#15759=CARTESIAN_POINT ( 'NONE',  ( -12.72397319118000070, -60.02144180272999563, -1.930910316632999946 ) ) ;
#15761=DIRECTION ( 'NONE',  ( 0.000000000000000000, 0.000000000000000000, 1.000000000000000000 ) ) ;
#15763=CIRCLE ( 'NONE', #47727, 0.5999999999999999778 ) ;
#15768=CIRCLE ( 'NONE', #42155, 11.19999999999999929 ) ;
#15771=CARTESIAN_POINT ( 'NONE',  ( -9.636775127258999873, -54.35967715709000458, 7.948072248856999700 ) ) ;
#15774=CARTESIAN_POINT ( 'NONE',  ( -7.631896578932000352, -18.77877526479000281, -10.36221705164000184 ) ) ;
#15776=CARTESIAN_POINT ( 'NONE',  ( 2.061613410425999771, -18.79429985524000202, -12.83797036855999885 ) ) ;
#15779=CARTESIAN_POINT ( 'NONE',  ( 1.750000000000000000, -18.75000000310999937, 12.50000000000000000 ) ) ;
#15781=CARTESIAN_POINT ( 'NONE',  ( -3.268529449828999844, -2.394807261822999855, -1.950076325099000085 ) ) ;
#15782=CARTESIAN_POINT ( 'NONE',  ( 1.845086187428521374, -0.9188386717781817925, -3.011634086822836398 ) ) ;
#15784=ORIENTED_EDGE ( 'NONE', *, *, #25263, .T. ) ;
#15786=CARTESIAN_POINT ( 'NONE',  ( -12.50000000000000000, -65.72928575305999743, 0.000000000000000000 ) ) ;
#15787=EDGE_CURVE ( 'NONE', #4635, #22997, #30576, .T. ) ;
#15791=CARTESIAN_POINT ( 'NONE',  ( -12.66008925480999814, -54.17289997881999852, 1.387046028394999908 ) ) ;
#15793=CARTESIAN_POINT ( 'NONE',  ( 1.477284502223000118, -61.52631500263999698, 12.77254812472999923 ) ) ;
#15798=CARTESIAN_POINT ( 'NONE',  ( 9.014444551600488964, -76.39432718886233431, -7.542217132489586362 ) ) ;
#15801=CARTESIAN_POINT ( 'NONE',  ( 1.750000000000000000, -58.55064714144999982, -12.65372179280999987 ) ) ;
#15802=CARTESIAN_POINT ( 'NONE',  ( -3.250000000000000000, -3.000000000000000000, 0.000000000000000000 ) ) ;
#15806=CIRCLE ( 'NONE', #42190, 1.750000000000001332 ) ;
#15807=CARTESIAN_POINT ( 'NONE',  ( 7.919595949288999570, -55.64999999965999677, -8.768124086712999699 ) ) ;
#15810=CARTESIAN_POINT ( 'NONE',  ( 0.000000000000000000, -18.84999999999999787, -11.89999999977000122 ) ) ;
#15811=CARTESIAN_POINT ( 'NONE',  ( 0.000000000000000000, -9.295797029142999435, 0.000000000000000000 ) ) ;
#15812=AXIS2_PLACEMENT_3D ( 'NONE', #16614, #7173, #3324 ) ;
#15816=EDGE_LOOP ( 'NONE', ( #5289, #52840, #20599, #33518 ) ) ;
#15820=CARTESIAN_POINT ( 'NONE',  ( -9.396085398178614767, -77.35208333333333997, -7.220923959705254802 ) ) ;
#15823=ORIENTED_EDGE ( 'NONE', *, *, #33081, .F. ) ;
#15825=ORIENTED_EDGE ( 'NONE', *, *, #19782, .F. ) ;
#15826=CARTESIAN_POINT ( 'NONE',  ( 2.764245102654999897, -2.355122700497000121, 1.982000095699999909 ) ) ;
#15833=CARTESIAN_POINT ( 'NONE',  ( -11.55452283565012728, -78.92300996100392751, 4.111075736105198608 ) ) ;
#15836=DIRECTION ( 'NONE',  ( 0.000000000000000000, -1.000000000000000000, 0.000000000000000000 ) ) ;
#15837=ADVANCED_FACE ( 'NONE', ( #39528 ), #58246, .F. ) ;
#15844=CARTESIAN_POINT ( 'NONE',  ( -3.210881389860447577, -3.087896390847898243, 0.5389748725432149667 ) ) ;
#15851=CARTESIAN_POINT ( 'NONE',  ( -8.308486710064240555, -76.26191577339538696, -8.308010501594221608 ) ) ;
#15852=CARTESIAN_POINT ( 'NONE',  ( 10.59548767699999949, -20.24263462181000151, 7.678667886068000215 ) ) ;
#15854=CARTESIAN_POINT ( 'NONE',  ( 1.103931348482591668, -24.62083748120022264, 12.50298439259066363 ) ) ;
#15858=CARTESIAN_POINT ( 'NONE',  ( -12.83836748062999966, -18.79372227161000097, -2.062147040910000229 ) ) ;
#15859=CARTESIAN_POINT ( 'NONE',  ( 12.65987830573000039, -24.93692962305999927, 0.9847759095506000149 ) ) ;
#15861=CARTESIAN_POINT ( 'NONE',  ( -3.044763360077934689, -78.30249503962149049, -11.37362071366816352 ) ) ;
#15862=AXIS2_PLACEMENT_3D ( 'NONE', #22989, #592, #14124 ) ;
#15864=CARTESIAN_POINT ( 'NONE',  ( 3.844527461940999480, -75.64423130519999461, -11.90714177081000003 ) ) ;
#15867=CARTESIAN_POINT ( 'NONE',  ( 10.36746145409304987, -55.03400544981041520, 7.635225828740804133 ) ) ;
#15868=DIRECTION ( 'NONE',  ( 0.7071067811814920612, -1.249159359038985910E-07, -0.7071067811915919821 ) ) ;
#15869=CARTESIAN_POINT ( 'NONE',  ( -1.799501877793999949, -18.71082276572999703, -12.60552511010000032 ) ) ;
#15873=CARTESIAN_POINT ( 'NONE',  ( 8.343860018000999190, -59.94999999967000548, 8.343860018000999190 ) ) ;
#15874=EDGE_CURVE ( 'NONE', #37266, #26517, #46012, .T. ) ;
#15875=VERTEX_POINT ( 'NONE', #57532 ) ;
#15876=CARTESIAN_POINT ( 'NONE',  ( -3.250000000000000000, -3.000000000000000000, 0.000000000000000000 ) ) ;
#15877=DIRECTION ( 'NONE',  ( 1.000000000000000000, 0.000000000000000000, 0.000000000000000000 ) ) ;
#15879=ORIENTED_EDGE ( 'NONE', *, *, #41105, .F. ) ;
#15882=DIRECTION ( 'NONE',  ( -1.000000000000000000, 0.000000000000000000, 0.000000000000000000 ) ) ;
#15883=B_SPLINE_CURVE_WITH_KNOTS ( 'NONE', 3,
 ( #24548, #37829, #18673, #55548, #32507, #28084, #41681, #36662, #19248, #37243 ),
 .UNSPECIFIED., .F., .F.,
 ( 4, 2, 2, 2, 4 ),
 ( 0.000000000000000000, 0.2500000000000000000, 0.5000000000000000000, 0.7500000000000000000, 1.000000000000000000 ),
 .UNSPECIFIED. ) ;
#15888=VERTEX_POINT ( 'NONE', #7657 ) ;
#15891=CARTESIAN_POINT ( 'NONE',  ( -8.485281374238999419, -18.75000000000000000, 8.485281374238999419 ) ) ;
#15893=ORIENTED_EDGE ( 'NONE', *, *, #57030, .T. ) ;
#15894=CARTESIAN_POINT ( 'NONE',  ( -12.70259419118153410, -24.73882758528178982, -1.314635108445226797 ) ) ;
#15897=CARTESIAN_POINT ( 'NONE',  ( 9.889431646000000242, -78.85035427783628847, 7.252463523969000292 ) ) ;
#15898=CARTESIAN_POINT ( 'NONE',  ( 9.243123479240180629, -24.91653773629412427, 8.441201027670452106 ) ) ;
#15899=AXIS2_PLACEMENT_3D ( 'NONE', #46420, #5372, #41678 ) ;
#15901=DIRECTION ( 'NONE',  ( 0.000000000000000000, 0.7071067811866525998, -0.7071067811864425456 ) ) ;
#15903=EDGE_CURVE ( 'NONE', #13012, #15167, #21232, .T. ) ;
#15908=CARTESIAN_POINT ( 'NONE',  ( -8.292771711448001071, -25.05529938523999789, 9.770424367364000773 ) ) ;
#15911=CARTESIAN_POINT ( 'NONE',  ( 10.53495260694000102, -60.02711197453000125, -7.618387230260000642 ) ) ;
#15912=CARTESIAN_POINT ( 'NONE',  ( -11.55418265775999842, -78.95546464548999666, 4.110954701505000308 ) ) ;
#15915=CARTESIAN_POINT ( 'NONE',  ( -3.678946202636633522, -77.94976169127751575, 11.44154515669267980 ) ) ;
#15917=ADVANCED_FACE ( 'NONE', ( #34798 ), #30364, .F. ) ;
#15918=ORIENTED_EDGE ( 'NONE', *, *, #57095, .T. ) ;
#15922=LINE ( 'NONE', #21205, #42680 ) ;
#15923=CARTESIAN_POINT ( 'NONE',  ( 1.027101072325000031, -2.234162460019999852, 3.569245810093000237 ) ) ;
#15926=VECTOR ( 'NONE', #29752, 999.9999999999998863 ) ;
#15927=CARTESIAN_POINT ( 'NONE',  ( -9.062526876912226470, -76.14485825892174375, 7.478624034300348278 ) ) ;
#15931=ORIENTED_EDGE ( 'NONE', *, *, #10109, .F. ) ;
#15932=CARTESIAN_POINT ( 'NONE',  ( -10.77133038181999503, -76.59021486849412952, -5.959359258312999508 ) ) ;
#15935=CARTESIAN_POINT ( 'NONE',  ( -7.601397897754999633, -18.75000000000000000, -9.369164850722000892 ) ) ;
#15943=CONICAL_SURFACE ( 'NONE', #20661, 12.14999999923000118, 0.7853981633972997312 ) ;
#15949=CARTESIAN_POINT ( 'NONE',  ( -7.836764916234015388, -24.30511429678721669, -9.850487231000789379 ) ) ;
#15950=EDGE_CURVE ( 'NONE', #38673, #37604, #300, .T. ) ;
#15954=EDGE_LOOP ( 'NONE', ( #41216, #21020, #25312, #1168, #16570 ) ) ;
#15955=VERTEX_POINT ( 'NONE', #54294 ) ;
#15960=CARTESIAN_POINT ( 'NONE',  ( 10.35410226330999883, -18.59601732823000120, 7.619716344073999892 ) ) ;
#15963=CARTESIAN_POINT ( 'NONE',  ( 0.6484536763455558406, -53.67597017258059822, 12.70397497887483063 ) ) ;
#15964=CARTESIAN_POINT ( 'NONE',  ( 11.66345872527999994, -77.95231164849001004, 5.269998857220999255 ) ) ;
#15966=DIRECTION ( 'NONE',  ( 0.000000000000000000, 0.000000000000000000, -1.000000000000000000 ) ) ;
#15969=VERTEX_POINT ( 'NONE', #46322 ) ;
#15974=CARTESIAN_POINT ( 'NONE',  ( 12.50412785609288058, -61.31985834570178184, -1.235051470171430577 ) ) ;
#15975=CARTESIAN_POINT ( 'NONE',  ( 7.919595949288999570, -59.94999999446000771, -8.768124086549999419 ) ) ;
#15981=CARTESIAN_POINT ( 'NONE',  ( -10.41144070832756618, -18.47453159777755261, 7.610433246107068506 ) ) ;
#15988=DIRECTION ( 'NONE',  ( 0.000000000000000000, -1.000000000000000000, 0.000000000000000000 ) ) ;
#15989=EDGE_CURVE ( 'NONE', #22563, #19308, #23584, .T. ) ;
#15991=ORIENTED_EDGE ( 'NONE', *, *, #17830, .T. ) ;
#15997=CARTESIAN_POINT ( 'NONE',  ( -9.770419344679000417, -16.94469452567000189, 8.292776877939001423 ) ) ;
#15999=CARTESIAN_POINT ( 'NONE',  ( -2.415176324861053825, -2.314881229756596603, -2.560669143145342996 ) ) ;
#16002=CARTESIAN_POINT ( 'NONE',  ( 1.807051837521999937, -54.49921584723999501, -12.77977401831000037 ) ) ;
#16006=VERTEX_POINT ( 'NONE', #55450 ) ;
#16008=CARTESIAN_POINT ( 'NONE',  ( 10.27304407731668690, -76.98877676696531580, 5.920460778062027529 ) ) ;
#16009=CARTESIAN_POINT ( 'NONE',  ( -0.9781264271446999947, -61.74031143843999558, -12.65967462882999861 ) ) ;
#16013=CARTESIAN_POINT ( 'NONE',  ( 10.47840054245999930, -23.78693148451999662, -7.622763498569999463 ) ) ;
#16016=CARTESIAN_POINT ( 'NONE',  ( 9.734666230076248539, -78.49530485907877164, 6.578030644441952290 ) ) ;
#16017=LINE ( 'NONE', #21019, #36205 ) ;
#16020=EDGE_CURVE ( 'NONE', #17027, #42621, #13949, .T. ) ;
#16021=CARTESIAN_POINT ( 'NONE',  ( -2.743382484896518925, -75.80000000000001137, -11.44562466199204032 ) ) ;
#16022=B_SPLINE_CURVE_WITH_KNOTS ( 'NONE', 3,
 ( #46399, #11535, #10669, #5926, #1519, #47275 ),
 .UNSPECIFIED., .F., .F.,
 ( 4, 1, 1, 4 ),
 ( 0.000000000000000000, 0.3333333333333000081, 0.6666666666667000474, 1.000000000000000000 ),
 .UNSPECIFIED. ) ;
#16024=CARTESIAN_POINT ( 'NONE',  ( -6.464912241513801260E-06, -79.20362641130290626, -11.95086305119197689 ) ) ;
#16025=CARTESIAN_POINT ( 'NONE',  ( 9.396085398178598780, -77.60208333333331154, 7.220923959705271677 ) ) ;
#16027=VECTOR ( 'NONE', #57680, 1000.000000000000114 ) ;
#16030=ADVANCED_FACE ( 'NONE', ( #54862 ), #35632, .T. ) ;
#16032=CARTESIAN_POINT ( 'NONE',  ( -7.770365053994759741, -54.56417299442668423, 10.20675369723379156 ) ) ;
#16035=CARTESIAN_POINT ( 'NONE',  ( 1.799502287743000029, -18.69283065396999888, 12.60413652832999887 ) ) ;
#16037=CARTESIAN_POINT ( 'NONE',  ( -7.220923959705292994, -76.22708333333335418, 9.396085398178589898 ) ) ;
#16038=ORIENTED_EDGE ( 'NONE', *, *, #32419, .F. ) ;
#16039=EDGE_LOOP ( 'NONE', ( #57416, #50030, #39184, #33308 ) ) ;
#16040=CARTESIAN_POINT ( 'NONE',  ( -12.54673279569000144, -53.97202488745999460, -0.9078290272348999990 ) ) ;
#16041=VERTEX_POINT ( 'NONE', #49575 ) ;
#16042=VERTEX_POINT ( 'NONE', #27108 ) ;
#16045=FACE_BOUND ( 'NONE', #37077, .T. ) ;
#16050=CIRCLE ( 'NONE', #43390, 1.750000000000002887 ) ;
#16057=CARTESIAN_POINT ( 'NONE',  ( 9.841120606634161661, -61.63627250028590510, 8.121699444636400145 ) ) ;
#16062=CARTESIAN_POINT ( 'NONE',  ( -9.752024281374076509, -76.65249643834691540, 6.553952695904345482 ) ) ;
#16066=ADVANCED_FACE ( 'NONE', ( #19147 ), #37142, .F. ) ;
#16068=CARTESIAN_POINT ( 'NONE',  ( 1.931086388455000025, -18.70221404512000163, -12.71798280854999952 ) ) ;
#16070=VECTOR ( 'NONE', #48213, 1000.000000000000114 ) ;
#16071=CYLINDRICAL_SURFACE ( 'NONE', #45749, 0.5000000000000006661 ) ;
#16073=CIRCLE ( 'NONE', #56611, 0.5000000000000001110 ) ;
#16074=CARTESIAN_POINT ( 'NONE',  ( -1.639137479228926164, -1.184957622258020926, -2.839660048845916052 ) ) ;
#16078=LINE ( 'NONE', #47967, #48666 ) ;
#16080=CARTESIAN_POINT ( 'NONE',  ( -3.248956906310343395, -1.591438635919541156, 0.4262020595363264497 ) ) ;
#16081=FACE_OUTER_BOUND ( 'NONE', #23158, .T. ) ;
#16082=DIRECTION ( 'NONE',  ( 0.000000000000000000, 1.000000000000000000, 0.000000000000000000 ) ) ;
#16085=CARTESIAN_POINT ( 'NONE',  ( -12.66761570926000147, -54.57632520071999949, 1.696752301450999978 ) ) ;
#16086=DIRECTION ( 'NONE',  ( 0.000000000000000000, -1.000000000000000000, 0.000000000000000000 ) ) ;
#16094=VECTOR ( 'NONE', #8097, 1000.000000000000000 ) ;
#16095=CARTESIAN_POINT ( 'NONE',  ( 2.381202143020299644, -76.34051971754411170, -11.52415263934972245 ) ) ;
#16101=CARTESIAN_POINT ( 'NONE',  ( -1.004305231718999991, -3.500000000000000000, 3.090933677959000203 ) ) ;
#16104=CARTESIAN_POINT ( 'NONE',  ( 4.914100338553271996, -75.80000000000001137, 11.02085870159172032 ) ) ;
#16105=EDGE_CURVE ( 'NONE', #18787, #54024, #13015, .T. ) ;
#16110=CARTESIAN_POINT ( 'NONE',  ( 7.648026768036999989, -60.04999998387000204, 10.12290050219000115 ) ) ;
#16112=VERTEX_POINT ( 'NONE', #32699 ) ;
#16113=CARTESIAN_POINT ( 'NONE',  ( -1.636761686205434385, -1.416666666666666297, 2.839805762151331958 ) ) ;
#16114=ORIENTED_EDGE ( 'NONE', *, *, #55399, .T. ) ;
#16117=EDGE_CURVE ( 'NONE', #13664, #11409, #50747, .T. ) ;
#16119=CARTESIAN_POINT ( 'NONE',  ( -3.444266691755999865, -78.40360489188999793, 11.59182779477000125 ) ) ;
#16120=CARTESIAN_POINT ( 'NONE',  ( 0.6330385443858000949, -2.195518323557999807, -3.341926243291000187 ) ) ;
#16121=ORIENTED_EDGE ( 'NONE', *, *, #2763, .T. ) ;
#16134=AXIS2_PLACEMENT_3D ( 'NONE', #56615, #57760, #8177 ) ;
#16141=CARTESIAN_POINT ( 'NONE',  ( 9.000000000000000000, -0.2000000000000000111, 0.000000000000000000 ) ) ;
#16144=CARTESIAN_POINT ( 'NONE',  ( -6.767262360081500283, -76.27600367820089389, -9.605998308841860123 ) ) ;
#16145=CARTESIAN_POINT ( 'NONE',  ( 10.21381326472000062, -22.77129148951999937, 7.668949790003000366 ) ) ;
#16146=CARTESIAN_POINT ( 'NONE',  ( -7.622785526051999661, -60.58712283452999259, -10.47836401508999948 ) ) ;
#16149=AXIS2_PLACEMENT_3D ( 'NONE', #18517, #31477, #49221 ) ;
#16151=CARTESIAN_POINT ( 'NONE',  ( -12.97861384075000046, -78.05778978748000441, -0.9459496016724999734 ) ) ;
#16152=VECTOR ( 'NONE', #3103, 1000.000000000000000 ) ;
#16154=CARTESIAN_POINT ( 'NONE',  ( -10.26030881462940947, -78.24069963102668623, -5.914557015925677952 ) ) ;
#16156=CARTESIAN_POINT ( 'NONE',  ( -0.5999999999999999778, -18.84999999999999787, -10.98362417419999915 ) ) ;
#16157=CARTESIAN_POINT ( 'NONE',  ( -12.26667365293000067, -76.09135856455000635, -1.533824757711000020 ) ) ;
#16158=EDGE_LOOP ( 'NONE', ( #40316, #50178, #1733, #53932 ) ) ;
#16161=CARTESIAN_POINT ( 'NONE',  ( 12.54715528154999937, -61.33180535358000185, 1.292252957172000061 ) ) ;
#16162=CARTESIAN_POINT ( 'NONE',  ( -5.286038998608000306, -79.16541925342001207, 11.30782674599000082 ) ) ;
#16163=CARTESIAN_POINT ( 'NONE',  ( -12.50000000000000000, -18.75000000000000000, -1.250000000000000000 ) ) ;
#16168=VERTEX_POINT ( 'NONE', #33581 ) ;
#16171=VERTEX_POINT ( 'NONE', #33863 ) ;
#16174=CARTESIAN_POINT ( 'NONE',  ( -8.190836719257346132, -55.61035107871763472, -7.342356150419313998 ) ) ;
#16181=ORIENTED_EDGE ( 'NONE', *, *, #1537, .F. ) ;
#16184=CARTESIAN_POINT ( 'NONE',  ( 11.74527629117004857, -77.95727216427877693, 1.539259998173173827 ) ) ;
#16187=ORIENTED_EDGE ( 'NONE', *, *, #2907, .F. ) ;
#16188=CARTESIAN_POINT ( 'NONE',  ( -2.599682250000723727, -2.548992540563667752, 1.997718607485681863 ) ) ;
#16192=CARTESIAN_POINT ( 'NONE',  ( 9.502896617881404495, -24.74094210335991662, 8.179425869167879171 ) ) ;
#16193=CIRCLE ( 'NONE', #7712, 1.750000000000001332 ) ;
#16194=CARTESIAN_POINT ( 'NONE',  ( 8.194873807802000698, -54.08956116737999764, 9.389185139509999445 ) ) ;
#16195=CARTESIAN_POINT ( 'NONE',  ( 7.610717068332717439, -18.47984996834297888, -10.41172376763008245 ) ) ;
#16201=CARTESIAN_POINT ( 'NONE',  ( -11.84062247810999935, -76.42595468096000388, 3.366775603358000080 ) ) ;
#16205=CARTESIAN_POINT ( 'NONE',  ( 10.31986335556999990, -61.08918510704999960, -7.753844818055000587 ) ) ;
#16206=CARTESIAN_POINT ( 'NONE',  ( 12.16303714866999997, -79.20820515958999408, 1.568404430622000190 ) ) ;
#16207=DIRECTION ( 'NONE',  ( -1.000000000000000000, 0.000000000000000000, 0.000000000000000000 ) ) ;
#16208=CARTESIAN_POINT ( 'NONE',  ( -7.342356150419245608, -59.98964892062633680, -8.190836719257406529 ) ) ;
#16213=CYLINDRICAL_SURFACE ( 'NONE', #27631, 0.5000000000000004441 ) ;
#16215=CARTESIAN_POINT ( 'NONE',  ( 3.553889031728000081, -2.214840391789000051, -0.1653587369246999894 ) ) ;
#16218=CARTESIAN_POINT ( 'NONE',  ( 0.000000000000000000, -6.100000000000000533, 0.000000000000000000 ) ) ;
#16222=ORIENTED_EDGE ( 'NONE', *, *, #35956, .T. ) ;
#16229=CARTESIAN_POINT ( 'NONE',  ( 1.025029370886000101E-14, -0.2000000000000005107, 0.000000000000000000 ) ) ;
#16232=CARTESIAN_POINT ( 'NONE',  ( -12.70556836343000029, -53.57227722738999631, 1.774192865971000122E-09 ) ) ;
#16234=AXIS2_PLACEMENT_3D ( 'NONE', #20295, #37710, #46015 ) ;
#16235=DIRECTION ( 'NONE',  ( 0.000000000000000000, -1.000000000000000000, 0.000000000000000000 ) ) ;
#16242=EDGE_CURVE ( 'NONE', #52133, #9420, #1372, .T. ) ;
#16244=CARTESIAN_POINT ( 'NONE',  ( 10.18496935386000146, -58.55064714674999493, -7.710095619709000481 ) ) ;
#16247=CARTESIAN_POINT ( 'NONE',  ( 1.532229594833856012, -17.87701036868171300, -12.51228690880882688 ) ) ;
#16248=DIRECTION ( 'NONE',  ( 0.000000000000000000, -1.000000000000000000, 0.000000000000000000 ) ) ;
#16250=VERTEX_POINT ( 'NONE', #33512 ) ;
#16251=EDGE_CURVE ( 'NONE', #9948, #37958, #47457, .T. ) ;
#16257=CARTESIAN_POINT ( 'NONE',  ( 7.974020021247000933, -17.36898233693000293, 9.929669236791999865 ) ) ;
#16259=CARTESIAN_POINT ( 'NONE',  ( 1.980584515752000119, -55.53514853344000102, 12.76303204600000107 ) ) ;
#16260=CARTESIAN_POINT ( 'NONE',  ( 9.135190432272999317, -76.77363952651001000, -8.185884657762999339 ) ) ;
#16262=CARTESIAN_POINT ( 'NONE',  ( -11.79999999999999893, -18.84999999999000053, 0.5999999999999999778 ) ) ;
#16266=EDGE_LOOP ( 'NONE', ( #47534, #17040, #48354, #11, #7765 ) ) ;
#16267=CARTESIAN_POINT ( 'NONE',  ( 7.644092900757153863, -55.27619833568790142, -10.09634159697595912 ) ) ;
#16272=LINE ( 'NONE', #15975, #8805 ) ;
#16279=CARTESIAN_POINT ( 'NONE',  ( -12.49306764015999960, -18.71943464842000182, -1.667917367065999912 ) ) ;
#16280=DIRECTION ( 'NONE',  ( 0.000000000000000000, 1.000000000000000000, 0.000000000000000000 ) ) ;
#16283=DIRECTION ( 'NONE',  ( -1.000000000000000000, 0.000000000000000000, 0.000000000000000000 ) ) ;
#16284=AXIS2_PLACEMENT_3D ( 'NONE', #54573, #4968, #31818 ) ;
#16285=B_SPLINE_CURVE_WITH_KNOTS ( 'NONE', 3,
 ( #12173, #34015, #42898, #20461, #7163, #2744 ),
 .UNSPECIFIED., .F., .F.,
 ( 4, 1, 1, 4 ),
 ( 0.000000000000000000, 0.3333333333333000081, 0.6666666666667000474, 1.000000000000000000 ),
 .UNSPECIFIED. ) ;
#16286=CARTESIAN_POINT ( 'NONE',  ( -7.710095619827000313, -58.55064714318000085, -10.18496935397999970 ) ) ;
#16288=ORIENTED_EDGE ( 'NONE', *, *, #39828, .F. ) ;
#16291=CARTESIAN_POINT ( 'NONE',  ( 10.12290050126000196, -60.04999999958999979, 7.648026767103999646 ) ) ;
#16294=EDGE_CURVE ( 'NONE', #51331, #3286, #160, .T. ) ;
#16297=CARTESIAN_POINT ( 'NONE',  ( 0.1434218413062385844, -2.378208186945148572, -3.516600075276243409 ) ) ;
#16301=CARTESIAN_POINT ( 'NONE',  ( 8.343860018000999190, -59.94999999967000548, 8.343860018000999190 ) ) ;
#16303=EDGE_LOOP ( 'NONE', ( #12043, #56744, #56261, #45968 ) ) ;
#16306=CARTESIAN_POINT ( 'NONE',  ( 1.582498447116000184, -60.95086122444999432, -12.55493832976000057 ) ) ;
#16312=CARTESIAN_POINT ( 'NONE',  ( 11.53783733622431917, -78.46305301807434773, 2.299832388111439307 ) ) ;
#16313=CARTESIAN_POINT ( 'NONE',  ( -8.532660243106189313, -61.92798380497763588, 9.433531203738310111 ) ) ;
#16316=CARTESIAN_POINT ( 'NONE',  ( 12.56594317982999875, -55.55000000504000468, -1.750000000000000000 ) ) ;
#16319=ADVANCED_FACE ( 'NONE', ( #51187 ), #803, .F. ) ;
#16320=FACE_OUTER_BOUND ( 'NONE', #4806, .T. ) ;
#16325=B_SPLINE_SURFACE_WITH_KNOTS ( 'NONE', 3, 3, ( 
 ( #15858, #33844, #51882, #56591 ),
 ( #11438, #29418, #34127, #13443 ),
 ( #48606, #25861, #17295, #53608 ),
 ( #8153, #21437, #31443, #17893 ),
 ( #9033, #53313, #44453, #12856 ),
 ( #30574, #17012, #13147, #48895 ),
 ( #43890, #48322, #31141, #26152 ),
 ( #49180, #3436, #49484, #12577 ),
 ( #44172, #58329, #3720, #39446 ),
 ( #27020, #21723, #7862, #39728 ),
 ( #35882, #21145, #53912, #8732 ) ),
 .UNSPECIFIED., .F., .F., .F.,
 ( 4, 1, 1, 1, 1, 1, 1, 1, 4 ),
 ( 4, 4 ),
 ( -0.02001211456244999728, 0.000000000000000000, 0.1666666666667000196, 0.3333333333333000081, 0.5000000000000000000, 0.6666666666667000474, 0.8333333333333000637, 1.000000000000000000, 1.020273719995999917 ),
 ( -0.3582002740325999635, 1.358863140973999961 ),
 .UNSPECIFIED. ) ;
#16330=CARTESIAN_POINT ( 'NONE',  ( 11.74999999999999289, -76.06041666666665435, 1.538071403320028452 ) ) ;
#16334=CARTESIAN_POINT ( 'NONE',  ( -12.46083735077000121, -55.11664398755999628, -1.628985986890000071 ) ) ;
#16338=AXIS2_PLACEMENT_3D ( 'NONE', #2655, #20366, #56095 ) ;
#16341=AXIS2_PLACEMENT_3D ( 'NONE', #19721, #7297, #46898 ) ;
#16345=ORIENTED_EDGE ( 'NONE', *, *, #5454, .T. ) ;
#16350=CARTESIAN_POINT ( 'NONE',  ( 7.718346056094000041, -21.74888345808999901, 10.07719973192000040 ) ) ;
#16355=FACE_OUTER_BOUND ( 'NONE', #6340, .T. ) ;
#16356=CARTESIAN_POINT ( 'NONE',  ( -7.956418361354000268, -54.27110680110000374, 9.787952249823998585 ) ) ;
#16359=CARTESIAN_POINT ( 'NONE',  ( -9.650965486090999690, -17.06598967526999999, -8.252456812006998987 ) ) ;
#16362=CARTESIAN_POINT ( 'NONE',  ( 0.9113424693944999211, -17.17464206440000041, -12.54674099557999867 ) ) ;
#16365=CARTESIAN_POINT ( 'NONE',  ( 0.1739064196789271433, -3.499999999999999556, 3.294261630741291746 ) ) ;
#16366=CARTESIAN_POINT ( 'NONE',  ( 3.493916750265503524, -1.488669189522607184, -0.5022341488964027212 ) ) ;
#16367=EDGE_CURVE ( 'NONE', #38753, #14405, #53063, .T. ) ;
#16370=DIRECTION ( 'NONE',  ( 1.000000000000000000, 0.000000000000000000, 0.000000000000000000 ) ) ;
#16372=CARTESIAN_POINT ( 'NONE',  ( -3.144532066837999906, -1.606752247163000025, 1.008949614594999877 ) ) ;
#16374=CARTESIAN_POINT ( 'NONE',  ( -12.55485633992000061, -54.64594908747999824, 1.580761757393000178 ) ) ;
#16375=CARTESIAN_POINT ( 'NONE',  ( 1.666698456695999919, -59.99181739808000202, 12.50018138922999889 ) ) ;
#16376=DIRECTION ( 'NONE',  ( 0.000000000000000000, 1.000000000000000000, 0.000000000000000000 ) ) ;
#16377=AXIS2_PLACEMENT_3D ( 'NONE', #50287, #36397, #13961 ) ;
#16384=CARTESIAN_POINT ( 'NONE',  ( -1.635567090190121142, -1.018497397474406929, 2.827602005665806661 ) ) ;
#16390=CARTESIAN_POINT ( 'NONE',  ( -10.25203062050054470, -17.87822876372841208, -7.730397977282122746 ) ) ;
#16394=DIRECTION ( 'NONE',  ( 0.000000000000000000, 0.000000000000000000, -1.000000000000000000 ) ) ;
#16396=EDGE_CURVE ( 'NONE', #24848, #1462, #38943, .T. ) ;
#16397=CARTESIAN_POINT ( 'NONE',  ( 0.000000000000000000, -23.15000000000000213, 11.89999999977000122 ) ) ;
#16398=ADVANCED_FACE ( 'NONE', ( #23691 ), #45567, .T. ) ;
#16400=ORIENTED_EDGE ( 'NONE', *, *, #49929, .T. ) ;
#16401=CARTESIAN_POINT ( 'NONE',  ( -0.8506806241676722058, -1.395833333333332815, 3.165411199172021739 ) ) ;
#16403=CIRCLE ( 'NONE', #49410, 1.749999999999997335 ) ;
#16408=CARTESIAN_POINT ( 'NONE',  ( -10.47313876284000145, -78.46108632805000127, 6.560901509735000303 ) ) ;
#16409=CARTESIAN_POINT ( 'NONE',  ( 10.53559655518999882, -60.00569178284000316, 7.620036226177999694 ) ) ;
#16417=ADVANCED_FACE ( 'NONE', ( #6264 ), #23111, .F. ) ;
#16420=DIRECTION ( 'NONE',  ( -1.000000000000000000, 0.000000000000000000, 0.000000000000000000 ) ) ;
#16423=DIRECTION ( 'NONE',  ( 0.7071067811865475727, 0.000000000000000000, 0.7071067811865475727 ) ) ;
#16427=CARTESIAN_POINT ( 'NONE',  ( 2.291577237701493353, -2.913270536965290702, 2.304101226941956515 ) ) ;
#16430=CARTESIAN_POINT ( 'NONE',  ( 12.00000000000000000, -55.54999999966999980, 0.000000000000000000 ) ) ;
#16431=CARTESIAN_POINT ( 'NONE',  ( -7.714303428875997959, -52.49705297113997204, 12.53545825868000385 ) ) ;
#16433=CARTESIAN_POINT ( 'NONE',  ( 10.38646360829000059, -22.77795407709999864, 7.655555357433999397 ) ) ;
#16434=EDGE_CURVE ( 'NONE', #11513, #19894, #31848, .T. ) ;
#16435=CARTESIAN_POINT ( 'NONE',  ( -7.956422463042999382, -61.32889896150999931, -9.787948076380001083 ) ) ;
#16440=CARTESIAN_POINT ( 'NONE',  ( 6.891227191158999510, -76.72567840438999553, -9.824000600561999974 ) ) ;
#16441=CARTESIAN_POINT ( 'NONE',  ( 12.50000000000000000, -23.24999999758999536, -1.750000000000000000 ) ) ;
#16442=CARTESIAN_POINT ( 'NONE',  ( 1.583004792607182853, -24.45209241162641334, -12.70616254410850665 ) ) ;
#16443=CARTESIAN_POINT ( 'NONE',  ( -11.84510048553000061, -75.96827307386000427, 4.031494313132999885 ) ) ;
#16444=ORIENTED_EDGE ( 'NONE', *, *, #7321, .T. ) ;
#16445=AXIS2_PLACEMENT_3D ( 'NONE', #13253, #8537, #53128 ) ;
#16449=CARTESIAN_POINT ( 'NONE',  ( -10.98449626305583138, -18.69382183571932643, -0.5845794248139971616 ) ) ;
#16450=CARTESIAN_POINT ( 'NONE',  ( -11.13365145556000080, -79.12931983984000794, 5.979534326088000284 ) ) ;
#16451=CARTESIAN_POINT ( 'NONE',  ( 12.61117324687999997, -55.58448536084999603, -1.798979683803999974 ) ) ;
#16456=ORIENTED_EDGE ( 'NONE', *, *, #42515, .F. ) ;
#16462=CARTESIAN_POINT ( 'NONE',  ( -10.48771805367000098, -58.55560171494000343, 7.686918321054999836 ) ) ;
#16470=B_SPLINE_CURVE_WITH_KNOTS ( 'NONE', 3,
 ( #19570, #28410, #36695, #5692, #50294, #18993, #15435, #45873, #54999, #14548, #32540, #46457, #50586, #10141, #46167, #23702, #37570, #55585, #33131, #10727, #51173, #12447, #38446, #57322 ),
 .UNSPECIFIED., .F., .F.,
 ( 4, 2, 2, 2, 2, 2, 2, 2, 2, 2, 2, 4 ),
 ( 0.000000000000000000, 0.1249999999999980294, 0.2499999999999960587, 0.3749999999999941158, 0.4374999999999937272, 0.4999999999999933387, 0.6249999999999925615, 0.7499999999999917843, 0.8124999999999926725, 0.8437499999999944489, 0.8749999999999963363, 1.000000000000000000 ),
 .UNSPECIFIED. ) ;
#16471=CARTESIAN_POINT ( 'NONE',  ( 11.79999999999999893, -18.84999999999000053, -0.5999999999999999778 ) ) ;
#16473=AXIS2_PLACEMENT_3D ( 'NONE', #36890, #51368, #10924 ) ;
#16474=ORIENTED_EDGE ( 'NONE', *, *, #13710, .T. ) ;
#16475=CARTESIAN_POINT ( 'NONE',  ( -3.250000000000000000, -2.600000000000000089, 0.000000000000000000 ) ) ;
#16477=CARTESIAN_POINT ( 'NONE',  ( -10.39285214024000048, -78.50546566091685463, 6.510605926401999533 ) ) ;
#16480=CARTESIAN_POINT ( 'NONE',  ( 7.619389775666999931, -55.39213701549999769, 10.35398629634000045 ) ) ;
#16481=EDGE_CURVE ( 'NONE', #18065, #42621, #25143, .T. ) ;
#16482=CARTESIAN_POINT ( 'NONE',  ( 7.792421629684946005, -17.70899070367055472, -10.18245656324600290 ) ) ;
#16483=DIRECTION ( 'NONE',  ( -0.7071067811865475727, 0.000000000000000000, 0.7071067811865475727 ) ) ;
#16486=CARTESIAN_POINT ( 'NONE',  ( 12.71466317168506066, -60.93795986706761170, -1.778778223978346285 ) ) ;
#16489=CARTESIAN_POINT ( 'NONE',  ( 3.007117222848000093, -75.80336186172000623, 11.93703523519999976 ) ) ;
#16490=LINE ( 'NONE', #25050, #45993 ) ;
#16492=CARTESIAN_POINT ( 'NONE',  ( 10.13694968399000018, -60.50834319308000175, -7.646073915548999622 ) ) ;
#16493=CARTESIAN_POINT ( 'NONE',  ( 9.889431646000000242, -78.78302033703000973, 7.252463523969000292 ) ) ;
#16495=CARTESIAN_POINT ( 'NONE',  ( -7.429974109835268514, -60.31614597266563749, -8.111636311568133806 ) ) ;
#16496=ADVANCED_FACE ( 'NONE', ( #57019 ), #21290, .F. ) ;
#16497=CARTESIAN_POINT ( 'NONE',  ( -26.50000000000000000, -39.30476017083000073, -1.122808443442999720E-13 ) ) ;
#16500=CARTESIAN_POINT ( 'NONE',  ( 1.247385801072999900, -24.47722256257999973, 12.50301438876999960 ) ) ;
#16501=CARTESIAN_POINT ( 'NONE',  ( 2.977898218353999926, -3.172466653419999894, -1.946686942756000072 ) ) ;
#16505=CARTESIAN_POINT ( 'NONE',  ( -2.787965030838566616, -75.80000000000003979, 11.63553696988441466 ) ) ;
#16512=EDGE_CURVE ( 'NONE', #35685, #42541, #57308, .T. ) ;
#16515=CARTESIAN_POINT ( 'NONE',  ( -7.974014308154000474, -61.43100890296999950, 9.929675091768999096 ) ) ;
#16516=AXIS2_PLACEMENT_3D ( 'NONE', #32207, #15388, #9799 ) ;
#16517=DIRECTION ( 'NONE',  ( 0.000000000000000000, 1.000000000000000000, 0.000000000000000000 ) ) ;
#16521=ORIENTED_EDGE ( 'NONE', *, *, #890, .F. ) ;
#16522=CARTESIAN_POINT ( 'NONE',  ( -12.70259395223330756, -54.06112126474956625, 1.314575638834851512 ) ) ;
#16525=CARTESIAN_POINT ( 'NONE',  ( -12.65375411747000101, -58.54977139013999476, 1.750000000000000000 ) ) ;
#16526=CIRCLE ( 'NONE', #11810, 14.00000000000000000 ) ;
#16533=EDGE_CURVE ( 'NONE', #37604, #44143, #24217, .T. ) ;
#16536=VERTEX_POINT ( 'NONE', #12150 ) ;
#16537=ORIENTED_EDGE ( 'NONE', *, *, #31016, .T. ) ;
#16541=ORIENTED_EDGE ( 'NONE', *, *, #51767, .F. ) ;
#16544=CARTESIAN_POINT ( 'NONE',  ( -1.718598680027600967, -54.55037066937041601, 12.71111582765235681 ) ) ;
#16545=CARTESIAN_POINT ( 'NONE',  ( -1.300465888139999970, -78.37242034399000090, -12.57433635189999954 ) ) ;
#16551=ORIENTED_EDGE ( 'NONE', *, *, #22643, .T. ) ;
#16552=CARTESIAN_POINT ( 'NONE',  ( -5.747123378374999980, -78.21567021303999923, 10.24856442990000005 ) ) ;
#16558=CARTESIAN_POINT ( 'NONE',  ( 10.78724245695320505, -76.48279647566602080, 4.717496507233430947 ) ) ;
#16563=CARTESIAN_POINT ( 'NONE',  ( -1.750000000001000089, -23.24999998674999802, 12.56594318051000059 ) ) ;
#16567=CARTESIAN_POINT ( 'NONE',  ( 10.01234990228999955, -23.29849137228000444, -7.653559502275999016 ) ) ;
#16570=ORIENTED_EDGE ( 'NONE', *, *, #52416, .F. ) ;
#16573=CARTESIAN_POINT ( 'NONE',  ( -8.190859204290999784, -59.94999999967000548, -7.342331066867000544 ) ) ;
#16576=DIRECTION ( 'NONE',  ( 1.000000000000000000, 0.000000000000000000, 0.000000000000000000 ) ) ;
#16577=DIRECTION ( 'NONE',  ( -0.9936845293270585300, 0.1122098755727947705, 0.000000000000000000 ) ) ;
#16581=CARTESIAN_POINT ( 'NONE',  ( 10.88122807191786023, -75.98028698031052386, 4.433341873219495355 ) ) ;
#16583=ORIENTED_EDGE ( 'NONE', *, *, #1310, .F. ) ;
#16584=DIRECTION ( 'NONE',  ( -1.000000000000000000, 0.000000000000000000, 0.000000000000000000 ) ) ;
#16585=CARTESIAN_POINT ( 'NONE',  ( -7.217308068640586605, -77.12565399570821967, 9.390397901522751667 ) ) ;
#16592=CARTESIAN_POINT ( 'NONE',  ( 10.01752098897000032, -23.19172009652000099, -7.660412494176999765 ) ) ;
#16593=CARTESIAN_POINT ( 'NONE',  ( 1.980584515752000119, -18.73514853375999678, 12.76303204602000108 ) ) ;
#16595=LINE ( 'NONE', #13306, #3822 ) ;
#16600=CARTESIAN_POINT ( 'NONE',  ( 10.12290050255000118, -55.55000002206000431, 7.648026768392999664 ) ) ;
#16603=CARTESIAN_POINT ( 'NONE',  ( -12.50000000000000000, -23.44678171330999916, -1.250000000000000000 ) ) ;
#16604=CARTESIAN_POINT ( 'NONE',  ( 9.050966798898000931, -59.94999999040999938, 7.919595949288999570 ) ) ;
#16609=AXIS2_PLACEMENT_3D ( 'NONE', #30636, #43663, #21502 ) ;
#16612=CARTESIAN_POINT ( 'NONE',  ( -12.70451681032499991, -61.97641660171719735, -0.5206746370656520906 ) ) ;
#16614=CARTESIAN_POINT ( 'NONE',  ( 8.485281374238999419, -55.64999999967000122, 8.485281374238999419 ) ) ;
#16617=CARTESIAN_POINT ( 'NONE',  ( -12.72394144133999916, -55.57839271467000231, -1.930881231431999856 ) ) ;
#16618=EDGE_LOOP ( 'NONE', ( #24432, #41817, #3647 ) ) ;
#16621=CARTESIAN_POINT ( 'NONE',  ( -7.247844507162001015, -55.54999999966999980, -9.722718241315000398 ) ) ;
#16626=ORIENTED_EDGE ( 'NONE', *, *, #3805, .T. ) ;
#16627=ORIENTED_EDGE ( 'NONE', *, *, #11674, .F. ) ;
#16631=CARTESIAN_POINT ( 'NONE',  ( -12.66315196852000113, -61.97802884675999735, 0.06065366946605000448 ) ) ;
#16633=CARTESIAN_POINT ( 'NONE',  ( 7.682331425175999762, -22.76486430425999785, 10.04115011118000211 ) ) ;
#16634=B_SPLINE_CURVE_WITH_KNOTS ( 'NONE', 3,
 ( #873, #41290, #9418, #27407, #23567, #45442 ),
 .UNSPECIFIED., .F., .F.,
 ( 4, 2, 4 ),
 ( 0.000000000000000000, 0.5000000000000000000, 1.000000000000000000 ),
 .UNSPECIFIED. ) ;
#16635=CARTESIAN_POINT ( 'NONE',  ( 9.689272046963719021, -61.77888144132615622, 8.274769670150060819 ) ) ;
#16639=EDGE_CURVE ( 'NONE', #36944, #5427, #27127, .T. ) ;
#16641=ORIENTED_EDGE ( 'NONE', *, *, #531, .T. ) ;
#16645=CARTESIAN_POINT ( 'NONE',  ( -7.948094694409999050, -17.55965255610999876, -9.636752590488001147 ) ) ;
#16648=CARTESIAN_POINT ( 'NONE',  ( -1.466594960159999905, -17.91841800947999985, -12.44238958332999800 ) ) ;
#16651=CARTESIAN_POINT ( 'NONE',  ( 12.80090744921000123, -19.23767312576000066, 1.980532734072999901 ) ) ;
#16653=CARTESIAN_POINT ( 'NONE',  ( 0.9372783843427989758, -3.499999999999999112, 3.216071100383696368 ) ) ;
#16654=CARTESIAN_POINT ( 'NONE',  ( -3.408105548625404158, -0.7711048338445120054, -0.9268356498114088682 ) ) ;
#16655=VECTOR ( 'NONE', #434, 1000.000000000000000 ) ;
#16659=CARTESIAN_POINT ( 'NONE',  ( -12.69619287811000063, -21.75083378359999742, 1.799475295154000065 ) ) ;
#16660=EDGE_CURVE ( 'NONE', #45569, #18184, #8929, .T. ) ;
#16661=VECTOR ( 'NONE', #10482, 1000.000000000000114 ) ;
#16662=CARTESIAN_POINT ( 'NONE',  ( 1.121545512341999951, -2.281343295938000004, -3.469001545188000524 ) ) ;
#16664=CARTESIAN_POINT ( 'NONE',  ( -12.77301916222999800, -53.74808379519999590, 1.052060437763999934 ) ) ;
#16666=CYLINDRICAL_SURFACE ( 'NONE', #56226, 3.250000000000000000 ) ;
#16672=CARTESIAN_POINT ( 'NONE',  ( 10.62752749630825377, -76.41453037466249043, -5.012216836189437252 ) ) ;
#16675=CARTESIAN_POINT ( 'NONE',  ( 1.750000000001000089, -60.04999998641999781, -12.56594318054000148 ) ) ;
#16678=CARTESIAN_POINT ( 'NONE',  ( -1.997276839918471714, -2.572916666666666519, -2.598917237794086788 ) ) ;
#16680=CARTESIAN_POINT ( 'NONE',  ( -11.79999999999999893, -23.15000000000000213, 0.000000000000000000 ) ) ;
#16681=CARTESIAN_POINT ( 'NONE',  ( -9.175589924978867273, -16.77304466868007538, -8.792768277111136399 ) ) ;
#16685=CARTESIAN_POINT ( 'NONE',  ( -10.98960559191257147, -23.51693928699113911, -0.4813395862331206199 ) ) ;
#16686=ORIENTED_EDGE ( 'NONE', *, *, #39527, .F. ) ;
#16687=CARTESIAN_POINT ( 'NONE',  ( -1.760728164551675023, -0.7500000000000000000, 3.046994028780342312 ) ) ;
#16688=ORIENTED_EDGE ( 'NONE', *, *, #55984, .T. ) ;
#16690=ORIENTED_EDGE ( 'NONE', *, *, #39130, .F. ) ;
#16692=DIRECTION ( 'NONE',  ( 0.7026410690473252618, 0.1122098755728027641, 0.7026410690473252618 ) ) ;
#16693=ORIENTED_EDGE ( 'NONE', *, *, #25230, .T. ) ;
#16694=CIRCLE ( 'NONE', #26072, 12.80000000000000071 ) ;
#16697=VERTEX_POINT ( 'NONE', #39349 ) ;
#16698=CARTESIAN_POINT ( 'NONE',  ( -7.389227917444999960, -78.34526476023999919, 9.720412100329001603 ) ) ;
#16700=CARTESIAN_POINT ( 'NONE',  ( -7.654537165486999584, -60.08056535122999975, 10.01332852690999964 ) ) ;
#16701=ORIENTED_EDGE ( 'NONE', *, *, #29008, .T. ) ;
#16704=CARTESIAN_POINT ( 'NONE',  ( -10.99999999999999822, -18.24999999999999645, 0.1600933372533455690 ) ) ;
#16706=CARTESIAN_POINT ( 'NONE',  ( -10.42531124905999995, -23.26485148473999942, -7.624341765453999997 ) ) ;
#16709=CARTESIAN_POINT ( 'NONE',  ( 7.468771752218000159, -77.17884144764001064, -10.77882862479000003 ) ) ;
#16716=CARTESIAN_POINT ( 'NONE',  ( 2.786504344070804606, -2.894472130040342872, 1.673888437967501641 ) ) ;
#16720=CARTESIAN_POINT ( 'NONE',  ( 3.521688171515000132, -3.548588873046000014, 0.7298424208991000084 ) ) ;
#16721=CARTESIAN_POINT ( 'NONE',  ( 10.18491080493000212, -23.30716680861999990, 7.640030264156999706 ) ) ;
#16722=CARTESIAN_POINT ( 'NONE',  ( -7.633478499842999199, -60.00098177563999968, -10.36292345936000103 ) ) ;
#16726=FACE_OUTER_BOUND ( 'NONE', #44838, .T. ) ;
#16728=CARTESIAN_POINT ( 'NONE',  ( -1.264141272797000060, -77.66925730074001422, -12.95149364859999963 ) ) ;
#16729=AXIS2_PLACEMENT_3D ( 'NONE', #4597, #32301, #22594 ) ;
#16732=CARTESIAN_POINT ( 'NONE',  ( -11.89104863444000060, -76.55941889705000847, 3.380364376359000111 ) ) ;
#16735=AXIS2_PLACEMENT_3D ( 'NONE', #25173, #39614, #57619 ) ;
#16736=CARTESIAN_POINT ( 'NONE',  ( 12.54987272481000105, -61.85113590103000547, 0.1385846084898000041 ) ) ;
#16737=CARTESIAN_POINT ( 'NONE',  ( 10.85397020026000092, -79.29714617087998363, -4.993565566466998895 ) ) ;
#16738=CARTESIAN_POINT ( 'NONE',  ( 7.654537085030999499, -18.71943307332999851, -10.01332844637000008 ) ) ;
#16742=CARTESIAN_POINT ( 'NONE',  ( -12.65372179310999989, -20.24935286375000132, 1.750000000000000000 ) ) ;
#16744=ORIENTED_EDGE ( 'NONE', *, *, #35296, .T. ) ;
#16748=AXIS2_PLACEMENT_3D ( 'NONE', #8518, #53996, #12939 ) ;
#16752=CARTESIAN_POINT ( 'NONE',  ( -9.931052046351343421, -60.92278631065439498, -7.764003813311978419 ) ) ;
#16757=B_SPLINE_CURVE_WITH_KNOTS ( 'NONE', 3,
 ( #48096, #16208, #7340, #20914, #38917, #56935, #16495, #3210, #15335, #42496, #17064, #49237, #8203, #22362, #39779, #16784, #3486, #21492 ),
 .UNSPECIFIED., .F., .F.,
 ( 4, 2, 2, 2, 2, 2, 2, 2, 4 ),
 ( 0.000000000000000000, 0.06250000000000272005, 0.1250000000000054401, 0.2500000000000012768, 0.5000000000000001110, 0.7499999999999960032, 0.8124999999999945599, 0.8749999999999932276, 1.000000000000000000 ),
 .UNSPECIFIED. ) ;
#16762=ADVANCED_FACE ( 'NONE', ( #54962 ), #40804, .F. ) ;
#16766=CARTESIAN_POINT ( 'NONE',  ( 3.168353074312903583, -2.372112023236606415, 0.8509228423427537269 ) ) ;
#16768=CARTESIAN_POINT ( 'NONE',  ( 3.086017585447000222, -79.19524289474686896, -11.86910201801999953 ) ) ;
#16770=CARTESIAN_POINT ( 'NONE',  ( 8.227509542961000122, -53.97460508840000415, 9.516261809240999625 ) ) ;
#16773=CARTESIAN_POINT ( 'NONE',  ( -12.70457850620681306, -16.82128713317816349, -0.5106122238182330131 ) ) ;
#16777=CARTESIAN_POINT ( 'NONE',  ( -10.77133038182000035, -76.48821396288001040, -5.959359258312999508 ) ) ;
#16780=CARTESIAN_POINT ( 'NONE',  ( -12.54901566180999950, -16.99264670699999868, 0.4731578885120000244 ) ) ;
#16784=CARTESIAN_POINT ( 'NONE',  ( -8.180687091746206008, -60.10655143787243304, -7.353725627631181538 ) ) ;
#16790=CARTESIAN_POINT ( 'NONE',  ( 0.000000000000000000, -23.15000000000000213, -11.79999999999999893 ) ) ;
#16791=ADVANCED_FACE ( 'NONE', ( #28082 ), #37528, .T. ) ;
#16792=CARTESIAN_POINT ( 'NONE',  ( 1.568694246062999786, -3.720626814303999996, -2.828919489903999995 ) ) ;
#16794=DIRECTION ( 'NONE',  ( 2.582636882131000189E-11, 0.000000000000000000, -1.000000000000000000 ) ) ;
#16795=CARTESIAN_POINT ( 'NONE',  ( -8.734625278329845699, -75.80000000000001137, 8.108151766267953420 ) ) ;
#16799=ORIENTED_EDGE ( 'NONE', *, *, #1400, .T. ) ;
#16800=CARTESIAN_POINT ( 'NONE',  ( -10.42274798264000069, -21.75365779208000205, -7.691916945395000482 ) ) ;
#16805=CARTESIAN_POINT ( 'NONE',  ( 1.829431482522000163, -1.554291850769000227, 3.403309575315999869 ) ) ;
#16807=CARTESIAN_POINT ( 'NONE',  ( -8.909545442950999927, -57.79999999967000690, 7.919595949288999570 ) ) ;
#16809=ORIENTED_EDGE ( 'NONE', *, *, #42593, .F. ) ;
#16812=CIRCLE ( 'NONE', #29069, 1.749999999999999556 ) ;
#16813=ADVANCED_FACE ( 'NONE', ( #28374 ), #36369, .F. ) ;
#16814=CARTESIAN_POINT ( 'NONE',  ( 11.00000000000000000, -23.75000000000000000, -1.203259120426999909E-14 ) ) ;
#16815=CARTESIAN_POINT ( 'NONE',  ( -10.35845616728999907, -60.09778595451999905, -7.627487606627999739 ) ) ;
#16816=EDGE_CURVE ( 'NONE', #19, #1253, #13995, .T. ) ;
#16818=ORIENTED_EDGE ( 'NONE', *, *, #37737, .T. ) ;
#16821=CARTESIAN_POINT ( 'NONE',  ( 1.636761686205427058, -1.166666666666666963, -2.839805762151336399 ) ) ;
#16822=AXIS2_PLACEMENT_3D ( 'NONE', #29250, #20697, #56426 ) ;
#16823=CARTESIAN_POINT ( 'NONE',  ( -12.53241208775999915, -59.56462890159999546, 1.667936697358999965 ) ) ;
#16825=EDGE_CURVE ( 'NONE', #2252, #1677, #55546, .T. ) ;
#16827=ORIENTED_EDGE ( 'NONE', *, *, #7112, .F. ) ;
#16828=ORIENTED_EDGE ( 'NONE', *, *, #47775, .F. ) ;
#16835=CARTESIAN_POINT ( 'NONE',  ( 6.777770385731999525, -76.84221882925000102, -9.662258766526001352 ) ) ;
#16839=LINE ( 'NONE', #30678, #49220 ) ;
#16841=CYLINDRICAL_SURFACE ( 'NONE', #2588, 14.00000000000000000 ) ;
#16849=DIRECTION ( 'NONE',  ( 0.7026410690473252618, -0.1122098755728027641, -0.7026410690473252618 ) ) ;
#16850=CARTESIAN_POINT ( 'NONE',  ( -7.635226873550689852, -18.23391307131834438, 10.36745167322480121 ) ) ;
#16852=B_SPLINE_CURVE_WITH_KNOTS ( 'NONE', 3,
 ( #34881, #30165, #21886, #16897, #58204, #8906, #30456, #53785 ),
 .UNSPECIFIED., .F., .F.,
 ( 4, 2, 2, 4 ),
 ( 0.000000000000000000, 0.4999999999999944489, 0.7499999999999972244, 1.000000000000000000 ),
 .UNSPECIFIED. ) ;
#16853=CARTESIAN_POINT ( 'NONE',  ( -12.64502302238000020, -19.22870851082999977, -1.799490220168999954 ) ) ;
#16856=CARTESIAN_POINT ( 'NONE',  ( 10.24998526317999925, -20.24916621771999914, -7.705142895619999877 ) ) ;
#16859=FACE_OUTER_BOUND ( 'NONE', #3253, .T. ) ;
#16860=ORIENTED_EDGE ( 'NONE', *, *, #51357, .T. ) ;
#16863=CARTESIAN_POINT ( 'NONE',  ( -3.250000000000000000, -2.004344010466332815, -0.1774124477927127019 ) ) ;
#16865=LINE ( 'NONE', #11863, #15551 ) ;
#16868=CARTESIAN_POINT ( 'NONE',  ( -1.171009383518375246, -2.152040482700231294, 3.318974785780838044 ) ) ;
#16871=CARTESIAN_POINT ( 'NONE',  ( -10.42531124905999995, -23.26485148473999942, -7.624341765453999997 ) ) ;
#16872=CARTESIAN_POINT ( 'NONE',  ( -7.674627477105999240, -22.75077028084999853, 10.14950121126000049 ) ) ;
#16875=ORIENTED_EDGE ( 'NONE', *, *, #46865, .F. ) ;
#16876=CARTESIAN_POINT ( 'NONE',  ( -9.616251104324094356, -78.64978193832848774, 6.835663575338875475 ) ) ;
#16877=CARTESIAN_POINT ( 'NONE',  ( -2.598229267968284351, -2.153525790767399695, -1.995724898132848812 ) ) ;
#16879=CARTESIAN_POINT ( 'NONE',  ( 0.000000000000000000, -39.49523982883999906, 0.000000000000000000 ) ) ;
#16885=CARTESIAN_POINT ( 'NONE',  ( 1.064301949326286190, -78.56405572308268859, 11.70180493458724236 ) ) ;
#16886=DIRECTION ( 'NONE',  ( -0.4045626180512096881, -0.8201574093740189308, -0.4045626180512096881 ) ) ;
#16892=DIRECTION ( 'NONE',  ( 0.000000000000000000, 0.000000000000000000, 1.000000000000000000 ) ) ;
#16897=CARTESIAN_POINT ( 'NONE',  ( -1.618935784732014715, -60.72751168617232054, 12.52134385804453132 ) ) ;
#16898=CARTESIAN_POINT ( 'NONE',  ( 13.94827586207000003, -45.69638659094999866, 8.082388075971999052E-06 ) ) ;
#16899=EDGE_CURVE ( 'NONE', #9471, #15167, #14921, .T. ) ;
#16900=CARTESIAN_POINT ( 'NONE',  ( 9.396085398178598780, -76.10208333333331154, 7.220923959705271677 ) ) ;
#16903=DIRECTION ( 'NONE',  ( 0.000000000000000000, 0.000000000000000000, -1.000000000000000000 ) ) ;
#16904=AXIS2_PLACEMENT_3D ( 'NONE', #44986, #54434, #49420 ) ;
#16906=CARTESIAN_POINT ( 'NONE',  ( -3.417863094299999904, -78.44998361729999203, 11.50296535110000029 ) ) ;
#16910=VECTOR ( 'NONE', #2190, 1000.000000000000227 ) ;
#16915=ADVANCED_FACE ( 'NONE', ( #49972 ), #35680, .T. ) ;
#16917=VERTEX_POINT ( 'NONE', #18671 ) ;
#16921=CARTESIAN_POINT ( 'NONE',  ( -12.77649732931999971, -62.10828417218999675, 0.06479631635403998446 ) ) ;
#16923=CARTESIAN_POINT ( 'NONE',  ( 7.627487525415999947, -23.29778754190000001, 10.35845608625999859 ) ) ;
#16925=CARTESIAN_POINT ( 'NONE',  ( 1.750000000000000000, -18.75000000310999937, 12.50000000000000000 ) ) ;
#16930=CARTESIAN_POINT ( 'NONE',  ( -7.619712398427999744, -55.39595871828999663, 10.35409979025000027 ) ) ;
#16932=ADVANCED_FACE ( 'NONE', ( #45837 ), #15097, .F. ) ;
#16933=CARTESIAN_POINT ( 'NONE',  ( -9.317995624416001377, -16.86762134170999872, -8.588852714006002032 ) ) ;
#16934=CARTESIAN_POINT ( 'NONE',  ( 7.648026768036999989, -60.04999998387000204, 10.12290050219000115 ) ) ;
#16936=VECTOR ( 'NONE', #17507, 1000.000000000000227 ) ;
#16938=DIRECTION ( 'NONE',  ( 0.000000000000000000, -1.000000000000000000, 0.000000000000000000 ) ) ;
#16940=CARTESIAN_POINT ( 'NONE',  ( 3.477442601125609656, -3.499999999999999556, 0.5952757321258587142 ) ) ;
#16941=CARTESIAN_POINT ( 'NONE',  ( -3.045222912875851673, -0.7922096678350301069, -1.778097659094616700 ) ) ;
#16943=CARTESIAN_POINT ( 'NONE',  ( 10.07627163191000008, -18.75000000310999937, 7.601397897754999633 ) ) ;
#16944=CARTESIAN_POINT ( 'NONE',  ( -1.758095523371000057, -55.07708336086999878, 12.57362173513000059 ) ) ;
#16945=CARTESIAN_POINT ( 'NONE',  ( -12.71658889741999943, -23.31584477285000290, 1.931087888049999979 ) ) ;
#16946=CARTESIAN_POINT ( 'NONE',  ( 0.7364373216886999085, -2.859035817501999865, -3.734094651500999618 ) ) ;
#16948=AXIS2_PLACEMENT_3D ( 'NONE', #49118, #53844, #17829 ) ;
#16949=CARTESIAN_POINT ( 'NONE',  ( -12.61117324687999997, -55.58448536084999603, 1.798979683803999974 ) ) ;
#16950=CARTESIAN_POINT ( 'NONE',  ( 0.8445585116414999760, -61.51040443210000319, 12.43380736240999873 ) ) ;
#16951=CARTESIAN_POINT ( 'NONE',  ( 2.598917237794088564, -3.197916666666666519, -1.997276839918468605 ) ) ;
#16952=VECTOR ( 'NONE', #52625, 1000.000000000000000 ) ;
#16955=CARTESIAN_POINT ( 'NONE',  ( -12.02231848918561319, -76.94547861865662242, 1.134278802166899025 ) ) ;
#16956=CARTESIAN_POINT ( 'NONE',  ( 11.12264838851901771, -76.42369462702311012, -3.807881462539005391 ) ) ;
#16962=CARTESIAN_POINT ( 'NONE',  ( 3.124639411803366240, -3.375269249970192842, 1.018784870465328618 ) ) ;
#16964=CARTESIAN_POINT ( 'NONE',  ( -1.335477334469999862E-14, -72.70000000000000284, 0.000000000000000000 ) ) ;
#16968=DIRECTION ( 'NONE',  ( -0.7071067811865475727, 0.000000000000000000, 0.7071067811865475727 ) ) ;
#16970=PLANE ( 'NONE',  #56353 ) ;
#16971=ORIENTED_EDGE ( 'NONE', *, *, #16434, .T. ) ;
#16974=CARTESIAN_POINT ( 'NONE',  ( 1.575772165398017455, -24.46154542799817122, 12.70597445617727317 ) ) ;
#16977=CARTESIAN_POINT ( 'NONE',  ( 2.598917237794080570, -1.302083333333333703, 1.997276839918479485 ) ) ;
#16980=B_SPLINE_CURVE_WITH_KNOTS ( 'NONE', 3,
 ( #43391, #1810, #2949, #37798, #39533, #44255, #22099, #39240 ),
 .UNSPECIFIED., .F., .F.,
 ( 4, 2, 2, 4 ),
 ( 0.000000000000000000, 0.5000000000000000000, 0.7500000000000000000, 1.000000000000000000 ),
 .UNSPECIFIED. ) ;
#16983=EDGE_LOOP ( 'NONE', ( #54155, #52480, #631, #42989 ) ) ;
#16985=CARTESIAN_POINT ( 'NONE',  ( -3.941558004887999900, -78.60478991842998653, -11.71306536694000044 ) ) ;
#16986=ADVANCED_FACE ( 'NONE', ( #11844 ), #28964, .F. ) ;
#16989=DIRECTION ( 'NONE',  ( 0.7071067811865473507, 1.433669009702094715E-08, -0.7071067811865473507 ) ) ;
#16996=CARTESIAN_POINT ( 'NONE',  ( 17.50000000000000000, -57.79999999999999716, 0.000000000000000000 ) ) ;
#16997=CARTESIAN_POINT ( 'NONE',  ( 7.199854605362999926, -76.91759889844999520, -10.39073109867000078 ) ) ;
#16999=DIRECTION ( 'NONE',  ( 0.000000000000000000, -1.000000000000000000, 0.000000000000000000 ) ) ;
#17002=CARTESIAN_POINT ( 'NONE',  ( -1.635769836470996941, -3.018359365201534139, 2.808997201014398204 ) ) ;
#17006=CARTESIAN_POINT ( 'NONE',  ( 3.665025684363000025, -3.545621233726000021, -1.025097465345000236 ) ) ;
#17008=CARTESIAN_POINT ( 'NONE',  ( -7.618386461959000044, -60.02712559312999474, -10.53495196325000016 ) ) ;
#17012=CARTESIAN_POINT ( 'NONE',  ( -12.66001647286000065, -17.36746073369999621, -1.381678996660999914 ) ) ;
#17013=CARTESIAN_POINT ( 'NONE',  ( -1.250000000000000000, -23.25000000000000000, -12.00000000000000000 ) ) ;
#17016=CARTESIAN_POINT ( 'NONE',  ( 1.689459950949288913, -24.29188253905320849, -12.71013585610226926 ) ) ;
#17017=CARTESIAN_POINT ( 'NONE',  ( 11.73828326341999961, -75.71624058713000238, -4.332684199240000034 ) ) ;
#17019=CARTESIAN_POINT ( 'NONE',  ( 0.000000000000000000, -9.295797029142999435, 0.000000000000000000 ) ) ;
#17020=CARTESIAN_POINT ( 'NONE',  ( -14.00000000000000000, -45.91785611817000046, 0.000000000000000000 ) ) ;
#17021=CARTESIAN_POINT ( 'NONE',  ( -10.99999999999999822, -18.25000000000001066, -0.1607611550118174248 ) ) ;
#17027=VERTEX_POINT ( 'NONE', #33094 ) ;
#17030=AXIS2_PLACEMENT_3D ( 'NONE', #3601, #8028, #21605 ) ;
#17032=VERTEX_POINT ( 'NONE', #2983 ) ;
#17034=CARTESIAN_POINT ( 'NONE',  ( -9.723174507563001612, -61.27697503937000079, -7.958760295438001009 ) ) ;
#17036=ORIENTED_EDGE ( 'NONE', *, *, #19287, .T. ) ;
#17040=ORIENTED_EDGE ( 'NONE', *, *, #39759, .F. ) ;
#17043=VERTEX_POINT ( 'NONE', #39273 ) ;
#17044=CARTESIAN_POINT ( 'NONE',  ( 10.98675469975087182, -18.58582062461607620, 0.5398555193318163026 ) ) ;
#17048=CARTESIAN_POINT ( 'NONE',  ( 1.026866341085000007E-14, -0.1000000000000002554, 0.000000000000000000 ) ) ;
#17049=EDGE_CURVE ( 'NONE', #34794, #45142, #7999, .T. ) ;
#17051=CARTESIAN_POINT ( 'NONE',  ( 8.596775676211999340, -53.66467110130999885, 9.310147894663000301 ) ) ;
#17052=CARTESIAN_POINT ( 'NONE',  ( 0.5705388283922003811, -18.65989902471944006, 10.98520465578114269 ) ) ;
#17054=DIRECTION ( 'NONE',  ( 1.000000000000000000, 0.000000000000000000, 0.000000000000000000 ) ) ;
#17058=CIRCLE ( 'NONE', #47270, 0.6000000000000008660 ) ;
#17061=CARTESIAN_POINT ( 'NONE',  ( -12.50412785605871946, -24.51985834634420414, 1.235051469882017861 ) ) ;
#17062=DIRECTION ( 'NONE',  ( 0.7071067811865474617, 0.000000000000000000, -0.7071067811865474617 ) ) ;
#17064=CARTESIAN_POINT ( 'NONE',  ( -7.995796640820073797, -60.48684619742725488, -7.555116226631964693 ) ) ;
#17065=CARTESIAN_POINT ( 'NONE',  ( -0.7820311386674927423, -78.43009031498998240, 12.04485182656622833 ) ) ;
#17069=CYLINDRICAL_SURFACE ( 'NONE', #9713, 14.00000000000000000 ) ;
#17070=CARTESIAN_POINT ( 'NONE',  ( -3.530714078838999903, -1.879486066823000234, 0.1002381994080999983 ) ) ;
#17073=CARTESIAN_POINT ( 'NONE',  ( 10.42531124908000173, -60.06485148440999922, 7.624341765471999821 ) ) ;
#17074=CARTESIAN_POINT ( 'NONE',  ( -11.47922858557694781, -76.18255052542706096, 2.508348395795582331 ) ) ;
#17079=EDGE_CURVE ( 'NONE', #10368, #21583, #34749, .T. ) ;
#17080=DIRECTION ( 'NONE',  ( 0.000000000000000000, 1.000000000000000000, 0.000000000000000000 ) ) ;
#17083=CARTESIAN_POINT ( 'NONE',  ( 9.396085398178630754, -76.99791666666666856, -7.220923959705230821 ) ) ;
#17084=CARTESIAN_POINT ( 'NONE',  ( -12.80090744918999945, -56.03767312542999690, -1.980532734072999901 ) ) ;
#17085=LINE ( 'NONE', #25937, #1577 ) ;
#17087=CARTESIAN_POINT ( 'NONE',  ( 12.43569926716000040, -24.88202093001000037, -0.4277578398254000547 ) ) ;
#17088=DIRECTION ( 'NONE',  ( 0.7071067811865475727, 0.000000000000000000, -0.7071067811865475727 ) ) ;
#17095=ORIENTED_EDGE ( 'NONE', *, *, #52260, .T. ) ;
#17099=CARTESIAN_POINT ( 'NONE',  ( 3.250000000000000444, -1.239583333333333481, -0.4254240051736113415 ) ) ;
#17102=CARTESIAN_POINT ( 'NONE',  ( -7.646788101807000082, -55.42771363232999704, -10.00831428589000005 ) ) ;
#17104=ORIENTED_EDGE ( 'NONE', *, *, #35004, .F. ) ;
#17105=ORIENTED_EDGE ( 'NONE', *, *, #14435, .F. ) ;
#17111=ORIENTED_EDGE ( 'NONE', *, *, #23707, .F. ) ;
#17114=CARTESIAN_POINT ( 'NONE',  ( -1.980611416588874629, -55.27402268162218490, 12.74335092660349567 ) ) ;
#17115=CARTESIAN_POINT ( 'NONE',  ( -12.75337166745000061, -77.17524667502999591, -1.077318095482000082 ) ) ;
#17117=CARTESIAN_POINT ( 'NONE',  ( -12.10214643675714008, -78.46315847178392744, -1.986460023565977062 ) ) ;
#17130=CARTESIAN_POINT ( 'NONE',  ( 2.798597658857805648, -3.047393581727702916, -2.136609592447876071 ) ) ;
#17131=EDGE_CURVE ( 'NONE', #1567, #38582, #4216, .T. ) ;
#17132=CARTESIAN_POINT ( 'NONE',  ( 12.75761570867000039, -22.77819125662999866, 1.931043762602999925 ) ) ;
#17133=CARTESIAN_POINT ( 'NONE',  ( 2.425729133266999670E-14, -6.000000000000000000, 0.000000000000000000 ) ) ;
#17134=DIRECTION ( 'NONE',  ( -0.7071067811814920612, -1.249159897326986052E-07, 0.7071067811915919821 ) ) ;
#17137=CARTESIAN_POINT ( 'NONE',  ( 10.18491080493000212, -18.69283319134000010, -7.640030264154999529 ) ) ;
#17140=VERTEX_POINT ( 'NONE', #17799 ) ;
#17150=CARTESIAN_POINT ( 'NONE',  ( -1.632307027713000069, -55.13072810409999391, -12.46200249210000166 ) ) ;
#17155=CARTESIAN_POINT ( 'NONE',  ( 0.8513654298648299923, -2.247209519113824161, -3.168457469390551395 ) ) ;
#17156=CARTESIAN_POINT ( 'NONE',  ( 11.89728672164147660, -78.94942626805544705, 0.01537117205770647047 ) ) ;
#17162=FACE_OUTER_BOUND ( 'NONE', #26529, .T. ) ;
#17163=DIRECTION ( 'NONE',  ( -1.000000000000000000, 0.000000000000000000, 0.000000000000000000 ) ) ;
#17164=ORIENTED_EDGE ( 'NONE', *, *, #16117, .F. ) ;
#17167=FACE_OUTER_BOUND ( 'NONE', #14693, .T. ) ;
#17174=VERTEX_POINT ( 'NONE', #23963 ) ;
#17175=CARTESIAN_POINT ( 'NONE',  ( 9.621742412375313691, -17.37938300089657417, -8.060146969350251211 ) ) ;
#17177=PLANE ( 'NONE',  #57261 ) ;
#17178=VERTEX_POINT ( 'NONE', #36959 ) ;
#17181=ORIENTED_EDGE ( 'NONE', *, *, #405, .T. ) ;
#17183=ORIENTED_EDGE ( 'NONE', *, *, #15692, .T. ) ;
#17191=ORIENTED_EDGE ( 'NONE', *, *, #51109, .T. ) ;
#17193=DIRECTION ( 'NONE',  ( -1.000000000000000000, 0.000000000000000000, 0.000000000000000000 ) ) ;
#17194=DIRECTION ( 'NONE',  ( 0.7071067811865475727, 0.000000000000000000, 0.7071067811865475727 ) ) ;
#17196=CARTESIAN_POINT ( 'NONE',  ( 7.655555357453000198, -19.22204592323999961, 10.38646360831000059 ) ) ;
#17199=LINE ( 'NONE', #21631, #8197 ) ;
#17202=CARTESIAN_POINT ( 'NONE',  ( 12.65987793663000005, -17.06302453494999583, -0.9847129294438998759 ) ) ;
#17203=CARTESIAN_POINT ( 'NONE',  ( -10.47513974133999959, -23.80361494181999760, -7.624776006159999397 ) ) ;
#17204=CARTESIAN_POINT ( 'NONE',  ( -11.44035017613066074, -76.68158408336353205, 2.681016756718579419 ) ) ;
#17209=CARTESIAN_POINT ( 'NONE',  ( -8.485548443539000729, -17.11931586736000455, -9.101490738460999097 ) ) ;
#17210=CARTESIAN_POINT ( 'NONE',  ( 7.653559626076999578, -55.50151115525000023, 10.01235002620999914 ) ) ;
#17213=CARTESIAN_POINT ( 'NONE',  ( 10.59551070214999946, -57.04351820043999766, -7.678690995233999672 ) ) ;
#17220=ADVANCED_FACE ( 'NONE', ( #36671 ), #22439, .F. ) ;
#17221=CARTESIAN_POINT ( 'NONE',  ( -1.669849926076999891, -55.42771399551000400, 12.48404299551000030 ) ) ;
#17222=CARTESIAN_POINT ( 'NONE',  ( -12.58335110166999904, -20.25111654322000021, 1.667961430005999945 ) ) ;
#17223=CARTESIAN_POINT ( 'NONE',  ( 2.997795270929999756, -2.833281426754000076, -2.074863749804000346 ) ) ;
#17226=FACE_OUTER_BOUND ( 'NONE', #5934, .T. ) ;
#17227=CARTESIAN_POINT ( 'NONE',  ( 0.5045596072229000528, -61.93528913004999481, 12.66210649714999903 ) ) ;
#17228=CARTESIAN_POINT ( 'NONE',  ( -0.4254240051736147277, -3.114583333333332593, -3.250000000000000888 ) ) ;
#17231=EDGE_CURVE ( 'NONE', #33530, #40010, #21385, .T. ) ;
#17232=CARTESIAN_POINT ( 'NONE',  ( -3.838255874262739731, -77.05221981673027187, -11.44667041316091272 ) ) ;
#17240=CARTESIAN_POINT ( 'NONE',  ( -12.79895559718999998, -60.60469146232000526, 2.015913954445999856 ) ) ;
#17242=CARTESIAN_POINT ( 'NONE',  ( -12.50000000000000000, -24.68359816828999698, -1.003641515615000035 ) ) ;
#17243=CARTESIAN_POINT ( 'NONE',  ( -7.764220096252848258, -17.74399029336390754, -10.21028322255594389 ) ) ;
#17244=AXIS2_PLACEMENT_3D ( 'NONE', #57026, #12155, #39302 ) ;
#17245=B_SPLINE_CURVE_WITH_KNOTS ( 'NONE', 3,
 ( #30812, #27554, #18432, #13985, #44705, #36134, #26385, #13394, #5141, #22849 ),
 .UNSPECIFIED., .F., .F.,
 ( 4, 2, 2, 2, 4 ),
 ( 0.000000000000000000, 0.2500000000000000555, 0.5000000000000001110, 0.7500000000000002220, 1.000000000000000000 ),
 .UNSPECIFIED. ) ;
#17250=VERTEX_POINT ( 'NONE', #15696 ) ;
#17251=CARTESIAN_POINT ( 'NONE',  ( -1.782734487917835953, -24.12245368560020253, 12.71547286926173825 ) ) ;
#17253=CARTESIAN_POINT ( 'NONE',  ( 0.000000000000000000, -2.660000000000000142, 0.000000000000000000 ) ) ;
#17263=CARTESIAN_POINT ( 'NONE',  ( 3.109857617603999813, -79.15086356186999694, -11.96079293226000040 ) ) ;
#17264=VERTEX_POINT ( 'NONE', #24555 ) ;
#17265=ORIENTED_EDGE ( 'NONE', *, *, #7349, .F. ) ;
#17270=DIRECTION ( 'NONE',  ( -0.7071067811865475727, 0.000000000000000000, 0.7071067811865475727 ) ) ;
#17273=CARTESIAN_POINT ( 'NONE',  ( -10.72428337452000058, -76.95682288379001079, 7.546888592172999566 ) ) ;
#17274=CARTESIAN_POINT ( 'NONE',  ( 11.48986902082000050, -77.02860818038000446, 5.271442771914999881 ) ) ;
#17277=DIRECTION ( 'NONE',  ( 0.000000000000000000, -1.000000000000000000, 0.000000000000000000 ) ) ;
#17279=DIRECTION ( 'NONE',  ( -0.7071067811865475727, 0.000000000000000000, 0.7071067811865475727 ) ) ;
#17280=CARTESIAN_POINT ( 'NONE',  ( -0.007828081787127551261, -2.975669492385137449, 3.249705167704726172 ) ) ;
#17282=VECTOR ( 'NONE', #56600, 1000.000000000000000 ) ;
#17286=CARTESIAN_POINT ( 'NONE',  ( 3.594201416108000036, -3.059342895222999736, 1.252117639952999850 ) ) ;
#17288=TOROIDAL_SURFACE ( 'NONE', #3968, 13.50000000000000000, 0.5000000000000000000 ) ;
#17289=ORIENTED_EDGE ( 'NONE', *, *, #43887, .F. ) ;
#17292=DIRECTION ( 'NONE',  ( 1.000000000000000000, 6.386283326366000088E-09, -1.411431172417000032E-10 ) ) ;
#17295=CARTESIAN_POINT ( 'NONE',  ( -12.59651451717999926, -18.60944962361000066, -1.801708894189000043 ) ) ;
#17296=CARTESIAN_POINT ( 'NONE',  ( -9.287618194362000423, -77.61375265978000471, -9.114789584104999065 ) ) ;
#17297=BREP_WITH_VOIDS ( 'NONE', #3218, ( #32916 ) );
#17298=DIRECTION ( 'NONE',  ( -0.9999548435846228323, 0.000000000000000000, -0.009503199022040118363 ) ) ;
#17299=CARTESIAN_POINT ( 'NONE',  ( 10.11462645681450034, -18.61287635839325461, 7.639895286233333138 ) ) ;
#17303=ADVANCED_FACE ( 'NONE', ( #25705 ), #1759, .F. ) ;
#17305=CARTESIAN_POINT ( 'NONE',  ( 7.627487525417000036, -18.70221245812999911, -10.35845608625999859 ) ) ;
#17310=VERTEX_POINT ( 'NONE', #43433 ) ;
#17314=ORIENTED_EDGE ( 'NONE', *, *, #48689, .F. ) ;
#17315=ORIENTED_EDGE ( 'NONE', *, *, #29008, .F. ) ;
#17317=VECTOR ( 'NONE', #18567, 1000.000000000000227 ) ;
#17318=LINE ( 'NONE', #56907, #37822 ) ;
#17325=CARTESIAN_POINT ( 'NONE',  ( 3.077458782618233357, -78.05205802293652084, 11.44329248034590485 ) ) ;
#17329=ORIENTED_EDGE ( 'NONE', *, *, #39977, .T. ) ;
#17332=EDGE_CURVE ( 'NONE', #48463, #37820, #54549, .T. ) ;
#17333=CARTESIAN_POINT ( 'NONE',  ( 9.422860735104000796, -53.54048607621999878, 8.643926020445999114 ) ) ;
#17334=CARTESIAN_POINT ( 'NONE',  ( -7.678690995240000206, -20.24351820077000141, -10.59551070215999857 ) ) ;
#17339=CARTESIAN_POINT ( 'NONE',  ( -10.14948852604999985, -19.24899164588000389, -7.674614791898999755 ) ) ;
#17348=CARTESIAN_POINT ( 'NONE',  ( -2.019183793707000074, -23.78720277242999970, 12.79944116704999857 ) ) ;
#17349=DIRECTION ( 'NONE',  ( 0.000000000000000000, -1.000000000000000000, 1.543800620547000024E-14 ) ) ;
#17350=EDGE_CURVE ( 'NONE', #22602, #20949, #35432, .T. ) ;
#17354=ADVANCED_FACE ( 'NONE', ( #47016 ), #20992, .F. ) ;
#17355=CARTESIAN_POINT ( 'NONE',  ( 12.46083365857999858, -60.48341615446999953, -1.628972628240000109 ) ) ;
#17359=VECTOR ( 'NONE', #55216, 1000.000000000000000 ) ;
#17362=DIRECTION ( 'NONE',  ( 0.07798810297687770732, 0.04890180918248850789, 0.9957542211071702676 ) ) ;
#17363=DIRECTION ( 'NONE',  ( -1.000000000000000000, 0.000000000000000000, 0.000000000000000000 ) ) ;
#17367=ORIENTED_EDGE ( 'NONE', *, *, #25909, .F. ) ;
#17368=CARTESIAN_POINT ( 'NONE',  ( -10.59548767699999949, -20.24263462181000151, -7.678667886068000215 ) ) ;
#17371=EDGE_CURVE ( 'NONE', #35060, #56888, #36191, .T. ) ;
#17373=CARTESIAN_POINT ( 'NONE',  ( -10.00844230538000090, -60.16891112520000462, 7.647097279411999793 ) ) ;
#17374=CARTESIAN_POINT ( 'NONE',  ( -3.536550279337999925, -1.729884069545000180, -0.5317485034389000109 ) ) ;
#17376=CARTESIAN_POINT ( 'NONE',  ( 12.72554383680000001, -23.20159311629000243, -1.930239506950999884 ) ) ;
#17377=CARTESIAN_POINT ( 'NONE',  ( -1.667936697358999965, -56.03537109808000594, 12.53241208775000004 ) ) ;
#17378=VERTEX_POINT ( 'NONE', #33976 ) ;
#17379=CARTESIAN_POINT ( 'NONE',  ( -12.71536175399154800, -54.67444297150642285, 1.781227265964418827 ) ) ;
#17380=CARTESIAN_POINT ( 'NONE',  ( 9.546819346421999697, -24.68527546640000025, -8.130850183241999929 ) ) ;
#17382=CARTESIAN_POINT ( 'NONE',  ( -10.04116292117000064, -59.56462890159999546, -7.682344222584999827 ) ) ;
#17384=AXIS2_PLACEMENT_3D ( 'NONE', #31872, #54338, #13877 ) ;
#17385=ORIENTED_EDGE ( 'NONE', *, *, #2465, .T. ) ;
#17386=CARTESIAN_POINT ( 'NONE',  ( 7.601397897754999633, -18.75000000000000000, -9.369164850722000892 ) ) ;
#17387=CARTESIAN_POINT ( 'NONE',  ( -10.26031322985315697, -77.74064956233091550, -5.914412738676674053 ) ) ;
#17389=EDGE_LOOP ( 'NONE', ( #1392, #20108, #4861, #47425, #35985 ) ) ;
#17390=CARTESIAN_POINT ( 'NONE',  ( -12.75763395697999947, -59.57795407677000554, 1.931043742978000077 ) ) ;
#17391=CARTESIAN_POINT ( 'NONE',  ( -9.317995624384998621, -53.66762134137999851, -8.588852713974999276 ) ) ;
#17394=ORIENTED_EDGE ( 'NONE', *, *, #30558, .F. ) ;
#17399=CARTESIAN_POINT ( 'NONE',  ( 12.54238271617994371, -18.47146427654176293, 1.749799002660173519 ) ) ;
#17400=ADVANCED_FACE ( 'NONE', ( #51728 ), #34265, .T. ) ;
#17403=CARTESIAN_POINT ( 'NONE',  ( 11.83733200052000178, -78.36477256742000463, 5.266624269285999915 ) ) ;
#17404=PRODUCT_DEFINITION_CONTEXT ( 'detailed design', #33019, 'design' ) ;
#17407=CARTESIAN_POINT ( 'NONE',  ( 12.99510751537000353, -26.30294702886003222, 6.911973076623003642 ) ) ;
#17411=CARTESIAN_POINT ( 'NONE',  ( 10.04568514501610998, -17.44913840260318949, 7.921286339712268365 ) ) ;
#17414=CARTESIAN_POINT ( 'NONE',  ( -11.91862232004000077, -76.03188042556000426, 3.079279237876999531 ) ) ;
#17416=CARTESIAN_POINT ( 'NONE',  ( 0.9591145717409618188, -2.996237724664126301, -3.388105781299149744 ) ) ;
#17417=CARTESIAN_POINT ( 'NONE',  ( 12.80900240957999969, -20.24634220924000161, 1.930989144707000005 ) ) ;
#17418=CARTESIAN_POINT ( 'NONE',  ( -12.87024489160000051, -19.21538333566000034, -2.062597265787999845 ) ) ;
#17422=CARTESIAN_POINT ( 'NONE',  ( 10.53101998747000145, -18.69360374348000065, -7.613962827178999859 ) ) ;
#17425=AXIS2_PLACEMENT_3D ( 'NONE', #30630, #34189, #43085 ) ;
#17426=ORIENTED_EDGE ( 'NONE', *, *, #36998, .F. ) ;
#17438=CARTESIAN_POINT ( 'NONE',  ( -1.466594960164999906, -54.71841800914999965, -12.44238958329999889 ) ) ;
#17443=CARTESIAN_POINT ( 'NONE',  ( 12.50000000000000000, -65.72928575305999743, 0.000000000000000000 ) ) ;
#17446=EDGE_CURVE ( 'NONE', #29475, #19884, #3624, .T. ) ;
#17450=CARTESIAN_POINT ( 'NONE',  ( 1.003693376009467508, -17.03776007890333943, 12.70247752664556273 ) ) ;
#17457=DIRECTION ( 'NONE',  ( 0.000000000000000000, 0.000000000000000000, -1.000000000000000000 ) ) ;
#17459=CARTESIAN_POINT ( 'NONE',  ( -12.50745077485999879, -53.80005551680000053, 2.011910316382000212E-09 ) ) ;
#17460=CARTESIAN_POINT ( 'NONE',  ( -11.00000000000000000, -23.74999999999999645, 0.1604995627986234297 ) ) ;
#17462=ORIENTED_EDGE ( 'NONE', *, *, #13710, .F. ) ;
#17463=ADVANCED_FACE ( 'NONE', ( #39574 ), #26859, .T. ) ;
#17464=DIRECTION ( 'NONE',  ( -1.000000000000000000, 0.000000000000000000, 0.000000000000000000 ) ) ;
#17467=CIRCLE ( 'NONE', #2403, 0.8000000000000000444 ) ;
#17468=FACE_OUTER_BOUND ( 'NONE', #5852, .T. ) ;
#17469=VERTEX_POINT ( 'NONE', #22143 ) ;
#17473=AXIS2_PLACEMENT_3D ( 'NONE', #47671, #38776, #7197 ) ;
#17477=CARTESIAN_POINT ( 'NONE',  ( 9.830801209626999437, -24.09088558010999748, 7.765011064334000679 ) ) ;
#17479=ADVANCED_FACE ( 'NONE', ( #16859 ), #53746, .F. ) ;
#17490=CARTESIAN_POINT ( 'NONE',  ( -9.990509419794001644, -76.27765497417000518, 8.015179320152999054 ) ) ;
#17492=CARTESIAN_POINT ( 'NONE',  ( 10.42531124903999995, -55.53514851492000304, -7.624341765436000173 ) ) ;
#17494=CARTESIAN_POINT ( 'NONE',  ( 12.83838672491000032, -18.79401612030999758, -2.062170725306000207 ) ) ;
#17495=CARTESIAN_POINT ( 'NONE',  ( -9.414507962619001802, -25.26263135926000203, -8.652357372777000677 ) ) ;
#17496=CARTESIAN_POINT ( 'NONE',  ( -11.67265798347707140, -76.69004288209750086, 1.396753407656934787 ) ) ;
#17497=ORIENTED_EDGE ( 'NONE', *, *, #50452, .T. ) ;
#17499=CARTESIAN_POINT ( 'NONE',  ( -7.633478597807999755, -55.59901960186999759, 10.36292351976000070 ) ) ;
#17502=CARTESIAN_POINT ( 'NONE',  ( -8.878349648294999952, -16.93036913510000119, -8.870329531829000302 ) ) ;
#17503=CARTESIAN_POINT ( 'NONE',  ( 7.653559502293999728, -60.09849137195000424, 10.01234990230000044 ) ) ;
#17504=CARTESIAN_POINT ( 'NONE',  ( -2.019183793707000074, -18.21279722757000030, -12.79944116704999857 ) ) ;
#17505=CARTESIAN_POINT ( 'NONE',  ( -0.3664097463224703644, -53.82809982435230012, 12.50575740040853390 ) ) ;
#17506=CARTESIAN_POINT ( 'NONE',  ( 10.55911395186000057, -56.01538333533000014, -7.642160924870000649 ) ) ;
#17507=DIRECTION ( 'NONE',  ( -0.7071067811865974218, 0.7071067811864975017, -8.595326187306963091E-09 ) ) ;
#17511=ORIENTED_EDGE ( 'NONE', *, *, #19753, .F. ) ;
#17512=CARTESIAN_POINT ( 'NONE',  ( 0.8521412958799197135, -1.455789518402647031, 3.164999420474257530 ) ) ;
#17513=CARTESIAN_POINT ( 'NONE',  ( -1.460729357743000056, -54.70908756765000192, 12.44211643236999976 ) ) ;
#17516=CARTESIAN_POINT ( 'NONE',  ( -3.122751374266999669, -1.580997856415000014, -1.547189057874000184 ) ) ;
#17519=FACE_BOUND ( 'NONE', #10130, .T. ) ;
#17520=EDGE_CURVE ( 'NONE', #8754, #50383, #51630, .T. ) ;
#17522=CARTESIAN_POINT ( 'NONE',  ( 0.9781264271447999148, -61.74031143843999558, 12.65967462882999861 ) ) ;
#17523=CARTESIAN_POINT ( 'NONE',  ( 12.61271781521000079, -18.80306329050999992, 1.798333084007999849 ) ) ;
#17526=FACE_OUTER_BOUND ( 'NONE', #528, .T. ) ;
#17527=VECTOR ( 'NONE', #42041, 1000.000000000000114 ) ;
#17532=DIRECTION ( 'NONE',  ( 1.000000000000000000, 0.000000000000000000, 0.000000000000000000 ) ) ;
#17534=CARTESIAN_POINT ( 'NONE',  ( -2.598917237794085455, -2.552083333333333481, -1.997276839918474600 ) ) ;
#17537=LINE ( 'NONE', #31978, #15318 ) ;
#17542=CARTESIAN_POINT ( 'NONE',  ( -12.50000000000000000, -55.55000000278000272, 1.750000000000000000 ) ) ;
#17546=ORIENTED_EDGE ( 'NONE', *, *, #35835, .F. ) ;
#17559=CARTESIAN_POINT ( 'NONE',  ( -10.70115325243999926, -78.54730848226999740, -6.181997344542000228 ) ) ;
#17562=VERTEX_POINT ( 'NONE', #7789 ) ;
#17564=DIRECTION ( 'NONE',  ( 0.000000000000000000, 0.000000000000000000, -1.000000000000000000 ) ) ;
#17569=LINE ( 'NONE', #34975, #15758 ) ;
#17570=EDGE_CURVE ( 'NONE', #54661, #25114, #27710, .T. ) ;
#17571=AXIS2_PLACEMENT_3D ( 'NONE', #52448, #2573, #25571 ) ;
#17573=CARTESIAN_POINT ( 'NONE',  ( -8.110204649352999340, -78.43694664278000062, 9.400142180594000862 ) ) ;
#17574=CARTESIAN_POINT ( 'NONE',  ( 5.354686402641000598, -76.58457105268000475, 11.45119097547000031 ) ) ;
#17575=ADVANCED_FACE ( 'NONE', ( #34921 ), #30870, .F. ) ;
#17577=AXIS2_PLACEMENT_3D ( 'NONE', #51009, #1709, #19703 ) ;
#17580=CARTESIAN_POINT ( 'NONE',  ( -10.01332852686999964, -55.51943464808999806, 7.654537165450999936 ) ) ;
#17581=CARTESIAN_POINT ( 'NONE',  ( -0.1382660771586305126, -2.978707574826329640, 3.247216946312587726 ) ) ;
#17583=CARTESIAN_POINT ( 'NONE',  ( -7.648026768019999366, -23.24999998419999869, -10.12290050217000115 ) ) ;
#17586=CARTESIAN_POINT ( 'NONE',  ( -3.370587613551000228, -1.760959338694000120, 0.9429417476038000068 ) ) ;
#17592=DIRECTION ( 'NONE',  ( 0.000000000000000000, 1.000000000000000000, 0.000000000000000000 ) ) ;
#17593=CARTESIAN_POINT ( 'NONE',  ( -9.692839446179998930, -78.46716024849999371, 7.074522137259999788 ) ) ;
#17595=CARTESIAN_POINT ( 'NONE',  ( 12.71798269385000069, -18.70221245812999911, -1.931086388578000079 ) ) ;
#17596=ORIENTED_EDGE ( 'NONE', *, *, #18189, .T. ) ;
#17597=CARTESIAN_POINT ( 'NONE',  ( -9.837773999814896086, -54.48535604133265764, 7.850041801394331387 ) ) ;
#17603=CARTESIAN_POINT ( 'NONE',  ( -3.858199361241999803, -0.8397668567873000089, -1.117275487237999965 ) ) ;
#17607=VECTOR ( 'NONE', #44834, 1000.000000000000000 ) ;
#17615=CYLINDRICAL_SURFACE ( 'NONE', #1996, 11.75000000000000000 ) ;
#17618=ORIENTED_EDGE ( 'NONE', *, *, #9007, .F. ) ;
#17620=AXIS2_PLACEMENT_3D ( 'NONE', #17925, #34742, #8185 ) ;
#17621=VERTEX_POINT ( 'NONE', #21074 ) ;
#17622=ORIENTED_EDGE ( 'NONE', *, *, #30060, .F. ) ;
#17623=CARTESIAN_POINT ( 'NONE',  ( -2.963063481827658219, -2.634561461520561032, -1.334362463457642534 ) ) ;
#17624=EDGE_CURVE ( 'NONE', #45467, #52988, #33363, .T. ) ;
#17626=CARTESIAN_POINT ( 'NONE',  ( -7.919595949288999570, -59.94999999969000015, -8.768124086712999699 ) ) ;
#17628=ORIENTED_EDGE ( 'NONE', *, *, #53424, .T. ) ;
#17631=FACE_BOUND ( 'NONE', #14346, .T. ) ;
#17632=CARTESIAN_POINT ( 'NONE',  ( -7.653559502275999016, -23.29849137228000444, -10.01234990228999955 ) ) ;
#17633=CARTESIAN_POINT ( 'NONE',  ( -3.783563790603477806, -77.29730020392733536, -11.14627141929872067 ) ) ;
#17634=DIRECTION ( 'NONE',  ( 1.000000000000000000, 0.000000000000000000, 0.000000000000000000 ) ) ;
#17635=EDGE_CURVE ( 'NONE', #11225, #39417, #50595, .T. ) ;
#17637=CYLINDRICAL_SURFACE ( 'NONE', #18082, 0.5000000000000006661 ) ;
#17639=CIRCLE ( 'NONE', #6318, 13.00000000000000000 ) ;
#17642=CARTESIAN_POINT ( 'NONE',  ( -12.50240681834000078, -24.68234730741999883, 1.005418943852999902 ) ) ;
#17643=LINE ( 'NONE', #4358, #56589 ) ;
#17644=CARTESIAN_POINT ( 'NONE',  ( 1.807051837523000026, -24.30078415243000123, 12.77977401834999860 ) ) ;
#17648=CARTESIAN_POINT ( 'NONE',  ( 2.939819053343999844, -1.106200577025999943, 2.890138559307000143 ) ) ;
#17649=LINE ( 'NONE', #26487, #57809 ) ;
#17650=AXIS2_PLACEMENT_3D ( 'NONE', #20101, #11533, #38091 ) ;
#17654=VECTOR ( 'NONE', #57906, 1000.000000000000000 ) ;
#17656=EDGE_CURVE ( 'NONE', #27335, #23838, #13907, .T. ) ;
#17659=DIRECTION ( 'NONE',  ( -0.7071067811865474617, 0.000000000000000000, 0.7071067811865474617 ) ) ;
#17661=DIRECTION ( 'NONE',  ( 1.000000000000000000, 0.000000000000000000, 0.000000000000000000 ) ) ;
#17665=CARTESIAN_POINT ( 'NONE',  ( -10.18491068059999805, -18.69283065396999888, -7.640030139758000161 ) ) ;
#17668=B_SPLINE_CURVE_WITH_KNOTS ( 'NONE', 3,
 ( #5536, #42734, #24721, #50731, #46014, #41559, #5829, #23836, #41852, #14975, #32973, #51018, #10568, #38866, #2581, #20583, #48045, #12580, #29993, #21440, #3724, #29708, #16442, #17016, #30286, #34998, #34132, #3439, #39451, #39157 ),
 .UNSPECIFIED., .F., .F.,
 ( 4, 2, 2, 2, 2, 2, 2, 2, 2, 2, 2, 2, 2, 2, 4 ),
 ( 0.000000000000000000, 0.1249999999999994171, 0.1874999999999991396, 0.2499999999999988898, 0.3124999999999986677, 0.3749999999999983347, 0.4999999999999971689, 0.5624999999999965583, 0.6249999999999960032, 0.6874999999999954481, 0.7499999999999950040, 0.8124999999999944489, 0.8437499999999948930, 0.8749999999999952260, 1.000000000000000000 ),
 .UNSPECIFIED. ) ;
#17672=CARTESIAN_POINT ( 'NONE',  ( -10.19022265129000004, -59.99634105610000034, 7.646946115762000673 ) ) ;
#17674=CARTESIAN_POINT ( 'NONE',  ( 3.525388664395999960, -0.7875064129436999405, -0.3052335303999000327 ) ) ;
#17675=CARTESIAN_POINT ( 'NONE',  ( 9.492565570809029296, -76.49917531041499785, -7.041922512536913814 ) ) ;
#17676=CARTESIAN_POINT ( 'NONE',  ( -1.799501877760999902, -55.51082434643999619, 12.60552522433000000 ) ) ;
#17677=ORIENTED_EDGE ( 'NONE', *, *, #3204, .T. ) ;
#17678=DIRECTION ( 'NONE',  ( 0.000000000000000000, 0.000000000000000000, 1.000000000000000000 ) ) ;
#17681=CARTESIAN_POINT ( 'NONE',  ( -10.38646360829999971, -59.57795407677000554, -7.655555357447999754 ) ) ;
#17684=ORIENTED_EDGE ( 'NONE', *, *, #43146, .T. ) ;
#17685=DIRECTION ( 'NONE',  ( 0.000000000000000000, 1.000000000000000000, 0.000000000000000000 ) ) ;
#17686=CARTESIAN_POINT ( 'NONE',  ( 11.75000000000000000, -77.95000000000000284, 2.316376715183999699E-14 ) ) ;
#17687=CARTESIAN_POINT ( 'NONE',  ( -1.667916687244999974, -23.29849137228000444, 12.49168433579000137 ) ) ;
#17690=CARTESIAN_POINT ( 'NONE',  ( -12.83044039277999993, -60.10639625617000092, 2.062670899148999926 ) ) ;
#17691=CARTESIAN_POINT ( 'NONE',  ( -8.260145278118999457, -53.85964900942000355, -9.643338478971999805 ) ) ;
#17695=ORIENTED_EDGE ( 'NONE', *, *, #46678, .F. ) ;
#17704=CARTESIAN_POINT ( 'NONE',  ( 10.36292447790000004, -18.79904187578000219, 7.633480004415999609 ) ) ;
#17705=DIRECTION ( 'NONE',  ( -0.7071067811865474617, 0.000000000000000000, -0.7071067811865474617 ) ) ;
#17707=VECTOR ( 'NONE', #43279, 1000.000000000000000 ) ;
#17708=PLANE ( 'NONE',  #3460 ) ;
#17709=CARTESIAN_POINT ( 'NONE',  ( -3.372301964606999825, -76.89007569364000005, 12.67255275672000003 ) ) ;
#17711=CARTESIAN_POINT ( 'NONE',  ( 13.63885489310999510, -22.78578169018999944, 7.254376133916000668 ) ) ;
#17715=EDGE_CURVE ( 'NONE', #36961, #21517, #20006, .T. ) ;
#17716=CARTESIAN_POINT ( 'NONE',  ( 8.532671861026141613, -16.87201063390074651, 9.433519686760231338 ) ) ;
#17719=CARTESIAN_POINT ( 'NONE',  ( 12.21199139566000014, -76.31204719422001403, 1.550091862394999964 ) ) ;
#17721=CARTESIAN_POINT ( 'NONE',  ( -3.137247185147045148, -3.311698843223778166, 1.599361815492593264 ) ) ;
#17722=CARTESIAN_POINT ( 'NONE',  ( 12.60413652831999975, -23.30716934606000024, 1.799502287743000029 ) ) ;
#17726=CARTESIAN_POINT ( 'NONE',  ( 7.284200816657673272, -76.87346977519162294, 9.621121000730060047 ) ) ;
#17728=CARTESIAN_POINT ( 'NONE',  ( -13.02716421901072685, -75.95264176747838292, -0.01989893052437335594 ) ) ;
#17729=B_SPLINE_SURFACE_WITH_KNOTS ( 'NONE', 3, 3, ( 
 ( #48839, #40854, #31681, #4846 ),
 ( #31387, #156, #53855, #36127 ),
 ( #3951, #26667, #22842, #50017 ),
 ( #17240, #18132, #17838, #49428 ),
 ( #49727, #9270, #39676, #31090 ),
 ( #12807, #54143, #26964, #446 ),
 ( #30806, #36415, #26379, #54443 ),
 ( #18425, #44699, #13979, #57979 ),
 ( #8678, #44995, #4550, #13684 ),
 ( #31975, #27548, #45591, #5136 ),
 ( #23135, #46469, #10150, #19295 ) ),
 .UNSPECIFIED., .F., .F., .F.,
 ( 4, 1, 1, 1, 1, 1, 1, 1, 4 ),
 ( 4, 4 ),
 ( -0.02001474922158999817, 0.000000000000000000, 0.1666666666667000196, 0.3333333333333000081, 0.5000000000000000000, 0.6666666666667000474, 0.8333333333333000637, 1.000000000000000000, 1.020283381528000133 ),
 ( -0.3582002740342999925, 1.358862457857999972 ),
 .UNSPECIFIED. ) ;
#17731=VERTEX_POINT ( 'NONE', #13955 ) ;
#17735=LINE ( 'NONE', #13583, #13532 ) ;
#17740=CARTESIAN_POINT ( 'NONE',  ( -2.065394024360999836, -55.37838567321000482, -12.82193048525000023 ) ) ;
#17749=CARTESIAN_POINT ( 'NONE',  ( -0.2494208068357447461, -17.00711039237069144, -12.50614183112945277 ) ) ;
#17751=CARTESIAN_POINT ( 'NONE',  ( 0.5204347304194590906, -78.56791883825732725, 11.73731741140708529 ) ) ;
#17753=ORIENTED_EDGE ( 'NONE', *, *, #49358, .F. ) ;
#17754=ADVANCED_FACE ( 'NONE', ( #53829 ), #15679, .F. ) ;
#17759=LINE ( 'NONE', #2805, #9945 ) ;
#17761=CARTESIAN_POINT ( 'NONE',  ( -12.50483450104916194, -53.93545458963708938, 0.6958188033158416719 ) ) ;
#17762=CARTESIAN_POINT ( 'NONE',  ( -9.723199427802001082, -54.32306055813000256, 7.958735710007999842 ) ) ;
#17763=PRODUCT_DEFINITION_SHAPE ( 'NONE', 'NONE',  #45957 ) ;
#17766=DIRECTION ( 'NONE',  ( 0.7071067811865475727, 0.000000000000000000, 0.7071067811865475727 ) ) ;
#17768=CARTESIAN_POINT ( 'NONE',  ( -12.00000000000000000, -55.54999999966999980, 1.250000000000000000 ) ) ;
#17769=ORIENTED_EDGE ( 'NONE', *, *, #49858, .T. ) ;
#17772=ADVANCED_FACE ( 'NONE', ( #48816 ), #9248, .F. ) ;
#17773=ORIENTED_EDGE ( 'NONE', *, *, #47567, .T. ) ;
#17779=CARTESIAN_POINT ( 'NONE',  ( 7.356278612544847384, -55.49583131490126675, -8.178338515874344239 ) ) ;
#17786=ORIENTED_EDGE ( 'NONE', *, *, #55271, .F. ) ;
#17792=CARTESIAN_POINT ( 'NONE',  ( -12.65069897394999998, -75.74449986905000287, -0.01932388167793000142 ) ) ;
#17795=CARTESIAN_POINT ( 'NONE',  ( 7.921329716846313040, -54.24906234234291702, -10.04564005580055053 ) ) ;
#17796=DIRECTION ( 'NONE',  ( -0.4045626182446106500, -0.8201574091832195545, -0.4045626182446106500 ) ) ;
#17797=CARTESIAN_POINT ( 'NONE',  ( 12.44209697062000153, -17.91557297456000342, -1.464771213333999844 ) ) ;
#17798=CARTESIAN_POINT ( 'NONE',  ( -10.36289662401999934, -23.20106470441999846, -7.633500902327000404 ) ) ;
#17799=CARTESIAN_POINT ( 'NONE',  ( 10.07627163191000008, -23.24999999688999708, -7.601397897754999633 ) ) ;
#17805=CARTESIAN_POINT ( 'NONE',  ( 1.997276839918466829, -3.322916666666666075, 2.598917237794090784 ) ) ;
#17807=CARTESIAN_POINT ( 'NONE',  ( -1.761265949708000100, -18.29141781213999707, -12.57448205042999945 ) ) ;
#17808=EDGE_CURVE ( 'NONE', #51923, #4102, #53236, .T. ) ;
#17809=CARTESIAN_POINT ( 'NONE',  ( 9.723174507645000020, -61.27697503925999456, 7.958760295356000825 ) ) ;
#17810=CARTESIAN_POINT ( 'NONE',  ( 10.24998526317999925, -57.04916621739000249, -7.705142895613999343 ) ) ;
#17814=CARTESIAN_POINT ( 'NONE',  ( -3.497194500561336294, -0.7605524168492561188, -0.4641820427686449424 ) ) ;
#17817=CARTESIAN_POINT ( 'NONE',  ( 0.4450739772405999939, -53.92186785164999918, 12.43586747591000119 ) ) ;
#17818=DIRECTION ( 'NONE',  ( -0.7071067811865474617, 0.000000000000000000, 0.7071067811865474617 ) ) ;
#17819=CARTESIAN_POINT ( 'NONE',  ( -3.702886505537000161, -1.801356099613000250, 0.2188527041987999855 ) ) ;
#17822=DIRECTION ( 'NONE',  ( 0.000000000000000000, 0.000000000000000000, -1.000000000000000000 ) ) ;
#17824=CARTESIAN_POINT ( 'NONE',  ( -0.8537148449456000154, -61.50498145875999256, 12.43377424877000159 ) ) ;
#17825=CARTESIAN_POINT ( 'NONE',  ( 12.46083735080000032, -18.31664398787999559, 1.628985986889000204 ) ) ;
#17829=DIRECTION ( 'NONE',  ( -0.7071067811865475727, 0.000000000000000000, 0.7071067811865475727 ) ) ;
#17830=EDGE_CURVE ( 'NONE', #13664, #51037, #55858, .T. ) ;
#17831=CARTESIAN_POINT ( 'NONE',  ( 0.1323022290353233765, -77.07890511624708552, -12.02134639614113709 ) ) ;
#17832=CARTESIAN_POINT ( 'NONE',  ( 4.579136177892999982, -78.91051207264999334, -11.61209283926000069 ) ) ;
#17838=CARTESIAN_POINT ( 'NONE',  ( -12.57354097144999905, -60.52384125708999818, 1.757953070309000054 ) ) ;
#17840=CARTESIAN_POINT ( 'NONE',  ( 12.50000000000000000, -24.68359816828999698, 1.003641515614000168 ) ) ;
#17842=AXIS2_PLACEMENT_3D ( 'NONE', #8408, #26406, #49156 ) ;
#17843=CARTESIAN_POINT ( 'NONE',  ( 12.54435570279975387, -55.27582218184407026, -1.733918077762380827 ) ) ;
#17852=DIRECTION ( 'NONE',  ( -1.000000000000000000, 0.000000000000000000, 0.000000000000000000 ) ) ;
#17862=CARTESIAN_POINT ( 'NONE',  ( -12.35615978905999945, -79.00715997148999747, -0.2389464526812000167 ) ) ;
#17865=CARTESIAN_POINT ( 'NONE',  ( 1.250000000000000000, -60.24678171298000251, -12.50000000000000000 ) ) ;
#17867=EDGE_CURVE ( 'NONE', #43853, #40579, #56240, .T. ) ;
#17873=CARTESIAN_POINT ( 'NONE',  ( -1.169957374810000061, -76.94917510722000031, -12.74520906849999946 ) ) ;
#17876=DIRECTION ( 'NONE',  ( 0.000000000000000000, 1.000000000000000000, -6.735242868878000753E-11 ) ) ;
#17878=CIRCLE ( 'NONE', #4646, 13.86363636363999952 ) ;
#17880=CARTESIAN_POINT ( 'NONE',  ( -5.489853033850980779, -76.78607156998435812, -10.46842530689402828 ) ) ;
#17886=CARTESIAN_POINT ( 'NONE',  ( 1.432628882339999965, -2.438376846448000013, -3.526139092948999743 ) ) ;
#17888=EDGE_LOOP ( 'NONE', ( #55558, #16121, #24816, #51390 ) ) ;
#17889=DIRECTION ( 'NONE',  ( -1.000000000000000000, 0.000000000000000000, 0.000000000000000000 ) ) ;
#17890=EDGE_CURVE ( 'NONE', #17264, #57279, #56357, .T. ) ;
#17893=CARTESIAN_POINT ( 'NONE',  ( -12.46083735080000032, -18.31664398787999559, -1.628985986889000204 ) ) ;
#17894=CARTESIAN_POINT ( 'NONE',  ( -1.338697082642999803, -78.13413240273000326, -12.94399764267999942 ) ) ;
#17897=CARTESIAN_POINT ( 'NONE',  ( -12.03549681466000010, -76.47233804731999385, 3.421427826494999991 ) ) ;
#17898=VERTEX_POINT ( 'NONE', #7127 ) ;
#17900=CARTESIAN_POINT ( 'NONE',  ( 7.919595949288999570, -59.94999999040999938, -9.050966798898000931 ) ) ;
#17902=CARTESIAN_POINT ( 'NONE',  ( -1.930989179114000143, -20.24546192895000019, -12.80896991329000123 ) ) ;
#17905=CARTESIAN_POINT ( 'NONE',  ( -0.7824435345810000220, -1.742598507946000019, 3.939770163431000061 ) ) ;
#17910=DIRECTION ( 'NONE',  ( 0.000000000000000000, 0.000000000000000000, 1.000000000000000000 ) ) ;
#17912=ORIENTED_EDGE ( 'NONE', *, *, #19838, .F. ) ;
#17913=PLANE ( 'NONE',  #962 ) ;
#17916=DIRECTION ( 'NONE',  ( 0.4045626180513098857, -0.8201574093739200100, 0.4045626180513098857 ) ) ;
#17917=ORIENTED_EDGE ( 'NONE', *, *, #683, .T. ) ;
#17921=ORIENTED_EDGE ( 'NONE', *, *, #32409, .F. ) ;
#17923=CARTESIAN_POINT ( 'NONE',  ( -3.250000000000000000, -2.600000000000000089, 0.000000000000000000 ) ) ;
#17925=CARTESIAN_POINT ( 'NONE',  ( 12.50000000000000000, -23.44678171330999916, 1.250000000000000000 ) ) ;
#17926=ORIENTED_EDGE ( 'NONE', *, *, #49819, .T. ) ;
#17928=ORIENTED_EDGE ( 'NONE', *, *, #9736, .T. ) ;
#17931=CARTESIAN_POINT ( 'NONE',  ( -7.601397897754999633, -55.55000000278000272, 10.07627163191000008 ) ) ;
#17932=CARTESIAN_POINT ( 'NONE',  ( -7.668949790020999302, -19.22870851082999977, -10.21381326473999884 ) ) ;
#17933=CARTESIAN_POINT ( 'NONE',  ( -5.915616301254464915, -77.28183550628908449, -10.26021406754873233 ) ) ;
#17934=CARTESIAN_POINT ( 'NONE',  ( 12.70556836352000118, -62.02772277195000328, 2.424222323408999617E-09 ) ) ;
#17935=CARTESIAN_POINT ( 'NONE',  ( 7.642160924878999673, -59.58461666436000570, -10.55911395187000146 ) ) ;
#17937=CIRCLE ( 'NONE', #25475, 12.50000000000000000 ) ;
#17939=DIRECTION ( 'NONE',  ( 0.7071067811865475727, 0.000000000000000000, 0.7071067811865475727 ) ) ;
#17942=CARTESIAN_POINT ( 'NONE',  ( -12.77657003524999979, -16.68789974453000369, 0.1588669551757000142 ) ) ;
#17944=CARTESIAN_POINT ( 'NONE',  ( 8.800000000000000711, 0.000000000000000000, 0.000000000000000000 ) ) ;
#17946=CARTESIAN_POINT ( 'NONE',  ( 3.500000000000000000, -3.500000000000000000, 1.049058100190999900E-13 ) ) ;
#17947=LINE ( 'NONE', #36238, #58061 ) ;
#17948=CARTESIAN_POINT ( 'NONE',  ( -1.342840445321999976, -1.150401880087000173, -3.364826939129000216 ) ) ;
#17949=CARTESIAN_POINT ( 'NONE',  ( 7.651160336697000020, -56.03767313780999615, 10.45205658995000064 ) ) ;
#17951=CARTESIAN_POINT ( 'NONE',  ( 12.66235429711000116, -61.93741783389999966, -0.4955846680318000130 ) ) ;
#17953=CARTESIAN_POINT ( 'NONE',  ( -13.63885489310999510, -22.78578169018999944, -7.254376133916000668 ) ) ;
#17959=DIRECTION ( 'NONE',  ( 0.000000000000000000, -1.000000000000000000, -2.922721309575999778E-13 ) ) ;
#17962=ORIENTED_EDGE ( 'NONE', *, *, #46535, .F. ) ;
#17967=FACE_OUTER_BOUND ( 'NONE', #9638, .T. ) ;
#17970=CARTESIAN_POINT ( 'NONE',  ( -10.47840054248000108, -60.58693148419000352, 7.622763498592000531 ) ) ;
#17972=CARTESIAN_POINT ( 'NONE',  ( 5.354686402641000598, -77.09581360186999177, 11.45119097547000031 ) ) ;
#17973=LINE ( 'NONE', #31224, #37799 ) ;
#17974=CARTESIAN_POINT ( 'NONE',  ( 12.55458806505999902, -24.16283916848999880, -1.575041344316999936 ) ) ;
#17975=CARTESIAN_POINT ( 'NONE',  ( -7.850068286643266724, -54.48530314308822398, -9.837745659579251623 ) ) ;
#17976=EDGE_LOOP ( 'NONE', ( #19377, #12165, #57819 ) ) ;
#17977=CARTESIAN_POINT ( 'NONE',  ( -1.689459950992686865, -54.50811746068543329, -12.71013585606787366 ) ) ;
#17984=ORIENTED_EDGE ( 'NONE', *, *, #21885, .F. ) ;
#17985=AXIS2_PLACEMENT_3D ( 'NONE', #6132, #24139, #42158 ) ;
#17987=CARTESIAN_POINT ( 'NONE',  ( 11.15483436911470072, -77.92097904722264445, -3.785860825438485566 ) ) ;
#17988=CARTESIAN_POINT ( 'NONE',  ( -1.667917367010000040, -23.28056692670000061, 12.49306752634999995 ) ) ;
#17989=ORIENTED_EDGE ( 'NONE', *, *, #29098, .T. ) ;
#17990=EDGE_LOOP ( 'NONE', ( #16688, #56840, #34160, #38664 ) ) ;
#17991=CARTESIAN_POINT ( 'NONE',  ( -10.30768118222999874, -55.05239703883000146, -7.634415485482000108 ) ) ;
#17993=EDGE_LOOP ( 'NONE', ( #33738, #52204, #18261, #13473 ) ) ;
#17996=CIRCLE ( 'NONE', #51934, 0.5000000000000004441 ) ;
#17998=ORIENTED_EDGE ( 'NONE', *, *, #27017, .T. ) ;
#18000=CARTESIAN_POINT ( 'NONE',  ( 8.485281374238999419, -55.54999999966999980, -8.485281374238999419 ) ) ;
#18002=CARTESIAN_POINT ( 'NONE',  ( -10.63665183518000035, -77.94466387191998535, 7.669898027128999374 ) ) ;
#18008=ORIENTED_EDGE ( 'NONE', *, *, #15950, .T. ) ;
#18009=CARTESIAN_POINT ( 'NONE',  ( -12.00000000000000000, -60.04999999966999980, 1.250000000000000000 ) ) ;
#18013=CARTESIAN_POINT ( 'NONE',  ( -0.4732678188519857110, -3.234965057628082619, 3.486999387683345386 ) ) ;
#18014=CARTESIAN_POINT ( 'NONE',  ( -10.21026245503029450, -17.74392421793578833, 7.764236519581510620 ) ) ;
#18016=CARTESIAN_POINT ( 'NONE',  ( -9.502896619458471861, -61.54094210167068013, -8.179425867623026036 ) ) ;
#18019=CARTESIAN_POINT ( 'NONE',  ( 6.375617654102788912, -77.38048332243674565, 10.18566900156049115 ) ) ;
#18020=CARTESIAN_POINT ( 'NONE',  ( -13.02337492114030937, -76.45447530479343357, -0.3199942328547237813 ) ) ;
#18023=VERTEX_POINT ( 'NONE', #44293 ) ;
#18027=CARTESIAN_POINT ( 'NONE',  ( -1.250000000000000000, -60.04999999966999980, 12.00000000000000000 ) ) ;
#18032=CARTESIAN_POINT ( 'NONE',  ( 0.9113424693958999123, -53.97464206407000376, -12.54674099554000044 ) ) ;
#18033=CARTESIAN_POINT ( 'NONE',  ( 4.498561486224415873, -76.04320336603228725, 10.85439371926396390 ) ) ;
#18036=ORIENTED_EDGE ( 'NONE', *, *, #57484, .F. ) ;
#18041=ADVANCED_FACE ( 'NONE', ( #8143 ), #21322, .T. ) ;
#18045=DIRECTION ( 'NONE',  ( 0.000000000000000000, 0.000000000000000000, -1.000000000000000000 ) ) ;
#18047=CARTESIAN_POINT ( 'NONE',  ( 0.000000000000000000, 4.040000000000000036, 0.000000000000000000 ) ) ;
#18048=DIRECTION ( 'NONE',  ( -0.7071067811865475727, 0.000000000000000000, -0.7071067811865475727 ) ) ;
#18050=VECTOR ( 'NONE', #1162, 1000.000000000000000 ) ;
#18053=CARTESIAN_POINT ( 'NONE',  ( 11.86920293296211959, -75.80000000000001137, -1.874119536907680406 ) ) ;
#18056=EDGE_CURVE ( 'NONE', #1253, #51275, #6608, .T. ) ;
#18058=DIRECTION ( 'NONE',  ( 0.7071067811865475727, 0.000000000000000000, 0.7071067811865475727 ) ) ;
#18060=CARTESIAN_POINT ( 'NONE',  ( 9.722718241315000398, -23.25000000000000000, -7.954951288349001004 ) ) ;
#18062=CARTESIAN_POINT ( 'NONE',  ( -12.54238271613678890, -55.27146427614203361, -1.749799002657778102 ) ) ;
#18065=VERTEX_POINT ( 'NONE', #12848 ) ;
#18068=DIRECTION ( 'NONE',  ( -0.7071067811814920612, -1.249159359038985910E-07, 0.7071067811915919821 ) ) ;
#18072=CARTESIAN_POINT ( 'NONE',  ( 7.981656248348999227, -24.71865039503999739, 10.08154475890999890 ) ) ;
#18079=VERTEX_POINT ( 'NONE', #39143 ) ;
#18082=AXIS2_PLACEMENT_3D ( 'NONE', #35625, #4050, #58077 ) ;
#18085=EDGE_CURVE ( 'NONE', #25178, #51185, #39438, .T. ) ;
#18088=CARTESIAN_POINT ( 'NONE',  ( -2.230724462936999775, -75.89422385439000607, 12.93113956155000110 ) ) ;
#18091=CARTESIAN_POINT ( 'NONE',  ( 7.710118476707999768, -21.74977139563000250, -10.18499221085999906 ) ) ;
#18101=CARTESIAN_POINT ( 'NONE',  ( -10.53494359615000064, -18.77285042833999995, 7.618393753193999807 ) ) ;
#18102=CARTESIAN_POINT ( 'NONE',  ( 0.000000000000000000, 4.040000000000000036, 0.000000000000000000 ) ) ;
#18107=B_SPLINE_CURVE_WITH_KNOTS ( 'NONE', 3,
 ( #43328, #16174, #34732, #35016, #57186, #53333, #12600, #3743, #25597, #8456, #21170, #39173, #44196, #29726, #52760, #12881, #12315, #48916 ),
 .UNSPECIFIED., .F., .F.,
 ( 4, 2, 2, 2, 2, 2, 2, 2, 4 ),
 ( 0.000000000000000000, 0.06250000000000124900, 0.1250000000000024980, 0.2500000000000053846, 0.5000000000000034417, 0.7500000000000014433, 0.8125000000000008882, 0.8750000000000003331, 1.000000000000000000 ),
 .UNSPECIFIED. ) ;
#18112=ORIENTED_EDGE ( 'NONE', *, *, #15370, .T. ) ;
#18113=CARTESIAN_POINT ( 'NONE',  ( 1.200170490674999924, -54.36594297968999712, 12.43444080546999864 ) ) ;
#18114=CARTESIAN_POINT ( 'NONE',  ( -2.065550207748000133, -60.22565079297999802, -12.82162303857000119 ) ) ;
#18115=CARTESIAN_POINT ( 'NONE',  ( -9.998727717461511233, -23.92738947620295065, 7.709134076961340121 ) ) ;
#18118=CARTESIAN_POINT ( 'NONE',  ( 0.000000000000000000, -80.70000000000000284, 0.000000000000000000 ) ) ;
#18119=CARTESIAN_POINT ( 'NONE',  ( -3.250000000000000000, -1.500000000000000000, 0.000000000000000000 ) ) ;
#18121=CARTESIAN_POINT ( 'NONE',  ( -0.5506765233274999449, -62.05954292211000478, 12.77514798316000011 ) ) ;
#18122=CARTESIAN_POINT ( 'NONE',  ( 12.59651451717999926, -18.60944962361000066, 1.801708894189000043 ) ) ;
#18125=CARTESIAN_POINT ( 'NONE',  ( 0.000000000000000000, -46.09579702914000165, 0.000000000000000000 ) ) ;
#18132=CARTESIAN_POINT ( 'NONE',  ( -12.68624828431999951, -60.56426635971000394, 1.886933512377000133 ) ) ;
#18134=CYLINDRICAL_SURFACE ( 'NONE', #24954, 0.5000000000000004441 ) ;
#18140=CARTESIAN_POINT ( 'NONE',  ( 0.000000000000000000, -5.899999999999999467, 0.000000000000000000 ) ) ;
#18142=ORIENTED_EDGE ( 'NONE', *, *, #49214, .F. ) ;
#18144=VERTEX_POINT ( 'NONE', #12282 ) ;
#18145=DIRECTION ( 'NONE',  ( 0.000000000000000000, 1.000000000000000000, 0.000000000000000000 ) ) ;
#18149=FACE_OUTER_BOUND ( 'NONE', #52853, .T. ) ;
#18153=CIRCLE ( 'NONE', #10663, 13.86363636363999952 ) ;
#18157=DIRECTION ( 'NONE',  ( -0.6562721000481037681, -0.7545243075597046767, -7.882643894065047749E-10 ) ) ;
#18158=CARTESIAN_POINT ( 'NONE',  ( -11.67960876285000005, -78.22858449693998750, 2.349052183356000079 ) ) ;
#18159=VERTEX_POINT ( 'NONE', #52731 ) ;
#18168=CARTESIAN_POINT ( 'NONE',  ( 11.83733200052000178, -78.20185341714999083, 5.266624269285999915 ) ) ;
#18176=CARTESIAN_POINT ( 'NONE',  ( -10.21380041493999968, -59.57152778012000027, 7.668936932637000048 ) ) ;
#18177=DIRECTION ( 'NONE',  ( 0.07798810159654839813, 0.04890177473143900166, -0.9957542229071799644 ) ) ;
#18182=CARTESIAN_POINT ( 'NONE',  ( -1.568660613942000071, -1.908528923320000237, -3.467930652269000102 ) ) ;
#18184=VERTEX_POINT ( 'NONE', #16141 ) ;
#18189=EDGE_CURVE ( 'NONE', #7374, #44340, #6535, .T. ) ;
#18191=CARTESIAN_POINT ( 'NONE',  ( -1.264141272797000060, -77.63459063407999849, -12.95149364859999963 ) ) ;
#18192=VECTOR ( 'NONE', #29634, 1000.000000000000000 ) ;
#18194=CARTESIAN_POINT ( 'NONE',  ( 12.71658889741999943, -23.31584477285000290, -1.931087888049999979 ) ) ;
#18195=EDGE_LOOP ( 'NONE', ( #26326, #53347, #39479, #38009 ) ) ;
#18197=CARTESIAN_POINT ( 'NONE',  ( -8.385799987675619960, -24.88809827228847738, -9.298537617332518934 ) ) ;
#18198=CYLINDRICAL_SURFACE ( 'NONE', #55953, 1.750000000000001332 ) ;
#18199=ADVANCED_FACE ( 'NONE', ( #57445 ), #30848, .F. ) ;
#18201=CARTESIAN_POINT ( 'NONE',  ( 0.000000000000000000, -55.54999999966999980, -12.00000000000000000 ) ) ;
#18203=EDGE_CURVE ( 'NONE', #54024, #43980, #7565, .T. ) ;
#18205=CARTESIAN_POINT ( 'NONE',  ( -0.7824435345810000220, -1.638598507945999927, 3.939770163431000061 ) ) ;
#18208=EDGE_LOOP ( 'NONE', ( #42309, #45306, #36782, #11619 ) ) ;
#18210=CARTESIAN_POINT ( 'NONE',  ( 3.600000000000000089, -0.6500000000000000222, 0.000000000000000000 ) ) ;
#18217=VERTEX_POINT ( 'NONE', #39719 ) ;
#18220=ORIENTED_EDGE ( 'NONE', *, *, #11136, .T. ) ;
#18222=CARTESIAN_POINT ( 'NONE',  ( -2.277289417900965951, -2.664078063540779251, -2.318001052940313222 ) ) ;
#18224=AXIS2_PLACEMENT_3D ( 'NONE', #41169, #37025, #23450 ) ;
#18226=CARTESIAN_POINT ( 'NONE',  ( -10.42531125070999920, -60.06485145371000556, 7.624341767111000756 ) ) ;
#18229=ORIENTED_EDGE ( 'NONE', *, *, #53703, .T. ) ;
#18233=CARTESIAN_POINT ( 'NONE',  ( -7.654537165467999671, -18.71943464842000182, -10.01332852689000141 ) ) ;
#18234=CARTESIAN_POINT ( 'NONE',  ( 11.44417895085270054, -77.07083333333331154, 3.075537641221564922 ) ) ;
#18235=EDGE_CURVE ( 'NONE', #33163, #46715, #41187, .T. ) ;
#18236=AXIS2_PLACEMENT_3D ( 'NONE', #24503, #52244, #38077 ) ;
#18237=CARTESIAN_POINT ( 'NONE',  ( 7.220923959705223716, -78.62291666666662593, 9.396085398178630754 ) ) ;
#18242=DIRECTION ( 'NONE',  ( 0.000000000000000000, 1.000000000000000000, 0.000000000000000000 ) ) ;
#18246=CARTESIAN_POINT ( 'NONE',  ( -0.9887300587124998597, -24.93410057768999977, 12.65963207090000076 ) ) ;
#18247=CARTESIAN_POINT ( 'NONE',  ( -12.56594317991999965, -60.04999999381999487, -1.750000000001000089 ) ) ;
#18248=CARTESIAN_POINT ( 'NONE',  ( -3.800400640911000050, -0.9038930985898999682, -1.100537862409999956 ) ) ;
#18249=DIRECTION ( 'NONE',  ( 0.000000000000000000, -1.000000000000000000, 0.000000000000000000 ) ) ;
#18250=CARTESIAN_POINT ( 'NONE',  ( 1.704789468941017461, -55.09653838334687492, -12.53199752951670121 ) ) ;
#18251=CARTESIAN_POINT ( 'NONE',  ( 10.18589226629999978, -55.51082276539999327, 7.641012305205999056 ) ) ;
#18253=CARTESIAN_POINT ( 'NONE',  ( 12.77306367233000017, -61.85881314422999822, -1.040970605966999862 ) ) ;
#18254=CARTESIAN_POINT ( 'NONE',  ( -7.714303428875997959, -15.69705297113999443, -12.53545825868000385 ) ) ;
#18257=CARTESIAN_POINT ( 'NONE',  ( 3.250000000000000000, -2.250000000000000000, 0.000000000000000000 ) ) ;
#18258=DIRECTION ( 'NONE',  ( 0.000000000000000000, 0.000000000000000000, -1.000000000000000000 ) ) ;
#18261=ORIENTED_EDGE ( 'NONE', *, *, #30633, .T. ) ;
#18263=AXIS2_PLACEMENT_3D ( 'NONE', #53468, #18048, #36040 ) ;
#18266=CARTESIAN_POINT ( 'NONE',  ( -1.980464439859999981, -58.55472017426999543, -12.85144117154000121 ) ) ;
#18269=PLANE ( 'NONE',  #32320 ) ;
#18271=CARTESIAN_POINT ( 'NONE',  ( 7.199854605362999926, -77.42884144764001064, -10.39073109867000078 ) ) ;
#18273=CARTESIAN_POINT ( 'NONE',  ( 12.44180635029999848, -24.09260544925000147, -1.459447571597000115 ) ) ;
#18274=CARTESIAN_POINT ( 'NONE',  ( -7.764005369683503410, -54.67720632257901769, -9.931049914567516623 ) ) ;
#18275=ORIENTED_EDGE ( 'NONE', *, *, #36617, .T. ) ;
#18276=AXIS2_PLACEMENT_3D ( 'NONE', #39390, #26373, #18925 ) ;
#18277=CARTESIAN_POINT ( 'NONE',  ( -1.501534314747794197, -54.24847048308625830, -12.70455943736288162 ) ) ;
#18279=DIRECTION ( 'NONE',  ( 0.000000000000000000, 0.000000000000000000, 1.000000000000000000 ) ) ;
#18281=CARTESIAN_POINT ( 'NONE',  ( -12.87024489158000051, -56.01538333533000014, -2.062597265787999845 ) ) ;
#18282=DIRECTION ( 'NONE',  ( 0.7592504785508672471, -0.04890181650111791178, -0.6489586451871721673 ) ) ;
#18285=CARTESIAN_POINT ( 'NONE',  ( 10.27340958486082911, -60.86161210392387488, -7.712164009451872637 ) ) ;
#18287=ORIENTED_EDGE ( 'NONE', *, *, #15507, .T. ) ;
#18288=EDGE_CURVE ( 'NONE', #49604, #35471, #49772, .T. ) ;
#18289=CARTESIAN_POINT ( 'NONE',  ( -7.618394506877000261, -55.57286435768999411, -10.53494428257999971 ) ) ;
#18296=CARTESIAN_POINT ( 'NONE',  ( 8.485281374238999419, 0.000000000000000000, -8.485281374238999419 ) ) ;
#18304=ORIENTED_EDGE ( 'NONE', *, *, #31348, .T. ) ;
#18308=VECTOR ( 'NONE', #7827, 1000.000000000000114 ) ;
#18309=CARTESIAN_POINT ( 'NONE',  ( 1.232226824161556822, -61.32290911199036998, -12.50408896753027399 ) ) ;
#18310=CARTESIAN_POINT ( 'NONE',  ( -2.469193059067599449, -3.286120914691780470, 2.507410431938543294 ) ) ;
#18311=CARTESIAN_POINT ( 'NONE',  ( 7.633089125635001082, -60.19007426270999872, -10.18115018433999985 ) ) ;
#18312=CARTESIAN_POINT ( 'NONE',  ( -1.307210027570999911, -79.13383490254000208, -12.19386267984000050 ) ) ;
#18317=CARTESIAN_POINT ( 'NONE',  ( 11.85843863511279750, -77.28708609005155949, -1.943283807933854135 ) ) ;
#18320=ORIENTED_EDGE ( 'NONE', *, *, #497, .F. ) ;
#18322=FACE_OUTER_BOUND ( 'NONE', #22702, .T. ) ;
#18329=CARTESIAN_POINT ( 'NONE',  ( 4.536962941760771528, -76.04292347826114451, 10.83842670349287829 ) ) ;
#18332=ORIENTED_EDGE ( 'NONE', *, *, #3399, .T. ) ;
#18333=CARTESIAN_POINT ( 'NONE',  ( -3.151328970204000157, -76.15439989502468165, -11.89977497055999578 ) ) ;
#18338=EDGE_CURVE ( 'NONE', #9760, #45320, #7217, .T. ) ;
#18342=ORIENTED_EDGE ( 'NONE', *, *, #21861, .F. ) ;
#18343=AXIS2_PLACEMENT_3D ( 'NONE', #1496, #24786, #42801 ) ;
#18345=CARTESIAN_POINT ( 'NONE',  ( 12.70722357730233476, -54.38971352745510046, 1.610228312158712649 ) ) ;
#18346=CARTESIAN_POINT ( 'NONE',  ( 5.412990059381605157, -75.80000000000001137, -10.58789199075580356 ) ) ;
#18357=ORIENTED_EDGE ( 'NONE', *, *, #10448, .T. ) ;
#18359=DIRECTION ( 'NONE',  ( 1.000000000000000000, 0.000000000000000000, 0.000000000000000000 ) ) ;
#18363=CARTESIAN_POINT ( 'NONE',  ( 10.13402523425000012, -23.72303809441999789, 7.647751776486000352 ) ) ;
#18370=ORIENTED_EDGE ( 'NONE', *, *, #57812, .T. ) ;
#18372=ORIENTED_EDGE ( 'NONE', *, *, #20574, .T. ) ;
#18375=AXIS2_PLACEMENT_3D ( 'NONE', #51709, #51994, #48149 ) ;
#18376=DIRECTION ( 'NONE',  ( 0.7071067811865474617, 0.000000000000000000, 0.7071067811865474617 ) ) ;
#18378=CARTESIAN_POINT ( 'NONE',  ( -2.140299208497000283, -75.94309928261999687, -12.62824205103000175 ) ) ;
#18379=CARTESIAN_POINT ( 'NONE',  ( -3.140773129254233798, -2.022905696757374194, -0.9277136712588065492 ) ) ;
#18381=CARTESIAN_POINT ( 'NONE',  ( 7.674614791514000167, -19.24899163938999891, -10.14948852566999804 ) ) ;
#18384=CARTESIAN_POINT ( 'NONE',  ( -10.31444895689000063, -24.30075145017000082, -7.758883253342000685 ) ) ;
#18385=ADVANCED_FACE ( 'NONE', ( #488, #27594 ), #31727, .T. ) ;
#18386=CARTESIAN_POINT ( 'NONE',  ( -8.190859204290999784, -59.94999999967000548, 7.342331066867000544 ) ) ;
#18394=CARTESIAN_POINT ( 'NONE',  ( 7.220923959705269013, -78.47708333333336839, -9.396085398178609438 ) ) ;
#18396=FACE_OUTER_BOUND ( 'NONE', #23027, .T. ) ;
#18411=ADVANCED_FACE ( 'NONE', ( #3996 ), #9025, .F. ) ;
#18412=CARTESIAN_POINT ( 'NONE',  ( -10.20000000000000107, -0.5000000000000000000, 0.000000000000000000 ) ) ;
#18413=CARTESIAN_POINT ( 'NONE',  ( 12.44180763926000033, -17.90743932638000047, 1.459474665415000150 ) ) ;
#18415=CARTESIAN_POINT ( 'NONE',  ( 12.50000000000000000, -39.30476017083000073, 0.000000000000000000 ) ) ;
#18416=CARTESIAN_POINT ( 'NONE',  ( 10.07615509324000058, -54.07367739666999285, -7.986954869161998261 ) ) ;
#18418=B_SPLINE_CURVE_WITH_KNOTS ( 'NONE', 3,
 ( #22945, #48935, #45099, #13192, #22349, #8477 ),
 .UNSPECIFIED., .F., .F.,
 ( 4, 2, 4 ),
 ( 0.000000000000000000, 0.5000000000000000000, 1.000000000000000000 ),
 .UNSPECIFIED. ) ;
#18422=CIRCLE ( 'NONE', #5096, 0.5000000000000004441 ) ;
#18425=CARTESIAN_POINT ( 'NONE',  ( -12.77568181207000109, -62.06511628600999586, 0.5294980821349999367 ) ) ;
#18432=CARTESIAN_POINT ( 'NONE',  ( 0.9356112540328053173, -61.54107830070423546, 12.50329130249443743 ) ) ;
#18434=CARTESIAN_POINT ( 'NONE',  ( 7.452378523309701741, -55.25278097498932794, 8.090910852015767318 ) ) ;
#18437=CARTESIAN_POINT ( 'NONE',  ( -3.500000000146000101, -0.7499999998540000101, 2.054632350152999929E-08 ) ) ;
#18438=VERTEX_POINT ( 'NONE', #18756 ) ;
#18439=DIRECTION ( 'NONE',  ( -0.7592504788686247341, -0.04890177850579158214, -0.6489586476785208502 ) ) ;
#18440=VERTEX_POINT ( 'NONE', #17583 ) ;
#18441=CARTESIAN_POINT ( 'NONE',  ( -1.798944584243999945, -18.78466771720000139, 12.61116915999999932 ) ) ;
#18442=FACE_OUTER_BOUND ( 'NONE', #20470, .T. ) ;
#18446=CARTESIAN_POINT ( 'NONE',  ( 14.00000000000000000, -9.295797029142999435, -3.100994084333000442E-11 ) ) ;
#18447=CARTESIAN_POINT ( 'NONE',  ( -11.22421241263000091, -78.71717670423001323, 3.993551959072000557 ) ) ;
#18450=ORIENTED_EDGE ( 'NONE', *, *, #7112, .T. ) ;
#18454=DIRECTION ( 'NONE',  ( 1.000000000000000000, 0.000000000000000000, 0.000000000000000000 ) ) ;
#18456=CARTESIAN_POINT ( 'NONE',  ( 12.51393054458000087, -76.64772347022000076, -3.351762257813000190 ) ) ;
#18459=DIRECTION ( 'NONE',  ( 0.7026410690473250398, 0.1122098755728047209, -0.7026410690473250398 ) ) ;
#18460=EDGE_CURVE ( 'NONE', #38307, #40915, #26077, .T. ) ;
#18461=CYLINDRICAL_SURFACE ( 'NONE', #46380, 0.5999999999999999778 ) ;
#18464=FACE_OUTER_BOUND ( 'NONE', #31113, .T. ) ;
#18465=CARTESIAN_POINT ( 'NONE',  ( 6.732436628721946370, -76.87268005267617355, -9.713303325498781504 ) ) ;
#18470=CARTESIAN_POINT ( 'NONE',  ( -0.6934022908089999548, -3.206912479849000075, 3.742362521638999961 ) ) ;
#18473=CARTESIAN_POINT ( 'NONE',  ( 0.5999999999999999778, -23.15000000000000213, 10.98362417419999915 ) ) ;
#18476=FACE_OUTER_BOUND ( 'NONE', #53125, .T. ) ;
#18478=CARTESIAN_POINT ( 'NONE',  ( 5.512103878356000131, -76.82285899393998818, 11.78783395355999986 ) ) ;
#18480=CARTESIAN_POINT ( 'NONE',  ( -7.624341766656999475, -60.06485146221000093, -10.42531125026000005 ) ) ;
#18481=CARTESIAN_POINT ( 'NONE',  ( 12.92177931909999877, -20.24263462181000151, -2.062503053667999797 ) ) ;
#18485=CARTESIAN_POINT ( 'NONE',  ( 7.705142895586000407, -21.75083378359999742, -10.24998526315000014 ) ) ;
#18488=CARTESIAN_POINT ( 'NONE',  ( -0.1204595238885999980, -0.6257393593719999814, 3.497926457646999943 ) ) ;
#18490=CARTESIAN_POINT ( 'NONE',  ( 0.000000000000000000, -63.73717104351998586, 0.000000000000000000 ) ) ;
#18491=ORIENTED_EDGE ( 'NONE', *, *, #1200, .T. ) ;
#18496=ORIENTED_EDGE ( 'NONE', *, *, #16512, .F. ) ;
#18503=ORIENTED_EDGE ( 'NONE', *, *, #10519, .T. ) ;
#18506=CARTESIAN_POINT ( 'NONE',  ( -0.2041385330985947544, -2.721221240235607741, -3.249266545227842418 ) ) ;
#18507=AXIS2_PLACEMENT_3D ( 'NONE', #13612, #53780, #22176 ) ;
#18508=TOROIDAL_SURFACE ( 'NONE', #32636, 17.50000000000000000, 5.000000000000000000 ) ;
#18511=EDGE_LOOP ( 'NONE', ( #28132, #34672, #53868 ) ) ;
#18513=VECTOR ( 'NONE', #36459, 1000.000000000000000 ) ;
#18514=ORIENTED_EDGE ( 'NONE', *, *, #16242, .T. ) ;
#18517=CARTESIAN_POINT ( 'NONE',  ( 17.50000000000000000, -51.86282895648000135, 3.979093998740999976E-10 ) ) ;
#18520=FACE_OUTER_BOUND ( 'NONE', #33088, .T. ) ;
#18521=DIRECTION ( 'NONE',  ( 0.000000000000000000, -1.000000000000000000, 1.221245327088000045E-14 ) ) ;
#18522=CARTESIAN_POINT ( 'NONE',  ( 7.612971414697999428, -55.47547470607999998, -10.53003223722000037 ) ) ;
#18527=CARTESIAN_POINT ( 'NONE',  ( -13.89248035986000041, -9.608407476587998985, -2.632528379381999666E-05 ) ) ;
#18531=CARTESIAN_POINT ( 'NONE',  ( 4.520621932142114829, -78.29753379422295723, 11.20346742569165777 ) ) ;
#18534=CARTESIAN_POINT ( 'NONE',  ( 0.000000000000000000, -9.638971321655001034, 0.000000000000000000 ) ) ;
#18535=CARTESIAN_POINT ( 'NONE',  ( 1.750000000000000000, -23.24999999758999536, 12.50000000000000000 ) ) ;
#18536=CARTESIAN_POINT ( 'NONE',  ( -0.4802748259353999960, -25.00526907281999911, 12.54896097834000024 ) ) ;
#18537=CARTESIAN_POINT ( 'NONE',  ( 12.00000000000000000, -79.25000000000000000, 1.072514965728000067E-08 ) ) ;
#18539=CARTESIAN_POINT ( 'NONE',  ( -0.1186549498682999831, -0.7591989345079001028, 3.445524895640000196 ) ) ;
#18540=CARTESIAN_POINT ( 'NONE',  ( 7.624341764906000130, -55.53514850498000044, 10.42531124851000079 ) ) ;
#18541=CARTESIAN_POINT ( 'NONE',  ( 10.59548767699999949, -57.04263462147999775, 7.678667886061999681 ) ) ;
#18542=CARTESIAN_POINT ( 'NONE',  ( -1.801750019963999971, -23.39007426722000105, -12.59656967653999970 ) ) ;
#18544=CARTESIAN_POINT ( 'NONE',  ( 0.000000000000000000, 0.000000000000000000, 0.000000000000000000 ) ) ;
#18545=CARTESIAN_POINT ( 'NONE',  ( 12.99510751537000353, -26.30294702886003222, -6.911973076623003642 ) ) ;
#18546=VECTOR ( 'NONE', #15901, 1000.000000000000000 ) ;
#18548=DIRECTION ( 'NONE',  ( 0.000000000000000000, -1.000000000000000000, 0.000000000000000000 ) ) ;
#18549=EDGE_CURVE ( 'NONE', #43269, #8841, #15192, .T. ) ;
#18553=ORIENTED_EDGE ( 'NONE', *, *, #56709, .T. ) ;
#18558=VECTOR ( 'NONE', #1933, 1000.000000000000000 ) ;
#18559=CARTESIAN_POINT ( 'NONE',  ( -1.980464483675000054, -57.04439829357999514, -12.85140862645999782 ) ) ;
#18562=CARTESIAN_POINT ( 'NONE',  ( 12.54980553584999825, -53.75222688831999562, 0.05649961219499999993 ) ) ;
#18563=CARTESIAN_POINT ( 'NONE',  ( -3.206516299415000049, -2.013032031398999777, -0.5298615117031000299 ) ) ;
#18564=VECTOR ( 'NONE', #50690, 1000.000000000000000 ) ;
#18565=CARTESIAN_POINT ( 'NONE',  ( 2.459153317701999963, -0.9829018800870999995, -3.188313159924000217 ) ) ;
#18567=DIRECTION ( 'NONE',  ( 0.9957542217955427377, -0.04890179608120209104, 0.07798810240277338768 ) ) ;
#18568=CARTESIAN_POINT ( 'NONE',  ( -7.954951288349001004, -18.75000000000000000, 9.722718241315000398 ) ) ;
#18569=EDGE_LOOP ( 'NONE', ( #54518, #10570, #42613, #11749, #31922, #3162, #17618, #9205 ) ) ;
#18571=CARTESIAN_POINT ( 'NONE',  ( 0.9935076048416776606, -53.83183812219430564, -12.70250268212331157 ) ) ;
#18574=EDGE_CURVE ( 'NONE', #21690, #19884, #6336, .T. ) ;
#18576=CARTESIAN_POINT ( 'NONE',  ( -12.58335110162999904, -58.54888345776999614, -1.667961430005999945 ) ) ;
#18578=EDGE_LOOP ( 'NONE', ( #19904, #16181, #35095 ) ) ;
#18580=CARTESIAN_POINT ( 'NONE',  ( 7.610436523699107170, -60.32540704676000587, -10.41144397134746136 ) ) ;
#18582=CARTESIAN_POINT ( 'NONE',  ( -10.19022281664999952, -55.60366258855000154, -7.646946378492000207 ) ) ;
#18584=EDGE_LOOP ( 'NONE', ( #2329, #21109, #49585, #5494 ) ) ;
#18585=CARTESIAN_POINT ( 'NONE',  ( -7.644092900757152087, -55.27619833568792274, 10.09634159697596800 ) ) ;
#18586=CARTESIAN_POINT ( 'NONE',  ( -12.50000000000000000, -60.04999999657000131, -1.750000000000000000 ) ) ;
#18588=ORIENTED_EDGE ( 'NONE', *, *, #22033, .T. ) ;
#18591=CARTESIAN_POINT ( 'NONE',  ( -8.414570695956999913, -55.64999999967000122, 8.414570695956999913 ) ) ;
#18593=CARTESIAN_POINT ( 'NONE',  ( -9.299140214180997788, -78.14275400357000478, -9.021566674317000434 ) ) ;
#18597=AXIS2_PLACEMENT_3D ( 'NONE', #44956, #4803, #44080 ) ;
#18601=CARTESIAN_POINT ( 'NONE',  ( 3.007117222848000093, -75.90736186172000544, 11.93703523519999976 ) ) ;
#18604=CARTESIAN_POINT ( 'NONE',  ( 2.752649745648064084, -2.544360987267859642, -2.286872036682715770 ) ) ;
#18606=CARTESIAN_POINT ( 'NONE',  ( -10.39285214024000048, -78.47279838679000363, 6.510605926401999533 ) ) ;
#18611=CARTESIAN_POINT ( 'NONE',  ( -1.336107520624923994, -77.43385316951449227, 11.99618174931092796 ) ) ;
#18612=CARTESIAN_POINT ( 'NONE',  ( -2.511165522482547097, -76.34295674094352080, 12.78297198345306818 ) ) ;
#18613=ORIENTED_EDGE ( 'NONE', *, *, #20105, .T. ) ;
#18621=EDGE_CURVE ( 'NONE', #39575, #3891, #6284, .T. ) ;
#18622=CARTESIAN_POINT ( 'NONE',  ( 0.0001230185931830488706, -76.07467095836980775, 11.74978004242729668 ) ) ;
#18626=CARTESIAN_POINT ( 'NONE',  ( 7.678655902612541162, -18.20623020282301852, -10.03844298039529370 ) ) ;
#18627=EDGE_CURVE ( 'NONE', #30461, #19, #47779, .T. ) ;
#18629=CARTESIAN_POINT ( 'NONE',  ( -5.496747179549230644, -76.28607285822243966, -10.38820195124879397 ) ) ;
#18631=CARTESIAN_POINT ( 'NONE',  ( 0.000000000000000000, -6.049999999381999949, 0.000000000000000000 ) ) ;
#18632=CARTESIAN_POINT ( 'NONE',  ( 12.50728313516224688, -17.00024825485536084, -0.1773837593737443152 ) ) ;
#18633=CARTESIAN_POINT ( 'NONE',  ( -8.485281374238999419, -18.75000000000000000, 8.485281374238999419 ) ) ;
#18634=CARTESIAN_POINT ( 'NONE',  ( 7.658894278891000162, -18.79060682915999791, -10.01676917982000070 ) ) ;
#18635=CARTESIAN_POINT ( 'NONE',  ( 8.441163348740026606, -17.08348045813557192, 9.243160721208877106 ) ) ;
#18636=VERTEX_POINT ( 'NONE', #42364 ) ;
#18638=CARTESIAN_POINT ( 'NONE',  ( 0.000000000000000000, -32.70420297070000260, 0.000000000000000000 ) ) ;
#18639=CARTESIAN_POINT ( 'NONE',  ( -7.919595949288999570, -55.64999999964999233, 9.050966799188000067 ) ) ;
#18641=ADVANCED_FACE ( 'NONE', ( #11077 ), #50646, .T. ) ;
#18642=CARTESIAN_POINT ( 'NONE',  ( 12.50409240828692958, -61.32129362315870225, 1.233800930082795677 ) ) ;
#18643=VECTOR ( 'NONE', #306, 1000.000000000000000 ) ;
#18645=DIRECTION ( 'NONE',  ( 1.000000000000000000, 0.000000000000000000, 0.000000000000000000 ) ) ;
#18647=CARTESIAN_POINT ( 'NONE',  ( -9.431004454606608078, -17.19940410572420930, -8.251853356785748161 ) ) ;
#18648=CIRCLE ( 'NONE', #56361, 0.5000000000000004441 ) ;
#18649=CARTESIAN_POINT ( 'NONE',  ( 0.000000000000000000, -33.10361340872000113, 0.000000000000000000 ) ) ;
#18654=ORIENTED_EDGE ( 'NONE', *, *, #54821, .T. ) ;
#18660=CARTESIAN_POINT ( 'NONE',  ( 7.756281347471999155, -24.22006031113999569, 10.15825374573999973 ) ) ;
#18661=CARTESIAN_POINT ( 'NONE',  ( 9.929702205026998740, -61.43097880247000120, 7.973987073312001073 ) ) ;
#18666=ORIENTED_EDGE ( 'NONE', *, *, #5903, .T. ) ;
#18667=LINE ( 'NONE', #50255, #46340 ) ;
#18671=CARTESIAN_POINT ( 'NONE',  ( 11.00000000000000000, -18.25000000000000000, 1.016729233725000008E-14 ) ) ;
#18673=CARTESIAN_POINT ( 'NONE',  ( -9.502921960388910350, -17.25907999995016695, 8.179400289350656550 ) ) ;
#18678=CARTESIAN_POINT ( 'NONE',  ( -7.660411271047999904, -23.19173735492000077, -10.01752031414999955 ) ) ;
#18679=CARTESIAN_POINT ( 'NONE',  ( -7.892048199460299784, -60.54946977258664731, 7.664266801481004698 ) ) ;
#18681=ORIENTED_EDGE ( 'NONE', *, *, #3683, .T. ) ;
#18685=CARTESIAN_POINT ( 'NONE',  ( -3.165411199172029288, -3.479166666666666963, 0.8506806241676482250 ) ) ;
#18686=CARTESIAN_POINT ( 'NONE',  ( -10.26699006316252749, -78.34166666666666856, -5.917523019358070790 ) ) ;
#18687=CARTESIAN_POINT ( 'NONE',  ( 10.42531124903999995, -55.53514851492000304, -7.624341765436000173 ) ) ;
#18688=CARTESIAN_POINT ( 'NONE',  ( 0.8293971963509981782, -2.893870552623438730, -3.421159378200740342 ) ) ;
#18691=DIRECTION ( 'NONE',  ( 0.000000000000000000, 0.000000000000000000, -1.000000000000000000 ) ) ;
#18693=EDGE_LOOP ( 'NONE', ( #11250, #46700, #36058, #15452 ) ) ;
#18695=CARTESIAN_POINT ( 'NONE',  ( -3.461985009909999800, -2.184444768727999975, 1.581285081509000046 ) ) ;
#18698=CARTESIAN_POINT ( 'NONE',  ( 7.646966600018000548, -23.19642081717000082, -10.19019745247000053 ) ) ;
#18701=CARTESIAN_POINT ( 'NONE',  ( 12.54705919859000041, -17.46307476627999833, 1.287183453418999868 ) ) ;
#18704=EDGE_CURVE ( 'NONE', #23873, #9942, #52661, .T. ) ;
#18705=DIRECTION ( 'NONE',  ( 0.000000000000000000, 1.000000000000000000, 0.000000000000000000 ) ) ;
#18716=VECTOR ( 'NONE', #28772, 1000.000000000000000 ) ;
#18717=ORIENTED_EDGE ( 'NONE', *, *, #6908, .T. ) ;
#18722=LINE ( 'NONE', #54153, #14869 ) ;
#18726=VERTEX_POINT ( 'NONE', #3358 ) ;
#18728=CARTESIAN_POINT ( 'NONE',  ( -1.933650113856000052, -18.59213746974000259, 12.70909635754000000 ) ) ;
#18729=PLANE ( 'NONE',  #5601 ) ;
#18734=CARTESIAN_POINT ( 'NONE',  ( -1.748404684387999897, -78.71803539972999886, 11.93442954260999933 ) ) ;
#18742=DIRECTION ( 'NONE',  ( 0.000000000000000000, -1.000000000000000000, 0.000000000000000000 ) ) ;
#18744=CARTESIAN_POINT ( 'NONE',  ( -9.247037010692000791, -77.48029308464001019, -9.074963555248000802 ) ) ;
#18746=CARTESIAN_POINT ( 'NONE',  ( -12.71798269385000069, -23.29778754190000001, -1.931086388578000079 ) ) ;
#18747=PLANE ( 'NONE',  #56730 ) ;
#18751=PLANE ( 'NONE',  #37139 ) ;
#18753=CARTESIAN_POINT ( 'NONE',  ( 11.00000000000000000, -4.000000000000000000, 0.000000000000000000 ) ) ;
#18755=AXIS2_PLACEMENT_3D ( 'NONE', #25914, #30625, #48658 ) ;
#18756=CARTESIAN_POINT ( 'NONE',  ( 9.505949683908001546, -79.00000000000000000, -6.906476714433999575 ) ) ;
#18758=CARTESIAN_POINT ( 'NONE',  ( 1.068619641472000170, -1.964980382298999961, -3.652926003266999899 ) ) ;
#18760=ORIENTED_EDGE ( 'NONE', *, *, #20710, .T. ) ;
#18761=CARTESIAN_POINT ( 'NONE',  ( 9.723174507645000020, -61.27697503925999456, 7.958760295356000825 ) ) ;
#18762=CARTESIAN_POINT ( 'NONE',  ( 7.892048199460342417, -60.54946977258678942, -7.664266801480966507 ) ) ;
#18763=CARTESIAN_POINT ( 'NONE',  ( -11.28030014521100810, -77.67311482005982270, 3.843155223038057677 ) ) ;
#18765=CARTESIAN_POINT ( 'NONE',  ( 11.82764905900999963, -77.26689612163998788, 5.426413045081000419 ) ) ;
#18767=AXIS2_PLACEMENT_3D ( 'NONE', #56785, #21626, #39348 ) ;
#18769=DIRECTION ( 'NONE',  ( 0.000000000000000000, 0.000000000000000000, 1.000000000000000000 ) ) ;
#18770=EDGE_LOOP ( 'NONE', ( #6528, #40152, #48121, #1035, #14896 ) ) ;
#18771=EDGE_CURVE ( 'NONE', #14108, #393, #34917, .T. ) ;
#18772=DIRECTION ( 'NONE',  ( 0.9999999999995751176, 0.000000000000000000, 9.217549102787771002E-07 ) ) ;
#18774=EDGE_CURVE ( 'NONE', #8187, #26186, #22289, .T. ) ;
#18776=CARTESIAN_POINT ( 'NONE',  ( 7.613962827179999948, -23.30639625649999758, -10.53101998747000145 ) ) ;
#18779=CARTESIAN_POINT ( 'NONE',  ( -3.587712099295000012, -1.780278923320000040, 1.801380527025000067 ) ) ;
#18780=CARTESIAN_POINT ( 'NONE',  ( 11.75000000000000000, -77.95000000000000284, 2.316376715183999699E-14 ) ) ;
#18782=ORIENTED_EDGE ( 'NONE', *, *, #43267, .F. ) ;
#18783=B_SPLINE_CURVE_WITH_KNOTS ( 'NONE', 3,
 ( #51236, #27602, #24056, #45936, #14610, #33189, #28474, #6343, #32311, #24358, #42371, #55357, #14899, #50942, #46232, #55947, #783, #23764, #18763, #55063, #50069 ),
 .UNSPECIFIED., .F., .F.,
 ( 4, 2, 2, 2, 2, 2, 2, 2, 2, 1, 4 ),
 ( 0.000000000000000000, 0.1250000000000000833, 0.2500000000000001665, 0.3750000000000001665, 0.5000000000000002220, 0.5625000000000002220, 0.6250000000000003331, 0.7500000000000002220, 0.8125000000000002220, 0.8750000000000001110, 1.000000000000000000 ),
 .UNSPECIFIED. ) ;
#18787=VERTEX_POINT ( 'NONE', #47963 ) ;
#18788=CARTESIAN_POINT ( 'NONE',  ( 0.000000000000000000, -3.500000000000000000, 0.000000000000000000 ) ) ;
#18789=CARTESIAN_POINT ( 'NONE',  ( 0.000000000000000000, 4.040000000000000036, 0.000000000000000000 ) ) ;
#18790=EDGE_CURVE ( 'NONE', #27707, #38980, #19892, .T. ) ;
#18791=DIRECTION ( 'NONE',  ( 0.000000000000000000, -1.000000000000000000, -9.323016642051001034E-14 ) ) ;
#18793=CARTESIAN_POINT ( 'NONE',  ( -1.931043762602999925, -59.57819125629999490, 12.75761570869000039 ) ) ;
#18795=ORIENTED_EDGE ( 'NONE', *, *, #9869, .F. ) ;
#18796=ORIENTED_EDGE ( 'NONE', *, *, #7728, .T. ) ;
#18797=CARTESIAN_POINT ( 'NONE',  ( 7.342356150419315775, -59.98964892062895871, 8.190836719257342580 ) ) ;
#18798=VECTOR ( 'NONE', #38680, 1000.000000000000000 ) ;
#18803=CARTESIAN_POINT ( 'NONE',  ( -8.583665413900087415, -53.82814424962094080, -9.102144265374381149 ) ) ;
#18804=ORIENTED_EDGE ( 'NONE', *, *, #23189, .T. ) ;
#18805=LINE ( 'NONE', #36797, #2634 ) ;
#18806=DIRECTION ( 'NONE',  ( -1.000000000000000000, 0.000000000000000000, 0.000000000000000000 ) ) ;
#18807=CONICAL_SURFACE ( 'NONE', #33871, 12.94999999994000106, 0.7853981633972997312 ) ;
#18808=FACE_OUTER_BOUND ( 'NONE', #31011, .T. ) ;
#18809=CARTESIAN_POINT ( 'NONE',  ( -12.24999999909999993, -80.79999999910000952, -7.143942175050000083E-09 ) ) ;
#18812=DIRECTION ( 'NONE',  ( 0.000000000000000000, -1.000000000000000000, 0.000000000000000000 ) ) ;
#18813=CARTESIAN_POINT ( 'NONE',  ( -7.678667886039000301, -58.55736537918999574, -10.59548767697000038 ) ) ;
#18815=CARTESIAN_POINT ( 'NONE',  ( 7.309900215520421796, -76.52113362030404176, 9.201699366411881797 ) ) ;
#18816=CARTESIAN_POINT ( 'NONE',  ( -0.5999999999999999778, -23.15000000000000213, -10.98362417419999915 ) ) ;
#18819=CARTESIAN_POINT ( 'NONE',  ( -1.770955775045925495, -78.06626119840052525, -11.95106029758639110 ) ) ;
#18821=EDGE_CURVE ( 'NONE', #19308, #25466, #2784, .T. ) ;
#18823=CARTESIAN_POINT ( 'NONE',  ( -1.750000000000000000, -57.05022860762000647, 12.65375411742999923 ) ) ;
#18825=CARTESIAN_POINT ( 'NONE',  ( 13.63885489310999510, -56.01421830980998351, 7.254376133916000668 ) ) ;
#18828=CARTESIAN_POINT ( 'NONE',  ( -1.211761727240999953, -0.6962337787935000133, 3.553101914771000125 ) ) ;
#18831=CARTESIAN_POINT ( 'NONE',  ( 1.569236785184999737E-14, 0.000000000000000000, 0.000000000000000000 ) ) ;
#18832=CARTESIAN_POINT ( 'NONE',  ( -2.065550207748000133, -23.42565079331000177, -12.82162303854000029 ) ) ;
#18833=CARTESIAN_POINT ( 'NONE',  ( 13.89248034750000116, -69.19159251015000223, 2.632538495191000193E-05 ) ) ;
#18834=CARTESIAN_POINT ( 'NONE',  ( -2.978010235239999748, -2.500894741108000030, 1.811261547873000088 ) ) ;
#18838=CARTESIAN_POINT ( 'NONE',  ( 11.19999999999999929, -74.80000000000001137, 0.000000000000000000 ) ) ;
#18845=EDGE_CURVE ( 'NONE', #23097, #12605, #31653, .T. ) ;
#18848=CARTESIAN_POINT ( 'NONE',  ( 12.54987159811999931, -53.74886760158999977, -0.1385534523824999975 ) ) ;
#18850=CARTESIAN_POINT ( 'NONE',  ( -3.336429633373000136, -0.6982797842361000429, 0.8683076097535999960 ) ) ;
#18851=CARTESIAN_POINT ( 'NONE',  ( 10.13881649148000008, -76.50783510652000530, -5.938594122520999719 ) ) ;
#18853=ORIENTED_EDGE ( 'NONE', *, *, #4889, .F. ) ;
#18854=CARTESIAN_POINT ( 'NONE',  ( 1.575772165460815666, -54.33845457181070060, -12.70597445614748366 ) ) ;
#18857=CARTESIAN_POINT ( 'NONE',  ( 11.63975115694809226, -75.93720323772257075, -1.845775132419555487 ) ) ;
#18858=CARTESIAN_POINT ( 'NONE',  ( 7.601397897754999633, -60.04999999966999980, 9.369164850722000892 ) ) ;
#18859=DIRECTION ( 'NONE',  ( -1.000000000000000000, 0.000000000000000000, 0.000000000000000000 ) ) ;
#18860=ADVANCED_FACE ( 'NONE', ( #27520 ), #128, .F. ) ;
#18861=CARTESIAN_POINT ( 'NONE',  ( 10.98464796637060026, -23.30469563149855361, 0.5810037832618359932 ) ) ;
#18862=ORIENTED_EDGE ( 'NONE', *, *, #54504, .T. ) ;
#18865=CARTESIAN_POINT ( 'NONE',  ( -1.667916687331000070, -18.70151115557999688, 12.49168451098999988 ) ) ;
#18867=DIRECTION ( 'NONE',  ( 0.000000000000000000, 0.000000000000000000, -1.000000000000000000 ) ) ;
#18871=CARTESIAN_POINT ( 'NONE',  ( 10.41172477448170497, -23.52013115057688353, -7.610718073406644635 ) ) ;
#18881=EDGE_LOOP ( 'NONE', ( #2959, #37735, #7071, #39221 ) ) ;
#18883=CARTESIAN_POINT ( 'NONE',  ( 9.569482281372000188, -76.67852883436000866, -7.743360016082000641 ) ) ;
#18885=B_SPLINE_SURFACE_WITH_KNOTS ( 'NONE', 3, 3, ( 
 ( #12779, #52946, #7495, #17503 ),
 ( #34341, #3639, #31061, #3074 ),
 ( #25784, #38783, #21642, #39649 ),
 ( #21068, #35198, #43810, #57654 ),
 ( #43513, #39933, #39074, #12496 ),
 ( #56801, #49099, #57082, #57949 ),
 ( #21352, #48809, #30775, #3922 ),
 ( #12212, #7784, #13063, #17210 ) ),
 .UNSPECIFIED., .F., .F., .F.,
 ( 4, 1, 1, 1, 1, 4 ),
 ( 4, 4 ),
 ( -0.01200407347463999970, 0.000000000000000000, 0.3333333333333000081, 0.6666666666667000474, 1.000000000000000000, 1.011997855551999947 ),
 ( -0.3559705542741999906, 1.355970554273999928 ),
 .UNSPECIFIED. ) ;
#18886=EDGE_CURVE ( 'NONE', #46616, #51746, #45562, .T. ) ;
#18887=AXIS2_PLACEMENT_3D ( 'NONE', #15073, #51406, #46697 ) ;
#18888=CARTESIAN_POINT ( 'NONE',  ( -1.161914544699476082, -1.947542654857316924, -3.323423654541866945 ) ) ;
#18889=CARTESIAN_POINT ( 'NONE',  ( 12.69619287815999975, -20.24916621771999914, 1.799475295154000065 ) ) ;
#18890=CARTESIAN_POINT ( 'NONE',  ( 9.000511195990998914, -79.32543968971000936, 8.067084866081000172 ) ) ;
#18893=EDGE_CURVE ( 'NONE', #41874, #20606, #29816, .T. ) ;
#18895=CARTESIAN_POINT ( 'NONE',  ( 3.088929962604149093, -2.826175003995697654, -1.008836435391547770 ) ) ;
#18896=CARTESIAN_POINT ( 'NONE',  ( -1.872499823463115165, -77.16255644686364690, -11.87122717985699794 ) ) ;
#18897=CARTESIAN_POINT ( 'NONE',  ( -10.06692933833248027, -18.29657287077820627, 7.655995045172840463 ) ) ;
#18901=CARTESIAN_POINT ( 'NONE',  ( 8.114920487384752690, -24.82884529334158685, 9.847900218102966008 ) ) ;
#18903=CARTESIAN_POINT ( 'NONE',  ( 7.836764916234119305, -24.30511429678713853, 9.850487231000405686 ) ) ;
#18906=CARTESIAN_POINT ( 'NONE',  ( -0.06404916490611077540, -76.07508406693142433, 11.74976712695074177 ) ) ;
#18910=CARTESIAN_POINT ( 'NONE',  ( 7.970415440365194115, -17.47707676838366808, -9.713035532436524733 ) ) ;
#18913=CARTESIAN_POINT ( 'NONE',  ( -6.532344017558930460, -76.27800419209582117, -9.766768203399665893 ) ) ;
#18917=DIRECTION ( 'NONE',  ( -0.7071067811865475727, 0.000000000000000000, 0.7071067811865475727 ) ) ;
#18918=CARTESIAN_POINT ( 'NONE',  ( 9.770419344679000417, -16.94469452567000189, -8.292776877939001423 ) ) ;
#18919=CARTESIAN_POINT ( 'NONE',  ( 8.872949060679459876, -16.98989818440303523, 8.813905828569408740 ) ) ;
#18922=CARTESIAN_POINT ( 'NONE',  ( 12.70395600756419263, -54.19327811274377638, 1.447166682392545312 ) ) ;
#18925=DIRECTION ( 'NONE',  ( -0.7071067811865474617, 0.000000000000000000, 0.7071067811865474617 ) ) ;
#18931=CARTESIAN_POINT ( 'NONE',  ( 10.98364304930883151, -23.23021036681280549, -0.5996544714383750252 ) ) ;
#18932=EDGE_CURVE ( 'NONE', #14174, #245, #55296, .T. ) ;
#18938=VERTEX_POINT ( 'NONE', #17809 ) ;
#18945=EDGE_CURVE ( 'NONE', #13072, #34714, #49657, .T. ) ;
#18946=CARTESIAN_POINT ( 'NONE',  ( 7.943805570375999991, -61.23402324491999593, 9.641149735098998974 ) ) ;
#18947=LINE ( 'NONE', #54669, #27749 ) ;
#18950=CARTESIAN_POINT ( 'NONE',  ( 3.249249792562667771, -1.841632792895788073, -0.4039650473228960648 ) ) ;
#18951=ORIENTED_EDGE ( 'NONE', *, *, #45353, .F. ) ;
#18952=CARTESIAN_POINT ( 'NONE',  ( -8.803747447820532201, -25.21568152340251601, 9.164340453613974091 ) ) ;
#18956=B_SPLINE_CURVE_WITH_KNOTS ( 'NONE', 3,
 ( #2525, #44121, #11389, #11960, #3670, #21670, #47414, #47703, #7526, #43540, #3104, #57112, #16678, #17534, #8381, #27256, #22251, #35525 ),
 .UNSPECIFIED., .F., .F.,
 ( 4, 2, 2, 2, 2, 2, 2, 2, 4 ),
 ( 0.000000000000000000, 0.1250000000000000000, 0.2500000000000000000, 0.3750000000000000000, 0.5000000000000000000, 0.6250000000000000000, 0.7500000000000000000, 0.8750000000000000000, 1.000000000000000000 ),
 .UNSPECIFIED. ) ;
#18959=CARTESIAN_POINT ( 'NONE',  ( -9.466955267137999286, -76.30209268829000280, -8.391502601560000940 ) ) ;
#18963=EDGE_CURVE ( 'NONE', #18159, #14764, #54116, .T. ) ;
#18964=B_SPLINE_CURVE_WITH_KNOTS ( 'NONE', 3,
 ( #19046, #37037, #14018, #55052, #27303, #31129, #35870, #17880, #8720, #44742, #31432, #4293, #22293, #53899, #18465, #9022, #13727, #4596 ),
 .UNSPECIFIED., .F., .F.,
 ( 4, 2, 2, 2, 2, 2, 2, 2, 4 ),
 ( 0.000000000000000000, 0.1250000000000000000, 0.2500000000000000000, 0.3750000000000000000, 0.5000000000000000000, 0.6250000000000000000, 0.7500000000000000000, 0.8750000000000000000, 1.000000000000000000 ),
 .UNSPECIFIED. ) ;
#18966=CARTESIAN_POINT ( 'NONE',  ( -8.950141054446001831, -25.20112627276999717, -8.958565985356999661 ) ) ;
#18967=CARTESIAN_POINT ( 'NONE',  ( -7.353725627630922190, -60.10655143787149512, 8.180687091746444040 ) ) ;
#18969=ORIENTED_EDGE ( 'NONE', *, *, #39304, .F. ) ;
#18975=DIRECTION ( 'NONE',  ( 0.000000000000000000, -1.000000000000000000, 0.000000000000000000 ) ) ;
#18978=CARTESIAN_POINT ( 'NONE',  ( 2.633249659506597951, -2.559142350340922967, 2.439935635806470327 ) ) ;
#18983=CARTESIAN_POINT ( 'NONE',  ( -1.359416874709192810E-05, -0.8285695117701413759, -3.421591653122290300 ) ) ;
#18987=CARTESIAN_POINT ( 'NONE',  ( -1.753528938721999886, -2.394178536415000114, -3.557562347021000271 ) ) ;
#18990=CARTESIAN_POINT ( 'NONE',  ( 7.758897894424999997, -24.30081253449000300, -10.31443085083000000 ) ) ;
#18993=CARTESIAN_POINT ( 'NONE',  ( -8.121706841713852043, -53.96372996666369204, -9.841114038372756667 ) ) ;
#18996=CARTESIAN_POINT ( 'NONE',  ( 10.19019671030999952, -55.60356357307000508, -7.646965722228999951 ) ) ;
#18999=LINE ( 'NONE', #27543, #49370 ) ;
#19004=CARTESIAN_POINT ( 'NONE',  ( 14.00000000000000000, -46.09579702914000165, 0.000000000000000000 ) ) ;
#19006=CARTESIAN_POINT ( 'NONE',  ( 12.52133763467702110, -54.87246868424995938, -1.618901766958426469 ) ) ;
#19007=ORIENTED_EDGE ( 'NONE', *, *, #26588, .T. ) ;
#19012=ORIENTED_EDGE ( 'NONE', *, *, #37486, .T. ) ;
#19013=ORIENTED_EDGE ( 'NONE', *, *, #10942, .F. ) ;
#19015=VECTOR ( 'NONE', #48432, 1000.000000000000000 ) ;
#19016=ORIENTED_EDGE ( 'NONE', *, *, #55500, .F. ) ;
#19017=ORIENTED_EDGE ( 'NONE', *, *, #48303, .F. ) ;
#19019=CARTESIAN_POINT ( 'NONE',  ( 0.5154756746315999338, -16.86759400236999795, 12.66205448072999928 ) ) ;
#19020=CARTESIAN_POINT ( 'NONE',  ( -9.850513605849648968, -54.49492088415082236, -7.836738268828330689 ) ) ;
#19031=DIRECTION ( 'NONE',  ( 0.5721800012453843731, -0.8201280669351780350, 0.000000000000000000 ) ) ;
#19032=CARTESIAN_POINT ( 'NONE',  ( -1.821913034590999348E-14, -80.60000000000000853, -12.05000000000000071 ) ) ;
#19034=CARTESIAN_POINT ( 'NONE',  ( 10.10713367729994872, -61.26653151294045330, 7.860990029212568508 ) ) ;
#19035=CARTESIAN_POINT ( 'NONE',  ( 1.750000000000000000, -60.04999999657000131, -12.50000000000000000 ) ) ;
#19036=CARTESIAN_POINT ( 'NONE',  ( -10.50899237707999845, -77.86882557138000038, 7.577845091584000770 ) ) ;
#19037=EDGE_CURVE ( 'NONE', #18065, #3338, #39265, .T. ) ;
#19039=DIRECTION ( 'NONE',  ( -0.4045602624632933519, 0.8201597332661866302, 0.4045602624632933519 ) ) ;
#19040=CARTESIAN_POINT ( 'NONE',  ( -8.444233576716495548, -76.63875340865895680, 8.172707986422794946 ) ) ;
#19041=B_SPLINE_CURVE_WITH_KNOTS ( 'NONE', 3,
 ( #15438, #37572, #6280, #32543, #45876, #55588 ),
 .UNSPECIFIED., .F., .F.,
 ( 4, 1, 1, 4 ),
 ( 0.000000000000000000, 0.3333333333333000081, 0.6666666666667000474, 1.000000000000000000 ),
 .UNSPECIFIED. ) ;
#19046=CARTESIAN_POINT ( 'NONE',  ( -11.75000000000000000, -76.70000000000000284, 1.487410190129999909E-14 ) ) ;
#19050=CARTESIAN_POINT ( 'NONE',  ( 11.99999999887680957, -79.24999999999998579, 1.256637070374686971 ) ) ;
#19051=EDGE_CURVE ( 'NONE', #3192, #24970, #43998, .T. ) ;
#19052=CARTESIAN_POINT ( 'NONE',  ( -1.209804193477999945, -2.416592054135000112, -3.608664049297999998 ) ) ;
#19055=CARTESIAN_POINT ( 'NONE',  ( -1.840981145238566263, -3.500000000000000888, -2.837856670349830690 ) ) ;
#19056=CARTESIAN_POINT ( 'NONE',  ( 7.401770473313899146, -60.25155696365192171, -8.137215171344832854 ) ) ;
#19057=ADVANCED_FACE ( 'NONE', ( #18396 ), #26353, .F. ) ;
#19060=CIRCLE ( 'NONE', #41677, 0.8000000000000000444 ) ;
#19061=CARTESIAN_POINT ( 'NONE',  ( 9.175280770439000477, -76.64017995137999151, -8.221808909867000636 ) ) ;
#19063=AXIS2_PLACEMENT_3D ( 'NONE', #43757, #57895, #3588 ) ;
#19065=DIRECTION ( 'NONE',  ( 0.000000000000000000, -1.000000000000000000, 0.000000000000000000 ) ) ;
#19069=DIRECTION ( 'NONE',  ( -0.7071067811865473507, 1.433669009702094715E-08, 0.7071067811865473507 ) ) ;
#19072=CARTESIAN_POINT ( 'NONE',  ( 7.764005369688973701, -54.67720632256306601, 9.931049914561711489 ) ) ;
#19076=EDGE_CURVE ( 'NONE', #31846, #42112, #8572, .T. ) ;
#19078=CARTESIAN_POINT ( 'NONE',  ( 3.250000000000000000, -2.750000000000000000, 0.000000000000000000 ) ) ;
#19081=B_SPLINE_CURVE_WITH_KNOTS ( 'NONE', 3,
 ( #14248, #9839, #139, #18115, #4826, #22825, #45572, #54426 ),
 .UNSPECIFIED., .F., .F.,
 ( 4, 2, 2, 4 ),
 ( 0.000000000000000000, 0.5000000000000026645, 0.7500000000000013323, 1.000000000000000000 ),
 .UNSPECIFIED. ) ;
#19085=ORIENTED_EDGE ( 'NONE', *, *, #38896, .F. ) ;
#19086=CARTESIAN_POINT ( 'NONE',  ( 8.130811096204000776, -61.48523690322999613, 9.546858433459998849 ) ) ;
#19087=ORIENTED_EDGE ( 'NONE', *, *, #40886, .T. ) ;
#19089=ORIENTED_EDGE ( 'NONE', *, *, #38573, .F. ) ;
#19093=DIRECTION ( 'NONE',  ( -1.000000000000000000, 0.000000000000000000, 0.000000000000000000 ) ) ;
#19098=CARTESIAN_POINT ( 'NONE',  ( 10.42531124908000173, -60.06485148440999922, 7.624341765471999821 ) ) ;
#19101=EDGE_CURVE ( 'NONE', #25114, #23377, #6491, .T. ) ;
#19102=AXIS2_PLACEMENT_3D ( 'NONE', #35655, #53685, #13523 ) ;
#19103=CARTESIAN_POINT ( 'NONE',  ( 7.626500902235000545, -60.11584477251999203, -10.35747158364999976 ) ) ;
#19105=CARTESIAN_POINT ( 'NONE',  ( 8.326578794153654428, -76.51178312418663552, 8.289917251876268267 ) ) ;
#19108=CARTESIAN_POINT ( 'NONE',  ( 8.485281374238999419, -59.94999999967000548, -8.485281374238999419 ) ) ;
#19110=CARTESIAN_POINT ( 'NONE',  ( -5.869402599192000025, -78.36567021304000491, 10.46661899222999992 ) ) ;
#19113=CARTESIAN_POINT ( 'NONE',  ( -12.72397198033999999, -18.77854962937000138, 1.930909771329999858 ) ) ;
#19116=B_SPLINE_CURVE_WITH_KNOTS ( 'NONE', 3,
 ( #40095, #48397, #13227, #22685, #17084, #35962 ),
 .UNSPECIFIED., .F., .F.,
 ( 4, 1, 1, 4 ),
 ( 0.000000000000000000, 0.3333333333333000081, 0.6666666666667000474, 1.000000000000000000 ),
 .UNSPECIFIED. ) ;
#19120=ADVANCED_FACE ( 'NONE', ( #24855 ), #669, .F. ) ;
#19122=CARTESIAN_POINT ( 'NONE',  ( 9.722718241315000398, -18.55321828668999729, 7.954951288349001004 ) ) ;
#19123=DIRECTION ( 'NONE',  ( -0.7071067811865474617, 0.000000000000000000, 0.7071067811865474617 ) ) ;
#19124=CARTESIAN_POINT ( 'NONE',  ( 12.57434559697999887, -23.71110719500000030, 1.760800161976000089 ) ) ;
#19129=CARTESIAN_POINT ( 'NONE',  ( -11.60215227398000160, -76.73358059650999508, 3.298237476086999909 ) ) ;
#19130=ORIENTED_EDGE ( 'NONE', *, *, #50184, .T. ) ;
#19133=CARTESIAN_POINT ( 'NONE',  ( -7.655983890242670675, -18.29663439995314178, -10.06694524887581288 ) ) ;
#19136=CARTESIAN_POINT ( 'NONE',  ( 12.77649734579999929, -53.49171487479999598, 0.06478328530388999251 ) ) ;
#19138=AXIS2_PLACEMENT_3D ( 'NONE', #33552, #51591, #57378 ) ;
#19139=CARTESIAN_POINT ( 'NONE',  ( -3.282842942682000054, -1.838913946619999962, -1.459606374259000194 ) ) ;
#19143=ORIENTED_EDGE ( 'NONE', *, *, #53135, .T. ) ;
#19145=CARTESIAN_POINT ( 'NONE',  ( 1.718598680027600523, -54.55037066937039469, -12.71111582765235148 ) ) ;
#19147=FACE_OUTER_BOUND ( 'NONE', #42500, .T. ) ;
#19149=CARTESIAN_POINT ( 'NONE',  ( 12.50000000000000000, -60.04999999725999515, -1.750000000000000000 ) ) ;
#19150=ORIENTED_EDGE ( 'NONE', *, *, #46483, .T. ) ;
#19153=CARTESIAN_POINT ( 'NONE',  ( -1.667917367065999912, -18.71943464842000182, 12.49306764015999960 ) ) ;
#19154=ORIENTED_EDGE ( 'NONE', *, *, #1578, .F. ) ;
#19156=VERTEX_POINT ( 'NONE', #48744 ) ;
#19159=AXIS2_PLACEMENT_3D ( 'NONE', #47410, #7229, #46537 ) ;
#19165=ORIENTED_EDGE ( 'NONE', *, *, #23876, .F. ) ;
#19168=DIRECTION ( 'NONE',  ( -1.000000000000000000, 0.000000000000000000, 0.000000000000000000 ) ) ;
#19176=ORIENTED_EDGE ( 'NONE', *, *, #9229, .T. ) ;
#19178=CARTESIAN_POINT ( 'NONE',  ( 7.568503529865000523, -76.30497314281001309, 9.708412483427999007 ) ) ;
#19179=AXIS2_PLACEMENT_3D ( 'NONE', #13660, #31655, #39937 ) ;
#19180=CARTESIAN_POINT ( 'NONE',  ( -1.647983664004335713, -2.263003773417186171, 3.111148793556432146 ) ) ;
#19181=DIRECTION ( 'NONE',  ( -1.000000000000000000, 0.000000000000000000, 0.000000000000000000 ) ) ;
#19182=CARTESIAN_POINT ( 'NONE',  ( 12.16303714866999997, -79.27753849292000154, 1.568404430622000190 ) ) ;
#19185=CARTESIAN_POINT ( 'NONE',  ( 2.620693402520182236, -2.799838841147761936, -1.925851656741417228 ) ) ;
#19186=CARTESIAN_POINT ( 'NONE',  ( -4.143196849663613790, -77.64733255783154675, -11.57321364922782969 ) ) ;
#19187=CARTESIAN_POINT ( 'NONE',  ( -9.723199429427999974, -17.52306056076000118, 7.958735708429999889 ) ) ;
#19188=TOROIDAL_SURFACE ( 'NONE', #13520, 26.50000000000000000, 14.00000000000000000 ) ;
#19189=B_SPLINE_SURFACE_WITH_KNOTS ( 'NONE', 3, 3, ( 
 ( #38749, #11896, #16035, #48214 ),
 ( #38167, #11613, #47643, #33735 ),
 ( #2748, #25749, #34019, #51773 ),
 ( #26028, #52056, #43772, #20750 ),
 ( #30457, #15738, #57336, #6878 ),
 ( #52340, #38461, #39328, #34597 ),
 ( #11322, #29301, #29874, #47350 ),
 ( #25172, #7461, #56478, #24888 ) ),
 .UNSPECIFIED., .F., .F., .F.,
 ( 4, 1, 1, 1, 1, 4 ),
 ( 4, 4 ),
 ( -0.01200407345747999885, 0.000000000000000000, 0.3333333333333000081, 0.6666666666667000474, 1.000000000000000000, 1.011997855551999947 ),
 ( -0.3559705542741000150, 1.355970554273999928 ),
 .UNSPECIFIED. ) ;
#19194=CARTESIAN_POINT ( 'NONE',  ( 8.792818914773597783, -25.22696626442860790, 9.175540344814811178 ) ) ;
#19196=CARTESIAN_POINT ( 'NONE',  ( -2.640046357426999890, -2.819378508794999849, 2.612394753782000034 ) ) ;
#19197=CIRCLE ( 'NONE', #2231, 14.00000000000000000 ) ;
#19200=CARTESIAN_POINT ( 'NONE',  ( 0.09944289326072909552, -76.07403084298707086, 11.74944078188181429 ) ) ;
#19203=ORIENTED_EDGE ( 'NONE', *, *, #17570, .T. ) ;
#19204=AXIS2_PLACEMENT_3D ( 'NONE', #46096, #41646, #41358 ) ;
#19206=CARTESIAN_POINT ( 'NONE',  ( 10.83169831117340642, -79.04172495591551240, -4.820018971670366525 ) ) ;
#19207=CARTESIAN_POINT ( 'NONE',  ( -1.276771495430000038E-14, -69.50420297070000686, 0.000000000000000000 ) ) ;
#19210=DIRECTION ( 'NONE',  ( 0.7071067811865474617, 0.000000000000000000, 0.7071067811865474617 ) ) ;
#19211=CARTESIAN_POINT ( 'NONE',  ( 9.310166272083998606, -16.86468533975999762, -8.596757084891999412 ) ) ;
#19215=CARTESIAN_POINT ( 'NONE',  ( 12.70455814335207378, -17.43992875976934798, 1.489882837238664770 ) ) ;
#19218=CARTESIAN_POINT ( 'NONE',  ( -2.383965290753023769, -77.84388370242140809, 11.78518095179793512 ) ) ;
#19220=DIRECTION ( 'NONE',  ( 0.000000000000000000, 0.000000000000000000, -1.000000000000000000 ) ) ;
#19221=CARTESIAN_POINT ( 'NONE',  ( 3.665025684363000025, -3.476287900391999752, -1.025097465345000236 ) ) ;
#19227=DIRECTION ( 'NONE',  ( 0.000000000000000000, 1.000000000000000000, 0.000000000000000000 ) ) ;
#19229=VERTEX_POINT ( 'NONE', #24129 ) ;
#19232=ORIENTED_EDGE ( 'NONE', *, *, #54587, .T. ) ;
#19236=CARTESIAN_POINT ( 'NONE',  ( 7.631889049370999878, -60.02121504819000108, 10.36222434951000082 ) ) ;
#19237=DIRECTION ( 'NONE',  ( 1.000000000000000000, 0.000000000000000000, 0.000000000000000000 ) ) ;
#19241=DIRECTION ( 'NONE',  ( 0.9999999930530777403, 0.000000000000000000, 0.0001178721535675973718 ) ) ;
#19243=EDGE_CURVE ( 'NONE', #11038, #43183, #7255, .T. ) ;
#19246=DIRECTION ( 'NONE',  ( 0.000000000000000000, 1.000000000000000000, 0.000000000000000000 ) ) ;
#19248=CARTESIAN_POINT ( 'NONE',  ( -8.251806177691921818, -17.19944067082638739, 9.431051272834954702 ) ) ;
#19254=CARTESIAN_POINT ( 'NONE',  ( -8.188293269161999177, -24.70494400568999893, -9.395718629078000816 ) ) ;
#19255=CIRCLE ( 'NONE', #52255, 1.750000000000001332 ) ;
#19256=CARTESIAN_POINT ( 'NONE',  ( 12.92177931909999877, -57.04263462147999775, -2.062503053667999797 ) ) ;
#19259=ORIENTED_EDGE ( 'NONE', *, *, #39730, .T. ) ;
#19264=EDGE_CURVE ( 'NONE', #44340, #26124, #48719, .T. ) ;
#19266=CARTESIAN_POINT ( 'NONE',  ( -9.783235115942000348, -17.46434390394999880, 7.961033122320000821 ) ) ;
#19267=DIRECTION ( 'NONE',  ( 1.000000000000000000, 0.000000000000000000, 0.000000000000000000 ) ) ;
#19268=CARTESIAN_POINT ( 'NONE',  ( 1.007525990681730432, -3.101944840528865655, 3.373179531834999079 ) ) ;
#19278=DIRECTION ( 'NONE',  ( -0.9999999999995751176, 0.000000000000000000, -9.217549100139771309E-07 ) ) ;
#19281=CARTESIAN_POINT ( 'NONE',  ( 9.317978910659999059, -25.13238463018999980, -8.588869595444998950 ) ) ;
#19283=AXIS2_PLACEMENT_3D ( 'NONE', #29600, #20190, #20759 ) ;
#19287=EDGE_CURVE ( 'NONE', #13102, #15626, #28450, .T. ) ;
#19289=CARTESIAN_POINT ( 'NONE',  ( 10.00831378476999944, -55.42769332259999260, -7.646786280026000249 ) ) ;
#19290=CARTESIAN_POINT ( 'NONE',  ( 0.000000000000000000, -13.07071424677999971, 0.000000000000000000 ) ) ;
#19295=CARTESIAN_POINT ( 'NONE',  ( -12.43640309388999832, -61.71747517570000241, -0.05224034426411999776 ) ) ;
#19300=ORIENTED_EDGE ( 'NONE', *, *, #2135, .T. ) ;
#19301=EDGE_CURVE ( 'NONE', #18636, #425, #8206, .T. ) ;
#19302=CARTESIAN_POINT ( 'NONE',  ( 13.95956770371999944, -45.71924237694000226, 5.182383547123999630E-05 ) ) ;
#19305=AXIS2_PLACEMENT_3D ( 'NONE', #29192, #10926, #28906 ) ;
#19308=VERTEX_POINT ( 'NONE', #2696 ) ;
#19316=AXIS2_PLACEMENT_3D ( 'NONE', #31101, #49442, #45604 ) ;
#19324=DIRECTION ( 'NONE',  ( 0.6489586447325770280, -0.04890182339238829945, 0.7592504784955730335 ) ) ;
#19326=CARTESIAN_POINT ( 'NONE',  ( -7.601397897754999633, -60.04999999657000131, -10.07627163191000008 ) ) ;
#19327=CIRCLE ( 'NONE', #54714, 12.05000000000000071 ) ;
#19328=CARTESIAN_POINT ( 'NONE',  ( -10.42274798266999980, -20.24634220924000161, 7.691916945430000041 ) ) ;
#19331=DIRECTION ( 'NONE',  ( 0.7071067811865475727, 0.000000000000000000, 0.7071067811865475727 ) ) ;
#19337=FACE_OUTER_BOUND ( 'NONE', #5214, .T. ) ;
#19340=CARTESIAN_POINT ( 'NONE',  ( -1.750000000001000089, -23.25000000990999993, -12.56594317857000043 ) ) ;
#19341=CARTESIAN_POINT ( 'NONE',  ( 2.234646451474000095, -2.642397890054000165, 3.080979982494000069 ) ) ;
#19343=B_SPLINE_CURVE_WITH_KNOTS ( 'NONE', 3,
 ( #49072, #26329, #13628, #49668, #35467, #48785 ),
 .UNSPECIFIED., .F., .F.,
 ( 4, 1, 1, 4 ),
 ( 0.000000000000000000, 0.3333333333333000081, 0.6666666666667000474, 1.000000000000000000 ),
 .UNSPECIFIED. ) ;
#19345=CARTESIAN_POINT ( 'NONE',  ( -2.460865576472458738, -3.500000000000000000, -2.303415178628417603 ) ) ;
#19346=CARTESIAN_POINT ( 'NONE',  ( 7.353725627631179762, -60.10655143787244015, -8.180687091746213113 ) ) ;
#19347=CARTESIAN_POINT ( 'NONE',  ( 3.250000000000000000, -2.850000000000000089, 0.000000000000000000 ) ) ;
#19348=CIRCLE ( 'NONE', #43838, 3.600000000000000089 ) ;
#19349=CARTESIAN_POINT ( 'NONE',  ( 1.931043742978000077, -59.57795407677000554, 12.75763395697999947 ) ) ;
#19350=CARTESIAN_POINT ( 'NONE',  ( -12.66315144082999922, -53.62197088156000291, -0.06064144874946000158 ) ) ;
#19352=EDGE_CURVE ( 'NONE', #53710, #7256, #23740, .T. ) ;
#19354=DIRECTION ( 'NONE',  ( 0.7071067811865474617, 3.445410891336226740E-11, 0.7071067811865474617 ) ) ;
#19357=CARTESIAN_POINT ( 'NONE',  ( 0.000000000000000000, -0.2000000000000005107, -13.99999999999696954 ) ) ;
#19358=CARTESIAN_POINT ( 'NONE',  ( 12.00000000000000000, -18.75000000000000000, 1.750000000000000000 ) ) ;
#19359=FACE_OUTER_BOUND ( 'NONE', #45155, .T. ) ;
#19361=CARTESIAN_POINT ( 'NONE',  ( -3.858199361241999803, -0.8744335234539000190, -1.117275487237999965 ) ) ;
#19368=VERTEX_POINT ( 'NONE', #45619 ) ;
#19371=CARTESIAN_POINT ( 'NONE',  ( -12.50657368826013993, -61.77245458960371138, -0.3553454088953992285 ) ) ;
#19377=ORIENTED_EDGE ( 'NONE', *, *, #19287, .F. ) ;
#19379=ORIENTED_EDGE ( 'NONE', *, *, #56141, .F. ) ;
#19383=CIRCLE ( 'NONE', #10922, 5.000000000000000888 ) ;
#19386=CARTESIAN_POINT ( 'NONE',  ( -7.705142895592000052, -58.55083378327000077, 10.24998526315000014 ) ) ;
#19394=DIRECTION ( 'NONE',  ( 0.000000000000000000, 0.000000000000000000, -1.000000000000000000 ) ) ;
#19395=CARTESIAN_POINT ( 'NONE',  ( -7.705142895613999343, -57.04916621739000249, -10.24998526317999925 ) ) ;
#19397=CARTESIAN_POINT ( 'NONE',  ( 8.344849100831723376, -76.51161235786649684, 8.271546587476944268 ) ) ;
#19398=CARTESIAN_POINT ( 'NONE',  ( 0.5812841321855933829, -23.30416868477314551, -10.98463311464191250 ) ) ;
#19407=LINE ( 'NONE', #55416, #21938 ) ;
#19410=DIRECTION ( 'NONE',  ( 0.7071067811865475727, 0.000000000000000000, -0.7071067811865475727 ) ) ;
#19411=CARTESIAN_POINT ( 'NONE',  ( -0.4865042478690436711, -3.500000000000000888, 3.248882910818546410 ) ) ;
#19412=FACE_OUTER_BOUND ( 'NONE', #57993, .T. ) ;
#19413=CARTESIAN_POINT ( 'NONE',  ( -1.477284502223000118, -24.72631500296999718, -12.77254812468999923 ) ) ;
#19414=CARTESIAN_POINT ( 'NONE',  ( 12.51072239526000196, -26.30294702885999669, 0.7871079366006996647 ) ) ;
#19416=CARTESIAN_POINT ( 'NONE',  ( -7.610716808838798642, -23.52015489479942190, -10.41172350877303820 ) ) ;
#19419=CARTESIAN_POINT ( 'NONE',  ( 7.686918321190000292, -21.75560170997999876, 10.48771805380000011 ) ) ;
#19421=CARTESIAN_POINT ( 'NONE',  ( -3.997988644197999708, -76.15750634111999773, 11.37999976687000014 ) ) ;
#19423=B_SPLINE_SURFACE_WITH_KNOTS ( 'NONE', 3, 3, ( 
 ( #57808, #58103, #17665, #48962 ),
 ( #34784, #34493, #52239, #12079 ),
 ( #29771, #26500, #30061, #21791 ),
 ( #17368, #30924, #47827, #35354 ),
 ( #7930, #16800, #7643, #7358 ),
 ( #43372, #53380, #12361, #12927 ),
 ( #43668, #2931, #3505, #45417 ),
 ( #35345, #58094, #9392, #13801 ) ),
 .UNSPECIFIED., .F., .F., .F.,
 ( 4, 1, 1, 1, 1, 4 ),
 ( 4, 4 ),
 ( -0.01200407345748999953, 0.000000000000000000, 0.3333333333333000081, 0.6666666666667000474, 1.000000000000000000, 1.011997855551999947 ),
 ( -0.3559705542741999906, 1.355970554273999928 ),
 .UNSPECIFIED. ) ;
#19428=CARTESIAN_POINT ( 'NONE',  ( 10.18249594442404415, -54.50907903244432617, 7.792385963361820878 ) ) ;
#19433=DIRECTION ( 'NONE',  ( 0.000000000000000000, 1.000000000000000000, 0.000000000000000000 ) ) ;
#19434=CARTESIAN_POINT ( 'NONE',  ( -1.667916687331000070, -55.50151115525000023, 12.49168451095999899 ) ) ;
#19435=ORIENTED_EDGE ( 'NONE', *, *, #13028, .F. ) ;
#19437=CARTESIAN_POINT ( 'NONE',  ( -0.5999999999999999778, -18.84999999999999787, -10.98362417419999915 ) ) ;
#19438=CARTESIAN_POINT ( 'NONE',  ( -2.099388381696000023E-14, -0.04999999937965000224, 0.000000000000000000 ) ) ;
#19439=VECTOR ( 'NONE', #15658, 1000.000000000000000 ) ;
#19440=ORIENTED_EDGE ( 'NONE', *, *, #23707, .T. ) ;
#19441=ADVANCED_FACE ( 'NONE', ( #12404 ), #16841, .T. ) ;
#19445=ORIENTED_EDGE ( 'NONE', *, *, #3397, .T. ) ;
#19447=CARTESIAN_POINT ( 'NONE',  ( 10.20678250203529025, -61.03575784435037122, -7.770339463558867621 ) ) ;
#19448=VERTEX_POINT ( 'NONE', #21550 ) ;
#19449=ORIENTED_EDGE ( 'NONE', *, *, #39082, .F. ) ;
#19450=CARTESIAN_POINT ( 'NONE',  ( -10.01676960210999923, -55.59061945207999855, -7.658895148190000057 ) ) ;
#19454=CARTESIAN_POINT ( 'NONE',  ( 12.72394144133999916, -55.57839271467000231, 1.930881231431999856 ) ) ;
#19455=CARTESIAN_POINT ( 'NONE',  ( 10.25201842917796924, -24.12180395215443696, -7.730408553586223697 ) ) ;
#19456=ORIENTED_EDGE ( 'NONE', *, *, #24089, .F. ) ;
#19457=CARTESIAN_POINT ( 'NONE',  ( -12.54673765596000123, -24.82199238237999950, -0.9174244429638999110 ) ) ;
#19459=CARTESIAN_POINT ( 'NONE',  ( -0.5222397221475469919, -16.83701780599070474, -12.70447686583903923 ) ) ;
#19461=CARTESIAN_POINT ( 'NONE',  ( -12.76303204294000082, -18.73514849292999784, -1.980584515756000030 ) ) ;
#19465=CARTESIAN_POINT ( 'NONE',  ( -3.438348731682000281, -76.61980657813998619, -11.82003900998999946 ) ) ;
#19468=CARTESIAN_POINT ( 'NONE',  ( 3.065643863220296694, -2.058380345162022618, -1.728768913878805602 ) ) ;
#19469=CARTESIAN_POINT ( 'NONE',  ( 7.986976573832000881, -61.52634345601000376, -10.07613380459999952 ) ) ;
#19470=CARTESIAN_POINT ( 'NONE',  ( 12.21456857099000004, -78.72553890088001083, -1.096995930408000142 ) ) ;
#19473=CONICAL_SURFACE ( 'NONE', #10973, 8.749999999256001360, 0.7853981633972997312 ) ;
#19475=CARTESIAN_POINT ( 'NONE',  ( -7.839627085707410181, -77.98089410207293781, 9.247057760909966007 ) ) ;
#19480=CARTESIAN_POINT ( 'NONE',  ( 12.50000000000000000, -55.54999999966999980, -1.250000000000000000 ) ) ;
#19482=CARTESIAN_POINT ( 'NONE',  ( -2.751186307780999929, -2.732297659067000062, 2.722370634480000273 ) ) ;
#19485=CARTESIAN_POINT ( 'NONE',  ( -10.64136828584240391, -76.16485984116189911, 4.983422431193929469 ) ) ;
#19489=ORIENTED_EDGE ( 'NONE', *, *, #8311, .F. ) ;
#19490=CARTESIAN_POINT ( 'NONE',  ( -9.000000000000000000, -0.5000000000000000000, 0.000000000000000000 ) ) ;
#19491=CARTESIAN_POINT ( 'NONE',  ( 0.000000000000000000, -80.70000000000000284, 0.000000000000000000 ) ) ;
#19496=CARTESIAN_POINT ( 'NONE',  ( 10.01676221091000052, -18.79058563473000021, -7.658899961851000526 ) ) ;
#19497=CARTESIAN_POINT ( 'NONE',  ( 7.958763980604000032, -17.52301961031999866, 9.723170659100999202 ) ) ;
#19503=CARTESIAN_POINT ( 'NONE',  ( -9.236974595845435232, -77.51476500836666617, -9.065058572735408049 ) ) ;
#19504=ADVANCED_FACE ( 'NONE', ( #14434 ), #54425, .F. ) ;
#19510=CARTESIAN_POINT ( 'NONE',  ( 10.98768939184196647, -23.45050660130683795, -0.5207199486368357944 ) ) ;
#19511=VECTOR ( 'NONE', #1761, 1000.000000000000000 ) ;
#19516=ORIENTED_EDGE ( 'NONE', *, *, #19661, .F. ) ;
#19517=EDGE_CURVE ( 'NONE', #37628, #42913, #40245, .T. ) ;
#19523=VERTEX_POINT ( 'NONE', #38044 ) ;
#19526=CARTESIAN_POINT ( 'NONE',  ( 10.31444895690999886, -61.10075144983999706, 7.758883253367000243 ) ) ;
#19527=CARTESIAN_POINT ( 'NONE',  ( 0.5999999999999999778, -18.84999999999000053, 11.79999999999999893 ) ) ;
#19532=VERTEX_POINT ( 'NONE', #33316 ) ;
#19537=CARTESIAN_POINT ( 'NONE',  ( -10.12290050256999940, -18.75000002239000096, -7.648026768411000376 ) ) ;
#19538=CARTESIAN_POINT ( 'NONE',  ( 10.35453599130000057, -76.65783510652001098, -6.064947188958000446 ) ) ;
#19541=CARTESIAN_POINT ( 'NONE',  ( -8.220407391935999897, -24.81950084232000364, -9.523310056109000499 ) ) ;
#19542=CARTESIAN_POINT ( 'NONE',  ( 12.87022657272000004, -56.01514526721999943, -2.062597299672999540 ) ) ;
#19549=CARTESIAN_POINT ( 'NONE',  ( -7.645391692608000334, -18.78469634161999835, 10.18949678827999961 ) ) ;
#19550=EDGE_CURVE ( 'NONE', #35953, #44782, #33246, .T. ) ;
#19552=CARTESIAN_POINT ( 'NONE',  ( 3.498582912420285407, -3.490953291830131811, -0.3978866406648630116 ) ) ;
#19558=DIRECTION ( 'NONE',  ( 0.9999548435846228323, 0.000000000000000000, 0.009503199022040218977 ) ) ;
#19559=ORIENTED_EDGE ( 'NONE', *, *, #34746, .F. ) ;
#19561=CARTESIAN_POINT ( 'NONE',  ( -0.8445585116414000559, -61.51040443210000319, -12.43380736240999873 ) ) ;
#19563=CARTESIAN_POINT ( 'NONE',  ( -7.889735440111223852, -55.04957415510977370, 7.666647577131773694 ) ) ;
#19567=CARTESIAN_POINT ( 'NONE',  ( 7.948089776770999926, -24.44033979720000360, -9.636757666087000018 ) ) ;
#19569=DIRECTION ( 'NONE',  ( 0.000000000000000000, -0.7071067811866525998, -0.7071067811864425456 ) ) ;
#19570=CARTESIAN_POINT ( 'NONE',  ( -7.624341764906000130, -55.53514850498000044, -10.42531124851000079 ) ) ;
#19573=CARTESIAN_POINT ( 'NONE',  ( 7.969034948567999876, -54.17623147781999648, -9.934750886883000121 ) ) ;
#19575=EDGE_CURVE ( 'NONE', #27322, #13927, #15768, .T. ) ;
#19583=CARTESIAN_POINT ( 'NONE',  ( -8.792808668394924254, -53.57303577587560994, 9.175550543417134719 ) ) ;
#19584=ORIENTED_EDGE ( 'NONE', *, *, #49441, .F. ) ;
#19589=ORIENTED_EDGE ( 'NONE', *, *, #44608, .T. ) ;
#19590=EDGE_CURVE ( 'NONE', #8688, #56557, #20494, .T. ) ;
#19591=ORIENTED_EDGE ( 'NONE', *, *, #37223, .T. ) ;
#19596=CARTESIAN_POINT ( 'NONE',  ( 1.667269374596999976, -18.79060116514999734, 12.49858097730999873 ) ) ;
#19605=EDGE_LOOP ( 'NONE', ( #58132, #19232, #7887, #25382 ) ) ;
#19607=CARTESIAN_POINT ( 'NONE',  ( -12.72923908218061406, -23.77554307156079005, 1.930512971251469478 ) ) ;
#19613=CARTESIAN_POINT ( 'NONE',  ( 0.000000000000000000, 4.040000000000000036, 0.000000000000000000 ) ) ;
#19619=CARTESIAN_POINT ( 'NONE',  ( -10.01749678874999994, -55.60819056964000140, 7.660430392551000445 ) ) ;
#19621=CARTESIAN_POINT ( 'NONE',  ( -1.250000000000000000, -55.54999999966999980, 12.00000000000000000 ) ) ;
#19622=CARTESIAN_POINT ( 'NONE',  ( 1.667936688463999895, -22.76486430425999785, -12.53239398059000109 ) ) ;
#19623=EDGE_CURVE ( 'NONE', #35254, #43036, #31140, .T. ) ;
#19624=DIRECTION ( 'NONE',  ( 0.000000000000000000, -1.000000000000000000, 0.000000000000000000 ) ) ;
#19625=CARTESIAN_POINT ( 'NONE',  ( 1.194090705999000024, -17.55968341096999552, -12.43436538489999954 ) ) ;
#19626=CARTESIAN_POINT ( 'NONE',  ( 0.000000000000000000, -2.660000000000000142, 0.000000000000000000 ) ) ;
#19627=CARTESIAN_POINT ( 'NONE',  ( -10.42531124905999995, -18.73514851523999880, 7.624341765453999997 ) ) ;
#19628=CARTESIAN_POINT ( 'NONE',  ( 2.234646451474000095, -2.677064556719999988, 3.080979982494000069 ) ) ;
#19630=EDGE_CURVE ( 'NONE', #33033, #25961, #40661, .T. ) ;
#19632=CARTESIAN_POINT ( 'NONE',  ( -2.925837195856660244, -3.499999999999999556, -1.558917296219500592 ) ) ;
#19633=CARTESIAN_POINT ( 'NONE',  ( 0.3116081092048096912, -18.31315380225280975, -10.99615594221662640 ) ) ;
#19637=CARTESIAN_POINT ( 'NONE',  ( 1.750000000001000089, -22.75100836360999779, -12.60354432389999957 ) ) ;
#19638=CARTESIAN_POINT ( 'NONE',  ( 0.000000000000000000, -0.09999999858569999511, 0.000000000000000000 ) ) ;
#19639=CARTESIAN_POINT ( 'NONE',  ( 1.750000000000000000, -23.24999999688999708, -12.50000000000000000 ) ) ;
#19648=CARTESIAN_POINT ( 'NONE',  ( -0.4617212151683000032, -1.236168933658999824, 3.989551193614000013 ) ) ;
#19654=AXIS2_PLACEMENT_3D ( 'NONE', #38705, #33690, #15988 ) ;
#19656=EDGE_LOOP ( 'NONE', ( #7026, #27351, #32308, #46416 ) ) ;
#19659=CARTESIAN_POINT ( 'NONE',  ( 7.634645345497309776, -18.52415927528287654, 10.10912681051257778 ) ) ;
#19661=EDGE_CURVE ( 'NONE', #2249, #10966, #7846, .T. ) ;
#19663=EDGE_CURVE ( 'NONE', #44855, #32127, #4940, .T. ) ;
#19664=EDGE_LOOP ( 'NONE', ( #52136, #31171, #10888 ) ) ;
#19665=ORIENTED_EDGE ( 'NONE', *, *, #55500, .T. ) ;
#19667=ORIENTED_EDGE ( 'NONE', *, *, #8464, .F. ) ;
#19670=EDGE_LOOP ( 'NONE', ( #16818, #19445, #19972 ) ) ;
#19671=CARTESIAN_POINT ( 'NONE',  ( -7.601397897754999633, -55.54999999966999980, 9.369164850722000892 ) ) ;
#19672=CARTESIAN_POINT ( 'NONE',  ( -7.691916945401000127, -58.55365779174999830, 10.42274798264000069 ) ) ;
#19677=CARTESIAN_POINT ( 'NONE',  ( -7.919595949288999570, -55.65000000488999632, -8.768124086549999419 ) ) ;
#19678=CARTESIAN_POINT ( 'NONE',  ( 0.002996482912751207480, -0.9843749999025924735, 3.305856831758737790 ) ) ;
#19679=AXIS2_PLACEMENT_3D ( 'NONE', #12347, #30334, #47810 ) ;
#19680=EDGE_CURVE ( 'NONE', #1025, #6714, #24057, .T. ) ;
#19683=CARTESIAN_POINT ( 'NONE',  ( -3.075537641221584018, -77.19583333333332575, 11.44417895085269876 ) ) ;
#19684=EDGE_CURVE ( 'NONE', #40274, #1677, #4652, .T. ) ;
#19685=FACE_OUTER_BOUND ( 'NONE', #55317, .T. ) ;
#19687=CARTESIAN_POINT ( 'NONE',  ( 3.011810901700481935, -76.55381572931285916, 11.35858098727523569 ) ) ;
#19688=CARTESIAN_POINT ( 'NONE',  ( -0.3116081092089518778, -23.68684619774715117, -10.99615594221646475 ) ) ;
#19692=CARTESIAN_POINT ( 'NONE',  ( -3.007576031741168610, -3.070405536610469888, 1.229591291355605298 ) ) ;
#19698=DIRECTION ( 'NONE',  ( 0.000000000000000000, 1.000000000000000000, 0.000000000000000000 ) ) ;
#19699=CARTESIAN_POINT ( 'NONE',  ( -8.315421822073089331, -76.26185017328086246, -8.301069858640518717 ) ) ;
#19701=EDGE_CURVE ( 'NONE', #38648, #19229, #831, .T. ) ;
#19702=CARTESIAN_POINT ( 'NONE',  ( -10.00831380746999955, -60.17230364551999600, -7.646786653150000390 ) ) ;
#19703=DIRECTION ( 'NONE',  ( -1.000000000000000000, 0.000000000000000000, 0.000000000000000000 ) ) ;
#19704=CARTESIAN_POINT ( 'NONE',  ( 10.04116292117000064, -59.56462890159999546, 7.682344222584999827 ) ) ;
#19707=CARTESIAN_POINT ( 'NONE',  ( -9.073558136264555429, -25.22808769493118319, -8.894842552359547128 ) ) ;
#19708=CARTESIAN_POINT ( 'NONE',  ( 1.750000000000000000, -18.75000000240999753, -12.50000000000000000 ) ) ;
#19712=CARTESIAN_POINT ( 'NONE',  ( -9.761040558467000139, -76.80558987842999841, -7.085928052393999366 ) ) ;
#19719=CARTESIAN_POINT ( 'NONE',  ( 12.66316452100000056, -61.97866137636000161, -0.04044945982128999445 ) ) ;
#19721=CARTESIAN_POINT ( 'NONE',  ( 8.485281374238999419, -18.75000000000000000, -8.485281374238999419 ) ) ;
#19726=ORIENTED_EDGE ( 'NONE', *, *, #11880, .T. ) ;
#19727=CARTESIAN_POINT ( 'NONE',  ( -12.50000000000000000, -55.54999999966999980, -1.250000000000000000 ) ) ;
#19729=VECTOR ( 'NONE', #31365, 1000.000000000000000 ) ;
#19731=ORIENTED_EDGE ( 'NONE', *, *, #37152, .T. ) ;
#19736=ORIENTED_EDGE ( 'NONE', *, *, #48653, .F. ) ;
#19739=CARTESIAN_POINT ( 'NONE',  ( -10.98521615365918080, -23.34051012009600612, -0.5703160980903254629 ) ) ;
#19740=EDGE_LOOP ( 'NONE', ( #14393, #52282, #2260, #49443, #47217, #32045, #13542, #37360, #34909 ) ) ;
#19741=ORIENTED_EDGE ( 'NONE', *, *, #36346, .T. ) ;
#19742=VECTOR ( 'NONE', #4578, 1000.000000000000000 ) ;
#19743=B_SPLINE_CURVE_WITH_KNOTS ( 'NONE', 3,
 ( #28187, #22908, #50372, #22616, #40920, #10208 ),
 .UNSPECIFIED., .F., .F.,
 ( 4, 2, 4 ),
 ( 0.000000000000000000, 0.5000000000000000000, 1.000000000000000000 ),
 .UNSPECIFIED. ) ;
#19747=ORIENTED_EDGE ( 'NONE', *, *, #43046, .F. ) ;
#19748=FACE_OUTER_BOUND ( 'NONE', #14607, .T. ) ;
#19750=EDGE_LOOP ( 'NONE', ( #21637, #18491, #46111, #21120 ) ) ;
#19751=CARTESIAN_POINT ( 'NONE',  ( -12.43646124688000043, -24.91751819622000141, 0.05236837568998999742 ) ) ;
#19753=EDGE_CURVE ( 'NONE', #8616, #20811, #28945, .T. ) ;
#19760=CARTESIAN_POINT ( 'NONE',  ( -9.662446363796000526, -76.42949170666001635, 7.627099640079999965 ) ) ;
#19762=CARTESIAN_POINT ( 'NONE',  ( -3.272648110252596165, -1.879334845439307067, -1.300867599518198858 ) ) ;
#19763=CONICAL_SURFACE ( 'NONE', #12214, 0.6999999997695030007, 0.7853981633972997312 ) ;
#19764=CARTESIAN_POINT ( 'NONE',  ( 10.47840054248000108, -60.58693148419000352, -7.622763498592000531 ) ) ;
#19765=CARTESIAN_POINT ( 'NONE',  ( -9.356096982537000173, -78.89205726075000769, 7.928589704419000128 ) ) ;
#19767=CARTESIAN_POINT ( 'NONE',  ( 12.70249541838869156, -17.03496187198601319, -0.9988462570604047519 ) ) ;
#19768=EDGE_CURVE ( 'NONE', #31323, #31846, #12915, .T. ) ;
#19769=CARTESIAN_POINT ( 'NONE',  ( 2.141122524434464047, -2.783241521950269526, -2.454054550522687617 ) ) ;
#19770=CARTESIAN_POINT ( 'NONE',  ( -2.676544870374850227, -77.44274814402791662, 11.77617227856609716 ) ) ;
#19772=ORIENTED_EDGE ( 'NONE', *, *, #22178, .T. ) ;
#19775=CARTESIAN_POINT ( 'NONE',  ( 9.433548213854539455, -25.12797454612102754, 8.532643227186095913 ) ) ;
#19776=AXIS2_PLACEMENT_3D ( 'NONE', #10143, #11310, #34298 ) ;
#19778=CARTESIAN_POINT ( 'NONE',  ( 3.699199734595000066, -3.138587262671999945, 0.3322231105728999934 ) ) ;
#19779=CIRCLE ( 'NONE', #13178, 0.6000000000000008660 ) ;
#19782=EDGE_CURVE ( 'NONE', #51555, #31846, #18418, .T. ) ;
#19783=CARTESIAN_POINT ( 'NONE',  ( -10.04720586219557177, -76.15599413331796086, 6.103539320034618854 ) ) ;
#19788=CARTESIAN_POINT ( 'NONE',  ( 12.76303204522000101, -23.26485147686999966, 1.980584515753000208 ) ) ;
#19789=EDGE_CURVE ( 'NONE', #8017, #4894, #13491, .T. ) ;
#19790=CARTESIAN_POINT ( 'NONE',  ( -1.980584515756000030, -60.06485150062000145, -12.76303204342999997 ) ) ;
#19791=DIRECTION ( 'NONE',  ( -1.000000000000000000, 0.000000000000000000, 0.000000000000000000 ) ) ;
#19795=CARTESIAN_POINT ( 'NONE',  ( 7.657744736620999859, -18.33080421803999727, -9.966195456754999071 ) ) ;
#19796=CARTESIAN_POINT ( 'NONE',  ( 8.179400486892387079, -17.25908162455774075, 9.502921779304051242 ) ) ;
#19802=CARTESIAN_POINT ( 'NONE',  ( -4.144949124996972323, -77.55034540772489038, -11.57804869542019155 ) ) ;
#19804=AXIS2_PLACEMENT_3D ( 'NONE', #31492, #49539, #44807 ) ;
#19809=EDGE_CURVE ( 'NONE', #30476, #55619, #13483, .T. ) ;
#19815=ORIENTED_EDGE ( 'NONE', *, *, #22742, .F. ) ;
#19819=ORIENTED_EDGE ( 'NONE', *, *, #16660, .F. ) ;
#19820=CARTESIAN_POINT ( 'NONE',  ( 10.08162962782999905, -17.28146287379999890, 7.981572332336000386 ) ) ;
#19821=AXIS2_PLACEMENT_3D ( 'NONE', #45312, #45011, #27853 ) ;
#19823=CARTESIAN_POINT ( 'NONE',  ( 7.880031981693000454, -79.23622702059999767, 8.980504559447000545 ) ) ;
#19824=CARTESIAN_POINT ( 'NONE',  ( 9.783241737811998462, -61.33564621498000946, 7.961026681588999843 ) ) ;
#19829=CARTESIAN_POINT ( 'NONE',  ( 11.09211448529823762, -78.07761170217334268, 4.008287385160122618 ) ) ;
#19830=EDGE_LOOP ( 'NONE', ( #25642, #25660, #23228 ) ) ;
#19834=DIRECTION ( 'NONE',  ( 0.000000000000000000, 1.000000000000000000, 0.000000000000000000 ) ) ;
#19838=EDGE_CURVE ( 'NONE', #11618, #26528, #27061, .T. ) ;
#19840=CARTESIAN_POINT ( 'NONE',  ( -7.657745562908000458, -23.66920625126000033, -9.966193613329998868 ) ) ;
#19843=AXIS2_PLACEMENT_3D ( 'NONE', #26777, #53963, #35633 ) ;
#19850=CARTESIAN_POINT ( 'NONE',  ( -7.758650587948999977, -17.84922688128999724, 9.996717134846999642 ) ) ;
#19852=CARTESIAN_POINT ( 'NONE',  ( -3.265816405937842060, -3.219552046736191553, 1.312226571638672512 ) ) ;
#19855=FACE_OUTER_BOUND ( 'NONE', #1242, .T. ) ;
#19861=CARTESIAN_POINT ( 'NONE',  ( 1.798954018877999994, -60.01530973353999343, -12.61117007304000026 ) ) ;
#19870=VERTEX_POINT ( 'NONE', #34623 ) ;
#19875=CARTESIAN_POINT ( 'NONE',  ( 7.634437838894000627, -55.05219468418000162, -10.30764259108000225 ) ) ;
#19884=VERTEX_POINT ( 'NONE', #52370 ) ;
#19887=CARTESIAN_POINT ( 'NONE',  ( -0.5999999999999999778, -23.15000000000000213, -10.98362417419999915 ) ) ;
#19888=EDGE_LOOP ( 'NONE', ( #52818, #31398, #30947, #47282 ) ) ;
#19890=AXIS2_PLACEMENT_3D ( 'NONE', #40017, #45056, #17592 ) ;
#19892=B_SPLINE_CURVE_WITH_KNOTS ( 'NONE', 3,
 ( #43228, #52379, #30203, #48249, #7786, #52948, #48525, #43813, #33769, #51808, #11365, #16074, #47386, #6918, #24925, #42943 ),
 .UNSPECIFIED., .F., .F.,
 ( 4, 2, 2, 2, 2, 2, 2, 4 ),
 ( 0.000000000000000000, 0.08929374297993872278, 0.1785874859598774456, 0.2678812289398161406, 0.3571749719197548911, 0.4464687148996936417, 0.5357624578796322812, 0.7143499438395097823 ),
 .UNSPECIFIED. ) ;
#19894=VERTEX_POINT ( 'NONE', #25200 ) ;
#19896=CARTESIAN_POINT ( 'NONE',  ( -0.8445585116437001050, -17.28959556757000016, 12.43380736237000050 ) ) ;
#19904=ORIENTED_EDGE ( 'NONE', *, *, #56554, .F. ) ;
#19909=VECTOR ( 'NONE', #32943, 1000.000000000000000 ) ;
#19915=CARTESIAN_POINT ( 'NONE',  ( -8.061017305527000687, -59.94999999967000548, 8.909545442949999838 ) ) ;
#19916=CARTESIAN_POINT ( 'NONE',  ( -7.593391408704848189, -76.63053360682752668, 8.968398750625850013 ) ) ;
#19917=ADVANCED_FACE ( 'NONE', ( #34907 ), #2207, .F. ) ;
#19922=DIRECTION ( 'NONE',  ( 0.7071067811864966135, 0.7071067811865965336, 5.001433494089977624E-08 ) ) ;
#19924=CARTESIAN_POINT ( 'NONE',  ( 1.758095523367999791, -18.27708336119999899, -12.57362173515999970 ) ) ;
#19926=DIRECTION ( 'NONE',  ( 0.000000000000000000, -0.7071067811864425456, 0.7071067811866525998 ) ) ;
#19928=CARTESIAN_POINT ( 'NONE',  ( -3.180605150700375638, -1.214306347645720985, 1.530408170426506897 ) ) ;
#19931=DIRECTION ( 'NONE',  ( 0.7071067811865475727, 0.000000000000000000, 0.7071067811865475727 ) ) ;
#19937=CARTESIAN_POINT ( 'NONE',  ( -1.189541931187000134, -77.06571553208000580, -12.95855809378999979 ) ) ;
#19943=CARTESIAN_POINT ( 'NONE',  ( -0.9157810684381340049, -76.31873599581450662, -11.71594503368780771 ) ) ;
#19946=VECTOR ( 'NONE', #56132, 1000.000000000000000 ) ;
#19949=CARTESIAN_POINT ( 'NONE',  ( 1.636761686205415067, -2.833333333333333481, 2.839805762151342616 ) ) ;
#19955=VECTOR ( 'NONE', #37089, 1000.000000000000114 ) ;
#19958=VERTEX_POINT ( 'NONE', #11353 ) ;
#19960=FACE_OUTER_BOUND ( 'NONE', #57007, .T. ) ;
#19961=DIRECTION ( 'NONE',  ( -1.000000000000000000, 0.000000000000000000, 0.000000000000000000 ) ) ;
#19964=ORIENTED_EDGE ( 'NONE', *, *, #32479, .T. ) ;
#19966=ADVANCED_FACE ( 'NONE', ( #16355 ), #25487, .F. ) ;
#19967=CARTESIAN_POINT ( 'NONE',  ( -10.07627163191000008, -18.75000000310999937, -7.601397897754999633 ) ) ;
#19969=EDGE_CURVE ( 'NONE', #13072, #17378, #20493, .T. ) ;
#19972=ORIENTED_EDGE ( 'NONE', *, *, #27381, .T. ) ;
#19974=VERTEX_POINT ( 'NONE', #34046 ) ;
#19975=CARTESIAN_POINT ( 'NONE',  ( -7.668949790015999746, -59.57129148919000272, 10.21381326473999884 ) ) ;
#19976=ORIENTED_EDGE ( 'NONE', *, *, #6625, .F. ) ;
#19980=CARTESIAN_POINT ( 'NONE',  ( 12.70556836347999941, -25.22772277227999993, 2.424222353299999887E-09 ) ) ;
#19981=CARTESIAN_POINT ( 'NONE',  ( 3.343750000583999960, -0.9062499994161000716, -3.925818329445000231E-08 ) ) ;
#19986=CARTESIAN_POINT ( 'NONE',  ( -7.653559502293999728, -60.09849137195000424, -10.01234990230000044 ) ) ;
#19988=CARTESIAN_POINT ( 'NONE',  ( 4.120651084761334459, -76.54600812598258130, 11.01093787941378643 ) ) ;
#19989=EDGE_CURVE ( 'NONE', #47619, #28634, #37438, .T. ) ;
#19992=CARTESIAN_POINT ( 'NONE',  ( -3.024915515467232474, -3.071593521866582410, 1.186391032666482825 ) ) ;
#20000=DIRECTION ( 'NONE',  ( 0.000000000000000000, 1.000000000000000000, 0.000000000000000000 ) ) ;
#20002=CARTESIAN_POINT ( 'NONE',  ( -10.36221643470000053, -60.02123873632999818, -7.631895748967999715 ) ) ;
#20003=CARTESIAN_POINT ( 'NONE',  ( 0.2613843059707509631, -3.500000000000000000, 3.291795858360297977 ) ) ;
#20005=CARTESIAN_POINT ( 'NONE',  ( 10.53101998748999968, -60.10639625617000092, 7.613962827198000660 ) ) ;
#20006=B_SPLINE_CURVE_WITH_KNOTS ( 'NONE', 3,
 ( #4528, #423, #22528, #26357, #45272, #36104, #21648, #44972, #4229, #35800, #39939, #54121, #13662, #3645, #35499, #13069, #57660, #40538 ),
 .UNSPECIFIED., .F., .F.,
 ( 4, 2, 2, 2, 2, 2, 2, 2, 4 ),
 ( 0.000000000000000000, 0.1250000000000001110, 0.2500000000000001665, 0.3750000000000001665, 0.5000000000000001110, 0.6250000000000001110, 0.7500000000000001110, 0.8750000000000001110, 1.000000000000000000 ),
 .UNSPECIFIED. ) ;
#20008=ADVANCED_FACE ( 'NONE', ( #52084 ), #20776, .F. ) ;
#20009=CARTESIAN_POINT ( 'NONE',  ( 12.77302471391999994, -24.72230123305000049, 1.481949986259999852 ) ) ;
#20011=CARTESIAN_POINT ( 'NONE',  ( 11.67610687481217902, -78.43638509158282091, -1.539212210575771067 ) ) ;
#20013=CARTESIAN_POINT ( 'NONE',  ( -11.96865137734000051, -76.26552026400000273, -1.496560055186000104 ) ) ;
#20014=ORIENTED_EDGE ( 'NONE', *, *, #53083, .T. ) ;
#20018=CARTESIAN_POINT ( 'NONE',  ( 8.343860018000999190, -59.94999999967000548, -8.343860018000999190 ) ) ;
#20020=CARTESIAN_POINT ( 'NONE',  ( -1.931086388578000079, -18.70221245812999911, -12.71798269385000069 ) ) ;
#20023=LINE ( 'NONE', #42163, #51977 ) ;
#20025=ORIENTED_EDGE ( 'NONE', *, *, #52839, .F. ) ;
#20027=ADVANCED_FACE ( 'NONE', ( #49685 ), #53476, .F. ) ;
#20033=ORIENTED_EDGE ( 'NONE', *, *, #10718, .T. ) ;
#20037=AXIS2_PLACEMENT_3D ( 'NONE', #42636, #34042, #51505 ) ;
#20038=ORIENTED_EDGE ( 'NONE', *, *, #50351, .T. ) ;
#20039=ORIENTED_EDGE ( 'NONE', *, *, #24170, .F. ) ;
#20041=ADVANCED_FACE ( 'NONE', ( #3631 ), #4510, .F. ) ;
#20047=CARTESIAN_POINT ( 'NONE',  ( -0.8504682047943638024, -2.496968858996786000, 3.168006968375890686 ) ) ;
#20050=CARTESIAN_POINT ( 'NONE',  ( -12.77649732927999970, -25.30828417252000051, 0.06479631635393000300 ) ) ;
#20054=DIRECTION ( 'NONE',  ( 0.000000000000000000, -1.000000000000000000, 0.000000000000000000 ) ) ;
#20056=DIRECTION ( 'NONE',  ( 1.000000000000000000, 0.000000000000000000, 0.000000000000000000 ) ) ;
#20057=AXIS2_PLACEMENT_3D ( 'NONE', #6487, #52237, #20930 ) ;
#20061=CARTESIAN_POINT ( 'NONE',  ( 12.17088485526999975, -75.70997293883000623, 1.845041276493999849 ) ) ;
#20063=CARTESIAN_POINT ( 'NONE',  ( 8.485281374238999419, -60.04999999966999980, -8.485281374238999419 ) ) ;
#20064=CARTESIAN_POINT ( 'NONE',  ( 11.93255069029000026, -79.21413110817999836, -2.830763026309000008 ) ) ;
#20067=CARTESIAN_POINT ( 'NONE',  ( 10.30361667856515417, -77.84302199712344361, 6.183189858139286343 ) ) ;
#20070=CARTESIAN_POINT ( 'NONE',  ( -1.538071403319991814, -77.91458333333333997, -11.75000000000000355 ) ) ;
#20071=DIRECTION ( 'NONE',  ( 0.000000000000000000, 0.000000000000000000, -1.000000000000000000 ) ) ;
#20074=CARTESIAN_POINT ( 'NONE',  ( -3.679349115619000354, -1.792405217095000003, 0.1044579997439999963 ) ) ;
#20077=CARTESIAN_POINT ( 'NONE',  ( -7.250009772427842059, -76.12782158799809906, 9.252138825763349672 ) ) ;
#20082=CARTESIAN_POINT ( 'NONE',  ( 12.70610460582542167, -24.45512899795008011, 1.580683094056565485 ) ) ;
#20083=DIRECTION ( 'NONE',  ( -1.000000000000000000, 0.000000000000000000, 0.000000000000000000 ) ) ;
#20088=CARTESIAN_POINT ( 'NONE',  ( -0.8494789362751314910, -3.204387569124965474, -3.247320870830982198 ) ) ;
#20089=CARTESIAN_POINT ( 'NONE',  ( -12.70457850616584317, -53.62128713286525539, -0.5106122237776331563 ) ) ;
#20090=VERTEX_POINT ( 'NONE', #58233 ) ;
#20092=CARTESIAN_POINT ( 'NONE',  ( 0.000000000000000000, 0.000000000000000000, 0.000000000000000000 ) ) ;
#20095=ADVANCED_FACE ( 'NONE', ( #8639 ), #23418, .F. ) ;
#20096=CARTESIAN_POINT ( 'NONE',  ( 1.347889543704216431, -77.31907281190599690, 11.99453198319526592 ) ) ;
#20099=CARTESIAN_POINT ( 'NONE',  ( 14.00000000000000000, -72.39999999999999147, -1.714505518806294638E-15 ) ) ;
#20101=CARTESIAN_POINT ( 'NONE',  ( 8.414570695956999913, -59.94999999967000548, 8.414570695956999913 ) ) ;
#20103=CARTESIAN_POINT ( 'NONE',  ( -1.980532758766000212, -22.76256650694000072, 12.80088938802999898 ) ) ;
#20105=EDGE_CURVE ( 'NONE', #43036, #23138, #21220, .T. ) ;
#20108=ORIENTED_EDGE ( 'NONE', *, *, #53953, .T. ) ;
#20112=CARTESIAN_POINT ( 'NONE',  ( 7.961057357828999592, -17.46431744651999907, 9.783210913639999617 ) ) ;
#20114=ADVANCED_FACE ( 'NONE', ( #37834 ), #40847, .F. ) ;
#20115=CARTESIAN_POINT ( 'NONE',  ( -5.440694134380999358, -78.91922042627000167, -10.76505340543000067 ) ) ;
#20116=LINE ( 'NONE', #47582, #1409 ) ;
#20117=DIRECTION ( 'NONE',  ( 0.7071067811865475727, 0.000000000000000000, 0.7071067811865475727 ) ) ;
#20118=CARTESIAN_POINT ( 'NONE',  ( 3.250000000000000000, -3.250000000000000000, 0.000000000000000000 ) ) ;
#20121=ORIENTED_EDGE ( 'NONE', *, *, #44954, .F. ) ;
#20122=CARTESIAN_POINT ( 'NONE',  ( 5.059105317731693141, -78.13973803206332036, 10.65395817999562667 ) ) ;
#20123=EDGE_LOOP ( 'NONE', ( #819, #25250, #12664 ) ) ;
#20129=AXIS2_PLACEMENT_3D ( 'NONE', #3164, #43898, #47185 ) ;
#20132=CARTESIAN_POINT ( 'NONE',  ( -7.655542440091000600, -19.22180874373999870, 10.38645071870000081 ) ) ;
#20137=( LENGTH_UNIT ( ) NAMED_UNIT ( * ) SI_UNIT ( .MILLI., .METRE. ) );
#20139=EDGE_LOOP ( 'NONE', ( #19143, #57628, #48005, #35440 ) ) ;
#20144=CARTESIAN_POINT ( 'NONE',  ( -8.385806979641005299, -53.91189752976736571, 9.298530586719172319 ) ) ;
#20146=CARTESIAN_POINT ( 'NONE',  ( -3.453171399369999950, -1.763032031398999999, -0.5706200895263999762 ) ) ;
#20154=EDGE_LOOP ( 'NONE', ( #30537, #10486, #57741, #40085, #52824 ) ) ;
#20156=CARTESIAN_POINT ( 'NONE',  ( 1.814305421036000121, -61.08941969298000174, -12.78003582256000215 ) ) ;
#20160=CARTESIAN_POINT ( 'NONE',  ( 10.45205659047000069, -56.03767314774999875, -7.651160337227000063 ) ) ;
#20163=CARTESIAN_POINT ( 'NONE',  ( 7.050812550749764540, -78.52208679444892425, 9.402307432884422056 ) ) ;
#20164=CARTESIAN_POINT ( 'NONE',  ( -10.20678250203529025, -61.03575784435037122, 7.770339463558867621 ) ) ;
#20168=AXIS2_PLACEMENT_3D ( 'NONE', #57602, #31597, #17163 ) ;
#20169=CARTESIAN_POINT ( 'NONE',  ( 7.633478597807999755, -55.59901960186999759, -10.36292351976000070 ) ) ;
#20171=CARTESIAN_POINT ( 'NONE',  ( -11.88151041292270094, -79.13151041431198962, -1.554433303865662142 ) ) ;
#20176=AXIS2_PLACEMENT_3D ( 'NONE', #46660, #1782, #24490 ) ;
#20178=ORIENTED_EDGE ( 'NONE', *, *, #17808, .F. ) ;
#20182=ORIENTED_EDGE ( 'NONE', *, *, #48945, .F. ) ;
#20183=ORIENTED_EDGE ( 'NONE', *, *, #53613, .T. ) ;
#20184=CARTESIAN_POINT ( 'NONE',  ( -1.980584515756000030, -23.26485150094000076, -12.76303204340999997 ) ) ;
#20186=ORIENTED_EDGE ( 'NONE', *, *, #46847, .F. ) ;
#20187=CARTESIAN_POINT ( 'NONE',  ( -0.9781264271453999903, -17.05968856123000066, 12.65967462879000038 ) ) ;
#20190=DIRECTION ( 'NONE',  ( 0.000000000000000000, -1.000000000000000000, 0.000000000000000000 ) ) ;
#20193=EDGE_CURVE ( 'NONE', #587, #23097, #11981, .T. ) ;
#20206=VECTOR ( 'NONE', #28288, 999.9999999999998863 ) ;
#20208=CARTESIAN_POINT ( 'NONE',  ( -9.764531328947487765, -76.65264217124246215, 6.535287190017895043 ) ) ;
#20209=CARTESIAN_POINT ( 'NONE',  ( 3.707796996315166016, -79.21874998086906317, -11.41868144588404377 ) ) ;
#20210=CARTESIAN_POINT ( 'NONE',  ( -9.992014434659999722, -54.63915351680999777, 7.762970980286999279 ) ) ;
#20212=TOROIDAL_SURFACE ( 'NONE', #19283, 26.50000000000000000, 14.00000000000000000 ) ;
#20215=CARTESIAN_POINT ( 'NONE',  ( 1.799501877793999949, -23.28917723430000208, -12.60552511010000032 ) ) ;
#20217=CARTESIAN_POINT ( 'NONE',  ( 1.798336774608999988, -18.80355501948000096, -12.61277771566000006 ) ) ;
#20222=CARTESIAN_POINT ( 'NONE',  ( -7.342331066867000544, -55.64999999967000122, -8.190859204290999784 ) ) ;
#20223=EDGE_LOOP ( 'NONE', ( #35485, #15299, #51488, #31414 ) ) ;
#20225=CARTESIAN_POINT ( 'NONE',  ( -1.666698456705999920, -55.60818260126999490, 12.50018138918999888 ) ) ;
#20228=CARTESIAN_POINT ( 'NONE',  ( -12.79971535682999928, -55.00965922235999983, 2.019101350716999921 ) ) ;
#20229=FACE_OUTER_BOUND ( 'NONE', #52601, .T. ) ;
#20234=CIRCLE ( 'NONE', #56967, 0.6000000000000008660 ) ;
#20238=DIRECTION ( 'NONE',  ( 0.7071067811865475727, 0.000000000000000000, 0.7071067811865475727 ) ) ;
#20245=EDGE_CURVE ( 'NONE', #48866, #18440, #23324, .T. ) ;
#20248=FACE_OUTER_BOUND ( 'NONE', #20154, .T. ) ;
#20249=ORIENTED_EDGE ( 'NONE', *, *, #2462, .T. ) ;
#20250=ADVANCED_FACE ( 'NONE', ( #2102 ), #52509, .F. ) ;
#20252=VERTEX_POINT ( 'NONE', #38377 ) ;
#20253=B_SPLINE_CURVE_WITH_KNOTS ( 'NONE', 3,
 ( #51978, #42532, #16244, #33939, #43692, #3247 ),
 .UNSPECIFIED., .F., .F.,
 ( 4, 1, 1, 4 ),
 ( 0.000000000000000000, 0.3333333333333000081, 0.6666666666667000474, 1.000000000000000000 ),
 .UNSPECIFIED. ) ;
#20254=ORIENTED_EDGE ( 'NONE', *, *, #19101, .T. ) ;
#20260=EDGE_CURVE ( 'NONE', #48350, #20090, #29686, .T. ) ;
#20262=CARTESIAN_POINT ( 'NONE',  ( -7.682331425181999407, -56.03513569577999931, 10.04115011118999945 ) ) ;
#20263=ORIENTED_EDGE ( 'NONE', *, *, #42497, .F. ) ;
#20264=DIRECTION ( 'NONE',  ( 1.000000000000000000, 0.000000000000000000, 0.000000000000000000 ) ) ;
#20272=AXIS2_PLACEMENT_3D ( 'NONE', #633, #50200, #8574 ) ;
#20275=VECTOR ( 'NONE', #19922, 1000.000000000000114 ) ;
#20276=LINE ( 'NONE', #29403, #10120 ) ;
#20277=CARTESIAN_POINT ( 'NONE',  ( -12.56594317991999965, -60.04999999381999487, -1.750000000001000089 ) ) ;
#20282=CARTESIAN_POINT ( 'NONE',  ( -10.13969151608854524, -76.24193945363813896, -5.960466986128117206 ) ) ;
#20283=DIRECTION ( 'NONE',  ( -0.7592504788685168204, 0.04890177849162108403, 0.6489586476797148951 ) ) ;
#20284=CARTESIAN_POINT ( 'NONE',  ( -0.8338927958969420962, -24.80053577746247129, 12.50366901602898650 ) ) ;
#20289=CARTESIAN_POINT ( 'NONE',  ( 12.54715528150999937, -24.53180535391000205, 1.292252957172000061 ) ) ;
#20292=CARTESIAN_POINT ( 'NONE',  ( 11.37976048585989020, -78.42608585681624334, -3.047580145233151683 ) ) ;
#20293=TOROIDAL_SURFACE ( 'NONE', #35335, 13.50000000000000000, 0.5000000000000000000 ) ;
#20295=CARTESIAN_POINT ( 'NONE',  ( -1.250000000000000000, -18.75000000000000000, 12.50000000000000000 ) ) ;
#20302=CARTESIAN_POINT ( 'NONE',  ( -17.49999986748943925, -13.07071424677999971, -0.002153571276233540773 ) ) ;
#20305=CARTESIAN_POINT ( 'NONE',  ( -8.999999998907000531, -3.999999998907000087, 1.966780300384000192E-09 ) ) ;
#20307=ORIENTED_EDGE ( 'NONE', *, *, #20837, .F. ) ;
#20308=CARTESIAN_POINT ( 'NONE',  ( 0.000000000000000000, -23.75000000000000000, 11.79999999999999893 ) ) ;
#20310=ORIENTED_EDGE ( 'NONE', *, *, #24546, .F. ) ;
#20312=CARTESIAN_POINT ( 'NONE',  ( 12.53239398061000109, -59.56486430393999854, 1.667936688463999895 ) ) ;
#20314=CARTESIAN_POINT ( 'NONE',  ( -8.838834764832000701, -18.75000000000000000, -8.838834764832000701 ) ) ;
#20316=EDGE_CURVE ( 'NONE', #32447, #52628, #21983, .T. ) ;
#20320=EDGE_LOOP ( 'NONE', ( #805, #16537, #43278, #38418 ) ) ;
#20325=EDGE_CURVE ( 'NONE', #237, #17178, #12383, .T. ) ;
#20328=CARTESIAN_POINT ( 'NONE',  ( -5.531768889155999958, -79.13776145859631583, -10.94525552207000096 ) ) ;
#20329=EDGE_CURVE ( 'NONE', #18079, #4024, #50878, .T. ) ;
#20331=CARTESIAN_POINT ( 'NONE',  ( 7.730439324435801396, -17.87809618957197699, -10.25198230928420173 ) ) ;
#20333=CARTESIAN_POINT ( 'NONE',  ( -11.75000000000000000, -77.20000000000000284, -1.435311119447000145E-14 ) ) ;
#20334=CARTESIAN_POINT ( 'NONE',  ( -12.70305331333694632, -16.96853698854184600, -0.8727610012099511483 ) ) ;
#20337=CARTESIAN_POINT ( 'NONE',  ( -8.260136572111999698, -24.94034376567000066, 9.643347111174000119 ) ) ;
#20342=CARTESIAN_POINT ( 'NONE',  ( 8.958641849996999085, -62.00112647771999974, -8.950065109854000056 ) ) ;
#20343=CARTESIAN_POINT ( 'NONE',  ( 0.000000000000000000, -46.09579702914000165, 0.000000000000000000 ) ) ;
#20345=CARTESIAN_POINT ( 'NONE',  ( 1.250000000000000000, -55.54999999966999980, 12.00000000000000000 ) ) ;
#20346=CARTESIAN_POINT ( 'NONE',  ( -6.395896118064722025, -77.46943306756942604, 10.23033580516363195 ) ) ;
#20347=DIRECTION ( 'NONE',  ( 0.7592504788685928707, 0.04890177849867949345, -0.6489586476790939473 ) ) ;
#20351=CARTESIAN_POINT ( 'NONE',  ( -9.396085398178614767, -77.85208333333332575, -7.220923959705254802 ) ) ;
#20353=DIRECTION ( 'NONE',  ( 0.7071067811865475727, 0.000000000000000000, 0.7071067811865475727 ) ) ;
#20354=CARTESIAN_POINT ( 'NONE',  ( -1.937973738374999977, -3.211110789882000383, 3.350311810597999873 ) ) ;
#20355=TOROIDAL_SURFACE ( 'NONE', #7166, 1.250000000000000000, 0.5000000000000000000 ) ;
#20359=CARTESIAN_POINT ( 'NONE',  ( -8.294246302884193511, -76.13736708880301762, 8.322727450349711731 ) ) ;
#20363=AXIS2_PLACEMENT_3D ( 'NONE', #9196, #40778, #44624 ) ;
#20365=EDGE_CURVE ( 'NONE', #58179, #25083, #31763, .T. ) ;
#20366=DIRECTION ( 'NONE',  ( 0.000000000000000000, -1.000000000000000000, 0.000000000000000000 ) ) ;
#20370=DIRECTION ( 'NONE',  ( 0.000000000000000000, 1.000000000000000000, 0.000000000000000000 ) ) ;
#20371=DIRECTION ( 'NONE',  ( 0.5721800009721869085, 0.8201280671257802357, 0.000000000000000000 ) ) ;
#20377=FACE_OUTER_BOUND ( 'NONE', #33676, .T. ) ;
#20385=PLANE ( 'NONE',  #52767 ) ;
#20386=CARTESIAN_POINT ( 'NONE',  ( -13.86301033151605289, -9.638971321655001034, -0.1317488955328472711 ) ) ;
#20387=ORIENTED_EDGE ( 'NONE', *, *, #49350, .F. ) ;
#20391=EDGE_CURVE ( 'NONE', #34093, #44548, #9130, .T. ) ;
#20393=CARTESIAN_POINT ( 'NONE',  ( 10.52693198617999926, -18.57847693927000066, 7.606025555766000146 ) ) ;
#20396=CARTESIAN_POINT ( 'NONE',  ( 3.075537641221555596, -75.94583333333332575, -11.44417895085270587 ) ) ;
#20397=AXIS2_PLACEMENT_3D ( 'NONE', #2743, #43767, #11606 ) ;
#20398=CARTESIAN_POINT ( 'NONE',  ( 5.421352887295999956, -77.00873275214000557, 11.59375966951999892 ) ) ;
#20399=VECTOR ( 'NONE', #30794, 1000.000000000000000 ) ;
#20401=FACE_OUTER_BOUND ( 'NONE', #51813, .T. ) ;
#20405=ORIENTED_EDGE ( 'NONE', *, *, #54032, .T. ) ;
#20410=LINE ( 'NONE', #38695, #2222 ) ;
#20414=ADVANCED_FACE ( 'NONE', ( #35677 ), #4036, .F. ) ;
#20415=CARTESIAN_POINT ( 'NONE',  ( -11.90000000000000036, -21.00000000000000000, -0.6999999999999999556 ) ) ;
#20416=CARTESIAN_POINT ( 'NONE',  ( -8.838834764832000701, -55.54999999966999980, -8.838834764832000701 ) ) ;
#20417=B_SPLINE_CURVE_WITH_KNOTS ( 'NONE', 3,
 ( #56711, #7115, #2975, #20975, #25115, #16267, #24541, #37821 ),
 .UNSPECIFIED., .F., .F.,
 ( 4, 2, 2, 4 ),
 ( 0.000000000000000000, 0.5000000000000052180, 0.7500000000000025535, 1.000000000000000000 ),
 .UNSPECIFIED. ) ;
#20418=CARTESIAN_POINT ( 'NONE',  ( -7.612971540276999960, -23.32452273707999879, 10.53003236233000095 ) ) ;
#20420=EDGE_CURVE ( 'NONE', #30548, #39794, #10299, .T. ) ;
#20422=PRESENTATION_STYLE_ASSIGNMENT (( #2419 ) ) ;
#20424=VERTEX_POINT ( 'NONE', #55457 ) ;
#20426=LINE ( 'NONE', #6253, #27786 ) ;
#20429=CARTESIAN_POINT ( 'NONE',  ( -7.756275637039999893, -17.77995361836999777, 10.15825999916999933 ) ) ;
#20431=CARTESIAN_POINT ( 'NONE',  ( -0.2605338304268313143, -2.369161478775310137, -3.510605834263762492 ) ) ;
#20439=EDGE_CURVE ( 'NONE', #57339, #26450, #28996, .T. ) ;
#20441=DIRECTION ( 'NONE',  ( -1.000000000000000000, 0.000000000000000000, 0.000000000000000000 ) ) ;
#20442=CARTESIAN_POINT ( 'NONE',  ( 1.798368564622000010, -59.99636757014000210, -12.61278090843000044 ) ) ;
#20443=CARTESIAN_POINT ( 'NONE',  ( -8.150146600852252732, -55.38467666605728112, 7.387512494710395394 ) ) ;
#20449=CARTESIAN_POINT ( 'NONE',  ( 11.24815246472408425, -78.47207392326706099, 3.394727518005801414 ) ) ;
#20450=DIRECTION ( 'NONE',  ( 0.4045626182452127795, -0.8201574091826254742, 0.4045626182452127795 ) ) ;
#20451=ORIENTED_EDGE ( 'NONE', *, *, #24749, .F. ) ;
#20452=AXIS2_PLACEMENT_3D ( 'NONE', #55807, #1504, #56673 ) ;
#20454=CARTESIAN_POINT ( 'NONE',  ( -3.630949683906000036, -75.80000000000001137, -11.17491406647000041 ) ) ;
#20455=AXIS2_PLACEMENT_3D ( 'NONE', #38633, #11498, #29753 ) ;
#20456=EDGE_CURVE ( 'NONE', #11044, #21614, #26162, .T. ) ;
#20457=AXIS2_PLACEMENT_3D ( 'NONE', #25137, #33700, #16577 ) ;
#20460=CARTESIAN_POINT ( 'NONE',  ( -10.26699006316255591, -77.75833333333332575, 5.917523019358029934 ) ) ;
#20461=CARTESIAN_POINT ( 'NONE',  ( -10.18499221076999994, -57.05022860182000244, 7.710118476618999850 ) ) ;
#20462=VECTOR ( 'NONE', #20054, 1000.000000000000000 ) ;
#20469=CARTESIAN_POINT ( 'NONE',  ( -12.72394223969999949, -23.22159774865999893, 1.930881086224999876 ) ) ;
#20470=EDGE_LOOP ( 'NONE', ( #27925, #36255, #2681, #37220 ) ) ;
#20471=VERTEX_POINT ( 'NONE', #14416 ) ;
#20472=CARTESIAN_POINT ( 'NONE',  ( -1.343382297838000047E-14, -80.79999999999999716, 0.000000000000000000 ) ) ;
#20474=EDGE_LOOP ( 'NONE', ( #33805, #18796, #55393, #34678 ) ) ;
#20482=ORIENTED_EDGE ( 'NONE', *, *, #14602, .T. ) ;
#20485=CIRCLE ( 'NONE', #30820, 1.750000000000001332 ) ;
#20486=CARTESIAN_POINT ( 'NONE',  ( -12.48409101790999998, -60.16970703802000031, -1.669510252625000080 ) ) ;
#20490=TOROIDAL_SURFACE ( 'NONE', #8088, 17.50000000000000000, 5.000000000000000000 ) ;
#20493=LINE ( 'NONE', #38490, #4424 ) ;
#20494=CIRCLE ( 'NONE', #57221, 14.00000000000000000 ) ;
#20495=AXIS2_PLACEMENT_3D ( 'NONE', #54654, #14193, #36636 ) ;
#20496=CARTESIAN_POINT ( 'NONE',  ( -10.53494359612999887, -55.57285042800999264, 7.618393753177000072 ) ) ;
#20499=CARTESIAN_POINT ( 'NONE',  ( 2.062670899361999766, -23.30639784948999704, -12.83044027760000105 ) ) ;
#20500=FACE_OUTER_BOUND ( 'NONE', #20931, .T. ) ;
#20505=CARTESIAN_POINT ( 'NONE',  ( -3.750250575282000121, -2.338355802843000486, 0.6493866540274000343 ) ) ;
#20506=DIRECTION ( 'NONE',  ( 0.000000000000000000, 0.000000000000000000, -1.000000000000000000 ) ) ;
#20507=ORIENTED_EDGE ( 'NONE', *, *, #24845, .T. ) ;
#20508=DIRECTION ( 'NONE',  ( 0.7071067810866970005, -6.386274622742979319E-09, 0.7071067812863980340 ) ) ;
#20511=CARTESIAN_POINT ( 'NONE',  ( -1.933650113858000230, -55.39213746940999528, 12.70909635752000177 ) ) ;
#20516=CARTESIAN_POINT ( 'NONE',  ( 1.194090705995999979, -61.24031658870000427, 12.43436538493000043 ) ) ;
#20518=CARTESIAN_POINT ( 'NONE',  ( 5.939680743703000668E-14, -6.000000000000000000, 0.000000000000000000 ) ) ;
#20521=EDGE_CURVE ( 'NONE', #4032, #10285, #7329, .T. ) ;
#20524=CARTESIAN_POINT ( 'NONE',  ( -2.431761726605123020, -1.043462501739716108, 2.188053907655647556 ) ) ;
#20535=TOROIDAL_SURFACE ( 'NONE', #29901, 1.250000000000000000, 0.5000000000000000000 ) ;
#20536=ORIENTED_EDGE ( 'NONE', *, *, #15692, .F. ) ;
#20537=CARTESIAN_POINT ( 'NONE',  ( -0.6484536763399982862, -25.12402982711039812, 12.70397497891742233 ) ) ;
#20538=EDGE_CURVE ( 'NONE', #17898, #40041, #24085, .T. ) ;
#20539=ORIENTED_EDGE ( 'NONE', *, *, #7468, .F. ) ;
#20541=CARTESIAN_POINT ( 'NONE',  ( 3.031768397182069918, -3.499999999999999556, -1.753150493843362634 ) ) ;
#20543=CARTESIAN_POINT ( 'NONE',  ( 9.396085398178630754, -77.49791666666665435, -7.220923959705230821 ) ) ;
#20548=ORIENTED_EDGE ( 'NONE', *, *, #36363, .T. ) ;
#20549=CARTESIAN_POINT ( 'NONE',  ( 3.236394086226999978, -2.780734372332999804, -1.046485274464999948 ) ) ;
#20555=FACE_OUTER_BOUND ( 'NONE', #32926, .T. ) ;
#20563=CARTESIAN_POINT ( 'NONE',  ( -8.343860018000999190, -60.54999999966955926, -8.343860018000999190 ) ) ;
#20568=CARTESIAN_POINT ( 'NONE',  ( 0.2494208068312679105, -24.99288960763016831, -12.50614183112954336 ) ) ;
#20574=EDGE_CURVE ( 'NONE', #456, #55491, #4988, .T. ) ;
#20577=ADVANCED_FACE ( 'NONE', ( #25532 ), #16970, .F. ) ;
#20581=CARTESIAN_POINT ( 'NONE',  ( -7.223656224191105757, -78.27159733532405994, -9.395165950963319190 ) ) ;
#20582=VECTOR ( 'NONE', #47031, 1000.000000000000114 ) ;
#20583=CARTESIAN_POINT ( 'NONE',  ( 0.5222397221644492493, -25.16298219402098013, -12.70447686583673708 ) ) ;
#20584=CARTESIAN_POINT ( 'NONE',  ( -6.672837361367000675, -75.65930287300999169, -9.910479691896998844 ) ) ;
#20588=EDGE_CURVE ( 'NONE', #38869, #1755, #7152, .T. ) ;
#20589=CARTESIAN_POINT ( 'NONE',  ( -11.00000000000000000, -18.25000000000000000, 0.000000000000000000 ) ) ;
#20590=CARTESIAN_POINT ( 'NONE',  ( -12.78963794847000024, -78.58340606474000367, -0.3129899442943999688 ) ) ;
#20591=CARTESIAN_POINT ( 'NONE',  ( 0.000000000000000000, -3.000000000000000000, -12.90000000000398472 ) ) ;
#20595=LINE ( 'NONE', #29434, #3783 ) ;
#20599=ORIENTED_EDGE ( 'NONE', *, *, #34985, .F. ) ;
#20605=ORIENTED_EDGE ( 'NONE', *, *, #24089, .T. ) ;
#20606=VERTEX_POINT ( 'NONE', #21106 ) ;
#20609=CARTESIAN_POINT ( 'NONE',  ( 1.247385803315000041, -61.27722255996999934, 12.50301438880000049 ) ) ;
#20615=CARTESIAN_POINT ( 'NONE',  ( -12.02296678431999943, -78.53420637899631629, 2.418109797047000242 ) ) ;
#20618=CARTESIAN_POINT ( 'NONE',  ( 0.000000000000000000, -3.500000000000000000, -8.500000000000000000 ) ) ;
#20620=CARTESIAN_POINT ( 'NONE',  ( 8.266608573609707022, -17.02766203690127966, -9.697383820329660509 ) ) ;
#20621=DIRECTION ( 'NONE',  ( 0.7071067811865474617, 0.000000000000000000, 0.7071067811865474617 ) ) ;
#20622=DIRECTION ( 'NONE',  ( 0.000000000000000000, -1.000000000000000000, 0.000000000000000000 ) ) ;
#20626=CARTESIAN_POINT ( 'NONE',  ( 1.623944433304999935, -76.08352863036999736, -12.20239005717999881 ) ) ;
#20629=CARTESIAN_POINT ( 'NONE',  ( 10.36292431360000066, -60.00096201600999990, -7.633479737330000070 ) ) ;
#20630=CARTESIAN_POINT ( 'NONE',  ( -10.61911868076999887, -78.48968720768000651, -6.134606423928000041 ) ) ;
#20631=CARTESIAN_POINT ( 'NONE',  ( 12.50000000000000000, -60.04999999657000131, 1.750000000000000000 ) ) ;
#20638=DIRECTION ( 'NONE',  ( -1.000000000000000000, 0.000000000000000000, 0.000000000000000000 ) ) ;
#20640=CARTESIAN_POINT ( 'NONE',  ( -2.418807028576000384, -2.534049145665999703, -2.608992216514999907 ) ) ;
#20644=CARTESIAN_POINT ( 'NONE',  ( -9.730498664387607022, -76.15210458349736200, 6.585771582669669222 ) ) ;
#20648=ORIENTED_EDGE ( 'NONE', *, *, #26789, .T. ) ;
#20649=CARTESIAN_POINT ( 'NONE',  ( 0.000000000000000000, -1.000000000000000000, 0.000000000000000000 ) ) ;
#20652=EDGE_CURVE ( 'NONE', #39067, #55619, #57693, .T. ) ;
#20654=DIRECTION ( 'NONE',  ( 1.000000000000000000, 0.000000000000000000, 0.000000000000000000 ) ) ;
#20655=DIRECTION ( 'NONE',  ( 0.000000000000000000, 1.000000000000000000, 0.000000000000000000 ) ) ;
#20657=CARTESIAN_POINT ( 'NONE',  ( 7.660411364622000008, -18.80826384815000196, -10.01752038683000023 ) ) ;
#20659=VERTEX_POINT ( 'NONE', #10892 ) ;
#20661=AXIS2_PLACEMENT_3D ( 'NONE', #11914, #8336, #35182 ) ;
#20669=CARTESIAN_POINT ( 'NONE',  ( 12.50385649911367558, -61.58436722984664158, 0.8579675320881684497 ) ) ;
#20670=DIRECTION ( 'NONE',  ( -0.7071067811865475727, 0.000000000000000000, -0.7071067811865475727 ) ) ;
#20671=DIRECTION ( 'NONE',  ( 0.000000000000000000, 0.000000000000000000, -1.000000000000000000 ) ) ;
#20675=VERTEX_POINT ( 'NONE', #24456 ) ;
#20678=ORIENTED_EDGE ( 'NONE', *, *, #55095, .T. ) ;
#20679=CARTESIAN_POINT ( 'NONE',  ( 7.659225706236999720, -18.31732796024000010, 9.963487823496000928 ) ) ;
#20683=CARTESIAN_POINT ( 'NONE',  ( 1.811016405462537060, -54.73826444594539709, 12.71771640060721964 ) ) ;
#20684=CARTESIAN_POINT ( 'NONE',  ( 11.60238327475000197, -76.95322811118001027, 5.404242916298000132 ) ) ;
#20686=CARTESIAN_POINT ( 'NONE',  ( 7.646944885454000307, -59.99635956511999524, 10.19022188675999985 ) ) ;
#20687=DIRECTION ( 'NONE',  ( 2.678911359553000079E-11, -1.000000000000000000, -2.678926851037000120E-11 ) ) ;
#20692=LINE ( 'NONE', #52281, #19946 ) ;
#20693=ORIENTED_EDGE ( 'NONE', *, *, #23477, .F. ) ;
#20696=VECTOR ( 'NONE', #30578, 1000.000000000000000 ) ;
#20697=DIRECTION ( 'NONE',  ( -0.7071067811865475727, 0.000000000000000000, -0.7071067811865475727 ) ) ;
#20699=CARTESIAN_POINT ( 'NONE',  ( -7.639893274949090873, -60.18715751166916306, -10.11462445492871787 ) ) ;
#20700=AXIS2_PLACEMENT_3D ( 'NONE', #17865, #35855, #53884 ) ;
#20703=CARTESIAN_POINT ( 'NONE',  ( -5.869402599192000025, -78.36567021304000491, 10.46661899222999992 ) ) ;
#20706=DIRECTION ( 'NONE',  ( -1.000000000000000000, 0.000000000000000000, 0.000000000000000000 ) ) ;
#20707=CARTESIAN_POINT ( 'NONE',  ( -12.50000000000000000, -61.48359816765000119, -1.003641516062000250 ) ) ;
#20710=EDGE_CURVE ( 'NONE', #3549, #52628, #18722, .T. ) ;
#20712=LINE ( 'NONE', #52305, #29479 ) ;
#20716=CARTESIAN_POINT ( 'NONE',  ( 3.342812627361237521, -2.025386568323031433, 1.104663108944964556 ) ) ;
#20724=ORIENTED_EDGE ( 'NONE', *, *, #28645, .F. ) ;
#20725=DIRECTION ( 'NONE',  ( 0.000000000000000000, 0.000000000000000000, -1.000000000000000000 ) ) ;
#20726=CARTESIAN_POINT ( 'NONE',  ( 7.216714108252452853, -77.02036381975230483, 9.394814173648345701 ) ) ;
#20727=CARTESIAN_POINT ( 'NONE',  ( -1.460729357734999789, -60.89091243169999501, -12.44211643244000065 ) ) ;
#20729=EDGE_CURVE ( 'NONE', #4628, #56848, #39360, .T. ) ;
#20732=CARTESIAN_POINT ( 'NONE',  ( 9.835223439032999337, -24.08138927656000305, -7.760980897158999525 ) ) ;
#20733=EDGE_CURVE ( 'NONE', #58285, #53612, #3960, .T. ) ;
#20736=CARTESIAN_POINT ( 'NONE',  ( 11.74786300771494219, -78.44881845960851763, 0.3511192646659174188 ) ) ;
#20738=ORIENTED_EDGE ( 'NONE', *, *, #45034, .F. ) ;
#20742=CARTESIAN_POINT ( 'NONE',  ( 7.919595949288999570, -55.65000000488999632, 8.768124086549999419 ) ) ;
#20743=CARTESIAN_POINT ( 'NONE',  ( -11.75000000000000711, -77.78958333333332575, 1.538071403319954955 ) ) ;
#20744=CARTESIAN_POINT ( 'NONE',  ( -7.686918321195999937, -58.55560170965000566, -10.48771805380999922 ) ) ;
#20745=VECTOR ( 'NONE', #52617, 1000.000000000000000 ) ;
#20749=VERTEX_POINT ( 'NONE', #49735 ) ;
#20750=CARTESIAN_POINT ( 'NONE',  ( 1.667961430005999945, -20.25111654322000021, 12.58335110166999904 ) ) ;
#20752=VERTEX_POINT ( 'NONE', #54729 ) ;
#20754=CARTESIAN_POINT ( 'NONE',  ( -12.54976795928000044, -53.75224499974000025, 0.05636009750359999987 ) ) ;
#20757=CARTESIAN_POINT ( 'NONE',  ( 10.19019669286999985, -23.19643762568000156, 7.646965578493999161 ) ) ;
#20759=DIRECTION ( 'NONE',  ( 0.9999999930530777403, 0.000000000000000000, 0.0001178721535675973718 ) ) ;
#20760=EDGE_CURVE ( 'NONE', #3286, #15875, #5062, .T. ) ;
#20764=EDGE_LOOP ( 'NONE', ( #41481, #2123, #44770, #44487, #22336 ) ) ;
#20769=DIRECTION ( 'NONE',  ( -0.9999999999998321343, 0.000000000000000000, -5.794540613806191565E-07 ) ) ;
#20776=PLANE ( 'NONE',  #18597 ) ;
#20780=CARTESIAN_POINT ( 'NONE',  ( 1.799502287743000029, -23.30716934606000024, -12.60413652831999975 ) ) ;
#20781=CIRCLE ( 'NONE', #4769, 0.8000000000000011546 ) ;
#20782=CARTESIAN_POINT ( 'NONE',  ( 7.919595949288999570, -55.65000000893999754, 9.050966798898000931 ) ) ;
#20783=CARTESIAN_POINT ( 'NONE',  ( 1.576170184332999824, -17.83913032783999952, -12.55466896104999996 ) ) ;
#20784=CARTESIAN_POINT ( 'NONE',  ( 11.75000000000000000, -75.95000000000000284, 0.000000000000000000 ) ) ;
#20786=CARTESIAN_POINT ( 'NONE',  ( -8.190859204290999784, -55.64999999967000122, -7.342331066867000544 ) ) ;
#20787=CARTESIAN_POINT ( 'NONE',  ( 1.271520795309928120, -1.404249853560488814, -3.289139988056414943 ) ) ;
#20790=DIRECTION ( 'NONE',  ( 0.000000000000000000, -1.000000000000000000, 0.000000000000000000 ) ) ;
#20792=CARTESIAN_POINT ( 'NONE',  ( -1.611853968441999907, -2.220016836959000539, -3.270131938172000208 ) ) ;
#20797=CARTESIAN_POINT ( 'NONE',  ( 0.000000000000000000, -5.899999999999999467, 0.000000000000000000 ) ) ;
#20799=DIRECTION ( 'NONE',  ( 1.205461585547979389E-11, 1.868136279038964309E-07, -0.9999999999999824585 ) ) ;
#20801=CARTESIAN_POINT ( 'NONE',  ( 7.853292460675339370, -76.38309044374258860, -8.740604184407734678 ) ) ;
#20806=DIRECTION ( 'NONE',  ( -1.000000000000000000, 0.000000000000000000, 0.000000000000000000 ) ) ;
#20807=CARTESIAN_POINT ( 'NONE',  ( -1.735649827337248263, -0.8020833187308676893, -3.013068263282779213 ) ) ;
#20809=CARTESIAN_POINT ( 'NONE',  ( -8.803761571656083973, -16.78431590349724445, -9.164326402687485995 ) ) ;
#20810=ADVANCED_FACE ( 'NONE', ( #454 ), #20535, .F. ) ;
#20811=VERTEX_POINT ( 'NONE', #165 ) ;
#20816=CARTESIAN_POINT ( 'NONE',  ( -0.2678032735367172346, -25.21432775288745276, 12.70526550769160323 ) ) ;
#20819=ORIENTED_EDGE ( 'NONE', *, *, #11193, .F. ) ;
#20820=AXIS2_PLACEMENT_3D ( 'NONE', #37679, #42703, #28220 ) ;
#20822=CARTESIAN_POINT ( 'NONE',  ( -5.917523019358058356, -77.38333333333329733, -10.26699006316253282 ) ) ;
#20826=ORIENTED_EDGE ( 'NONE', *, *, #29733, .T. ) ;
#20828=CARTESIAN_POINT ( 'NONE',  ( -11.75000000000000000, -78.20000000000000284, 1.702919296826999607E-14 ) ) ;
#20832=DIRECTION ( 'NONE',  ( -9.149080738879000281E-11, 1.000000000000000000, 8.583834452030000788E-10 ) ) ;
#20837=EDGE_CURVE ( 'NONE', #31027, #19156, #25246, .T. ) ;
#20838=CARTESIAN_POINT ( 'NONE',  ( -5.917523019358107206, -77.21666666666666856, 10.26699006316250795 ) ) ;
#20840=EDGE_CURVE ( 'NONE', #3891, #46308, #36136, .T. ) ;
#20846=CARTESIAN_POINT ( 'NONE',  ( -0.3037430299689138358, -2.982705603859970633, 3.237211740786743785 ) ) ;
#20850=CARTESIAN_POINT ( 'NONE',  ( -8.096452064242996016, -59.58578169018998949, 13.15643568217000769 ) ) ;
#20852=CARTESIAN_POINT ( 'NONE',  ( -8.587885547135288178, -76.25922932029355650, -8.019350720283787481 ) ) ;
#20853=CARTESIAN_POINT ( 'NONE',  ( 10.55911395186000057, -22.78461666469000235, 7.642160924865000204 ) ) ;
#20854=CARTESIAN_POINT ( 'NONE',  ( -9.389195554442999025, -61.51043214172000262, -8.194863653299998774 ) ) ;
#20856=CARTESIAN_POINT ( 'NONE',  ( 10.35845616728999907, -60.09778595451999905, 7.627487606627999739 ) ) ;
#20857=B_SPLINE_CURVE_WITH_KNOTS ( 'NONE', 3,
 ( #40613, #211, #27016, #53907, #22893, #54491, #40904, #8728, #36180, #50066, #31136, #23186, #31732, #49479, #4001, #13734, #49175, #18473 ),
 .UNSPECIFIED., .F., .F.,
 ( 4, 2, 2, 2, 2, 2, 2, 2, 4 ),
 ( 0.000000000000000000, 0.06250000000000185962, 0.1250000000000037192, 0.2500000000000024980, 0.5000000000000000000, 0.7499999999999974465, 0.8124999999999968914, 0.8749999999999962252, 1.000000000000000000 ),
 .UNSPECIFIED. ) ;
#20858=TOROIDAL_SURFACE ( 'NONE', #53867, 26.50000000000000000, 14.00000000000000000 ) ;
#20860=CARTESIAN_POINT ( 'NONE',  ( -3.346450045594000056, -76.91303030157000364, 12.57540552286999791 ) ) ;
#20864=LINE ( 'NONE', #8156, #50890 ) ;
#20865=CARTESIAN_POINT ( 'NONE',  ( 4.394064475695000027, -76.23537712840000324, -11.55491662800999997 ) ) ;
#20870=CARTESIAN_POINT ( 'NONE',  ( 10.61187473961000016, -78.96149350880999407, -6.572462896270000243 ) ) ;
#20871=CARTESIAN_POINT ( 'NONE',  ( 0.000000000000000000, -72.89999999999999147, 0.000000000000000000 ) ) ;
#20875=DIRECTION ( 'NONE',  ( 0.000000000000000000, -1.000000000000000000, 9.237395726959999468E-14 ) ) ;
#20880=ORIENTED_EDGE ( 'NONE', *, *, #2040, .T. ) ;
#20882=CARTESIAN_POINT ( 'NONE',  ( 12.64502302235999842, -56.02870851050000311, 1.799490220168999954 ) ) ;
#20884=ORIENTED_EDGE ( 'NONE', *, *, #12944, .F. ) ;
#20886=ORIENTED_EDGE ( 'NONE', *, *, #22557, .F. ) ;
#20889=CARTESIAN_POINT ( 'NONE',  ( 11.75000000000000000, -77.95000000000000284, 2.316376715183999699E-14 ) ) ;
#20892=EDGE_LOOP ( 'NONE', ( #27105, #14130, #9061, #7876 ) ) ;
#20893=CARTESIAN_POINT ( 'NONE',  ( 12.43640296263000167, -53.88252466098000326, -0.05222744260233999625 ) ) ;
#20895=VERTEX_POINT ( 'NONE', #19887 ) ;
#20896=VECTOR ( 'NONE', #34824, 999.9999999999998863 ) ;
#20897=CARTESIAN_POINT ( 'NONE',  ( 11.81418954875000082, -78.82161355975632944, 3.289986436736999753 ) ) ;
#20899=AXIS2_PLACEMENT_3D ( 'NONE', #24956, #42396, #50680 ) ;
#20900=CARTESIAN_POINT ( 'NONE',  ( 9.788022091658000079, -54.27120090369999872, 7.956349397036000859 ) ) ;
#20901=CARTESIAN_POINT ( 'NONE',  ( 9.689263856525805352, -17.02111184948868328, -8.274777959192654464 ) ) ;
#20908=CARTESIAN_POINT ( 'NONE',  ( -7.618394338636999663, -23.22713821270000167, 10.53494418059000104 ) ) ;
#20909=CARTESIAN_POINT ( 'NONE',  ( 11.75000000000000000, -78.54999999999999716, 0.000000000000000000 ) ) ;
#20911=CARTESIAN_POINT ( 'NONE',  ( 10.53562597590999950, -60.00558297591999946, -7.620013358898000355 ) ) ;
#20912=CARTESIAN_POINT ( 'NONE',  ( -11.38660623898999980, -78.97827941498000826, -4.554589311945999697 ) ) ;
#20914=CARTESIAN_POINT ( 'NONE',  ( -7.356278612544759454, -60.10416868444603722, -8.178338515874420622 ) ) ;
#20915=CARTESIAN_POINT ( 'NONE',  ( 3.229154007622224931, -78.40340539145115883, 11.62820000353926986 ) ) ;
#20916=DIRECTION ( 'NONE',  ( 1.000000000000000000, 0.000000000000000000, 0.000000000000000000 ) ) ;
#20920=CARTESIAN_POINT ( 'NONE',  ( 12.59651352883999920, -60.19056208351000237, -1.801710201210000140 ) ) ;
#20921=FACE_OUTER_BOUND ( 'NONE', #33270, .T. ) ;
#20922=CYLINDRICAL_SURFACE ( 'NONE', #8738, 0.5000000000000006661 ) ;
#20924=CARTESIAN_POINT ( 'NONE',  ( 1.977932612850999972, -2.640452063625000179, -2.957236955477999807 ) ) ;
#20927=CARTESIAN_POINT ( 'NONE',  ( 0.03141490047175235500, -75.80000000000001137, 12.11027917007127463 ) ) ;
#20930=DIRECTION ( 'NONE',  ( -0.9999548435846228323, 0.000000000000000000, -0.009503199022040218977 ) ) ;
#20931=EDGE_LOOP ( 'NONE', ( #30599, #45864, #51413 ) ) ;
#20936=CARTESIAN_POINT ( 'NONE',  ( -3.250000000000000000, -2.000000000000000000, 0.000000000000000000 ) ) ;
#20937=CARTESIAN_POINT ( 'NONE',  ( -0.6280215140811999941, -0.7428930985899000472, -3.647896628088999726 ) ) ;
#20940=CARTESIAN_POINT ( 'NONE',  ( -12.70253230845862724, -53.82944272754753001, -0.9891673677568084688 ) ) ;
#20941=ORIENTED_EDGE ( 'NONE', *, *, #13103, .T. ) ;
#20946=CARTESIAN_POINT ( 'NONE',  ( -10.53003236235000095, -60.12452273675999947, -7.612971540294999784 ) ) ;
#20948=VECTOR ( 'NONE', #861, 1000.000000000000114 ) ;
#20949=VERTEX_POINT ( 'NONE', #51193 ) ;
#20952=CARTESIAN_POINT ( 'NONE',  ( 1.799502287691000069, -55.49283319101999723, -12.60413670417000098 ) ) ;
#20955=ADVANCED_FACE ( 'NONE', ( #10444 ), #38171, .F. ) ;
#20956=CARTESIAN_POINT ( 'NONE',  ( 12.70259395223311039, -54.06112126473090740, -1.314575638816234182 ) ) ;
#20958=ORIENTED_EDGE ( 'NONE', *, *, #4029, .T. ) ;
#20961=ADVANCED_FACE ( 'NONE', ( #6005 ), #46776, .F. ) ;
#20963=CARTESIAN_POINT ( 'NONE',  ( 9.523369619462000557, -17.18054357685999989, 8.220347091616000412 ) ) ;
#20965=CARTESIAN_POINT ( 'NONE',  ( 0.000000000000000000, -2.660000000000000142, 0.000000000000000000 ) ) ;
#20966=CARTESIAN_POINT ( 'NONE',  ( 1.217390015638971645, -53.98106975037926958, 12.70229597936534560 ) ) ;
#20967=CARTESIAN_POINT ( 'NONE',  ( -1.316656843623999817, -78.28533949426000049, -12.73088833989999991 ) ) ;
#20974=ORIENTED_EDGE ( 'NONE', *, *, #53205, .T. ) ;
#20975=CARTESIAN_POINT ( 'NONE',  ( 7.709154088362968338, -54.87253195859279487, -9.998702477015203982 ) ) ;
#20984=DIRECTION ( 'NONE',  ( 0.000000000000000000, 1.000000000000000000, 0.000000000000000000 ) ) ;
#20986=CARTESIAN_POINT ( 'NONE',  ( -12.50000000000000000, -61.48359816765000119, -1.003641516062000250 ) ) ;
#20987=LINE ( 'NONE', #39569, #47976 ) ;
#20988=CARTESIAN_POINT ( 'NONE',  ( -7.642160924865000204, -22.78461666469000235, 10.55911395186000057 ) ) ;
#20990=CARTESIAN_POINT ( 'NONE',  ( 10.04115011118000211, -22.76486430425999785, -7.682331425175999762 ) ) ;
#20992=PLANE ( 'NONE',  #19654 ) ;
#20994=ORIENTED_EDGE ( 'NONE', *, *, #29485, .T. ) ;
#20997=CARTESIAN_POINT ( 'NONE',  ( -3.235440615655987617, -2.008688020932666518, -0.3548227715288363449 ) ) ;
#20999=CARTESIAN_POINT ( 'NONE',  ( -12.72966282071492472, -18.23110224986362837, 1.931329623869561862 ) ) ;
#21001=CARTESIAN_POINT ( 'NONE',  ( -3.412661197378369593, -2.269647688907610927, -0.8619490756354352134 ) ) ;
#21005=CARTESIAN_POINT ( 'NONE',  ( 11.52686684160662267, -75.96526634729282534, 2.278194760864160173 ) ) ;
#21007=ORIENTED_EDGE ( 'NONE', *, *, #204, .F. ) ;
#21010=CARTESIAN_POINT ( 'NONE',  ( -11.75000000000000000, -77.20000000000000284, -1.435311119447000145E-14 ) ) ;
#21011=CARTESIAN_POINT ( 'NONE',  ( -0.5999999999999999778, -23.15000000000999947, 11.79999999999999893 ) ) ;
#21015=CARTESIAN_POINT ( 'NONE',  ( 10.48774103545000003, -57.04527981721000174, -7.686941364801000098 ) ) ;
#21019=CARTESIAN_POINT ( 'NONE',  ( 1.980584515756000030, -60.06485150062000145, 12.76303204342999997 ) ) ;
#21020=ORIENTED_EDGE ( 'NONE', *, *, #19809, .T. ) ;
#21021=EDGE_CURVE ( 'NONE', #55921, #18184, #28724, .T. ) ;
#21028=LINE ( 'NONE', #11607, #56689 ) ;
#21029=VECTOR ( 'NONE', #58382, 1000.000000000000000 ) ;
#21034=CYLINDRICAL_SURFACE ( 'NONE', #23563, 12.90000000000000036 ) ;
#21036=FACE_OUTER_BOUND ( 'NONE', #20139, .T. ) ;
#21039=CARTESIAN_POINT ( 'NONE',  ( -12.77306291382000047, -53.74129324268999852, -1.041150512314999999 ) ) ;
#21046=AXIS2_PLACEMENT_3D ( 'NONE', #18201, #45947, #54211 ) ;
#21054=EDGE_CURVE ( 'NONE', #9689, #51555, #56192, .T. ) ;
#21055=CARTESIAN_POINT ( 'NONE',  ( -12.78037829250999913, -61.09316779356999660, -1.812823010630000065 ) ) ;
#21058=CARTESIAN_POINT ( 'NONE',  ( 8.792818914745540226, -62.02696626405479208, 9.175540344916807811 ) ) ;
#21066=FACE_OUTER_BOUND ( 'NONE', #55832, .T. ) ;
#21067=CARTESIAN_POINT ( 'NONE',  ( -10.18949731070999931, -18.78470987703000006, -7.645392562261999814 ) ) ;
#21068=CARTESIAN_POINT ( 'NONE',  ( 7.678667886039000301, -58.55736537918999574, 10.59548767697000038 ) ) ;
#21069=CARTESIAN_POINT ( 'NONE',  ( -0.005523896503903000417, -16.93036543774000080, -12.55021156880999911 ) ) ;
#21070=EDGE_CURVE ( 'NONE', #49814, #55458, #41445, .T. ) ;
#21071=CARTESIAN_POINT ( 'NONE',  ( -9.369164850722000892, -60.04999999966999980, 7.601397897754999633 ) ) ;
#21074=CARTESIAN_POINT ( 'NONE',  ( -12.50745077485999879, -53.80005551680000053, 2.011910316382000212E-09 ) ) ;
#21076=ORIENTED_EDGE ( 'NONE', *, *, #36998, .T. ) ;
#21077=CARTESIAN_POINT ( 'NONE',  ( -1.456717367586000012E-14, -79.29999999999999716, 0.000000000000000000 ) ) ;
#21078=VECTOR ( 'NONE', #20347, 1000.000000000000114 ) ;
#21080=CARTESIAN_POINT ( 'NONE',  ( 7.686918321221999584, -20.24439829127999957, -10.48771805383000100 ) ) ;
#21081=CARTESIAN_POINT ( 'NONE',  ( 2.732748911140999937, -3.323893098590000150, -2.413281231417000239 ) ) ;
#21083=CARTESIAN_POINT ( 'NONE',  ( -12.66322081666000088, -53.61838367289999496, 0.1487102037790999920 ) ) ;
#21085=CARTESIAN_POINT ( 'NONE',  ( -1.636761686205420396, -3.083333333333333925, -2.839805762151339508 ) ) ;
#21086=B_SPLINE_CURVE_WITH_KNOTS ( 'NONE', 3,
 ( #44881, #43725, #21269, #13572, #4136, #53738 ),
 .UNSPECIFIED., .F., .F.,
 ( 4, 2, 4 ),
 ( 0.000000000000000000, 0.5000000000000000000, 1.000000000000000000 ),
 .UNSPECIFIED. ) ;
#21087=AXIS2_PLACEMENT_3D ( 'NONE', #17133, #18242, #36522 ) ;
#21088=DIRECTION ( 'NONE',  ( 1.000000000000000000, 0.000000000000000000, 0.000000000000000000 ) ) ;
#21093=CARTESIAN_POINT ( 'NONE',  ( 9.768846781487011910, -76.40261481437684665, -6.528746261247764693 ) ) ;
#21096=LINE ( 'NONE', #3101, #40617 ) ;
#21099=CARTESIAN_POINT ( 'NONE',  ( 1.496667148433702188, -3.438256644742763601, 2.927442453955206414 ) ) ;
#21102=CARTESIAN_POINT ( 'NONE',  ( -10.36746145411166431, -18.23400545010064633, -7.635225828759649502 ) ) ;
#21106=CARTESIAN_POINT ( 'NONE',  ( -13.86363636363000218, -46.43897132165000130, -1.277887489420000009E-05 ) ) ;
#21108=DIRECTION ( 'NONE',  ( 0.5721800015181066623, -0.8201280667449074580, 0.000000000000000000 ) ) ;
#21109=ORIENTED_EDGE ( 'NONE', *, *, #6751, .T. ) ;
#21111=FACE_OUTER_BOUND ( 'NONE', #46044, .T. ) ;
#21112=ORIENTED_EDGE ( 'NONE', *, *, #19590, .T. ) ;
#21118=ORIENTED_EDGE ( 'NONE', *, *, #47517, .F. ) ;
#21120=ORIENTED_EDGE ( 'NONE', *, *, #460, .F. ) ;
#21122=CARTESIAN_POINT ( 'NONE',  ( -10.98521938008736853, -18.65929923595803785, 0.5702549022851668425 ) ) ;
#21124=CARTESIAN_POINT ( 'NONE',  ( -8.190859204290999784, -59.94999999967000548, 7.342331066867000544 ) ) ;
#21127=FACE_OUTER_BOUND ( 'NONE', #8924, .T. ) ;
#21132=CARTESIAN_POINT ( 'NONE',  ( 2.252478813166476801, -2.914525471928731459, 2.342577926442860559 ) ) ;
#21136=DIRECTION ( 'NONE',  ( 0.000000000000000000, 0.000000000000000000, -1.000000000000000000 ) ) ;
#21139=CARTESIAN_POINT ( 'NONE',  ( -1.209804193477999945, -2.381925387468999400, -3.608664049297999998 ) ) ;
#21140=CARTESIAN_POINT ( 'NONE',  ( -1.247385801055000076, -17.52277743740000204, 12.50301438876999960 ) ) ;
#21141=CARTESIAN_POINT ( 'NONE',  ( -8.533826143255001995, -61.80526450216999734, -9.213084459936000670 ) ) ;
#21142=EDGE_CURVE ( 'NONE', #37515, #48410, #2626, .T. ) ;
#21145=CARTESIAN_POINT ( 'NONE',  ( -12.66313295597999833, -16.82196533882000011, 0.06049275240485999655 ) ) ;
#21146=CARTESIAN_POINT ( 'NONE',  ( 11.79660191402999914, -76.83668768631000034, 5.494707494196000575 ) ) ;
#21149=CARTESIAN_POINT ( 'NONE',  ( -12.50745077494999968, -61.79994448255000350, -2.661703094427999907E-09 ) ) ;
#21150=CARTESIAN_POINT ( 'NONE',  ( 8.559075968402000356, -75.76731679589001089, -8.919964875508998858 ) ) ;
#21151=VERTEX_POINT ( 'NONE', #44056 ) ;
#21152=ADVANCED_FACE ( 'NONE', ( #21036 ), #3532, .F. ) ;
#21154=CARTESIAN_POINT ( 'NONE',  ( 5.865376297750441863E-14, -72.84999999994899156, 13.94999999994999840 ) ) ;
#21155=CARTESIAN_POINT ( 'NONE',  ( 12.83677138650999972, -60.02737696024999536, 2.062839765282999949 ) ) ;
#21156=CARTESIAN_POINT ( 'NONE',  ( -1.806885568419999810, -79.19518329857000083, -12.66522665019000016 ) ) ;
#21162=ORIENTED_EDGE ( 'NONE', *, *, #45263, .F. ) ;
#21167=ORIENTED_EDGE ( 'NONE', *, *, #38310, .F. ) ;
#21170=CARTESIAN_POINT ( 'NONE',  ( -7.555116226631051646, -55.11315380193744318, -7.995796640820927337 ) ) ;
#21174=ORIENTED_EDGE ( 'NONE', *, *, #43404, .T. ) ;
#21179=CIRCLE ( 'NONE', #54198, 5.000000000000000000 ) ;
#21181=CARTESIAN_POINT ( 'NONE',  ( 12.66314509266000066, -53.62135249290999894, -0.04032083120558000583 ) ) ;
#21182=EDGE_LOOP ( 'NONE', ( #3400, #38315, #527, #938, #50027, #41643 ) ) ;
#21186=CARTESIAN_POINT ( 'NONE',  ( 10.52693198617000014, -55.37847693893999690, 7.606025555747000233 ) ) ;
#21190=CIRCLE ( 'NONE', #37211, 0.5999999999999999778 ) ;
#21194=CARTESIAN_POINT ( 'NONE',  ( -7.633089125616000281, -23.39007426303999893, 10.18115018432999896 ) ) ;
#21197=CARTESIAN_POINT ( 'NONE',  ( -12.77649734584999841, -16.69171487512999974, -0.06478328530401999963 ) ) ;
#21205=CARTESIAN_POINT ( 'NONE',  ( -12.50000000000000000, -60.04999999725999515, 1.750000000000000000 ) ) ;
#21206=CARTESIAN_POINT ( 'NONE',  ( -3.020029971748000364, -3.012862276481999668, -1.880661267551000160 ) ) ;
#21209=DIRECTION ( 'NONE',  ( 0.6562721000481037681, -0.7545243075597046767, 7.874481590556048732E-10 ) ) ;
#21210=CARTESIAN_POINT ( 'NONE',  ( -7.836763323857902641, -17.69488832272180900, 9.850488778970195369 ) ) ;
#21214=EDGE_CURVE ( 'NONE', #25466, #2738, #55780, .T. ) ;
#21215=DIRECTION ( 'NONE',  ( 1.000000000000000000, 0.000000000000000000, 0.000000000000000000 ) ) ;
#21217=CIRCLE ( 'NONE', #37232, 0.5000000000000001110 ) ;
#21219=B_SPLINE_CURVE_WITH_KNOTS ( 'NONE', 3,
 ( #52530, #7081, #25082, #12087, #48401, #34211, #51685, #33645, #38657, #24798, #25651, #20940, #39231, #20089, #15648, #16232 ),
 .UNSPECIFIED., .F., .F.,
 ( 4, 2, 2, 2, 2, 2, 2, 4 ),
 ( 0.000000000000000000, 0.2499999999999956701, 0.3749999999999965028, 0.4374999999999968914, 0.4999999999999973355, 0.6249999999999980016, 0.7499999999999987788, 1.000000000000000000 ),
 .UNSPECIFIED. ) ;
#21220=B_SPLINE_CURVE_WITH_KNOTS ( 'NONE', 3,
 ( #10700, #1847, #24263, #46429, #9522, #5664, #1266, #50268, #41687, #28676, #36670, #5959, #54686, #15103, #41980, #27509 ),
 .UNSPECIFIED., .F., .F.,
 ( 4, 2, 2, 2, 2, 2, 2, 4 ),
 ( 0.000000000000000000, 0.2500000000000092704, 0.3750000000000126565, 0.5000000000000160982, 0.6250000000000195399, 0.6875000000000184297, 0.7500000000000172085, 1.000000000000000000 ),
 .UNSPECIFIED. ) ;
#21222=CARTESIAN_POINT ( 'NONE',  ( -7.605690822197999523, -60.22565082124000213, 10.52682217037000001 ) ) ;
#21223=CARTESIAN_POINT ( 'NONE',  ( -3.110062099568999816, -0.6770460165488999538, -2.005045321468000186 ) ) ;
#21225=FACE_OUTER_BOUND ( 'NONE', #57477, .T. ) ;
#21228=CARTESIAN_POINT ( 'NONE',  ( -12.70249541834471074, -53.83496187168930902, 0.9988462571234606457 ) ) ;
#21230=CARTESIAN_POINT ( 'NONE',  ( -3.587712099295000012, -1.710945589986999860, 1.801380527025000067 ) ) ;
#21232=LINE ( 'NONE', #16814, #53524 ) ;
#21236=EDGE_CURVE ( 'NONE', #19368, #7896, #23352, .T. ) ;
#21237=ORIENTED_EDGE ( 'NONE', *, *, #1578, .T. ) ;
#21243=ORIENTED_EDGE ( 'NONE', *, *, #6554, .T. ) ;
#21248=VERTEX_POINT ( 'NONE', #43480 ) ;
#21249=ADVANCED_FACE ( 'NONE', ( #25461 ), #57771, .F. ) ;
#21252=CARTESIAN_POINT ( 'NONE',  ( -12.50000000000000000, -51.86282895648000135, 0.000000000000000000 ) ) ;
#21253=CARTESIAN_POINT ( 'NONE',  ( -3.040431873813000063, -78.64994354880001026, 12.26916943822000050 ) ) ;
#21258=VECTOR ( 'NONE', #24353, 1000.000000000000000 ) ;
#21260=ORIENTED_EDGE ( 'NONE', *, *, #13124, .F. ) ;
#21266=DIRECTION ( 'NONE',  ( 0.000000000000000000, -1.000000000000000000, 0.000000000000000000 ) ) ;
#21269=CARTESIAN_POINT ( 'NONE',  ( 12.50657384757278479, -53.82752583170963590, -0.3552644803360501813 ) ) ;
#21270=DIRECTION ( 'NONE',  ( 0.7071067811865474617, 0.000000000000000000, -0.7071067811865474617 ) ) ;
#21271=CARTESIAN_POINT ( 'NONE',  ( -12.71798280854999952, -18.70221404512000163, -1.931086388455000025 ) ) ;
#21275=CARTESIAN_POINT ( 'NONE',  ( 10.24996238026999862, -21.75171076523999858, -7.705119999407000542 ) ) ;
#21279=EDGE_LOOP ( 'NONE', ( #44264, #36364, #10824, #54336, #32000 ) ) ;
#21284=CARTESIAN_POINT ( 'NONE',  ( -12.70610308059024440, -17.54479009146447765, 1.580620443413589982 ) ) ;
#21289=CARTESIAN_POINT ( 'NONE',  ( -1.667269374601999976, -55.59060116482999803, -12.49858097728999873 ) ) ;
#21290=CYLINDRICAL_SURFACE ( 'NONE', #36581, 1.750000000000001332 ) ;
#21291=CARTESIAN_POINT ( 'NONE',  ( 11.32560461271045149, -75.97108467502835083, 3.151449499211164351 ) ) ;
#21294=CARTESIAN_POINT ( 'NONE',  ( -8.971989909486167036, -78.64261696927431444, 7.658931699842775664 ) ) ;
#21295=EDGE_CURVE ( 'NONE', #12596, #51331, #49752, .T. ) ;
#21296=PLANE ( 'NONE',  #2189 ) ;
#21299=ADVANCED_FACE ( 'NONE', ( #40782, #17468 ), #17177, .T. ) ;
#21301=CARTESIAN_POINT ( 'NONE',  ( 3.599999993293999889, -0.2000000067061999953, 5.600095136020000205E-09 ) ) ;
#21303=CARTESIAN_POINT ( 'NONE',  ( 3.417874729156432867, -78.54962478900189637, 11.24133698585978891 ) ) ;
#21305=ORIENTED_EDGE ( 'NONE', *, *, #56889, .T. ) ;
#21308=CARTESIAN_POINT ( 'NONE',  ( -7.601397897754999633, -60.04999999725999515, 10.07627163191000008 ) ) ;
#21309=ADVANCED_FACE ( 'NONE', ( #31025 ), #31798, .F. ) ;
#21311=CARTESIAN_POINT ( 'NONE',  ( -3.075537641221584018, -77.69583333333332575, 11.44417895085269876 ) ) ;
#21315=AXIS2_PLACEMENT_3D ( 'NONE', #36252, #18258, #46013 ) ;
#21317=VECTOR ( 'NONE', #41423, 1000.000000000000114 ) ;
#21318=CARTESIAN_POINT ( 'NONE',  ( -12.70299718804919742, -61.82583482774937522, -0.8845454260942260394 ) ) ;
#21320=DIRECTION ( 'NONE',  ( 0.000000000000000000, -1.000000000000000000, 0.000000000000000000 ) ) ;
#21321=ORIENTED_EDGE ( 'NONE', *, *, #10634, .F. ) ;
#21322=CONICAL_SURFACE ( 'NONE', #44085, 13.89999999994999946, 0.7853981633972997312 ) ;
#21326=CARTESIAN_POINT ( 'NONE',  ( 11.03890801094999929, -78.76613151614000685, -5.342433469444999972 ) ) ;
#21327=EDGE_LOOP ( 'NONE', ( #19130, #42947, #45243 ) ) ;
#21333=VERTEX_POINT ( 'NONE', #8319 ) ;
#21339=CARTESIAN_POINT ( 'NONE',  ( -12.83677138650999972, -60.02737696024999536, -2.062839765282999949 ) ) ;
#21341=CARTESIAN_POINT ( 'NONE',  ( 7.627487606607999737, -18.70221404512000163, 10.35845616727999996 ) ) ;
#21342=CARTESIAN_POINT ( 'NONE',  ( 0.000000000000000000, -55.54999999966999980, 12.50000000000000000 ) ) ;
#21345=CARTESIAN_POINT ( 'NONE',  ( 12.54715396801999994, -17.46815137273999952, -1.292200816715999956 ) ) ;
#21348=VERTEX_POINT ( 'NONE', #13321 ) ;
#21349=CARTESIAN_POINT ( 'NONE',  ( -8.478741751108000102, -53.92187496570999627, 9.108230428579000559 ) ) ;
#21351=CARTESIAN_POINT ( 'NONE',  ( -8.194873807832001589, -17.28956116771000140, -9.389185139535999980 ) ) ;
#21352=CARTESIAN_POINT ( 'NONE',  ( 7.613962827161000035, -55.49360374314999689, 10.53101998745000145 ) ) ;
#21353=CARTESIAN_POINT ( 'NONE',  ( 7.601397897754999633, -18.75000000240999753, 10.07627163191000008 ) ) ;
#21355=DIRECTION ( 'NONE',  ( 0.009503199022040095811, 0.000000000000000000, -0.9999548435846228323 ) ) ;
#21357=CARTESIAN_POINT ( 'NONE',  ( 0.2424258809980906204, -3.499999999999999556, 3.292477318001853170 ) ) ;
#21361=CARTESIAN_POINT ( 'NONE',  ( -3.172909266784524451, -3.500000000000001332, -1.019795895214234083 ) ) ;
#21362=CARTESIAN_POINT ( 'NONE',  ( -2.061613410425999771, -55.59429985491999560, 12.83797036852999796 ) ) ;
#21364=VECTOR ( 'NONE', #49401, 1000.000000000000000 ) ;
#21365=CARTESIAN_POINT ( 'NONE',  ( -1.820775719418999739, -3.635837631243000079, 3.058566008963000016 ) ) ;
#21368=CARTESIAN_POINT ( 'NONE',  ( -12.44209697057999975, -54.71557297424000410, 1.464771213333999844 ) ) ;
#21370=CARTESIAN_POINT ( 'NONE',  ( -0.005119011379994000376, -61.73813862155999743, 12.43705489347999915 ) ) ;
#21371=CARTESIAN_POINT ( 'NONE',  ( 12.70556836352000118, -62.02772277195000328, 2.424222323408999617E-09 ) ) ;
#21374=CARTESIAN_POINT ( 'NONE',  ( -5.101716603136247308, -77.04332471689124873, -10.93886256472661778 ) ) ;
#21375=ADVANCED_FACE ( 'NONE', ( #26319 ), #46002, .F. ) ;
#21376=CARTESIAN_POINT ( 'NONE',  ( 8.298649457567281118, -76.38737123282477626, -8.318302812671584334 ) ) ;
#21379=CARTESIAN_POINT ( 'NONE',  ( -1.327657890597083279, -1.010175696052641348, 2.983557525922736708 ) ) ;
#21380=ADVANCED_FACE ( 'NONE', ( #44634 ), #36348, .T. ) ;
#21383=CARTESIAN_POINT ( 'NONE',  ( -0.8982906067046061427, -0.8151041484501103662, -3.345820488051431507 ) ) ;
#21385=B_SPLINE_CURVE_WITH_KNOTS ( 'NONE', 3,
 ( #18386, #13941, #31937, #23095, #50269, #49980, #9523, #45551, #18679, #41106, #54971, #697, #27801, #45847, #983, #18967, #10991, #56435 ),
 .UNSPECIFIED., .F., .F.,
 ( 4, 2, 2, 2, 2, 2, 2, 2, 4 ),
 ( 0.000000000000000000, 0.06249999999999567013, 0.1249999999999913403, 0.2499999999999929501, 0.4999999999999955591, 0.7499999999999991118, 0.8125000000000019984, 0.8750000000000048850, 1.000000000000000000 ),
 .UNSPECIFIED. ) ;
#21387=CARTESIAN_POINT ( 'NONE',  ( 6.031068391564602393, -75.80000000000002558, 10.45132295220961538 ) ) ;
#21391=CARTESIAN_POINT ( 'NONE',  ( -10.98384481689545034, -23.22882187213843963, -0.5959944459583164100 ) ) ;
#21392=ORIENTED_EDGE ( 'NONE', *, *, #1146, .T. ) ;
#21393=CARTESIAN_POINT ( 'NONE',  ( -0.5222397221919125032, -25.16298219400451686, 12.70447686583787572 ) ) ;
#21395=CARTESIAN_POINT ( 'NONE',  ( 10.12290050122000018, -55.54999999974999980, -7.648026767069000087 ) ) ;
#21396=CIRCLE ( 'NONE', #34583, 12.90000000000000036 ) ;
#21397=VERTEX_POINT ( 'NONE', #17768 ) ;
#21398=CARTESIAN_POINT ( 'NONE',  ( 1.800092392015347098, -3.500000000000000000, -3.095232311630156108 ) ) ;
#21401=CIRCLE ( 'NONE', #56269, 1.749999999999997780 ) ;
#21402=B_SPLINE_SURFACE_WITH_KNOTS ( 'NONE', 3, 3, ( 
 ( #36449, #50923, #54478, #37324 ),
 ( #14594, #18746, #14013, #32011 ),
 ( #50340, #9891, #9598, #45627 ),
 ( #769, #27873, #45918, #5453 ),
 ( #37032, #55046, #57864, #29829 ),
 ( #17418, #35404, #16853, #25415 ),
 ( #3279, #21271, #57570, #16279 ),
 ( #34259, #52291, #39278, #44289 ) ),
 .UNSPECIFIED., .F., .F., .F.,
 ( 4, 1, 1, 1, 1, 4 ),
 ( 4, 4 ),
 ( -0.01200407347463999970, 0.000000000000000000, 0.3333333333333000081, 0.6666666666667000474, 1.000000000000000000, 1.011997855551999947 ),
 ( -0.3559705542741000150, 1.355970554273999928 ),
 .UNSPECIFIED. ) ;
#21405=VERTEX_POINT ( 'NONE', #9201 ) ;
#21406=CARTESIAN_POINT ( 'NONE',  ( 9.070041738308999513, -79.31372763096999279, 8.129404524763000239 ) ) ;
#21410=DIRECTION ( 'NONE',  ( 0.000000000000000000, -1.000000000000000000, 0.000000000000000000 ) ) ;
#21412=CARTESIAN_POINT ( 'NONE',  ( 3.708203932500000022, -75.80000000000001137, 11.41267819554000162 ) ) ;
#21415=DIRECTION ( 'NONE',  ( -4.762495317921000031E-11, 1.000000000000000000, -4.762546956201999894E-11 ) ) ;
#21419=CARTESIAN_POINT ( 'NONE',  ( -1.349038754591999956, -78.12242034399000090, -13.04399231589999886 ) ) ;
#21421=CARTESIAN_POINT ( 'NONE',  ( 11.69353635062999963, -78.11477256742000463, 5.202647212677000255 ) ) ;
#21423=CARTESIAN_POINT ( 'NONE',  ( -1.276771495430000038E-14, -69.50420297070000686, 0.000000000000000000 ) ) ;
#21427=CARTESIAN_POINT ( 'NONE',  ( 2.056655112429589760, -2.920778328515915678, 2.518430561230568632 ) ) ;
#21429=CARTESIAN_POINT ( 'NONE',  ( -13.94827586207000003, -33.10361340872000113, -8.082385102019000922E-06 ) ) ;
#21432=CARTESIAN_POINT ( 'NONE',  ( -1.568660613942000071, -1.839195589987000057, -3.467930652269000102 ) ) ;
#21437=CARTESIAN_POINT ( 'NONE',  ( -12.68625206996000010, -18.23580249185999946, -1.886949102778999965 ) ) ;
#21438=CARTESIAN_POINT ( 'NONE',  ( 12.72558241036999860, -23.20131830507999737, 1.930284820930999956 ) ) ;
#21440=CARTESIAN_POINT ( 'NONE',  ( 1.217390015642369372, -24.81893024925991753, -12.70229597941076172 ) ) ;
#21441=CARTESIAN_POINT ( 'NONE',  ( 10.18629808814000093, -76.37939569223999570, 7.004515126288999305 ) ) ;
#21442=ORIENTED_EDGE ( 'NONE', *, *, #12940, .F. ) ;
#21443=DIRECTION ( 'NONE',  ( 0.000000000000000000, -1.000000000000000000, 0.000000000000000000 ) ) ;
#21445=AXIS2_PLACEMENT_3D ( 'NONE', #50026, #8988, #44408 ) ;
#21447=CARTESIAN_POINT ( 'NONE',  ( 12.54981857179000038, -61.84836586168999872, -0.03768635776142000016 ) ) ;
#21448=CARTESIAN_POINT ( 'NONE',  ( -1.799475295154000065, -21.75083378359999742, -12.69619287811000063 ) ) ;
#21450=AXIS2_PLACEMENT_3D ( 'NONE', #56808, #33261, #52383 ) ;
#21451=ADVANCED_FACE ( 'NONE', ( #41658 ), #54941, .F. ) ;
#21455=ORIENTED_EDGE ( 'NONE', *, *, #51033, .T. ) ;
#21456=CARTESIAN_POINT ( 'NONE',  ( -12.70556836347999941, -16.77227722772000007, 1.774192816106000118E-09 ) ) ;
#21458=AXIS2_PLACEMENT_3D ( 'NONE', #392, #31331, #4787 ) ;
#21462=CARTESIAN_POINT ( 'NONE',  ( -10.45204383623999966, -59.56256649442000395, 7.651147548074000326 ) ) ;
#21467=ORIENTED_EDGE ( 'NONE', *, *, #24749, .T. ) ;
#21469=CARTESIAN_POINT ( 'NONE',  ( -1.629367637659999923, -18.31736356602000271, 12.46114270826000059 ) ) ;
#21471=LINE ( 'NONE', #26462, #49661 ) ;
#21473=EDGE_LOOP ( 'NONE', ( #10749, #11910, #23157, #57518, #12582, #54157 ) ) ;
#21474=CARTESIAN_POINT ( 'NONE',  ( 12.70556836343000029, -53.57227722738999631, -1.774194422348999890E-09 ) ) ;
#21475=ORIENTED_EDGE ( 'NONE', *, *, #55835, .F. ) ;
#21478=CARTESIAN_POINT ( 'NONE',  ( 8.652389292562999046, -53.53734871844999788, 9.414476472778000371 ) ) ;
#21479=LINE ( 'NONE', #25615, #43071 ) ;
#21482=CARTESIAN_POINT ( 'NONE',  ( 12.70255466323004967, -61.54616562044007111, -1.306323829481652821 ) ) ;
#21484=CARTESIAN_POINT ( 'NONE',  ( -10.12290050256999940, -18.75000002239000096, -7.648026768411000376 ) ) ;
#21485=CARTESIAN_POINT ( 'NONE',  ( -10.35410175339000105, -23.40399325350999860, 7.619715687203000520 ) ) ;
#21488=CARTESIAN_POINT ( 'NONE',  ( -12.43570956085999946, -17.12016029981999665, 0.4384071701242000518 ) ) ;
#21489=VECTOR ( 'NONE', #15221, 1000.000000000000114 ) ;
#21492=CARTESIAN_POINT ( 'NONE',  ( -8.190859204290999784, -59.94999999967000548, -7.342331066867000544 ) ) ;
#21493=CARTESIAN_POINT ( 'NONE',  ( 2.362319013936999834, -1.467935987230000183, -3.378608031078000007 ) ) ;
#21498=CARTESIAN_POINT ( 'NONE',  ( 1.405334850312945250, -24.31492947779451796, 12.50716844834712660 ) ) ;
#21499=CARTESIAN_POINT ( 'NONE',  ( -3.306807500130999777, -3.438473948318000240, 1.312446816095000024 ) ) ;
#21502=DIRECTION ( 'NONE',  ( 1.000000000000000000, 0.000000000000000000, 0.000000000000000000 ) ) ;
#21509=B_SPLINE_CURVE_WITH_KNOTS ( 'NONE', 3,
 ( #49989, #27226, #416, #18686, #9535, #50566, #50277, #49399, #9827, #14238, #27518, #14529, #18394, #36968, #44966, #4520, #4222, #27809 ),
 .UNSPECIFIED., .F., .F.,
 ( 4, 2, 2, 2, 2, 2, 2, 2, 4 ),
 ( 0.000000000000000000, 0.1249999999999999722, 0.2499999999999999445, 0.3749999999999998890, 0.4999999999999998890, 0.6249999999999998890, 0.7499999999999997780, 0.8749999999999998890, 1.000000000000000000 ),
 .UNSPECIFIED. ) ;
#21513=CARTESIAN_POINT ( 'NONE',  ( -3.526725475056999848, -1.050894741108000074, -0.2894248236847000166 ) ) ;
#21515=CARTESIAN_POINT ( 'NONE',  ( 12.66314513616999982, -25.17864743362000013, 0.04033065750139999683 ) ) ;
#21516=CARTESIAN_POINT ( 'NONE',  ( -9.369164850722000892, -55.54999999966999980, -7.601397897754999633 ) ) ;
#21517=VERTEX_POINT ( 'NONE', #28355 ) ;
#21518=CARTESIAN_POINT ( 'NONE',  ( 12.57042253521000141, -62.90094976977999863, 0.000000000000000000 ) ) ;
#21521=CARTESIAN_POINT ( 'NONE',  ( -2.589715347022274017, -1.653783639445655762, -2.004944695761151863 ) ) ;
#21525=DIRECTION ( 'NONE',  ( 0.000000000000000000, -0.1122098755727947705, -0.9936845293270585300 ) ) ;
#21526=CARTESIAN_POINT ( 'NONE',  ( 9.298485322489097982, -61.68812323674666231, -8.385852789353158698 ) ) ;
#21528=STYLED_ITEM ( 'NONE', ( #20422 ), #17297 ) ;
#21529=ADVANCED_FACE ( 'NONE', ( #24524 ), #27119, .T. ) ;
#21530=CARTESIAN_POINT ( 'NONE',  ( -0.7999999997951999786, -18.85000000927000130, 11.99999999979999821 ) ) ;
#21531=CARTESIAN_POINT ( 'NONE',  ( -7.765024210398999926, -54.70905971351000119, -9.830784063398999351 ) ) ;
#21535=ORIENTED_EDGE ( 'NONE', *, *, #37817, .F. ) ;
#21537=CARTESIAN_POINT ( 'NONE',  ( 0.7999999997951999786, -18.85000000927000130, -11.99999999979999821 ) ) ;
#21539=ORIENTED_EDGE ( 'NONE', *, *, #15617, .F. ) ;
#21542=CARTESIAN_POINT ( 'NONE',  ( -5.917523019358058356, -75.88333333333329733, -10.26699006316253282 ) ) ;
#21543=CARTESIAN_POINT ( 'NONE',  ( 11.54974070075000014, -78.53893426687999124, 5.138670156068000594 ) ) ;
#21546=DIRECTION ( 'NONE',  ( -0.7071067811865475727, 0.000000000000000000, 0.7071067811865475727 ) ) ;
#21547=EDGE_CURVE ( 'NONE', #35878, #1239, #56510, .T. ) ;
#21549=DIRECTION ( 'NONE',  ( 0.7071067811865475727, 0.000000000000000000, -0.7071067811865475727 ) ) ;
#21550=CARTESIAN_POINT ( 'NONE',  ( 7.624341764923000753, -18.73514850530999709, 10.42531124853000080 ) ) ;
#21552=ORIENTED_EDGE ( 'NONE', *, *, #42573, .T. ) ;
#21555=DIRECTION ( 'NONE',  ( 0.000000000000000000, -1.000000000000000000, 0.000000000000000000 ) ) ;
#21558=AXIS2_PLACEMENT_3D ( 'NONE', #45052, #4605, #40011 ) ;
#21560=CARTESIAN_POINT ( 'NONE',  ( -3.422254106058401746, -78.35090439325858824, 11.58678479484117219 ) ) ;
#21561=EDGE_CURVE ( 'NONE', #17250, #38390, #9232, .T. ) ;
#21563=CARTESIAN_POINT ( 'NONE',  ( 8.838834764832000701, -55.54999999966999980, 8.838834764832000701 ) ) ;
#21565=CARTESIAN_POINT ( 'NONE',  ( 10.38646360831000059, -19.22204592323999961, -7.655555357453000198 ) ) ;
#21570=VERTEX_POINT ( 'NONE', #46401 ) ;
#21575=CARTESIAN_POINT ( 'NONE',  ( -8.130813118348999780, -54.11476110100999648, 9.546856411314999846 ) ) ;
#21580=CARTESIAN_POINT ( 'NONE',  ( 1.288488638075999893, -54.26435060599999360, -12.54709296479000002 ) ) ;
#21581=CARTESIAN_POINT ( 'NONE',  ( 9.770627950922811777, -75.99681967017289708, 6.526574872315616282 ) ) ;
#21583=VERTEX_POINT ( 'NONE', #36640 ) ;
#21584=LINE ( 'NONE', #3580, #6709 ) ;
#21585=CARTESIAN_POINT ( 'NONE',  ( -12.00000000000000000, -23.25000000000000000, 1.750000000000000000 ) ) ;
#21587=DIRECTION ( 'NONE',  ( 0.7071067811865475727, 0.000000000000000000, 0.7071067811865475727 ) ) ;
#21589=CARTESIAN_POINT ( 'NONE',  ( -1.208267226945607176, -17.17409317850119876, 12.70228502423926997 ) ) ;
#21592=DIRECTION ( 'NONE',  ( 0.000000000000000000, -1.000000000000000000, 0.000000000000000000 ) ) ;
#21594=B_SPLINE_CURVE_WITH_KNOTS ( 'NONE', 3,
 ( #31802, #32670, #849, #23255, #18833, #27955 ),
 .UNSPECIFIED., .F., .F.,
 ( 4, 1, 1, 4 ),
 ( 0.000000000000000000, 0.3333333311589000147, 0.6666666623179000606, 0.9999999934768000198 ),
 .UNSPECIFIED. ) ;
#21595=ORIENTED_EDGE ( 'NONE', *, *, #30291, .T. ) ;
#21601=CARTESIAN_POINT ( 'NONE',  ( -11.79999999999999893, -18.84999999999000053, 0.5999999999999999778 ) ) ;
#21603=CARTESIAN_POINT ( 'NONE',  ( -10.99071003982055572, -23.54576790506902029, 0.4528411669630135195 ) ) ;
#21604=CARTESIAN_POINT ( 'NONE',  ( 10.13881649148000008, -76.90783510652001098, -5.938594122520999719 ) ) ;
#21605=DIRECTION ( 'NONE',  ( 0.000000000000000000, -0.8191989531316462569, -0.5735094377497330642 ) ) ;
#21606=CARTESIAN_POINT ( 'NONE',  ( -9.369164850722000892, -60.04999999966999980, 7.601397897754999633 ) ) ;
#21607=CARTESIAN_POINT ( 'NONE',  ( -11.75000000000000000, -76.30000000000001137, 1.487410190129999909E-14 ) ) ;
#21609=EDGE_LOOP ( 'NONE', ( #30934, #8540, #12752, #48497 ) ) ;
#21611=AXIS2_PLACEMENT_3D ( 'NONE', #20518, #2232, #21088 ) ;
#21614=VERTEX_POINT ( 'NONE', #55827 ) ;
#21619=EDGE_CURVE ( 'NONE', #29817, #16042, #34512, .T. ) ;
#21624=ORIENTED_EDGE ( 'NONE', *, *, #28194, .F. ) ;
#21626=DIRECTION ( 'NONE',  ( 0.000000000000000000, 1.000000000000000000, 0.000000000000000000 ) ) ;
#21631=CARTESIAN_POINT ( 'NONE',  ( -12.00000000000000000, -18.75000000000000000, 1.250000000000000000 ) ) ;
#21633=CARTESIAN_POINT ( 'NONE',  ( 12.54901566180999950, -16.99264670699999868, -0.4731578885118999933 ) ) ;
#21634=DIRECTION ( 'NONE',  ( 0.000000000000000000, 0.000000000000000000, 1.000000000000000000 ) ) ;
#21635=ADVANCED_FACE ( 'NONE', ( #29515 ), #25096, .F. ) ;
#21637=ORIENTED_EDGE ( 'NONE', *, *, #21880, .T. ) ;
#21639=DIRECTION ( 'NONE',  ( 0.000000000000000000, 1.000000000000000000, 0.000000000000000000 ) ) ;
#21640=CYLINDRICAL_SURFACE ( 'NONE', #43723, 12.90000000000000036 ) ;
#21641=CARTESIAN_POINT ( 'NONE',  ( -10.31988039474999930, -17.71085245535000396, -7.753829094184000681 ) ) ;
#21642=CARTESIAN_POINT ( 'NONE',  ( 7.668936932637000048, -59.57152778012000027, 10.21380041493999968 ) ) ;
#21643=CARTESIAN_POINT ( 'NONE',  ( -2.061649843245999758, -18.79438692412999856, -12.83797346714000120 ) ) ;
#21645=CARTESIAN_POINT ( 'NONE',  ( 10.24996238027999951, -58.55171076491000548, -7.705119999413000187 ) ) ;
#21646=CARTESIAN_POINT ( 'NONE',  ( -1.626826133776999786E-14, -74.80000000000001137, 0.000000000000000000 ) ) ;
#21648=CARTESIAN_POINT ( 'NONE',  ( -1.636761686205434385, -1.916666666666666741, 2.839805762151331958 ) ) ;
#21651=DIRECTION ( 'NONE',  ( -0.9999548435846228323, 0.000000000000000000, -0.009503199022040118363 ) ) ;
#21652=CARTESIAN_POINT ( 'NONE',  ( 1.933504092460999857, -55.39593152692000189, 12.70940235704999921 ) ) ;
#21653=CARTESIAN_POINT ( 'NONE',  ( -12.80900240953000058, -21.75365779208000205, 1.930989144707000005 ) ) ;
#21654=CARTESIAN_POINT ( 'NONE',  ( 1.881026021997999953, -2.552403522605000141, 3.308707285175000123 ) ) ;
#21656=CIRCLE ( 'NONE', #27300, 12.80000000000000071 ) ;
#21657=DIRECTION ( 'NONE',  ( 0.000000000000000000, -0.7071067811866525998, -0.7071067811864425456 ) ) ;
#21659=CARTESIAN_POINT ( 'NONE',  ( -0.8520291216319383354, -1.997329406447212685, 3.167964011321702689 ) ) ;
#21660=CARTESIAN_POINT ( 'NONE',  ( 9.722718241315000398, -60.04999999966999980, -7.954951288349001004 ) ) ;
#21664=CARTESIAN_POINT ( 'NONE',  ( 7.287274196408028537, -76.77647172171292311, 9.625134870786519414 ) ) ;
#21668=LINE ( 'NONE', #56538, #16027 ) ;
#21670=CARTESIAN_POINT ( 'NONE',  ( 1.997276839918477265, -2.677083333333333481, -2.598917237794082791 ) ) ;
#21674=CARTESIAN_POINT ( 'NONE',  ( -10.18249594443699735, -17.70907903275769613, -7.792385963400852766 ) ) ;
#21680=VERTEX_POINT ( 'NONE', #20386 ) ;
#21681=AXIS2_PLACEMENT_3D ( 'NONE', #56296, #19698, #11718 ) ;
#21682=CARTESIAN_POINT ( 'NONE',  ( 1.308715794696073020, -24.74404499195298968, 12.70256747357037419 ) ) ;
#21684=DIRECTION ( 'NONE',  ( 0.000000000000000000, -1.000000000000000000, 0.000000000000000000 ) ) ;
#21690=VERTEX_POINT ( 'NONE', #2390 ) ;
#21692=CARTESIAN_POINT ( 'NONE',  ( -12.04891275065999956, -78.43148691446999976, -1.977722186035000274 ) ) ;
#21696=CARTESIAN_POINT ( 'NONE',  ( 8.485281374238999419, -60.74999999967048581, 8.485281374238999419 ) ) ;
#21697=B_SPLINE_CURVE_WITH_KNOTS ( 'NONE', 3,
 ( #12710, #35721, #49027, #26561, #44892, #3569 ),
 .UNSPECIFIED., .F., .F.,
 ( 4, 1, 1, 4 ),
 ( 0.000000000000000000, 0.3333333333333000081, 0.6666666666667000474, 1.000000000000000000 ),
 .UNSPECIFIED. ) ;
#21699=AXIS2_PLACEMENT_3D ( 'NONE', #27993, #54594, #50170 ) ;
#21701=VECTOR ( 'NONE', #14560, 1000.000000000000000 ) ;
#21704=CARTESIAN_POINT ( 'NONE',  ( -10.63665183518000035, -77.95590642111000079, 7.669898027128999374 ) ) ;
#21705=CARTESIAN_POINT ( 'NONE',  ( 12.30436613475999863, -78.05926792646000933, -3.523071432600000108 ) ) ;
#21710=CARTESIAN_POINT ( 'NONE',  ( 12.56594317989000054, -23.24999999414999863, 1.750000000001000089 ) ) ;
#21711=CARTESIAN_POINT ( 'NONE',  ( -0.1776184920840612746, -2.979648444064375123, 3.245463997345638063 ) ) ;
#21716=CARTESIAN_POINT ( 'NONE',  ( -0.3113020967593000399, -2.664182682366000421, 3.793306396812999637 ) ) ;
#21719=CARTESIAN_POINT ( 'NONE',  ( -7.619712170668999640, -60.20404510030000012, -10.35409959312000083 ) ) ;
#21720=CARTESIAN_POINT ( 'NONE',  ( -3.250000000000000000, -1.000000000000000000, 1.223542571470000149E-13 ) ) ;
#21723=CARTESIAN_POINT ( 'NONE',  ( -12.66314509270999977, -16.82135249322999826, 0.04032083120557000688 ) ) ;
#21724=CARTESIAN_POINT ( 'NONE',  ( 0.000000000000000000, -18.75000000000000000, -12.50000000000000000 ) ) ;
#21725=CARTESIAN_POINT ( 'NONE',  ( 1.001315002179000047, -24.68522411714000242, -12.50000000000000000 ) ) ;
#21726=CARTESIAN_POINT ( 'NONE',  ( -6.753896588641000065, -75.57222202327999128, -10.03086863324999989 ) ) ;
#21729=CARTESIAN_POINT ( 'NONE',  ( 12.82230166705999963, -60.22260937973999972, 2.065916748305000272 ) ) ;
#21730=CARTESIAN_POINT ( 'NONE',  ( 7.653559502277999194, -18.70150862776000267, -10.01234990228999955 ) ) ;
#21731=CIRCLE ( 'NONE', #16234, 0.5000000000000004441 ) ;
#21736=VERTEX_POINT ( 'NONE', #52770 ) ;
#21737=ADVANCED_FACE ( 'NONE', ( #57770 ), #44785, .F. ) ;
#21740=VECTOR ( 'NONE', #27666, 1000.000000000000114 ) ;
#21746=DIRECTION ( 'NONE',  ( 0.000000000000000000, 1.000000000000000000, 0.000000000000000000 ) ) ;
#21748=ORIENTED_EDGE ( 'NONE', *, *, #33712, .T. ) ;
#21749=EDGE_LOOP ( 'NONE', ( #13450, #56131, #33950, #27774 ) ) ;
#21751=CARTESIAN_POINT ( 'NONE',  ( 1.537484947575329830, -78.06258978500997614, 11.74336395611926243 ) ) ;
#21759=CARTESIAN_POINT ( 'NONE',  ( 7.645398650953000086, -55.58468617124000133, 10.18948982067999864 ) ) ;
#21760=CARTESIAN_POINT ( 'NONE',  ( -7.691893942719999266, -21.75453807238000081, -10.42272502862000039 ) ) ;
#21761=DIRECTION ( 'NONE',  ( 0.000000000000000000, -1.000000000000000000, 0.000000000000000000 ) ) ;
#21762=DIRECTION ( 'NONE',  ( 0.000000000000000000, 1.000000000000000000, 0.000000000000000000 ) ) ;
#21763=CARTESIAN_POINT ( 'NONE',  ( 7.654537165486999584, -60.08056535122999975, -10.01332852690999964 ) ) ;
#21764=EDGE_CURVE ( 'NONE', #35060, #47903, #57736, .T. ) ;
#21765=CARTESIAN_POINT ( 'NONE',  ( -10.18499221075000172, -21.74977139925000102, -7.710118476595999581 ) ) ;
#21767=VECTOR ( 'NONE', #28069, 1000.000000000000000 ) ;
#21768=EDGE_CURVE ( 'NONE', #18144, #48697, #48924, .T. ) ;
#21773=CARTESIAN_POINT ( 'NONE',  ( 10.45204383622999877, -22.76256649475000060, -7.651147548059999970 ) ) ;
#21776=CARTESIAN_POINT ( 'NONE',  ( -3.420836093188877935, -78.44788026401511161, 11.58194243861089134 ) ) ;
#21784=DIRECTION ( 'NONE',  ( -1.000000000000000000, 0.000000000000000000, -2.582636882130999866E-11 ) ) ;
#21785=EDGE_CURVE ( 'NONE', #15969, #13888, #43919, .T. ) ;
#21786=DIRECTION ( 'NONE',  ( 0.000000000000000000, -1.000000000000000000, 0.000000000000000000 ) ) ;
#21787=CARTESIAN_POINT ( 'NONE',  ( -7.970415440364950754, -17.47707676838395230, 9.713035532436663289 ) ) ;
#21790=ORIENTED_EDGE ( 'NONE', *, *, #57492, .T. ) ;
#21791=CARTESIAN_POINT ( 'NONE',  ( -10.04115011120000034, -19.23513569609999863, -7.682331425195999763 ) ) ;
#21796=CARTESIAN_POINT ( 'NONE',  ( -9.966224254750001066, -60.46904904752999954, 7.657729124028000101 ) ) ;
#21797=CARTESIAN_POINT ( 'NONE',  ( -3.195973530103000115, -0.6111989345079000824, 0.8317538331999000389 ) ) ;
#21799=CARTESIAN_POINT ( 'NONE',  ( 12.83675988120999989, -23.22754371161000009, -2.062832873794000044 ) ) ;
#21800=CARTESIAN_POINT ( 'NONE',  ( -1.667936688463999895, -59.56486430393999854, 12.53239398061000109 ) ) ;
#21801=ORIENTED_EDGE ( 'NONE', *, *, #56263, .F. ) ;
#21802=B_SPLINE_CURVE_WITH_KNOTS ( 'NONE', 3,
 ( #48795, #26338, #44356, #3910, #21912, #39921, #28378, #5659, #10105, #1262, #14516, #33097, #27505, #36954, #49975, #23383, #18379, #32508 ),
 .UNSPECIFIED., .F., .F.,
 ( 4, 2, 2, 2, 2, 2, 2, 2, 4 ),
 ( 0.000000000000000000, 0.1249999999999999722, 0.2500000000000000000, 0.3750000000000000000, 0.5000000000000001110, 0.6250000000000001110, 0.7500000000000000000, 0.8750000000000000000, 1.000000000000000000 ),
 .UNSPECIFIED. ) ;
#21803=EDGE_CURVE ( 'NONE', #30548, #2165, #21471, .T. ) ;
#21804=CYLINDRICAL_SURFACE ( 'NONE', #54088, 1.750000000000001332 ) ;
#21805=CARTESIAN_POINT ( 'NONE',  ( 9.298485322488877713, -24.88812323703113805, -8.385852789304612642 ) ) ;
#21806=CARTESIAN_POINT ( 'NONE',  ( -12.52785477537235082, -18.20586572947692972, 1.668513103013892884 ) ) ;
#21807=EDGE_CURVE ( 'NONE', #19884, #17378, #58065, .T. ) ;
#21808=CARTESIAN_POINT ( 'NONE',  ( -10.35747145890000098, -55.48415267986000288, -7.626500777218999438 ) ) ;
#21813=CARTESIAN_POINT ( 'NONE',  ( 11.79999999999999893, -18.84999999999000053, -0.5999999999999999778 ) ) ;
#21814=DIRECTION ( 'NONE',  ( 1.000000000000000000, 3.441642669434999888E-11, 0.000000000000000000 ) ) ;
#21816=AXIS2_PLACEMENT_3D ( 'NONE', #29296, #47345, #48209 ) ;
#21817=CARTESIAN_POINT ( 'NONE',  ( 1.668607604520048415, -55.00618368707859673, 12.52787843847549887 ) ) ;
#21818=CARTESIAN_POINT ( 'NONE',  ( -10.15833271780000047, -54.58011549179999378, -7.756208840337999177 ) ) ;
#21821=ORIENTED_EDGE ( 'NONE', *, *, #12057, .T. ) ;
#21825=CARTESIAN_POINT ( 'NONE',  ( 10.19022281666000040, -18.80366258888000175, 7.646946378508999942 ) ) ;
#21828=CARTESIAN_POINT ( 'NONE',  ( -12.92190527446000026, -78.08724936260999527, -0.9418163832602000074 ) ) ;
#21833=CARTESIAN_POINT ( 'NONE',  ( 0.000000000000000000, -1.355252715606880543E-17, -3.800000000000270717 ) ) ;
#21835=ORIENTED_EDGE ( 'NONE', *, *, #25244, .F. ) ;
#21839=CARTESIAN_POINT ( 'NONE',  ( 1.750000000001000089, -60.04999998641999781, -12.56594318054000148 ) ) ;
#21840=CARTESIAN_POINT ( 'NONE',  ( 1.317981885658178198, -3.004763700841414753, -3.265141604934490793 ) ) ;
#21842=DIRECTION ( 'NONE',  ( -1.894056205636980548E-11, 1.538484108169980264E-07, 0.9999999999999882316 ) ) ;
#21846=CARTESIAN_POINT ( 'NONE',  ( 10.53101990620000095, -23.30639784948999704, -7.613962745608000127 ) ) ;
#21853=AXIS2_PLACEMENT_3D ( 'NONE', #9594, #32875, #42350 ) ;
#21860=CARTESIAN_POINT ( 'NONE',  ( -0.5154756746322000094, -53.66759400203999775, -12.66205448068000017 ) ) ;
#21861=EDGE_CURVE ( 'NONE', #52710, #37361, #40945, .T. ) ;
#21863=CARTESIAN_POINT ( 'NONE',  ( 9.772926403074635004, -75.99679253653761180, 6.523134133395031675 ) ) ;
#21868=EDGE_CURVE ( 'NONE', #48419, #36474, #53566, .T. ) ;
#21869=CARTESIAN_POINT ( 'NONE',  ( 8.485281374238999419, -55.54999999966999980, 8.485281374238999419 ) ) ;
#21880=EDGE_CURVE ( 'NONE', #4894, #35836, #50976, .T. ) ;
#21885=EDGE_CURVE ( 'NONE', #20606, #47713, #5357, .T. ) ;
#21886=CARTESIAN_POINT ( 'NONE',  ( -1.423904377723695935, -61.10512805135450520, 12.50677628660337248 ) ) ;
#21889=DIRECTION ( 'NONE',  ( 0.000000000000000000, -1.000000000000000000, 0.000000000000000000 ) ) ;
#21891=VERTEX_POINT ( 'NONE', #23509 ) ;
#21893=AXIS2_PLACEMENT_3D ( 'NONE', #7053, #11206, #11776 ) ;
#21895=CARTESIAN_POINT ( 'NONE',  ( 2.624826629463999694, -78.90983510652000632, 11.97953966613999910 ) ) ;
#21896=ORIENTED_EDGE ( 'NONE', *, *, #28267, .T. ) ;
#21897=CARTESIAN_POINT ( 'NONE',  ( 9.414507962619001802, -25.26263135926000203, 8.652357372777000677 ) ) ;
#21901=AXIS2_PLACEMENT_3D ( 'NONE', #2413, #30405, #7982 ) ;
#21905=VERTEX_POINT ( 'NONE', #1105 ) ;
#21910=VECTOR ( 'NONE', #29509, 1000.000000000000000 ) ;
#21911=CARTESIAN_POINT ( 'NONE',  ( -2.203951651292999969, -75.80714300465999145, 12.77594201493999826 ) ) ;
#21912=CARTESIAN_POINT ( 'NONE',  ( 2.663461512100961048, -2.200631673208123917, -1.905539629302623217 ) ) ;
#21913=CARTESIAN_POINT ( 'NONE',  ( 8.610991514451539430, -53.62512235746365263, -9.355860133842407222 ) ) ;
#21916=CARTESIAN_POINT ( 'NONE',  ( 12.77562786370999959, -16.73761952138000098, -0.5426593252874999385 ) ) ;
#21917=CARTESIAN_POINT ( 'NONE',  ( -9.516272955293000990, -24.82538765621999843, -8.227498559427999680 ) ) ;
#21918=CARTESIAN_POINT ( 'NONE',  ( -11.73895145468623724, -76.69513831007681404, 0.6305574448010526911 ) ) ;
#21919=EDGE_LOOP ( 'NONE', ( #13043, #7034, #1223, #1673 ) ) ;
#21921=CARTESIAN_POINT ( 'NONE',  ( -7.943801774140000660, -54.36598212437999678, 9.641153612765998915 ) ) ;
#21923=CARTESIAN_POINT ( 'NONE',  ( -7.758899961888999997, -17.69918178096000005, -10.31442855573999928 ) ) ;
#21925=DIRECTION ( 'NONE',  ( 0.000000000000000000, 1.000000000000000000, 0.000000000000000000 ) ) ;
#21927=CARTESIAN_POINT ( 'NONE',  ( 10.21380041493999968, -59.57152778012000027, -7.668936932637000048 ) ) ;
#21933=CARTESIAN_POINT ( 'NONE',  ( 1.638701331945049633, -1.434920423400078304, 2.842861795934006786 ) ) ;
#21934=CARTESIAN_POINT ( 'NONE',  ( -1.691611010928999903, -54.56917308736999672, 12.66722148965999928 ) ) ;
#21936=CARTESIAN_POINT ( 'NONE',  ( -2.342185844934999928, -3.569198934507999965, 2.328138035414999862 ) ) ;
#21938=VECTOR ( 'NONE', #28827, 1000.000000000000114 ) ;
#21939=FACE_OUTER_BOUND ( 'NONE', #40280, .T. ) ;
#21941=DIRECTION ( 'NONE',  ( 0.000000000000000000, 0.000000000000000000, -1.000000000000000000 ) ) ;
#21942=CARTESIAN_POINT ( 'NONE',  ( 12.49989298250000047, -18.80773379996000116, 1.666426105558000081 ) ) ;
#21946=CARTESIAN_POINT ( 'NONE',  ( 11.03313870319343160, -76.66973052364008367, -4.907352434147976616 ) ) ;
#21947=B_SPLINE_SURFACE_WITH_KNOTS ( 'NONE', 3, 3, ( 
 ( #14686, #1726, #50737, #33275 ),
 ( #14981, #19719, #21447, #47480 ),
 ( #12018, #38586, #16736, #47760 ),
 ( #56892, #43899, #25008, #56601 ),
 ( #34430, #52460, #38872, #29999 ),
 ( #39737, #39456, #16161, #57460 ),
 ( #34718, #11734, #39161, #57747 ),
 ( #57170, #3165, #48053, #3443 ),
 ( #21729, #44182, #52748, #11449 ),
 ( #21155, #29712, #51891, #12302 ),
 ( #30292, #34139, #35005, #25872 ) ),
 .UNSPECIFIED., .F., .F., .F.,
 ( 4, 1, 1, 1, 1, 1, 1, 1, 4 ),
 ( 4, 4 ),
 ( -0.01994534136800000038, 0.000000000000000000, 0.1666666666667000196, 0.3333333333333000081, 0.5000000000000000000, 0.6666666666667000474, 0.8333333333333000637, 1.000000000000000000, 1.020519780480000138 ),
 ( -0.3582002740342999925, 1.358566136078000142 ),
 .UNSPECIFIED. ) ;
#21952=DIRECTION ( 'NONE',  ( 0.000000000000000000, -1.000000000000000000, 0.000000000000000000 ) ) ;
#21955=CARTESIAN_POINT ( 'NONE',  ( -12.52134121557681468, -23.92745484923118937, -1.618935178668596375 ) ) ;
#21958=CONICAL_SURFACE ( 'NONE', #54968, 12.94999999994000106, 0.7853981633972997312 ) ;
#21963=CARTESIAN_POINT ( 'NONE',  ( -12.50000000000000000, -55.55000000278000272, 1.750000000000000000 ) ) ;
#21968=CARTESIAN_POINT ( 'NONE',  ( 1.749899258081075271, -55.41283151199909440, 12.55433901288162168 ) ) ;
#21970=CARTESIAN_POINT ( 'NONE',  ( 3.165411199172025292, -1.270833333333332815, 0.8506806241676674318 ) ) ;
#21971=CARTESIAN_POINT ( 'NONE',  ( 11.44417895085271475, -77.52916666666665435, -3.075537641221520069 ) ) ;
#21973=CARTESIAN_POINT ( 'NONE',  ( 2.019183793707000074, -23.78720277242999970, -12.79944116704999857 ) ) ;
#21978=CARTESIAN_POINT ( 'NONE',  ( 12.30892827549999957, -78.74849350881000021, -1.105470418167000091 ) ) ;
#21980=ORIENTED_EDGE ( 'NONE', *, *, #55969, .F. ) ;
#21982=VECTOR ( 'NONE', #33771, 1000.000000000000000 ) ;
#21983=B_SPLINE_CURVE_WITH_KNOTS ( 'NONE', 3,
 ( #53708, #35083, #8830, #26242, #40414, #57831, #52828, #57540 ),
 .UNSPECIFIED., .F., .F.,
 ( 4, 2, 2, 4 ),
 ( 0.000000000000000000, 0.5000000000000000000, 0.7500000000000000000, 1.000000000000000000 ),
 .UNSPECIFIED. ) ;
#21989=CARTESIAN_POINT ( 'NONE',  ( 5.759449073023001020, -78.34443890784000075, 11.78163922240000083 ) ) ;
#21990=CARTESIAN_POINT ( 'NONE',  ( -8.971242061857001460, -76.80658961653000461, -8.906291659541000882 ) ) ;
#21991=AXIS2_PLACEMENT_3D ( 'NONE', #25119, #7979, #25692 ) ;
#21995=CARTESIAN_POINT ( 'NONE',  ( -10.53003236230999917, -55.47547726255000100, 7.612971540256999958 ) ) ;
#21996=CARTESIAN_POINT ( 'NONE',  ( -0.003967600564047823151, -2.975581622302581497, 3.249709392134530805 ) ) ;
#21998=AXIS2_PLACEMENT_3D ( 'NONE', #50001, #27530, #19278 ) ;
#22002=CARTESIAN_POINT ( 'NONE',  ( -3.804208684430999909, -3.285148731141000145, -0.1186911049137999996 ) ) ;
#22004=VECTOR ( 'NONE', #23633, 1000.000000000000000 ) ;
#22006=CARTESIAN_POINT ( 'NONE',  ( 0.000000000000000000, -23.15000000000000213, -11.89999999977000122 ) ) ;
#22007=CARTESIAN_POINT ( 'NONE',  ( 7.648026768019999366, -23.24999998419999869, 10.12290050217000115 ) ) ;
#22010=CARTESIAN_POINT ( 'NONE',  ( -3.201433918554999813, -77.87744717221998769, 12.61309089657999927 ) ) ;
#22012=CARTESIAN_POINT ( 'NONE',  ( 12.60413652832999887, -18.69283065396999888, -1.799502287743000029 ) ) ;
#22014=EDGE_CURVE ( 'NONE', #48012, #3043, #22931, .T. ) ;
#22015=CARTESIAN_POINT ( 'NONE',  ( -10.06692933811712365, -55.09657286937044063, 7.655995045256465126 ) ) ;
#22017=EDGE_CURVE ( 'NONE', #47194, #52418, #54529, .T. ) ;
#22022=CARTESIAN_POINT ( 'NONE',  ( -1.667936697358999965, -59.56462890159999546, -12.53241208775999915 ) ) ;
#22026=CARTESIAN_POINT ( 'NONE',  ( 8.485281374238999419, -18.75000000000000000, 8.485281374238999419 ) ) ;
#22028=VERTEX_POINT ( 'NONE', #18226 ) ;
#22029=ORIENTED_EDGE ( 'NONE', *, *, #16899, .F. ) ;
#22031=VECTOR ( 'NONE', #18068, 999.9999999999998863 ) ;
#22033=EDGE_CURVE ( 'NONE', #47003, #35953, #8483, .T. ) ;
#22037=ORIENTED_EDGE ( 'NONE', *, *, #17446, .F. ) ;
#22038=ORIENTED_EDGE ( 'NONE', *, *, #17635, .F. ) ;
#22039=CIRCLE ( 'NONE', #21087, 13.00000000000000000 ) ;
#22041=CARTESIAN_POINT ( 'NONE',  ( -1.490118887467393627, -0.9426324846354789955, -3.733870388342663826 ) ) ;
#22042=VERTEX_POINT ( 'NONE', #14642 ) ;
#22044=VERTEX_POINT ( 'NONE', #49812 ) ;
#22047=FACE_OUTER_BOUND ( 'NONE', #20223, .T. ) ;
#22049=CARTESIAN_POINT ( 'NONE',  ( -7.220923959705292994, -78.72708333333336839, 9.396085398178589898 ) ) ;
#22053=CARTESIAN_POINT ( 'NONE',  ( -9.966224254735001509, -23.66904904784999886, 7.657729124005999921 ) ) ;
#22055=CIRCLE ( 'NONE', #25863, 9.000000000000000000 ) ;
#22061=CARTESIAN_POINT ( 'NONE',  ( -0.5154756746315999338, -25.13240599763000205, 12.66205448072999928 ) ) ;
#22063=CARTESIAN_POINT ( 'NONE',  ( -12.05000000000000071, -74.80000000000001137, 0.000000000000000000 ) ) ;
#22064=CARTESIAN_POINT ( 'NONE',  ( 3.591303024676000266, -1.295096044169000038, -0.4777876730464000188 ) ) ;
#22068=CARTESIAN_POINT ( 'NONE',  ( 0.000000000000000000, -0.1000000007601000024, -10.29999999923999887 ) ) ;
#22073=DIRECTION ( 'NONE',  ( 0.000000000000000000, 0.000000000000000000, -1.000000000000000000 ) ) ;
#22084=CARTESIAN_POINT ( 'NONE',  ( -0.6004213309738001270, -0.6558122488618000068, -3.487579485068999841 ) ) ;
#22086=CARTESIAN_POINT ( 'NONE',  ( -8.838834764832000701, -60.04999999966999980, -8.838834764832000701 ) ) ;
#22087=CARTESIAN_POINT ( 'NONE',  ( -2.062670899361999766, -60.10639784916000394, 12.83044027763000017 ) ) ;
#22088=ORIENTED_EDGE ( 'NONE', *, *, #43438, .F. ) ;
#22091=CARTESIAN_POINT ( 'NONE',  ( -0.5458445578339461424, -1.713104424745484300, -3.230288565804697143 ) ) ;
#22092=CARTESIAN_POINT ( 'NONE',  ( -10.04115011118999945, -56.03513569577999931, -7.682331425181999407 ) ) ;
#22097=ADVANCED_FACE ( 'NONE', ( #33080 ), #41181, .T. ) ;
#22099=CARTESIAN_POINT ( 'NONE',  ( -12.55432891850757748, -55.41272687720891099, 1.749897736046110541 ) ) ;
#22100=CARTESIAN_POINT ( 'NONE',  ( 11.67628222315400599, -77.93643586021261171, -1.539162911442760517 ) ) ;
#22101=DIRECTION ( 'NONE',  ( 0.7071067811865475727, 0.000000000000000000, -0.7071067811865475727 ) ) ;
#22102=EDGE_CURVE ( 'NONE', #10870, #25466, #9238, .T. ) ;
#22105=CARTESIAN_POINT ( 'NONE',  ( -12.58335110165999993, -57.05111654290000445, 1.667961430005999945 ) ) ;
#22106=CARTESIAN_POINT ( 'NONE',  ( -7.647736468613000049, -55.07704514418999509, -10.13404651203999940 ) ) ;
#22107=VECTOR ( 'NONE', #5418, 1000.000000000000000 ) ;
#22109=EDGE_LOOP ( 'NONE', ( #14740, #7958 ) ) ;
#22110=VERTEX_POINT ( 'NONE', #29524 ) ;
#22114=EDGE_LOOP ( 'NONE', ( #56234, #9653, #7319, #27481 ) ) ;
#22119=CARTESIAN_POINT ( 'NONE',  ( -8.110204649352999340, -78.42570409358999939, 9.400142180594000862 ) ) ;
#22125=CARTESIAN_POINT ( 'NONE',  ( 10.25203062049729041, -17.87822876371741998, 7.730397977284573230 ) ) ;
#22128=CARTESIAN_POINT ( 'NONE',  ( -3.151328970204000157, -76.15639898940999331, -11.89977497056000111 ) ) ;
#22130=B_SPLINE_SURFACE_WITH_KNOTS ( 'NONE', 3, 3, ( 
 ( #13797, #46003, #23828, #5527 ),
 ( #6118, #40680, #18251, #31799 ),
 ( #27376, #1132, #22962, #32096 ),
 ( #18541, #40972, #14098, #9678 ),
 ( #5248, #23253, #41262, #36823 ),
 ( #54838, #14381, #32381, #19704 ),
 ( #20005, #20856, #38575, #42727 ),
 ( #52170, #25285, #37989, #33557 ) ),
 .UNSPECIFIED., .F., .F., .F.,
 ( 4, 1, 1, 1, 1, 4 ),
 ( 4, 4 ),
 ( -0.01200407345748999953, 0.000000000000000000, 0.3333333333333000081, 0.6666666666667000474, 1.000000000000000000, 1.011997855551999947 ),
 ( -0.3559705542741999906, 1.355970554273999928 ),
 .UNSPECIFIED. ) ;
#22133=CARTESIAN_POINT ( 'NONE',  ( -3.554945896888052737, -3.345802747932901777, 0.1544303516782937480 ) ) ;
#22134=DIRECTION ( 'NONE',  ( 0.9999999999998321343, 0.000000000000000000, 5.794540611356191117E-07 ) ) ;
#22137=EDGE_CURVE ( 'NONE', #47867, #35763, #34817, .T. ) ;
#22139=CARTESIAN_POINT ( 'NONE',  ( 10.53003236233000095, -18.67547726287999765, -7.612971540274999782 ) ) ;
#22143=CARTESIAN_POINT ( 'NONE',  ( -2.099388381696000338E-14, -0.1000000000000002554, -12.80000000000033467 ) ) ;
#22146=CIRCLE ( 'NONE', #55161, 14.00000000000000000 ) ;
#22148=CYLINDRICAL_SURFACE ( 'NONE', #25741, 14.00000000000000000 ) ;
#22149=CARTESIAN_POINT ( 'NONE',  ( -7.624341766629000539, -55.53514853726999689, 10.42531125022999916 ) ) ;
#22150=DIRECTION ( 'NONE',  ( 0.000000000000000000, 0.8191944460894733382, -0.5735158755397804509 ) ) ;
#22154=CARTESIAN_POINT ( 'NONE',  ( -10.10713367717059796, -24.46653151341558896, -7.860990029285546576 ) ) ;
#22155=CARTESIAN_POINT ( 'NONE',  ( 11.73168449440016481, -75.95508173438524580, 0.7621015541101189283 ) ) ;
#22158=ORIENTED_EDGE ( 'NONE', *, *, #3718, .F. ) ;
#22160=CARTESIAN_POINT ( 'NONE',  ( -3.168364096407636499, -2.122297881318587542, -0.8517483099742300112 ) ) ;
#22161=AXIS2_PLACEMENT_3D ( 'NONE', #54694, #5389, #23397 ) ;
#22168=CARTESIAN_POINT ( 'NONE',  ( 5.939518926465330750, -78.53233929404970581, 10.13791247079975832 ) ) ;
#22170=VERTEX_POINT ( 'NONE', #29805 ) ;
#22173=CARTESIAN_POINT ( 'NONE',  ( 10.17807092908048539, -75.79999999999999716, -6.222892922246035852 ) ) ;
#22176=DIRECTION ( 'NONE',  ( 0.000000000000000000, 0.000000000000000000, -1.000000000000000000 ) ) ;
#22178=EDGE_CURVE ( 'NONE', #9689, #47619, #23969, .T. ) ;
#22180=CARTESIAN_POINT ( 'NONE',  ( 10.12290050253000118, -23.24999997822999731, -7.648026768374000639 ) ) ;
#22182=CARTESIAN_POINT ( 'NONE',  ( -12.71005379442735084, -61.09489531480230085, -1.687596143085857481 ) ) ;
#22184=DIRECTION ( 'NONE',  ( 1.000000000000000000, 0.000000000000000000, 0.000000000000000000 ) ) ;
#22189=FACE_OUTER_BOUND ( 'NONE', #7504, .T. ) ;
#22190=VERTEX_POINT ( 'NONE', #21252 ) ;
#22191=CARTESIAN_POINT ( 'NONE',  ( 7.660411271047999904, -23.19173735492000077, 10.01752031414999955 ) ) ;
#22193=ADVANCED_FACE ( 'NONE', ( #12398 ), #17708, .T. ) ;
#22194=CARTESIAN_POINT ( 'NONE',  ( 8.137215171343429532, -55.34844303568876711, -7.401770473315444576 ) ) ;
#22196=ADVANCED_FACE ( 'NONE', ( #35991 ), #36453, .F. ) ;
#22200=ORIENTED_EDGE ( 'NONE', *, *, #30527, .F. ) ;
#22201=ORIENTED_EDGE ( 'NONE', *, *, #56456, .F. ) ;
#22206=CARTESIAN_POINT ( 'NONE',  ( -2.150406028006000003, -75.63298130519999063, 12.46554692171000056 ) ) ;
#22208=LINE ( 'NONE', #3347, #23298 ) ;
#22211=CARTESIAN_POINT ( 'NONE',  ( 12.66315144086999922, -16.82197088188999601, 0.06064144874956999692 ) ) ;
#22212=DIRECTION ( 'NONE',  ( 0.000000000000000000, -1.000000000000000000, 0.000000000000000000 ) ) ;
#22219=CARTESIAN_POINT ( 'NONE',  ( -10.19022281666000040, -18.80366258888000175, -7.646946378508999942 ) ) ;
#22220=CARTESIAN_POINT ( 'NONE',  ( -1.247385803317999864, -61.27722255996999934, -12.50301438880000049 ) ) ;
#22221=CARTESIAN_POINT ( 'NONE',  ( -0.8537148449481999357, -17.29501854091000013, -12.43377424872999981 ) ) ;
#22224=CARTESIAN_POINT ( 'NONE',  ( 10.04116292115999975, -56.03537109808000594, -7.682344222575999915 ) ) ;
#22231=CARTESIAN_POINT ( 'NONE',  ( 1.698401934078999975, -54.57985954063000378, 12.66748707609000135 ) ) ;
#22232=VECTOR ( 'NONE', #27087, 1000.000000000000000 ) ;
#22234=CARTESIAN_POINT ( 'NONE',  ( 1.655866326982999848, -1.964893323557999949, -3.604003584276000094 ) ) ;
#22238=CARTESIAN_POINT ( 'NONE',  ( -1.761265949705000056, -60.50858218752999562, 12.57448205046000034 ) ) ;
#22239=CARTESIAN_POINT ( 'NONE',  ( 12.72394144137000005, -18.77839271500000251, 1.930881231431999856 ) ) ;
#22240=VECTOR ( 'NONE', #50278, 1000.000000000000000 ) ;
#22243=VECTOR ( 'NONE', #46693, 1000.000000000000114 ) ;
#22244=CARTESIAN_POINT ( 'NONE',  ( -10.97571145796055703, -76.91879331913770557, 5.030464531489157842 ) ) ;
#22245=CARTESIAN_POINT ( 'NONE',  ( -6.042059545598000625, -78.58551785422000080, 10.44717322784999958 ) ) ;
#22251=CARTESIAN_POINT ( 'NONE',  ( -3.250000000000001332, -2.510416666666666075, -0.4254240051736181139 ) ) ;
#22259=ORIENTED_EDGE ( 'NONE', *, *, #35924, .F. ) ;
#22262=ORIENTED_EDGE ( 'NONE', *, *, #39759, .T. ) ;
#22264=VERTEX_POINT ( 'NONE', #10610 ) ;
#22266=EDGE_CURVE ( 'NONE', #31399, #42913, #6456, .T. ) ;
#22269=CARTESIAN_POINT ( 'NONE',  ( 0.005523896503950999348, -25.06963456225999920, -12.55021156880999911 ) ) ;
#22274=CARTESIAN_POINT ( 'NONE',  ( -1.301498323113999822, -79.03504199407001352, -12.14058299385000161 ) ) ;
#22276=ORIENTED_EDGE ( 'NONE', *, *, #13019, .T. ) ;
#22284=CONICAL_SURFACE ( 'NONE', #41134, 12.84999999993999964, 0.7853981633972997312 ) ;
#22285=CARTESIAN_POINT ( 'NONE',  ( 5.554616340558999887, -77.67073543972999516, 11.53062854294000061 ) ) ;
#22286=ADVANCED_FACE ( 'NONE', ( #5869 ), #41892, .F. ) ;
#22289=CIRCLE ( 'NONE', #43082, 0.5000000000000004441 ) ;
#22292=CARTESIAN_POINT ( 'NONE',  ( -10.24996238027999951, -58.55171076491000548, 7.705119999413000187 ) ) ;
#22293=CARTESIAN_POINT ( 'NONE',  ( 3.262409307125078595, -76.84669750786996190, -11.36051482961531001 ) ) ;
#22297=EDGE_CURVE ( 'NONE', #2251, #16536, #52829, .T. ) ;
#22298=CARTESIAN_POINT ( 'NONE',  ( -2.963791440107999886, -3.228697272162000420, 2.387889716789000083 ) ) ;
#22302=EDGE_CURVE ( 'NONE', #25015, #11513, #15609, .T. ) ;
#22303=CARTESIAN_POINT ( 'NONE',  ( 5.865376297750809157E-14, -72.79999999999999716, 13.89999999999999858 ) ) ;
#22306=CARTESIAN_POINT ( 'NONE',  ( -3.129814719915999799, -78.37698894087999690, 12.62985940900000159 ) ) ;
#22308=CARTESIAN_POINT ( 'NONE',  ( 12.69619287811000063, -21.75083378359999742, -1.799475295154000065 ) ) ;
#22309=EDGE_LOOP ( 'NONE', ( #47716, #58190, #815, #19203 ) ) ;
#22310=CARTESIAN_POINT ( 'NONE',  ( -8.813891479040833588, -25.01010130368336348, -8.872963530600353366 ) ) ;
#22313=CARTESIAN_POINT ( 'NONE',  ( 7.640030139758000161, -18.69283065396999888, -10.18491068059999805 ) ) ;
#22316=CARTESIAN_POINT ( 'NONE',  ( 2.627446458840999810, -1.635584759237999952, 3.037392460054000320 ) ) ;
#22317=CARTESIAN_POINT ( 'NONE',  ( -1.931043762602999925, -56.02180874340999850, -12.75761570867999950 ) ) ;
#22319=ADVANCED_FACE ( 'NONE', ( #51927 ), #12049, .F. ) ;
#22320=ORIENTED_EDGE ( 'NONE', *, *, #10858, .F. ) ;
#22321=CIRCLE ( 'NONE', #54369, 1.749999999999998890 ) ;
#22327=ORIENTED_EDGE ( 'NONE', *, *, #35924, .T. ) ;
#22332=EDGE_LOOP ( 'NONE', ( #29736, #31461, #15353, #4299 ) ) ;
#22334=VECTOR ( 'NONE', #3541, 1000.000000000000000 ) ;
#22336=ORIENTED_EDGE ( 'NONE', *, *, #7254, .F. ) ;
#22337=CARTESIAN_POINT ( 'NONE',  ( 7.553727747492950506, -60.48581381148435554, 7.997114030238977378 ) ) ;
#22340=ORIENTED_EDGE ( 'NONE', *, *, #2907, .T. ) ;
#22341=DIRECTION ( 'NONE',  ( 0.7071067811865474617, 0.000000000000000000, -0.7071067811865474617 ) ) ;
#22345=CYLINDRICAL_SURFACE ( 'NONE', #7622, 1.750000000000001332 ) ;
#22346=CARTESIAN_POINT ( 'NONE',  ( -7.627487606607999737, -18.70221404512000163, -10.35845616727999996 ) ) ;
#22349=CARTESIAN_POINT ( 'NONE',  ( -1.405334848770694034, -54.48507051970170068, 12.50716844827185348 ) ) ;
#22350=CARTESIAN_POINT ( 'NONE',  ( 7.678690995210999404, -58.55648180022999583, -10.59551070212999946 ) ) ;
#22351=LINE ( 'NONE', #39770, #29362 ) ;
#22359=CARTESIAN_POINT ( 'NONE',  ( -12.43647099681000157, -17.08193128089000012, -0.03491583288330000340 ) ) ;
#22360=CARTESIAN_POINT ( 'NONE',  ( 10.45205659049000069, -19.23767314807999895, -7.651160337241000420 ) ) ;
#22361=CARTESIAN_POINT ( 'NONE',  ( 1.288488638074000159, -24.53564939367999997, 12.54709296483000003 ) ) ;
#22362=CARTESIAN_POINT ( 'NONE',  ( -8.137215171344100995, -60.25155696365447255, -7.401770473314702059 ) ) ;
#22364=CARTESIAN_POINT ( 'NONE',  ( -3.095372243593999873, -1.512137290291999836, 1.882642529173000012 ) ) ;
#22366=ADVANCED_FACE ( 'NONE', ( #48083 ), #25614, .F. ) ;
#22369=CARTESIAN_POINT ( 'NONE',  ( 12.43410103870000150, -61.24137177736000126, -1.192638008239000014 ) ) ;
#22372=FACE_BOUND ( 'NONE', #9867, .T. ) ;
#22375=FACE_OUTER_BOUND ( 'NONE', #6152, .T. ) ;
#22376=AXIS2_PLACEMENT_3D ( 'NONE', #42188, #37747, #15016 ) ;
#22387=CARTESIAN_POINT ( 'NONE',  ( -9.788011744299998540, -61.32881292732000134, 7.956359616248999345 ) ) ;
#22388=CARTESIAN_POINT ( 'NONE',  ( 0.000000000000000000, -55.54999999966999980, 12.00000000000000000 ) ) ;
#22389=CARTESIAN_POINT ( 'NONE',  ( -3.476885736642000069, -0.7853606339641999723, 0.9048613863073000640 ) ) ;
#22390=CARTESIAN_POINT ( 'NONE',  ( -10.71931710301092266, -76.33463918441997009, -4.979328733251163541 ) ) ;
#22391=CARTESIAN_POINT ( 'NONE',  ( 12.43356840162999966, -24.71269674488000234, -0.8410229959428999758 ) ) ;
#22392=CARTESIAN_POINT ( 'NONE',  ( -1.930989179114000143, -58.55453807205000061, 12.80896991324999945 ) ) ;
#22398=CARTESIAN_POINT ( 'NONE',  ( -12.75761570869000039, -59.57819125629999490, -1.931043762602999925 ) ) ;
#22401=CARTESIAN_POINT ( 'NONE',  ( 10.26605847043819075, -77.90552223423264877, -5.914160144501205529 ) ) ;
#22402=CARTESIAN_POINT ( 'NONE',  ( 3.250000000000000000, -1.250000000000000000, 0.000000000000000000 ) ) ;
#22403=ORIENTED_EDGE ( 'NONE', *, *, #49041, .T. ) ;
#22404=EDGE_CURVE ( 'NONE', #40525, #2165, #43755, .T. ) ;
#22406=CARTESIAN_POINT ( 'NONE',  ( -9.213130513665999999, -53.79475660653999824, -8.533779407502999348 ) ) ;
#22409=ORIENTED_EDGE ( 'NONE', *, *, #3204, .F. ) ;
#22410=VECTOR ( 'NONE', #31397, 1000.000000000000000 ) ;
#22415=ORIENTED_EDGE ( 'NONE', *, *, #40204, .T. ) ;
#22419=CARTESIAN_POINT ( 'NONE',  ( 11.91901974179999968, -77.27860818038000446, 5.468333046474000980 ) ) ;
#22425=ORIENTED_EDGE ( 'NONE', *, *, #29942, .F. ) ;
#22426=CARTESIAN_POINT ( 'NONE',  ( 0.000000000000000000, -0.6500000000000000222, 0.000000000000000000 ) ) ;
#22428=CARTESIAN_POINT ( 'NONE',  ( -6.282410744257000523, -75.96962114363998353, 10.58616248715999930 ) ) ;
#22431=CARTESIAN_POINT ( 'NONE',  ( 0.4088352756822764000, -2.714880510813482584, 3.556394378621883234 ) ) ;
#22434=DIRECTION ( 'NONE',  ( -0.7026410690473252618, -0.1122098755728027641, 0.7026410690473252618 ) ) ;
#22436=CARTESIAN_POINT ( 'NONE',  ( 10.65724243470759269, -77.26040116651306278, -5.779895665056474563 ) ) ;
#22439=B_SPLINE_SURFACE_WITH_KNOTS ( 'NONE', 3, 3, ( 
 ( #1267, #5381, #14521, #27510 ),
 ( #54687, #41400, #1551, #55262 ),
 ( #19542, #10398, #37540, #23675 ),
 ( #19256, #32514, #14810, #50558 ),
 ( #23388, #15105, #28678, #46730 ),
 ( #10111, #28383, #36377, #46141 ),
 ( #32226, #54403, #10701, #32806 ),
 ( #24264, #37250, #33102, #42280 ) ),
 .UNSPECIFIED., .F., .F., .F.,
 ( 4, 1, 1, 1, 1, 4 ),
 ( 4, 4 ),
 ( -0.01200407345746999990, 0.000000000000000000, 0.3333333333333000081, 0.6666666666667000474, 1.000000000000000000, 1.011997855551999947 ),
 ( -0.3559705542741999906, 1.355970554273999928 ),
 .UNSPECIFIED. ) ;
#22443=CARTESIAN_POINT ( 'NONE',  ( -12.57042253521000141, -52.69905023022000279, 0.000000000000000000 ) ) ;
#22444=DIRECTION ( 'NONE',  ( -1.000000000000000000, 0.000000000000000000, 0.000000000000000000 ) ) ;
#22446=CARTESIAN_POINT ( 'NONE',  ( 7.709155920968100872, -23.92747430419191090, 9.998700314111166776 ) ) ;
#22452=CARTESIAN_POINT ( 'NONE',  ( 4.507156365786499919, -76.04314103804109948, 10.85083221517958663 ) ) ;
#22454=CARTESIAN_POINT ( 'NONE',  ( -8.485281374238999419, 0.000000000000000000, 8.485281374238999419 ) ) ;
#22455=ORIENTED_EDGE ( 'NONE', *, *, #42244, .T. ) ;
#22457=DIRECTION ( 'NONE',  ( 0.7026410690473252618, 0.1122098755728027641, -0.7026410690473252618 ) ) ;
#22469=CARTESIAN_POINT ( 'NONE',  ( 8.424622201753786399, -75.79999999999998295, -8.402754719800665129 ) ) ;
#22471=CARTESIAN_POINT ( 'NONE',  ( 8.305672835130092579, -76.38744052775911086, -8.311290054389553816 ) ) ;
#22479=ADVANCED_FACE ( 'NONE', ( #51544 ), #47126, .F. ) ;
#22482=DIRECTION ( 'NONE',  ( 0.7071067811865475727, 0.000000000000000000, 0.7071067811865475727 ) ) ;
#22487=VERTEX_POINT ( 'NONE', #5773 ) ;
#22490=CARTESIAN_POINT ( 'NONE',  ( 7.943805570349000256, -24.43402324524999969, 9.641149735076000482 ) ) ;
#22492=B_SPLINE_CURVE_WITH_KNOTS ( 'NONE', 3,
 ( #56864, #53009, #48307, #49163, #34407, #3141 ),
 .UNSPECIFIED., .F., .F.,
 ( 4, 1, 1, 4 ),
 ( 0.000000000000000000, 0.3333333333333000081, 0.6666666666667000474, 1.000000000000000000 ),
 .UNSPECIFIED. ) ;
#22498=ORIENTED_EDGE ( 'NONE', *, *, #44185, .F. ) ;
#22503=B_SPLINE_CURVE_WITH_KNOTS ( 'NONE', 3,
 ( #32481, #45811, #660, #15071, #14487, #23355 ),
 .UNSPECIFIED., .F., .F.,
 ( 4, 1, 1, 4 ),
 ( 0.000000000000000000, 0.3333333333333000081, 0.6666666666667000474, 1.000000000000000000 ),
 .UNSPECIFIED. ) ;
#22506=CARTESIAN_POINT ( 'NONE',  ( -12.80820168571000117, -75.83158071878000328, -0.01956446631054999802 ) ) ;
#22507=AXIS2_PLACEMENT_3D ( 'NONE', #33390, #51427, #10983 ) ;
#22509=CARTESIAN_POINT ( 'NONE',  ( 12.80088938724999892, -59.56256651724000051, 1.980532758767000301 ) ) ;
#22511=CARTESIAN_POINT ( 'NONE',  ( 12.68702648026999924, -18.24922088193000036, -1.889939500033999797 ) ) ;
#22512=CARTESIAN_POINT ( 'NONE',  ( -11.61705142569443794, -76.68723828451983593, 1.824568759944894536 ) ) ;
#22515=EDGE_LOOP ( 'NONE', ( #42480, #25307, #20249, #8832, #53564 ) ) ;
#22521=CARTESIAN_POINT ( 'NONE',  ( -10.18948933931999967, -18.78467389927000042, 7.645397892297999931 ) ) ;
#22523=CARTESIAN_POINT ( 'NONE',  ( 0.000000000000000000, -23.15000000000000213, 11.89999999977000122 ) ) ;
#22528=CARTESIAN_POINT ( 'NONE',  ( -3.165411199172029288, -1.979166666666666297, 0.8506806241676482250 ) ) ;
#22530=ORIENTED_EDGE ( 'NONE', *, *, #3397, .F. ) ;
#22531=DIRECTION ( 'NONE',  ( 0.9999548435846228323, 0.000000000000000000, 0.009503199022040218977 ) ) ;
#22532=CARTESIAN_POINT ( 'NONE',  ( 0.005928781627640000024, -53.59886949703999903, 12.66336824414000084 ) ) ;
#22533=CARTESIAN_POINT ( 'NONE',  ( -1.666698456695999919, -59.99181739808000202, -12.50018138922999889 ) ) ;
#22534=CARTESIAN_POINT ( 'NONE',  ( 3.504303451278000026, -2.516831454374000021, -1.857678891402000154 ) ) ;
#22535=CIRCLE ( 'NONE', #14984, 0.5000000000000006661 ) ;
#22537=DIRECTION ( 'NONE',  ( 0.000000000000000000, -0.7071067811866525998, -0.7071067811864425456 ) ) ;
#22538=CARTESIAN_POINT ( 'NONE',  ( -2.598917237794085455, -1.552083333333333037, -1.997276839918474600 ) ) ;
#22540=CARTESIAN_POINT ( 'NONE',  ( -0.9212224518285999642, -61.61954101805999784, 12.54670315985999984 ) ) ;
#22541=CARTESIAN_POINT ( 'NONE',  ( 12.83836748062999966, -18.79372227161000097, 2.062147040910000229 ) ) ;
#22544=ADVANCED_FACE ( 'NONE', ( #46542 ), #50640, .F. ) ;
#22546=CARTESIAN_POINT ( 'NONE',  ( -8.908963061728000454, -79.23128271215000495, -8.963338373884001342 ) ) ;
#22550=CARTESIAN_POINT ( 'NONE',  ( -1.501534314757656308, -61.35152951622679041, 12.70455943744299354 ) ) ;
#22553=CARTESIAN_POINT ( 'NONE',  ( 0.000000000000000000, -33.10361340872000113, 0.000000000000000000 ) ) ;
#22557=EDGE_CURVE ( 'NONE', #19958, #48994, #6358, .T. ) ;
#22558=DIRECTION ( 'NONE',  ( -1.000000000000000000, 0.000000000000000000, 0.000000000000000000 ) ) ;
#22561=CARTESIAN_POINT ( 'NONE',  ( 8.838834764832000701, -23.25000000000000000, -8.838834764832000701 ) ) ;
#22562=EDGE_LOOP ( 'NONE', ( #45241, #25671, #10676, #20884 ) ) ;
#22563=VERTEX_POINT ( 'NONE', #37652 ) ;
#22566=CARTESIAN_POINT ( 'NONE',  ( -1.750000000000000000, -60.04999999966999980, -12.00000000000000000 ) ) ;
#22568=DIRECTION ( 'NONE',  ( 0.000000000000000000, -1.000000000000000000, 0.000000000000000000 ) ) ;
#22570=DIRECTION ( 'NONE',  ( 0.000000000000000000, -1.000000000000000000, 0.000000000000000000 ) ) ;
#22571=CARTESIAN_POINT ( 'NONE',  ( 1.666727925315000025, -23.19174481776000007, -12.50018462903999961 ) ) ;
#22575=CARTESIAN_POINT ( 'NONE',  ( 10.24094026722000095, -79.20834499803000028, -6.917727457792000045 ) ) ;
#22579=CARTESIAN_POINT ( 'NONE',  ( 14.00000000000000000, -0.2000000000000005107, 0.000000000000000000 ) ) ;
#22585=CARTESIAN_POINT ( 'NONE',  ( 12.45567317068999991, -78.14634877619000974, -3.566394712320999805 ) ) ;
#22586=CARTESIAN_POINT ( 'NONE',  ( 5.621201030502000151, -78.17027720837999993, 11.49883638144000031 ) ) ;
#22592=CYLINDRICAL_SURFACE ( 'NONE', #45009, 0.5000000000000006661 ) ;
#22593=LINE ( 'NONE', #202, #42797 ) ;
#22594=DIRECTION ( 'NONE',  ( 0.9999548435846228323, 0.000000000000000000, 0.009503199022040118363 ) ) ;
#22595=TOROIDAL_SURFACE ( 'NONE', #38608, 1.250000000000000000, 0.5000000000000000000 ) ;
#22600=CARTESIAN_POINT ( 'NONE',  ( -3.796701970596999764, -2.846418933659000228, 0.2667143827384000354 ) ) ;
#22602=VERTEX_POINT ( 'NONE', #6064 ) ;
#22604=CARTESIAN_POINT ( 'NONE',  ( -14.00000000000000000, -72.89999999999999147, 0.000000000000000000 ) ) ;
#22605=CARTESIAN_POINT ( 'NONE',  ( -1.250000000000000000, -18.75000000000000000, -12.50000000000000000 ) ) ;
#22606=CARTESIAN_POINT ( 'NONE',  ( 2.062502994258999856, -58.55648180022999583, 12.92181194095999963 ) ) ;
#22607=CARTESIAN_POINT ( 'NONE',  ( -9.287618194362000423, -77.57908599310999875, -9.114789584104999065 ) ) ;
#22608=EDGE_CURVE ( 'NONE', #29770, #24848, #6413, .T. ) ;
#22610=CARTESIAN_POINT ( 'NONE',  ( 11.25874264225000054, -76.71236898706999341, -4.774966140054999642 ) ) ;
#22612=ORIENTED_EDGE ( 'NONE', *, *, #46449, .T. ) ;
#22613=CARTESIAN_POINT ( 'NONE',  ( -12.50000000000000000, -63.73717104351998586, 0.000000000000000000 ) ) ;
#22614=CARTESIAN_POINT ( 'NONE',  ( 9.102137319295220408, -53.82814024817236742, -8.583672456402702267 ) ) ;
#22616=CARTESIAN_POINT ( 'NONE',  ( -1.532229594827145380, -17.87701036866945259, 12.51228690880938110 ) ) ;
#22619=CARTESIAN_POINT ( 'NONE',  ( -3.249661007175000282, -0.7327531080796000351, 2.357191814219000037 ) ) ;
#22620=CARTESIAN_POINT ( 'NONE',  ( -1.799502287691000069, -60.10716680829000325, -12.60413670423000099 ) ) ;
#22625=DIRECTION ( 'NONE',  ( 0.000000000000000000, -1.000000000000000000, 0.000000000000000000 ) ) ;
#22628=EDGE_CURVE ( 'NONE', #35471, #11586, #51570, .T. ) ;
#22631=DIRECTION ( 'NONE',  ( 1.000000000000000000, 0.000000000000000000, 0.000000000000000000 ) ) ;
#22635=ORIENTED_EDGE ( 'NONE', *, *, #27697, .F. ) ;
#22638=CIRCLE ( 'NONE', #57479, 10.40000000000000036 ) ;
#22643=EDGE_CURVE ( 'NONE', #54661, #11972, #2863, .T. ) ;
#22644=ORIENTED_EDGE ( 'NONE', *, *, #27495, .T. ) ;
#22649=CARTESIAN_POINT ( 'NONE',  ( -7.642147947518999729, -22.78485473281999774, -10.55910102242999926 ) ) ;
#22651=CARTESIAN_POINT ( 'NONE',  ( 11.74999999999999289, -78.56041666666666856, 1.538071403320028452 ) ) ;
#22655=CONICAL_SURFACE ( 'NONE', #64, 0.6999999997695000031, 0.7853981633972997312 ) ;
#22656=CARTESIAN_POINT ( 'NONE',  ( -10.36222489919000012, -23.22120223852000009, 7.631889817950999522 ) ) ;
#22657=DIRECTION ( 'NONE',  ( -0.9957542217955486219, -0.04890179608105237746, -0.07798810240279377415 ) ) ;
#22659=CARTESIAN_POINT ( 'NONE',  ( 3.230515030065010951, -78.30642889406193774, 11.63305551197263021 ) ) ;
#22663=CARTESIAN_POINT ( 'NONE',  ( 7.601397897754999633, -55.54999999966999980, -9.369164850722000892 ) ) ;
#22664=CARTESIAN_POINT ( 'NONE',  ( 0.4356486348717999446, -24.88064955810000001, 12.43591427121000237 ) ) ;
#22666=CARTESIAN_POINT ( 'NONE',  ( -1.162810066705999956, -0.7833146285216000537, 3.409566898876999819 ) ) ;
#22670=CARTESIAN_POINT ( 'NONE',  ( 12.55458806508999992, -60.96283916815999504, -1.575041344316999936 ) ) ;
#22677=DIRECTION ( 'NONE',  ( -1.000000000000000000, 0.000000000000000000, 0.000000000000000000 ) ) ;
#22680=EDGE_LOOP ( 'NONE', ( #45231, #2463, #1666, #19667, #12987 ) ) ;
#22683=CARTESIAN_POINT ( 'NONE',  ( -1.980532734072999901, -59.56232686814000488, -12.80090744966000038 ) ) ;
#22685=CARTESIAN_POINT ( 'NONE',  ( -12.85144117167999944, -57.04527983067000463, -1.980464439859999981 ) ) ;
#22687=CARTESIAN_POINT ( 'NONE',  ( -8.971242061857001460, -77.31783216571999162, -8.906291659541000882 ) ) ;
#22689=CARTESIAN_POINT ( 'NONE',  ( 12.61112459819999998, -23.21565178569999688, -1.798929298655999931 ) ) ;
#22690=CARTESIAN_POINT ( 'NONE',  ( -7.648026766715999791, -55.54999999381000464, -10.12290050087000104 ) ) ;
#22694=CARTESIAN_POINT ( 'NONE',  ( 10.88867600136477520, -75.91842355713455959, -4.512338881074533958 ) ) ;
#22697=CARTESIAN_POINT ( 'NONE',  ( -12.58338334673999981, -57.05199022587000002, -1.667961445601999992 ) ) ;
#22701=CARTESIAN_POINT ( 'NONE',  ( -1.799490225533999732, -22.77152778045000048, 12.64500484462999985 ) ) ;
#22702=EDGE_LOOP ( 'NONE', ( #43508, #16456, #18654 ) ) ;
#22704=CARTESIAN_POINT ( 'NONE',  ( -9.641218323587999350, -54.36606991882000273, -7.943737929401001985 ) ) ;
#22712=ORIENTED_EDGE ( 'NONE', *, *, #55001, .T. ) ;
#22716=CARTESIAN_POINT ( 'NONE',  ( 7.344138154013000630, -78.16668243576999942, -10.86413439232000044 ) ) ;
#22723=PLANE ( 'NONE',  #38218 ) ;
#22726=EDGE_CURVE ( 'NONE', #52059, #25178, #18956, .T. ) ;
#22727=CARTESIAN_POINT ( 'NONE',  ( 1.001315002657000131, -61.48522411647999775, -12.50000000000000000 ) ) ;
#22728=CARTESIAN_POINT ( 'NONE',  ( -0.7737575051148579686, -3.456640438237565061, -3.432738176510635952 ) ) ;
#22733=CARTESIAN_POINT ( 'NONE',  ( -10.79065230704753198, -77.08694916350313520, -5.396898631840323368 ) ) ;
#22734=CARTESIAN_POINT ( 'NONE',  ( -9.748677221152634687, -76.51023458671352273, -8.641220746763186966 ) ) ;
#22735=AXIS2_PLACEMENT_3D ( 'NONE', #50096, #40936, #58055 ) ;
#22739=DIRECTION ( 'NONE',  ( 0.000000000000000000, 0.000000000000000000, 1.000000000000000000 ) ) ;
#22741=CARTESIAN_POINT ( 'NONE',  ( 7.639893274927809230, -23.38715751204583171, 10.11462445490727546 ) ) ;
#22742=EDGE_CURVE ( 'NONE', #28360, #13397, #40247, .T. ) ;
#22746=CARTESIAN_POINT ( 'NONE',  ( 0.003566689646507039367, -76.07464878890591820, 11.74978033122256704 ) ) ;
#22748=DIRECTION ( 'NONE',  ( 0.000000000000000000, 1.000000000000000000, 0.000000000000000000 ) ) ;
#22749=ORIENTED_EDGE ( 'NONE', *, *, #23349, .T. ) ;
#22750=LINE ( 'NONE', #36903, #49280 ) ;
#22755=CARTESIAN_POINT ( 'NONE',  ( -1.342463812738999916E-14, -80.75000000002938805, 0.000000000000000000 ) ) ;
#22757=CARTESIAN_POINT ( 'NONE',  ( -1.750000000001000089, -55.55000001292999912, -12.56594318049000059 ) ) ;
#22759=VERTEX_POINT ( 'NONE', #53554 ) ;
#22760=VECTOR ( 'NONE', #26021, 1000.000000000000000 ) ;
#22762=CARTESIAN_POINT ( 'NONE',  ( -0.5999999998848000171, -23.14999999478999726, -11.79999999988000070 ) ) ;
#22773=CARTESIAN_POINT ( 'NONE',  ( 8.343860018000999190, -55.64999999967000122, 8.343860018000999190 ) ) ;
#22774=EDGE_LOOP ( 'NONE', ( #40653, #50824, #25536, #12820, #9787 ) ) ;
#22778=CARTESIAN_POINT ( 'NONE',  ( -7.601397897754999633, -23.24999999758999536, 10.07627163191000008 ) ) ;
#22779=CARTESIAN_POINT ( 'NONE',  ( 12.50000000000000000, -13.07071424677999971, 0.000000000000000000 ) ) ;
#22782=ORIENTED_EDGE ( 'NONE', *, *, #31173, .F. ) ;
#22789=DIRECTION ( 'NONE',  ( 0.000000000000000000, 3.439130521500999441E-11, -1.000000000000000000 ) ) ;
#22790=ORIENTED_EDGE ( 'NONE', *, *, #3245, .F. ) ;
#22791=CARTESIAN_POINT ( 'NONE',  ( 9.369164850722000892, -55.54999999966999980, 7.601397897754999633 ) ) ;
#22799=CARTESIAN_POINT ( 'NONE',  ( 10.62738844531999938, -76.71202665592998926, -6.424126605269999679 ) ) ;
#22804=CARTESIAN_POINT ( 'NONE',  ( 0.000000000000000000, -60.04999999966999980, 12.00000000000000000 ) ) ;
#22805=CARTESIAN_POINT ( 'NONE',  ( -11.52318292100913233, -76.68414653309548612, 2.296907436951973747 ) ) ;
#22807=ORIENTED_EDGE ( 'NONE', *, *, #5195, .F. ) ;
#22812=CYLINDRICAL_SURFACE ( 'NONE', #54200, 11.75000000000000000 ) ;
#22815=DIRECTION ( 'NONE',  ( 0.000000000000000000, 1.000000000000000000, 0.000000000000000000 ) ) ;
#22817=CARTESIAN_POINT ( 'NONE',  ( 10.38645071868999992, -59.57819125629999490, -7.655542440085000067 ) ) ;
#22823=CARTESIAN_POINT ( 'NONE',  ( 0.005523896503961000029, -53.73036543741000060, 12.55021156877000088 ) ) ;
#22825=CARTESIAN_POINT ( 'NONE',  ( -10.09635298636609058, -23.52373519997163953, 7.644087781972075391 ) ) ;
#22831=DIRECTION ( 'NONE',  ( 0.000000000000000000, 1.000000000000000000, 0.000000000000000000 ) ) ;
#22834=CARTESIAN_POINT ( 'NONE',  ( 9.963464501270999918, -55.11723479348000154, -7.659241807016999637 ) ) ;
#22836=ADVANCED_FACE ( 'NONE', ( #44398 ), #17729, .F. ) ;
#22841=CIRCLE ( 'NONE', #46419, 0.5000000000000004441 ) ;
#22842=CARTESIAN_POINT ( 'NONE',  ( -12.59651352883999920, -60.19056208351000237, 1.801710201210000140 ) ) ;
#22843=LINE ( 'NONE', #44996, #21701 ) ;
#22844=DIRECTION ( 'NONE',  ( -1.000000000000000000, 0.000000000000000000, 0.000000000000000000 ) ) ;
#22848=CIRCLE ( 'NONE', #55854, 13.86363636363999952 ) ;
#22849=CARTESIAN_POINT ( 'NONE',  ( -1.001315002657000131, -61.48522411647999775, 12.50000000000000000 ) ) ;
#22856=EDGE_CURVE ( 'NONE', #28471, #35775, #45027, .T. ) ;
#22857=VERTEX_POINT ( 'NONE', #28127 ) ;
#22858=ORIENTED_EDGE ( 'NONE', *, *, #56979, .F. ) ;
#22859=CARTESIAN_POINT ( 'NONE',  ( 0.000000000000000000, -0.2000000000000000111, -3.600000000000000089 ) ) ;
#22860=AXIS2_PLACEMENT_3D ( 'NONE', #22026, #29720, #7303 ) ;
#22861=DIRECTION ( 'NONE',  ( 0.9999548435846228323, 0.000000000000000000, 0.009503199022040218977 ) ) ;
#22864=CARTESIAN_POINT ( 'NONE',  ( 1.056237665594999875, -25.04866013698000060, -12.77256098197999989 ) ) ;
#22867=CARTESIAN_POINT ( 'NONE',  ( 11.86573868791000130, -78.48725095961999898, -1.065667360763999927 ) ) ;
#22870=CARTESIAN_POINT ( 'NONE',  ( -1.232226823824148054, -17.47709088732338856, -12.50408896749709342 ) ) ;
#22875=CARTESIAN_POINT ( 'NONE',  ( -10.24996238026999862, -21.75171076523999858, 7.705119999407000542 ) ) ;
#22876=CARTESIAN_POINT ( 'NONE',  ( -10.46686097783000058, -76.78266118432999576, 7.365735401690999495 ) ) ;
#22883=CARTESIAN_POINT ( 'NONE',  ( -10.18589226633000067, -60.08917723397000543, 7.641012305241000391 ) ) ;
#22884=CARTESIAN_POINT ( 'NONE',  ( -8.970693127363905006, -78.24378014202663678, 7.659364560157510660 ) ) ;
#22889=CARTESIAN_POINT ( 'NONE',  ( -2.707053224964000027, -2.789967474678999526, 2.675433656965999774 ) ) ;
#22891=EDGE_CURVE ( 'NONE', #29025, #4628, #24241, .T. ) ;
#22892=ORIENTED_EDGE ( 'NONE', *, *, #41163, .F. ) ;
#22893=CARTESIAN_POINT ( 'NONE',  ( -0.5705388283852488307, -23.34010097529044003, 10.98520465578149441 ) ) ;
#22894=DIRECTION ( 'NONE',  ( -0.7071067811865475727, 0.000000000000000000, 0.7071067811865475727 ) ) ;
#22897=CARTESIAN_POINT ( 'NONE',  ( 2.062597265787999845, -59.58461666436000570, 12.87024489159000140 ) ) ;
#22898=CARTESIAN_POINT ( 'NONE',  ( 11.82764905900999963, -77.30156278830001781, 5.426413045081000419 ) ) ;
#22900=CIRCLE ( 'NONE', #12529, 12.50000000000000000 ) ;
#22902=CARTESIAN_POINT ( 'NONE',  ( 9.546815224142999767, -17.31472046677999899, 8.130854305520999858 ) ) ;
#22904=CIRCLE ( 'NONE', #19159, 12.25000000000000000 ) ;
#22905=FACE_OUTER_BOUND ( 'NONE', #10373, .T. ) ;
#22906=DIRECTION ( 'NONE',  ( 0.000000000000000000, 0.000000000000000000, -1.000000000000000000 ) ) ;
#22908=CARTESIAN_POINT ( 'NONE',  ( -1.749722766159037324, -18.52411007112459274, 12.54673760678534755 ) ) ;
#22911=CARTESIAN_POINT ( 'NONE',  ( 4.010845454633999552, -1.563237677197000020, -0.2065758488482999922 ) ) ;
#22912=CARTESIAN_POINT ( 'NONE',  ( -1.799490225533999732, -56.02847221959000024, -12.64500484464000074 ) ) ;
#22913=FACE_OUTER_BOUND ( 'NONE', #48289, .T. ) ;
#22916=CARTESIAN_POINT ( 'NONE',  ( -12.50000000000000000, -24.68359816828999698, -1.003641515615000035 ) ) ;
#22918=ORIENTED_EDGE ( 'NONE', *, *, #38310, .T. ) ;
#22921=FACE_OUTER_BOUND ( 'NONE', #14438, .T. ) ;
#22925=CIRCLE ( 'NONE', #24819, 0.6000000000000008660 ) ;
#22928=CARTESIAN_POINT ( 'NONE',  ( -2.437508518915010303, -2.658928065967017584, -2.157570479308826172 ) ) ;
#22929=AXIS2_PLACEMENT_3D ( 'NONE', #16497, #7629, #40971 ) ;
#22931=LINE ( 'NONE', #32638, #8181 ) ;
#22933=ORIENTED_EDGE ( 'NONE', *, *, #49017, .T. ) ;
#22934=CARTESIAN_POINT ( 'NONE',  ( -7.958763982144999360, -54.32301960774000094, -9.723170657514000226 ) ) ;
#22938=AXIS2_PLACEMENT_3D ( 'NONE', #16879, #30143, #48753 ) ;
#22939=CARTESIAN_POINT ( 'NONE',  ( 10.00844281756000065, -55.43109810584000030, 7.647097920671999560 ) ) ;
#22940=EDGE_CURVE ( 'NONE', #51133, #4628, #23862, .T. ) ;
#22941=CARTESIAN_POINT ( 'NONE',  ( -7.705142895619999877, -20.24916621771999914, -10.24998526317999925 ) ) ;
#22942=CARTESIAN_POINT ( 'NONE',  ( -8.179414028884684384, -24.74093020613540617, 9.502908389705549297 ) ) ;
#22945=CARTESIAN_POINT ( 'NONE',  ( -1.750000000001000089, -55.54999998977000075, 12.56594317853999954 ) ) ;
#22948=CARTESIAN_POINT ( 'NONE',  ( 1.980464483675000054, -21.75560170741999855, -12.85140862641999959 ) ) ;
#22956=CARTESIAN_POINT ( 'NONE',  ( 0.8445585116436000739, -24.71040443242999984, 12.43380736237000050 ) ) ;
#22960=CARTESIAN_POINT ( 'NONE',  ( 1.997783339681999948, -1.048587262671999865, -3.414494216060000475 ) ) ;
#22962=CARTESIAN_POINT ( 'NONE',  ( 10.21380041493999968, -56.02847221959000024, 7.668936932630000314 ) ) ;
#22963=CARTESIAN_POINT ( 'NONE',  ( -1.886823409076000102, -23.76319684362000118, -12.68610076205999881 ) ) ;
#22965=DIRECTION ( 'NONE',  ( 0.000000000000000000, -1.000000000000000000, 0.000000000000000000 ) ) ;
#22966=CARTESIAN_POINT ( 'NONE',  ( 0.000000000000000000, -0.6500000000000000222, -3.599999999999761613 ) ) ;
#22969=DIRECTION ( 'NONE',  ( 0.000000000000000000, 1.000000000000000000, 0.000000000000000000 ) ) ;
#22973=ORIENTED_EDGE ( 'NONE', *, *, #20588, .T. ) ;
#22975=VECTOR ( 'NONE', #48119, 1000.000000000000114 ) ;
#22978=CARTESIAN_POINT ( 'NONE',  ( -1.980532758766000212, -56.03743349309000621, -12.80088938803999810 ) ) ;
#22980=CARTESIAN_POINT ( 'NONE',  ( 12.77562786365999870, -53.53761952105000432, -0.5426593252874000184 ) ) ;
#22982=CARTESIAN_POINT ( 'NONE',  ( -3.383423064118999957, -0.8512077160052000657, -2.181280105692999793 ) ) ;
#22983=CARTESIAN_POINT ( 'NONE',  ( 8.485281374238999419, -60.04999999966999980, 8.485281374238999419 ) ) ;
#22984=CARTESIAN_POINT ( 'NONE',  ( -8.179414027356866512, -61.54093020445927209, 9.502908391262463894 ) ) ;
#22986=ORIENTED_EDGE ( 'NONE', *, *, #40043, .F. ) ;
#22987=DIRECTION ( 'NONE',  ( 0.000000000000000000, -1.000000000000000000, 0.000000000000000000 ) ) ;
#22989=CARTESIAN_POINT ( 'NONE',  ( 12.00000000000000000, -23.25000000000000000, 0.000000000000000000 ) ) ;
#22991=CARTESIAN_POINT ( 'NONE',  ( -12.60552511012999943, -60.08917723397000543, -1.799501877793999949 ) ) ;
#22993=ORIENTED_EDGE ( 'NONE', *, *, #54655, .F. ) ;
#22995=CARTESIAN_POINT ( 'NONE',  ( 10.07627163191000008, -55.55000000278000272, 7.601397897754999633 ) ) ;
#22996=ORIENTED_EDGE ( 'NONE', *, *, #38488, .T. ) ;
#22997=VERTEX_POINT ( 'NONE', #23424 ) ;
#22998=LINE ( 'NONE', #13841, #32988 ) ;
#23001=VERTEX_POINT ( 'NONE', #1302 ) ;
#23009=CARTESIAN_POINT ( 'NONE',  ( 5.622921568558999716, -77.92073543972999516, 11.67242091225999978 ) ) ;
#23011=AXIS2_PLACEMENT_3D ( 'NONE', #12593, #39744, #57180 ) ;
#23014=ORIENTED_EDGE ( 'NONE', *, *, #35413, .T. ) ;
#23018=CARTESIAN_POINT ( 'NONE',  ( -0.5814085523173397885, -2.237425844885325699, 3.471270272878386631 ) ) ;
#23019=CARTESIAN_POINT ( 'NONE',  ( 8.260136572142000588, -61.74034376533999335, -9.643347111204001010 ) ) ;
#23020=CARTESIAN_POINT ( 'NONE',  ( -11.38660623898999980, -79.04761274831000151, -4.554589311945999697 ) ) ;
#23022=CARTESIAN_POINT ( 'NONE',  ( -3.453171399369999950, -1.763032031398999999, -0.5706200895263999762 ) ) ;
#23025=CARTESIAN_POINT ( 'NONE',  ( 5.911099458924215178, -77.21592629394673679, -10.46277219946754400 ) ) ;
#23027=EDGE_LOOP ( 'NONE', ( #13175, #50491, #8032, #12852 ) ) ;
#23036=CARTESIAN_POINT ( 'NONE',  ( 2.317456097674912563, -76.05899144437520931, 11.51905596437094914 ) ) ;
#23040=CARTESIAN_POINT ( 'NONE',  ( 7.639893379697014097, -18.61284423925059173, -10.11462454831195323 ) ) ;
#23045=DIRECTION ( 'NONE',  ( 0.000000000000000000, 0.000000000000000000, -1.000000000000000000 ) ) ;
#23047=DIRECTION ( 'NONE',  ( 0.000000000000000000, 0.000000000000000000, 1.000000000000000000 ) ) ;
#23048=CARTESIAN_POINT ( 'NONE',  ( 7.619712398446999657, -18.59595871862000038, -10.35409979026999849 ) ) ;
#23051=CARTESIAN_POINT ( 'NONE',  ( 11.75000000000000000, -76.95000000000000284, 0.000000000000000000 ) ) ;
#23055=CARTESIAN_POINT ( 'NONE',  ( 11.50401822733106627, -76.43342449743093425, -2.391363945934446011 ) ) ;
#23058=CARTESIAN_POINT ( 'NONE',  ( -9.019406119850758685, -17.00707871055384146, -8.666949039027842971 ) ) ;
#23059=EDGE_CURVE ( 'NONE', #54879, #36311, #50891, .T. ) ;
#23060=B_SPLINE_CURVE_WITH_KNOTS ( 'NONE', 3,
 ( #40111, #40413, #58124, #17387, #57830, #8829, #30659, #13544, #4100, #44847, #31535, #48412, #8239, #7949, #4401, #8, #35373, #48695, #22401, #17987, #53398, #22100, #25952, #17686 ),
 .UNSPECIFIED., .F., .F.,
 ( 4, 2, 2, 2, 2, 2, 2, 2, 2, 2, 2, 4 ),
 ( 0.000000000000000000, 0.1250000000000000278, 0.2500000000000000555, 0.3750000000000001110, 0.4375000000000001110, 0.5000000000000001110, 0.6250000000000001110, 0.6875000000000000000, 0.7499999999999998890, 0.8750000000000000000, 0.9375000000000000000, 1.000000000000000000 ),
 .UNSPECIFIED. ) ;
#23061=CARTESIAN_POINT ( 'NONE',  ( -12.56594317819999951, -55.54999998572999687, -1.750000000000000000 ) ) ;
#23063=CARTESIAN_POINT ( 'NONE',  ( -12.54977961484000026, -25.04832888628999754, -0.03757501521676000211 ) ) ;
#23064=ORIENTED_EDGE ( 'NONE', *, *, #11689, .T. ) ;
#23065=ORIENTED_EDGE ( 'NONE', *, *, #5195, .T. ) ;
#23069=DIRECTION ( 'NONE',  ( 0.000000000000000000, -1.000000000000000000, 0.000000000000000000 ) ) ;
#23070=CARTESIAN_POINT ( 'NONE',  ( 10.31444895689000063, -24.30075145017000082, 7.758883253342000685 ) ) ;
#23072=CARTESIAN_POINT ( 'NONE',  ( 10.00831380746999955, -60.17230364551999600, 7.646786653150000390 ) ) ;
#23077=AXIS2_PLACEMENT_3D ( 'NONE', #4235, #53835, #17818 ) ;
#23080=EDGE_LOOP ( 'NONE', ( #51042, #41900, #24526 ) ) ;
#23083=AXIS2_PLACEMENT_3D ( 'NONE', #31282, #35724, #22150 ) ;
#23084=CARTESIAN_POINT ( 'NONE',  ( -1.370379768245999841E-14, -74.59999999999999432, 0.000000000000000000 ) ) ;
#23086=CARTESIAN_POINT ( 'NONE',  ( 5.964045881227000301, -75.66430287301000135, 10.18467341643999902 ) ) ;
#23087=CARTESIAN_POINT ( 'NONE',  ( -1.980584515752000119, -60.06485146591000301, 12.76303204605000197 ) ) ;
#23093=CARTESIAN_POINT ( 'NONE',  ( -9.205846894750999709, -25.00798911347999720, -8.541134278086001785 ) ) ;
#23094=B_SPLINE_CURVE_WITH_KNOTS ( 'NONE', 3,
 ( #37158, #6161, #36576, #23872, #888, #13846, #55173, #14714, #10603, #5863, #41887, #41303, #54877, #28587, #54599, #15014, #36287, #51054, #1464, #19455, #50175, #31844, #18871, #46631 ),
 .UNSPECIFIED., .F., .F.,
 ( 4, 2, 2, 2, 2, 2, 2, 2, 2, 2, 2, 4 ),
 ( 0.000000000000000000, 0.1250000000000006661, 0.2500000000000013323, 0.3750000000000019984, 0.4375000000000026645, 0.5000000000000033307, 0.6250000000000039968, 0.7500000000000046629, 0.8125000000000049960, 0.8437500000000042188, 0.8750000000000035527, 1.000000000000000000 ),
 .UNSPECIFIED. ) ;
#23095=CARTESIAN_POINT ( 'NONE',  ( -8.178338515874317594, -60.10416868444268346, 7.356278612544878470 ) ) ;
#23097=VERTEX_POINT ( 'NONE', #44327 ) ;
#23098=EDGE_CURVE ( 'NONE', #51331, #22110, #36051, .T. ) ;
#23103=CARTESIAN_POINT ( 'NONE',  ( -10.01676221091000052, -18.79058563473000021, 7.658899961851000526 ) ) ;
#23105=DIRECTION ( 'NONE',  ( 0.000000000000000000, 1.000000000000000000, 0.000000000000000000 ) ) ;
#23111=CYLINDRICAL_SURFACE ( 'NONE', #46050, 0.5000000000000006661 ) ;
#23113=ORIENTED_EDGE ( 'NONE', *, *, #37892, .F. ) ;
#23116=CARTESIAN_POINT ( 'NONE',  ( -0.9955135976122998498, -2.700810831311999838, 3.839279387930000009 ) ) ;
#23119=CARTESIAN_POINT ( 'NONE',  ( 7.660431276880000695, -23.19179487662999861, -10.01749742441000102 ) ) ;
#23122=CARTESIAN_POINT ( 'NONE',  ( 12.79895942954000176, -18.19538174383999873, 2.015930660725000045 ) ) ;
#23123=B_SPLINE_SURFACE_WITH_KNOTS ( 'NONE', 3, 3, ( 
 ( #52933, #12482, #18088, #54397, #13934, #36081, #691, #54100, #31341, #35477, #27210, #45249, #35185, #8634, #4798, #39919, #49679, #22799, #40808 ),
 ( #30761, #31929, #21911, #49974, #45545, #400, #13344, #8340, #40217, #44355, #5090, #53217, #9517, #13642, #36371, #31637, #27504, #48794, #31047 ),
 ( #23086, #57934, #41099, #9225, #22506, #110, #18378, #12765, #4505, #40517, #3909, #26337, #17490, #53508, #13048, #26919, #49082, #49383, #26620 ),
 ( #44656, #4209, #22206, #58228, #17792, #35779, #53808, #8931, #44950, #42562, #975, #54964, #54680, #51432, #18959, #51140, #1261, #15099, #15401 ) ),
 .UNSPECIFIED., .F., .F., .F.,
 ( 4, 4 ),
 ( 4, 1, 1, 1, 1, 1, 1, 1, 1, 1, 1, 1, 1, 1, 1, 1, 4 ),
 ( -0.3708084972812999980, 1.370808497280999960 ),
 ( 0.4876602516776999963, 0.5203093532865000759, 0.5529584548952999334, 0.5856075565039999820, 0.6182566581127999505, 0.6509057597216000302, 0.6835548613303999987, 0.7162039629391000473, 0.7488530645478999048, 0.7815021661566999844, 0.8141512677654999530, 0.8468003693742000015, 0.8794494709829999701, 0.9120985725918000497, 0.9447476742004999872, 0.9773967758092999558, 1.010045877418000115 ),
 .UNSPECIFIED. ) ;
#23124=PLANE ( 'NONE',  #8824 ) ;
#23126=B_SPLINE_CURVE_WITH_KNOTS ( 'NONE', 3,
 ( #6995, #24999, #47176, #6412, #12009, #6707 ),
 .UNSPECIFIED., .F., .F.,
 ( 4, 2, 4 ),
 ( 0.000000000000000000, 0.5000000000000000000, 1.000000000000000000 ),
 .UNSPECIFIED. ) ;
#23127=CARTESIAN_POINT ( 'NONE',  ( 8.950130560535999535, -53.59887407320999841, -8.958576480190000524 ) ) ;
#23131=AXIS2_PLACEMENT_3D ( 'NONE', #45396, #32363, #40952 ) ;
#23135=CARTESIAN_POINT ( 'NONE',  ( -12.77649794763000024, -62.10831393445000259, -0.06464137375187999079 ) ) ;
#23137=DIRECTION ( 'NONE',  ( -1.000000000000000000, 0.000000000000000000, 0.000000000000000000 ) ) ;
#23138=VERTEX_POINT ( 'NONE', #3597 ) ;
#23142=CARTESIAN_POINT ( 'NONE',  ( 7.401770473313850296, -55.34844303569387591, 8.137215171344873710 ) ) ;
#23143=EDGE_LOOP ( 'NONE', ( #49285, #43207, #28140, #50078 ) ) ;
#23144=ORIENTED_EDGE ( 'NONE', *, *, #7027, .T. ) ;
#23147=ORIENTED_EDGE ( 'NONE', *, *, #55384, .T. ) ;
#23148=ORIENTED_EDGE ( 'NONE', *, *, #49164, .T. ) ;
#23149=EDGE_CURVE ( 'NONE', #27335, #41402, #39607, .T. ) ;
#23151=CARTESIAN_POINT ( 'NONE',  ( 2.839805762151334179, -1.291666666666666075, 1.636761686205429056 ) ) ;
#23155=CARTESIAN_POINT ( 'NONE',  ( 12.00000000000000000, -18.84999999997999964, -0.7999999999999001243 ) ) ;
#23156=CARTESIAN_POINT ( 'NONE',  ( -10.44428606408999904, -78.37314678282000102, -6.033606583391000200 ) ) ;
#23157=ORIENTED_EDGE ( 'NONE', *, *, #3749, .F. ) ;
#23158=EDGE_LOOP ( 'NONE', ( #40241, #757, #30818, #51208 ) ) ;
#23161=CARTESIAN_POINT ( 'NONE',  ( 0.6454797251309331019, -17.11193487860316154, 12.50471521368260497 ) ) ;
#23163=DIRECTION ( 'NONE',  ( 0.000000000000000000, 0.000000000000000000, -1.000000000000000000 ) ) ;
#23164=CARTESIAN_POINT ( 'NONE',  ( -10.18491068059999805, -23.30716934606000024, 7.640030139755999983 ) ) ;
#23165=CARTESIAN_POINT ( 'NONE',  ( -12.75936573546999853, -77.33770759395000027, -1.003864233875000123 ) ) ;
#23170=DIRECTION ( 'NONE',  ( 0.7071067811865475727, 0.000000000000000000, -0.7071067811865475727 ) ) ;
#23172=EDGE_CURVE ( 'NONE', #1755, #56911, #37240, .T. ) ;
#23176=CARTESIAN_POINT ( 'NONE',  ( 2.905579743612289878, -2.888279987876714916, 1.454858905742103747 ) ) ;
#23178=B_SPLINE_CURVE_WITH_KNOTS ( 'NONE', 3,
 ( #51082, #28030, #41918, #6186, #41623, #1202, #54628, #19775, #24198, #49915, #54339, #19194, #55200, #37186, #18901, #23327, #54905, #42215, #27447, #1490, #36893, #13878, #14743, #27737 ),
 .UNSPECIFIED., .F., .F.,
 ( 4, 2, 2, 2, 2, 2, 2, 2, 2, 2, 2, 4 ),
 ( 0.000000000000000000, 0.1250000000000006939, 0.2500000000000013878, 0.3750000000000016653, 0.4375000000000018319, 0.5000000000000018874, 0.6250000000000022204, 0.7500000000000025535, 0.8125000000000027756, 0.8437500000000022204, 0.8750000000000017764, 1.000000000000000000 ),
 .UNSPECIFIED. ) ;
#23179=AXIS2_PLACEMENT_3D ( 'NONE', #39368, #49990, #41409 ) ;
#23183=CARTESIAN_POINT ( 'NONE',  ( 3.542727183245000244, -3.072224769576999748, -1.391102635753999950 ) ) ;
#23186=CARTESIAN_POINT ( 'NONE',  ( 0.4515105396429240914, -23.54721902467404959, 10.99076531923714661 ) ) ;
#23187=DIRECTION ( 'NONE',  ( -1.000000000000000000, 0.000000000000000000, 0.000000000000000000 ) ) ;
#23189=EDGE_CURVE ( 'NONE', #10285, #24723, #40779, .T. ) ;
#23191=CARTESIAN_POINT ( 'NONE',  ( -3.201433918554999813, -77.91211383888000341, 12.61309089657999927 ) ) ;
#23194=CARTESIAN_POINT ( 'NONE',  ( 11.16700323483553348, -78.47423932945110892, 3.653994498481349495 ) ) ;
#23195=EDGE_LOOP ( 'NONE', ( #17928, #2602, #43232, #57338 ) ) ;
#23199=CARTESIAN_POINT ( 'NONE',  ( 7.655555357433999397, -22.77795407709999864, -10.38646360829000059 ) ) ;
#23202=CARTESIAN_POINT ( 'NONE',  ( -0.7824435345810000220, -1.673265174611999972, 3.939770163431000061 ) ) ;
#23203=CARTESIAN_POINT ( 'NONE',  ( -1.667916687244999974, -55.50150862742999891, -12.49168433577000137 ) ) ;
#23205=EDGE_LOOP ( 'NONE', ( #12038, #48759, #37897, #37742, #27745 ) ) ;
#23207=DIRECTION ( 'NONE',  ( -1.000000000000000000, 0.000000000000000000, 0.000000000000000000 ) ) ;
#23208=VERTEX_POINT ( 'NONE', #17762 ) ;
#23211=CARTESIAN_POINT ( 'NONE',  ( 0.000000000000000000, -39.49523982883999906, 0.000000000000000000 ) ) ;
#23216=AXIS2_PLACEMENT_3D ( 'NONE', #38645, #48670, #39509 ) ;
#23217=ORIENTED_EDGE ( 'NONE', *, *, #531, .F. ) ;
#23219=CARTESIAN_POINT ( 'NONE',  ( -2.921860942912723580, -2.637121803128768871, -1.423448106538530267 ) ) ;
#23221=EDGE_CURVE ( 'NONE', #13012, #2890, #11959, .T. ) ;
#23222=B_SPLINE_SURFACE_WITH_KNOTS ( 'NONE', 3, 3, ( 
 ( #721, #45576, #18698, #23119 ),
 ( #10422, #36692, #51170, #42005 ),
 ( #10724, #14545, #28702, #46164 ),
 ( #46753, #33425, #15431, #5689 ),
 ( #18990, #1287, #46454, #5982 ),
 ( #6272, #42305, #23989, #19567 ),
 ( #24289, #27824, #32247, #11016 ),
 ( #41126, #1872, #55881, #37860 ),
 ( #5403, #50291, #45870, #41422 ),
 ( #1005, #19281, #36982, #54996 ),
 ( #10138, #28113, #47040, #38442 ),
 ( #6570, #25442, #12160, #52609 ),
 ( #29571, #6861, #56459, #20732 ),
 ( #16013, #7443, #39021, #56749 ),
 ( #57033, #34290, #33716, #24581 ),
 ( #7150, #30146, #38730, #34576 ),
 ( #43461, #48196, #42597, #16592 ) ),
 .UNSPECIFIED., .F., .F., .F.,
 ( 4, 1, 1, 1, 1, 1, 1, 1, 1, 1, 1, 1, 1, 1, 4 ),
 ( 4, 4 ),
 ( -0.01011786823680000010, 0.000000000000000000, 0.08333333333333001192, 0.1666666666667000196, 0.2500000000000000000, 0.3333333333333000081, 0.4166666666666999919, 0.5000000000000000000, 0.5833333333333000637, 0.6666666666667000474, 0.7500000000000000000, 0.8333333333333000637, 0.9166666666667000474, 1.000000000000000000, 1.010371592463000123 ),
 ( -0.3559705548529999986, 1.357613344742000017 ),
 .UNSPECIFIED. ) ;
#23228=ORIENTED_EDGE ( 'NONE', *, *, #42573, .F. ) ;
#23231=DIRECTION ( 'NONE',  ( 1.000000000000000000, 0.000000000000000000, 0.000000000000000000 ) ) ;
#23232=CARTESIAN_POINT ( 'NONE',  ( -12.02332076413289208, -78.43441775370509106, 2.418180990960641541 ) ) ;
#23234=CARTESIAN_POINT ( 'NONE',  ( 11.74999999999999289, -77.06041666666664014, 1.538071403320028452 ) ) ;
#23235=CARTESIAN_POINT ( 'NONE',  ( 1.538071403319964281, -78.66458333333332575, 11.75000000000000711 ) ) ;
#23236=CARTESIAN_POINT ( 'NONE',  ( -7.668936932637000048, -59.57152778012000027, -10.21380041493999968 ) ) ;
#23238=CARTESIAN_POINT ( 'NONE',  ( 11.31056051666590889, -76.47239290234516318, 3.271005276656067107 ) ) ;
#23242=CARTESIAN_POINT ( 'NONE',  ( 12.18685347097914118, -78.20858279583087835, 0.8549723098153251266 ) ) ;
#23245=DIRECTION ( 'NONE',  ( 0.000000000000000000, -1.000000000000000000, 2.878889714326999635E-13 ) ) ;
#23247=CARTESIAN_POINT ( 'NONE',  ( -0.9212224518303000487, -24.81954101839000160, 12.54670315981999984 ) ) ;
#23249=CARTESIAN_POINT ( 'NONE',  ( 3.618123952455000403, -1.801525618456000011, -0.1863489967816000237 ) ) ;
#23253=CARTESIAN_POINT ( 'NONE',  ( 10.42274798264000069, -58.55365779174999830, 7.691916945401000127 ) ) ;
#23254=CARTESIAN_POINT ( 'NONE',  ( -1.666698456700999920, -23.19181739840000134, -12.50018138921000066 ) ) ;
#23255=CARTESIAN_POINT ( 'NONE',  ( 13.94241845804000057, -69.26002936526001008, 4.312607202219999873E-05 ) ) ;
#23256=CARTESIAN_POINT ( 'NONE',  ( -1.667474681734999908, -3.461675931787000060, 2.801048656332000064 ) ) ;
#23257=EDGE_CURVE ( 'NONE', #25542, #891, #3470, .T. ) ;
#23260=CARTESIAN_POINT ( 'NONE',  ( -11.79999999999999893, -23.15000000000999947, -0.5999999999999999778 ) ) ;
#23269=AXIS2_PLACEMENT_3D ( 'NONE', #55623, #32287, #19031 ) ;
#23270=DIRECTION ( 'NONE',  ( 0.000000000000000000, -1.000000000000000000, 0.000000000000000000 ) ) ;
#23273=CYLINDRICAL_SURFACE ( 'NONE', #36807, 1.750000000000000000 ) ;
#23275=CARTESIAN_POINT ( 'NONE',  ( -9.022377653937999398, -77.81737393437001060, -8.854484771337999049 ) ) ;
#23276=CARTESIAN_POINT ( 'NONE',  ( -4.310687854694967847, -76.39525775715499378, -11.00524620388241814 ) ) ;
#23279=CARTESIAN_POINT ( 'NONE',  ( -0.8898229089153880667, -53.77675468783602497, -12.70296869040735999 ) ) ;
#23281=EDGE_CURVE ( 'NONE', #29379, #31775, #44994, .T. ) ;
#23282=CARTESIAN_POINT ( 'NONE',  ( -3.630949683906000036, -75.80000000000001137, -11.17491406647000041 ) ) ;
#23283=DIRECTION ( 'NONE',  ( 0.000000000000000000, 0.000000000000000000, 1.000000000000000000 ) ) ;
#23286=CARTESIAN_POINT ( 'NONE',  ( -2.062673488410000200, -18.67547726287999765, 12.82904109062999964 ) ) ;
#23290=EDGE_CURVE ( 'NONE', #57774, #13927, #41073, .T. ) ;
#23291=( NAMED_UNIT ( * ) SI_UNIT ( $, .STERADIAN. ) SOLID_ANGLE_UNIT ( ) );
#23293=ORIENTED_EDGE ( 'NONE', *, *, #25230, .F. ) ;
#23294=CYLINDRICAL_SURFACE ( 'NONE', #56347, 1.750000000000000000 ) ;
#23298=VECTOR ( 'NONE', #26339, 1000.000000000000000 ) ;
#23299=DIRECTION ( 'NONE',  ( -1.000000000000000000, 0.000000000000000000, 0.000000000000000000 ) ) ;
#23300=CARTESIAN_POINT ( 'NONE',  ( 10.41144070832756618, -18.47453159777755261, -7.610433246107068506 ) ) ;
#23301=CARTESIAN_POINT ( 'NONE',  ( -7.710118476714000302, -58.54977139529999164, 10.18499221086999995 ) ) ;
#23302=CIRCLE ( 'NONE', #35544, 0.5000000000000004441 ) ;
#23303=DIRECTION ( 'NONE',  ( 0.000000000000000000, 0.7071067811866525998, -0.7071067811864425456 ) ) ;
#23305=VECTOR ( 'NONE', #6023, 1000.000000000000000 ) ;
#23310=CARTESIAN_POINT ( 'NONE',  ( 9.754023262367999436, -76.18045457895999562, -7.509630405475999915 ) ) ;
#23312=VECTOR ( 'NONE', #35158, 1000.000000000000000 ) ;
#23314=CARTESIAN_POINT ( 'NONE',  ( -3.047510419343540278, -2.390893416076438349, -1.759566424157797293 ) ) ;
#23315=CARTESIAN_POINT ( 'NONE',  ( 7.618394338655000375, -60.02713821237000502, -10.53494418060999926 ) ) ;
#23316=CARTESIAN_POINT ( 'NONE',  ( 10.16243366810999937, -79.25472372342998995, -6.864696462387000153 ) ) ;
#23319=CARTESIAN_POINT ( 'NONE',  ( 12.50483465194472465, -24.86452578687064019, 0.6958747604659799579 ) ) ;
#23320=CARTESIAN_POINT ( 'NONE',  ( -8.710754228814030498, -76.98910444386174845, 8.358220830707420390 ) ) ;
#23322=B_SPLINE_CURVE_WITH_KNOTS ( 'NONE', 3,
 ( #38182, #11052, #47654, #7182, #2192, #15750 ),
 .UNSPECIFIED., .F., .F.,
 ( 4, 2, 4 ),
 ( 0.000000000000000000, 0.5000000000000000000, 1.000000000000000000 ),
 .UNSPECIFIED. ) ;
#23324=B_SPLINE_CURVE_WITH_KNOTS ( 'NONE', 3,
 ( #28937, #34225, #15949, #47565, #47272, #25378, #46982, #6510 ),
 .UNSPECIFIED., .F., .F.,
 ( 4, 2, 2, 4 ),
 ( 0.000000000000000000, 0.4999999999999971134, 0.7499999999999985567, 1.000000000000000000 ),
 .UNSPECIFIED. ) ;
#23327=CARTESIAN_POINT ( 'NONE',  ( 7.921335223404320836, -24.55094696616630401, 10.04563431748756130 ) ) ;
#23332=CARTESIAN_POINT ( 'NONE',  ( 0.04984446912208501806, -76.07435069114738724, 11.74969986336399153 ) ) ;
#23339=LINE ( 'NONE', #54920, #6282 ) ;
#23341=CARTESIAN_POINT ( 'NONE',  ( 0.000000000000000000, 0.000000000000000000, 12.00000000000000000 ) ) ;
#23342=CARTESIAN_POINT ( 'NONE',  ( 10.36289663187999999, -18.79893657682999830, -7.633501051924000080 ) ) ;
#23343=CARTESIAN_POINT ( 'NONE',  ( 13.99936781018472232, -46.09579702914000165, 0.1330447863085613691 ) ) ;
#23346=CARTESIAN_POINT ( 'NONE',  ( 12.71107039379005066, -54.54871969218108063, 1.717622521766782873 ) ) ;
#23349=EDGE_CURVE ( 'NONE', #46033, #41082, #22503, .T. ) ;
#23350=CARTESIAN_POINT ( 'NONE',  ( 11.28642253013168606, -76.73199622251708263, 4.309372704845956470 ) ) ;
#23351=CARTESIAN_POINT ( 'NONE',  ( 12.52134121561634750, -60.72745484868493548, 1.618935178750384285 ) ) ;
#23352=CIRCLE ( 'NONE', #16735, 3.600000000000000089 ) ;
#23354=AXIS2_PLACEMENT_3D ( 'NONE', #8359, #27233, #31657 ) ;
#23355=CARTESIAN_POINT ( 'NONE',  ( 10.42531124905999995, -23.26485148473999942, 7.624341765453999997 ) ) ;
#23359=ADVANCED_FACE ( 'NONE', ( #33067 ), #9489, .F. ) ;
#23362=ORIENTED_EDGE ( 'NONE', *, *, #49369, .F. ) ;
#23365=ORIENTED_EDGE ( 'NONE', *, *, #34201, .F. ) ;
#23366=CARTESIAN_POINT ( 'NONE',  ( 8.999999998907000531, -3.999999998907000087, -1.966783332313999974E-09 ) ) ;
#23368=EDGE_CURVE ( 'NONE', #56557, #37071, #25202, .T. ) ;
#23369=CARTESIAN_POINT ( 'NONE',  ( 7.618386461959000044, -60.02712559312999474, 10.53495196325000016 ) ) ;
#23370=DIRECTION ( 'NONE',  ( -0.009503199022040095811, 0.000000000000000000, 0.9999548435846228323 ) ) ;
#23374=ADVANCED_FACE ( 'NONE', ( #23640 ), #12918, .F. ) ;
#23375=EDGE_LOOP ( 'NONE', ( #28011, #10524, #55239, #38154, #43979 ) ) ;
#23376=CARTESIAN_POINT ( 'NONE',  ( 7.655984445742698874, -60.50337239307589954, -10.06694410270556617 ) ) ;
#23377=VERTEX_POINT ( 'NONE', #5923 ) ;
#23383=CARTESIAN_POINT ( 'NONE',  ( -3.000161766333798496, -2.032779362115749056, -1.313064309588372502 ) ) ;
#23385=CARTESIAN_POINT ( 'NONE',  ( 7.648026768024999811, -18.75000001589999954, -10.12290050218000026 ) ) ;
#23387=CARTESIAN_POINT ( 'NONE',  ( 1.667917367010000040, -60.08056692637000396, -12.49306752636999995 ) ) ;
#23388=CARTESIAN_POINT ( 'NONE',  ( 12.92181194095999963, -58.55648180022999583, -2.062502994258999856 ) ) ;
#23395=ADVANCED_FACE ( 'NONE', ( #10667 ), #340, .F. ) ;
#23396=CARTESIAN_POINT ( 'NONE',  ( -1.636761686205434607, -3.416666666666666519, 2.839805762151332402 ) ) ;
#23397=DIRECTION ( 'NONE',  ( 0.4045602624632262945, 0.8201597332662526885, -0.4045602624632262945 ) ) ;
#23398=DIRECTION ( 'NONE',  ( -0.7071067811865475727, 0.000000000000000000, 0.7071067811865475727 ) ) ;
#23399=AXIS2_PLACEMENT_3D ( 'NONE', #23853, #28271, #27983 ) ;
#23400=CARTESIAN_POINT ( 'NONE',  ( 2.162570926564036267, -3.427626334641581174, -2.781109552613596492 ) ) ;
#23404=DIRECTION ( 'NONE',  ( 0.7071067811865475727, 0.000000000000000000, -0.7071067811865475727 ) ) ;
#23406=ORIENTED_EDGE ( 'NONE', *, *, #372, .F. ) ;
#23408=CARTESIAN_POINT ( 'NONE',  ( 3.503826891403000410, -2.000465391789000069, 1.486277921227999954 ) ) ;
#23411=FACE_OUTER_BOUND ( 'NONE', #32894, .T. ) ;
#23412=LINE ( 'NONE', #44982, #12839 ) ;
#23413=CARTESIAN_POINT ( 'NONE',  ( 0.4261031628618374700, -1.966084445875545095, 3.248887486669486346 ) ) ;
#23414=DIRECTION ( 'NONE',  ( 1.000000000000000000, -1.534448722697999916E-11, 4.093422659635999854E-14 ) ) ;
#23416=CARTESIAN_POINT ( 'NONE',  ( -10.45204383630000144, -19.23743350652000217, -7.651147548127999798 ) ) ;
#23417=CARTESIAN_POINT ( 'NONE',  ( -12.94500186834999944, -78.49632521500998905, -0.3167920335189999825 ) ) ;
#23418=B_SPLINE_SURFACE_WITH_KNOTS ( 'NONE', 3, 3, ( 
 ( #26925, #17798, #31053, #26626 ),
 ( #44661, #35784, #53813, #13647 ),
 ( #36088, #31642, #406, #9231 ),
 ( #17203, #13940, #49389, #36376 ),
 ( #18384, #54402, #3914, #48514 ),
 ( #35482, #26055, #35191, #53223 ),
 ( #12770, #8937, #21917, #39925 ),
 ( #17495, #13054, #23093, #23674 ),
 ( #55261, #18966, #28090, #41104 ),
 ( #9815, #54970, #55555, #10397 ),
 ( #33101, #23961, #19541, #19254 ),
 ( #982, #32513, #49979, #36958 ),
 ( #14520, #14809, #5095, #32805 ),
 ( #50851, #5379, #1550, #19840 ),
 ( #28382, #6247, #37539, #46729 ),
 ( #50557, #45550, #42279, #46140 ),
 ( #37249, #696, #10110, #18678 ) ),
 .UNSPECIFIED., .F., .F., .F.,
 ( 4, 1, 1, 1, 1, 1, 1, 1, 1, 1, 1, 1, 1, 1, 4 ),
 ( 4, 4 ),
 ( -0.01011400514348999996, 0.000000000000000000, 0.08333333333333001192, 0.1666666666667000196, 0.2500000000000000000, 0.3333333333333000081, 0.4166666666666999919, 0.5000000000000000000, 0.5833333333333000637, 0.6666666666667000474, 0.7500000000000000000, 0.8333333333333000637, 0.9166666666667000474, 1.000000000000000000, 1.010365328128000062 ),
 ( -0.3559705546945000076, 1.357612395619000045 ),
 .UNSPECIFIED. ) ;
#23424=CARTESIAN_POINT ( 'NONE',  ( -12.56594317984999876, -18.75000000536999778, 1.750000000000000000 ) ) ;
#23428=CARTESIAN_POINT ( 'NONE',  ( 12.50679926046298540, -54.49581646307559879, -1.424414840068722210 ) ) ;
#23433=DIRECTION ( 'NONE',  ( 0.7592504785509028853, -0.04890181650812019248, -0.6489586451866029559 ) ) ;
#23437=ORIENTED_EDGE ( 'NONE', *, *, #29733, .F. ) ;
#23439=CARTESIAN_POINT ( 'NONE',  ( 1.698401934077000019, -17.77985954096000043, 12.66748707612999958 ) ) ;
#23441=AXIS2_PLACEMENT_3D ( 'NONE', #32505, #45542, #55253 ) ;
#23444=DIRECTION ( 'NONE',  ( -0.7071067811865473507, 1.433669009702094715E-08, -0.7071067811865473507 ) ) ;
#23446=VERTEX_POINT ( 'NONE', #25211 ) ;
#23447=ORIENTED_EDGE ( 'NONE', *, *, #57827, .T. ) ;
#23450=DIRECTION ( 'NONE',  ( -1.000000000000000000, 0.000000000000000000, 0.000000000000000000 ) ) ;
#23452=CARTESIAN_POINT ( 'NONE',  ( 10.21026636382018715, -61.05606635917384040, 7.764233071724031099 ) ) ;
#23454=CARTESIAN_POINT ( 'NONE',  ( 5.488019371950999314, -76.75873275214000557, 11.73632836356999931 ) ) ;
#23456=FACE_OUTER_BOUND ( 'NONE', #41441, .T. ) ;
#23457=CARTESIAN_POINT ( 'NONE',  ( -7.142344700882925501, -76.62645210080975744, 9.337520193347636166 ) ) ;
#23469=ORIENTED_EDGE ( 'NONE', *, *, #26299, .F. ) ;
#23470=CARTESIAN_POINT ( 'NONE',  ( 1.081559480311999888, -3.500000000000000000, -3.328697807033000000 ) ) ;
#23472=CARTESIAN_POINT ( 'NONE',  ( 0.1577469407304877558, -18.24957415542310457, -11.00002392222777381 ) ) ;
#23475=CARTESIAN_POINT ( 'NONE',  ( 12.50000000000000000, -17.31640971966000109, -1.003652782652999953 ) ) ;
#23477=EDGE_CURVE ( 'NONE', #21690, #13072, #29630, .T. ) ;
#23478=LINE ( 'NONE', #28480, #1837 ) ;
#23482=CARTESIAN_POINT ( 'NONE',  ( -4.505485344499866152, -76.29322575161846487, -10.85157014020616906 ) ) ;
#23487=CARTESIAN_POINT ( 'NONE',  ( -2.839805762151343949, -2.958333333333331705, 1.636761686205412181 ) ) ;
#23492=CARTESIAN_POINT ( 'NONE',  ( -3.599999993293999889, -0.2000000067061999953, -5.600095662875000459E-09 ) ) ;
#23494=ORIENTED_EDGE ( 'NONE', *, *, #23943, .T. ) ;
#23503=ORIENTED_EDGE ( 'NONE', *, *, #55384, .F. ) ;
#23504=VERTEX_POINT ( 'NONE', #6920 ) ;
#23505=DIRECTION ( 'NONE',  ( 0.000000000000000000, 0.000000000000000000, -1.000000000000000000 ) ) ;
#23506=AXIS2_PLACEMENT_3D ( 'NONE', #35257, #35856, #17564 ) ;
#23507=ORIENTED_EDGE ( 'NONE', *, *, #17332, .T. ) ;
#23508=DIRECTION ( 'NONE',  ( -1.893719484533980254E-11, -1.538483569415980182E-07, -0.9999999999999882316 ) ) ;
#23509=CARTESIAN_POINT ( 'NONE',  ( 7.342331066867000544, -55.64999999967000122, -8.190859204290999784 ) ) ;
#23511=CARTESIAN_POINT ( 'NONE',  ( -8.060167321872524937, -54.17936585329436383, -9.621722524781038288 ) ) ;
#23512=EDGE_CURVE ( 'NONE', #28878, #7381, #33185, .T. ) ;
#23518=DIRECTION ( 'NONE',  ( 0.7071067811865475727, 0.000000000000000000, -0.7071067811865475727 ) ) ;
#23521=CARTESIAN_POINT ( 'NONE',  ( 0.000000000000000000, 4.040000000000000036, 0.000000000000000000 ) ) ;
#23524=CARTESIAN_POINT ( 'NONE',  ( 2.297810458696917024, -76.55893299319272671, 11.52286801981460229 ) ) ;
#23528=CARTESIAN_POINT ( 'NONE',  ( -8.815468636818138748, -78.01289059936662795, -8.261290690983104312 ) ) ;
#23530=CARTESIAN_POINT ( 'NONE',  ( -12.70956139859000089, -18.59498835749000278, 1.933780970936999966 ) ) ;
#23532=CARTESIAN_POINT ( 'NONE',  ( 12.99510751537000353, -63.10294702886003648, 6.911973076623003642 ) ) ;
#23535=CARTESIAN_POINT ( 'NONE',  ( -10.01676216528999852, -60.00941514989000325, -7.658899892539000831 ) ) ;
#23538=CARTESIAN_POINT ( 'NONE',  ( -7.601397897754999633, -23.24999999758999536, 10.07627163191000008 ) ) ;
#23540=CARTESIAN_POINT ( 'NONE',  ( 12.43652404745000162, -24.92065244538000002, 0.1284256373645999982 ) ) ;
#23543=CARTESIAN_POINT ( 'NONE',  ( 0.000000000000000000, -23.15000000000000213, -11.89999999977000122 ) ) ;
#23546=CARTESIAN_POINT ( 'NONE',  ( 11.45652112554999924, -75.89040228657998455, -4.228683781523999485 ) ) ;
#23552=CARTESIAN_POINT ( 'NONE',  ( 10.20679554288637014, -54.56427274253432813, 7.770327721630681417 ) ) ;
#23554=CARTESIAN_POINT ( 'NONE',  ( -1.750000000000000000, -18.75000000240999753, 12.50000000000000000 ) ) ;
#23556=VECTOR ( 'NONE', #9855, 1000.000000000000000 ) ;
#23561=CYLINDRICAL_SURFACE ( 'NONE', #54165, 1.750000000000000000 ) ;
#23562=CARTESIAN_POINT ( 'NONE',  ( 8.909545442949999838, -59.94999999967000548, 8.061017305527000687 ) ) ;
#23563=AXIS2_PLACEMENT_3D ( 'NONE', #39039, #3322, #57050 ) ;
#23565=CARTESIAN_POINT ( 'NONE',  ( 3.643968819545335691, -75.84956472831228780, -11.20974552281418823 ) ) ;
#23566=ORIENTED_EDGE ( 'NONE', *, *, #36821, .T. ) ;
#23567=CARTESIAN_POINT ( 'NONE',  ( -12.50728617048089575, -17.00024476471455870, -0.1757989196447104219 ) ) ;
#23569=VERTEX_POINT ( 'NONE', #19708 ) ;
#23571=CARTESIAN_POINT ( 'NONE',  ( 11.74988006023992071, -76.93969616181793469, -1.039067677832774095 ) ) ;
#23573=DIRECTION ( 'NONE',  ( 0.000000000000000000, -1.000000000000000000, 0.000000000000000000 ) ) ;
#23574=ORIENTED_EDGE ( 'NONE', *, *, #38239, .T. ) ;
#23577=ORIENTED_EDGE ( 'NONE', *, *, #16251, .F. ) ;
#23578=CARTESIAN_POINT ( 'NONE',  ( 12.49989298246999958, -55.60773379962999741, 1.666426105558999948 ) ) ;
#23581=CARTESIAN_POINT ( 'NONE',  ( -12.70956478397999945, -23.40497526616000101, -1.933781249744999986 ) ) ;
#23584=B_SPLINE_CURVE_WITH_KNOTS ( 'NONE', 3,
 ( #23282, #41287, #49872, #32407, #45737, #5273, #23565, #40706, #36562, #36271, #31829, #871, #10291, #22694, #37430, #18857, #4981, #9704 ),
 .UNSPECIFIED., .F., .F.,
 ( 4, 2, 2, 2, 2, 2, 2, 2, 4 ),
 ( 0.000000000000000000, 0.1250000000000000000, 0.2500000000000000000, 0.3750000000000000000, 0.5000000000000000000, 0.6250000000000000000, 0.7500000000000000000, 0.8750000000000000000, 1.000000000000000000 ),
 .UNSPECIFIED. ) ;
#23587=CARTESIAN_POINT ( 'NONE',  ( 0.8804656547936360322, -16.97196605292967320, -12.70299681151658255 ) ) ;
#23592=ORIENTED_EDGE ( 'NONE', *, *, #6297, .T. ) ;
#23593=CARTESIAN_POINT ( 'NONE',  ( -1.476182556144000069, -76.40189909139999713, 12.22114576030999977 ) ) ;
#23595=CARTESIAN_POINT ( 'NONE',  ( -2.921934676155967914, -1.896386797793808254, -1.963134887269489814 ) ) ;
#23597=ADVANCED_FACE ( 'NONE', ( #38799 ), #34357, .F. ) ;
#23598=CARTESIAN_POINT ( 'NONE',  ( 7.624757096145000190, -60.60351363786999457, -10.47516529250999895 ) ) ;
#23599=CARTESIAN_POINT ( 'NONE',  ( 6.688645397968000950, -78.84642772177998893, 10.27915892414000076 ) ) ;
#23603=CARTESIAN_POINT ( 'NONE',  ( 2.307541886207349346, -2.788560972538888905, -2.288008278024395548 ) ) ;
#23604=CARTESIAN_POINT ( 'NONE',  ( 9.418236657459665651, -77.35379839889799314, 7.544531841333499855 ) ) ;
#23605=CARTESIAN_POINT ( 'NONE',  ( -9.837774000978795286, -17.68535604387229299, 7.850041800338160236 ) ) ;
#23606=ORIENTED_EDGE ( 'NONE', *, *, #27484, .T. ) ;
#23611=CARTESIAN_POINT ( 'NONE',  ( -0.2932567490044000191, -2.500169754918000198, -3.702492619799000462 ) ) ;
#23612=ADVANCED_FACE ( 'NONE', ( #52394 ), #6329, .T. ) ;
#23615=CARTESIAN_POINT ( 'NONE',  ( 8.510637803266750012, -76.00995353112250541, 8.100988122022512172 ) ) ;
#23618=ORIENTED_EDGE ( 'NONE', *, *, #5363, .T. ) ;
#23619=ADVANCED_FACE ( 'NONE', ( #52105 ), #37637, .F. ) ;
#23622=DIRECTION ( 'NONE',  ( -0.7071067811865475727, 0.000000000000000000, -0.7071067811865475727 ) ) ;
#23623=VECTOR ( 'NONE', #38741, 1000.000000000000000 ) ;
#23624=CARTESIAN_POINT ( 'NONE',  ( 1.025029370886000101E-14, -0.2000000000000005107, 0.000000000000000000 ) ) ;
#23629=CARTESIAN_POINT ( 'NONE',  ( 7.620012214426000519, -18.79439747922000237, -10.53562508625000049 ) ) ;
#23630=LINE ( 'NONE', #41642, #17359 ) ;
#23631=VERTEX_POINT ( 'NONE', #37927 ) ;
#23633=DIRECTION ( 'NONE',  ( -1.411446131769000029E-10, -6.386278974555000074E-09, 1.000000000000000000 ) ) ;
#23636=CARTESIAN_POINT ( 'NONE',  ( 4.230813626878798139, -77.79940820322376283, 11.25355361728754922 ) ) ;
#23639=CARTESIAN_POINT ( 'NONE',  ( 12.50485692592770626, -61.66593462659085390, -0.6924071803391340652 ) ) ;
#23640=FACE_OUTER_BOUND ( 'NONE', #4489, .T. ) ;
#23641=CIRCLE ( 'NONE', #56646, 0.5000000000000004441 ) ;
#23647=ORIENTED_EDGE ( 'NONE', *, *, #45300, .T. ) ;
#23650=EDGE_CURVE ( 'NONE', #34714, #44555, #55951, .T. ) ;
#23651=ORIENTED_EDGE ( 'NONE', *, *, #26588, .F. ) ;
#23655=CARTESIAN_POINT ( 'NONE',  ( 7.981656248376999940, -61.51865039470999363, 10.08154475893999980 ) ) ;
#23656=DIRECTION ( 'NONE',  ( 0.000000000000000000, 1.000000000000000000, 0.000000000000000000 ) ) ;
#23659=ORIENTED_EDGE ( 'NONE', *, *, #36924, .T. ) ;
#23660=CARTESIAN_POINT ( 'NONE',  ( -10.10447584118665887, -24.45118490549160484, 7.864774383118550816 ) ) ;
#23668=EDGE_CURVE ( 'NONE', #55921, #30078, #4475, .T. ) ;
#23674=CARTESIAN_POINT ( 'NONE',  ( -9.101516360816999551, -24.88066799059000189, -8.485522730740999720 ) ) ;
#23675=CARTESIAN_POINT ( 'NONE',  ( 12.53239398060000021, -56.03513569577999931, -1.667936688463999895 ) ) ;
#23677=ORIENTED_EDGE ( 'NONE', *, *, #38488, .F. ) ;
#23679=VECTOR ( 'NONE', #47578, 1000.000000000000114 ) ;
#23685=CARTESIAN_POINT ( 'NONE',  ( 8.190859204290999784, -59.94999999967000548, -7.342331066867000544 ) ) ;
#23686=CARTESIAN_POINT ( 'NONE',  ( 2.077614454027474356, -3.074804716019511108, 2.843664572838004112 ) ) ;
#23691=FACE_OUTER_BOUND ( 'NONE', #54171, .T. ) ;
#23693=ORIENTED_EDGE ( 'NONE', *, *, #50416, .F. ) ;
#23694=EDGE_CURVE ( 'NONE', #32275, #40010, #35511, .T. ) ;
#23695=FACE_OUTER_BOUND ( 'NONE', #54358, .T. ) ;
#23696=CARTESIAN_POINT ( 'NONE',  ( -8.190817883596805515, -55.56980390652987722, 7.342377162852848471 ) ) ;
#23702=CARTESIAN_POINT ( 'NONE',  ( -10.04568514500204834, -54.24913840230841799, -7.921286339674650456 ) ) ;
#23706=CARTESIAN_POINT ( 'NONE',  ( 10.52682159589000044, -55.37432398227000618, -7.605688676848999741 ) ) ;
#23707=EDGE_CURVE ( 'NONE', #35685, #26753, #25511, .T. ) ;
#23717=CARTESIAN_POINT ( 'NONE',  ( -7.921329716846313040, -54.24906234234291702, 10.04564005580055053 ) ) ;
#23722=EDGE_LOOP ( 'NONE', ( #42033, #6922, #58062, #12943 ) ) ;
#23728=ORIENTED_EDGE ( 'NONE', *, *, #7349, .T. ) ;
#23730=CARTESIAN_POINT ( 'NONE',  ( 0.8537148449481000156, -17.29501854091000013, 12.43377424872999981 ) ) ;
#23737=ORIENTED_EDGE ( 'NONE', *, *, #2671, .T. ) ;
#23740=LINE ( 'NONE', #15173, #23305 ) ;
#23741=CARTESIAN_POINT ( 'NONE',  ( 1.318114156659812908, -61.53572477165494803, -12.70261578166418737 ) ) ;
#23743=CYLINDRICAL_SURFACE ( 'NONE', #34111, 12.05000000000000071 ) ;
#23744=CARTESIAN_POINT ( 'NONE',  ( -10.38645071867999903, -22.77819125662999866, 7.655542440070999710 ) ) ;
#23748=CARTESIAN_POINT ( 'NONE',  ( -9.455880892872714938, -76.64914396672122621, 6.975925114676199357 ) ) ;
#23755=DIRECTION ( 'NONE',  ( 0.000000000000000000, -1.000000000000000000, 0.000000000000000000 ) ) ;
#23758=LINE ( 'NONE', #19627, #21258 ) ;
#23760=ORIENTED_EDGE ( 'NONE', *, *, #41347, .T. ) ;
#23762=ADVANCED_FACE ( 'NONE', ( #17226 ), #22284, .F. ) ;
#23763=CARTESIAN_POINT ( 'NONE',  ( 0.5999999999999999778, -18.84999999999999787, -10.98362417419999915 ) ) ;
#23764=CARTESIAN_POINT ( 'NONE',  ( -10.19635340580301097, -77.65732487548163476, 5.890683536056261715 ) ) ;
#23767=CARTESIAN_POINT ( 'NONE',  ( -10.55511172854000002, -77.89828514651000546, 7.611100925114999249 ) ) ;
#23771=CARTESIAN_POINT ( 'NONE',  ( 12.76303204298000082, -60.06485150663000638, -1.980584515756000030 ) ) ;
#23775=PLANE ( 'NONE',  #44606 ) ;
#23778=CARTESIAN_POINT ( 'NONE',  ( 2.863963203921999767, -1.163821851618000114, 2.815564610575000071 ) ) ;
#23782=DIRECTION ( 'NONE',  ( 0.000000000000000000, 1.000000000000000000, 0.000000000000000000 ) ) ;
#23791=DIRECTION ( 'NONE',  ( 0.000000000000000000, 0.000000000000000000, -1.000000000000000000 ) ) ;
#23792=ADVANCED_FACE ( 'NONE', ( #8368 ), #19473, .F. ) ;
#23793=ORIENTED_EDGE ( 'NONE', *, *, #23929, .F. ) ;
#23794=EDGE_LOOP ( 'NONE', ( #41775, #45173, #31109, #24314, #8643, #55094, #2699 ) ) ;
#23797=CARTESIAN_POINT ( 'NONE',  ( 10.42531125072000009, -55.53514854654000032, 7.624341767124000135 ) ) ;
#23800=CARTESIAN_POINT ( 'NONE',  ( 3.397703318627999458, -2.301921241517000283, -0.1580915791678000060 ) ) ;
#23806=LINE ( 'NONE', #19677, #19909 ) ;
#23807=CARTESIAN_POINT ( 'NONE',  ( 2.714678808024538537, -0.9374999996105841671, 1.968551052210687491 ) ) ;
#23810=CARTESIAN_POINT ( 'NONE',  ( -8.583677312632392642, -24.97185920791575597, 9.102132574107123730 ) ) ;
#23811=VECTOR ( 'NONE', #27393, 999.9999999999998863 ) ;
#23812=CARTESIAN_POINT ( 'NONE',  ( 7.653559626114000203, -60.09848884406000025, -10.01235002625000092 ) ) ;
#23815=DIRECTION ( 'NONE',  ( 0.000000000000000000, 1.000000000000000000, 0.000000000000000000 ) ) ;
#23817=CARTESIAN_POINT ( 'NONE',  ( 0.8338927961504822850, -61.60053577702804262, -12.50366901606078684 ) ) ;
#23820=AXIS2_PLACEMENT_3D ( 'NONE', #7214, #6924, #24930 ) ;
#23821=CARTESIAN_POINT ( 'NONE',  ( -12.83838672491000032, -18.79401612030999758, 2.062170725306000207 ) ) ;
#23824=LINE ( 'NONE', #14965, #12877 ) ;
#23826=FACE_OUTER_BOUND ( 'NONE', #49154, .T. ) ;
#23827=EDGE_CURVE ( 'NONE', #41145, #15626, #57670, .T. ) ;
#23828=CARTESIAN_POINT ( 'NONE',  ( 10.18491068058999893, -55.49283065365000311, 7.640030139739999449 ) ) ;
#23829=CARTESIAN_POINT ( 'NONE',  ( -2.062312494845999655, -23.22715659892999795, -12.83634740209000036 ) ) ;
#23831=CARTESIAN_POINT ( 'NONE',  ( 3.079612352930999997, -2.255588905189000126, -1.632544367598999902 ) ) ;
#23835=CARTESIAN_POINT ( 'NONE',  ( 1.629367637654999923, -60.48263643365999798, 12.46114270829000148 ) ) ;
#23836=CARTESIAN_POINT ( 'NONE',  ( -1.308715794654506714, -24.74404499199616225, -12.70256747356970628 ) ) ;
#23837=CARTESIAN_POINT ( 'NONE',  ( -10.11011427823000020, -76.30152490496999462, -6.578289829005000477 ) ) ;
#23838=VERTEX_POINT ( 'NONE', #54130 ) ;
#23845=CARTESIAN_POINT ( 'NONE',  ( 12.77657003520000067, -53.48789974419999993, -0.1588669551757000142 ) ) ;
#23851=CARTESIAN_POINT ( 'NONE',  ( -1.423702045482348355, -0.7708333333332365589, 3.195623485684481846 ) ) ;
#23853=CARTESIAN_POINT ( 'NONE',  ( 0.000000000000000000, -6.100000000000000533, 0.000000000000000000 ) ) ;
#23854=ORIENTED_EDGE ( 'NONE', *, *, #38292, .F. ) ;
#23858=VERTEX_POINT ( 'NONE', #54997 ) ;
#23861=DIRECTION ( 'NONE',  ( -0.7071067811865475727, 0.000000000000000000, 0.7071067811865475727 ) ) ;
#23862=B_SPLINE_CURVE_WITH_KNOTS ( 'NONE', 3,
 ( #29016, #15145, #15446, #28716, #14559, #10436 ),
 .UNSPECIFIED., .F., .F.,
 ( 4, 1, 1, 4 ),
 ( 0.000000000000000000, 0.3333333311588953518, 0.6666666623178907347, 0.9999999934767860310 ),
 .UNSPECIFIED. ) ;
#23863=ORIENTED_EDGE ( 'NONE', *, *, #53645, .T. ) ;
#23865=CIRCLE ( 'NONE', #31392, 8.500000000000000000 ) ;
#23871=CARTESIAN_POINT ( 'NONE',  ( 12.79895942951000087, -54.99538174351000208, 2.015930660723999956 ) ) ;
#23872=CARTESIAN_POINT ( 'NONE',  ( 7.764217752274555018, -24.25600304964931198, -10.21028588416213800 ) ) ;
#23873=VERTEX_POINT ( 'NONE', #27534 ) ;
#23874=CARTESIAN_POINT ( 'NONE',  ( -12.43359700617999941, -24.70705514168999883, -0.8500729763772000291 ) ) ;
#23875=CARTESIAN_POINT ( 'NONE',  ( 8.251802458334349666, -24.80055625133919150, 9.431055090842324518 ) ) ;
#23876=EDGE_CURVE ( 'NONE', #1253, #51133, #13965, .T. ) ;
#23877=DIRECTION ( 'NONE',  ( 0.000000000000000000, -1.000000000000000000, 9.095767555747001212E-12 ) ) ;
#23881=CARTESIAN_POINT ( 'NONE',  ( -12.70253230850552484, -17.02944272789559577, -0.9891673677432125666 ) ) ;
#23885=CARTESIAN_POINT ( 'NONE',  ( 1.623944433304999935, -76.15286196370999505, -12.20239005717999881 ) ) ;
#23886=CARTESIAN_POINT ( 'NONE',  ( -0.6665627444282328229, -2.459101225494768173, -3.519322218571878658 ) ) ;
#23888=CARTESIAN_POINT ( 'NONE',  ( 8.438902753042999194, -78.66805746472999772, -8.898539530003999332 ) ) ;
#23890=CARTESIAN_POINT ( 'NONE',  ( -10.14950121161999874, -59.55077027461999961, -7.674627477469999626 ) ) ;
#23892=CARTESIAN_POINT ( 'NONE',  ( 11.93057425389842230, -78.28777072277550531, -1.853708691180695034 ) ) ;
#23893=DIRECTION ( 'NONE',  ( -1.000000000000000000, 0.000000000000000000, 0.000000000000000000 ) ) ;
#23894=AXIS2_PLACEMENT_3D ( 'NONE', #2917, #20916, #38919 ) ;
#23895=VERTEX_POINT ( 'NONE', #50292 ) ;
#23896=CARTESIAN_POINT ( 'NONE',  ( -12.50000000000000000, -55.55000000278000272, 1.750000000000000000 ) ) ;
#23901=CARTESIAN_POINT ( 'NONE',  ( 3.866260457929000083, -2.040678692333000033, -0.1798930524384000085 ) ) ;
#23905=CARTESIAN_POINT ( 'NONE',  ( -8.279988104818777117, -76.13722974528235454, 8.336922021432648933 ) ) ;
#23910=CARTESIAN_POINT ( 'NONE',  ( 12.70299718800749034, -25.02583482805175308, 0.8845454261173205657 ) ) ;
#23915=ADVANCED_FACE ( 'NONE', ( #14253 ), #142, .F. ) ;
#23918=CARTESIAN_POINT ( 'NONE',  ( 7.981651535810999398, -17.28135615487000010, -10.08154952397000059 ) ) ;
#23919=CARTESIAN_POINT ( 'NONE',  ( 7.714303428875997959, -52.49705297113997204, -12.53545825868000385 ) ) ;
#23922=CARTESIAN_POINT ( 'NONE',  ( 12.80000000000000071, -6.000000000000000000, 0.000000000000000000 ) ) ;
#23924=CARTESIAN_POINT ( 'NONE',  ( -9.998152690805172327, -77.90614940129853494, 6.679595771618969557 ) ) ;
#23928=CARTESIAN_POINT ( 'NONE',  ( -2.963791440107999886, -3.194030605494999620, 2.387889716789000083 ) ) ;
#23929=EDGE_CURVE ( 'NONE', #19894, #23873, #37372, .T. ) ;
#23931=CARTESIAN_POINT ( 'NONE',  ( 1.704789469149224468, -18.29653838474853345, -12.53199752960647828 ) ) ;
#23935=EDGE_LOOP ( 'NONE', ( #57059, #7534, #55035, #13547, #12153 ) ) ;
#23939=EDGE_LOOP ( 'NONE', ( #7540, #9412, #7596, #25059 ) ) ;
#23941=EDGE_CURVE ( 'NONE', #34968, #43600, #23412, .T. ) ;
#23943=EDGE_CURVE ( 'NONE', #43546, #18440, #32248, .T. ) ;
#23944=CARTESIAN_POINT ( 'NONE',  ( 10.19019669288000074, -59.99643762534999780, 7.646965578510999784 ) ) ;
#23945=CARTESIAN_POINT ( 'NONE',  ( 0.000000000000000000, -23.25000000000000000, 12.00000000000000000 ) ) ;
#23948=ORIENTED_EDGE ( 'NONE', *, *, #7086, .F. ) ;
#23950=VERTEX_POINT ( 'NONE', #40841 ) ;
#23952=CARTESIAN_POINT ( 'NONE',  ( -8.799999998347999508, 1.651506137787999915E-09, -5.811488053374000191E-09 ) ) ;
#23954=DIRECTION ( 'NONE',  ( -0.9999999999995751176, 0.000000000000000000, -9.217549095371770968E-07 ) ) ;
#23961=CARTESIAN_POINT ( 'NONE',  ( -8.252521514711000705, -24.93405767894999769, -9.650901483139000092 ) ) ;
#23963=CARTESIAN_POINT ( 'NONE',  ( 9.546815224142999767, -17.31472046677999899, 8.130854305520999858 ) ) ;
#23969=B_SPLINE_CURVE_WITH_KNOTS ( 'NONE', 3,
 ( #11547, #17114, #35100, #11257, #16544, #29238, #34238, #38970, #47580, #2966, #47285, #2397, #52558, #51992, #52845, #3261, #15963, #12111, #47860, #20966, #25105, #48147, #7677, #43132, #25678, #2690, #20683, #38682, #30096, #16259 ),
 .UNSPECIFIED., .F., .F.,
 ( 4, 2, 2, 2, 2, 2, 2, 2, 2, 2, 2, 2, 2, 2, 4 ),
 ( 0.000000000000000000, 0.1250000000000017764, 0.1875000000000011380, 0.2500000000000004996, 0.3124999999999998890, 0.3749999999999992784, 0.4999999999999981126, 0.5624999999999975575, 0.6249999999999970024, 0.6874999999999964473, 0.7499999999999958922, 0.8124999999999953371, 0.8437499999999951150, 0.8749999999999948930, 1.000000000000000000 ),
 .UNSPECIFIED. ) ;
#23971=CARTESIAN_POINT ( 'NONE',  ( -7.646091287767998956, -18.29149945126999910, 10.13691902392999999 ) ) ;
#23972=CONICAL_SURFACE ( 'NONE', #9825, 12.14999999923000118, 0.7853981633972997312 ) ;
#23974=CARTESIAN_POINT ( 'NONE',  ( -3.095526911397207925, -3.210505338566441491, 1.678399268257390942 ) ) ;
#23978=CARTESIAN_POINT ( 'NONE',  ( 3.269729146447236889, -0.8932291625415327285, -0.8778406017527962124 ) ) ;
#23980=EDGE_LOOP ( 'NONE', ( #3118, #51327, #43759, #10068 ) ) ;
#23984=CARTESIAN_POINT ( 'NONE',  ( 1.200170490667999967, -61.23405701964999537, -12.43444080554000131 ) ) ;
#23986=EDGE_CURVE ( 'NONE', #13118, #21333, #1006, .T. ) ;
#23989=CARTESIAN_POINT ( 'NONE',  ( 7.961052042448998556, -24.53567435024999810, -9.783216378915000178 ) ) ;
#23992=LINE ( 'NONE', #1290, #26992 ) ;
#23993=DIRECTION ( 'NONE',  ( 0.000000000000000000, 1.000000000000000000, 0.000000000000000000 ) ) ;
#23996=CARTESIAN_POINT ( 'NONE',  ( 7.646944981205999525, -55.60364172484999301, -10.19022195329000091 ) ) ;
#24005=EDGE_CURVE ( 'NONE', #27991, #13401, #3373, .T. ) ;
#24006=CARTESIAN_POINT ( 'NONE',  ( -9.841113773926924324, -53.96371975908724750, 8.121706172282767255 ) ) ;
#24007=ORIENTED_EDGE ( 'NONE', *, *, #3721, .T. ) ;
#24009=EDGE_CURVE ( 'NONE', #46616, #20659, #12161, .T. ) ;
#24012=AXIS2_PLACEMENT_3D ( 'NONE', #12507, #34642, #13075 ) ;
#24014=ORIENTED_EDGE ( 'NONE', *, *, #35064, .T. ) ;
#24016=B_SPLINE_CURVE_WITH_KNOTS ( 'NONE', 3,
 ( #9006, #50330, #36440, #41459, #27286, #26991 ),
 .UNSPECIFIED., .F., .F.,
 ( 4, 2, 4 ),
 ( 0.000000000000000000, 0.5000000000000000000, 1.000000000000000000 ),
 .UNSPECIFIED. ) ;
#24017=VECTOR ( 'NONE', #24635, 1000.000000000000000 ) ;
#24018=EDGE_LOOP ( 'NONE', ( #13765, #51845, #50021, #30168 ) ) ;
#24019=ORIENTED_EDGE ( 'NONE', *, *, #47097, .T. ) ;
#24020=CARTESIAN_POINT ( 'NONE',  ( -1.382886570147999983, -17.36901780168000187, 12.65982054476000052 ) ) ;
#24021=CARTESIAN_POINT ( 'NONE',  ( -9.546815223803999828, -54.11472046612000497, -8.130854305859001485 ) ) ;
#24026=CONICAL_SURFACE ( 'NONE', #25904, 10.29999999923999887, 0.7853981633972997312 ) ;
#24030=ORIENTED_EDGE ( 'NONE', *, *, #32214, .F. ) ;
#24034=CARTESIAN_POINT ( 'NONE',  ( 0.5222397222514810755, -61.96298219368188853, -12.70447686587992564 ) ) ;
#24038=DIRECTION ( 'NONE',  ( 1.000000000000000000, 0.000000000000000000, 0.000000000000000000 ) ) ;
#24040=EDGE_CURVE ( 'NONE', #7896, #49658, #40174, .T. ) ;
#24043=FACE_OUTER_BOUND ( 'NONE', #39113, .T. ) ;
#24046=CARTESIAN_POINT ( 'NONE',  ( -7.624757993428000091, -18.19647951307999989, -10.47516388919000008 ) ) ;
#24047=PLANE ( 'NONE',  #34419 ) ;
#24050=DIRECTION ( 'NONE',  ( 1.000000000000000000, 0.000000000000000000, 0.000000000000000000 ) ) ;
#24051=CARTESIAN_POINT ( 'NONE',  ( 0.07399134906894000441, -2.225452884884000060, 3.805339572302000040 ) ) ;
#24053=ORIENTED_EDGE ( 'NONE', *, *, #9229, .F. ) ;
#24056=CARTESIAN_POINT ( 'NONE',  ( 11.44555184246232749, -77.46784554053439820, 3.079248999555209032 ) ) ;
#24057=B_SPLINE_CURVE_WITH_KNOTS ( 'NONE', 3,
 ( #545, #26767, #26472, #27650, #36803, #8776 ),
 .UNSPECIFIED., .F., .F.,
 ( 4, 1, 1, 4 ),
 ( 0.000000000000000000, 0.3333333311524483422, 0.6666666623049967155, 0.9999999934574449467 ),
 .UNSPECIFIED. ) ;
#24058=VECTOR ( 'NONE', #12274, 1000.000000000000000 ) ;
#24060=CARTESIAN_POINT ( 'NONE',  ( 0.000000000000000000, -15.89905023022000030, 0.000000000000000000 ) ) ;
#24061=LINE ( 'NONE', #19639, #31345 ) ;
#24063=DIRECTION ( 'NONE',  ( 1.000000000000000000, 0.000000000000000000, 0.000000000000000000 ) ) ;
#24064=VECTOR ( 'NONE', #30200, 1000.000000000000114 ) ;
#24067=CARTESIAN_POINT ( 'NONE',  ( -2.495479390352245197, -76.30759454100098083, -11.48357277819591893 ) ) ;
#24072=CARTESIAN_POINT ( 'NONE',  ( -0.8506806241676722058, -2.895833333333333481, 3.165411199172022627 ) ) ;
#24074=DIRECTION ( 'NONE',  ( 0.000000000000000000, 0.000000000000000000, -1.000000000000000000 ) ) ;
#24079=ORIENTED_EDGE ( 'NONE', *, *, #58074, .F. ) ;
#24082=DIRECTION ( 'NONE',  ( 0.000000000000000000, 1.000000000000000000, 0.000000000000000000 ) ) ;
#24085=B_SPLINE_CURVE_WITH_KNOTS ( 'NONE', 3,
 ( #32415, #18580, #32705, #50754, #40714, #9710, #5278, #36278, #55162, #50461, #5855, #46622, #14707, #6151, #41877, #49878, #1455, #9422, #19447, #54301, #18285, #13838, #45446, #31835 ),
 .UNSPECIFIED., .F., .F.,
 ( 4, 2, 2, 2, 2, 2, 2, 2, 2, 2, 2, 4 ),
 ( 0.000000000000000000, 0.1249999999999982236, 0.2499999999999964473, 0.3749999999999946709, 0.4374999999999943934, 0.4999999999999941158, 0.6249999999999946709, 0.7499999999999953371, 0.8124999999999942268, 0.8437499999999936717, 0.8749999999999931166, 1.000000000000000000 ),
 .UNSPECIFIED. ) ;
#24088=EDGE_LOOP ( 'NONE', ( #52631, #55184, #30544, #22918 ) ) ;
#24089=EDGE_CURVE ( 'NONE', #1101, #50911, #25221, .T. ) ;
#24094=ORIENTED_EDGE ( 'NONE', *, *, #58151, .F. ) ;
#24096=CARTESIAN_POINT ( 'NONE',  ( -3.233444005277000155, -2.053647766280000120, 0.09179859873625999256 ) ) ;
#24097=EDGE_LOOP ( 'NONE', ( #29888, #43819, #19584, #32633, #26119 ) ) ;
#24102=CARTESIAN_POINT ( 'NONE',  ( 12.16339525242990049, -79.21041714176394066, 1.568450607538854236 ) ) ;
#24105=ADVANCED_FACE ( 'NONE', ( #49932 ), #56233, .T. ) ;
#24109=CARTESIAN_POINT ( 'NONE',  ( -7.613962745625999062, -60.10639784916000394, -10.53101990622000095 ) ) ;
#24111=CARTESIAN_POINT ( 'NONE',  ( 7.912034776018140647, -76.51566614544198330, 8.694818093870058107 ) ) ;
#24114=CARTESIAN_POINT ( 'NONE',  ( -3.035031770661409833, -3.072304190615608999, 1.160088070061187304 ) ) ;
#24119=DIRECTION ( 'NONE',  ( 0.000000000000000000, -1.000000000000000000, 0.000000000000000000 ) ) ;
#24122=CARTESIAN_POINT ( 'NONE',  ( -10.52682159652000138, -60.22567232035000018, -7.605689092069000345 ) ) ;
#24123=CARTESIAN_POINT ( 'NONE',  ( 1.375482337540088640, -3.499999999999999112, 3.058649307113923577 ) ) ;
#24125=DIRECTION ( 'NONE',  ( 0.000000000000000000, 1.000000000000000000, 0.000000000000000000 ) ) ;
#24127=CARTESIAN_POINT ( 'NONE',  ( -8.611000705966242563, -25.17488119224633536, -9.355851007297125932 ) ) ;
#24128=EDGE_CURVE ( 'NONE', #26499, #13623, #23339, .T. ) ;
#24129=CARTESIAN_POINT ( 'NONE',  ( -10.12290050126000196, -60.04999999958999979, -7.648026767103999646 ) ) ;
#24132=CARTESIAN_POINT ( 'NONE',  ( 12.07501500767000024, -76.43047190101000865, 1.824161567967000019 ) ) ;
#24138=CARTESIAN_POINT ( 'NONE',  ( 10.27342224347061084, -54.73842478141837375, 7.712153330296829701 ) ) ;
#24139=DIRECTION ( 'NONE',  ( 0.000000000000000000, 1.000000000000000000, 0.000000000000000000 ) ) ;
#24146=CIRCLE ( 'NONE', #51515, 0.6000000000000008660 ) ;
#24147=DIRECTION ( 'NONE',  ( -1.000000000000000000, 0.000000000000000000, 0.000000000000000000 ) ) ;
#24148=CARTESIAN_POINT ( 'NONE',  ( -10.42531124903999995, -55.53514851492000304, 7.624341765436000173 ) ) ;
#24151=CIRCLE ( 'NONE', #45825, 0.8000000000000000444 ) ;
#24160=DIRECTION ( 'NONE',  ( 0.000000000000000000, 0.000000000000000000, -1.000000000000000000 ) ) ;
#24161=ORIENTED_EDGE ( 'NONE', *, *, #9639, .F. ) ;
#24162=ORIENTED_EDGE ( 'NONE', *, *, #23512, .T. ) ;
#24164=EDGE_CURVE ( 'NONE', #7256, #587, #45877, .T. ) ;
#24167=EDGE_LOOP ( 'NONE', ( #28356, #54799, #15665 ) ) ;
#24168=CARTESIAN_POINT ( 'NONE',  ( 12.54673279569000144, -53.97202488745999460, 0.9078290272348999990 ) ) ;
#24170=EDGE_CURVE ( 'NONE', #45467, #11618, #28859, .T. ) ;
#24172=CARTESIAN_POINT ( 'NONE',  ( -12.72558241036999860, -23.20131830507999737, -1.930284820930999956 ) ) ;
#24176=CARTESIAN_POINT ( 'NONE',  ( -1.782734487924091393, -17.87754631440509812, -12.71547286926139186 ) ) ;
#24182=CARTESIAN_POINT ( 'NONE',  ( -9.844172144369998989, -75.93141745127000775, 7.391061701651999272 ) ) ;
#24183=VECTOR ( 'NONE', #31822, 1000.000000000000000 ) ;
#24184=CARTESIAN_POINT ( 'NONE',  ( 1.615685760171753360, -2.186269987821578553, 3.127213907787655511 ) ) ;
#24185=CARTESIAN_POINT ( 'NONE',  ( 12.50000000000000000, -13.07071422275999950, 0.000000000000000000 ) ) ;
#24186=CARTESIAN_POINT ( 'NONE',  ( -7.766269599678000013, -78.58776125908998722, -9.491266709826000181 ) ) ;
#24189=CARTESIAN_POINT ( 'NONE',  ( 12.70299804978429137, -16.97411689984641470, -0.8844418155417017591 ) ) ;
#24191=CARTESIAN_POINT ( 'NONE',  ( 3.004897403630924391, -2.819918783981688826, -1.236614688018551123 ) ) ;
#24192=CARTESIAN_POINT ( 'NONE',  ( -9.993982900435000261, -78.00313153835666924, 6.676790657254138672 ) ) ;
#24194=AXIS2_PLACEMENT_3D ( 'NONE', #31435, #13730, #26715 ) ;
#24198=CARTESIAN_POINT ( 'NONE',  ( 9.346069275190213688, -25.16527745691412221, 8.620894635682162743 ) ) ;
#24199=VECTOR ( 'NONE', #32933, 1000.000000000000000 ) ;
#24201=CARTESIAN_POINT ( 'NONE',  ( -3.824246539154000146, -2.306685987230000290, -0.5962100206719000983 ) ) ;
#24204=CARTESIAN_POINT ( 'NONE',  ( -9.012532435264512642, -76.14435526899964657, 7.538916498839152602 ) ) ;
#24208=ORIENTED_EDGE ( 'NONE', *, *, #50223, .F. ) ;
#24209=CARTESIAN_POINT ( 'NONE',  ( 12.70451647735429823, -24.55458569105848454, 1.498866843994218545 ) ) ;
#24210=CARTESIAN_POINT ( 'NONE',  ( 11.63677945028385174, -79.08342241646654713, -2.480315150004160696 ) ) ;
#24215=CARTESIAN_POINT ( 'NONE',  ( 10.35398565887000011, -18.59211376270000216, -7.619387877927000119 ) ) ;
#24216=DIRECTION ( 'NONE',  ( 0.000000000000000000, 1.000000000000000000, 0.000000000000000000 ) ) ;
#24217=B_SPLINE_CURVE_WITH_KNOTS ( 'NONE', 3,
 ( #43168, #29273, #43745, #52598, #16872, #24569 ),
 .UNSPECIFIED., .F., .F.,
 ( 4, 1, 1, 4 ),
 ( 0.000000000000000000, 0.3333333333333000081, 0.6666666666667000474, 1.000000000000000000 ),
 .UNSPECIFIED. ) ;
#24218=EDGE_LOOP ( 'NONE', ( #47719, #15015, #13461 ) ) ;
#24219=ADVANCED_FACE ( 'NONE', ( #32464 ), #39259, .T. ) ;
#24223=CARTESIAN_POINT ( 'NONE',  ( 2.690846299717935874, -77.31017771206632005, 11.76998691515812112 ) ) ;
#24228=CARTESIAN_POINT ( 'NONE',  ( -0.6934022908089999548, -3.137579146514999806, 3.742362521638999961 ) ) ;
#24229=CIRCLE ( 'NONE', #56306, 1.750000000000000666 ) ;
#24231=CARTESIAN_POINT ( 'NONE',  ( 1.405334850311761752, -17.68507052220335751, -12.50716844834626684 ) ) ;
#24235=ORIENTED_EDGE ( 'NONE', *, *, #34552, .F. ) ;
#24237=ORIENTED_EDGE ( 'NONE', *, *, #35004, .T. ) ;
#24240=ADVANCED_FACE ( 'NONE', ( #45500 ), #25108, .T. ) ;
#24241=CIRCLE ( 'NONE', #45967, 13.86363636363999952 ) ;
#24243=CARTESIAN_POINT ( 'NONE',  ( 8.194873807830999723, -17.28956116771000140, 9.389185139535999980 ) ) ;
#24245=CARTESIAN_POINT ( 'NONE',  ( 6.578523888628000194, -78.66055396357999996, 10.10992338718000028 ) ) ;
#24246=CARTESIAN_POINT ( 'NONE',  ( 10.15323304115999825, -61.03079615981999950, 7.760925857031000241 ) ) ;
#24252=CARTESIAN_POINT ( 'NONE',  ( 7.630100270854876854, -78.11902925543334675, 8.993494391708773961 ) ) ;
#24257=DIRECTION ( 'NONE',  ( 0.000000000000000000, 1.000000000000000000, 0.000000000000000000 ) ) ;
#24258=CARTESIAN_POINT ( 'NONE',  ( -12.80000000000000071, -6.000000000000000000, 0.000000000000000000 ) ) ;
#24263=CARTESIAN_POINT ( 'NONE',  ( 12.70451681032941238, -61.97641660161944799, 0.5206746372120837352 ) ) ;
#24264=CARTESIAN_POINT ( 'NONE',  ( 12.82904109066000053, -60.12452273675999947, -2.062673488410000200 ) ) ;
#24266=ORIENTED_EDGE ( 'NONE', *, *, #16512, .T. ) ;
#24271=CARTESIAN_POINT ( 'NONE',  ( -8.220399303327999618, -17.18050618273999675, 9.523318109998999859 ) ) ;
#24274=CARTESIAN_POINT ( 'NONE',  ( 3.405878126756061608, -3.020524467000565760, 0.8975563214481486751 ) ) ;
#24279=CARTESIAN_POINT ( 'NONE',  ( -7.624341766629000539, -55.53514853726999689, 10.42531125022999916 ) ) ;
#24283=CARTESIAN_POINT ( 'NONE',  ( -1.691611010926999947, -61.03082691197000287, -12.66722148972999840 ) ) ;
#24284=AXIS2_PLACEMENT_3D ( 'NONE', #22773, #26597, #41077 ) ;
#24289=CARTESIAN_POINT ( 'NONE',  ( 8.292771711448001071, -25.05529938523999789, -9.770424367364000773 ) ) ;
#24291=CARTESIAN_POINT ( 'NONE',  ( -7.601397897754999633, -18.75000000240999753, -10.07627163191000008 ) ) ;
#24292=FACE_OUTER_BOUND ( 'NONE', #8995, .T. ) ;
#24293=ORIENTED_EDGE ( 'NONE', *, *, #2858, .F. ) ;
#24294=EDGE_CURVE ( 'NONE', #10086, #31168, #54354, .T. ) ;
#24296=AXIS2_PLACEMENT_3D ( 'NONE', #15281, #2303, #5837 ) ;
#24299=CARTESIAN_POINT ( 'NONE',  ( 8.252512830309999714, -53.86594982524999864, -9.650910120403001002 ) ) ;
#24305=CARTESIAN_POINT ( 'NONE',  ( 12.76303204294000082, -18.73514849292999784, 1.980584515756000030 ) ) ;
#24307=DIRECTION ( 'NONE',  ( 0.000000000000000000, -1.000000000000000000, 0.000000000000000000 ) ) ;
#24314=ORIENTED_EDGE ( 'NONE', *, *, #21547, .F. ) ;
#24315=VERTEX_POINT ( 'NONE', #36037 ) ;
#24318=VERTEX_POINT ( 'NONE', #11852 ) ;
#24319=ORIENTED_EDGE ( 'NONE', *, *, #51038, .F. ) ;
#24320=CARTESIAN_POINT ( 'NONE',  ( -1.460729357738999923, -17.90908756797999857, 12.44211643240000065 ) ) ;
#24323=B_SPLINE_SURFACE_WITH_KNOTS ( 'NONE', 3, 3, ( 
 ( #45473, #51072, #37462, #40740 ),
 ( #23315, #28016, #46063, #32152 ),
 ( #27726, #15030, #18311, #28304 ),
 ( #23598, #41610, #1191, #37176 ),
 ( #36594, #5879, #1479, #33026 ),
 ( #19469, #5015, #13868, #31862 ),
 ( #9451, #23019, #41031, #54616 ),
 ( #14154, #9738, #38914, #42202 ),
 ( #51657, #20342, #2347, #24770 ),
 ( #51939, #42493, #38630, #56932 ),
 ( #29750, #56360, #10915, #56648 ),
 ( #2062, #43075, #6467, #28895 ),
 ( #16205, #38337, #25052, #47805 ),
 ( #19764, #34182, #16492, #47524 ),
 ( #6760, #52219, #34471, #10620 ),
 ( #15911, #2633, #28601, #46648 ),
 ( #20911, #20629, #7336, #15619 ) ),
 .UNSPECIFIED., .F., .F., .F.,
 ( 4, 1, 1, 1, 1, 1, 1, 1, 1, 1, 1, 1, 1, 1, 4 ),
 ( 4, 4 ),
 ( -0.01011786823686000071, 0.000000000000000000, 0.08333333333333001192, 0.1666666666667000196, 0.2500000000000000000, 0.3333333333333000081, 0.4166666666666999919, 0.5000000000000000000, 0.5833333333333000637, 0.6666666666667000474, 0.7500000000000000000, 0.8333333333333000637, 0.9166666666667000474, 1.000000000000000000, 1.010371592463000123 ),
 ( -0.3559705548529999986, 1.357613344763000107 ),
 .UNSPECIFIED. ) ;
#24328=EDGE_CURVE ( 'NONE', #26684, #41458, #4845, .T. ) ;
#24329=ORIENTED_EDGE ( 'NONE', *, *, #48364, .T. ) ;
#24332=DIRECTION ( 'NONE',  ( 0.7071067811865474617, 0.000000000000000000, 0.7071067811865474617 ) ) ;
#24334=EDGE_CURVE ( 'NONE', #45569, #40274, #58102, .T. ) ;
#24336=CARTESIAN_POINT ( 'NONE',  ( 1.583004792652944692, -61.25209241118513859, -12.70616254415345558 ) ) ;
#24339=CARTESIAN_POINT ( 'NONE',  ( -1.165746613897999928E-14, -72.79999999999999716, 0.000000000000000000 ) ) ;
#24340=CARTESIAN_POINT ( 'NONE',  ( -10.01235002622999914, -18.70151115557999688, 7.653559626094000201 ) ) ;
#24343=CARTESIAN_POINT ( 'NONE',  ( 0.000000000000000000, 4.040000000000000036, 0.000000000000000000 ) ) ;
#24344=CARTESIAN_POINT ( 'NONE',  ( 4.597354753046301035, -79.22265623326045159, -11.09475667319383341 ) ) ;
#24345=CARTESIAN_POINT ( 'NONE',  ( -10.13402152808999901, -55.07694524364999467, 7.647754144006999155 ) ) ;
#24348=CARTESIAN_POINT ( 'NONE',  ( 1.931086388578000079, -23.29778754190000001, -12.71798269385000069 ) ) ;
#24349=CYLINDRICAL_SURFACE ( 'NONE', #30615, 12.50000000000000000 ) ;
#24351=ADVANCED_FACE ( 'NONE', ( #33973 ), #45088, .F. ) ;
#24353=DIRECTION ( 'NONE',  ( 0.9957542217959282072, -0.04890179607409141094, 0.07798810240231221491 ) ) ;
#24355=CARTESIAN_POINT ( 'NONE',  ( -3.453171399369999950, -1.763032031398999999, -0.5706200895263999762 ) ) ;
#24356=ORIENTED_EDGE ( 'NONE', *, *, #8253, .F. ) ;
#24358=CARTESIAN_POINT ( 'NONE',  ( -0.7705914100935935540, -77.57837515258907501, 11.74754681604737883 ) ) ;
#24361=CARTESIAN_POINT ( 'NONE',  ( -12.77649734579999929, -53.49171487479999598, -0.06478328530389998452 ) ) ;
#24364=CIRCLE ( 'NONE', #10242, 11.00000000000000000 ) ;
#24366=ADVANCED_FACE ( 'NONE', ( #47599 ), #18508, .F. ) ;
#24367=CARTESIAN_POINT ( 'NONE',  ( -13.49939038839240979, -46.09579702914000165, -0.1282931867975413143 ) ) ;
#24373=CARTESIAN_POINT ( 'NONE',  ( -0.1204595238885999980, -0.7297393593719998517, 3.497926457646999943 ) ) ;
#24380=ORIENTED_EDGE ( 'NONE', *, *, #151, .F. ) ;
#24381=EDGE_LOOP ( 'NONE', ( #39408, #37781 ) ) ;
#24383=CARTESIAN_POINT ( 'NONE',  ( -12.50483465198260014, -61.66452578640176796, -0.6958747608064493884 ) ) ;
#24387=ORIENTED_EDGE ( 'NONE', *, *, #17715, .T. ) ;
#24390=ORIENTED_EDGE ( 'NONE', *, *, #3254, .F. ) ;
#24395=EDGE_LOOP ( 'NONE', ( #18588, #13531, #35595, #24676, #49674, #21467, #32706, #11758, #14989, #22712, #49478, #33600 ) ) ;
#24396=CARTESIAN_POINT ( 'NONE',  ( -0.2685658639872000042, -2.674331454374000216, -3.390759574055000058 ) ) ;
#24401=CARTESIAN_POINT ( 'NONE',  ( -7.919595949288999570, -55.64999999965999677, 8.768124086712999699 ) ) ;
#24402=FACE_OUTER_BOUND ( 'NONE', #9642, .T. ) ;
#24403=CIRCLE ( 'NONE', #7460, 0.8000000000000011546 ) ;
#24410=CARTESIAN_POINT ( 'NONE',  ( 6.020971146719677591, -76.53215365127321945, 10.09761672016582246 ) ) ;
#24413=CARTESIAN_POINT ( 'NONE',  ( -12.56594317819999951, -55.54999998572999687, -1.750000000000000000 ) ) ;
#24421=CARTESIAN_POINT ( 'NONE',  ( -8.505985592041961141, -76.26002876382779050, -8.106429104623925852 ) ) ;
#24422=CARTESIAN_POINT ( 'NONE',  ( 10.55910102244999926, -19.21514526754999963, 7.642147947538999730 ) ) ;
#24423=DIRECTION ( 'NONE',  ( 0.000000000000000000, -1.000000000000000000, 0.000000000000000000 ) ) ;
#24427=CARTESIAN_POINT ( 'NONE',  ( 12.66232158686000098, -25.13482640580999927, 0.5080765942054999984 ) ) ;
#24429=CYLINDRICAL_SURFACE ( 'NONE', #55232, 1.750000000000000000 ) ;
#24431=CARTESIAN_POINT ( 'NONE',  ( -8.677390326068000093, -76.10643013234999898, 8.592813855578000926 ) ) ;
#24432=ORIENTED_EDGE ( 'NONE', *, *, #17808, .T. ) ;
#24438=CARTESIAN_POINT ( 'NONE',  ( 7.861037107661897672, -54.33338873118993462, 10.10708465680652957 ) ) ;
#24440=CARTESIAN_POINT ( 'NONE',  ( -1.799502287743000029, -18.69283065396999888, -12.60413652832999887 ) ) ;
#24446=DIRECTION ( 'NONE',  ( 1.000000000000000000, 0.000000000000000000, 0.000000000000000000 ) ) ;
#24448=EDGE_CURVE ( 'NONE', #44346, #35538, #32941, .T. ) ;
#24456=CARTESIAN_POINT ( 'NONE',  ( 12.50000000000000000, -60.04999999657000131, 1.750000000000000000 ) ) ;
#24458=ORIENTED_EDGE ( 'NONE', *, *, #43359, .F. ) ;
#24460=CONICAL_SURFACE ( 'NONE', #37639, 3.425000000527000044, 0.7853981633972997312 ) ;
#24465=CARTESIAN_POINT ( 'NONE',  ( -0.4257295889298650660, -2.486564122683458944, 3.250694461378448974 ) ) ;
#24468=CARTESIAN_POINT ( 'NONE',  ( -12.65987830573000039, -24.93692962305999927, -0.9847759095506000149 ) ) ;
#24471=CARTESIAN_POINT ( 'NONE',  ( -7.648026768008000076, -55.55000001556999933, 10.12290050216000026 ) ) ;
#24476=CARTESIAN_POINT ( 'NONE',  ( 9.569482281372000188, -76.71319550101999596, -7.743360016082000641 ) ) ;
#24478=FACE_OUTER_BOUND ( 'NONE', #47491, .T. ) ;
#24479=CARTESIAN_POINT ( 'NONE',  ( 9.000511195990998914, -79.25610635638000190, 8.067084866081000172 ) ) ;
#24481=DIRECTION ( 'NONE',  ( 1.000000000000000000, 0.000000000000000000, 0.000000000000000000 ) ) ;
#24482=CARTESIAN_POINT ( 'NONE',  ( 1.430424515561402377, -2.762473447842865415, -2.917857303619362686 ) ) ;
#24483=CARTESIAN_POINT ( 'NONE',  ( 11.96897150190605075, -77.78965215004572542, -1.561179379743549367 ) ) ;
#24487=CARTESIAN_POINT ( 'NONE',  ( 7.220923959705269013, -77.97708333333335418, -9.396085398178609438 ) ) ;
#24488=DIRECTION ( 'NONE',  ( 0.000000000000000000, 0.000000000000000000, -1.000000000000000000 ) ) ;
#24489=TOROIDAL_SURFACE ( 'NONE', #8460, 1.250000000000000000, 0.5000000000000000000 ) ;
#24490=DIRECTION ( 'NONE',  ( 0.000000000000000000, 0.000000000000000000, -1.000000000000000000 ) ) ;
#24491=CARTESIAN_POINT ( 'NONE',  ( -1.257078809512000017, -2.978982885733000074, -3.494882541721000102 ) ) ;
#24495=CARTESIAN_POINT ( 'NONE',  ( -10.95378741321288274, -76.17043301730200255, 4.259322154369808544 ) ) ;
#24496=CARTESIAN_POINT ( 'NONE',  ( 10.14948852600000073, -22.75100835510000152, -7.674614791843000106 ) ) ;
#24498=CARTESIAN_POINT ( 'NONE',  ( -7.624341766647000362, -18.73514853758999976, 10.42531125024999916 ) ) ;
#24502=DIRECTION ( 'NONE',  ( 0.000000000000000000, 1.000000000000000000, 0.000000000000000000 ) ) ;
#24503=CARTESIAN_POINT ( 'NONE',  ( -12.50000000000000000, -18.75000000000000000, 0.000000000000000000 ) ) ;
#24504=PLANE ( 'NONE',  #53412 ) ;
#24506=CARTESIAN_POINT ( 'NONE',  ( 2.900236547156423761, -3.308449514079526033, -1.699047120294984392 ) ) ;
#24513=CARTESIAN_POINT ( 'NONE',  ( 6.378305113030960705, -77.28349241254731794, 10.18992046857810330 ) ) ;
#24517=AXIS2_PLACEMENT_3D ( 'NONE', #40966, #36235, #36527 ) ;
#24520=DIRECTION ( 'NONE',  ( 0.7071067811865475727, 0.000000000000000000, 0.7071067811865475727 ) ) ;
#24524=FACE_OUTER_BOUND ( 'NONE', #13027, .T. ) ;
#24526=ORIENTED_EDGE ( 'NONE', *, *, #34883, .T. ) ;
#24531=CARTESIAN_POINT ( 'NONE',  ( 9.213130513696000889, -16.99475660687000200, 8.533779407534000327 ) ) ;
#24535=CARTESIAN_POINT ( 'NONE',  ( -11.19913774713999999, -78.86173899011001254, -4.479602790820000457 ) ) ;
#24536=CARTESIAN_POINT ( 'NONE',  ( 13.95956770449999951, -33.08075762116000362, 5.182382778583999788E-05 ) ) ;
#24537=DIRECTION ( 'NONE',  ( 0.07798810297945017733, -0.04890180924492008863, -0.9957542211039027702 ) ) ;
#24540=ORIENTED_EDGE ( 'NONE', *, *, #47407, .T. ) ;
#24541=CARTESIAN_POINT ( 'NONE',  ( 7.639893379675799068, -55.41284423887101696, -10.11462454828658686 ) ) ;
#24546=EDGE_CURVE ( 'NONE', #48410, #51331, #39850, .T. ) ;
#24548=CARTESIAN_POINT ( 'NONE',  ( -9.723199429427999974, -17.52306056076000118, 7.958735708429999889 ) ) ;
#24553=CARTESIAN_POINT ( 'NONE',  ( 7.710095619827000313, -58.55064714318000085, 10.18496935397999970 ) ) ;
#24554=CARTESIAN_POINT ( 'NONE',  ( -12.76303204298000082, -60.06485150663000638, 1.980584515756000030 ) ) ;
#24555=CARTESIAN_POINT ( 'NONE',  ( 7.601397897754999633, -55.54999999966999980, 9.369164850722000892 ) ) ;
#24557=EDGE_LOOP ( 'NONE', ( #48568, #28079, #51055, #46402 ) ) ;
#24560=CARTESIAN_POINT ( 'NONE',  ( -7.601397897754999633, -55.54999999966999980, -9.369164850722000892 ) ) ;
#24564=CARTESIAN_POINT ( 'NONE',  ( 3.281580320494910996, -3.029571175170358011, 1.280763927392095436 ) ) ;
#24569=CARTESIAN_POINT ( 'NONE',  ( -7.648026766735999793, -23.25000000582000226, 10.12290050089000104 ) ) ;
#24574=ADVANCED_FACE ( 'NONE', ( #54034 ), #42108, .F. ) ;
#24575=CARTESIAN_POINT ( 'NONE',  ( 0.000000000000000000, 4.040000000000000036, 0.000000000000000000 ) ) ;
#24576=CARTESIAN_POINT ( 'NONE',  ( 0.006333666751048999850, -62.13262644267000212, -12.77652491961000081 ) ) ;
#24577=FACE_OUTER_BOUND ( 'NONE', #6085, .T. ) ;
#24581=CARTESIAN_POINT ( 'NONE',  ( 10.00844230537000001, -23.36891112553000127, -7.647097279392999880 ) ) ;
#24584=CARTESIAN_POINT ( 'NONE',  ( 6.199008894429987926, -78.52998459842886803, 9.981703030362384155 ) ) ;
#24586=ORIENTED_EDGE ( 'NONE', *, *, #12384, .T. ) ;
#24587=AXIS2_PLACEMENT_3D ( 'NONE', #24812, #20670, #42825 ) ;
#24588=DIRECTION ( 'NONE',  ( 0.000000000000000000, 0.000000000000000000, -1.000000000000000000 ) ) ;
#24590=CARTESIAN_POINT ( 'NONE',  ( 7.620012214408999895, -55.59439747889000216, -10.53562508622999871 ) ) ;
#24593=CARTESIAN_POINT ( 'NONE',  ( -3.126089899156312857, -79.19010414275966525, -11.62900749261814326 ) ) ;
#24594=LINE ( 'NONE', #10434, #23556 ) ;
#24603=ORIENTED_EDGE ( 'NONE', *, *, #656, .F. ) ;
#24605=AXIS2_PLACEMENT_3D ( 'NONE', #29580, #47637, #15730 ) ;
#24609=CARTESIAN_POINT ( 'NONE',  ( 1.484804496640999893, -17.28130846616999605, 12.77261165608999960 ) ) ;
#24612=CARTESIAN_POINT ( 'NONE',  ( -13.63885489310999510, -56.01421830980998351, -7.254376133916000668 ) ) ;
#24620=AXIS2_PLACEMENT_3D ( 'NONE', #44861, #12395, #30385 ) ;
#24623=CARTESIAN_POINT ( 'NONE',  ( -12.49837680052000088, -60.00957148770000060, -1.667051419334000029 ) ) ;
#24625=CARTESIAN_POINT ( 'NONE',  ( 7.730443418333229566, -60.92191635792816129, 10.25197760567252558 ) ) ;
#24627=CARTESIAN_POINT ( 'NONE',  ( 0.000000000000000000, -0.5000000000000000000, 0.000000000000000000 ) ) ;
#24630=CARTESIAN_POINT ( 'NONE',  ( -9.630374193854642328, -76.65109570096610980, 6.732137028299512771 ) ) ;
#24632=CARTESIAN_POINT ( 'NONE',  ( -10.52682159589000044, -55.37432398227000618, 7.605688676848999741 ) ) ;
#24635=DIRECTION ( 'NONE',  ( 0.000000000000000000, -1.000000000000000000, -9.403026372076000847E-14 ) ) ;
#24636=CARTESIAN_POINT ( 'NONE',  ( -11.00000000000000000, -18.25000000000000000, 0.000000000000000000 ) ) ;
#24641=CARTESIAN_POINT ( 'NONE',  ( -3.099241092295174305, -1.710269946423099929, 1.691961027787603378 ) ) ;
#24642=ORIENTED_EDGE ( 'NONE', *, *, #17350, .F. ) ;
#24643=CARTESIAN_POINT ( 'NONE',  ( -1.894625102906858594, -3.499999999999999556, -2.799120236218770597 ) ) ;
#24647=B_SPLINE_CURVE_WITH_KNOTS ( 'NONE', 3,
 ( #35626, #53655, #13195, #19398, #41245, #45695, #15254, #32951, #36808, #32656, #19688, #834, #42129, #1407, #5515, #32081, #10247, #18816 ),
 .UNSPECIFIED., .F., .F.,
 ( 4, 2, 2, 2, 2, 2, 2, 2, 4 ),
 ( 0.000000000000000000, 0.06250000000000079103, 0.1250000000000015821, 0.2500000000000031086, 0.5000000000000023315, 0.7500000000000016653, 0.8125000000000025535, 0.8750000000000034417, 1.000000000000000000 ),
 .UNSPECIFIED. ) ;
#24650=CARTESIAN_POINT ( 'NONE',  ( -3.346450045594000056, -76.84369696823999618, 12.57540552286999791 ) ) ;
#24654=B_SPLINE_CURVE_WITH_KNOTS ( 'NONE', 3,
 ( #28051, #365, #27761, #45804, #23346, #18345, #1511, #5339, #18922, #32471, #31600, #50517, #9189, #27174, #36335, #54360 ),
 .UNSPECIFIED., .F., .F.,
 ( 4, 2, 2, 2, 2, 2, 2, 4 ),
 ( 0.000000000000000000, 0.2499999999999954481, 0.3749999999999962252, 0.4374999999999965583, 0.4999999999999970024, 0.6249999999999976685, 0.7499999999999985567, 1.000000000000000000 ),
 .UNSPECIFIED. ) ;
#24657=ADVANCED_FACE ( 'NONE', ( #4434 ), #30738, .F. ) ;
#24660=CIRCLE ( 'NONE', #35976, 1.750000000000001332 ) ;
#24664=DIRECTION ( 'NONE',  ( -0.7592504788685899841, -0.04890177849874939586, -0.6489586476790920599 ) ) ;
#24672=FACE_OUTER_BOUND ( 'NONE', #10384, .T. ) ;
#24673=DIRECTION ( 'NONE',  ( 0.000000000000000000, 1.000000000000000000, 0.000000000000000000 ) ) ;
#24676=ORIENTED_EDGE ( 'NONE', *, *, #8769, .F. ) ;
#24683=CARTESIAN_POINT ( 'NONE',  ( -10.42531125072000009, -55.53514854654000032, -7.624341767124000135 ) ) ;
#24685=COLOUR_RGB ( '', 0.66274510, 0.83137255, 0.94901961) ;
#24687=ORIENTED_EDGE ( 'NONE', *, *, #53630, .F. ) ;
#24691=EDGE_CURVE ( 'NONE', #23377, #35060, #49166, .T. ) ;
#24692=CARTESIAN_POINT ( 'NONE',  ( -1.777724524818122598, -78.83678780677392695, 12.13456374090698553 ) ) ;
#24695=DIRECTION ( 'NONE',  ( -1.000000000000000000, 0.000000000000000000, 0.000000000000000000 ) ) ;
#24700=CARTESIAN_POINT ( 'NONE',  ( 2.303363178838841119, -76.55889284051112043, 11.52175839890178288 ) ) ;
#24706=VECTOR ( 'NONE', #47494, 1000.000000000000000 ) ;
#24709=CARTESIAN_POINT ( 'NONE',  ( -12.00000000000000000, -55.54999999966999980, -1.750000000000000000 ) ) ;
#24713=DIRECTION ( 'NONE',  ( 0.000000000000000000, 0.000000000000000000, -1.000000000000000000 ) ) ;
#24714=DIRECTION ( 'NONE',  ( 1.000000000000000000, 0.000000000000000000, 1.147010004337999914E-14 ) ) ;
#24718=CARTESIAN_POINT ( 'NONE',  ( 12.77301895549999955, -25.05186686373999905, 1.052127376137000025 ) ) ;
#24721=CARTESIAN_POINT ( 'NONE',  ( -1.930860503526836469, -23.77417505915145668, -12.72930866331899225 ) ) ;
#24723=VERTEX_POINT ( 'NONE', #32155 ) ;
#24725=CARTESIAN_POINT ( 'NONE',  ( -10.40000000000000036, 0.000000000000000000, 0.000000000000000000 ) ) ;
#24729=CARTESIAN_POINT ( 'NONE',  ( 12.83838672487999943, -55.59401611997999737, -2.062170725306000207 ) ) ;
#24731=DIRECTION ( 'NONE',  ( 1.000000000000000000, 0.000000000000000000, 0.000000000000000000 ) ) ;
#24732=CARTESIAN_POINT ( 'NONE',  ( -12.00000000000000000, -18.84999999999999787, 0.000000000000000000 ) ) ;
#24735=CARTESIAN_POINT ( 'NONE',  ( -7.601397897754999633, -18.75000000310999937, 10.07627163191000008 ) ) ;
#24737=ORIENTED_EDGE ( 'NONE', *, *, #52565, .T. ) ;
#24739=CARTESIAN_POINT ( 'NONE',  ( 12.87022657274000004, -59.58485473249000108, 2.062597299672999540 ) ) ;
#24744=AXIS2_PLACEMENT_3D ( 'NONE', #46136, #36665, #41682 ) ;
#24745=VERTEX_POINT ( 'NONE', #13871 ) ;
#24746=ORIENTED_EDGE ( 'NONE', *, *, #25046, .T. ) ;
#24749=EDGE_CURVE ( 'NONE', #39417, #38447, #42794, .T. ) ;
#24757=CARTESIAN_POINT ( 'NONE',  ( 9.102117850491421081, -24.97186524165807242, 8.583692176894766490 ) ) ;
#24759=CARTESIAN_POINT ( 'NONE',  ( 9.073547343531414455, -16.77191135192954619, -8.894853367293087842 ) ) ;
#24764=VECTOR ( 'NONE', #48383, 999.9999999999998863 ) ;
#24766=CARTESIAN_POINT ( 'NONE',  ( 11.79999999999999893, -23.15000000000999947, 0.5999999999999999778 ) ) ;
#24768=CARTESIAN_POINT ( 'NONE',  ( -7.948089776770999926, -24.44033979720000360, 9.636757666087000018 ) ) ;
#24770=CARTESIAN_POINT ( 'NONE',  ( 8.798028344890999719, -61.73813495650999528, -8.790623041469000754 ) ) ;
#24771=CARTESIAN_POINT ( 'NONE',  ( -12.02296678431999943, -78.43220577152999340, 2.418109797047000242 ) ) ;
#24774=CARTESIAN_POINT ( 'NONE',  ( -11.64898813392143317, -77.57617276172848619, -3.925102516053998070 ) ) ;
#24780=CARTESIAN_POINT ( 'NONE',  ( 1.798944584243999945, -23.21533228280000216, 12.61116915999999932 ) ) ;
#24781=CARTESIAN_POINT ( 'NONE',  ( -14.00000000000000000, -6.100000000000000533, 0.000000000000000000 ) ) ;
#24782=CARTESIAN_POINT ( 'NONE',  ( -3.669758066562000209, -2.393766836959000166, -0.5721248644209000478 ) ) ;
#24785=CARTESIAN_POINT ( 'NONE',  ( -8.887117850294183441, -76.14310715044948097, 7.686514976405625532 ) ) ;
#24786=DIRECTION ( 'NONE',  ( 0.000000000000000000, 1.000000000000000000, 0.000000000000000000 ) ) ;
#24788=DIRECTION ( 'NONE',  ( 0.7071067811865475727, 0.000000000000000000, -0.7071067811865475727 ) ) ;
#24790=CARTESIAN_POINT ( 'NONE',  ( 8.815588752397863104, -76.73947780777287164, -8.371812616114789662 ) ) ;
#24792=DIRECTION ( 'NONE',  ( -1.000000000000000000, 0.000000000000000000, 0.000000000000000000 ) ) ;
#24793=CARTESIAN_POINT ( 'NONE',  ( -8.909545442949999838, -57.79999999967000690, -7.919595949288999570 ) ) ;
#24798=CARTESIAN_POINT ( 'NONE',  ( -12.70255494770078109, -54.05391159001328560, -1.306413223709476323 ) ) ;
#24801=AXIS2_PLACEMENT_3D ( 'NONE', #11941, #51815, #47393 ) ;
#24803=CARTESIAN_POINT ( 'NONE',  ( 12.50000000000000000, -23.24999999688999708, 1.750000000000000000 ) ) ;
#24810=CARTESIAN_POINT ( 'NONE',  ( 1.667916687331000070, -55.50151115525000023, -12.49168451095999899 ) ) ;
#24812=CARTESIAN_POINT ( 'NONE',  ( -8.485281374238999419, 0.000000000000000000, -8.485281374238999419 ) ) ;
#24813=DIRECTION ( 'NONE',  ( 0.7071067811865974218, 0.7071067811864975017, 8.595327382698963620E-09 ) ) ;
#24815=ORIENTED_EDGE ( 'NONE', *, *, #23694, .F. ) ;
#24816=ORIENTED_EDGE ( 'NONE', *, *, #56755, .T. ) ;
#24819=AXIS2_PLACEMENT_3D ( 'NONE', #10630, #10334, #32742 ) ;
#24820=EDGE_LOOP ( 'NONE', ( #11939, #28841, #28946, #25474 ) ) ;
#24821=CARTESIAN_POINT ( 'NONE',  ( 7.645398650971000798, -18.78468617155999709, 10.18948982068999953 ) ) ;
#24822=CARTESIAN_POINT ( 'NONE',  ( -7.220923959705244144, -75.87291666666665435, -9.396085398178621872 ) ) ;
#24823=CARTESIAN_POINT ( 'NONE',  ( 5.486311112560000147, -78.09489713918000575, 11.38883617360999878 ) ) ;
#24825=CARTESIAN_POINT ( 'NONE',  ( 0.000000000000000000, 4.040000000000000036, 0.000000000000000000 ) ) ;
#24827=DIRECTION ( 'NONE',  ( -0.9957542217959268749, -0.04890179607413128876, -0.07798810240230209800 ) ) ;
#24830=CARTESIAN_POINT ( 'NONE',  ( -0.9088587313318036154, -78.18115558532333864, 11.75905384473932713 ) ) ;
#24831=ORIENTED_EDGE ( 'NONE', *, *, #10266, .T. ) ;
#24833=CARTESIAN_POINT ( 'NONE',  ( 14.00000000000000000, -69.50420297070000686, 0.000000000000000000 ) ) ;
#24836=UNCERTAINTY_MEASURE_WITH_UNIT (LENGTH_MEASURE( 1.000000000000000082E-05 ), #24962, 'distance_accuracy_value', 'NONE');
#24838=AXIS2_PLACEMENT_3D ( 'NONE', #36828, #1712, #19123 ) ;
#24840=DIRECTION ( 'NONE',  ( 0.7071067811865474617, 0.000000000000000000, 0.7071067811865474617 ) ) ;
#24845=EDGE_CURVE ( 'NONE', #12605, #19229, #41436, .T. ) ;
#24846=CARTESIAN_POINT ( 'NONE',  ( -7.674614791501999989, -59.55100836074000625, -10.14948852566000070 ) ) ;
#24848=VERTEX_POINT ( 'NONE', #56077 ) ;
#24853=CARTESIAN_POINT ( 'NONE',  ( -7.969034948596000589, -17.37623147815000024, 9.934750886910000744 ) ) ;
#24855=FACE_OUTER_BOUND ( 'NONE', #41631, .T. ) ;
#24858=CARTESIAN_POINT ( 'NONE',  ( 1.886823409076999969, -55.03680315604999151, -12.68610076202999792 ) ) ;
#24860=DIRECTION ( 'NONE',  ( 0.7071067811865474617, 0.000000000000000000, -0.7071067811865474617 ) ) ;
#24864=CARTESIAN_POINT ( 'NONE',  ( 10.98754182310580063, -18.54785535412668551, -0.5242772304895085833 ) ) ;
#24865=CARTESIAN_POINT ( 'NONE',  ( 1.389926494650000066, -61.42381336221999533, -12.65988803926999928 ) ) ;
#24869=DIRECTION ( 'NONE',  ( 0.000000000000000000, 0.000000000000000000, -1.000000000000000000 ) ) ;
#24872=CARTESIAN_POINT ( 'NONE',  ( -9.850507816072157752, -61.10508874482341213, 7.836744050180310950 ) ) ;
#24873=PLANE ( 'NONE',  #31151 ) ;
#24875=ORIENTED_EDGE ( 'NONE', *, *, #13028, .T. ) ;
#24877=CARTESIAN_POINT ( 'NONE',  ( -8.800000000000000711, 0.000000000000000000, 0.000000000000000000 ) ) ;
#24878=CIRCLE ( 'NONE', #57851, 13.89999999999999858 ) ;
#24880=DIRECTION ( 'NONE',  ( 1.000000000000000000, 0.000000000000000000, 0.000000000000000000 ) ) ;
#24885=AXIS2_PLACEMENT_3D ( 'NONE', #42429, #52157, #6695 ) ;
#24888=CARTESIAN_POINT ( 'NONE',  ( 1.667916687331000070, -23.29848884437999956, 12.49168451098999988 ) ) ;
#24890=CARTESIAN_POINT ( 'NONE',  ( -12.83836862999999973, -23.20626272212999908, 2.062146390630000159 ) ) ;
#24893=DIRECTION ( 'NONE',  ( 0.7592504785508701337, 0.04890181650104810651, 0.6489586451871740547 ) ) ;
#24895=ORIENTED_EDGE ( 'NONE', *, *, #11308, .F. ) ;
#24901=EDGE_CURVE ( 'NONE', #26739, #52133, #46891, .T. ) ;
#24903=AXIS2_PLACEMENT_3D ( 'NONE', #12554, #38551, #25551 ) ;
#24904=ORIENTED_EDGE ( 'NONE', *, *, #41779, .T. ) ;
#24905=VERTEX_POINT ( 'NONE', #38054 ) ;
#24910=CARTESIAN_POINT ( 'NONE',  ( -12.77301895554999867, -61.85186686341000240, -1.052127376138000114 ) ) ;
#24913=CARTESIAN_POINT ( 'NONE',  ( -10.35747158362999976, -18.68415522710999710, 7.626500902215000544 ) ) ;
#24919=CARTESIAN_POINT ( 'NONE',  ( -10.31444587876999996, -54.49924218061999426, 7.758886158083000417 ) ) ;
#24922=CARTESIAN_POINT ( 'NONE',  ( 1.931043742978000077, -19.22204592323999961, -12.75763395699000036 ) ) ;
#24923=DIRECTION ( 'NONE',  ( -1.000000000000000000, 0.000000000000000000, 0.000000000000000000 ) ) ;
#24925=CARTESIAN_POINT ( 'NONE',  ( -3.255604724290822816, -1.122525214333685240, -0.8495354805320418645 ) ) ;
#24927=CARTESIAN_POINT ( 'NONE',  ( 12.00000000000000000, -60.04999999966999980, 0.000000000000000000 ) ) ;
#24928=ORIENTED_EDGE ( 'NONE', *, *, #41163, .T. ) ;
#24930=DIRECTION ( 'NONE',  ( -1.000000000000000000, 0.000000000000000000, 0.000000000000000000 ) ) ;
#24934=CARTESIAN_POINT ( 'NONE',  ( -12.83677071375000089, -55.57261389723999656, 2.062839858856999609 ) ) ;
#24936=CARTESIAN_POINT ( 'NONE',  ( 1.460729357734999789, -60.89091243169999501, 12.44211643244000065 ) ) ;
#24937=CARTESIAN_POINT ( 'NONE',  ( -2.598917237794085455, -3.052083333333332593, -1.997276839918474600 ) ) ;
#24947=DIRECTION ( 'NONE',  ( 0.000000000000000000, -1.000000000000000000, 0.000000000000000000 ) ) ;
#24948=CARTESIAN_POINT ( 'NONE',  ( -1.359416874709192810E-05, -0.8285695117701413759, -3.421591653122290300 ) ) ;
#24951=DIRECTION ( 'NONE',  ( 0.000000000000000000, -1.000000000000000000, 0.000000000000000000 ) ) ;
#24954=AXIS2_PLACEMENT_3D ( 'NONE', #58277, #30808, #22844 ) ;
#24956=CARTESIAN_POINT ( 'NONE',  ( 0.000000000000000000, -2.660000000000000142, 0.000000000000000000 ) ) ;
#24957=ORIENTED_EDGE ( 'NONE', *, *, #24005, .T. ) ;
#24958=CARTESIAN_POINT ( 'NONE',  ( -1.980584515752000119, -23.26485146623999967, 12.76303204602000108 ) ) ;
#24959=ORIENTED_EDGE ( 'NONE', *, *, #41832, .T. ) ;
#24960=ORIENTED_EDGE ( 'NONE', *, *, #48454, .F. ) ;
#24961=FACE_BOUND ( 'NONE', #24381, .T. ) ;
#24962=( LENGTH_UNIT ( ) NAMED_UNIT ( * ) SI_UNIT ( .MILLI., .METRE. ) );
#24963=CARTESIAN_POINT ( 'NONE',  ( 5.917523019358082337, -77.46666666666666856, -10.26699006316252394 ) ) ;
#24968=CARTESIAN_POINT ( 'NONE',  ( 13.90000000000005720, -72.79999999999999716, 0.000000000000000000 ) ) ;
#24969=ADVANCED_FACE ( 'NONE', ( #7056 ), #55785, .F. ) ;
#24970=VERTEX_POINT ( 'NONE', #2638 ) ;
#24979=CIRCLE ( 'NONE', #12743, 13.86363636363999952 ) ;
#24984=AXIS2_PLACEMENT_3D ( 'NONE', #5577, #51062, #28005 ) ;
#24985=DIRECTION ( 'NONE',  ( 0.9999999999995751176, 0.000000000000000000, 9.217554799814770620E-07 ) ) ;
#24986=CARTESIAN_POINT ( 'NONE',  ( 0.2494208061600084736, -61.79288960742137249, -12.50614183116600842 ) ) ;
#24990=DIRECTION ( 'NONE',  ( 1.000000000000000000, 0.000000000000000000, 0.000000000000000000 ) ) ;
#24991=CARTESIAN_POINT ( 'NONE',  ( -13.63885489310999510, -56.01421830980998351, 7.254376133916000668 ) ) ;
#24994=CARTESIAN_POINT ( 'NONE',  ( 10.42272502865000128, -20.24546192895000019, 7.691893942754999713 ) ) ;
#24995=CARTESIAN_POINT ( 'NONE',  ( -9.516272955320999927, -61.62538765589000178, -8.227498559458000571 ) ) ;
#24996=CIRCLE ( 'NONE', #31588, 0.5000000000000004441 ) ;
#24999=CARTESIAN_POINT ( 'NONE',  ( 12.54238271613678890, -55.27146427614202651, 1.749799002657778324 ) ) ;
#25000=CARTESIAN_POINT ( 'NONE',  ( 11.88928085110999966, -78.33531299227999511, 5.289737169833999886 ) ) ;
#25002=CARTESIAN_POINT ( 'NONE',  ( 10.26636020442522934, -78.40548738728304556, -5.914272961825407293 ) ) ;
#25004=CARTESIAN_POINT ( 'NONE',  ( 1.413608202523000124, -75.94734000069999524, 12.28110795171000014 ) ) ;
#25005=ORIENTED_EDGE ( 'NONE', *, *, #55153, .T. ) ;
#25008=CARTESIAN_POINT ( 'NONE',  ( 12.54901606610000009, -61.80731603467000213, 0.4733145588202999909 ) ) ;
#25009=CARTESIAN_POINT ( 'NONE',  ( -12.34629048376999982, -79.26738212572000464, -1.838093833240000086 ) ) ;
#25010=CARTESIAN_POINT ( 'NONE',  ( -7.601397897754999633, -55.55000000278000272, 10.07627163191000008 ) ) ;
#25015=VERTEX_POINT ( 'NONE', #20345 ) ;
#25016=EDGE_CURVE ( 'NONE', #46987, #29817, #58142, .T. ) ;
#25025=ORIENTED_EDGE ( 'NONE', *, *, #52887, .T. ) ;
#25030=ORIENTED_EDGE ( 'NONE', *, *, #56903, .F. ) ;
#25034=ORIENTED_EDGE ( 'NONE', *, *, #19630, .T. ) ;
#25035=CARTESIAN_POINT ( 'NONE',  ( -12.74366183107908945, -23.52185227221844954, -1.980611001122017045 ) ) ;
#25040=CARTESIAN_POINT ( 'NONE',  ( 7.660431561264000599, -55.60820826791000115, 10.01749754193999919 ) ) ;
#25041=DIRECTION ( 'NONE',  ( 0.000000000000000000, -1.000000000000000000, 0.000000000000000000 ) ) ;
#25043=CARTESIAN_POINT ( 'NONE',  ( -11.75165102744716705, -77.20451201809390795, -0.7683522248362885110 ) ) ;
#25046=EDGE_CURVE ( 'NONE', #26170, #7381, #16757, .T. ) ;
#25048=CARTESIAN_POINT ( 'NONE',  ( -7.620037246293000166, -23.20567269824999812, 10.53559750859000133 ) ) ;
#25049=EDGE_CURVE ( 'NONE', #47646, #58285, #21401, .T. ) ;
#25050=CARTESIAN_POINT ( 'NONE',  ( 12.50000000000000000, -18.75000000310999937, -1.750000000000000000 ) ) ;
#25052=CARTESIAN_POINT ( 'NONE',  ( 9.996770077891000028, -60.95065455317000414, -7.758602204140999881 ) ) ;
#25053=CARTESIAN_POINT ( 'NONE',  ( 9.000511195990998914, -79.29077302305000785, 8.067084866081000172 ) ) ;
#25055=CARTESIAN_POINT ( 'NONE',  ( 0.000000000000000000, 4.040000000000000036, 0.000000000000000000 ) ) ;
#25056=CARTESIAN_POINT ( 'NONE',  ( 12.00000000000000000, -60.04999999966999980, -1.750000000000000000 ) ) ;
#25059=ORIENTED_EDGE ( 'NONE', *, *, #8416, .F. ) ;
#25062=CARTESIAN_POINT ( 'NONE',  ( -0.7999999999999001243, -18.84999999997999964, -12.00000000000000000 ) ) ;
#25063=DIRECTION ( 'NONE',  ( -1.000000000000000000, 0.000000000000000000, 0.000000000000000000 ) ) ;
#25064=CARTESIAN_POINT ( 'NONE',  ( -0.4333679777835000024, -2.853257899543000242, 3.531240579163999804 ) ) ;
#25065=AXIS2_PLACEMENT_3D ( 'NONE', #45561, #23105, #54115 ) ;
#25069=CARTESIAN_POINT ( 'NONE',  ( -9.354514546012950404, -76.14787076493711027, 7.112430735605655308 ) ) ;
#25073=AXIS2_PLACEMENT_3D ( 'NONE', #31236, #30370, #26241 ) ;
#25075=CARTESIAN_POINT ( 'NONE',  ( 5.894077591580000330, -76.71473343234410436, -10.80721126920999708 ) ) ;
#25078=CARTESIAN_POINT ( 'NONE',  ( -8.798028344891999808, -61.73813495650999528, 8.790623041469000754 ) ) ;
#25081=DIRECTION ( 'NONE',  ( -0.07798810297947010584, -0.04890180924492011638, 0.9957542211039013269 ) ) ;
#25082=CARTESIAN_POINT ( 'NONE',  ( -12.72924182828835349, -55.02450359958543658, -1.930521792058781383 ) ) ;
#25083=VERTEX_POINT ( 'NONE', #44809 ) ;
#25084=CYLINDRICAL_SURFACE ( 'NONE', #354, 0.5000000000000006661 ) ;
#25085=DIRECTION ( 'NONE',  ( -0.7071067811865475727, 0.000000000000000000, 0.7071067811865475727 ) ) ;
#25090=CARTESIAN_POINT ( 'NONE',  ( 0.9356112496015772662, -54.05892169590293861, -12.50329130245239639 ) ) ;
#25091=CARTESIAN_POINT ( 'NONE',  ( 1.930989144707000005, -57.04634220890999785, -12.80900240956999880 ) ) ;
#25093=CARTESIAN_POINT ( 'NONE',  ( 1.247385801071000166, -17.52277743742000027, -12.50301438876999960 ) ) ;
#25096=CYLINDRICAL_SURFACE ( 'NONE', #49789, 11.75000000000000000 ) ;
#25097=ORIENTED_EDGE ( 'NONE', *, *, #30291, .F. ) ;
#25103=CARTESIAN_POINT ( 'NONE',  ( 9.395773752832997872, -17.29509747843999889, 8.188237371225000061 ) ) ;
#25105=CARTESIAN_POINT ( 'NONE',  ( 1.318114156667296921, -54.06427522772043659, 12.70261578158577187 ) ) ;
#25107=CARTESIAN_POINT ( 'NONE',  ( -9.134707332315000983, -77.73029308464001019, -8.964724163292999037 ) ) ;
#25108=CONICAL_SURFACE ( 'NONE', #34526, 13.94999999997000018, 0.7853981633972997312 ) ;
#25110=DIRECTION ( 'NONE',  ( 0.000000000000000000, -1.000000000000000000, 0.000000000000000000 ) ) ;
#25111=DIRECTION ( 'NONE',  ( 0.000000000000000000, -1.000000000000000000, 0.000000000000000000 ) ) ;
#25114=VERTEX_POINT ( 'NONE', #17946 ) ;
#25115=CARTESIAN_POINT ( 'NONE',  ( 7.678655902623765073, -55.00623020231258664, -10.03844298032646165 ) ) ;
#25119=CARTESIAN_POINT ( 'NONE',  ( 0.000000000000000000, -4.000000000000000000, 0.000000000000000000 ) ) ;
#25125=DIRECTION ( 'NONE',  ( -0.9999476293090542312, 0.000000000000000000, -0.01023418971888952027 ) ) ;
#25128=CARTESIAN_POINT ( 'NONE',  ( -7.674627477108999507, -56.04922971914000129, -10.14950121126000049 ) ) ;
#25130=ORIENTED_EDGE ( 'NONE', *, *, #47250, .T. ) ;
#25135=CARTESIAN_POINT ( 'NONE',  ( -5.747123378374999980, -78.61567021304000491, 10.24856442990000005 ) ) ;
#25137=CARTESIAN_POINT ( 'NONE',  ( 0.000000000000000000, -60.04999999966999980, -12.50000000000000000 ) ) ;
#25143=LINE ( 'NONE', #33991, #30907 ) ;
#25148=CARTESIAN_POINT ( 'NONE',  ( 1.295048492659000017, -61.32893519093000378, -12.54716442239999985 ) ) ;
#25156=CARTESIAN_POINT ( 'NONE',  ( -8.894916816534069071, -62.02809132899626121, 9.073484344827472015 ) ) ;
#25158=CIRCLE ( 'NONE', #38333, 0.8000000000000011546 ) ;
#25159=DIRECTION ( 'NONE',  ( -0.4045602622699926987, 0.8201597334568855313, 0.4045602622699926987 ) ) ;
#25160=CARTESIAN_POINT ( 'NONE',  ( -1.378523866479640203, -75.79999999999999716, -11.70433083598206458 ) ) ;
#25162=EDGE_CURVE ( 'NONE', #31399, #53636, #53418, .T. ) ;
#25165=CARTESIAN_POINT ( 'NONE',  ( 9.369164850722000892, -55.54999999966999980, 7.601397897754999633 ) ) ;
#25166=CARTESIAN_POINT ( 'NONE',  ( -9.396085398178650294, -77.74791666666668277, 7.220923959705211281 ) ) ;
#25170=CARTESIAN_POINT ( 'NONE',  ( -17.50000000000000000, -26.93717104351999936, -4.519587204488000183E-10 ) ) ;
#25172=CARTESIAN_POINT ( 'NONE',  ( 2.062673488410000200, -23.32452273707999879, 12.82904109062999964 ) ) ;
#25173=CARTESIAN_POINT ( 'NONE',  ( 0.000000000000000000, -0.2000000000000000111, 0.000000000000000000 ) ) ;
#25176=CARTESIAN_POINT ( 'NONE',  ( -12.65989785476000051, -53.85665906507999523, -0.9744897697748000631 ) ) ;
#25178=VERTEX_POINT ( 'NONE', #43937 ) ;
#25188=ORIENTED_EDGE ( 'NONE', *, *, #54032, .F. ) ;
#25190=CARTESIAN_POINT ( 'NONE',  ( -12.70253258974437571, -24.97063167674132345, 0.9890392130068401677 ) ) ;
#25191=EDGE_CURVE ( 'NONE', #1897, #11731, #8489, .T. ) ;
#25192=AXIS2_PLACEMENT_3D ( 'NONE', #51869, #29690, #24985 ) ;
#25193=LINE ( 'NONE', #7481, #55003 ) ;
#25200=CARTESIAN_POINT ( 'NONE',  ( -1.250000000000000000, -60.04999999966999980, 12.00000000000000000 ) ) ;
#25202=CIRCLE ( 'NONE', #49757, 14.00000000000000000 ) ;
#25205=CARTESIAN_POINT ( 'NONE',  ( 1.034214221880000141E-14, 0.2999999999999999334, 0.000000000000000000 ) ) ;
#25206=CARTESIAN_POINT ( 'NONE',  ( 3.343750000583999960, -0.9062499994161000716, -3.925818329445000231E-08 ) ) ;
#25208=CARTESIAN_POINT ( 'NONE',  ( 1.666698456700999920, -18.80818260160000222, -12.50018138921000066 ) ) ;
#25211=CARTESIAN_POINT ( 'NONE',  ( 1.250000000000000000, -18.75000000000000000, 12.00000000000000000 ) ) ;
#25212=CYLINDRICAL_SURFACE ( 'NONE', #9062, 1.750000000000000000 ) ;
#25213=ORIENTED_EDGE ( 'NONE', *, *, #20420, .T. ) ;
#25214=DIRECTION ( 'NONE',  ( 0.000000000000000000, 1.000000000000000000, 0.000000000000000000 ) ) ;
#25215=CARTESIAN_POINT ( 'NONE',  ( -12.89999999994999769, -2.999999999951000085, -1.886268936261000296E-09 ) ) ;
#25216=CARTESIAN_POINT ( 'NONE',  ( -12.50386483992572195, -24.78505343634594382, 0.8574420492267335048 ) ) ;
#25218=CARTESIAN_POINT ( 'NONE',  ( -1.985556276454000235, -2.710628508794999725, -3.057679240689000100 ) ) ;
#25221=B_SPLINE_CURVE_WITH_KNOTS ( 'NONE', 3,
 ( #39309, #30440, #48470, #57599, #35146, #53178, #17749, #41060, #4753, #13893 ),
 .UNSPECIFIED., .F., .F.,
 ( 4, 2, 2, 2, 4 ),
 ( 0.000000000000000000, 0.2500000000000000000, 0.5000000000000000000, 0.7500000000000000000, 1.000000000000000000 ),
 .UNSPECIFIED. ) ;
#25222=CARTESIAN_POINT ( 'NONE',  ( -12.82229880955999946, -55.37735182805000278, 2.065917129154000165 ) ) ;
#25225=DIRECTION ( 'NONE',  ( -0.7071067811865475727, 0.000000000000000000, 0.7071067811865475727 ) ) ;
#25226=DIRECTION ( 'NONE',  ( -2.273759822993975071E-11, -5.531791025963690614E-21, 1.000000000000000000 ) ) ;
#25230=EDGE_CURVE ( 'NONE', #26696, #1538, #36818, .T. ) ;
#25231=CARTESIAN_POINT ( 'NONE',  ( 9.936789827135878994, -76.40459641371209898, -6.277323833409170106 ) ) ;
#25244=EDGE_CURVE ( 'NONE', #13888, #47937, #1926, .T. ) ;
#25246=CIRCLE ( 'NONE', #47852, 12.90000000000000036 ) ;
#25247=ORIENTED_EDGE ( 'NONE', *, *, #7725, .T. ) ;
#25248=CARTESIAN_POINT ( 'NONE',  ( 0.9935076047277175970, -24.96816187751455018, 12.70250268217055201 ) ) ;
#25250=ORIENTED_EDGE ( 'NONE', *, *, #12994, .F. ) ;
#25251=CARTESIAN_POINT ( 'NONE',  ( -2.839805762151343949, -1.458333333333332815, 1.636761686205411737 ) ) ;
#25257=LINE ( 'NONE', #51851, #3527 ) ;
#25260=CARTESIAN_POINT ( 'NONE',  ( -1.750000000001000089, -60.05000000958000328, -12.56594317859000043 ) ) ;
#25263=EDGE_CURVE ( 'NONE', #47780, #11901, #27950, .T. ) ;
#25265=DIRECTION ( 'NONE',  ( -0.7071067811865474617, 0.000000000000000000, -0.7071067811865474617 ) ) ;
#25273=DIRECTION ( 'NONE',  ( 0.7071067811865475727, 0.000000000000000000, 0.7071067811865475727 ) ) ;
#25274=CARTESIAN_POINT ( 'NONE',  ( -0.01376364114532320840, -2.975804675509202912, 3.249696318060919076 ) ) ;
#25278=CARTESIAN_POINT ( 'NONE',  ( -13.97864847978000036, -33.03331574007000881, -0.0001086647257827000004 ) ) ;
#25279=CARTESIAN_POINT ( 'NONE',  ( -12.99510751537000353, -52.49705297113997204, 6.911973076623003642 ) ) ;
#25281=CARTESIAN_POINT ( 'NONE',  ( -9.337502430872199000, -76.25149124130676626, -7.139128148582318367 ) ) ;
#25282=CARTESIAN_POINT ( 'NONE',  ( 10.01332844637000008, -18.71943307332999851, 7.654537085030999499 ) ) ;
#25283=CARTESIAN_POINT ( 'NONE',  ( -7.660411271065999728, -59.99173735459000056, -10.01752031416000044 ) ) ;
#25285=CARTESIAN_POINT ( 'NONE',  ( 10.35747158364999976, -60.11584477251999203, 7.626500902235000545 ) ) ;
#25287=CARTESIAN_POINT ( 'NONE',  ( 9.175280770439000477, -76.70951328470999897, -8.221808909867000636 ) ) ;
#25288=CARTESIAN_POINT ( 'NONE',  ( 9.931052045582879018, -24.12278631287863462, 7.764003813945582699 ) ) ;
#25291=CARTESIAN_POINT ( 'NONE',  ( -9.104818479629999572, -76.61049510581999300, 8.138539985441999747 ) ) ;
#25293=EDGE_CURVE ( 'NONE', #16042, #37958, #23824, .T. ) ;
#25295=B_SPLINE_CURVE_WITH_KNOTS ( 'NONE', 3,
 ( #15802, #6062, #42385, #23487, #10506, #10211, #37650, #24072, #51542, #42672, #1956, #19949, #2240, #15511, #28190, #1085, #11387, #55664 ),
 .UNSPECIFIED., .F., .F.,
 ( 4, 2, 2, 2, 2, 2, 2, 2, 4 ),
 ( 0.000000000000000000, 0.1250000000000001665, 0.2500000000000002776, 0.3750000000000002776, 0.5000000000000002220, 0.6250000000000001110, 0.7500000000000001110, 0.8750000000000000000, 1.000000000000000000 ),
 .UNSPECIFIED. ) ;
#25296=EDGE_CURVE ( 'NONE', #7601, #52710, #16694, .T. ) ;
#25297=CARTESIAN_POINT ( 'NONE',  ( -10.98364301412004984, -18.76988149294739472, -0.5996551156055939247 ) ) ;
#25298=CARTESIAN_POINT ( 'NONE',  ( 7.601397897754999633, -23.24999999758999536, -10.07627163191000008 ) ) ;
#25299=CARTESIAN_POINT ( 'NONE',  ( -1.931087888240000217, -18.68415268018999953, -12.71658872085999903 ) ) ;
#25307=ORIENTED_EDGE ( 'NONE', *, *, #56554, .T. ) ;
#25309=CARTESIAN_POINT ( 'NONE',  ( -10.48774103545000003, -57.04527981721000174, 7.686941364801000098 ) ) ;
#25312=ORIENTED_EDGE ( 'NONE', *, *, #20652, .F. ) ;
#25315=ORIENTED_EDGE ( 'NONE', *, *, #37529, .F. ) ;
#25316=CIRCLE ( 'NONE', #58320, 0.5000000000000004441 ) ;
#25319=CARTESIAN_POINT ( 'NONE',  ( -7.217511925163520914, -78.12578035745170268, 9.390386475653141218 ) ) ;
#25322=EDGE_LOOP ( 'NONE', ( #22200, #1822, #23659, #49508 ) ) ;
#25325=CARTESIAN_POINT ( 'NONE',  ( 7.646966891740999195, -55.60358255701000019, 10.19019756604999927 ) ) ;
#25326=AXIS2_PLACEMENT_3D ( 'NONE', #10389, #49677, #41097 ) ;
#25327=CARTESIAN_POINT ( 'NONE',  ( 7.770365054039128694, -17.76417299472041122, -10.20675369723943859 ) ) ;
#25328=CYLINDRICAL_SURFACE ( 'NONE', #36441, 1.750000000000001332 ) ;
#25333=CARTESIAN_POINT ( 'NONE',  ( -7.974014308125999762, -24.63100890329999970, 9.929675091742998561 ) ) ;
#25335=EDGE_CURVE ( 'NONE', #41874, #22190, #11720, .T. ) ;
#25337=DIRECTION ( 'NONE',  ( 0.7071067811865475727, 0.000000000000000000, -0.7071067811865475727 ) ) ;
#25338=CARTESIAN_POINT ( 'NONE',  ( 11.03890801094999929, -78.66213151614000765, -5.342433469444999972 ) ) ;
#25339=CARTESIAN_POINT ( 'NONE',  ( -1.750000000001000089, -60.04999998641999781, 12.56594318054000148 ) ) ;
#25342=FACE_OUTER_BOUND ( 'NONE', #39557, .T. ) ;
#25344=VECTOR ( 'NONE', #23444, 1000.000000000000227 ) ;
#25348=CARTESIAN_POINT ( 'NONE',  ( -3.408418700480000396, -3.491675407298000078, -1.019786534199000005 ) ) ;
#25352=CARTESIAN_POINT ( 'NONE',  ( -11.66824396372028971, -76.18874584464074928, 1.566409294560152654 ) ) ;
#25360=EDGE_CURVE ( 'NONE', #54154, #10368, #39210, .T. ) ;
#25362=CARTESIAN_POINT ( 'NONE',  ( -8.958641849998000950, -62.00112647771999974, 8.950065109854000056 ) ) ;
#25363=DIRECTION ( 'NONE',  ( 1.000000000000000000, 0.000000000000000000, 0.000000000000000000 ) ) ;
#25372=CARTESIAN_POINT ( 'NONE',  ( -10.24996238029999951, -57.04828923575999511, -7.705119999435999567 ) ) ;
#25374=EDGE_CURVE ( 'NONE', #20090, #46623, #7549, .T. ) ;
#25375=ORIENTED_EDGE ( 'NONE', *, *, #14208, .T. ) ;
#25376=CARTESIAN_POINT ( 'NONE',  ( 12.70556836347999941, -16.77227722772000007, -1.774194455291999869E-09 ) ) ;
#25378=CARTESIAN_POINT ( 'NONE',  ( -7.644093100845077871, -23.52380578988463711, -10.09634101412614804 ) ) ;
#25382=ORIENTED_EDGE ( 'NONE', *, *, #32927, .F. ) ;
#25388=CARTESIAN_POINT ( 'NONE',  ( 9.778561352719998823, -16.95143577368999743, 8.284566532398999428 ) ) ;
#25393=CARTESIAN_POINT ( 'NONE',  ( 7.079708506942000490, -78.42792498495001041, -10.47296538612000028 ) ) ;
#25394=CARTESIAN_POINT ( 'NONE',  ( 13.99609303101000002, -32.95862266598000190, 3.303296644036000229E-05 ) ) ;
#25395=CARTESIAN_POINT ( 'NONE',  ( 12.50000000000000000, -63.73717104351998586, 0.000000000000000000 ) ) ;
#25396=LINE ( 'NONE', #20118, #41731 ) ;
#25399=ORIENTED_EDGE ( 'NONE', *, *, #46369, .F. ) ;
#25406=DIRECTION ( 'NONE',  ( 0.6489586469534662783, -0.04890178980865751007, -0.7592504787603602256 ) ) ;
#25411=CARTESIAN_POINT ( 'NONE',  ( -7.648026768036999989, -60.04999998387000204, -10.12290050219000115 ) ) ;
#25412=AXIS2_PLACEMENT_3D ( 'NONE', #49144, #13994, #22861 ) ;
#25415=CARTESIAN_POINT ( 'NONE',  ( -12.53241208775999915, -19.23537109840999904, -1.667936697358999965 ) ) ;
#25417=EDGE_CURVE ( 'NONE', #38307, #56848, #33362, .T. ) ;
#25419=CARTESIAN_POINT ( 'NONE',  ( 0.000000000000000000, -18.75000000000000000, 12.00000000000000000 ) ) ;
#25427=CARTESIAN_POINT ( 'NONE',  ( -12.70228859453985670, -17.17803615247013838, 1.213484947683437509 ) ) ;
#25429=CARTESIAN_POINT ( 'NONE',  ( 1.312589504071557833, -2.405348311454605259, -3.269350533498157407 ) ) ;
#25434=CARTESIAN_POINT ( 'NONE',  ( 11.58635484046792641, -75.96315356379447792, 1.957992045167118667 ) ) ;
#25436=ORIENTED_EDGE ( 'NONE', *, *, #1215, .T. ) ;
#25442=CARTESIAN_POINT ( 'NONE',  ( 9.934814764470999648, -24.62368287829000124, -7.968971842743999723 ) ) ;
#25445=CARTESIAN_POINT ( 'NONE',  ( 0.1682664256278402770, -78.57055743907643830, 11.74683409834875825 ) ) ;
#25449=CARTESIAN_POINT ( 'NONE',  ( -8.838834764832000701, -55.54999999966999980, -8.838834764832000701 ) ) ;
#25450=LINE ( 'NONE', #38156, #45230 ) ;
#25453=CARTESIAN_POINT ( 'NONE',  ( -12.71798269388000158, -60.09778754156999980, -1.931086388578000079 ) ) ;
#25454=CARTESIAN_POINT ( 'NONE',  ( 10.98362417419999915, -18.84999999999999787, -0.5999999999999999778 ) ) ;
#25459=CIRCLE ( 'NONE', #11319, 13.86363636363999952 ) ;
#25461=FACE_OUTER_BOUND ( 'NONE', #23205, .T. ) ;
#25463=VERTEX_POINT ( 'NONE', #47841 ) ;
#25464=CARTESIAN_POINT ( 'NONE',  ( -12.54705919854999863, -54.26307476595999901, -1.287183453418999868 ) ) ;
#25466=VERTEX_POINT ( 'NONE', #7372 ) ;
#25474=ORIENTED_EDGE ( 'NONE', *, *, #35530, .F. ) ;
#25475=AXIS2_PLACEMENT_3D ( 'NONE', #8112, #18145, #44414 ) ;
#25481=FACE_OUTER_BOUND ( 'NONE', #12460, .T. ) ;
#25483=CARTESIAN_POINT ( 'NONE',  ( 1.750000000001000089, -19.24899163674999869, 12.60354432393000046 ) ) ;
#25487=PLANE ( 'NONE',  #7294 ) ;
#25488=CARTESIAN_POINT ( 'NONE',  ( -8.950130560535999535, -53.59887407320999841, 8.958576480190000524 ) ) ;
#25491=CARTESIAN_POINT ( 'NONE',  ( -7.986982684666001475, -17.27364722735000058, -10.07612755993999976 ) ) ;
#25492=CIRCLE ( 'NONE', #2882, 13.94827586206999825 ) ;
#25494=DIRECTION ( 'NONE',  ( -0.6489586447325241814, -0.04890182339223182045, -0.7592504784956282116 ) ) ;
#25499=ADVANCED_FACE ( 'NONE', ( #35076 ), #50301, .F. ) ;
#25501=CARTESIAN_POINT ( 'NONE',  ( 1.766902510613357569, -3.500000000000000444, 2.864370435608821985 ) ) ;
#25502=CARTESIAN_POINT ( 'NONE',  ( -3.505293455996059127, -1.741927197408730921, 0.3622374202452205427 ) ) ;
#25506=DIRECTION ( 'NONE',  ( 0.000000000000000000, 1.000000000000000000, 0.000000000000000000 ) ) ;
#25507=CARTESIAN_POINT ( 'NONE',  ( -12.60552511010000032, -18.71082276572999703, 1.799501877793999949 ) ) ;
#25508=CARTESIAN_POINT ( 'NONE',  ( 3.250357114718000151, -1.764977233352999830, -1.258728819614999939 ) ) ;
#25510=CARTESIAN_POINT ( 'NONE',  ( -12.83838672487999943, -55.59401611997999737, 2.062170725306000207 ) ) ;
#25511=LINE ( 'NONE', #40250, #31766 ) ;
#25512=CARTESIAN_POINT ( 'NONE',  ( 2.061613410425999771, -60.00570014443000133, 12.83797036857999885 ) ) ;
#25514=DIRECTION ( 'NONE',  ( -1.000000000000000000, 0.000000000000000000, 0.000000000000000000 ) ) ;
#25518=CARTESIAN_POINT ( 'NONE',  ( 9.746895442825083578, -76.40235638873841140, -6.561501312551729193 ) ) ;
#25526=DIRECTION ( 'NONE',  ( 0.000000000000000000, 1.000000000000000000, 0.000000000000000000 ) ) ;
#25532=FACE_OUTER_BOUND ( 'NONE', #47366, .T. ) ;
#25533=ORIENTED_EDGE ( 'NONE', *, *, #42360, .T. ) ;
#25536=ORIENTED_EDGE ( 'NONE', *, *, #40760, .T. ) ;
#25538=FACE_OUTER_BOUND ( 'NONE', #58237, .T. ) ;
#25542=VERTEX_POINT ( 'NONE', #49873 ) ;
#25544=ORIENTED_EDGE ( 'NONE', *, *, #57256, .F. ) ;
#25545=CARTESIAN_POINT ( 'NONE',  ( 7.398464061248616552, -55.34839576620328927, -8.140250184779796783 ) ) ;
#25546=ORIENTED_EDGE ( 'NONE', *, *, #53953, .F. ) ;
#25548=DIRECTION ( 'NONE',  ( 0.7071067811864970576, 3.544461080512985563E-08, -0.7071067811865970887 ) ) ;
#25549=DIRECTION ( 'NONE',  ( 0.000000000000000000, 0.000000000000000000, 1.000000000000000000 ) ) ;
#25551=DIRECTION ( 'NONE',  ( -1.000000000000000000, 0.000000000000000000, 0.000000000000000000 ) ) ;
#25554=CARTESIAN_POINT ( 'NONE',  ( -3.299302781710000243, -77.40086001149001049, 12.69174137596000129 ) ) ;
#25559=CIRCLE ( 'NONE', #148, 0.5000000000000004441 ) ;
#25561=CARTESIAN_POINT ( 'NONE',  ( 7.601397897754999633, -55.55000000209000177, 10.07627163191000008 ) ) ;
#25562=CARTESIAN_POINT ( 'NONE',  ( 2.471377992193831474, -2.907507802367013561, 2.123914601439464533 ) ) ;
#25567=CARTESIAN_POINT ( 'NONE',  ( -2.963791440107999886, -3.263363938828000244, 2.387889716789000083 ) ) ;
#25568=CARTESIAN_POINT ( 'NONE',  ( 10.53003236233000095, -23.32452273707999879, 7.612971540276999960 ) ) ;
#25569=CARTESIAN_POINT ( 'NONE',  ( -8.870414881026999154, -61.86963060230000622, -8.878264461126001095 ) ) ;
#25571=DIRECTION ( 'NONE',  ( 0.7071067811865474617, 0.000000000000000000, 0.7071067811865474617 ) ) ;
#25574=CARTESIAN_POINT ( 'NONE',  ( -3.346450045594000056, -76.94769696823999539, 12.57540552286999791 ) ) ;
#25578=CARTESIAN_POINT ( 'NONE',  ( 10.53066010801000019, -75.87533071877999191, 6.475268442873999497 ) ) ;
#25581=B_SPLINE_CURVE_WITH_KNOTS ( 'NONE', 3,
 ( #30021, #48076, #3189, #57195, #52200, #20609 ),
 .UNSPECIFIED., .F., .F.,
 ( 4, 2, 4 ),
 ( 0.000000000000000000, 0.5000000000000000000, 1.000000000000000000 ),
 .UNSPECIFIED. ) ;
#25582=FACE_OUTER_BOUND ( 'NONE', #31145, .T. ) ;
#25584=CARTESIAN_POINT ( 'NONE',  ( -9.018516758304000902, -79.14420186241999033, -9.073560724760000085 ) ) ;
#25585=CARTESIAN_POINT ( 'NONE',  ( -1.931087888049999979, -23.31584477285000290, -12.71658889741999943 ) ) ;
#25591=VERTEX_POINT ( 'NONE', #18858 ) ;
#25595=ORIENTED_EDGE ( 'NONE', *, *, #47283, .F. ) ;
#25597=CARTESIAN_POINT ( 'NONE',  ( -7.892048199455462765, -55.05053022673563845, -7.664266801485842606 ) ) ;
#25601=ORIENTED_EDGE ( 'NONE', *, *, #20439, .T. ) ;
#25602=EDGE_LOOP ( 'NONE', ( #26843, #44057, #2468, #13774 ) ) ;
#25604=CARTESIAN_POINT ( 'NONE',  ( 5.919062813527654399, -78.03099449878986604, 10.27295981138281356 ) ) ;
#25606=EDGE_LOOP ( 'NONE', ( #1373, #47349, #41878 ) ) ;
#25607=CARTESIAN_POINT ( 'NONE',  ( 12.43646312217999927, -53.87951485525000095, 0.1257251053154000153 ) ) ;
#25608=ORIENTED_EDGE ( 'NONE', *, *, #19623, .T. ) ;
#25613=CARTESIAN_POINT ( 'NONE',  ( 7.762982794220000038, -54.63910040255000666, 9.991998894170999179 ) ) ;
#25614=PLANE ( 'NONE',  #26081 ) ;
#25615=CARTESIAN_POINT ( 'NONE',  ( 13.99999999961999819, -72.70000000038000110, -1.691901775850999968E-09 ) ) ;
#25620=DIRECTION ( 'NONE',  ( -3.788638658030000158E-11, 1.000000000000000000, 0.000000000000000000 ) ) ;
#25622=CARTESIAN_POINT ( 'NONE',  ( -12.22985280536000019, -76.45708432191999293, -1.402219185755000153 ) ) ;
#25624=CARTESIAN_POINT ( 'NONE',  ( 7.624341766629000539, -55.53514853726999689, -10.42531125022999916 ) ) ;
#25626=CARTESIAN_POINT ( 'NONE',  ( 6.688645397968000950, -78.81176105510999719, 10.27915892414000076 ) ) ;
#25629=LINE ( 'NONE', #52508, #53098 ) ;
#25632=CARTESIAN_POINT ( 'NONE',  ( 12.72394223973000038, -60.02159774832999517, -1.930881086224999876 ) ) ;
#25633=CARTESIAN_POINT ( 'NONE',  ( 0.000000000000000000, -32.88214388149999934, 0.000000000000000000 ) ) ;
#25635=CARTESIAN_POINT ( 'NONE',  ( -3.342386390799999774, -1.861752247163000140, 0.8450881718492999628 ) ) ;
#25637=CARTESIAN_POINT ( 'NONE',  ( 12.56594317823000040, -18.74999998606000062, 1.750000000000000000 ) ) ;
#25638=CARTESIAN_POINT ( 'NONE',  ( -10.40284373066038803, -75.80000000000003979, 5.607632974479940025 ) ) ;
#25642=ORIENTED_EDGE ( 'NONE', *, *, #5762, .F. ) ;
#25647=CARTESIAN_POINT ( 'NONE',  ( -7.986976573832000881, -61.52634345601000376, 10.07613380459999952 ) ) ;
#25648=CARTESIAN_POINT ( 'NONE',  ( -3.150225605703000475, -1.751833096891999952, -1.400642508557000010 ) ) ;
#25651=CARTESIAN_POINT ( 'NONE',  ( -12.70228549156885123, -53.97187149226591174, -1.205357499401769950 ) ) ;
#25652=ORIENTED_EDGE ( 'NONE', *, *, #12045, .F. ) ;
#25659=VECTOR ( 'NONE', #58404, 1000.000000000000000 ) ;
#25660=ORIENTED_EDGE ( 'NONE', *, *, #37001, .T. ) ;
#25661=CARTESIAN_POINT ( 'NONE',  ( 10.07627163191000008, -60.04999999657000131, -7.601397897754999633 ) ) ;
#25662=CARTESIAN_POINT ( 'NONE',  ( -1.980584515752000119, -55.53514853344000102, -12.76303204600000107 ) ) ;
#25663=CARTESIAN_POINT ( 'NONE',  ( 2.062502994258999856, -57.04351820043999766, -12.92181194098999875 ) ) ;
#25667=CARTESIAN_POINT ( 'NONE',  ( -12.75761570867999950, -56.02180874340999850, 1.931043762602999925 ) ) ;
#25671=ORIENTED_EDGE ( 'NONE', *, *, #8778, .T. ) ;
#25672=ORIENTED_EDGE ( 'NONE', *, *, #54184, .T. ) ;
#25675=EDGE_LOOP ( 'NONE', ( #875, #50109, #1981, #58286 ) ) ;
#25678=CARTESIAN_POINT ( 'NONE',  ( 1.722320550003394679, -54.56336311145909690, 12.71171904433208866 ) ) ;
#25679=CARTESIAN_POINT ( 'NONE',  ( 12.49589899905999957, -77.31018438914000512, -3.422742383397000321 ) ) ;
#25681=CARTESIAN_POINT ( 'NONE',  ( -8.838834764832000701, -18.75000000000000000, 8.838834764832000701 ) ) ;
#25682=DIRECTION ( 'NONE',  ( -0.7071067811865475727, 0.000000000000000000, -0.7071067811865475727 ) ) ;
#25688=ORIENTED_EDGE ( 'NONE', *, *, #35064, .F. ) ;
#25689=EDGE_CURVE ( 'NONE', #47356, #29025, #3982, .T. ) ;
#25692=DIRECTION ( 'NONE',  ( -1.000000000000000000, 0.000000000000000000, 0.000000000000000000 ) ) ;
#25693=VECTOR ( 'NONE', #26202, 1000.000000000000114 ) ;
#25695=CARTESIAN_POINT ( 'NONE',  ( 12.00000000000000000, -18.75000000000000000, -1.250000000000000000 ) ) ;
#25701=CARTESIAN_POINT ( 'NONE',  ( 10.53003223722999948, -23.32452529362999982, -7.612971414713999962 ) ) ;
#25702=CARTESIAN_POINT ( 'NONE',  ( -12.85144117164000122, -58.55472016995999951, 1.980464439859999981 ) ) ;
#25704=CIRCLE ( 'NONE', #302, 1.750000000000001332 ) ;
#25705=FACE_OUTER_BOUND ( 'NONE', #21919, .T. ) ;
#25706=ADVANCED_FACE ( 'NONE', ( #52378 ), #5500, .F. ) ;
#25707=ORIENTED_EDGE ( 'NONE', *, *, #42922, .F. ) ;
#25710=DIRECTION ( 'NONE',  ( 1.158063445486000064E-14, 0.000000000000000000, -1.000000000000000000 ) ) ;
#25711=ADVANCED_FACE ( 'NONE', ( #4223 ), #12497, .T. ) ;
#25713=CARTESIAN_POINT ( 'NONE',  ( 13.99936781018472232, -32.88214388149999934, 0.1330447863085613691 ) ) ;
#25721=CARTESIAN_POINT ( 'NONE',  ( 10.85622085026185069, -75.98074828373636080, 4.494179903487589556 ) ) ;
#25726=CARTESIAN_POINT ( 'NONE',  ( 1.995598161747699439, -2.278437428562636757, -2.597973788337413215 ) ) ;
#25731=CARTESIAN_POINT ( 'NONE',  ( 5.295455463754168868, -78.53769345340680275, 10.50214436971515575 ) ) ;
#25732=CARTESIAN_POINT ( 'NONE',  ( 8.838834764832000701, -60.04999999966999980, -8.838834764832000701 ) ) ;
#25741=AXIS2_PLACEMENT_3D ( 'NONE', #58168, #4443, #8870 ) ;
#25745=EDGE_CURVE ( 'NONE', #42100, #2183, #44090, .T. ) ;
#25746=VERTEX_POINT ( 'NONE', #39650 ) ;
#25747=CARTESIAN_POINT ( 'NONE',  ( 0.000000000000000000, -4.000000000000000000, -8.999999999999927169 ) ) ;
#25749=CARTESIAN_POINT ( 'NONE',  ( 1.931043762602999925, -19.22180874373999870, 12.75761570870000128 ) ) ;
#25756=CARTESIAN_POINT ( 'NONE',  ( -12.66314509266000066, -53.62135249290999894, 0.04032083120558000583 ) ) ;
#25757=VERTEX_POINT ( 'NONE', #3075 ) ;
#25759=ORIENTED_EDGE ( 'NONE', *, *, #12181, .T. ) ;
#25760=CARTESIAN_POINT ( 'NONE',  ( 10.52682159650000138, -23.42567232067999683, 7.605689092050000433 ) ) ;
#25761=AXIS2_PLACEMENT_3D ( 'NONE', #52891, #43752, #8011 ) ;
#25763=AXIS2_PLACEMENT_3D ( 'NONE', #18118, #25864, #39449 ) ;
#25767=VERTEX_POINT ( 'NONE', #25785 ) ;
#25768=ORIENTED_EDGE ( 'NONE', *, *, #55685, .F. ) ;
#25772=CARTESIAN_POINT ( 'NONE',  ( -12.70956478401000034, -60.20497526583999814, -1.933781249744999986 ) ) ;
#25774=FACE_OUTER_BOUND ( 'NONE', #48778, .T. ) ;
#25775=CARTESIAN_POINT ( 'NONE',  ( 13.86363636363000218, -32.36102867817999851, 1.277888278705000044E-05 ) ) ;
#25780=CARTESIAN_POINT ( 'NONE',  ( -8.220399303298000504, -53.98050618241000365, 9.523318109972001011 ) ) ;
#25783=CARTESIAN_POINT ( 'NONE',  ( -7.760941378066999796, -17.76914109191999813, -10.15321372496999963 ) ) ;
#25784=CARTESIAN_POINT ( 'NONE',  ( 7.642147947533000085, -59.58485473249000108, 10.55910102243999837 ) ) ;
#25785=CARTESIAN_POINT ( 'NONE',  ( 12.50240681836000078, -61.48234730679999416, -1.005418944265000114 ) ) ;
#25791=EDGE_LOOP ( 'NONE', ( #48295, #14324, #36430, #4632, #14562 ) ) ;
#25792=CARTESIAN_POINT ( 'NONE',  ( 12.49999990534960226, -49.87071424677999687, 0.001538265197309672755 ) ) ;
#25793=AXIS2_PLACEMENT_3D ( 'NONE', #7651, #33926, #47258 ) ;
#25794=FACE_OUTER_BOUND ( 'NONE', #985, .T. ) ;
#25795=CARTESIAN_POINT ( 'NONE',  ( -12.75761570870000128, -19.22180874373999870, 1.931043762602999925 ) ) ;
#25796=CARTESIAN_POINT ( 'NONE',  ( -0.4933341540935000102, -3.017260803691999893, 3.612264854784000168 ) ) ;
#25798=CARTESIAN_POINT ( 'NONE',  ( -12.77562786365999870, -53.53761952105000432, 0.5426593252874999385 ) ) ;
#25799=CARTESIAN_POINT ( 'NONE',  ( -1.980584515756000030, -60.06485150062000145, -12.76303204342999997 ) ) ;
#25800=CARTESIAN_POINT ( 'NONE',  ( -3.250000000000000000, -2.100000000000000089, 0.000000000000000000 ) ) ;
#25805=DIRECTION ( 'NONE',  ( 0.9859154929576978699, -0.1672442547472993701, 2.241735036661995419E-11 ) ) ;
#25807=CARTESIAN_POINT ( 'NONE',  ( 10.85325925093383681, -76.41847643180719274, -4.501722357903592986 ) ) ;
#25809=DIRECTION ( 'NONE',  ( -0.7071067811865475727, 0.000000000000000000, 0.7071067811865475727 ) ) ;
#25810=CARTESIAN_POINT ( 'NONE',  ( -3.249671636765069316, -1.085071008848613960, 0.6795062066016868130 ) ) ;
#25811=DIRECTION ( 'NONE',  ( 0.7026410690473250398, -0.1122098755728047209, 0.7026410690473250398 ) ) ;
#25813=CARTESIAN_POINT ( 'NONE',  ( -0.7612530485432564831, -3.494945300038082348, 3.169665447793446500 ) ) ;
#25816=CARTESIAN_POINT ( 'NONE',  ( 10.45812042142963350, -75.79999999999999716, 6.020400211397366697 ) ) ;
#25822=ORIENTED_EDGE ( 'NONE', *, *, #12233, .T. ) ;
#25823=CARTESIAN_POINT ( 'NONE',  ( 7.644093100861836021, -60.32380578946132488, 10.09634101415691809 ) ) ;
#25824=EDGE_LOOP ( 'NONE', ( #39755, #51775, #14510, #49731, #43553, #42333 ) ) ;
#25826=CARTESIAN_POINT ( 'NONE',  ( 0.8506806241676508895, -1.354166666666666297, 3.165411199172028400 ) ) ;
#25827=ORIENTED_EDGE ( 'NONE', *, *, #27057, .F. ) ;
#25828=CIRCLE ( 'NONE', #55088, 5.000000000000000000 ) ;
#25831=ORIENTED_EDGE ( 'NONE', *, *, #45897, .F. ) ;
#25832=CARTESIAN_POINT ( 'NONE',  ( -5.996769837547000215, -78.92093781725999690, 10.80604144232000152 ) ) ;
#25833=VERTEX_POINT ( 'NONE', #21353 ) ;
#25834=CARTESIAN_POINT ( 'NONE',  ( 8.090910852014799204, -55.25278097498591734, -7.452378523310748015 ) ) ;
#25838=CIRCLE ( 'NONE', #39070, 12.50000000000000000 ) ;
#25840=DIRECTION ( 'NONE',  ( 0.9957542217969250764, 0.04890179605521120104, -0.07798810240142199646 ) ) ;
#25843=CARTESIAN_POINT ( 'NONE',  ( 5.691226796558999546, -77.84489713918000575, 11.81421328157999895 ) ) ;
#25846=FACE_OUTER_BOUND ( 'NONE', #15586, .T. ) ;
#25849=CARTESIAN_POINT ( 'NONE',  ( 7.954951288349001004, -23.25000000000000000, -9.722718241315000398 ) ) ;
#25850=EDGE_CURVE ( 'NONE', #54702, #49897, #664, .T. ) ;
#25851=CARTESIAN_POINT ( 'NONE',  ( 1.226192273942385391, -2.945367736052959540, 3.009049604377801224 ) ) ;
#25853=CARTESIAN_POINT ( 'NONE',  ( -1.247385801080000078, -24.47722256257000240, -12.50301438876999960 ) ) ;
#25855=CARTESIAN_POINT ( 'NONE',  ( -3.268529449828999844, -2.325473928489000031, -1.950076325099000085 ) ) ;
#25857=CARTESIAN_POINT ( 'NONE',  ( -7.758655887927999650, -60.95078616210999911, -9.996711281005000060 ) ) ;
#25859=CIRCLE ( 'NONE', #8884, 1.250000000000000000 ) ;
#25861=CARTESIAN_POINT ( 'NONE',  ( -12.70926961119000076, -18.59159259619999816, -1.933875435151000133 ) ) ;
#25862=CARTESIAN_POINT ( 'NONE',  ( 9.175280770439000477, -76.74417995138000492, -8.221808909867000636 ) ) ;
#25863=AXIS2_PLACEMENT_3D ( 'NONE', #3084, #16082, #11658 ) ;
#25864=DIRECTION ( 'NONE',  ( 0.000000000000000000, 1.000000000000000000, 0.000000000000000000 ) ) ;
#25867=CARTESIAN_POINT ( 'NONE',  ( 9.003374968273998746, -76.27138176936000491, -8.471312771788998219 ) ) ;
#25868=ORIENTED_EDGE ( 'NONE', *, *, #6596, .F. ) ;
#25871=DIRECTION ( 'NONE',  ( -1.000000000000000000, 0.000000000000000000, 0.000000000000000000 ) ) ;
#25872=CARTESIAN_POINT ( 'NONE',  ( 12.49997170193999985, -59.99201514515999634, 1.666513530428000101 ) ) ;
#25873=CARTESIAN_POINT ( 'NONE',  ( -1.667936688463999895, -19.23513569609999863, -12.53239398062000198 ) ) ;
#25876=CARTESIAN_POINT ( 'NONE',  ( -12.65375411746000012, -21.74977139047000207, 1.750000000000000000 ) ) ;
#25878=ORIENTED_EDGE ( 'NONE', *, *, #3473, .F. ) ;
#25882=EDGE_CURVE ( 'NONE', #8017, #34968, #5674, .T. ) ;
#25884=CARTESIAN_POINT ( 'NONE',  ( 12.69619287815999975, -57.04916621739000249, 1.799475295154000065 ) ) ;
#25886=ORIENTED_EDGE ( 'NONE', *, *, #16639, .T. ) ;
#25888=VERTEX_POINT ( 'NONE', #18687 ) ;
#25889=EDGE_CURVE ( 'NONE', #43183, #6045, #32235, .T. ) ;
#25891=CARTESIAN_POINT ( 'NONE',  ( 0.000000000000000000, -60.04999999966999980, -12.00000000000000000 ) ) ;
#25892=DIRECTION ( 'NONE',  ( 0.5000000000000744960, -0.7071067811864422126, -0.5000000000000744960 ) ) ;
#25893=EDGE_CURVE ( 'NONE', #18079, #27707, #991, .T. ) ;
#25894=AXIS2_PLACEMENT_3D ( 'NONE', #8064, #21639, #12775 ) ;
#25895=ORIENTED_EDGE ( 'NONE', *, *, #42973, .F. ) ;
#25896=CARTESIAN_POINT ( 'NONE',  ( 10.99606201159937058, -18.31532548058919829, 0.3145367810815102305 ) ) ;
#25897=ORIENTED_EDGE ( 'NONE', *, *, #16367, .F. ) ;
#25901=CARTESIAN_POINT ( 'NONE',  ( 7.659225706216000518, -55.11732795990999989, 9.963487823480999594 ) ) ;
#25904=AXIS2_PLACEMENT_3D ( 'NONE', #5493, #11112, #23791 ) ;
#25905=CARTESIAN_POINT ( 'NONE',  ( 12.70455691847901214, -61.36014620563325650, -1.489817752282083463 ) ) ;
#25908=CARTESIAN_POINT ( 'NONE',  ( -7.658900562714999971, -23.20940503079999928, 10.01676248781999945 ) ) ;
#25909=EDGE_CURVE ( 'NONE', #4126, #49275, #38258, .T. ) ;
#25914=CARTESIAN_POINT ( 'NONE',  ( 0.000000000000000000, -2.900000000000000355, 0.000000000000000000 ) ) ;
#25916=FACE_OUTER_BOUND ( 'NONE', #18569, .T. ) ;
#25917=CARTESIAN_POINT ( 'NONE',  ( 0.000000000000000000, -49.87071424677999687, 0.000000000000000000 ) ) ;
#25922=CARTESIAN_POINT ( 'NONE',  ( -3.247122682022999918, -2.002034555870999988, -1.453237460094999989 ) ) ;
#25932=VECTOR ( 'NONE', #46238, 999.9999999999998863 ) ;
#25936=AXIS2_PLACEMENT_3D ( 'NONE', #12334, #48362, #39767 ) ;
#25937=CARTESIAN_POINT ( 'NONE',  ( 12.70556836352000118, -62.02772277195000328, 2.424222323408999617E-09 ) ) ;
#25939=CARTESIAN_POINT ( 'NONE',  ( 12.77656765293000163, -25.31198129913999750, -0.1555235816856000153 ) ) ;
#25942=DIRECTION ( 'NONE',  ( -1.000000000000000000, 0.000000000000000000, 0.000000000000000000 ) ) ;
#25945=DIRECTION ( 'NONE',  ( -0.7071067811865475727, 0.000000000000000000, -0.7071067811865475727 ) ) ;
#25950=ADVANCED_FACE ( 'NONE', ( #26934 ), #5106, .F. ) ;
#25951=CARTESIAN_POINT ( 'NONE',  ( 0.000000000000000000, -9.638971321655001034, 0.000000000000000000 ) ) ;
#25952=CARTESIAN_POINT ( 'NONE',  ( 11.74923627718826502, -77.94158813120921536, -0.7696914254377311693 ) ) ;
#25953=CARTESIAN_POINT ( 'NONE',  ( -3.250000000000000000, -1.000000000000000000, 1.223542571470000149E-13 ) ) ;
#25954=CARTESIAN_POINT ( 'NONE',  ( -7.619389775666999931, -55.39213701549999769, -10.35398629634000045 ) ) ;
#25956=EDGE_LOOP ( 'NONE', ( #18342, #57478, #14274, #48078 ) ) ;
#25957=ADVANCED_FACE ( 'NONE', ( #40825 ), #41215, .F. ) ;
#25958=ORIENTED_EDGE ( 'NONE', *, *, #38157, .T. ) ;
#25961=VERTEX_POINT ( 'NONE', #23685 ) ;
#25964=CARTESIAN_POINT ( 'NONE',  ( -11.44417895085270942, -75.82083333333332575, -3.075537641221545826 ) ) ;
#25965=CARTESIAN_POINT ( 'NONE',  ( -1.243328516745999979, -77.78579772561000993, -12.73826093197000020 ) ) ;
#25967=DIRECTION ( 'NONE',  ( 0.000000000000000000, 0.000000000000000000, 1.000000000000000000 ) ) ;
#25970=VECTOR ( 'NONE', #17362, 1000.000000000000227 ) ;
#25972=CARTESIAN_POINT ( 'NONE',  ( 7.764220096248216407, -17.74399029335688383, 10.21028322255854626 ) ) ;
#25973=EDGE_LOOP ( 'NONE', ( #53400, #16444, #40347, #43914, #2421, #52139 ) ) ;
#25980=CARTESIAN_POINT ( 'NONE',  ( -12.50239399162999909, -54.11640749821000185, 1.003653728895000041 ) ) ;
#25981=CARTESIAN_POINT ( 'NONE',  ( 12.49306752634999995, -23.28056692670000061, 1.667917367010000040 ) ) ;
#25982=DIRECTION ( 'NONE',  ( 0.000000000000000000, 1.000000000000000000, 0.000000000000000000 ) ) ;
#25985=CARTESIAN_POINT ( 'NONE',  ( 10.01235002622999914, -18.70151115557999688, -7.653559626094000201 ) ) ;
#25989=EDGE_LOOP ( 'NONE', ( #8628, #21821, #17989 ) ) ;
#25996=EDGE_CURVE ( 'NONE', #51746, #7307, #30688, .T. ) ;
#26000=CARTESIAN_POINT ( 'NONE',  ( -10.21026636380264740, -24.25606635949579371, -7.764233071689755405 ) ) ;
#26001=CARTESIAN_POINT ( 'NONE',  ( 9.540682851482767290, -75.99946523393471409, 6.860877985616982144 ) ) ;
#26004=DIRECTION ( 'NONE',  ( 0.000000000000000000, 1.000000000000000000, 0.000000000000000000 ) ) ;
#26010=CARTESIAN_POINT ( 'NONE',  ( 1.501534314746039600, -17.44847048340742290, 12.70455943740098803 ) ) ;
#26012=CARTESIAN_POINT ( 'NONE',  ( -1.869988834943083544, -78.58576359787208787, 11.64790316465944819 ) ) ;
#26014=VERTEX_POINT ( 'NONE', #31945 ) ;
#26020=LINE ( 'NONE', #52904, #1925 ) ;
#26021=DIRECTION ( 'NONE',  ( -0.7071067810866970005, 6.386274622742979319E-09, 0.7071067812863980340 ) ) ;
#26025=CIRCLE ( 'NONE', #13767, 12.25000000000000000 ) ;
#26027=AXIS2_PLACEMENT_3D ( 'NONE', #50584, #54708, #36693 ) ;
#26028=CARTESIAN_POINT ( 'NONE',  ( 2.062503053667999797, -20.24263462181000151, 12.92177931909999877 ) ) ;
#26029=CARTESIAN_POINT ( 'NONE',  ( -11.75000000000000711, -76.28958333333332575, 1.538071403319954955 ) ) ;
#26030=ORIENTED_EDGE ( 'NONE', *, *, #42244, .F. ) ;
#26037=VERTEX_POINT ( 'NONE', #5390 ) ;
#26047=FACE_OUTER_BOUND ( 'NONE', #9940, .T. ) ;
#26050=CARTESIAN_POINT ( 'NONE',  ( 7.654537085030000299, -23.28056692670000061, 10.01332844637000008 ) ) ;
#26052=CARTESIAN_POINT ( 'NONE',  ( 12.76303204291999904, -55.53514849259999409, 1.980584515756000030 ) ) ;
#26054=CARTESIAN_POINT ( 'NONE',  ( 12.79971535686000017, -18.20965922269000004, -2.019101350716999921 ) ) ;
#26055=CARTESIAN_POINT ( 'NONE',  ( -9.929702205000999982, -24.63097880280000140, -7.973987073284000360 ) ) ;
#26057=ORIENTED_EDGE ( 'NONE', *, *, #6580, .F. ) ;
#26061=CARTESIAN_POINT ( 'NONE',  ( -9.934825859755001431, -17.37633188891999936, -7.968960864700001423 ) ) ;
#26063=ADVANCED_FACE ( 'NONE', ( #49400 ), #20355, .F. ) ;
#26064=FACE_OUTER_BOUND ( 'NONE', #45524, .T. ) ;
#26065=CARTESIAN_POINT ( 'NONE',  ( -1.582498447119000229, -17.84913877521999837, -12.55493832972999968 ) ) ;
#26067=CARTESIAN_POINT ( 'NONE',  ( 10.55910102243999837, -59.58485473249000108, -7.642147947533000085 ) ) ;
#26068=DIRECTION ( 'NONE',  ( -1.000000000000000000, 0.000000000000000000, 0.000000000000000000 ) ) ;
#26070=DIRECTION ( 'NONE',  ( 0.000000000000000000, -1.000000000000000000, 0.000000000000000000 ) ) ;
#26072=AXIS2_PLACEMENT_3D ( 'NONE', #28539, #20000, #2287 ) ;
#26074=CARTESIAN_POINT ( 'NONE',  ( -1.636392600175404999, -1.518396803410333895, 2.841196409148389890 ) ) ;
#26075=CARTESIAN_POINT ( 'NONE',  ( 0.8537148449505999048, -54.09501854057999992, 12.43377424869000158 ) ) ;
#26077=CIRCLE ( 'NONE', #27969, 12.50000000000000000 ) ;
#26078=CARTESIAN_POINT ( 'NONE',  ( -3.710753042444999927, -2.736382899542999958, -0.8462355775293999294 ) ) ;
#26081=AXIS2_PLACEMENT_3D ( 'NONE', #47514, #39189, #25041 ) ;
#26082=CARTESIAN_POINT ( 'NONE',  ( -12.66232176271000043, -53.66513311386999874, 0.5079086068997999970 ) ) ;
#26084=CARTESIAN_POINT ( 'NONE',  ( -3.166600152060512929, -2.080649301304957177, 0.8522904230390753177 ) ) ;
#26088=B_SPLINE_CURVE_WITH_KNOTS ( 'NONE', 3,
 ( #2736, #20736, #11882, #36761, #16312, #42890, #34293, #20449, #29859, #54780, #37052, #38152, #47914, #45942, #23194, #11305, #34005, #56174, #2447, #38445, #29286, #56463, #47335, #16016, #5474, #50364, #14323, #33428, #41489, #32318, #27895, #9914, #15434, #1076, #55884, #51465, #20163, #29004, #47043, #6573, #24584, #42600, #2163, #15722, #33720, #3309, #48199, #22168, #58188, #25731, #44615, #7446, #4170, #53467, #49047, #21303, #12729, #3021, #48472, #40176, #26581, #35438, #8594, #39311, #16885, #12446, #17751, #44319, #53180, #25445, #35739, #13009, #26012, #30722, #53770, #31009 ),
 .UNSPECIFIED., .F., .F.,
 ( 4, 2, 2, 2, 2, 2, 1, 1, 2, 2, 2, 2, 1, 2, 2, 1, 1, 1, 2, 2, 2, 2, 2, 1, 1, 1, 1, 1, 2, 2, 2, 2, 2, 1, 1, 1, 2, 2, 2, 2, 1, 1, 2, 2, 2, 4 ),
 ( 0.000000000000000000, 0.06249999999998635813, 0.1249999999999727163, 0.1406249999999693023, 0.1425781249999689138, 0.1435546874999686917, 0.1445312499999684697, 0.1484374999999675815, 0.1562499999999656664, 0.1874999999999584499, 0.2499999999999439060, 0.2812499999999366618, 0.2851562499999358846, 0.2856445312499357181, 0.2861328124999355516, 0.2871093749999354405, 0.2890624999999352185, 0.2968749999999345524, 0.3124999999999332201, 0.3749999999999282241, 0.4374999999999232836, 0.4687499999999208411, 0.4843749999999195643, 0.4921874999999190092, 0.4960937499999186207, 0.4980468749999185096, 0.4990234374999184541, 0.4995117187499184541, 0.4997558593749183986, 0.4999999999999182876, 0.5624999999999316103, 0.5937499999999382716, 0.6093749999999416023, 0.6171874999999432676, 0.6210937499999440448, 0.6230468749999443778, 0.6240234374999445999, 0.6249999999999448219, 0.6874999999999542588, 0.7187499999999590328, 0.7343749999999613642, 0.7421874999999625855, 0.7460937499999631406, 0.7499999999999636957, 0.8749999999999819034, 1.000000000000000000 ),
 .UNSPECIFIED. ) ;
#26091=EDGE_CURVE ( 'NONE', #49809, #4894, #15763, .T. ) ;
#26093=CARTESIAN_POINT ( 'NONE',  ( 7.674614791488999721, -22.75100836106000202, 10.14948852564000070 ) ) ;
#26098=CARTESIAN_POINT ( 'NONE',  ( 12.65372179310999989, -20.24935286375000132, -1.750000000000000000 ) ) ;
#26099=CARTESIAN_POINT ( 'NONE',  ( -10.10448976476253158, -17.54884052606732681, -7.864761218165275736 ) ) ;
#26100=B_SPLINE_CURVE_WITH_KNOTS ( 'NONE', 3,
 ( #5750, #27883, #29058, #45930, #19050, #41188 ),
 .UNSPECIFIED., .F., .F.,
 ( 4, 2, 4 ),
 ( 0.000000000000000000, 0.5000000000000000000, 1.000000000000000000 ),
 .UNSPECIFIED. ) ;
#26104=CARTESIAN_POINT ( 'NONE',  ( -10.98363357722940314, -23.18990228819912147, -0.5998278677060955300 ) ) ;
#26107=CARTESIAN_POINT ( 'NONE',  ( 1.980611416588517359, -23.52597731806571701, 12.74335092662995805 ) ) ;
#26109=ORIENTED_EDGE ( 'NONE', *, *, #29073, .F. ) ;
#26110=DIRECTION ( 'NONE',  ( 1.000000000000000000, 0.000000000000000000, 0.000000000000000000 ) ) ;
#26112=ORIENTED_EDGE ( 'NONE', *, *, #10459, .F. ) ;
#26113=DIRECTION ( 'NONE',  ( 0.000000000000000000, -1.000000000000000000, 0.000000000000000000 ) ) ;
#26115=VECTOR ( 'NONE', #20283, 1000.000000000000000 ) ;
#26119=ORIENTED_EDGE ( 'NONE', *, *, #48742, .F. ) ;
#26121=CARTESIAN_POINT ( 'NONE',  ( -3.402929133075000223, -78.31652404215999752, 11.45270446182999891 ) ) ;
#26122=VECTOR ( 'NONE', #18521, 1000.000000000000000 ) ;
#26124=VERTEX_POINT ( 'NONE', #55566 ) ;
#26125=FACE_OUTER_BOUND ( 'NONE', #28655, .T. ) ;
#26126=FACE_BOUND ( 'NONE', #39898, .T. ) ;
#26130=DIRECTION ( 'NONE',  ( 0.000000000000000000, 1.000000000000000000, 0.000000000000000000 ) ) ;
#26134=CARTESIAN_POINT ( 'NONE',  ( 1.235365857667927836, -79.04166666667985908, 11.79166666709374134 ) ) ;
#26135=CARTESIAN_POINT ( 'NONE',  ( -3.250880417296999614, -76.64007569364000005, 12.21627067396000044 ) ) ;
#26137=CARTESIAN_POINT ( 'NONE',  ( -6.464912241513801260E-06, -79.20362641130290626, -11.95086305119197689 ) ) ;
#26139=CARTESIAN_POINT ( 'NONE',  ( -10.42272502862000039, -58.55453807205000061, 7.691893942725999800 ) ) ;
#26140=CARTESIAN_POINT ( 'NONE',  ( -2.299886044274590535, -3.037960577415522945, 2.295943121830337663 ) ) ;
#26142=EDGE_CURVE ( 'NONE', #21397, #58285, #23302, .T. ) ;
#26145=CARTESIAN_POINT ( 'NONE',  ( -3.804208684430999909, -3.319815397808000057, -0.1186911049137999996 ) ) ;
#26152=CARTESIAN_POINT ( 'NONE',  ( -12.43356773666999970, -17.28739071017999862, -0.8411682846947000636 ) ) ;
#26153=CARTESIAN_POINT ( 'NONE',  ( -3.274010471232999819, -77.44723873689001437, 12.59444704299999884 ) ) ;
#26154=VECTOR ( 'NONE', #5794, 1000.000000000000000 ) ;
#26156=CARTESIAN_POINT ( 'NONE',  ( -10.42531124908000173, -60.06485148440999922, -7.624341765471999821 ) ) ;
#26157=CARTESIAN_POINT ( 'NONE',  ( -5.178179572192000535, -75.67130441998999402, -10.91684957994999827 ) ) ;
#26158=B_SPLINE_CURVE_WITH_KNOTS ( 'NONE', 3,
 ( #38240, #19659, #6661, #37660, #55675, #51263 ),
 .UNSPECIFIED., .F., .F.,
 ( 4, 2, 4 ),
 ( 0.000000000000000000, 0.5000000000000000000, 1.000000000000000000 ),
 .UNSPECIFIED. ) ;
#26160=DIRECTION ( 'NONE',  ( 0.000000000000000000, 0.000000000000000000, -1.000000000000000000 ) ) ;
#26161=FACE_OUTER_BOUND ( 'NONE', #45060, .T. ) ;
#26162=CIRCLE ( 'NONE', #45022, 9.000000000000000000 ) ;
#26164=CARTESIAN_POINT ( 'NONE',  ( -1.931086388455000025, -23.29778595484999926, -12.71798280855999863 ) ) ;
#26170=VERTEX_POINT ( 'NONE', #6723 ) ;
#26175=VERTEX_POINT ( 'NONE', #51896 ) ;
#26176=ORIENTED_EDGE ( 'NONE', *, *, #18203, .T. ) ;
#26178=CARTESIAN_POINT ( 'NONE',  ( -10.45205659047000069, -56.03767314774999875, 7.651160337227000063 ) ) ;
#26180=ORIENTED_EDGE ( 'NONE', *, *, #19809, .F. ) ;
#26181=ORIENTED_EDGE ( 'NONE', *, *, #16020, .T. ) ;
#26184=CARTESIAN_POINT ( 'NONE',  ( 2.030241441219323928, -1.014979566676556644, -3.469969701195170231 ) ) ;
#26185=B_SPLINE_SURFACE_WITH_KNOTS ( 'NONE', 3, 3, ( 
 ( #25048, #29747, #47800, #34179 ),
 ( #20908, #11492, #7620, #25908 ),
 ( #38910, #52785, #21194, #12338 ),
 ( #7332, #29180, #42780, #39195 ),
 ( #57209, #47227, #43070, #6758 ),
 ( #15615, #25333, #30327, #24768 ),
 ( #15908, #20337, #38332, #33893 ),
 ( #29465, #3479, #30620, #49531 ),
 ( #57785, #13784, #53958, #40665 ),
 ( #8196, #9077, #31486, #44799 ),
 ( #49229, #9375, #31189, #8780 ),
 ( #26771, #35038, #27064, #58375 ),
 ( #13495, #30903, #45103, #4051 ),
 ( #4657, #49828, #31784, #22053 ),
 ( #35928, #21485, #4351, #40062 ),
 ( #39771, #22656, #257, #39492 ),
 ( #12903, #57495, #40367, #26475 ) ),
 .UNSPECIFIED., .F., .F., .F.,
 ( 4, 1, 1, 1, 1, 1, 1, 1, 1, 1, 1, 1, 1, 1, 4 ),
 ( 4, 4 ),
 ( -0.01011786823680000010, 0.000000000000000000, 0.08333333333333001192, 0.1666666666667000196, 0.2500000000000000000, 0.3333333333333000081, 0.4166666666666999919, 0.5000000000000000000, 0.5833333333333000637, 0.6666666666667000474, 0.7500000000000000000, 0.8333333333333000637, 0.9166666666667000474, 1.000000000000000000, 1.010371592463000123 ),
 ( -0.3559705548529999986, 1.357613344742000017 ),
 .UNSPECIFIED. ) ;
#26186=VERTEX_POINT ( 'NONE', #50741 ) ;
#26189=CARTESIAN_POINT ( 'NONE',  ( -11.55418265775999842, -79.02279858628688203, 4.110954701505000308 ) ) ;
#26191=CARTESIAN_POINT ( 'NONE',  ( 12.65375411747000101, -58.54977139013999476, -1.750000000000000000 ) ) ;
#26192=EDGE_CURVE ( 'NONE', #10827, #50383, #5397, .T. ) ;
#26193=CARTESIAN_POINT ( 'NONE',  ( -7.705119999407000542, -21.75171076523999858, -10.24996238026999862 ) ) ;
#26197=CARTESIAN_POINT ( 'NONE',  ( 7.691893942748999180, -57.04546192861999998, -10.42272502865000128 ) ) ;
#26202=DIRECTION ( 'NONE',  ( 0.7071067811814418791, 1.254536121802073994E-07, 0.7071067811916420531 ) ) ;
#26204=DIRECTION ( 'NONE',  ( 0.000000000000000000, 0.000000000000000000, -1.000000000000000000 ) ) ;
#26212=DIRECTION ( 'NONE',  ( -1.000000000000000000, 0.000000000000000000, 0.000000000000000000 ) ) ;
#26216=FACE_OUTER_BOUND ( 'NONE', #17990, .T. ) ;
#26226=CARTESIAN_POINT ( 'NONE',  ( -10.13694968399000018, -60.50834319308000175, 7.646073915548999622 ) ) ;
#26229=CARTESIAN_POINT ( 'NONE',  ( 12.77649794757999935, -25.30831393477999924, 0.06464137375187999079 ) ) ;
#26234=AXIS2_PLACEMENT_3D ( 'NONE', #3018, #2444, #24869 ) ;
#26235=CARTESIAN_POINT ( 'NONE',  ( -1.318116285635148266, -1.693330829645463664, -3.001025458541523694 ) ) ;
#26240=CARTESIAN_POINT ( 'NONE',  ( 10.35453599130000057, -76.65783510652001098, -6.064947188958000446 ) ) ;
#26241=DIRECTION ( 'NONE',  ( 0.7071067811865970887, 0.000000000000000000, 0.7071067811864981678 ) ) ;
#26242=CARTESIAN_POINT ( 'NONE',  ( -1.618935784558787949, -54.87248831271473648, -12.52134385796515836 ) ) ;
#26243=ORIENTED_EDGE ( 'NONE', *, *, #2763, .F. ) ;
#26245=CARTESIAN_POINT ( 'NONE',  ( -9.934825859728000808, -54.17633188858999915, -7.968960864672001598 ) ) ;
#26247=VERTEX_POINT ( 'NONE', #9384 ) ;
#26251=DIRECTION ( 'NONE',  ( -0.7071067811865475727, 0.000000000000000000, -0.7071067811865475727 ) ) ;
#26257=CARTESIAN_POINT ( 'NONE',  ( -3.226165562315000290, -77.88915923096000427, 12.71052925661000010 ) ) ;
#26260=CARTESIAN_POINT ( 'NONE',  ( 13.13047446164998711, -22.78578169018998878, -0.8260994316375004365 ) ) ;
#26264=CARTESIAN_POINT ( 'NONE',  ( 9.355955347604632877, -16.82516908802490008, 8.610895743743158803 ) ) ;
#26265=ORIENTED_EDGE ( 'NONE', *, *, #58151, .T. ) ;
#26267=CARTESIAN_POINT ( 'NONE',  ( 10.54796701376999835, -75.81043591312999297, 6.346365727669000201 ) ) ;
#26269=CARTESIAN_POINT ( 'NONE',  ( 11.70615142939037590, -76.45809945638056604, 1.224787512100862230 ) ) ;
#26270=CARTESIAN_POINT ( 'NONE',  ( 1.749899258080120479, -60.18716848725620139, -12.55433901293723586 ) ) ;
#26271=CARTESIAN_POINT ( 'NONE',  ( -3.264119181477372678, -3.379906652641984088, -1.321296673820179457 ) ) ;
#26272=VECTOR ( 'NONE', #7912, 1000.000000000000000 ) ;
#26273=CARTESIAN_POINT ( 'NONE',  ( 12.58335110161999815, -21.74888345808999901, 1.667961430005999945 ) ) ;
#26274=CARTESIAN_POINT ( 'NONE',  ( 7.958776492191999452, -24.47699850276000078, -9.723157982392999443 ) ) ;
#26277=EDGE_CURVE ( 'NONE', #46351, #37150, #17947, .T. ) ;
#26278=CARTESIAN_POINT ( 'NONE',  ( 10.07719973192000040, -21.74888345808999901, -7.718346056094000041 ) ) ;
#26282=VERTEX_POINT ( 'NONE', #22063 ) ;
#26287=LINE ( 'NONE', #52877, #42911 ) ;
#26289=CIRCLE ( 'NONE', #57409, 1.250000000000000000 ) ;
#26293=CARTESIAN_POINT ( 'NONE',  ( -9.841120606706802221, -24.83627250047061352, -8.121699444506939258 ) ) ;
#26294=CARTESIAN_POINT ( 'NONE',  ( 10.85714576078767735, -75.98073128594312209, 4.491944191334621195 ) ) ;
#26298=CARTESIAN_POINT ( 'NONE',  ( 11.31412585176551389, -78.97437522268991472, 3.657762637097759395 ) ) ;
#26299=EDGE_CURVE ( 'NONE', #29230, #11806, #53653, .T. ) ;
#26302=DIRECTION ( 'NONE',  ( -1.000000000000000000, 3.441642669434999888E-11, 0.000000000000000000 ) ) ;
#26305=DIRECTION ( 'NONE',  ( -1.000000000000000000, 0.000000000000000000, 0.000000000000000000 ) ) ;
#26306=ORIENTED_EDGE ( 'NONE', *, *, #57095, .F. ) ;
#26312=CARTESIAN_POINT ( 'NONE',  ( 7.601397897754999633, -23.25000000000000000, -9.369164850722000892 ) ) ;
#26314=EDGE_CURVE ( 'NONE', #49897, #44346, #2460, .T. ) ;
#26317=DIRECTION ( 'NONE',  ( 0.000000000000000000, 1.000000000000000000, 0.000000000000000000 ) ) ;
#26318=DIRECTION ( 'NONE',  ( 0.7071067811865474617, 0.000000000000000000, -0.7071067811865474617 ) ) ;
#26319=FACE_OUTER_BOUND ( 'NONE', #37669, .T. ) ;
#26323=VECTOR ( 'NONE', #36119, 1000.000000000000114 ) ;
#26324=EDGE_LOOP ( 'NONE', ( #5358, #20678, #18332, #239, #18320 ) ) ;
#26325=CARTESIAN_POINT ( 'NONE',  ( 11.81418954875000082, -78.82361295229000575, 3.289986436736999753 ) ) ;
#26326=ORIENTED_EDGE ( 'NONE', *, *, #23149, .T. ) ;
#26327=CARTESIAN_POINT ( 'NONE',  ( 10.15323304112999914, -24.23079616014999971, 7.760925857005999795 ) ) ;
#26328=VECTOR ( 'NONE', #27574, 1000.000000000000000 ) ;
#26329=CARTESIAN_POINT ( 'NONE',  ( -10.45204383622999877, -22.76256649475000060, 7.651147548059999970 ) ) ;
#26332=EDGE_LOOP ( 'NONE', ( #40200, #8037, #57833, #47208 ) ) ;
#26333=ORIENTED_EDGE ( 'NONE', *, *, #27126, .F. ) ;
#26337=CARTESIAN_POINT ( 'NONE',  ( -2.468957475121000389, -76.22189569223999683, 12.56811386993000035 ) ) ;
#26338=CARTESIAN_POINT ( 'NONE',  ( 3.250000000000001332, -2.240126334641624695, -0.4032474491995221011 ) ) ;
#26339=DIRECTION ( 'NONE',  ( -0.9957542233908834861, -0.04890176544943922177, 0.07798810124080873818 ) ) ;
#26341=DIRECTION ( 'NONE',  ( 1.000000000000000000, 0.000000000000000000, 0.000000000000000000 ) ) ;
#26343=DIRECTION ( 'NONE',  ( -0.9999476293090542312, 0.000000000000000000, -0.01023418971888952027 ) ) ;
#26345=ORIENTED_EDGE ( 'NONE', *, *, #1866, .F. ) ;
#26348=CARTESIAN_POINT ( 'NONE',  ( -8.284626357322000700, -53.75139346809000074, 9.778502130833000905 ) ) ;
#26349=CARTESIAN_POINT ( 'NONE',  ( 12.76303204291999904, -55.53514849259999409, 1.980584515756000030 ) ) ;
#26350=CARTESIAN_POINT ( 'NONE',  ( -9.778561352719998823, -16.95143577368999743, -8.284566532398999428 ) ) ;
#26351=DIRECTION ( 'NONE',  ( 0.6489586447440038874, 0.04890182322783028640, -0.7592504784964048126 ) ) ;
#26353=CYLINDRICAL_SURFACE ( 'NONE', #37377, 3.250000000000000000 ) ;
#26357=CARTESIAN_POINT ( 'NONE',  ( -2.839805762151343949, -1.958333333333333259, 1.636761686205411737 ) ) ;
#26359=CARTESIAN_POINT ( 'NONE',  ( -8.768124086712999699, -55.64999999965999677, -7.919595949288999570 ) ) ;
#26360=DIRECTION ( 'NONE',  ( 1.000000000000000000, 0.000000000000000000, 0.000000000000000000 ) ) ;
#26361=CARTESIAN_POINT ( 'NONE',  ( -12.53241208773999915, -22.76462890193000277, 1.667936697358999965 ) ) ;
#26363=CARTESIAN_POINT ( 'NONE',  ( 0.2795141487000000202, -3.262566639609999708, -3.635069219502999882 ) ) ;
#26365=CIRCLE ( 'NONE', #41472, 30.49999999999998934 ) ;
#26366=CARTESIAN_POINT ( 'NONE',  ( -0.8506806241676574398, -1.604166666666666519, -3.165411199172027068 ) ) ;
#26367=CARTESIAN_POINT ( 'NONE',  ( 0.000000000000000000, -2.949999999935999817, 0.000000000000000000 ) ) ;
#26368=CARTESIAN_POINT ( 'NONE',  ( -2.061649843245999758, -60.00561307554999502, 12.83797346717000210 ) ) ;
#26369=CARTESIAN_POINT ( 'NONE',  ( 12.48375942317000131, -18.62730665102000316, 1.669542353227000175 ) ) ;
#26373=DIRECTION ( 'NONE',  ( -0.7071067811865475727, 0.000000000000000000, -0.7071067811865475727 ) ) ;
#26379=CARTESIAN_POINT ( 'NONE',  ( -12.54673349189000042, -61.62806887777999520, 0.9076721992840999231 ) ) ;
#26381=CARTESIAN_POINT ( 'NONE',  ( -12.50680023853919565, -24.30414033429957499, -1.424451025645344426 ) ) ;
#26382=CARTESIAN_POINT ( 'NONE',  ( 9.339517261602930276, -75.80000000000001137, 7.561296970547564555 ) ) ;
#26385=CARTESIAN_POINT ( 'NONE',  ( -0.2494208061606092153, -61.79288960742086800, 12.50614183116564604 ) ) ;
#26387=DIRECTION ( 'NONE',  ( -1.000000000000000000, 0.000000000000000000, 0.000000000000000000 ) ) ;
#26389=ORIENTED_EDGE ( 'NONE', *, *, #12414, .F. ) ;
#26391=ORIENTED_EDGE ( 'NONE', *, *, #21785, .F. ) ;
#26392=CARTESIAN_POINT ( 'NONE',  ( -2.099388381696000023E-14, -0.04999999937965000224, 0.000000000000000000 ) ) ;
#26398=CARTESIAN_POINT ( 'NONE',  ( 1.632307027708999936, -23.66927189556999878, -12.46200249212000166 ) ) ;
#26402=CARTESIAN_POINT ( 'NONE',  ( -9.546819346421999697, -24.68527546640000025, 8.130850183241999929 ) ) ;
#26403=CARTESIAN_POINT ( 'NONE',  ( -5.574502783093999270, -79.09338212571999804, -11.02980955859000112 ) ) ;
#26405=CARTESIAN_POINT ( 'NONE',  ( 12.80088938717999980, -56.03743348177000172, -1.980532758767000301 ) ) ;
#26406=DIRECTION ( 'NONE',  ( 0.000000000000000000, -1.000000000000000000, 0.000000000000000000 ) ) ;
#26408=CIRCLE ( 'NONE', #31117, 14.00000000000000000 ) ;
#26410=AXIS2_PLACEMENT_3D ( 'NONE', #22553, #28128, #13685 ) ;
#26413=CARTESIAN_POINT ( 'NONE',  ( 12.60698020661999941, -78.23342962590999150, -3.609717992041000301 ) ) ;
#26414=CARTESIAN_POINT ( 'NONE',  ( 5.552077009241000560, -78.08319635864999952, 11.35743496097000005 ) ) ;
#26419=CARTESIAN_POINT ( 'NONE',  ( -10.07719973192999952, -58.54888345776999614, 7.718346056099999686 ) ) ;
#26420=CARTESIAN_POINT ( 'NONE',  ( 1.173288415578912947, -2.946837913471963333, 3.030131958616116172 ) ) ;
#26424=CARTESIAN_POINT ( 'NONE',  ( 2.234646451474000095, -2.573064556719999896, 3.080979982494000069 ) ) ;
#26426=ORIENTED_EDGE ( 'NONE', *, *, #23368, .F. ) ;
#26433=CARTESIAN_POINT ( 'NONE',  ( 7.349802007153999561, -77.65542860837000205, -10.73869877321999944 ) ) ;
#26434=CARTESIAN_POINT ( 'NONE',  ( -7.635227771907816319, -60.56609606928231671, -10.36745004612171783 ) ) ;
#26435=CARTESIAN_POINT ( 'NONE',  ( 6.173289772713999923, -76.32831948348000140, 10.88346660266000221 ) ) ;
#26439=CARTESIAN_POINT ( 'NONE',  ( -1.667961445601999992, -21.74800977511999989, -12.58338334669999981 ) ) ;
#26440=AXIS2_PLACEMENT_3D ( 'NONE', #18047, #54356, #49638 ) ;
#26443=CARTESIAN_POINT ( 'NONE',  ( -1.931086388578000079, -55.50221245779999890, -12.71798269383000068 ) ) ;
#26450=VERTEX_POINT ( 'NONE', #37399 ) ;
#26451=ORIENTED_EDGE ( 'NONE', *, *, #16660, .T. ) ;
#26453=CARTESIAN_POINT ( 'NONE',  ( 12.49168451095999899, -55.50151115525000023, 1.667916687331000070 ) ) ;
#26462=CARTESIAN_POINT ( 'NONE',  ( 10.07627163191000008, -55.55000000278000272, 7.601397897754999633 ) ) ;
#26463=ORIENTED_EDGE ( 'NONE', *, *, #44940, .T. ) ;
#26469=CYLINDRICAL_SURFACE ( 'NONE', #44369, 1.750000000000000000 ) ;
#26470=CARTESIAN_POINT ( 'NONE',  ( 0.4820079653519915852, -18.48385402702554359, 10.98957811953277641 ) ) ;
#26471=CARTESIAN_POINT ( 'NONE',  ( 11.67645908292204382, -77.43648248267068368, -1.539101508411103492 ) ) ;
#26472=CARTESIAN_POINT ( 'NONE',  ( 13.98934701867000108, -46.22186981632000169, 1.420930503148999987E-05 ) ) ;
#26473=CARTESIAN_POINT ( 'NONE',  ( 7.612971540294999784, -60.12452273675999947, -10.53003236235000095 ) ) ;
#26475=CARTESIAN_POINT ( 'NONE',  ( -10.01752098897000032, -23.19172009652000099, 7.660412494176999765 ) ) ;
#26482=CARTESIAN_POINT ( 'NONE',  ( 10.42531124905999995, -18.73514851523999880, -7.624341765453999997 ) ) ;
#26483=CARTESIAN_POINT ( 'NONE',  ( -1.667269374596999976, -23.20939883484999910, 12.49858097730999873 ) ) ;
#26486=CARTESIAN_POINT ( 'NONE',  ( 2.821058886968999868, -1.193281426753999952, 2.773385340853000258 ) ) ;
#26487=CARTESIAN_POINT ( 'NONE',  ( 7.624341766629000539, -55.53514853726999689, -10.42531125022999916 ) ) ;
#26489=CARTESIAN_POINT ( 'NONE',  ( 12.48375848566000101, -60.17270426026000507, -1.669543623995999981 ) ) ;
#26490=LINE ( 'NONE', #22068, #31578 ) ;
#26491=CARTESIAN_POINT ( 'NONE',  ( -12.99510751537000353, -15.69705297113999443, -6.911973076623003642 ) ) ;
#26495=CARTESIAN_POINT ( 'NONE',  ( -12.57042253521000141, -26.10094976978000147, 0.000000000000000000 ) ) ;
#26499=VERTEX_POINT ( 'NONE', #12005 ) ;
#26500=CARTESIAN_POINT ( 'NONE',  ( -10.38645071870000081, -19.22180874373999870, -7.655542440091000600 ) ) ;
#26504=CARTESIAN_POINT ( 'NONE',  ( 8.343860018000999190, -60.54999999966955926, 8.343860018000999190 ) ) ;
#26505=CARTESIAN_POINT ( 'NONE',  ( -1.267719250440999978, -1.620138932810000210, 3.650372561581000319 ) ) ;
#26507=LINE ( 'NONE', #44836, #17317 ) ;
#26508=CARTESIAN_POINT ( 'NONE',  ( -9.722718241315000398, -23.25000000000000000, 7.954951288349001004 ) ) ;
#26510=CARTESIAN_POINT ( 'NONE',  ( 0.000000000000000000, -23.15000000000000213, -12.00000000000000000 ) ) ;
#26511=CARTESIAN_POINT ( 'NONE',  ( 9.431008681916170033, -24.80059307779984579, -8.251849286024803831 ) ) ;
#26513=CARTESIAN_POINT ( 'NONE',  ( 0.000000000000000000, -18.75000000000000000, 12.50000000000000000 ) ) ;
#26515=ADVANCED_FACE ( 'NONE', ( #56585 ), #1296, .F. ) ;
#26517=VERTEX_POINT ( 'NONE', #21140 ) ;
#26518=DIRECTION ( 'NONE',  ( -1.000000000000000000, 0.000000000000000000, 0.000000000000000000 ) ) ;
#26520=CARTESIAN_POINT ( 'NONE',  ( 8.441176280282578048, -61.71652561705573703, -9.243148036168024717 ) ) ;
#26521=CARTESIAN_POINT ( 'NONE',  ( 0.4254240051736215000, -1.135416666666666963, -3.250000000000000000 ) ) ;
#26522=ORIENTED_EDGE ( 'NONE', *, *, #29814, .T. ) ;
#26524=CARTESIAN_POINT ( 'NONE',  ( -12.92181194095999963, -58.55648180022999583, 2.062502994258999856 ) ) ;
#26525=CARTESIAN_POINT ( 'NONE',  ( -7.760941378042000238, -54.56914109158999793, -10.15321372494000052 ) ) ;
#26526=EDGE_CURVE ( 'NONE', #23631, #15888, #52735, .T. ) ;
#26528=VERTEX_POINT ( 'NONE', #2856 ) ;
#26529=EDGE_LOOP ( 'NONE', ( #18008, #45522, #1433 ) ) ;
#26531=DIRECTION ( 'NONE',  ( 0.000000000000000000, 0.000000000000000000, 1.000000000000000000 ) ) ;
#26534=FACE_OUTER_BOUND ( 'NONE', #51677, .T. ) ;
#26537=CARTESIAN_POINT ( 'NONE',  ( 12.60698020661999941, -78.22218707672999471, -3.609717992041000301 ) ) ;
#26539=CARTESIAN_POINT ( 'NONE',  ( 12.00000000000000000, -18.75000000000000000, 0.000000000000000000 ) ) ;
#26542=ADVANCED_FACE ( 'NONE', ( #11432 ), #6702, .F. ) ;
#26544=CARTESIAN_POINT ( 'NONE',  ( 10.20679554289463731, -17.76427274283123481, 7.770327721672145138 ) ) ;
#26545=ORIENTED_EDGE ( 'NONE', *, *, #15903, .F. ) ;
#26547=CARTESIAN_POINT ( 'NONE',  ( -9.662446363796000526, -76.49882503999000960, 7.627099640079999965 ) ) ;
#26549=CARTESIAN_POINT ( 'NONE',  ( -2.818391366050096991, -2.902451986714001286, -2.210571898668216129 ) ) ;
#26550=CARTESIAN_POINT ( 'NONE',  ( -7.792421629684946005, -17.70899070367055472, 10.18245656324600290 ) ) ;
#26555=DIRECTION ( 'NONE',  ( 0.000000000000000000, 0.000000000000000000, 1.000000000000000000 ) ) ;
#26558=VERTEX_POINT ( 'NONE', #42722 ) ;
#26560=DIRECTION ( 'NONE',  ( 0.000000000000000000, -1.000000000000000000, 0.000000000000000000 ) ) ;
#26561=CARTESIAN_POINT ( 'NONE',  ( 7.710118476714000302, -58.54977139529999164, -10.18499221086999995 ) ) ;
#26569=CARTESIAN_POINT ( 'NONE',  ( -1.930638663168000146, -55.57877936677999742, -12.72375916870000090 ) ) ;
#26570=CARTESIAN_POINT ( 'NONE',  ( 11.54042753142849520, -75.96480956287521735, 2.208758157258925436 ) ) ;
#26572=ORIENTED_EDGE ( 'NONE', *, *, #26789, .F. ) ;
#26579=CARTESIAN_POINT ( 'NONE',  ( -1.308715794677037136, -17.25595500803412463, 12.70256747357091598 ) ) ;
#26581=CARTESIAN_POINT ( 'NONE',  ( 3.137847802567000688, -78.55121997915446741, 11.32185723005353495 ) ) ;
#26588=EDGE_CURVE ( 'NONE', #46129, #18440, #56298, .T. ) ;
#26590=CARTESIAN_POINT ( 'NONE',  ( -1.750000000000000000, -55.55000000278000272, -12.50000000000000000 ) ) ;
#26591=CARTESIAN_POINT ( 'NONE',  ( -10.98965142020557373, -23.51557447649329191, 0.4775239249278388498 ) ) ;
#26593=ORIENTED_EDGE ( 'NONE', *, *, #40509, .T. ) ;
#26594=CARTESIAN_POINT ( 'NONE',  ( -12.76303204294999993, -23.26485150694999859, 1.980584515756000030 ) ) ;
#26595=CARTESIAN_POINT ( 'NONE',  ( -12.70451647739338696, -61.35458569071866464, -1.498866844003992060 ) ) ;
#26597=DIRECTION ( 'NONE',  ( -0.7071067811865475727, 0.000000000000000000, -0.7071067811865475727 ) ) ;
#26599=ORIENTED_EDGE ( 'NONE', *, *, #17890, .T. ) ;
#26600=CARTESIAN_POINT ( 'NONE',  ( 1.001315002179000047, -24.68522411714000242, -12.50000000000000000 ) ) ;
#26602=CARTESIAN_POINT ( 'NONE',  ( -5.950798862880000151, -78.96731654267000522, 10.72320280238000123 ) ) ;
#26603=EDGE_LOOP ( 'NONE', ( #27928, #46600, #54299, #38756 ) ) ;
#26604=CARTESIAN_POINT ( 'NONE',  ( 10.30458248778999852, -23.76332651811999952, 7.636263891322999875 ) ) ;
#26613=ORIENTED_EDGE ( 'NONE', *, *, #41744, .T. ) ;
#26614=ORIENTED_EDGE ( 'NONE', *, *, #48689, .T. ) ;
#26619=CIRCLE ( 'NONE', #39818, 8.500000000000000000 ) ;
#26620=CARTESIAN_POINT ( 'NONE',  ( 11.22440497532000059, -76.55645138378999093, -3.648307665617999795 ) ) ;
#26622=CARTESIAN_POINT ( 'NONE',  ( 7.624341766629000539, -55.53514853726999689, -10.42531125022999916 ) ) ;
#26625=CARTESIAN_POINT ( 'NONE',  ( 12.57433760367000097, -18.28878254117000068, -1.760777649351999985 ) ) ;
#26626=CARTESIAN_POINT ( 'NONE',  ( -10.01749676170999948, -23.19181054693000021, -7.660430254659999605 ) ) ;
#26627=CARTESIAN_POINT ( 'NONE',  ( -10.82077207570563537, -76.66777856290951831, 4.579176815933520217 ) ) ;
#26630=CARTESIAN_POINT ( 'NONE',  ( -7.756275637014999447, -54.57995361804000112, 10.15825999914999933 ) ) ;
#26633=ADVANCED_FACE ( 'NONE', ( #37338 ), #20490, .F. ) ;
#26634=CARTESIAN_POINT ( 'NONE',  ( -7.765024210423000284, -17.90905971384000139, -9.830784063418001040 ) ) ;
#26636=CARTESIAN_POINT ( 'NONE',  ( -1.930009203935999951, -18.79900967682999635, -12.72537718777000038 ) ) ;
#26637=DIRECTION ( 'NONE',  ( 0.000000000000000000, 0.000000000000000000, -1.000000000000000000 ) ) ;
#26644=CARTESIAN_POINT ( 'NONE',  ( 2.597074403235505535, -1.403616780896163041, 1.995008052711377822 ) ) ;
#26645=CARTESIAN_POINT ( 'NONE',  ( -1.194090706002000069, -54.35968341064000242, 12.43436538485999954 ) ) ;
#26646=CARTESIAN_POINT ( 'NONE',  ( -12.60413670420000010, -23.30716680861999990, 1.799502287691000069 ) ) ;
#26647=CARTESIAN_POINT ( 'NONE',  ( 3.698594611804000287, -2.026219782538000391, -1.432312655390999945 ) ) ;
#26649=AXIS2_PLACEMENT_3D ( 'NONE', #3360, #21355, #39372 ) ;
#26650=CARTESIAN_POINT ( 'NONE',  ( 1.997276839918477265, -1.677083333333332815, -2.598917237794082791 ) ) ;
#26652=CARTESIAN_POINT ( 'NONE',  ( -1.930638663164000235, -60.02122063256000217, 12.72375916875000179 ) ) ;
#26653=CARTESIAN_POINT ( 'NONE',  ( 12.77649795263000065, -16.69168567756999977, -0.06462540730616000983 ) ) ;
#26658=CARTESIAN_POINT ( 'NONE',  ( 10.50279984750154405, -77.24346446326944715, 5.851000335417166909 ) ) ;
#26659=CARTESIAN_POINT ( 'NONE',  ( -5.967760218777000247, -78.67259870393999677, 10.31870413016000043 ) ) ;
#26660=B_SPLINE_SURFACE_WITH_KNOTS ( 'NONE', 3, 3, ( 
 ( #38905, #44794, #58072, #17632 ),
 ( #35621, #4346, #4937, #4650 ),
 ( #22649, #45096, #58370, #45395 ),
 ( #31779, #21760, #26193, #35033 ),
 ( #17334, #54244, #22941, #9367 ),
 ( #4045, #40659, #17932, #49224 ),
 ( #48647, #22346, #12898, #18233 ),
 ( #30613, #35922, #53649, #8773 ) ),
 .UNSPECIFIED., .F., .F., .F.,
 ( 4, 1, 1, 1, 1, 4 ),
 ( 4, 4 ),
 ( -0.01200407347463999970, 0.000000000000000000, 0.3333333333333000081, 0.6666666666667000474, 1.000000000000000000, 1.011997855551999947 ),
 ( -0.3559705542741999906, 1.355970554273999928 ),
 .UNSPECIFIED. ) ;
#26667=CARTESIAN_POINT ( 'NONE',  ( -12.70926857202000093, -60.20841990675999966, 1.933876778424000076 ) ) ;
#26669=DIRECTION ( 'NONE',  ( -0.7071067811865474617, 0.000000000000000000, 0.7071067811865474617 ) ) ;
#26671=AXIS2_PLACEMENT_3D ( 'NONE', #24575, #42301, #20441 ) ;
#26672=B_SPLINE_CURVE_WITH_KNOTS ( 'NONE', 3,
 ( #54189, #31724, #45336, #22884, #40895, #485, #36456, #54483, #32016, #50058 ),
 .UNSPECIFIED., .F., .F.,
 ( 4, 2, 2, 2, 4 ),
 ( 0.000000000000000000, 0.2499999999999998890, 0.5000000000000000000, 0.7500000000000001110, 1.000000000000000000 ),
 .UNSPECIFIED. ) ;
#26673=CARTESIAN_POINT ( 'NONE',  ( 12.00000000000000000, -79.25000000000000000, 1.072514965728000067E-08 ) ) ;
#26677=CARTESIAN_POINT ( 'NONE',  ( 8.178338515874312264, -55.49583131490126675, 7.356278612544881135 ) ) ;
#26678=ORIENTED_EDGE ( 'NONE', *, *, #15989, .F. ) ;
#26681=CARTESIAN_POINT ( 'NONE',  ( -2.616124927519058563, -0.7500000000000001110, 2.353768604702249689 ) ) ;
#26683=FACE_OUTER_BOUND ( 'NONE', #52196, .T. ) ;
#26684=VERTEX_POINT ( 'NONE', #55059 ) ;
#26691=ORIENTED_EDGE ( 'NONE', *, *, #9647, .T. ) ;
#26693=CARTESIAN_POINT ( 'NONE',  ( 2.613357750217999875, -78.77637553137999760, 11.92719643999999946 ) ) ;
#26694=EDGE_CURVE ( 'NONE', #6154, #326, #10033, .T. ) ;
#26695=ORIENTED_EDGE ( 'NONE', *, *, #46100, .F. ) ;
#26696=VERTEX_POINT ( 'NONE', #52384 ) ;
#26699=B_SPLINE_SURFACE_WITH_KNOTS ( 'NONE', 3, 3, ( 
 ( #42172, #51624, #15297, #33291 ),
 ( #6437, #11178, #38019, #6732 ),
 ( #24739, #42754, #2318, #20312 ),
 ( #3456, #30303, #52476, #57473 ),
 ( #47777, #7883, #25884, #2886 ),
 ( #30597, #48067, #20882, #48629 ),
 ( #30882, #30012, #44476, #43617 ),
 ( #3180, #38886, #39469, #26453 ) ),
 .UNSPECIFIED., .F., .F., .F.,
 ( 4, 1, 1, 1, 1, 4 ),
 ( 4, 4 ),
 ( -0.01200407347464999865, 0.000000000000000000, 0.3333333333333000081, 0.6666666666667000474, 1.000000000000000000, 1.011997855551999947 ),
 ( -0.3559705542741999906, 1.355970554273999928 ),
 .UNSPECIFIED. ) ;
#26704=CARTESIAN_POINT ( 'NONE',  ( -10.89021090039136119, -79.10416666669993901, 4.844266348695080993 ) ) ;
#26707=DIRECTION ( 'NONE',  ( 1.000000000000000000, 0.000000000000000000, 0.000000000000000000 ) ) ;
#26708=B_SPLINE_CURVE_WITH_KNOTS ( 'NONE', 3,
 ( #31769, #18797, #13179, #31172, #49213, #4335, #8762, #22337, #40351, #1675, #41809, #6957, #29380, #10823, #28799, #1384, #28206, #33223 ),
 .UNSPECIFIED., .F., .F.,
 ( 4, 2, 2, 2, 2, 2, 2, 2, 4 ),
 ( 0.000000000000000000, 0.06249999999999379663, 0.1249999999999875933, 0.2499999999999862332, 0.4999999999999847899, 0.7499999999999832356, 0.8124999999999849010, 0.8749999999999864553, 1.000000000000000000 ),
 .UNSPECIFIED. ) ;
#26711=DIRECTION ( 'NONE',  ( 1.000000000000000000, 0.000000000000000000, 0.000000000000000000 ) ) ;
#26714=CIRCLE ( 'NONE', #20129, 14.00000000000000000 ) ;
#26715=DIRECTION ( 'NONE',  ( 0.8965517241377957136, -0.4429390544366978988, 5.195107294746977201E-07 ) ) ;
#26718=CARTESIAN_POINT ( 'NONE',  ( -2.707053224964000027, -2.720634141345999790, 2.675433656965999774 ) ) ;
#26720=AXIS2_PLACEMENT_3D ( 'NONE', #20092, #51392, #10948 ) ;
#26722=FACE_OUTER_BOUND ( 'NONE', #58358, .T. ) ;
#26726=CARTESIAN_POINT ( 'NONE',  ( -1.338697082642999803, -78.09946573606998754, -12.94399764267999942 ) ) ;
#26727=ADVANCED_FACE ( 'NONE', ( #28763 ), #25212, .F. ) ;
#26729=CARTESIAN_POINT ( 'NONE',  ( 12.92181194095000052, -21.75648180056000314, -2.062502994258999856 ) ) ;
#26730=ORIENTED_EDGE ( 'NONE', *, *, #50522, .T. ) ;
#26733=CARTESIAN_POINT ( 'NONE',  ( -1.799490220168999954, -22.77129148951999937, -12.64502302235000109 ) ) ;
#26736=CARTESIAN_POINT ( 'NONE',  ( -3.161392481395000065, -1.852626005360999972, -1.501864700490999960 ) ) ;
#26737=CARTESIAN_POINT ( 'NONE',  ( -2.062670899361999766, -55.49360215019999742, -12.83044027758000105 ) ) ;
#26739=VERTEX_POINT ( 'NONE', #38503 ) ;
#26743=EDGE_LOOP ( 'NONE', ( #5857, #47786, #28311, #27116 ) ) ;
#26749=EDGE_LOOP ( 'NONE', ( #34729, #43322, #10893, #7537, #57991 ) ) ;
#26752=ORIENTED_EDGE ( 'NONE', *, *, #15874, .T. ) ;
#26753=VERTEX_POINT ( 'NONE', #10784 ) ;
#26754=CARTESIAN_POINT ( 'NONE',  ( -2.982898973896713102, -2.633265934789509544, -1.289165251780844512 ) ) ;
#26755=CARTESIAN_POINT ( 'NONE',  ( 9.722718241315000398, -18.75000000000000000, -7.954951288349001004 ) ) ;
#26760=EDGE_CURVE ( 'NONE', #26528, #36311, #16078, .T. ) ;
#26761=EDGE_LOOP ( 'NONE', ( #14204, #14344, #6314, #17695 ) ) ;
#26764=FACE_OUTER_BOUND ( 'NONE', #23080, .T. ) ;
#26765=CARTESIAN_POINT ( 'NONE',  ( 0.5999999999999999778, -18.84999999999999787, 10.98362417419999915 ) ) ;
#26767=CARTESIAN_POINT ( 'NONE',  ( 14.00000000000000000, -46.13782243168999742, 5.544480867911000210E-06 ) ) ;
#26769=CARTESIAN_POINT ( 'NONE',  ( 7.654537085013999764, -55.51943307300000185, -10.01332844635999919 ) ) ;
#26771=CARTESIAN_POINT ( 'NONE',  ( -10.08161778466999969, -24.71855282893000094, 7.981584069265998949 ) ) ;
#26776=CARTESIAN_POINT ( 'NONE',  ( -12.77651047532000028, -16.69104280938000073, -0.04320343284645000032 ) ) ;
#26777=CARTESIAN_POINT ( 'NONE',  ( 0.000000000000000000, -0.09999999995300053179, 0.000000000000000000 ) ) ;
#26778=CARTESIAN_POINT ( 'NONE',  ( -2.061649843245999758, -23.20561307587000144, 12.83797346714000120 ) ) ;
#26780=DIRECTION ( 'NONE',  ( -0.7071067811865474617, 0.000000000000000000, 0.7071067811865474617 ) ) ;
#26781=CARTESIAN_POINT ( 'NONE',  ( -1.113858406170999960, -0.8703954782496999831, 3.266031882984000045 ) ) ;
#26782=CARTESIAN_POINT ( 'NONE',  ( 0.000000000000000000, -39.30476017083000073, 0.000000000000000000 ) ) ;
#26783=CIRCLE ( 'NONE', #1375, 0.5000000000000006661 ) ;
#26785=CARTESIAN_POINT ( 'NONE',  ( 12.68624828431999951, -60.56426635971000394, -1.886933512377000133 ) ) ;
#26787=DIRECTION ( 'NONE',  ( 0.7592504788685918715, -0.04890177849870949028, 0.6489586476790929481 ) ) ;
#26789=EDGE_CURVE ( 'NONE', #48346, #26170, #37918, .T. ) ;
#26792=CARTESIAN_POINT ( 'NONE',  ( -10.20000000000000107, -0.2000000000000000111, 0.000000000000000000 ) ) ;
#26796=EDGE_CURVE ( 'NONE', #23377, #29770, #7860, .T. ) ;
#26798=DIRECTION ( 'NONE',  ( -0.9859154929576978699, -0.1672442547472993701, -2.241745476049995391E-11 ) ) ;
#26800=LINE ( 'NONE', #54282, #20948 ) ;
#26805=CARTESIAN_POINT ( 'NONE',  ( 2.970509141730999669, -1.114596044169000155, 2.718337110757000019 ) ) ;
#26806=CARTESIAN_POINT ( 'NONE',  ( -10.10989699479836723, -76.34329898052499175, -6.122700102344563078 ) ) ;
#26807=DIRECTION ( 'NONE',  ( -0.7026410690473252618, 0.1122098755728027641, 0.7026410690473252618 ) ) ;
#26808=CARTESIAN_POINT ( 'NONE',  ( -1.667917367065999912, -55.51943464808999806, 12.49306764013999960 ) ) ;
#26812=CARTESIAN_POINT ( 'NONE',  ( -12.56594317984999876, -18.75000000536999778, 1.750000000000000000 ) ) ;
#26814=CARTESIAN_POINT ( 'NONE',  ( -12.80896991324999945, -58.55453807205000061, -1.930989179114000143 ) ) ;
#26818=CYLINDRICAL_SURFACE ( 'NONE', #30372, 0.5000000000000004441 ) ;
#26822=CARTESIAN_POINT ( 'NONE',  ( -9.523369619434999933, -53.98054357652999613, -8.220347091585999522 ) ) ;
#26823=AXIS2_PLACEMENT_3D ( 'NONE', #51836, #11391, #2527 ) ;
#26826=ORIENTED_EDGE ( 'NONE', *, *, #48303, .T. ) ;
#26833=CARTESIAN_POINT ( 'NONE',  ( 12.50240633877000107, -17.31762602171999887, 1.005381409788000058 ) ) ;
#26836=CARTESIAN_POINT ( 'NONE',  ( 6.944463141141999252, -76.66805712980000465, -9.899892744310998083 ) ) ;
#26838=CARTESIAN_POINT ( 'NONE',  ( 8.096452064242996016, -22.78578169018999944, 13.15643568217000769 ) ) ;
#26843=ORIENTED_EDGE ( 'NONE', *, *, #2566, .F. ) ;
#26845=CARTESIAN_POINT ( 'NONE',  ( -10.62397638184999948, -76.09413970748998679, -6.218250916117999516 ) ) ;
#26848=CARTESIAN_POINT ( 'NONE',  ( 3.349726343964253061, -3.124127367323429993, 1.080338306304951201 ) ) ;
#26849=EDGE_CURVE ( 'NONE', #22110, #37067, #24146, .T. ) ;
#26852=CARTESIAN_POINT ( 'NONE',  ( -9.102117851653074965, -61.77186524101082910, -8.583692175771709287 ) ) ;
#26855=CARTESIAN_POINT ( 'NONE',  ( -5.469229351563153152, -76.96241952032323752, 10.75691535272135191 ) ) ;
#26857=CARTESIAN_POINT ( 'NONE',  ( -2.176888680478372251, -76.06416033132352084, -12.84412808549582685 ) ) ;
#26858=CIRCLE ( 'NONE', #7073, 1.749999999999999556 ) ;
#26859=CYLINDRICAL_SURFACE ( 'NONE', #37549, 14.00000000000000000 ) ;
#26860=VERTEX_POINT ( 'NONE', #41998 ) ;
#26862=AXIS2_PLACEMENT_3D ( 'NONE', #56066, #20622, #15611 ) ;
#26864=LINE ( 'NONE', #40749, #12551 ) ;
#26870=CARTESIAN_POINT ( 'NONE',  ( -1.930009203937000040, -55.59900967650000325, -12.72537718775000037 ) ) ;
#26871=CARTESIAN_POINT ( 'NONE',  ( 8.992038628173702364, -76.00517836237398228, 7.564405201256904299 ) ) ;
#26873=DIRECTION ( 'NONE',  ( 0.000000000000000000, 0.000000000000000000, 1.000000000000000000 ) ) ;
#26874=EDGE_LOOP ( 'NONE', ( #34802, #18795, #48002, #21167 ) ) ;
#26875=ADVANCED_FACE ( 'NONE', ( #10716 ), #14728, .T. ) ;
#26878=CIRCLE ( 'NONE', #33458, 0.5000000000000006661 ) ;
#26884=DIRECTION ( 'NONE',  ( 0.000000000000000000, -1.000000000000000000, 1.786847118832000041E-14 ) ) ;
#26889=DIRECTION ( 'NONE',  ( -0.7071067811865474617, 3.444154817369226517E-11, 0.7071067811865474617 ) ) ;
#26891=CARTESIAN_POINT ( 'NONE',  ( 4.529234587808285362, -76.35572474536435550, -10.87075400981678541 ) ) ;
#26896=LINE ( 'NONE', #26594, #16070 ) ;
#26901=VERTEX_POINT ( 'NONE', #52314 ) ;
#26904=ORIENTED_EDGE ( 'NONE', *, *, #29814, .F. ) ;
#26906=ORIENTED_EDGE ( 'NONE', *, *, #51975, .T. ) ;
#26907=CARTESIAN_POINT ( 'NONE',  ( 9.205846894750999709, -25.00798911347999720, 8.541134278086001785 ) ) ;
#26908=CARTESIAN_POINT ( 'NONE',  ( 7.553727747526362890, -55.11418618783646650, -7.997114030208058111 ) ) ;
#26913=ORIENTED_EDGE ( 'NONE', *, *, #39082, .T. ) ;
#26919=CARTESIAN_POINT ( 'NONE',  ( -1.848949294450000114, -76.44493281993999290, -12.67465850452999909 ) ) ;
#26924=CARTESIAN_POINT ( 'NONE',  ( 12.66322081671000177, -16.81838367322000138, -0.1487102037789999887 ) ) ;
#26925=CARTESIAN_POINT ( 'NONE',  ( -10.53559655517000060, -23.20569178316999981, -7.620036226160999959 ) ) ;
#26933=CARTESIAN_POINT ( 'NONE',  ( 2.839805762151335511, -3.291666666666666963, 1.636761686205429278 ) ) ;
#26934=FACE_OUTER_BOUND ( 'NONE', #52189, .T. ) ;
#26941=B_SPLINE_CURVE_WITH_KNOTS ( 'NONE', 3,
 ( #19981, #33536, #50699, #23807, #37680, #1688, #33238, #19678, #55696, #51282 ),
 .UNSPECIFIED., .F., .F.,
 ( 4, 2, 2, 2, 4 ),
 ( 0.000000000000000000, 0.2500000000000001110, 0.5000000000000002220, 0.7500000000000001110, 1.000000000000000000 ),
 .UNSPECIFIED. ) ;
#26943=EDGE_CURVE ( 'NONE', #14108, #13029, #620, .T. ) ;
#26944=CARTESIAN_POINT ( 'NONE',  ( -0.9781264271459999549, -53.85968856090000401, 12.65967462873999949 ) ) ;
#26946=CARTESIAN_POINT ( 'NONE',  ( 3.961774695119000267, -3.559381257025999723, 0.1872869280730999897 ) ) ;
#26950=CARTESIAN_POINT ( 'NONE',  ( -1.295048492659000017, -61.32893519093000378, 12.54716442239999985 ) ) ;
#26951=CARTESIAN_POINT ( 'NONE',  ( 12.54976795933000133, -16.95224500006000312, -0.05636009750358999398 ) ) ;
#26952=CIRCLE ( 'NONE', #57138, 0.8000000000000011546 ) ;
#26956=CARTESIAN_POINT ( 'NONE',  ( 11.52046713918511678, -76.67862562347951894, -3.639311417233032309 ) ) ;
#26957=CARTESIAN_POINT ( 'NONE',  ( -1.784936172681000022, -79.28226414830000124, -12.51137403398999837 ) ) ;
#26958=EDGE_CURVE ( 'NONE', #13118, #30023, #29848, .T. ) ;
#26962=CARTESIAN_POINT ( 'NONE',  ( -1.003693376006966176, -61.76223992080762315, 12.70247752668375085 ) ) ;
#26964=CARTESIAN_POINT ( 'NONE',  ( -12.54705830253000087, -61.33699017322999936, 1.287129557046000183 ) ) ;
#26971=CARTESIAN_POINT ( 'NONE',  ( 7.387512494710292366, -55.38467666605775008, 8.150146600852341550 ) ) ;
#26972=ORIENTED_EDGE ( 'NONE', *, *, #3651, .F. ) ;
#26974=CARTESIAN_POINT ( 'NONE',  ( -12.05000000000000071, -80.60000000000000853, 0.000000000000000000 ) ) ;
#26976=ORIENTED_EDGE ( 'NONE', *, *, #13474, .F. ) ;
#26979=DIRECTION ( 'NONE',  ( 0.000000000000000000, 0.000000000000000000, -1.000000000000000000 ) ) ;
#26983=CARTESIAN_POINT ( 'NONE',  ( 1.466594960159999905, -24.08158199052000015, -12.44238958332999800 ) ) ;
#26987=CARTESIAN_POINT ( 'NONE',  ( 0.4463049390680999817, -78.54644978676999756, -12.20198613296999923 ) ) ;
#26988=ORIENTED_EDGE ( 'NONE', *, *, #46678, .T. ) ;
#26989=EDGE_LOOP ( 'NONE', ( #6853, #12878, #15004, #14712, #54206, #48450 ) ) ;
#26990=LINE ( 'NONE', #45025, #19742 ) ;
#26991=CARTESIAN_POINT ( 'NONE',  ( -12.50000000000000000, -17.31762331506999786, -1.005384022379999909 ) ) ;
#26992=VECTOR ( 'NONE', #19569, 1000.000000000000000 ) ;
#26999=CARTESIAN_POINT ( 'NONE',  ( 7.317687889309999250, -77.59130236656999102, -10.69177725920999933 ) ) ;
#27004=DIRECTION ( 'NONE',  ( 0.000000000000000000, -1.000000000000000000, 0.000000000000000000 ) ) ;
#27007=CARTESIAN_POINT ( 'NONE',  ( -10.18589234707000202, -55.51082434643999619, 7.641012386020999969 ) ) ;
#27008=CARTESIAN_POINT ( 'NONE',  ( 12.00000000000000000, 0.000000000000000000, 0.000000000000000000 ) ) ;
#27011=CARTESIAN_POINT ( 'NONE',  ( -12.00000000000000000, -23.15000000002000036, -0.7999999999999001243 ) ) ;
#27013=CARTESIAN_POINT ( 'NONE',  ( -3.054513261463999818, -2.902870392637999952, -2.270689576097000284 ) ) ;
#27016=CARTESIAN_POINT ( 'NONE',  ( -0.5962167095188449784, -23.22841244209519473, 10.98383273456533260 ) ) ;
#27017=EDGE_CURVE ( 'NONE', #19308, #54154, #29701, .T. ) ;
#27020=CARTESIAN_POINT ( 'NONE',  ( -12.77651065923999951, -16.69103388611000227, 0.04307580168117999125 ) ) ;
#27021=CARTESIAN_POINT ( 'NONE',  ( 5.715297388934000189, -78.32148429990999716, 11.69132169264999987 ) ) ;
#27022=CARTESIAN_POINT ( 'NONE',  ( -7.770369683918966430, -61.03583903303037772, -10.20674856005918940 ) ) ;
#27023=CARTESIAN_POINT ( 'NONE',  ( 12.71658872085999903, -18.68415268018999953, -1.931087888240000217 ) ) ;
#27024=EDGE_LOOP ( 'NONE', ( #44058, #32565, #4860, #40946, #30894, #53946 ) ) ;
#27026=EDGE_CURVE ( 'NONE', #8613, #17621, #39790, .T. ) ;
#27031=CARTESIAN_POINT ( 'NONE',  ( -1.180494763713999973, -0.7191883867189999835, 3.461421590595000097 ) ) ;
#27032=CARTESIAN_POINT ( 'NONE',  ( -1.799502287743000029, -55.49283065365000311, -12.60413652829999975 ) ) ;
#27034=EDGE_LOOP ( 'NONE', ( #45024, #53405, #6006, #51945, #11456 ) ) ;
#27036=FACE_OUTER_BOUND ( 'NONE', #33750, .T. ) ;
#27037=EDGE_LOOP ( 'NONE', ( #56122, #23647, #51456, #21980 ) ) ;
#27045=AXIS2_PLACEMENT_3D ( 'NONE', #55962, #6653, #37062 ) ;
#27046=EDGE_CURVE ( 'NONE', #44555, #47200, #26952, .T. ) ;
#27049=CARTESIAN_POINT ( 'NONE',  ( -3.000189226121413810, -2.632099266311925145, -1.248401069550000297 ) ) ;
#27051=CARTESIAN_POINT ( 'NONE',  ( -0.7832439075705196485, -1.738450387085815896, 3.943800212226620694 ) ) ;
#27057=EDGE_CURVE ( 'NONE', #33164, #38869, #12923, .T. ) ;
#27059=CARTESIAN_POINT ( 'NONE',  ( 0.5812841321856091481, -18.69583131522389507, 10.98463311464191605 ) ) ;
#27060=CARTESIAN_POINT ( 'NONE',  ( 11.79999999999999893, -23.15000000000000213, 0.5999999999999999778 ) ) ;
#27061=LINE ( 'NONE', #50406, #33661 ) ;
#27062=CARTESIAN_POINT ( 'NONE',  ( 7.641012305205999056, -55.51082276539999327, -10.18589226629999978 ) ) ;
#27064=CARTESIAN_POINT ( 'NONE',  ( -9.788011744275999959, -24.52881292764999799, 7.956359616222000497 ) ) ;
#27067=CARTESIAN_POINT ( 'NONE',  ( -11.03276040983153550, -77.98620529984978589, -4.895327290354793526 ) ) ;
#27070=CARTESIAN_POINT ( 'NONE',  ( -12.82229880959000035, -18.57735182838000298, 2.065917129154000165 ) ) ;
#27071=PLANE ( 'NONE',  #49982 ) ;
#27072=CARTESIAN_POINT ( 'NONE',  ( 0.4701041210474999898, -25.00796934423999929, 12.54901038416000070 ) ) ;
#27075=CARTESIAN_POINT ( 'NONE',  ( -0.1236500535340000068, -0.6721180847798000624, 3.590573661457999943 ) ) ;
#27076=EDGE_CURVE ( 'NONE', #25463, #38188, #53091, .T. ) ;
#27078=CARTESIAN_POINT ( 'NONE',  ( 1.405334848747999743, -54.48507051966527115, -12.50716844827338825 ) ) ;
#27082=DIRECTION ( 'NONE',  ( 0.000000000000000000, 0.7071067811866525998, -0.7071067811864425456 ) ) ;
#27084=FACE_OUTER_BOUND ( 'NONE', #35139, .T. ) ;
#27087=DIRECTION ( 'NONE',  ( 2.678911359553000079E-11, 1.000000000000000000, 2.678924269122999951E-11 ) ) ;
#27088=CIRCLE ( 'NONE', #44091, 0.6000000000000008660 ) ;
#27089=CARTESIAN_POINT ( 'NONE',  ( -1.823750004803999641E-14, -80.79999999999999716, 0.000000000000000000 ) ) ;
#27097=PLANE ( 'NONE',  #13439 ) ;
#27099=CARTESIAN_POINT ( 'NONE',  ( -10.08161778468999970, -61.51855282861000518, 7.981584069293999661 ) ) ;
#27101=CARTESIAN_POINT ( 'NONE',  ( 0.7999999999999001243, -23.15000000002000036, -12.00000000000000000 ) ) ;
#27102=CARTESIAN_POINT ( 'NONE',  ( 8.664753834735311244, -76.49051551431000462, -8.038626423221995054 ) ) ;
#27103=CARTESIAN_POINT ( 'NONE',  ( 12.83836862999999973, -23.20626272212999908, -2.062146390630000159 ) ) ;
#27104=CARTESIAN_POINT ( 'NONE',  ( -2.062502994258999856, -57.04351820043999766, 12.92181194098999875 ) ) ;
#27105=ORIENTED_EDGE ( 'NONE', *, *, #12341, .T. ) ;
#27106=CARTESIAN_POINT ( 'NONE',  ( -10.42531124908000173, -60.06485148440999922, -7.624341765471999821 ) ) ;
#27107=CARTESIAN_POINT ( 'NONE',  ( -0.5999999999999999778, -23.15000000000000213, 10.98362417419999915 ) ) ;
#27108=CARTESIAN_POINT ( 'NONE',  ( 12.76303204513999923, -55.53514852210999919, -1.980584515753000208 ) ) ;
#27110=CARTESIAN_POINT ( 'NONE',  ( -12.49306752636999995, -60.08056692637000396, -1.667917367010000040 ) ) ;
#27114=CARTESIAN_POINT ( 'NONE',  ( 2.839805762151339952, -1.208333333333333481, -1.636761686205418176 ) ) ;
#27116=ORIENTED_EDGE ( 'NONE', *, *, #34513, .F. ) ;
#27117=CARTESIAN_POINT ( 'NONE',  ( -10.35410226329999794, -55.39601732791000188, -7.619716344056000068 ) ) ;
#27119=CONICAL_SURFACE ( 'NONE', #1710, 13.94999999959000014, 0.7853981633972997312 ) ;
#27126=EDGE_CURVE ( 'NONE', #53713, #10870, #45831, .T. ) ;
#27127=CIRCLE ( 'NONE', #1718, 1.250000000000000444 ) ;
#27129=CARTESIAN_POINT ( 'NONE',  ( -1.258617752331000039, -77.69871687587999531, -12.89490358089000033 ) ) ;
#27134=FACE_OUTER_BOUND ( 'NONE', #56480, .T. ) ;
#27137=CARTESIAN_POINT ( 'NONE',  ( 11.50190934395000042, -76.77899180865000517, -3.421415122956000143 ) ) ;
#27139=CARTESIAN_POINT ( 'NONE',  ( 0.7248607164131247727, -3.490744342946634937, -3.444725236542351521 ) ) ;
#27140=CARTESIAN_POINT ( 'NONE',  ( 12.83044039274999903, -18.69360374348000065, 2.062670899148999926 ) ) ;
#27144=DIRECTION ( 'NONE',  ( -0.7071067811865475727, 0.000000000000000000, -0.7071067811865475727 ) ) ;
#27146=B_SPLINE_SURFACE_WITH_KNOTS ( 'NONE', 3, 3, ( 
 ( #9996, #40400, #293, #31519, #17972, #40992, #4689, #583, #22687, #40699, #18271, #54286, #5266, #14118, #864, #50155, #9698, #23275, #41280, #47581, #7107, #38395, #24823, #43706, #34525, #57272, #2398, #16545, #25393, #30389, #21543, #3262, #21253, #39549, #39258 ),
 ( #16835, #47861, #52846, #20684, #20398, #57554, #11548, #17115, #35101, #48426, #11828, #53134, #56414, #43989, #51993, #33956, #38971, #25107, #25965, #34818, #12683, #15964, #29525, #52560, #42840, #48148, #29808, #20967, #43133, #3542, #2691, #7390, #7967, #12399, #38683 ),
 ( #56703, #16260, #56983, #43409, #52274, #2967, #34239, #12112, #30675, #30097, #7678, #25679, #48712, #36583, #8545, #54314, #31252, #44271, #27129, #9144, #41020, #36292, #23009, #30960, #49294, #21828, #18593, #4417, #54605, #54017, #17403, #53723, #35387, #13854, #3828 ),
 ( #26836, #53416, #31550, #4118, #31850, #17709, #13261, #612, #45167, #35992, #8845, #44864, #22419, #40431, #13558, #14142, #4717, #32142, #49892, #8258, #48998, #22, #39833, #26257, #18002, #57846, #49597, #12963, #22716, #26537, #9436, #44564, #40729, #22119, #27427 ) ),
 .UNSPECIFIED., .F., .F., .F.,
 ( 4, 4 ),
 ( 4, 1, 1, 1, 1, 1, 1, 1, 1, 1, 1, 1, 1, 1, 1, 1, 1, 1, 1, 1, 1, 1, 1, 1, 1, 1, 1, 1, 1, 1, 1, 1, 4 ),
 ( -0.3708084972814000291, 1.370808497280999960 ),
 ( -0.02000000000000000042, 0.01250000000000000069, 0.04499999999999999833, 0.07749999999999999944, 0.1100000000000000006, 0.1424999999999999878, 0.1749999999999999889, 0.2074999999999999900, 0.2399999999999999911, 0.2725000000000000200, 0.3049999999999999933, 0.3375000000000000222, 0.3699999999999999956, 0.4025000000000000244, 0.4349999999999999978, 0.4675000000000000266, 0.5000000000000000000, 0.5324999999999999734, 0.5649999999999999467, 0.5975000000000000311, 0.6300000000000000044, 0.6624999999999999778, 0.6949999999999999512, 0.7275000000000000355, 0.7600000000000000089, 0.7924999999999999822, 0.8249999999999999556, 0.8575000000000000400, 0.8900000000000000133, 0.9224999999999999867, 0.9549999999999999600, 0.9875000000000000444, 1.020000000000000018 ),
 .UNSPECIFIED. ) ;
#27149=EDGE_CURVE ( 'NONE', #37361, #2615, #3413, .T. ) ;
#27150=FACE_OUTER_BOUND ( 'NONE', #4514, .T. ) ;
#27158=AXIS2_PLACEMENT_3D ( 'NONE', #24343, #48443, #12978 ) ;
#27159=CARTESIAN_POINT ( 'NONE',  ( 1.641871293650414065, -76.06380281422384826, 11.64119219785805193 ) ) ;
#27161=CARTESIAN_POINT ( 'NONE',  ( 12.50000000000000000, -60.04999999657000131, 1.750000000000000000 ) ) ;
#27163=CARTESIAN_POINT ( 'NONE',  ( 3.007117222848000093, -75.90536276733411114, 11.93703523519999443 ) ) ;
#27168=EDGE_CURVE ( 'NONE', #56093, #52467, #52429, .T. ) ;
#27172=ORIENTED_EDGE ( 'NONE', *, *, #28163, .F. ) ;
#27174=CARTESIAN_POINT ( 'NONE',  ( 12.70457850616319284, -53.62128713286528381, 0.5106122238224051202 ) ) ;
#27180=DIRECTION ( 'NONE',  ( 0.000000000000000000, -1.000000000000000000, 0.000000000000000000 ) ) ;
#27182=ADVANCED_FACE ( 'NONE', ( #26216 ), #32632, .F. ) ;
#27184=DIRECTION ( 'NONE',  ( -0.7071067811865475727, 0.000000000000000000, -0.7071067811865475727 ) ) ;
#27186=ORIENTED_EDGE ( 'NONE', *, *, #12994, .T. ) ;
#27187=ORIENTED_EDGE ( 'NONE', *, *, #17867, .T. ) ;
#27192=ORIENTED_EDGE ( 'NONE', *, *, #42497, .T. ) ;
#27193=LINE ( 'NONE', #31033, #42461 ) ;
#27194=EDGE_CURVE ( 'NONE', #42621, #22170, #6227, .T. ) ;
#27196=VECTOR ( 'NONE', #56012, 1000.000000000000000 ) ;
#27198=DIRECTION ( 'NONE',  ( -1.000000000000000000, 0.000000000000000000, 0.000000000000000000 ) ) ;
#27203=VERTEX_POINT ( 'NONE', #9982 ) ;
#27205=VERTEX_POINT ( 'NONE', #9396 ) ;
#27210=CARTESIAN_POINT ( 'NONE',  ( 6.368865985159000154, -76.34029810977999375, 11.47429970984000036 ) ) ;
#27211=CIRCLE ( 'NONE', #22507, 30.49999999999999289 ) ;
#27214=DIRECTION ( 'NONE',  ( -1.000000000000000000, 0.000000000000000000, 0.000000000000000000 ) ) ;
#27217=CARTESIAN_POINT ( 'NONE',  ( -11.52225979636347653, -76.68411619956043523, 2.301538105231448306 ) ) ;
#27225=CARTESIAN_POINT ( 'NONE',  ( -12.70305380117054916, -61.83154493736395096, 0.8725910144712079042 ) ) ;
#27226=CARTESIAN_POINT ( 'NONE',  ( -11.75000000000000355, -78.31041666666666856, -1.538071403320004249 ) ) ;
#27228=DIRECTION ( 'NONE',  ( -1.000000000000000000, 0.000000000000000000, 0.000000000000000000 ) ) ;
#27230=CARTESIAN_POINT ( 'NONE',  ( 10.53003223724999948, -60.12452529330000317, -7.612971414731999786 ) ) ;
#27233=DIRECTION ( 'NONE',  ( 0.000000000000000000, -1.000000000000000000, 0.000000000000000000 ) ) ;
#27235=ORIENTED_EDGE ( 'NONE', *, *, #29485, .F. ) ;
#27236=CARTESIAN_POINT ( 'NONE',  ( -2.015551294784000191, -54.99652295122999845, 12.79857978891999970 ) ) ;
#27238=CARTESIAN_POINT ( 'NONE',  ( 1.960212941618999949, -2.639484372332999929, 3.447996340602999865 ) ) ;
#27239=CARTESIAN_POINT ( 'NONE',  ( 12.48375848564000101, -23.37270426058999817, -1.669543623995999981 ) ) ;
#27242=CARTESIAN_POINT ( 'NONE',  ( -1.636761686205420396, -1.583333333333333481, -2.839805762151339508 ) ) ;
#27243=CARTESIAN_POINT ( 'NONE',  ( -10.07627163191000008, -18.75000000310999937, -7.601397897754999633 ) ) ;
#27249=CARTESIAN_POINT ( 'NONE',  ( 9.516265623847999677, -53.97460635707999899, -8.227505979398999969 ) ) ;
#27253=CARTESIAN_POINT ( 'NONE',  ( 0.000000000000000000, 0.000000000000000000, 0.000000000000000000 ) ) ;
#27255=CIRCLE ( 'NONE', #16904, 14.00000000000000000 ) ;
#27256=CARTESIAN_POINT ( 'NONE',  ( -3.165411199172024848, -2.520833333333333037, -0.8506806241676611036 ) ) ;
#27258=CARTESIAN_POINT ( 'NONE',  ( 12.56594317984999876, -18.75000000536999778, -1.750000000000000000 ) ) ;
#27261=EDGE_CURVE ( 'NONE', #21583, #27787, #41270, .T. ) ;
#27262=ORIENTED_EDGE ( 'NONE', *, *, #53342, .F. ) ;
#27264=EDGE_CURVE ( 'NONE', #2615, #36484, #11930, .T. ) ;
#27267=B_SPLINE_CURVE_WITH_KNOTS ( 'NONE', 3,
 ( #27258, #36417, #26098, #40857, #49430, #9272 ),
 .UNSPECIFIED., .F., .F.,
 ( 4, 1, 1, 4 ),
 ( 0.000000000000000000, 0.3333333333333000081, 0.6666666666667000474, 1.000000000000000000 ),
 .UNSPECIFIED. ) ;
#27273=CYLINDRICAL_SURFACE ( 'NONE', #39609, 12.50000000000000000 ) ;
#27277=DIRECTION ( 'NONE',  ( 5.381131437589000085E-11, -1.000000000000000000, -8.802795847113000035E-11 ) ) ;
#27279=CARTESIAN_POINT ( 'NONE',  ( -0.5045596072229999729, -25.13528913037999857, -12.66210649709999991 ) ) ;
#27282=CARTESIAN_POINT ( 'NONE',  ( -5.780852911904999836, -78.65969526808000012, 10.41696410405000073 ) ) ;
#27284=VERTEX_POINT ( 'NONE', #35950 ) ;
#27286=CARTESIAN_POINT ( 'NONE',  ( -12.50412681322478292, -17.48010473091721195, -1.235016000439554062 ) ) ;
#27292=CARTESIAN_POINT ( 'NONE',  ( 12.47598273373999866, -77.64680700753000053, -3.494640443823999743 ) ) ;
#27296=CARTESIAN_POINT ( 'NONE',  ( 12.76303204294000082, -18.73514849292999784, 1.980584515756000030 ) ) ;
#27300=AXIS2_PLACEMENT_3D ( 'NONE', #51689, #42527, #29215 ) ;
#27302=CARTESIAN_POINT ( 'NONE',  ( -10.01234990230000044, -60.09849137196000157, 7.653559502293999728 ) ) ;
#27303=CARTESIAN_POINT ( 'NONE',  ( -10.11087014619704760, -76.74276732863665984, -6.123559706077069009 ) ) ;
#27305=VECTOR ( 'NONE', #7747, 1000.000000000000114 ) ;
#27310=CARTESIAN_POINT ( 'NONE',  ( 3.665025684363000025, -3.580287900391999845, -1.025097465345000236 ) ) ;
#27316=DIRECTION ( 'NONE',  ( 0.7071067811865475727, 0.000000000000000000, -0.7071067811865475727 ) ) ;
#27317=CARTESIAN_POINT ( 'NONE',  ( 1.799502287743000029, -55.49283065365000311, 12.60413652829999975 ) ) ;
#27318=CARTESIAN_POINT ( 'NONE',  ( -10.64207148833999916, -76.93386827587001164, 7.489034475093999887 ) ) ;
#27321=CARTESIAN_POINT ( 'NONE',  ( 4.447441989892999992, -76.14829627867000283, -11.69528159757000019 ) ) ;
#27322=VERTEX_POINT ( 'NONE', #18838 ) ;
#27323=DIRECTION ( 'NONE',  ( 0.000000000000000000, -1.000000000000000000, 0.000000000000000000 ) ) ;
#27324=DIRECTION ( 'NONE',  ( 0.000000000000000000, -1.000000000000000000, -3.788556036780999566E-11 ) ) ;
#27326=DIRECTION ( 'NONE',  ( -1.000000000000000000, 0.000000000000000000, 0.000000000000000000 ) ) ;
#27329=CARTESIAN_POINT ( 'NONE',  ( 4.010845454633999552, -1.528571010530000107, -0.2065758488482999922 ) ) ;
#27332=ORIENTED_EDGE ( 'NONE', *, *, #51357, .F. ) ;
#27334=DIRECTION ( 'NONE',  ( -0.7071067811864980568, 0.7071067811865969777, -8.066391409586970286E-09 ) ) ;
#27335=VERTEX_POINT ( 'NONE', #26792 ) ;
#27338=CARTESIAN_POINT ( 'NONE',  ( 12.50000000000000000, -18.75000000310999937, -1.750000000000000000 ) ) ;
#27339=CARTESIAN_POINT ( 'NONE',  ( 7.601397897754999633, -60.04999999657000131, 10.07627163191000008 ) ) ;
#27342=CONICAL_SURFACE ( 'NONE', #9446, 11.90000000008999947, 0.7853981633972997312 ) ;
#27343=ORIENTED_EDGE ( 'NONE', *, *, #21214, .F. ) ;
#27344=B_SPLINE_SURFACE_WITH_KNOTS ( 'NONE', 3, 3, ( 
 ( #2469, #52630, #12185, #2184 ),
 ( #56483, #16617, #29307, #38755 ),
 ( #3044, #48494, #7466, #11617 ),
 ( #51777, #29592, #6884, #16334 ),
 ( #11327, #47648, #52062, #29879 ),
 ( #8034, #47935, #25464, #7176 ),
 ( #21039, #25176, #16040, #34602 ),
 ( #39043, #42910, #47354, #57055 ),
 ( #43199, #2752, #30170, #7751 ),
 ( #34887, #25756, #33740, #43776 ),
 ( #34023, #3328, #20754, #56195 ) ),
 .UNSPECIFIED., .F., .F., .F.,
 ( 4, 1, 1, 1, 1, 1, 1, 1, 4 ),
 ( 4, 4 ),
 ( -0.02001211456242000045, 0.000000000000000000, 0.1666666666667000196, 0.3333333333333000081, 0.5000000000000000000, 0.6666666666667000474, 0.8333333333333000637, 1.000000000000000000, 1.020273719995999917 ),
 ( -0.3582002740308999900, 1.358863140970000050 ),
 .UNSPECIFIED. ) ;
#27346=AXIS2_PLACEMENT_3D ( 'NONE', #16621, #7179, #7756 ) ;
#27347=CARTESIAN_POINT ( 'NONE',  ( -1.154017715338188976, -2.697074207813733082, -3.037772683525615580 ) ) ;
#27348=EDGE_CURVE ( 'NONE', #12253, #22602, #54566, .T. ) ;
#27351=ORIENTED_EDGE ( 'NONE', *, *, #27495, .F. ) ;
#27356=DIRECTION ( 'NONE',  ( 0.7071067811865474617, 0.000000000000000000, 0.7071067811865474617 ) ) ;
#27357=CARTESIAN_POINT ( 'NONE',  ( -0.5999381870725719601, -18.76980390684870059, 10.98362755083785203 ) ) ;
#27359=CARTESIAN_POINT ( 'NONE',  ( 0.000000000000000000, -55.54999999966999980, 12.50000000000000000 ) ) ;
#27363=CARTESIAN_POINT ( 'NONE',  ( -12.56594317823000040, -18.74999998606000062, -1.750000000000000000 ) ) ;
#27365=CARTESIAN_POINT ( 'NONE',  ( 10.07627163191000008, -18.75000000240999753, -7.601397897754999633 ) ) ;
#27367=CARTESIAN_POINT ( 'NONE',  ( 11.93555832086495805, -78.19079259615151045, -1.854496582926224546 ) ) ;
#27370=DIRECTION ( 'NONE',  ( 0.000000000000000000, 1.000000000000000000, 0.000000000000000000 ) ) ;
#27372=CARTESIAN_POINT ( 'NONE',  ( -1.466594960159999905, -24.08158199052000015, 12.44238958332999800 ) ) ;
#27374=CARTESIAN_POINT ( 'NONE',  ( -0.7382763017137000672, -1.859138932810000089, 3.717378721030999866 ) ) ;
#27376=CARTESIAN_POINT ( 'NONE',  ( 10.55910102243999837, -56.01514526721999943, 7.642147947524999374 ) ) ;
#27378=CARTESIAN_POINT ( 'NONE',  ( 12.43356840166999788, -61.51269674456000303, -0.8410229959425999935 ) ) ;
#27380=LINE ( 'NONE', #40078, #6890 ) ;
#27381=EDGE_CURVE ( 'NONE', #27979, #49445, #7204, .T. ) ;
#27382=AXIS2_PLACEMENT_3D ( 'NONE', #32012, #17766, #7746 ) ;
#27383=DIRECTION ( 'NONE',  ( 0.000000000000000000, 1.000000000000000000, 0.000000000000000000 ) ) ;
#27384=CARTESIAN_POINT ( 'NONE',  ( -7.919595949288999570, -55.64999999965999677, 8.768124086712999699 ) ) ;
#27389=B_SPLINE_SURFACE_WITH_KNOTS ( 'NONE', 3, 3, ( 
 ( #28847, #25299, #24440, #43317 ),
 ( #38874, #20020, #15869, #56894 ),
 ( #33855, #43607, #49190, #25873 ),
 ( #53922, #17902, #12866, #30585 ),
 ( #31150, #8444, #21448, #26439 ),
 ( #35006, #39457, #26733, #44183 ),
 ( #44462, #26164, #57748, #3444 ),
 ( #35589, #25585, #57461, #53617 ) ),
 .UNSPECIFIED., .F., .F., .F.,
 ( 4, 1, 1, 1, 1, 4 ),
 ( 4, 4 ),
 ( -0.01200407345745999922, 0.000000000000000000, 0.3333333333333000081, 0.6666666666667000474, 1.000000000000000000, 1.011997855551999947 ),
 ( -0.3559705542741999906, 1.355970554273999928 ),
 .UNSPECIFIED. ) ;
#27393=DIRECTION ( 'NONE',  ( -0.7071067812087692417, 2.829525585096875613E-07, 0.7071067811642691714 ) ) ;
#27396=CARTESIAN_POINT ( 'NONE',  ( 12.77651047528000028, -53.49104280904999342, 0.04320343284637000181 ) ) ;
#27397=CARTESIAN_POINT ( 'NONE',  ( -11.79999999999999893, -18.84999999999999787, 0.000000000000000000 ) ) ;
#27398=CARTESIAN_POINT ( 'NONE',  ( -3.685431006892999850, -1.816964919272999968, -0.5541339066752000164 ) ) ;
#27400=CARTESIAN_POINT ( 'NONE',  ( -7.958776490640000034, -61.27699850015999772, 9.723157983991999487 ) ) ;
#27403=DIRECTION ( 'NONE',  ( 0.000000000000000000, -1.000000000000000000, 0.000000000000000000 ) ) ;
#27404=LINE ( 'NONE', #36848, #39174 ) ;
#27405=DIRECTION ( 'NONE',  ( -0.7071067811704841999, -1.939412262328955489E-07, 0.7071067812025843002 ) ) ;
#27407=CARTESIAN_POINT ( 'NONE',  ( -12.50659830547393980, -17.02653383374055807, -0.3508384619336013532 ) ) ;
#27410=AXIS2_PLACEMENT_3D ( 'NONE', #18125, #18705, #27830 ) ;
#27412=CARTESIAN_POINT ( 'NONE',  ( -1.931043742978000077, -19.22204592323999961, 12.75763395699000036 ) ) ;
#27421=ADVANCED_FACE ( 'NONE', ( #4375 ), #31509, .F. ) ;
#27426=DIRECTION ( 'NONE',  ( 1.000000000000000000, 0.000000000000000000, 0.000000000000000000 ) ) ;
#27427=CARTESIAN_POINT ( 'NONE',  ( -9.767718346792999995, -78.44420564057999457, 7.129174073149000534 ) ) ;
#27432=ORIENTED_EDGE ( 'NONE', *, *, #36754, .F. ) ;
#27436=CARTESIAN_POINT ( 'NONE',  ( -3.453171399369999950, -1.863032031399000088, -0.5706200895263999762 ) ) ;
#27438=CARTESIAN_POINT ( 'NONE',  ( 11.93255069029000026, -79.28346444151000583, -2.830763026309000008 ) ) ;
#27442=CARTESIAN_POINT ( 'NONE',  ( 2.689698932207084336, -77.40716824597529921, 11.76506754417692413 ) ) ;
#27443=CARTESIAN_POINT ( 'NONE',  ( -13.99936781018472232, -9.295797029142999435, -0.1330447863085613691 ) ) ;
#27447=CARTESIAN_POINT ( 'NONE',  ( 7.770369683894697843, -24.23583903337609158, 10.20674856003130948 ) ) ;
#27453=CARTESIAN_POINT ( 'NONE',  ( 8.312408207604118360, -76.01187192366691647, 8.304083412923050744 ) ) ;
#27462=DIRECTION ( 'NONE',  ( -1.000000000000000000, 0.000000000000000000, 0.000000000000000000 ) ) ;
#27464=CYLINDRICAL_SURFACE ( 'NONE', #26440, 11.75000000000000000 ) ;
#27466=ORIENTED_EDGE ( 'NONE', *, *, #12940, .T. ) ;
#27467=EDGE_CURVE ( 'NONE', #42030, #25015, #13764, .T. ) ;
#27468=VECTOR ( 'NONE', #36482, 1000.000000000000000 ) ;
#27470=CARTESIAN_POINT ( 'NONE',  ( 12.76303204294000082, -18.73514849292999784, 1.980584515756000030 ) ) ;
#27474=CARTESIAN_POINT ( 'NONE',  ( -12.00000000000000000, -55.54999999966999980, -1.250000000000000000 ) ) ;
#27475=CARTESIAN_POINT ( 'NONE',  ( -8.060167320296210747, -17.37936585541824996, -9.621722526397146424 ) ) ;
#27477=DIRECTION ( 'NONE',  ( -1.000000000000000000, 0.000000000000000000, 0.000000000000000000 ) ) ;
#27479=CARTESIAN_POINT ( 'NONE',  ( -12.43569926716000040, -24.88202093001000037, 0.4277578398255000303 ) ) ;
#27480=ORIENTED_EDGE ( 'NONE', *, *, #36109, .T. ) ;
#27481=ORIENTED_EDGE ( 'NONE', *, *, #26091, .F. ) ;
#27484=EDGE_CURVE ( 'NONE', #1025, #2377, #41130, .T. ) ;
#27486=ORIENTED_EDGE ( 'NONE', *, *, #8150, .T. ) ;
#27488=CARTESIAN_POINT ( 'NONE',  ( 8.533826143225001104, -25.00526450249999755, 9.213084459905999779 ) ) ;
#27490=CARTESIAN_POINT ( 'NONE',  ( 7.756281347497000489, -61.02006031080999549, 10.15825374577000062 ) ) ;
#27495=EDGE_CURVE ( 'NONE', #7896, #14715, #11895, .T. ) ;
#27497=CARTESIAN_POINT ( 'NONE',  ( -8.121699804427876757, -24.83626205760389993, 9.841121124182388158 ) ) ;
#27504=CARTESIAN_POINT ( 'NONE',  ( 6.842107050174999650, -76.58777295158999721, -11.01216002263999982 ) ) ;
#27505=CARTESIAN_POINT ( 'NONE',  ( -1.681307385754345685, -2.082147688907624694, -2.810393918989617212 ) ) ;
#27509=CARTESIAN_POINT ( 'NONE',  ( 12.76303204525000012, -60.06485147653999945, 1.980584515753000208 ) ) ;
#27510=CARTESIAN_POINT ( 'NONE',  ( 12.49168433577000137, -55.50150862742999891, -1.667916687244999974 ) ) ;
#27517=CARTESIAN_POINT ( 'NONE',  ( -10.19019671031999863, -18.80356357339999818, 7.646965722246000574 ) ) ;
#27518=CARTESIAN_POINT ( 'NONE',  ( 3.075537641221555596, -78.44583333333332575, -11.44417895085270587 ) ) ;
#27520=FACE_OUTER_BOUND ( 'NONE', #8186, .T. ) ;
#27530=DIRECTION ( 'NONE',  ( 0.000000000000000000, 1.000000000000000000, 0.000000000000000000 ) ) ;
#27534=CARTESIAN_POINT ( 'NONE',  ( -1.750000000000000000, -60.04999999657000131, 12.50000000000000000 ) ) ;
#27536=DIRECTION ( 'NONE',  ( 0.9936845293270585300, 0.1122098755727947705, 0.000000000000000000 ) ) ;
#27539=CARTESIAN_POINT ( 'NONE',  ( -7.651160336710000287, -19.23767313813999991, -10.45205658995999976 ) ) ;
#27541=CARTESIAN_POINT ( 'NONE',  ( 9.101506735319000896, -53.91932813864999474, -8.485532457216999447 ) ) ;
#27543=CARTESIAN_POINT ( 'NONE',  ( -12.89999999994999769, -2.999999999951000085, -1.886268936261000296E-09 ) ) ;
#27545=CARTESIAN_POINT ( 'NONE',  ( -0.1380878921325282283, -62.02734402296150762, 12.70555840936477310 ) ) ;
#27547=CONICAL_SURFACE ( 'NONE', #1167, 3.471875000818999801, 0.7853981633972997312 ) ;
#27548=CARTESIAN_POINT ( 'NONE',  ( -12.66314513620999804, -61.97864743329000703, -0.04033065750138999789 ) ) ;
#27550=CARTESIAN_POINT ( 'NONE',  ( 1.250000000000000000, -55.35321828636000419, 12.50000000000000000 ) ) ;
#27551=EDGE_LOOP ( 'NONE', ( #55217, #1198, #39013, #55165 ) ) ;
#27553=VECTOR ( 'NONE', #2985, 1000.000000000000000 ) ;
#27554=CARTESIAN_POINT ( 'NONE',  ( 1.103931350763639241, -61.42083747905927993, 12.50298439261563388 ) ) ;
#27556=CARTESIAN_POINT ( 'NONE',  ( 8.140250184777904963, -55.34839576619644674, 7.398464061250712653 ) ) ;
#27561=DIRECTION ( 'NONE',  ( 0.000000000000000000, 1.000000000000000000, 0.000000000000000000 ) ) ;
#27562=EDGE_LOOP ( 'NONE', ( #17385, #51410, #51626, #12475 ) ) ;
#27566=CARTESIAN_POINT ( 'NONE',  ( 1.750000000001000089, -55.55000001292999912, 12.56594318049000059 ) ) ;
#27567=CARTESIAN_POINT ( 'NONE',  ( 2.062323307449999810, -23.22713153192000135, -12.83634826442999888 ) ) ;
#27569=CARTESIAN_POINT ( 'NONE',  ( 7.624341766656999475, -60.06485146221000093, 10.42531125026000005 ) ) ;
#27570=CARTESIAN_POINT ( 'NONE',  ( -3.846946059935000051, -78.43062821897001413, -11.43190855169999942 ) ) ;
#27571=ADVANCED_FACE ( 'NONE', ( #11663 ), #16666, .F. ) ;
#27574=DIRECTION ( 'NONE',  ( 0.7071067811864980568, 0.7071067811865969777, -2.302419900729990164E-09 ) ) ;
#27577=ADVANCED_FACE ( 'NONE', ( #20229 ), #44589, .F. ) ;
#27581=CARTESIAN_POINT ( 'NONE',  ( -10.42272502862000039, -21.75453807238000081, 7.691893942719999266 ) ) ;
#27582=CARTESIAN_POINT ( 'NONE',  ( 5.421352887295999956, -76.67165190241000516, 11.59375966951999892 ) ) ;
#27585=DIRECTION ( 'NONE',  ( 0.000000000000000000, 0.000000000000000000, 1.000000000000000000 ) ) ;
#27590=CARTESIAN_POINT ( 'NONE',  ( -11.00000000000000000, -23.75000000000000000, 0.000000000000000000 ) ) ;
#27594=FACE_OUTER_BOUND ( 'NONE', #8891, .T. ) ;
#27596=CARTESIAN_POINT ( 'NONE',  ( 3.772660615778999915, -2.077883300257999721, 0.5031134774969999723 ) ) ;
#27599=DIRECTION ( 'NONE',  ( 0.000000000000000000, 0.000000000000000000, -1.000000000000000000 ) ) ;
#27600=CARTESIAN_POINT ( 'NONE',  ( 0.4515105396355221234, -18.45278097531555161, -10.99076531923743083 ) ) ;
#27602=CARTESIAN_POINT ( 'NONE',  ( 11.74514291648612918, -77.45731891081528886, 1.539200744266281173 ) ) ;
#27605=CARTESIAN_POINT ( 'NONE',  ( -9.234979314279001983, -77.04487755778998803, -9.168119495123999485 ) ) ;
#27609=ORIENTED_EDGE ( 'NONE', *, *, #56755, .F. ) ;
#27610=EDGE_CURVE ( 'NONE', #35538, #5930, #22321, .T. ) ;
#27611=CIRCLE ( 'NONE', #6894, 1.250000000000000444 ) ;
#27612=CARTESIAN_POINT ( 'NONE',  ( -9.502896617869424745, -24.74094210337188926, -8.179425869181063291 ) ) ;
#27618=CARTESIAN_POINT ( 'NONE',  ( -0.4617212151683000032, -1.132168933658999954, 3.989551193614000013 ) ) ;
#27619=CARTESIAN_POINT ( 'NONE',  ( -1.799475304559999822, -57.04828923575999511, -12.69616050746999925 ) ) ;
#27621=ORIENTED_EDGE ( 'NONE', *, *, #24448, .F. ) ;
#27624=ORIENTED_EDGE ( 'NONE', *, *, #20710, .F. ) ;
#27629=ORIENTED_EDGE ( 'NONE', *, *, #53205, .F. ) ;
#27631=AXIS2_PLACEMENT_3D ( 'NONE', #34190, #52512, #52228 ) ;
#27632=ORIENTED_EDGE ( 'NONE', *, *, #51138, .F. ) ;
#27634=CARTESIAN_POINT ( 'NONE',  ( 0.05356364311145376395, -2.727063383492749349, -3.249227035622031856 ) ) ;
#27637=DIRECTION ( 'NONE',  ( -1.000000000000000000, -1.534448722697999916E-11, -3.998226783829999760E-14 ) ) ;
#27639=VERTEX_POINT ( 'NONE', #3939 ) ;
#27643=ADVANCED_FACE ( 'NONE', ( #39386 ), #8965, .F. ) ;
#27645=TOROIDAL_SURFACE ( 'NONE', #22938, 26.50000000000000000, 14.00000000000000000 ) ;
#27648=CARTESIAN_POINT ( 'NONE',  ( -8.872958366904050820, -25.01010144684924086, 8.813896669003202788 ) ) ;
#27649=AXIS2_PLACEMENT_3D ( 'NONE', #25449, #7157, #25159 ) ;
#27650=CARTESIAN_POINT ( 'NONE',  ( 13.94241847916999966, -46.33997059779999717, 4.312626734956999977E-05 ) ) ;
#27656=FACE_OUTER_BOUND ( 'NONE', #46481, .T. ) ;
#27659=CARTESIAN_POINT ( 'NONE',  ( -1.750000000001000089, -60.04999998641999781, 12.56594318054000148 ) ) ;
#27660=EDGE_CURVE ( 'NONE', #26860, #20749, #11323, .T. ) ;
#27661=FACE_BOUND ( 'NONE', #21609, .T. ) ;
#27662=CARTESIAN_POINT ( 'NONE',  ( -1.632307027708999936, -23.66927189556999878, 12.46200249212000166 ) ) ;
#27664=CARTESIAN_POINT ( 'NONE',  ( -1.528023617186000216, -0.8891593309027000513, -3.828850291668000061 ) ) ;
#27666=DIRECTION ( 'NONE',  ( 0.9957542233426779354, 0.04890176637353889355, 0.07798810127684829840 ) ) ;
#27673=DIRECTION ( 'NONE',  ( 0.000000000000000000, 1.000000000000000000, 0.000000000000000000 ) ) ;
#27676=VERTEX_POINT ( 'NONE', #18412 ) ;
#27677=EDGE_CURVE ( 'NONE', #48697, #46616, #25158, .T. ) ;
#27679=TOROIDAL_SURFACE ( 'NONE', #55045, 1.250000000000000000, 0.5000000000000000000 ) ;
#27682=CARTESIAN_POINT ( 'NONE',  ( -1.750000000000000000, -18.75000000310999937, -12.50000000000000000 ) ) ;
#27686=LINE ( 'NONE', #27101, #24183 ) ;
#27691=CIRCLE ( 'NONE', #20176, 1.750000000000000000 ) ;
#27692=CARTESIAN_POINT ( 'NONE',  ( -1.583004792650378079, -54.34790758811381295, -12.70616254407330104 ) ) ;
#27694=CARTESIAN_POINT ( 'NONE',  ( -7.601397897754999633, -18.75000000310999937, 10.07627163191000008 ) ) ;
#27695=EDGE_CURVE ( 'NONE', #30078, #30606, #23992, .T. ) ;
#27697=EDGE_CURVE ( 'NONE', #36041, #7374, #28227, .T. ) ;
#27701=CARTESIAN_POINT ( 'NONE',  ( -1.799502287691000069, -18.69283319134000010, 12.60413670420000010 ) ) ;
#27703=ORIENTED_EDGE ( 'NONE', *, *, #50223, .T. ) ;
#27704=CARTESIAN_POINT ( 'NONE',  ( -7.624341766647000362, -18.73514853758999976, 10.42531125024999916 ) ) ;
#27707=VERTEX_POINT ( 'NONE', #27826 ) ;
#27708=CARTESIAN_POINT ( 'NONE',  ( 12.70926961117000076, -55.39159259587000150, 1.933875435151000133 ) ) ;
#27709=CARTESIAN_POINT ( 'NONE',  ( 8.485281374238999419, -55.54999999966999980, -8.485281374238999419 ) ) ;
#27710=B_SPLINE_CURVE_WITH_KNOTS ( 'NONE', 3,
 ( #10559, #11936, #19411, #43519, #42439, #16365, #6116, #21357, #55720, #20003, #43817, #16653, #24123, #57380, #12218, #3362, #25501, #29915, #3080, #34346, #34637, #42141, #38789, #16940, #30500 ),
 .UNSPECIFIED., .F., .F.,
 ( 4, 1, 1, 1, 1, 1, 2, 2, 1, 1, 1, 2, 2, 1, 2, 2, 4 ),
 ( 0.000000000000000000, 0.1250000000000003331, 0.1875000000000004996, 0.2187500000000005829, 0.2343750000000006106, 0.2421875000000006384, 0.2460937500000006661, 0.2500000000000006661, 0.3750000000000012768, 0.4375000000000016098, 0.4687500000000017764, 0.4843750000000017764, 0.5000000000000017764, 0.6250000000000014433, 0.6875000000000012212, 0.7500000000000011102, 1.000000000000000000 ),
 .UNSPECIFIED. ) ;
#27712=ORIENTED_EDGE ( 'NONE', *, *, #18085, .F. ) ;
#27715=CARTESIAN_POINT ( 'NONE',  ( -1.811016405462517076, -17.93826444627195116, -12.71771640064051034 ) ) ;
#27717=VECTOR ( 'NONE', #55082, 1000.000000000000000 ) ;
#27721=CARTESIAN_POINT ( 'NONE',  ( -9.722718241315000398, -23.25000000000000000, -7.247844507162001015 ) ) ;
#27722=CARTESIAN_POINT ( 'NONE',  ( 11.50190934395000042, -76.70965847532001192, -3.421415122956000143 ) ) ;
#27724=DIRECTION ( 'NONE',  ( 0.07798810159119662355, -0.04890177459382791247, 0.9957542229143573342 ) ) ;
#27725=CARTESIAN_POINT ( 'NONE',  ( 3.313940609516682123, -2.126588154580539403, 1.183591495650892833 ) ) ;
#27726=CARTESIAN_POINT ( 'NONE',  ( 7.605690822197999523, -60.22565082124000213, -10.52682217037000001 ) ) ;
#27727=CARTESIAN_POINT ( 'NONE',  ( 11.03890801094999929, -78.73146484947000090, -5.342433469444999972 ) ) ;
#27729=CARTESIAN_POINT ( 'NONE',  ( 12.71536175402335722, -17.87444297183331088, -1.781227265980052099 ) ) ;
#27732=CARTESIAN_POINT ( 'NONE',  ( -8.421892176740767511, -77.11363408704187350, -8.655124593329036387 ) ) ;
#27734=EDGE_LOOP ( 'NONE', ( #36718, #34813, #48990 ) ) ;
#27737=CARTESIAN_POINT ( 'NONE',  ( 7.624341766639000539, -23.26485146254000114, 10.42531125024000005 ) ) ;
#27742=CARTESIAN_POINT ( 'NONE',  ( 4.496626815610547112, -76.04321716337622661, 10.85519476661798777 ) ) ;
#27745=ORIENTED_EDGE ( 'NONE', *, *, #12032, .F. ) ;
#27748=B_SPLINE_CURVE_WITH_KNOTS ( 'NONE', 3,
 ( #47693, #47402, #39666, #11664, #16951, #52395, #34932, #8087, #29640, #17228, #2802, #21085, #56529, #24937, #35218, #38801, #11376, #52965 ),
 .UNSPECIFIED., .F., .F.,
 ( 4, 2, 2, 2, 2, 2, 2, 2, 4 ),
 ( 0.000000000000000000, 0.1250000000000000000, 0.2500000000000000000, 0.3750000000000000000, 0.5000000000000000000, 0.6250000000000000000, 0.7500000000000000000, 0.8750000000000000000, 1.000000000000000000 ),
 .UNSPECIFIED. ) ;
#27749=VECTOR ( 'NONE', #24537, 1000.000000000000000 ) ;
#27755=CARTESIAN_POINT ( 'NONE',  ( -12.50000000000000000, -39.30476012429000576, 0.000000000000000000 ) ) ;
#27756=CARTESIAN_POINT ( 'NONE',  ( 9.029856014872001069, -16.66737842935999936, -9.038878718683999836 ) ) ;
#27757=CARTESIAN_POINT ( 'NONE',  ( -8.096452064242996016, -59.58578169018998949, -13.15643568217000769 ) ) ;
#27758=B_SPLINE_CURVE_WITH_KNOTS ( 'NONE', 3,
 ( #46273, #32938, #37085, #41233, #46565, #11126, #6089, #27929 ),
 .UNSPECIFIED., .F., .F.,
 ( 4, 2, 2, 4 ),
 ( 0.000000000000000000, 0.5000000000000000000, 0.7500000000000000000, 1.000000000000000000 ),
 .UNSPECIFIED. ) ;
#27759=ORIENTED_EDGE ( 'NONE', *, *, #9040, .F. ) ;
#27761=CARTESIAN_POINT ( 'NONE',  ( 12.72924182828753636, -55.02450359957972381, 1.930521792060713837 ) ) ;
#27766=EDGE_CURVE ( 'NONE', #33521, #35763, #50293, .T. ) ;
#27769=CARTESIAN_POINT ( 'NONE',  ( -8.872949060675491495, -16.98989818440328392, -8.813905828572767831 ) ) ;
#27774=ORIENTED_EDGE ( 'NONE', *, *, #7357, .T. ) ;
#27778=ORIENTED_EDGE ( 'NONE', *, *, #204, .T. ) ;
#27779=DIRECTION ( 'NONE',  ( -1.000000000000000000, 0.000000000000000000, 0.000000000000000000 ) ) ;
#27781=CARTESIAN_POINT ( 'NONE',  ( 7.633403016722000167, -60.18650073818000124, 10.18126993295000027 ) ) ;
#27786=VECTOR ( 'NONE', #42284, 1000.000000000000000 ) ;
#27787=VERTEX_POINT ( 'NONE', #723 ) ;
#27788=ORIENTED_EDGE ( 'NONE', *, *, #27870, .F. ) ;
#27791=AXIS2_PLACEMENT_3D ( 'NONE', #25681, #11829, #43707 ) ;
#27792=DIRECTION ( 'NONE',  ( 0.000000000000000000, -1.000000000000000000, 0.000000000000000000 ) ) ;
#27800=CARTESIAN_POINT ( 'NONE',  ( 1.931086388578000079, -60.09778754156999980, -12.71798269388000158 ) ) ;
#27801=CARTESIAN_POINT ( 'NONE',  ( -7.434020715870205187, -60.31691643837059758, 8.107762507646519623 ) ) ;
#27803=ORIENTED_EDGE ( 'NONE', *, *, #20840, .T. ) ;
#27808=CARTESIAN_POINT ( 'NONE',  ( -1.997276839918484148, -3.427083333333333925, 2.598917237794077018 ) ) ;
#27809=CARTESIAN_POINT ( 'NONE',  ( 11.75000000000000000, -78.54999999999999716, 0.000000000000000000 ) ) ;
#27810=DIRECTION ( 'NONE',  ( 1.000000000000000000, 0.000000000000000000, 0.000000000000000000 ) ) ;
#27811=CARTESIAN_POINT ( 'NONE',  ( 1.001315001700999963, -54.11477588220000001, 12.50000000000000000 ) ) ;
#27820=CARTESIAN_POINT ( 'NONE',  ( -1.322675138774000114, -1.903566864579000040, -3.739459546867000217 ) ) ;
#27824=CARTESIAN_POINT ( 'NONE',  ( 8.260136572111999698, -24.94034376567000066, -9.643347111174000119 ) ) ;
#27826=CARTESIAN_POINT ( 'NONE',  ( 3.250000000000000000, -1.350000000000000089, 0.000000000000000000 ) ) ;
#27827=LINE ( 'NONE', #1875, #14379 ) ;
#27830=DIRECTION ( 'NONE',  ( -1.000000000000000000, 0.000000000000000000, 0.000000000000000000 ) ) ;
#27833=DIRECTION ( 'NONE',  ( 0.000000000000000000, 1.000000000000000000, 0.000000000000000000 ) ) ;
#27836=CIRCLE ( 'NONE', #23131, 13.89999999999999858 ) ;
#27841=DIRECTION ( 'NONE',  ( 0.000000000000000000, 0.000000000000000000, -1.000000000000000000 ) ) ;
#27842=ORIENTED_EDGE ( 'NONE', *, *, #58074, .T. ) ;
#27847=ORIENTED_EDGE ( 'NONE', *, *, #21236, .T. ) ;
#27850=VERTEX_POINT ( 'NONE', #11304 ) ;
#27852=ORIENTED_EDGE ( 'NONE', *, *, #18338, .F. ) ;
#27853=DIRECTION ( 'NONE',  ( -0.7071067811865475727, 0.000000000000000000, 0.7071067811865475727 ) ) ;
#27854=CARTESIAN_POINT ( 'NONE',  ( 0.000000000000000000, 4.040000000000000036, 0.000000000000000000 ) ) ;
#27860=ORIENTED_EDGE ( 'NONE', *, *, #42023, .F. ) ;
#27862=CARTESIAN_POINT ( 'NONE',  ( -1.750000000000000000, -60.04999999725999515, -12.50000000000000000 ) ) ;
#27864=CARTESIAN_POINT ( 'NONE',  ( 1.980610890454856055, -60.32073889451354631, -12.74374574609741018 ) ) ;
#27866=CARTESIAN_POINT ( 'NONE',  ( 10.42531124908000173, -60.06485148440999922, 7.624341765471999821 ) ) ;
#27868=( BOUNDED_SURFACE ( )  B_SPLINE_SURFACE ( 3, 3, ( 
 ( #54258, #28239, #14090, #13791 ),
 ( #37106, #18825, #54835, #23532 ),
 ( #10854, #56582, #47744, #15559 ),
 ( #52162, #38276, #56008, #56874 ),
 ( #16431, #7277, #20850, #47463 ),
 ( #25279, #24991, #6403, #43011 ),
 ( #47169, #34414, #11430, #38854 ) ),
 .UNSPECIFIED., .F., .F., .F. ) 
 B_SPLINE_SURFACE_WITH_KNOTS ( ( 4, 3, 4 ),
 ( 4, 4 ),
 ( 0.000000000000000000, 1.000000000000000000, 2.000000000000000000 ),
 ( 0.000000000000000000, 1.000000000000000000 ),
 .UNSPECIFIED. ) 
 GEOMETRIC_REPRESENTATION_ITEM ( )  RATIONAL_B_SPLINE_SURFACE ( (
 ( 1.196373642248999891, 1.184225762575999985, 1.184225762575999985, 1.196373642248999891),
 ( 0.9447739570234999773, 0.9351807998836999536, 0.9351807998836999536, 0.9447739570234999773),
 ( 0.9447739570234999773, 0.9351807998836999536, 0.9351807998836999536, 0.9447739570234999773),
 ( 1.196373642248999891, 1.184225762575999985, 1.184225762575999985, 1.196373642248999891),
 ( 0.9447739570234999773, 0.9351807998836999536, 0.9351807998836999536, 0.9447739570234999773),
 ( 0.9447739570234999773, 0.9351807998836999536, 0.9351807998836999536, 0.9447739570234999773),
 ( 1.196373642248999891, 1.184225762575999985, 1.184225762575999985, 1.196373642248999891) ) ) 
 REPRESENTATION_ITEM ( '' )  SURFACE ( )  );
#27869=CARTESIAN_POINT ( 'NONE',  ( 11.80688451001000061, -77.70231164849001004, 5.334804138346999736 ) ) ;
#27870=EDGE_CURVE ( 'NONE', #3967, #6729, #54297, .T. ) ;
#27873=CARTESIAN_POINT ( 'NONE',  ( -12.80896991324000034, -21.75453807238000081, -1.930989179114000143 ) ) ;
#27878=FACE_BOUND ( 'NONE', #54109, .T. ) ;
#27880=AXIS2_PLACEMENT_3D ( 'NONE', #9828, #10122, #27810 ) ;
#27883=CARTESIAN_POINT ( 'NONE',  ( 10.44683666364205266, -79.24999999999997158, 6.036782290497776593 ) ) ;
#27886=CARTESIAN_POINT ( 'NONE',  ( -4.801183948427951265, -78.89166666666666572, -10.79468190471831690 ) ) ;
#27888=PLANE ( 'NONE',  #39257 ) ;
#27889=B_SPLINE_CURVE_WITH_KNOTS ( 'NONE', 3,
 ( #21604, #39608, #31311, #34878, #23571, #12738 ),
 .UNSPECIFIED., .F., .F.,
 ( 4, 2, 4 ),
 ( 0.000000000000000000, 0.5000000000000000000, 1.000000000000000000 ),
 .UNSPECIFIED. ) ;
#27890=EDGE_CURVE ( 'NONE', #20252, #20752, #43464, .T. ) ;
#27892=CARTESIAN_POINT ( 'NONE',  ( -3.201433918554999813, -77.84278050555001016, 12.61309089657999927 ) ) ;
#27895=CARTESIAN_POINT ( 'NONE',  ( 9.532736212859026281, -78.49731003545609553, 6.867370139290200015 ) ) ;
#27896=DIRECTION ( 'NONE',  ( 0.000000000000000000, 0.000000000000000000, -1.000000000000000000 ) ) ;
#27904=CARTESIAN_POINT ( 'NONE',  ( 2.028166799595999770, -0.9151276875359000140, -3.466423845304999585 ) ) ;
#27907=CARTESIAN_POINT ( 'NONE',  ( -1.250000000000000000, -23.25000000000000000, 12.00000000000000000 ) ) ;
#27910=EDGE_LOOP ( 'NONE', ( #9587, #13711, #53044, #21539 ) ) ;
#27914=ORIENTED_EDGE ( 'NONE', *, *, #47501, .T. ) ;
#27915=FACE_OUTER_BOUND ( 'NONE', #45081, .T. ) ;
#27916=ORIENTED_EDGE ( 'NONE', *, *, #51695, .T. ) ;
#27919=CARTESIAN_POINT ( 'NONE',  ( -1.423977246384270590, -2.689414678050281893, -2.927659162848880392 ) ) ;
#27921=ORIENTED_EDGE ( 'NONE', *, *, #4777, .T. ) ;
#27925=ORIENTED_EDGE ( 'NONE', *, *, #11634, .T. ) ;
#27926=CARTESIAN_POINT ( 'NONE',  ( 0.000000000000000000, -2.660000000000000142, 0.000000000000000000 ) ) ;
#27928=ORIENTED_EDGE ( 'NONE', *, *, #27076, .F. ) ;
#27929=CARTESIAN_POINT ( 'NONE',  ( 1.750000000001000089, -18.75000001325000198, 12.56594318051000059 ) ) ;
#27932=EDGE_CURVE ( 'NONE', #26558, #46040, #5650, .T. ) ;
#27933=CARTESIAN_POINT ( 'NONE',  ( -1.484271920566999698E-14, -80.79999999999999716, 0.000000000000000000 ) ) ;
#27934=CARTESIAN_POINT ( 'NONE',  ( -12.99510751537000353, -15.69705297113999443, 6.911973076623003642 ) ) ;
#27936=CARTESIAN_POINT ( 'NONE',  ( 11.75000000000000000, -77.04999999999999716, 0.000000000000000000 ) ) ;
#27940=CARTESIAN_POINT ( 'NONE',  ( 2.740029395673595047, -76.55575388350786170, 11.42608732962110984 ) ) ;
#27944=CARTESIAN_POINT ( 'NONE',  ( 10.65674263929012788, -78.16410729663259360, -5.672678603144905018 ) ) ;
#27950=LINE ( 'NONE', #41546, #30784 ) ;
#27952=CARTESIAN_POINT ( 'NONE',  ( -10.36289662403999756, -60.00106470408999826, -7.633500902345000227 ) ) ;
#27953=CARTESIAN_POINT ( 'NONE',  ( 12.70556836322084315, -25.22772277445464439, -0.2597962961525307479 ) ) ;
#27954=CARTESIAN_POINT ( 'NONE',  ( -1.667260628941999778, -23.20942012473999938, -12.49858003894999925 ) ) ;
#27955=CARTESIAN_POINT ( 'NONE',  ( 13.86363636363000218, -69.16102867818000277, 1.277888278513000037E-05 ) ) ;
#27956=CARTESIAN_POINT ( 'NONE',  ( -2.239251858213000101, -3.482118084780000178, 2.225821419444999893 ) ) ;
#27957=CARTESIAN_POINT ( 'NONE',  ( -7.770369683894697843, -24.23583903337609158, -10.20674856003130948 ) ) ;
#27959=AXIS2_PLACEMENT_3D ( 'NONE', #16229, #20370, #41934 ) ;
#27961=LINE ( 'NONE', #46011, #37323 ) ;
#27962=DIRECTION ( 'NONE',  ( 0.000000000000000000, 1.000000000000000000, 0.000000000000000000 ) ) ;
#27964=CARTESIAN_POINT ( 'NONE',  ( 3.752244608269999837, -75.81839300465999543, -11.62132640531999961 ) ) ;
#27965=ORIENTED_EDGE ( 'NONE', *, *, #24845, .F. ) ;
#27969=AXIS2_PLACEMENT_3D ( 'NONE', #53598, #46516, #1061 ) ;
#27971=CARTESIAN_POINT ( 'NONE',  ( 7.610436392395274474, -55.27459049260378521, 10.41144384036934056 ) ) ;
#27973=CARTESIAN_POINT ( 'NONE',  ( 12.56594317823000040, -23.25000001387000026, -1.750000000000000000 ) ) ;
#27976=CARTESIAN_POINT ( 'NONE',  ( -2.473380543883999749, -1.377984372333000085, -3.177361517278999958 ) ) ;
#27979=VERTEX_POINT ( 'NONE', #1796 ) ;
#27983=DIRECTION ( 'NONE',  ( 1.000000000000000000, 0.000000000000000000, 0.000000000000000000 ) ) ;
#27985=CARTESIAN_POINT ( 'NONE',  ( -12.60552522433000000, -55.51082434643999619, -1.799501877760999902 ) ) ;
#27986=CARTESIAN_POINT ( 'NONE',  ( 8.768124086712999699, -55.64999999965999677, 7.919595949288999570 ) ) ;
#27990=CARTESIAN_POINT ( 'NONE',  ( -1.667961430005999945, -21.74888345808999901, 12.58335110161999815 ) ) ;
#27991=VERTEX_POINT ( 'NONE', #51963 ) ;
#27993=CARTESIAN_POINT ( 'NONE',  ( 8.485281374238999419, -18.75000000000000000, 8.485281374238999419 ) ) ;
#27996=ORIENTED_EDGE ( 'NONE', *, *, #14827, .T. ) ;
#27997=CARTESIAN_POINT ( 'NONE',  ( 12.46083735077000121, -55.11664398755999628, 1.628985986890000071 ) ) ;
#27999=CARTESIAN_POINT ( 'NONE',  ( -12.79972228482999874, -23.79021513454000214, -2.019125729023000027 ) ) ;
#28003=CARTESIAN_POINT ( 'NONE',  ( -7.674614791499999811, -56.04899163905999870, 10.14948852566000070 ) ) ;
#28005=DIRECTION ( 'NONE',  ( -0.9999463328794432337, 0.000000000000000000, 0.01036008498777044214 ) ) ;
#28006=EDGE_CURVE ( 'NONE', #15123, #46904, #37408, .T. ) ;
#28008=AXIS2_PLACEMENT_3D ( 'NONE', #22804, #21634, #39639 ) ;
#28011=ORIENTED_EDGE ( 'NONE', *, *, #34201, .T. ) ;
#28013=CARTESIAN_POINT ( 'NONE',  ( -11.91862232004000077, -75.96254709223001100, 3.079279237876999531 ) ) ;
#28015=CARTESIAN_POINT ( 'NONE',  ( -2.268810067667969221, -2.280055725771751085, 2.689892472967077008 ) ) ;
#28016=CARTESIAN_POINT ( 'NONE',  ( 7.631896413346999530, -60.02122715173999978, -10.36221694968000051 ) ) ;
#28017=B_SPLINE_CURVE_WITH_KNOTS ( 'NONE', 3,
 ( #35087, #44260, #53121, #12670, #21817, #9283, #21968, #57697 ),
 .UNSPECIFIED., .F., .F.,
 ( 4, 2, 2, 4 ),
 ( 0.000000000000000000, 0.5000000000000000000, 0.7500000000000000000, 1.000000000000000000 ),
 .UNSPECIFIED. ) ;
#28018=CARTESIAN_POINT ( 'NONE',  ( 8.438902753042999194, -78.70272413139998946, -8.898539530003999332 ) ) ;
#28021=CARTESIAN_POINT ( 'NONE',  ( 12.70451544424452450, -17.44534321913721797, -1.498804046739477869 ) ) ;
#28023=CARTESIAN_POINT ( 'NONE',  ( 2.910828549648142527, -2.813461382813009948, -1.464431053388650650 ) ) ;
#28024=CARTESIAN_POINT ( 'NONE',  ( 11.32629911350350049, -77.32711347535936852, 4.017011466391305241 ) ) ;
#28026=ADVANCED_FACE ( 'NONE', ( #2661 ), #6200, .F. ) ;
#28030=CARTESIAN_POINT ( 'NONE',  ( 10.41144098943260055, -23.52546312060280798, 7.610433527965647649 ) ) ;
#28033=CARTESIAN_POINT ( 'NONE',  ( 3.018378881891000010, -2.180961001041000102, 2.164217357939999697 ) ) ;
#28036=CARTESIAN_POINT ( 'NONE',  ( 8.622285323087540476, -76.00886100035398840, 7.982628424629189645 ) ) ;
#28039=ORIENTED_EDGE ( 'NONE', *, *, #53277, .T. ) ;
#28040=CARTESIAN_POINT ( 'NONE',  ( 8.130813118010999929, -17.31476110167000115, -9.546856411651999608 ) ) ;
#28041=DIRECTION ( 'NONE',  ( 0.000000000000000000, -1.000000000000000000, 0.000000000000000000 ) ) ;
#28043=DIRECTION ( 'NONE',  ( 0.000000000000000000, -1.000000000000000000, 0.000000000000000000 ) ) ;
#28045=LINE ( 'NONE', #36911, #44365 ) ;
#28046=CARTESIAN_POINT ( 'NONE',  ( 10.19019671031999863, -18.80356357339999818, -7.646965722246000574 ) ) ;
#28047=CARTESIAN_POINT ( 'NONE',  ( -5.786987246029717369, -78.26865275249193132, 10.31969880544682105 ) ) ;
#28051=CARTESIAN_POINT ( 'NONE',  ( 12.76303204291999904, -55.53514849259999409, 1.980584515756000030 ) ) ;
#28054=CARTESIAN_POINT ( 'NONE',  ( 11.81845385912002833, -77.71935230467143185, 2.469272334833096494 ) ) ;
#28055=CARTESIAN_POINT ( 'NONE',  ( 11.51387517028932983, -76.43373939162262332, -2.343431589605189380 ) ) ;
#28057=CARTESIAN_POINT ( 'NONE',  ( -12.50728617043997382, -53.80024476438079262, -0.1757989195630510482 ) ) ;
#28058=CARTESIAN_POINT ( 'NONE',  ( -1.624989163556999772E-14, -74.69999999881999031, -11.09999999881999955 ) ) ;
#28061=DIRECTION ( 'NONE',  ( 0.07798810297990088625, -0.04890180925216059543, -0.9957542211035118607 ) ) ;
#28063=DIRECTION ( 'NONE',  ( 0.000000000000000000, 0.000000000000000000, -1.000000000000000000 ) ) ;
#28064=EDGE_LOOP ( 'NONE', ( #32975, #40932, #31512, #6080 ) ) ;
#28068=ORIENTED_EDGE ( 'NONE', *, *, #48882, .F. ) ;
#28069=DIRECTION ( 'NONE',  ( 0.000000000000000000, -1.000000000000000000, 0.000000000000000000 ) ) ;
#28072=CARTESIAN_POINT ( 'NONE',  ( 7.969039355710000549, -61.42377467811000002, 9.934746417661001416 ) ) ;
#28074=ADVANCED_FACE ( 'NONE', ( #15359 ), #24504, .F. ) ;
#28078=LINE ( 'NONE', #32791, #44412 ) ;
#28079=ORIENTED_EDGE ( 'NONE', *, *, #55001, .F. ) ;
#28082=FACE_OUTER_BOUND ( 'NONE', #41229, .T. ) ;
#28084=CARTESIAN_POINT ( 'NONE',  ( -8.813906588467560255, -16.98989792586478131, 8.872948313426432421 ) ) ;
#28085=CYLINDRICAL_SURFACE ( 'NONE', #24744, 0.5000000000000006661 ) ;
#28087=DIRECTION ( 'NONE',  ( 0.9999999999999994449, -3.428898372810997945E-08, -7.232769369940996221E-12 ) ) ;
#28088=CONICAL_SURFACE ( 'NONE', #55461, 3.699999993671000187, 0.7853981633972997312 ) ;
#28090=CARTESIAN_POINT ( 'NONE',  ( -8.870414880995999951, -25.06963060262999932, -8.878264461096000204 ) ) ;
#28094=ORIENTED_EDGE ( 'NONE', *, *, #10165, .T. ) ;
#28100=CARTESIAN_POINT ( 'NONE',  ( 8.485281374238999419, -55.64999999967000122, -8.485281374238999419 ) ) ;
#28101=CARTESIAN_POINT ( 'NONE',  ( -3.372337180869588558, -2.721983097397393081, 1.223328859044781503 ) ) ;
#28110=CARTESIAN_POINT ( 'NONE',  ( -7.674627477122999863, -19.24922971947000150, -10.14950121128000049 ) ) ;
#28113=CARTESIAN_POINT ( 'NONE',  ( 9.650948395506999233, -24.93402498662999989, -8.252474012539000370 ) ) ;
#28116=CARTESIAN_POINT ( 'NONE',  ( 2.842489150044962720, -1.893179537874919438, 1.637331356070920396 ) ) ;
#28117=CARTESIAN_POINT ( 'NONE',  ( 1.980584515752000119, -23.26485146623999967, -12.76303204602000108 ) ) ;
#28120=CARTESIAN_POINT ( 'NONE',  ( -1.828834964158999821, -79.10810244884000042, -12.81907926638999839 ) ) ;
#28121=B_SPLINE_SURFACE_WITH_KNOTS ( 'NONE', 3, 3, ( 
 ( #16119, #56849, #7253, #16408, #30546, #48293, #17559, #43860, #16985, #8406, #30830, #48864, #57423, #21978, #35253, #53284, #31111, #7832, #44142, #25832, #3408, #12830, #17862, #30252, #45021, #26403, #12547, #17263, #34967, #22575, #9002, #44425, #3976, #21406, #39418 ),
 ( #26121, #57708, #16698, #3690, #13117, #21692, #39989, #52998, #58003, #26987, #48579, #44725, #39700, #34679, #35551, #53579, #31413, #26693, #13414, #8121, #49152, #12260, #4575, #8703, #57132, #4278, #22274, #40290, #58301, #35851, #52708, #53881, #49456, #2115, #19823 ),
 ( #46995, #50039, #45614, #33670, #37814, #10679, #23156, #41161, #27570, #755, #28660, #29239, #28953, #45318, #6524, #10972, #24245, #11258, #18734, #56125, #4868, #49751, #184, #24535, #40876, #20115, #47286, #51708, #46708, #5155, #36728, #42547, #42261, #15086, #38105 ),
 ( #40587, #1827, #51126, #15386, #18158, #33082, #54742, #15673, #6814, #55836, #33381, #36152, #51417, #22867, #54169, #13709, #6229, #31704, #9294, #27282, #468, #18447, #36436, #54464, #14000, #31998, #9586, #6906, #56215, #51796, #51507, #55928, #47087, #1919, #2205 ) ),
 .UNSPECIFIED., .F., .F., .F.,
 ( 4, 4 ),
 ( 4, 1, 1, 1, 1, 1, 1, 1, 1, 1, 1, 1, 1, 1, 1, 1, 1, 1, 1, 1, 1, 1, 1, 1, 1, 1, 1, 1, 1, 1, 1, 1, 4 ),
 ( -0.3708084972812999980, 1.370808497280999960 ),
 ( -0.01035614953205000154, 0.006472593457530000441, 0.02330133644711000068, 0.04013007943667999677, 0.05695882242625999875, 0.07378756541584000073, 0.09061630840541999576, 0.1074450513949999908, 0.1242737943845999976, 0.1411025373741000011, 0.1579312803636999940, 0.1747600233533000147, 0.1915887663428999799, 0.2084175093325000006, 0.2252462523220000179, 0.2420749953115999831, 0.2589037383012000038, 0.2757324812907999689, 0.2925612242803000140, 0.3093899672698999792, 0.3262187102594999999, 0.3430474532491000206, 0.3598761962386999858, 0.3767049392282000309, 0.3935336822177999960, 0.4103624252073999612, 0.4271911681970000374, 0.4440199111864999715, 0.4608486541761000477, 0.4776773971657000128, 0.4945061401552999780, 0.5113348831447999121, 0.5281636261344000438 ),
 .UNSPECIFIED. ) ;
#28127=CARTESIAN_POINT ( 'NONE',  ( 0.000000000000000000, 0.000000000000000000, -10.40000000000006963 ) ) ;
#28128=DIRECTION ( 'NONE',  ( 0.000000000000000000, 1.000000000000000000, 0.000000000000000000 ) ) ;
#28130=AXIS2_PLACEMENT_3D ( 'NONE', #51462, #14835, #9844 ) ;
#28131=CARTESIAN_POINT ( 'NONE',  ( -7.730439324398687972, -54.67809618926516890, 10.25198230927261456 ) ) ;
#28132=ORIENTED_EDGE ( 'NONE', *, *, #9852, .T. ) ;
#28136=ORIENTED_EDGE ( 'NONE', *, *, #20316, .T. ) ;
#28139=ORIENTED_EDGE ( 'NONE', *, *, #14552, .T. ) ;
#28140=ORIENTED_EDGE ( 'NONE', *, *, #58078, .F. ) ;
#28141=CARTESIAN_POINT ( 'NONE',  ( 1.930009203935999951, -18.79900967682999635, 12.72537718777000038 ) ) ;
#28151=ORIENTED_EDGE ( 'NONE', *, *, #40608, .F. ) ;
#28156=CARTESIAN_POINT ( 'NONE',  ( -0.9356112518082062568, -17.25892169759421080, 12.50329130247410880 ) ) ;
#28159=CARTESIAN_POINT ( 'NONE',  ( -10.55910102242999926, -22.78485473281999774, 7.642147947518999729 ) ) ;
#28160=CARTESIAN_POINT ( 'NONE',  ( 11.60238327475000197, -76.61614726144999565, 5.404242916298000132 ) ) ;
#28163=EDGE_CURVE ( 'NONE', #13927, #31547, #11973, .T. ) ;
#28164=CARTESIAN_POINT ( 'NONE',  ( -9.380331153422687862, -76.64831997961195498, 7.077055143005254401 ) ) ;
#28172=CIRCLE ( 'NONE', #10289, 0.8000000000000000444 ) ;
#28173=DIRECTION ( 'NONE',  ( -1.000000000000000000, 0.000000000000000000, 0.000000000000000000 ) ) ;
#28175=DIRECTION ( 'NONE',  ( 0.000000000000000000, 0.000000000000000000, -1.000000000000000000 ) ) ;
#28177=CARTESIAN_POINT ( 'NONE',  ( 8.251802458185739653, -61.60055625091321474, 9.431055091036006033 ) ) ;
#28178=CARTESIAN_POINT ( 'NONE',  ( 8.190836719257466925, -59.98964892062851106, -7.342356150419175442 ) ) ;
#28184=CARTESIAN_POINT ( 'NONE',  ( -9.723199427802001082, -54.32306055813000256, 7.958735710007999842 ) ) ;
#28187=CARTESIAN_POINT ( 'NONE',  ( -1.750000000001000089, -18.74999999009000007, 12.56594317857000043 ) ) ;
#28190=CARTESIAN_POINT ( 'NONE',  ( 2.839805762151335511, -2.791666666666667407, 1.636761686205429278 ) ) ;
#28194=EDGE_CURVE ( 'NONE', #43036, #48350, #17085, .T. ) ;
#28204=ORIENTED_EDGE ( 'NONE', *, *, #9956, .T. ) ;
#28206=CARTESIAN_POINT ( 'NONE',  ( 8.190817883596542615, -60.03019609282340951, 7.342377162853137129 ) ) ;
#28208=ORIENTED_EDGE ( 'NONE', *, *, #27484, .F. ) ;
#28210=CARTESIAN_POINT ( 'NONE',  ( 0.000000000000000000, -46.43897132165000130, 0.000000000000000000 ) ) ;
#28213=CARTESIAN_POINT ( 'NONE',  ( -7.655542440077000244, -56.02180874340999850, 10.38645071868999992 ) ) ;
#28214=ORIENTED_EDGE ( 'NONE', *, *, #39753, .T. ) ;
#28215=ADVANCED_FACE ( 'NONE', ( #30930 ), #48832, .F. ) ;
#28220=DIRECTION ( 'NONE',  ( 1.000000000000000000, 0.000000000000000000, 0.000000000000000000 ) ) ;
#28222=CARTESIAN_POINT ( 'NONE',  ( -3.911457351643479186, -78.54938062601392801, -11.62361573341717857 ) ) ;
#28224=FACE_OUTER_BOUND ( 'NONE', #33430, .T. ) ;
#28226=CARTESIAN_POINT ( 'NONE',  ( -7.642147947533000085, -59.58485473249000108, -10.55910102243999837 ) ) ;
#28227=B_SPLINE_CURVE_WITH_KNOTS ( 'NONE', 3,
 ( #55584, #41424, #37569, #32539, #31668, #36985 ),
 .UNSPECIFIED., .F., .F.,
 ( 4, 2, 4 ),
 ( 0.000000000000000000, 0.5000000000000000000, 1.000000000000000000 ),
 .UNSPECIFIED. ) ;
#28230=CARTESIAN_POINT ( 'NONE',  ( 8.309590093900645513, -76.51194161182486653, 8.306937813281372485 ) ) ;
#28234=DIRECTION ( 'NONE',  ( 2.582635147408000164E-11, 0.000000000000000000, -1.000000000000000000 ) ) ;
#28235=CARTESIAN_POINT ( 'NONE',  ( 11.75000000000000000, -76.55000000000001137, 0.000000000000000000 ) ) ;
#28237=DIRECTION ( 'NONE',  ( 0.9999999999995751176, 0.000000000000000000, 9.217549097710770925E-07 ) ) ;
#28239=CARTESIAN_POINT ( 'NONE',  ( 13.13047446164998711, -56.01421830981000483, -0.8260994316375004365 ) ) ;
#28241=CARTESIAN_POINT ( 'NONE',  ( 0.5999999998848000171, -23.14999999478999726, 11.79999999988000070 ) ) ;
#28242=CARTESIAN_POINT ( 'NONE',  ( 12.70619440579097770, -24.46151788318003995, -1.571771935829441968 ) ) ;
#28243=CARTESIAN_POINT ( 'NONE',  ( -1.930628539545000022, -23.22124444086000139, -12.72375828104000028 ) ) ;
#28246=CARTESIAN_POINT ( 'NONE',  ( 12.77657007940999989, -25.31210281330999834, 0.1589025507404999982 ) ) ;
#28251=CARTESIAN_POINT ( 'NONE',  ( 1.886823409074000146, -60.56319684329000097, 12.68610076208999971 ) ) ;
#28253=CARTESIAN_POINT ( 'NONE',  ( -4.047764079874000664, -76.07042549139001153, 11.52168212187000051 ) ) ;
#28258=CARTESIAN_POINT ( 'NONE',  ( 7.624341764906000130, -55.53514850498000044, 10.42531124851000079 ) ) ;
#28260=CARTESIAN_POINT ( 'NONE',  ( 10.35453599130000057, -76.65783510652001098, -6.064947188958000446 ) ) ;
#28262=VECTOR ( 'NONE', #14482, 1000.000000000000000 ) ;
#28263=CARTESIAN_POINT ( 'NONE',  ( 0.000000000000000000, -55.54999999966999980, -12.50000000000000000 ) ) ;
#28267=EDGE_CURVE ( 'NONE', #21151, #44472, #27686, .T. ) ;
#28271=DIRECTION ( 'NONE',  ( 0.000000000000000000, 1.000000000000000000, 0.000000000000000000 ) ) ;
#28273=EDGE_CURVE ( 'NONE', #29770, #43853, #45138, .T. ) ;
#28277=ORIENTED_EDGE ( 'NONE', *, *, #36593, .T. ) ;
#28283=CARTESIAN_POINT ( 'NONE',  ( -10.00844281756000065, -55.43109810584000030, -7.647097920671999560 ) ) ;
#28286=ORIENTED_EDGE ( 'NONE', *, *, #23943, .F. ) ;
#28287=CARTESIAN_POINT ( 'NONE',  ( 12.57354471034999932, -55.07622323954000620, 1.757967544833999973 ) ) ;
#28288=DIRECTION ( 'NONE',  ( -0.9999999999999992228, 4.158392524217991108E-08, -7.899477153235985639E-12 ) ) ;
#28291=CARTESIAN_POINT ( 'NONE',  ( -12.77657007940999989, -25.31210281330999834, -0.1589025507404999982 ) ) ;
#28294=CARTESIAN_POINT ( 'NONE',  ( -1.318114156675707971, -17.26427522807030712, -12.70261578162816996 ) ) ;
#28299=CARTESIAN_POINT ( 'NONE',  ( -12.22985280536000019, -76.52641765524998618, -1.402219185755000153 ) ) ;
#28300=ADVANCED_FACE ( 'NONE', ( #50444 ), #27146, .F. ) ;
#28301=B_SPLINE_SURFACE_WITH_KNOTS ( 'NONE', 3, 3, ( 
 ( #41708, #14828, #32826, #22533 ),
 ( #9253, #8960, #44978, #40543 ),
 ( #18114, #36108, #45276, #46748 ),
 ( #5978, #6268, #52034, #47327 ),
 ( #46450, #24283, #6566, #20727 ),
 ( #37856, #47036, #1569, #29567 ),
 ( #15427, #16009, #29278, #19561 ),
 ( #42883, #38437, #38145, #42592 ),
 ( #24576, #6856, #2155, #55577 ),
 ( #56454, #38725, #56746, #47623 ),
 ( #33421, #15126, #10417, #28995 ),
 ( #7146, #24865, #25148, #23984 ),
 ( #20156, #33124, #16306, #42001 ),
 ( #56167, #1867, #11011, #51166 ),
 ( #50871, #15715, #33709, #10720 ),
 ( #51748, #55877, #19861, #51458 ),
 ( #11298, #2440, #20442, #33996 ) ),
 .UNSPECIFIED., .F., .F., .F.,
 ( 4, 1, 1, 1, 1, 1, 1, 1, 1, 1, 1, 1, 1, 1, 4 ),
 ( 4, 4 ),
 ( -0.01011408452875999994, 0.000000000000000000, 0.08333333333333001192, 0.1666666666667000196, 0.2500000000000000000, 0.3333333333333000081, 0.4166666666666999919, 0.5000000000000000000, 0.5833333333333000637, 0.6666666666667000474, 0.7500000000000000000, 0.8333333333333000637, 0.9166666666667000474, 1.000000000000000000, 1.010362559108000102 ),
 ( -0.3559705546268999710, 1.357612419623000166 ),
 .UNSPECIFIED. ) ;
#28303=CARTESIAN_POINT ( 'NONE',  ( -12.69999999999999929, 0.000000000000000000, 0.000000000000000000 ) ) ;
#28304=CARTESIAN_POINT ( 'NONE',  ( 7.646788277353000041, -60.17228598344999568, -10.00831419132999933 ) ) ;
#28305=CARTESIAN_POINT ( 'NONE',  ( -5.950798862880000151, -78.93264987601000371, 10.72320280238000123 ) ) ;
#28308=CARTESIAN_POINT ( 'NONE',  ( 9.546819346760999636, -61.48527546573999558, -8.130850182902999990 ) ) ;
#28309=CARTESIAN_POINT ( 'NONE',  ( -1.770201408374824092, -78.16324107959532341, -11.94606885956166842 ) ) ;
#28310=CARTESIAN_POINT ( 'NONE',  ( 0.000000000000000000, 4.040000000000000036, 0.000000000000000000 ) ) ;
#28311=ORIENTED_EDGE ( 'NONE', *, *, #36363, .F. ) ;
#28313=CARTESIAN_POINT ( 'NONE',  ( 3.075537641221555596, -77.94583333333332575, -11.44417895085270587 ) ) ;
#28314=CARTESIAN_POINT ( 'NONE',  ( -1.750000000001000089, -55.55000001292999912, -12.56594318049000059 ) ) ;
#28316=CARTESIAN_POINT ( 'NONE',  ( -3.370529087814999603, -2.253484528251000096, 1.902593404626000018 ) ) ;
#28319=EDGE_CURVE ( 'NONE', #15053, #33154, #44965, .T. ) ;
#28320=CARTESIAN_POINT ( 'NONE',  ( -10.80861225507516821, -76.16775967368776890, 4.608194527468379320 ) ) ;
#28323=ORIENTED_EDGE ( 'NONE', *, *, #15507, .F. ) ;
#28328=CIRCLE ( 'NONE', #54732, 14.00000000000000000 ) ;
#28330=CARTESIAN_POINT ( 'NONE',  ( -0.4254240051736286610, -2.385416666666666075, 3.249999999999997780 ) ) ;
#28334=CARTESIAN_POINT ( 'NONE',  ( 10.18114972182000066, -18.60990354280999881, -7.633087078986000584 ) ) ;
#28335=CARTESIAN_POINT ( 'NONE',  ( 8.096452064242996016, -59.58578169018998949, -13.15643568217000769 ) ) ;
#28337=FACE_OUTER_BOUND ( 'NONE', #29521, .T. ) ;
#28339=CARTESIAN_POINT ( 'NONE',  ( -14.00000000000000000, -45.89236309322999574, -1.352041732758999914E-05 ) ) ;
#28340=CARTESIAN_POINT ( 'NONE',  ( -5.581034037647778057, -77.86612145202063573, 10.76842700904854411 ) ) ;
#28344=B_SPLINE_CURVE_WITH_KNOTS ( 'NONE', 3,
 ( #28954, #3263, #25394, #37815, #24536, #42549 ),
 .UNSPECIFIED., .F., .F.,
 ( 4, 1, 1, 4 ),
 ( 0.000000000000000000, 0.3333333333333000081, 0.6666666666667000474, 0.9999998688569219363 ),
 .UNSPECIFIED. ) ;
#28346=AXIS2_PLACEMENT_3D ( 'NONE', #5617, #4464, #4755 ) ;
#28348=CARTESIAN_POINT ( 'NONE',  ( -8.179400486886379440, -17.25908162456390471, -9.502921779309215111 ) ) ;
#28352=B_SPLINE_SURFACE_WITH_KNOTS ( 'NONE', 3, 3, ( 
 ( #27230, #36389, #48526, #4818 ),
 ( #49102, #53233, #8071, #30779 ),
 ( #26067, #22817, #21927, #4525 ),
 ( #44969, #3642, #21645, #39652 ),
 ( #17213, #57952, #17810, #35201 ),
 ( #17506, #53526, #44673, #22224 ),
 ( #40235, #58249, #35796, #53826 ),
 ( #8952, #31359, #49403, #14533 ) ),
 .UNSPECIFIED., .F., .F., .F.,
 ( 4, 1, 1, 1, 1, 4 ),
 ( 4, 4 ),
 ( -0.01200407347463999970, 0.000000000000000000, 0.3333333333333000081, 0.6666666666667000474, 1.000000000000000000, 1.011997855551999947 ),
 ( -0.3559705542741999906, 1.355970554273999928 ),
 .UNSPECIFIED. ) ;
#28354=EDGE_CURVE ( 'NONE', #40118, #6488, #12364, .T. ) ;
#28355=CARTESIAN_POINT ( 'NONE',  ( 3.250000000000000000, -1.750000000000000000, 0.000000000000000000 ) ) ;
#28356=ORIENTED_EDGE ( 'NONE', *, *, #7484, .F. ) ;
#28360=VERTEX_POINT ( 'NONE', #5870 ) ;
#28361=CARTESIAN_POINT ( 'NONE',  ( -1.250000000000000000, -18.75000000000000000, -12.00000000000000000 ) ) ;
#28363=CARTESIAN_POINT ( 'NONE',  ( 9.389195554442999025, -61.51043214172000262, 8.194863653299998774 ) ) ;
#28368=ORIENTED_EDGE ( 'NONE', *, *, #4311, .F. ) ;
#28369=CARTESIAN_POINT ( 'NONE',  ( -7.624341764926000131, -23.26485149464000202, 10.42531124853000080 ) ) ;
#28370=AXIS2_PLACEMENT_3D ( 'NONE', #23211, #523, #22631 ) ;
#28371=ORIENTED_EDGE ( 'NONE', *, *, #15370, .F. ) ;
#28374=FACE_OUTER_BOUND ( 'NONE', #51485, .T. ) ;
#28378=CARTESIAN_POINT ( 'NONE',  ( 1.788035749175998834, -2.171010677132999334, -2.743726783948167380 ) ) ;
#28382=CARTESIAN_POINT ( 'NONE',  ( -7.606021324597999289, -23.42158946275000275, -10.52692925327000140 ) ) ;
#28383=CARTESIAN_POINT ( 'NONE',  ( 12.75763395697999947, -59.57795407677000554, -1.931043742978000077 ) ) ;
#28385=VERTEX_POINT ( 'NONE', #14721 ) ;
#28391=CARTESIAN_POINT ( 'NONE',  ( -8.533817832784000856, -16.99473856456000220, 9.213092693308000847 ) ) ;
#28394=CARTESIAN_POINT ( 'NONE',  ( 0.6142349777637159391, -3.110991548698613496, 3.465482938499039545 ) ) ;
#28398=EDGE_CURVE ( 'NONE', #19870, #23895, #5990, .T. ) ;
#28402=VERTEX_POINT ( 'NONE', #51348 ) ;
#28407=CARTESIAN_POINT ( 'NONE',  ( -12.80090744918999945, -22.76232687447999936, 1.980532734072999901 ) ) ;
#28409=CARTESIAN_POINT ( 'NONE',  ( 1.996168837740194935, -1.924424498446639209, 2.598685398968098248 ) ) ;
#28410=CARTESIAN_POINT ( 'NONE',  ( -7.610436392397138761, -55.27459049263858759, -10.41144384037119153 ) ) ;
#28413=EDGE_CURVE ( 'NONE', #22110, #29384, #32718, .T. ) ;
#28414=CARTESIAN_POINT ( 'NONE',  ( 11.00823205989000009, -78.70025095962000705, -6.817946738202000034 ) ) ;
#28419=CARTESIAN_POINT ( 'NONE',  ( -1.980584515752000119, -60.06485146591000301, 12.76303204605000197 ) ) ;
#28423=CARTESIAN_POINT ( 'NONE',  ( -5.869402599192000025, -78.46567021303999923, 10.46661899222999992 ) ) ;
#28429=EDGE_CURVE ( 'NONE', #11038, #19532, #56265, .T. ) ;
#28431=DIRECTION ( 'NONE',  ( -1.000000000000000000, 0.000000000000000000, 0.000000000000000000 ) ) ;
#28433=ORIENTED_EDGE ( 'NONE', *, *, #52693, .T. ) ;
#28436=CARTESIAN_POINT ( 'NONE',  ( 7.624341764926000131, -23.26485149464000202, -10.42531124853000080 ) ) ;
#28439=CARTESIAN_POINT ( 'NONE',  ( 1.798368564625000054, -18.80363242954000214, 12.61278090841000044 ) ) ;
#28440=CYLINDRICAL_SURFACE ( 'NONE', #53737, 3.250000000000000000 ) ;
#28445=CARTESIAN_POINT ( 'NONE',  ( -10.07627163191000008, -55.55000000209000177, 7.601397897754999633 ) ) ;
#28450=LINE ( 'NONE', #27862, #30789 ) ;
#28454=DIRECTION ( 'NONE',  ( 0.000000000000000000, -1.000000000000000000, 0.000000000000000000 ) ) ;
#28461=CARTESIAN_POINT ( 'NONE',  ( -10.18948933931000234, -55.58467389893999666, 7.645397892281000196 ) ) ;
#28464=CARTESIAN_POINT ( 'NONE',  ( -7.618394506893999996, -18.77286435802000142, -10.53494428259999971 ) ) ;
#28469=DIRECTION ( 'NONE',  ( 0.000000000000000000, -1.000000000000000000, 0.000000000000000000 ) ) ;
#28471=VERTEX_POINT ( 'NONE', #56350 ) ;
#28472=CARTESIAN_POINT ( 'NONE',  ( 9.505949683908001546, -79.00000000000000000, -6.906476714433999575 ) ) ;
#28474=CARTESIAN_POINT ( 'NONE',  ( 5.918882701593904727, -77.53100531885093005, 10.27291346163489827 ) ) ;
#28475=CARTESIAN_POINT ( 'NONE',  ( 12.77297283019000140, -61.52822696498000710, -1.476112654660999723 ) ) ;
#28477=CONICAL_SURFACE ( 'NONE', #21853, 13.94999999959000014, 0.7853981633972997312 ) ;
#28478=CARTESIAN_POINT ( 'NONE',  ( -9.287618194362000423, -77.50975265977999129, -9.114789584104999065 ) ) ;
#28480=CARTESIAN_POINT ( 'NONE',  ( 0.7999999999999001243, -18.84999999997999964, 12.00000000000000000 ) ) ;
#28482=DIRECTION ( 'NONE',  ( -0.009503199022040095811, 0.000000000000000000, 0.9999548435846228323 ) ) ;
#28487=DIRECTION ( 'NONE',  ( -0.7071067811865474617, 0.000000000000000000, 0.7071067811865474617 ) ) ;
#28494=DIRECTION ( 'NONE',  ( 0.000000000000000000, 1.000000000000000000, 0.000000000000000000 ) ) ;
#28495=VECTOR ( 'NONE', #17685, 1000.000000000000000 ) ;
#28497=EDGE_LOOP ( 'NONE', ( #40655, #31178, #48065, #11838 ) ) ;
#28501=CYLINDRICAL_SURFACE ( 'NONE', #20899, 12.50000000000000000 ) ;
#28502=ORIENTED_EDGE ( 'NONE', *, *, #9972, .T. ) ;
#28504=ORIENTED_EDGE ( 'NONE', *, *, #20260, .T. ) ;
#28505=ORIENTED_EDGE ( 'NONE', *, *, #25016, .T. ) ;
#28509=CARTESIAN_POINT ( 'NONE',  ( 10.45204383628000144, -56.03743350618999841, 7.651147548114000330 ) ) ;
#28510=B_SPLINE_CURVE_WITH_KNOTS ( 'NONE', 3,
 ( #14685, #29139, #19133, #37128, #28844, #32395 ),
 .UNSPECIFIED., .F., .F.,
 ( 4, 2, 4 ),
 ( 0.000000000000000000, 0.5000000000000000000, 1.000000000000000000 ),
 .UNSPECIFIED. ) ;
#28513=CARTESIAN_POINT ( 'NONE',  ( -7.668936932630000314, -56.02847221959000024, 10.21380041493999968 ) ) ;
#28514=ORIENTED_EDGE ( 'NONE', *, *, #44103, .F. ) ;
#28520=CARTESIAN_POINT ( 'NONE',  ( -1.307248514406967876, -79.06671355138394119, -12.19422169117518173 ) ) ;
#28527=CARTESIAN_POINT ( 'NONE',  ( 4.546247888304588258, -76.54303117012038626, 10.83464402558239037 ) ) ;
#28531=CARTESIAN_POINT ( 'NONE',  ( 1.001315002657000131, -61.48522411647999775, -12.50000000000000000 ) ) ;
#28539=CARTESIAN_POINT ( 'NONE',  ( 0.000000000000000000, -2.900000000000000355, 0.000000000000000000 ) ) ;
#28543=CARTESIAN_POINT ( 'NONE',  ( 12.74331206681030793, -23.52649290803818616, -1.980611467279665305 ) ) ;
#28547=FACE_OUTER_BOUND ( 'NONE', #34247, .T. ) ;
#28551=CARTESIAN_POINT ( 'NONE',  ( 8.894005208714999000, -76.35846261908999111, -8.368406312348000142 ) ) ;
#28552=ORIENTED_EDGE ( 'NONE', *, *, #52260, .F. ) ;
#28555=EDGE_CURVE ( 'NONE', #14936, #31290, #21479, .T. ) ;
#28559=CARTESIAN_POINT ( 'NONE',  ( 9.998727717461520115, -23.92738947620295065, -7.709134076961339233 ) ) ;
#28563=CARTESIAN_POINT ( 'NONE',  ( -8.414570695956999913, -59.94999999967000548, -8.414570695956999913 ) ) ;
#28565=ORIENTED_EDGE ( 'NONE', *, *, #22726, .T. ) ;
#28568=DIRECTION ( 'NONE',  ( 0.6489586469528968449, -0.04890178981565979077, -0.7592504787603958638 ) ) ;
#28571=AXIS2_PLACEMENT_3D ( 'NONE', #25891, #43918, #3464 ) ;
#28572=ADVANCED_FACE ( 'NONE', ( #39487 ), #25328, .F. ) ;
#28573=CARTESIAN_POINT ( 'NONE',  ( 10.42531125074000009, -18.73514854687000053, 7.624341767140999870 ) ) ;
#28574=ORIENTED_EDGE ( 'NONE', *, *, #35443, .T. ) ;
#28577=DIRECTION ( 'NONE',  ( -0.4045837979900098746, 0.8201365135195225475, -0.4045837979900098746 ) ) ;
#28578=ORIENTED_EDGE ( 'NONE', *, *, #29087, .F. ) ;
#28579=ORIENTED_EDGE ( 'NONE', *, *, #28398, .T. ) ;
#28585=ORIENTED_EDGE ( 'NONE', *, *, #15251, .F. ) ;
#28586=CARTESIAN_POINT ( 'NONE',  ( 12.66737112512999985, -54.56697834100999955, 1.690666607834999891 ) ) ;
#28587=CARTESIAN_POINT ( 'NONE',  ( 9.697372265328400687, -24.97233735039882063, -8.266620275706634047 ) ) ;
#28589=CARTESIAN_POINT ( 'NONE',  ( -12.77651047016999897, -25.30895689136000115, 0.04321256188109000307 ) ) ;
#28591=CARTESIAN_POINT ( 'NONE',  ( -12.00000000000000000, -60.04999999966999980, 0.000000000000000000 ) ) ;
#28593=CARTESIAN_POINT ( 'NONE',  ( -1.217390015621637067, -17.18106975071298237, -12.70229597940931399 ) ) ;
#28594=CARTESIAN_POINT ( 'NONE',  ( -12.70395600760253352, -17.39327811307525451, -1.447166682405202298 ) ) ;
#28597=CARTESIAN_POINT ( 'NONE',  ( 1.623944433304999935, -76.11819529704000331, -12.20239005717999881 ) ) ;
#28599=EDGE_CURVE ( 'NONE', #14715, #54222, #43636, .T. ) ;
#28601=CARTESIAN_POINT ( 'NONE',  ( 10.18949719147000010, -60.01529250184999853, -7.645392405676999736 ) ) ;
#28602=CARTESIAN_POINT ( 'NONE',  ( -5.531768889155999958, -79.13976085113000636, -10.94525552207000096 ) ) ;
#28604=CARTESIAN_POINT ( 'NONE',  ( 12.70228859454079817, -17.17803615246131699, -1.213484947661823909 ) ) ;
#28606=CARTESIAN_POINT ( 'NONE',  ( 12.50657368821661741, -24.97245458995924849, 0.3553454087122077110 ) ) ;
#28607=CARTESIAN_POINT ( 'NONE',  ( 10.49970183384550637, -78.34114056985468721, 5.963879664039239969 ) ) ;
#28609=CIRCLE ( 'NONE', #21991, 9.000000000000000000 ) ;
#28611=ORIENTED_EDGE ( 'NONE', *, *, #41967, .T. ) ;
#28616=CARTESIAN_POINT ( 'NONE',  ( 1.712913800556999933, -3.546465114847999978, -3.088999176916999989 ) ) ;
#28619=CARTESIAN_POINT ( 'NONE',  ( -8.304425937606323416, -76.13746526952284910, 8.312567492877647624 ) ) ;
#28624=CARTESIAN_POINT ( 'NONE',  ( 12.71162862750088429, -24.23964265628594106, 1.720599174827327271 ) ) ;
#28626=CARTESIAN_POINT ( 'NONE',  ( -8.414570695956999913, -55.64999999967000122, -8.414570695956999913 ) ) ;
#28628=DIRECTION ( 'NONE',  ( 0.000000000000000000, -1.000000000000000000, 0.000000000000000000 ) ) ;
#28632=CARTESIAN_POINT ( 'NONE',  ( 7.943801774166999508, -17.56598212471000053, -9.641153612788999183 ) ) ;
#28633=CARTESIAN_POINT ( 'NONE',  ( -8.096452064242996016, -56.01421830980998351, -13.15643568217000769 ) ) ;
#28634=VERTEX_POINT ( 'NONE', #43345 ) ;
#28639=CARTESIAN_POINT ( 'NONE',  ( -11.27280967271781797, -77.92393960097702177, 4.319288305624113811 ) ) ;
#28641=ADVANCED_FACE ( 'NONE', ( #2901 ), #26660, .F. ) ;
#28643=CARTESIAN_POINT ( 'NONE',  ( -12.50745077485999879, -53.80005551680000053, 2.011910316382000212E-09 ) ) ;
#28644=CARTESIAN_POINT ( 'NONE',  ( -9.298479816475497373, -17.11187382770906495, -8.385858173857444697 ) ) ;
#28645=EDGE_CURVE ( 'NONE', #28865, #33521, #14454, .T. ) ;
#28649=AXIS2_PLACEMENT_3D ( 'NONE', #1008, #42601, #50881 ) ;
#28651=VERTEX_POINT ( 'NONE', #44211 ) ;
#28655=EDGE_LOOP ( 'NONE', ( #44140, #8321, #25688 ) ) ;
#28657=CARTESIAN_POINT ( 'NONE',  ( 7.631896578932000352, -18.77877526479000281, 10.36221705164000184 ) ) ;
#28659=DIRECTION ( 'NONE',  ( 0.000000000000000000, -1.000000000000000000, 0.000000000000000000 ) ) ;
#28660=CARTESIAN_POINT ( 'NONE',  ( 4.671825910118999836, -78.48810965511999882, -11.12032239270999945 ) ) ;
#28661=CARTESIAN_POINT ( 'NONE',  ( 10.13402523426999835, -60.52303809408999768, 7.647751776506999555 ) ) ;
#28665=EDGE_LOOP ( 'NONE', ( #35170, #28214, #53623, #12503 ) ) ;
#28671=CARTESIAN_POINT ( 'NONE',  ( -9.998734510784624163, -18.07263061081724942, -7.709128441133644927 ) ) ;
#28674=ADVANCED_FACE ( 'NONE', ( #40951 ), #39766, .F. ) ;
#28676=CARTESIAN_POINT ( 'NONE',  ( 12.71005379442530980, -61.09489531493035486, 1.687596142995509974 ) ) ;
#28678=CARTESIAN_POINT ( 'NONE',  ( 12.69619287811999797, -58.55083378327000077, -1.799475295154000065 ) ) ;
#28680=EDGE_LOOP ( 'NONE', ( #41575, #24162, #39120, #11331 ) ) ;
#28685=CARTESIAN_POINT ( 'NONE',  ( -9.621742410712839089, -54.17938299872298558, 8.060146970971464597 ) ) ;
#28686=CIRCLE ( 'NONE', #53183, 12.05000000000000071 ) ;
#28688=CARTESIAN_POINT ( 'NONE',  ( 2.965694224434944903, -3.454766459150870439, -1.895013073882325205 ) ) ;
#28689=DIRECTION ( 'NONE',  ( 0.000000000000000000, 0.000000000000000000, 1.000000000000000000 ) ) ;
#28693=DIRECTION ( 'NONE',  ( -1.000000000000000000, 0.000000000000000000, 0.000000000000000000 ) ) ;
#28695=ORIENTED_EDGE ( 'NONE', *, *, #22742, .T. ) ;
#28697=CIRCLE ( 'NONE', #3251, 0.5000000000000004441 ) ;
#28698=CARTESIAN_POINT ( 'NONE',  ( -11.75162232059617295, -78.71241119902158800, -1.843960194169528943 ) ) ;
#28702=CARTESIAN_POINT ( 'NONE',  ( 7.633089125616000281, -23.39007426303999893, -10.18115018432999896 ) ) ;
#28705=DIRECTION ( 'NONE',  ( 0.000000000000000000, 1.000000000000000000, 0.000000000000000000 ) ) ;
#28710=CARTESIAN_POINT ( 'NONE',  ( 7.956418361354000268, -54.27110680110000374, -9.787952249823998585 ) ) ;
#28716=CARTESIAN_POINT ( 'NONE',  ( -13.94241845804000057, -32.46002936525999871, -4.312607201059000272E-05 ) ) ;
#28719=DIRECTION ( 'NONE',  ( 0.000000000000000000, -1.000000000000000000, 0.000000000000000000 ) ) ;
#28720=ORIENTED_EDGE ( 'NONE', *, *, #54655, .T. ) ;
#28724=LINE ( 'NONE', #1312, #52548 ) ;
#28725=ORIENTED_EDGE ( 'NONE', *, *, #46673, .T. ) ;
#28726=ORIENTED_EDGE ( 'NONE', *, *, #39380, .F. ) ;
#28728=TOROIDAL_SURFACE ( 'NONE', #9909, 1.250000000000000000, 0.5000000000000000000 ) ;
#28729=ORIENTED_EDGE ( 'NONE', *, *, #23694, .T. ) ;
#28731=CARTESIAN_POINT ( 'NONE',  ( 0.005119011380136999703, -17.06186137810999881, 12.43705489344000092 ) ) ;
#28732=LINE ( 'NONE', #6600, #16910 ) ;
#28738=DIRECTION ( 'NONE',  ( 0.000000000000000000, -1.000000000000000000, 0.000000000000000000 ) ) ;
#28739=ORIENTED_EDGE ( 'NONE', *, *, #372, .T. ) ;
#28743=CARTESIAN_POINT ( 'NONE',  ( 1.811016405462491541, -60.86173555339116348, -12.71771640067482601 ) ) ;
#28745=CARTESIAN_POINT ( 'NONE',  ( 0.000000000000000000, -23.15000000000000213, 12.00000000000000000 ) ) ;
#28751=CARTESIAN_POINT ( 'NONE',  ( -8.064342063058008492, -76.63498362770486949, 8.546452962956790245 ) ) ;
#28756=FACE_OUTER_BOUND ( 'NONE', #22562, .T. ) ;
#28758=CARTESIAN_POINT ( 'NONE',  ( 0.5390150933986999071, -16.73739108348000215, -12.77520261005000002 ) ) ;
#28760=FACE_OUTER_BOUND ( 'NONE', #15, .T. ) ;
#28761=EDGE_CURVE ( 'NONE', #27335, #27676, #17569, .T. ) ;
#28763=FACE_OUTER_BOUND ( 'NONE', #18511, .T. ) ;
#28765=CARTESIAN_POINT ( 'NONE',  ( 9.102117851719468078, -61.77186524099414555, 8.583692175706325145 ) ) ;
#28767=DIRECTION ( 'NONE',  ( 0.000000000000000000, -1.000000000000000000, 0.000000000000000000 ) ) ;
#28770=AXIS2_PLACEMENT_3D ( 'NONE', #16996, #39133, #4286 ) ;
#28772=DIRECTION ( 'NONE',  ( 0.000000000000000000, -1.000000000000000000, 0.000000000000000000 ) ) ;
#28773=DIRECTION ( 'NONE',  ( 0.000000000000000000, 1.000000000000000000, 0.000000000000000000 ) ) ;
#28779=CARTESIAN_POINT ( 'NONE',  ( -1.489949360950307389, -76.31481021185051361, -11.66158060881517855 ) ) ;
#28784=CARTESIAN_POINT ( 'NONE',  ( -11.75000000000000000, -76.30000000000001137, 1.487410190129999909E-14 ) ) ;
#28791=ORIENTED_EDGE ( 'NONE', *, *, #44976, .F. ) ;
#28793=CARTESIAN_POINT ( 'NONE',  ( -12.50745077494999968, -61.79994448255000350, -2.661703094427999907E-09 ) ) ;
#28794=CARTESIAN_POINT ( 'NONE',  ( -10.07627163191000008, -60.04999999657000131, 7.601397897754999633 ) ) ;
#28795=VERTEX_POINT ( 'NONE', #19035 ) ;
#28797=ORIENTED_EDGE ( 'NONE', *, *, #8092, .T. ) ;
#28799=CARTESIAN_POINT ( 'NONE',  ( 8.150146600852364642, -60.21532333328941178, 7.387512494710262168 ) ) ;
#28804=CARTESIAN_POINT ( 'NONE',  ( 0.000000000000000000, 0.000000000000000000, -8.800000000000000711 ) ) ;
#28805=EDGE_LOOP ( 'NONE', ( #2437, #17677, #17036, #39618 ) ) ;
#28806=CARTESIAN_POINT ( 'NONE',  ( -7.640030139739999449, -55.49283065365000311, 10.18491068058999893 ) ) ;
#28815=CYLINDRICAL_SURFACE ( 'NONE', #53173, 12.05000000000000071 ) ;
#28816=ADVANCED_FACE ( 'NONE', ( #45328 ), #9747, .F. ) ;
#28819=CARTESIAN_POINT ( 'NONE',  ( 8.318733234480337302, -76.51185634578514794, 8.297783748491672995 ) ) ;
#28822=CARTESIAN_POINT ( 'NONE',  ( -2.531016240223846303, -3.046284654864954700, 2.042466395675148316 ) ) ;
#28827=DIRECTION ( 'NONE',  ( -0.7071067811864976127, 0.7071067811865975328, 1.047747575656995313E-09 ) ) ;
#28828=CARTESIAN_POINT ( 'NONE',  ( -8.080493018338632538, -76.26413923100619741, -8.538429872746517546 ) ) ;
#28830=CARTESIAN_POINT ( 'NONE',  ( -10.18114973714999927, -60.19009320380000361, -7.633087466122999487 ) ) ;
#28836=CARTESIAN_POINT ( 'NONE',  ( -7.635227771886311743, -23.76609606960563070, -10.36745004610104637 ) ) ;
#28838=CARTESIAN_POINT ( 'NONE',  ( 1.750000000001000089, -60.05000000958000328, 12.56594317859000043 ) ) ;
#28840=CARTESIAN_POINT ( 'NONE',  ( 1.396436198717000199, -76.03442085042999565, 12.13192147124999920 ) ) ;
#28841=ORIENTED_EDGE ( 'NONE', *, *, #26091, .T. ) ;
#28844=CARTESIAN_POINT ( 'NONE',  ( -7.850068285607218144, -17.68530314558974581, -9.837745660718102414 ) ) ;
#28847=CARTESIAN_POINT ( 'NONE',  ( -2.062673488738000049, -18.67547470641000018, -12.82904091339000097 ) ) ;
#28851=CARTESIAN_POINT ( 'NONE',  ( 0.000000000000000000, -9.638971321655001034, 0.000000000000000000 ) ) ;
#28853=ORIENTED_EDGE ( 'NONE', *, *, #26277, .F. ) ;
#28855=LINE ( 'NONE', #1734, #4948 ) ;
#28857=CONICAL_SURFACE ( 'NONE', #20397, 13.94999999959000014, 0.7853981633972997312 ) ;
#28858=ORIENTED_EDGE ( 'NONE', *, *, #25049, .T. ) ;
#28859=CIRCLE ( 'NONE', #2503, 1.749999999999999334 ) ;
#28862=CARTESIAN_POINT ( 'NONE',  ( 0.000000000000000000, -72.89999999999999147, 0.000000000000000000 ) ) ;
#28865=VERTEX_POINT ( 'NONE', #11919 ) ;
#28875=ORIENTED_EDGE ( 'NONE', *, *, #58265, .T. ) ;
#28876=CARTESIAN_POINT ( 'NONE',  ( 12.54902617714999913, -53.79030198112999273, 0.4617931494615999943 ) ) ;
#28878=VERTEX_POINT ( 'NONE', #37903 ) ;
#28879=CARTESIAN_POINT ( 'NONE',  ( -12.54981857173999948, -25.04836586201999893, 0.03768635776136999849 ) ) ;
#28885=EDGE_CURVE ( 'NONE', #35553, #38791, #4467, .T. ) ;
#28886=CARTESIAN_POINT ( 'NONE',  ( 0.000000000000000000, -15.06282895647999887, 0.000000000000000000 ) ) ;
#28890=EDGE_CURVE ( 'NONE', #36778, #800, #55985, .T. ) ;
#28891=CARTESIAN_POINT ( 'NONE',  ( -7.685416442687999172, -76.55401027050999119, -9.616126112745998711 ) ) ;
#28895=CARTESIAN_POINT ( 'NONE',  ( 9.641208724103000449, -61.23394297667999808, -7.943747389727000119 ) ) ;
#28896=CARTESIAN_POINT ( 'NONE',  ( -1.307210027570999911, -79.09916823586999612, -12.19386267984000050 ) ) ;
#28900=DIRECTION ( 'NONE',  ( 0.000000000000000000, -1.000000000000000000, 0.000000000000000000 ) ) ;
#28901=CARTESIAN_POINT ( 'NONE',  ( -3.099413287474135803, -78.15434610508248170, -11.66500092276903011 ) ) ;
#28902=CARTESIAN_POINT ( 'NONE',  ( 5.694538069269999623E-14, -72.84999999994899156, 0.000000000000000000 ) ) ;
#28904=ORIENTED_EDGE ( 'NONE', *, *, #40886, .F. ) ;
#28906=DIRECTION ( 'NONE',  ( 0.9859154929576978699, -0.1672442547472993701, 2.241733975738995337E-11 ) ) ;
#28907=PLANE ( 'NONE',  #39844 ) ;
#28908=VECTOR ( 'NONE', #54810, 1000.000000000000000 ) ;
#28910=CARTESIAN_POINT ( 'NONE',  ( -1.791942608155000061, -1.881074315393999941, -3.430764814325999890 ) ) ;
#28913=CARTESIAN_POINT ( 'NONE',  ( -9.653806611548578331, -76.15120867658298209, 6.697802937877729512 ) ) ;
#28914=CARTESIAN_POINT ( 'NONE',  ( 10.12290050253000118, -23.24999997822999731, -7.648026768374000639 ) ) ;
#28918=DIRECTION ( 'NONE',  ( 0.000000000000000000, 1.000000000000000000, 1.048986614577000002E-10 ) ) ;
#28925=DIRECTION ( 'NONE',  ( 1.000000000000000000, 0.000000000000000000, 0.000000000000000000 ) ) ;
#28926=CARTESIAN_POINT ( 'NONE',  ( 0.000000000000000000, -52.49705297114005020, -12.53545825868000207 ) ) ;
#28927=EDGE_LOOP ( 'NONE', ( #48920, #44910, #44851 ) ) ;
#28929=LINE ( 'NONE', #38082, #37093 ) ;
#28932=CARTESIAN_POINT ( 'NONE',  ( 2.320007599203503634, -77.81275085298281624, 11.90349632493328613 ) ) ;
#28937=CARTESIAN_POINT ( 'NONE',  ( -8.130811096542000627, -24.68523690389000080, -9.546858433121998999 ) ) ;
#28938=EDGE_CURVE ( 'NONE', #308, #38673, #24229, .T. ) ;
#28939=CARTESIAN_POINT ( 'NONE',  ( 0.000000000000000000, -2.949999999935999817, 0.000000000000000000 ) ) ;
#28940=CARTESIAN_POINT ( 'NONE',  ( -12.49168433577000137, -55.50150862742999891, 1.667916687244999974 ) ) ;
#28941=VECTOR ( 'NONE', #29413, 1000.000000000000227 ) ;
#28945=CIRCLE ( 'NONE', #56316, 1.750000000000000000 ) ;
#28946=ORIENTED_EDGE ( 'NONE', *, *, #19789, .F. ) ;
#28950=ORIENTED_EDGE ( 'NONE', *, *, #28398, .F. ) ;
#28951=CARTESIAN_POINT ( 'NONE',  ( 8.596775676242998543, -16.86467110163999905, 9.310147894694001280 ) ) ;
#28953=CARTESIAN_POINT ( 'NONE',  ( 10.85716400461000042, -78.54559109126999772, -5.254475923155999872 ) ) ;
#28954=CARTESIAN_POINT ( 'NONE',  ( 14.00000000000000000, -32.88214388149999934, 0.000000000000000000 ) ) ;
#28955=LINE ( 'NONE', #16262, #49437 ) ;
#28961=EDGE_CURVE ( 'NONE', #48419, #2165, #22208, .T. ) ;
#28964=PLANE ( 'NONE',  #16822 ) ;
#28966=DIRECTION ( 'NONE',  ( 0.7071067811864981678, 0.000000000000000000, 0.7071067811865970887 ) ) ;
#28968=DIRECTION ( 'NONE',  ( 0.000000000000000000, 1.000000000000000000, 0.000000000000000000 ) ) ;
#28979=CARTESIAN_POINT ( 'NONE',  ( 9.723174507645000020, -61.27697503925999456, 7.958760295356000825 ) ) ;
#28980=EDGE_CURVE ( 'NONE', #23138, #42100, #45427, .T. ) ;
#28982=CARTESIAN_POINT ( 'NONE',  ( -8.950130560568000604, -16.79887407354000217, 8.958576480220999727 ) ) ;
#28985=CARTESIAN_POINT ( 'NONE',  ( -0.8622078521763266723, -3.355252669283040667, -3.415065585293687533 ) ) ;
#28988=CARTESIAN_POINT ( 'NONE',  ( 1.798336774613000122, -55.60355501915000076, -12.61277771564000005 ) ) ;
#28995=CARTESIAN_POINT ( 'NONE',  ( 0.8537148449456000154, -61.50498145875999256, -12.43377424877000159 ) ) ;
#28996=CIRCLE ( 'NONE', #51650, 0.5000000000000004441 ) ;
#28997=CARTESIAN_POINT ( 'NONE',  ( -7.710095619821999868, -21.75064714351000106, -10.18496935396999881 ) ) ;
#29000=AXIS2_PLACEMENT_3D ( 'NONE', #48171, #51438, #34551 ) ;
#29004=CARTESIAN_POINT ( 'NONE',  ( 6.655614189731015706, -78.52578135515757651, 9.682981938576327607 ) ) ;
#29005=DIRECTION ( 'NONE',  ( -0.7071067811865475727, 0.000000000000000000, -0.7071067811865475727 ) ) ;
#29008=EDGE_CURVE ( 'NONE', #57339, #26739, #17199, .T. ) ;
#29009=AXIS2_PLACEMENT_3D ( 'NONE', #6679, #42699, #20264 ) ;
#29011=CARTESIAN_POINT ( 'NONE',  ( 8.284626357322000700, -53.75139346809000074, -9.778502130833999217 ) ) ;
#29013=CYLINDRICAL_SURFACE ( 'NONE', #56630, 0.5000000000000004441 ) ;
#29016=CARTESIAN_POINT ( 'NONE',  ( -14.00000000000000000, -32.70420297070000260, 0.000000000000000000 ) ) ;
#29020=ORIENTED_EDGE ( 'NONE', *, *, #18338, .T. ) ;
#29021=EDGE_CURVE ( 'NONE', #25888, #47851, #13723, .T. ) ;
#29025=VERTEX_POINT ( 'NONE', #25775 ) ;
#29030=CARTESIAN_POINT ( 'NONE',  ( -1.044910384896000188, -16.94473505805000002, 12.77260826199000121 ) ) ;
#29031=CARTESIAN_POINT ( 'NONE',  ( -10.12290050255000118, -55.55000002206000431, -7.648026768392999664 ) ) ;
#29033=CARTESIAN_POINT ( 'NONE',  ( -12.51072239526000196, -52.49705297114005020, 0.7871079366006996647 ) ) ;
#29034=AXIS2_PLACEMENT_3D ( 'NONE', #53283, #31110, #57707 ) ;
#29038=VERTEX_POINT ( 'NONE', #16925 ) ;
#29039=ORIENTED_EDGE ( 'NONE', *, *, #46918, .T. ) ;
#29042=CARTESIAN_POINT ( 'NONE',  ( -12.68703394093999925, -60.55066116444000102, -1.889962945498999902 ) ) ;
#29044=AXIS2_PLACEMENT_3D ( 'NONE', #55572, #10128, #28693 ) ;
#29045=LINE ( 'NONE', #30188, #50202 ) ;
#29055=DIRECTION ( 'NONE',  ( 0.000000000000000000, 0.000000000000000000, -1.000000000000000000 ) ) ;
#29058=CARTESIAN_POINT ( 'NONE',  ( 11.02435598615611489, -79.24999999999998579, 4.903336801626744901 ) ) ;
#29061=CARTESIAN_POINT ( 'NONE',  ( -2.033046685338129933, -1.172096679664639707, 2.984826379946394326 ) ) ;
#29063=CARTESIAN_POINT ( 'NONE',  ( 0.5584036861551523456, -3.500000000000000444, -3.445874424517756829 ) ) ;
#29067=CARTESIAN_POINT ( 'NONE',  ( -10.59876350475000173, -77.39874337786000069, 7.550195564144000393 ) ) ;
#29069=AXIS2_PLACEMENT_3D ( 'NONE', #21724, #3437, #48607 ) ;
#29072=CARTESIAN_POINT ( 'NONE',  ( 10.07627163191000008, -23.24999999758999536, 7.601397897754999633 ) ) ;
#29073=EDGE_CURVE ( 'NONE', #10595, #16041, #20485, .T. ) ;
#29079=CARTESIAN_POINT ( 'NONE',  ( 7.634645345446648079, -55.32415927443057058, 10.10912681045544126 ) ) ;
#29086=ORIENTED_EDGE ( 'NONE', *, *, #8716, .T. ) ;
#29087=EDGE_CURVE ( 'NONE', #23838, #58165, #47847, .T. ) ;
#29098=EDGE_CURVE ( 'NONE', #50613, #38246, #17639, .T. ) ;
#29102=CARTESIAN_POINT ( 'NONE',  ( -2.887306206174000245, -3.099943126209999900, -1.798010284767999956 ) ) ;
#29104=DIRECTION ( 'NONE',  ( -6.735242868878000753E-11, -1.000000000000000000, 0.000000000000000000 ) ) ;
#29107=LINE ( 'NONE', #47152, #34039 ) ;
#29117=CARTESIAN_POINT ( 'NONE',  ( -3.003502455080446776, -3.070129738312371348, 1.239521229451738371 ) ) ;
#29121=CIRCLE ( 'NONE', #38566, 12.50000000000000000 ) ;
#29123=PLANE ( 'NONE',  #45348 ) ;
#29125=CARTESIAN_POINT ( 'NONE',  ( 10.35845608625999859, -18.70221245812999911, 7.627487525417000036 ) ) ;
#29129=CARTESIAN_POINT ( 'NONE',  ( 12.43359700617999941, -24.70705514168999883, 0.8500729763772000291 ) ) ;
#29132=CARTESIAN_POINT ( 'NONE',  ( 1.535733471446528275, -78.33339274391919105, -11.74722481345108704 ) ) ;
#29134=CARTESIAN_POINT ( 'NONE',  ( 11.31564005662000127, -75.97748313630999917, -4.176683572666000543 ) ) ;
#29139=CARTESIAN_POINT ( 'NONE',  ( -7.634645345497448332, -18.52415927528491579, -10.10912681051243567 ) ) ;
#29140=CARTESIAN_POINT ( 'NONE',  ( -4.743262841170142963, -76.29154122859117138, -10.75029064995872652 ) ) ;
#29143=CARTESIAN_POINT ( 'NONE',  ( 12.68702648024000190, -55.04922088160000015, -1.889939500033999797 ) ) ;
#29146=CYLINDRICAL_SURFACE ( 'NONE', #9528, 0.5999999999999999778 ) ;
#29149=DIRECTION ( 'NONE',  ( 0.000000000000000000, 0.000000000000000000, -1.000000000000000000 ) ) ;
#29150=AXIS2_PLACEMENT_3D ( 'NONE', #58006, #21410, #48296 ) ;
#29156=VERTEX_POINT ( 'NONE', #45404 ) ;
#29159=AXIS2_PLACEMENT_3D ( 'NONE', #38516, #25226, #25805 ) ;
#29161=ORIENTED_EDGE ( 'NONE', *, *, #25046, .F. ) ;
#29168=CARTESIAN_POINT ( 'NONE',  ( -1.995546491236848352, -2.528183067936913275, 2.597540663301302732 ) ) ;
#29171=CARTESIAN_POINT ( 'NONE',  ( -12.49997170191999984, -23.19201514549000009, -1.666513530428999967 ) ) ;
#29180=CARTESIAN_POINT ( 'NONE',  ( -7.636246406686000299, -23.76323123101999713, 10.30460653225000023 ) ) ;
#29184=CARTESIAN_POINT ( 'NONE',  ( 7.601397897754999633, -18.75000000240999753, 10.07627163191000008 ) ) ;
#29185=CARTESIAN_POINT ( 'NONE',  ( 12.21456857099000004, -78.69087223421999511, -1.096995930408000142 ) ) ;
#29188=CARTESIAN_POINT ( 'NONE',  ( 0.2837406302606167996, -77.92307676773893377, 12.06313962186550270 ) ) ;
#29190=ORIENTED_EDGE ( 'NONE', *, *, #37559, .T. ) ;
#29192=CARTESIAN_POINT ( 'NONE',  ( -17.50000000000000000, -51.86282895648000135, -3.979077900507000222E-10 ) ) ;
#29193=CARTESIAN_POINT ( 'NONE',  ( 1.929975092517999924, -23.20107256264000029, 12.72537404210999945 ) ) ;
#29194=AXIS2_PLACEMENT_3D ( 'NONE', #1365, #5481, #56252 ) ;
#29196=CARTESIAN_POINT ( 'NONE',  ( -3.597461531748000318, -3.264312248862000221, 1.427805196757999884 ) ) ;
#29200=CARTESIAN_POINT ( 'NONE',  ( -11.41855217635170838, -76.18078835300777030, 2.773217851598793526 ) ) ;
#29205=CARTESIAN_POINT ( 'NONE',  ( 12.72966770606015530, -23.76881200365913571, 1.931346186345839211 ) ) ;
#29207=CARTESIAN_POINT ( 'NONE',  ( -1.636761686205434607, -2.416666666666666963, 2.839805762151332402 ) ) ;
#29208=CARTESIAN_POINT ( 'NONE',  ( -8.292771711479000274, -61.85529938492000213, 9.770424367394999976 ) ) ;
#29215=DIRECTION ( 'NONE',  ( 1.000000000000000000, 0.000000000000000000, 0.000000000000000000 ) ) ;
#29216=CARTESIAN_POINT ( 'NONE',  ( -8.130811096204000776, -61.48523690322999613, -9.546858433459998849 ) ) ;
#29222=CARTESIAN_POINT ( 'NONE',  ( -0.8338927956455162160, -53.99946422210319952, -12.50366901599826797 ) ) ;
#29223=CARTESIAN_POINT ( 'NONE',  ( 1.931087888049999979, -55.48415522678000400, -12.71658889739000031 ) ) ;
#29227=CARTESIAN_POINT ( 'NONE',  ( 12.71758670595498053, -54.73493368741875997, -1.809547514116605971 ) ) ;
#29229=EDGE_CURVE ( 'NONE', #52985, #49658, #33655, .T. ) ;
#29230=VERTEX_POINT ( 'NONE', #20986 ) ;
#29234=CARTESIAN_POINT ( 'NONE',  ( 10.47840693002000023, -18.21310507181999938, 7.622759963130000038 ) ) ;
#29235=AXIS2_PLACEMENT_3D ( 'NONE', #32193, #50235, #5064 ) ;
#29236=AXIS2_PLACEMENT_3D ( 'NONE', #9580, #5149, #26979 ) ;
#29238=CARTESIAN_POINT ( 'NONE',  ( -1.575772165460815666, -54.33845457181071481, 12.70597445614748544 ) ) ;
#29239=CARTESIAN_POINT ( 'NONE',  ( 8.299965097802999736, -78.51685037320000049, -8.752034438815000428 ) ) ;
#29240=FACE_OUTER_BOUND ( 'NONE', #6007, .T. ) ;
#29241=CYLINDRICAL_SURFACE ( 'NONE', #6992, 0.5000000000000006661 ) ;
#29245=DIRECTION ( 'NONE',  ( 0.000000000000000000, -1.000000000000000000, 0.000000000000000000 ) ) ;
#29246=EDGE_LOOP ( 'NONE', ( #30888, #3604, #49458 ) ) ;
#29249=DIRECTION ( 'NONE',  ( 0.000000000000000000, 1.000000000000000000, 0.000000000000000000 ) ) ;
#29250=CARTESIAN_POINT ( 'NONE',  ( 8.061017305527000687, -59.94999999967000548, -8.909545442949999838 ) ) ;
#29255=CARTESIAN_POINT ( 'NONE',  ( -7.678667886068000215, -20.24263462181000151, 10.59548767699999949 ) ) ;
#29258=DIRECTION ( 'NONE',  ( 0.000000000000000000, -1.000000000000000000, 0.000000000000000000 ) ) ;
#29260=ORIENTED_EDGE ( 'NONE', *, *, #8219, .T. ) ;
#29265=CARTESIAN_POINT ( 'NONE',  ( -10.07615509326000058, -17.27367739700000016, 7.986954869189998973 ) ) ;
#29268=CARTESIAN_POINT ( 'NONE',  ( -0.3956897636865157608, -2.133947066360573519, 3.499075337960325882 ) ) ;
#29271=CARTESIAN_POINT ( 'NONE',  ( 1.669849926076999891, -55.42771399551000400, -12.48404299551000030 ) ) ;
#29273=CARTESIAN_POINT ( 'NONE',  ( -7.674614791514000167, -19.24899163938999891, 10.14948852566999804 ) ) ;
#29276=ORIENTED_EDGE ( 'NONE', *, *, #38157, .F. ) ;
#29277=CARTESIAN_POINT ( 'NONE',  ( -11.75000000000000000, -78.70000000000000284, -1.701764645356999850E-14 ) ) ;
#29278=CARTESIAN_POINT ( 'NONE',  ( -0.9113424693929998988, -61.62535793526999583, -12.54674099561999867 ) ) ;
#29280=CIRCLE ( 'NONE', #1169, 11.00000000000000000 ) ;
#29286=CARTESIAN_POINT ( 'NONE',  ( 9.965884746006045347, -78.49300387697907411, 6.229937699784958482 ) ) ;
#29287=CARTESIAN_POINT ( 'NONE',  ( -7.861032689964853049, -61.26660299196984738, 10.10708926016829778 ) ) ;
#29288=ORIENTED_EDGE ( 'NONE', *, *, #23290, .F. ) ;
#29291=LINE ( 'NONE', #57041, #20745 ) ;
#29296=CARTESIAN_POINT ( 'NONE',  ( 8.838834764832000701, -55.54999999966999980, 8.838834764832000701 ) ) ;
#29299=CARTESIAN_POINT ( 'NONE',  ( -8.610991514451539430, -53.62512235746365263, 9.355860133842407222 ) ) ;
#29300=ORIENTED_EDGE ( 'NONE', *, *, #27695, .T. ) ;
#29301=CARTESIAN_POINT ( 'NONE',  ( 1.931086388455000025, -23.29778595484999926, 12.71798280855999863 ) ) ;
#29302=CARTESIAN_POINT ( 'NONE',  ( -12.82202361517000000, -23.42627773034000427, 2.066043355638000012 ) ) ;
#29306=TOROIDAL_SURFACE ( 'NONE', #44392, 1.250000000000000000, 0.5000000000000000000 ) ;
#29307=CARTESIAN_POINT ( 'NONE',  ( -12.61112375829999976, -55.58433928934000079, -1.798929377343999825 ) ) ;
#29309=ORIENTED_EDGE ( 'NONE', *, *, #45850, .T. ) ;
#29310=CARTESIAN_POINT ( 'NONE',  ( 8.485281374238999419, -18.75000000000000000, -8.485281374238999419 ) ) ;
#29313=CARTESIAN_POINT ( 'NONE',  ( 7.601397897754999633, -23.25000000000000000, 9.369164850722000892 ) ) ;
#29321=CARTESIAN_POINT ( 'NONE',  ( -1.392423410630999929E-14, -75.80000000000001137, 0.000000000000000000 ) ) ;
#29322=B_SPLINE_CURVE_WITH_KNOTS ( 'NONE', 3,
 ( #13208, #3494, #8209, #39503, #12639, #40077 ),
 .UNSPECIFIED., .F., .F.,
 ( 4, 1, 1, 4 ),
 ( 0.000000000000000000, 0.3333333333333000081, 0.6666666666667000474, 1.000000000000000000 ),
 .UNSPECIFIED. ) ;
#29323=CARTESIAN_POINT ( 'NONE',  ( -12.43652404748999984, -61.72065244505999715, -0.1284256373645000227 ) ) ;
#29326=CARTESIAN_POINT ( 'NONE',  ( 7.668949790020999302, -19.22870851082999977, 10.21381326473999884 ) ) ;
#29327=CARTESIAN_POINT ( 'NONE',  ( 0.000000000000000000, -32.70420297070000260, 0.000000000000000000 ) ) ;
#29331=DIRECTION ( 'NONE',  ( 0.000000000000000000, 0.000000000000000000, 1.000000000000000000 ) ) ;
#29335=CARTESIAN_POINT ( 'NONE',  ( -1.750000000000000000, -21.74977139337000054, -12.65375411739000100 ) ) ;
#29336=CARTESIAN_POINT ( 'NONE',  ( 2.062673488738000049, -23.32452529362999982, -12.82904091339000097 ) ) ;
#29337=EDGE_CURVE ( 'NONE', #40915, #56632, #1618, .T. ) ;
#29339=CARTESIAN_POINT ( 'NONE',  ( 13.86363636363000218, -32.36102867817999851, 1.277888278705000044E-05 ) ) ;
#29342=CARTESIAN_POINT ( 'NONE',  ( 12.50000000000000000, -18.75000000000000000, -1.250000000000000000 ) ) ;
#29344=DIRECTION ( 'NONE',  ( 1.000000000000000000, 0.000000000000000000, 0.000000000000000000 ) ) ;
#29347=CARTESIAN_POINT ( 'NONE',  ( 12.50240681834000078, -24.68234730741999883, -1.005418943851999813 ) ) ;
#29348=CARTESIAN_POINT ( 'NONE',  ( -1.930628539546999978, -55.57875555881000196, 12.72375828102000028 ) ) ;
#29352=CARTESIAN_POINT ( 'NONE',  ( -12.54673671095000209, -53.97796527404000244, 0.9173654211234000266 ) ) ;
#29354=CARTESIAN_POINT ( 'NONE',  ( 1.667260628937999867, -60.00942012442000362, 12.49858003896999925 ) ) ;
#29359=CARTESIAN_POINT ( 'NONE',  ( 9.766266492730634852, -76.40258437943595027, -6.532607198706168461 ) ) ;
#29362=VECTOR ( 'NONE', #40366, 1000.000000000000000 ) ;
#29363=CARTESIAN_POINT ( 'NONE',  ( 1.750000000000000000, -57.05022860762000647, -12.65375411742999923 ) ) ;
#29370=CIRCLE ( 'NONE', #14321, 1.750000000000001332 ) ;
#29372=CARTESIAN_POINT ( 'NONE',  ( 12.00000000000000000, -18.84999999999999787, 0.5999999999999999778 ) ) ;
#29373=CARTESIAN_POINT ( 'NONE',  ( 0.000000000000000000, -23.15000000000000213, -12.00000000000000000 ) ) ;
#29375=EDGE_CURVE ( 'NONE', #8523, #32213, #20276, .T. ) ;
#29376=CARTESIAN_POINT ( 'NONE',  ( 1.718598679964348896, -24.24962933043864766, 12.71111582768155124 ) ) ;
#29377=EDGE_CURVE ( 'NONE', #18726, #49572, #34982, .T. ) ;
#29379=VERTEX_POINT ( 'NONE', #42714 ) ;
#29380=CARTESIAN_POINT ( 'NONE',  ( 8.107762507645077221, -60.31691643837567796, 7.434020715871779039 ) ) ;
#29381=CARTESIAN_POINT ( 'NONE',  ( 1.538071403320016461, -77.43541666666664014, -11.74999999999999822 ) ) ;
#29384=VERTEX_POINT ( 'NONE', #57150 ) ;
#29386=ORIENTED_EDGE ( 'NONE', *, *, #39474, .T. ) ;
#29388=B_SPLINE_CURVE_WITH_KNOTS ( 'NONE', 3,
 ( #28914, #24496, #38355, #33632, #51954, #55799 ),
 .UNSPECIFIED., .F., .F.,
 ( 4, 1, 1, 4 ),
 ( 0.000000000000000000, 0.3333333333333000081, 0.6666666666667000474, 1.000000000000000000 ),
 .UNSPECIFIED. ) ;
#29397=CARTESIAN_POINT ( 'NONE',  ( -11.75000000000000000, -77.29999999999999716, 0.000000000000000000 ) ) ;
#29403=CARTESIAN_POINT ( 'NONE',  ( 12.00000000000000000, -23.15000000002000036, 0.7999999999999001243 ) ) ;
#29404=CARTESIAN_POINT ( 'NONE',  ( -1.247385803317999864, -61.27722255996999934, -12.50301438880000049 ) ) ;
#29413=DIRECTION ( 'NONE',  ( -0.7071067811705339379, 1.925103501360094241E-07, -0.7071067812025347843 ) ) ;
#29415=CARTESIAN_POINT ( 'NONE',  ( -7.645391636782999711, -60.01530450324999322, -10.18949673577000148 ) ) ;
#29416=DIRECTION ( 'NONE',  ( 0.000000000000000000, -1.000000000000000000, 0.000000000000000000 ) ) ;
#29418=CARTESIAN_POINT ( 'NONE',  ( -12.72394144137000005, -18.77839271500000251, -1.930881231431999856 ) ) ;
#29419=CARTESIAN_POINT ( 'NONE',  ( -9.339950055924999717, -78.11329442843999971, -9.061158367717998985 ) ) ;
#29422=CARTESIAN_POINT ( 'NONE',  ( 7.169497772410326597, -78.37458968298378181, -9.346273223251115425 ) ) ;
#29423=CARTESIAN_POINT ( 'NONE',  ( 1.618935784642556275, -23.92751168673077800, -12.52134385800271410 ) ) ;
#29424=CARTESIAN_POINT ( 'NONE',  ( -6.371817981013998988, -76.16336784646999547, -10.59357524699000130 ) ) ;
#29427=CYLINDRICAL_SURFACE ( 'NONE', #9754, 11.75000000000000000 ) ;
#29429=CARTESIAN_POINT ( 'NONE',  ( -3.689662007795999621, -78.48144319244001110, 11.36357164112000007 ) ) ;
#29430=CARTESIAN_POINT ( 'NONE',  ( 12.66008925480999814, -54.17289997881999852, -1.387046028394999908 ) ) ;
#29433=FACE_OUTER_BOUND ( 'NONE', #34569, .T. ) ;
#29434=CARTESIAN_POINT ( 'NONE',  ( -12.50000000000000000, -63.73717104351998586, -1.871520963622999753E-13 ) ) ;
#29435=ORIENTED_EDGE ( 'NONE', *, *, #31389, .F. ) ;
#29443=ORIENTED_EDGE ( 'NONE', *, *, #51767, .T. ) ;
#29450=CARTESIAN_POINT ( 'NONE',  ( 12.54983130235000033, -53.74901607425999828, 0.1356732392833999989 ) ) ;
#29453=CARTESIAN_POINT ( 'NONE',  ( 7.919595949288999570, -59.94999999446000771, -8.768124086549999419 ) ) ;
#29455=AXIS2_PLACEMENT_3D ( 'NONE', #8238, #35372, #35975 ) ;
#29456=CARTESIAN_POINT ( 'NONE',  ( 9.108265402946999600, -53.92189187171000242, 8.478706101031999509 ) ) ;
#29458=CARTESIAN_POINT ( 'NONE',  ( 7.635226873550689852, -18.23391307131834438, -10.36745167322480121 ) ) ;
#29460=CARTESIAN_POINT ( 'NONE',  ( -10.26032959198470884, -77.24059631258572267, -5.914278839158486178 ) ) ;
#29461=AXIS2_PLACEMENT_3D ( 'NONE', #53842, #5126, #27536 ) ;
#29465=CARTESIAN_POINT ( 'NONE',  ( -8.652376385601000308, -25.26264602966000083, 9.414489258817999584 ) ) ;
#29468=LINE ( 'NONE', #24185, #15343 ) ;
#29469=CARTESIAN_POINT ( 'NONE',  ( -5.950798862880000151, -78.89798320933999776, 10.72320280238000123 ) ) ;
#29472=EDGE_CURVE ( 'NONE', #35168, #7317, #11060, .T. ) ;
#29473=CARTESIAN_POINT ( 'NONE',  ( 3.945923481703957680, -77.70070240490868230, -11.63927170873302863 ) ) ;
#29475=VERTEX_POINT ( 'NONE', #20563 ) ;
#29477=CARTESIAN_POINT ( 'NONE',  ( 12.72554383682000001, -60.00159311597000311, -1.930239506950999884 ) ) ;
#29479=VECTOR ( 'NONE', #7709, 1000.000000000000000 ) ;
#29480=CARTESIAN_POINT ( 'NONE',  ( 1.750000000001000089, -23.25000000990999993, 12.56594317857000043 ) ) ;
#29481=CARTESIAN_POINT ( 'NONE',  ( 0.6912376084024000056, -2.021356624101999788, -3.649169745438999968 ) ) ;
#29484=B_SPLINE_CURVE_WITH_KNOTS ( 'NONE', 3,
 ( #23061, #18062, #49947, #54076, #14776, #4482 ),
 .UNSPECIFIED., .F., .F.,
 ( 4, 2, 4 ),
 ( 0.000000000000000000, 0.5000000000000000000, 1.000000000000000000 ),
 .UNSPECIFIED. ) ;
#29485=EDGE_CURVE ( 'NONE', #3332, #16171, #46885, .T. ) ;
#29486=CARTESIAN_POINT ( 'NONE',  ( -0.3046678973520325906, -76.07670231100695446, 11.75299617503634764 ) ) ;
#29488=CARTESIAN_POINT ( 'NONE',  ( 10.07627163191000008, -23.24999999758999536, 7.601397897754999633 ) ) ;
#29489=FACE_OUTER_BOUND ( 'NONE', #34212, .T. ) ;
#29490=ORIENTED_EDGE ( 'NONE', *, *, #18460, .F. ) ;
#29491=LINE ( 'NONE', #38649, #40807 ) ;
#29493=ADVANCED_FACE ( 'NONE', ( #12278 ), #38561, .F. ) ;
#29495=CARTESIAN_POINT ( 'NONE',  ( 3.250000000000000000, -2.250000000000000000, 0.000000000000000000 ) ) ;
#29496=CARTESIAN_POINT ( 'NONE',  ( -7.758897894450000443, -61.10081253415999925, 10.31443085085999911 ) ) ;
#29499=CARTESIAN_POINT ( 'NONE',  ( 7.633478597825000378, -18.79901960220000134, -10.36292351978000070 ) ) ;
#29501=EDGE_LOOP ( 'NONE', ( #53487, #32197, #44723 ) ) ;
#29506=DIRECTION ( 'NONE',  ( 1.000000000000000000, 0.000000000000000000, 0.000000000000000000 ) ) ;
#29507=AXIS2_PLACEMENT_3D ( 'NONE', #11800, #2660, #20654 ) ;
#29509=DIRECTION ( 'NONE',  ( 0.000000000000000000, -1.000000000000000000, 0.000000000000000000 ) ) ;
#29510=CARTESIAN_POINT ( 'NONE',  ( 1.103931346181417528, -54.17916251664232163, -12.50298439256130578 ) ) ;
#29511=CARTESIAN_POINT ( 'NONE',  ( 1.667936688463999895, -59.56486430393999854, -12.53239398061000109 ) ) ;
#29512=ADVANCED_FACE ( 'NONE', ( #30268 ), #22592, .F. ) ;
#29515=FACE_OUTER_BOUND ( 'NONE', #31912, .T. ) ;
#29520=CONICAL_SURFACE ( 'NONE', #4065, 12.84999999995999964, 0.7853981633972997312 ) ;
#29521=EDGE_LOOP ( 'NONE', ( #26545, #5069, #54000, #16400, #26695, #47945, #27803, #9611, #1977, #22973, #13415, #39268, #7168 ) ) ;
#29522=CARTESIAN_POINT ( 'NONE',  ( 8.485548443539000729, -17.11931586736000455, 9.101490738460999097 ) ) ;
#29524=CARTESIAN_POINT ( 'NONE',  ( 8.768124086549999419, -59.94999999446000771, 7.919595949288999570 ) ) ;
#29525=CARTESIAN_POINT ( 'NONE',  ( 5.554616340558999887, -78.00781628945000534, 11.53062854294000061 ) ) ;
#29526=FACE_OUTER_BOUND ( 'NONE', #41620, .T. ) ;
#29529=CONICAL_SURFACE ( 'NONE', #15390, 13.94999999937999924, 0.7853981633972997312 ) ;
#29532=CARTESIAN_POINT ( 'NONE',  ( 11.61663471297537242, -78.06380585108666992, 2.038423278490623325 ) ) ;
#29540=DIRECTION ( 'NONE',  ( 0.000000000000000000, -1.000000000000000000, 0.000000000000000000 ) ) ;
#29541=CYLINDRICAL_SURFACE ( 'NONE', #13429, 1.750000000000001332 ) ;
#29543=CARTESIAN_POINT ( 'NONE',  ( -7.668936932643000581, -19.22847221992000044, 10.21380041495000057 ) ) ;
#29547=FILL_AREA_STYLE_COLOUR ( '', #46097 ) ;
#29550=ADVANCED_FACE ( 'NONE', ( #4885 ), #55005, .F. ) ;
#29553=CARTESIAN_POINT ( 'NONE',  ( 10.06692847421147086, -60.50343452142983125, 7.655995225842833207 ) ) ;
#29555=CARTESIAN_POINT ( 'NONE',  ( -9.101506735347999921, -17.11932813898000205, 8.485532457246998561 ) ) ;
#29557=CARTESIAN_POINT ( 'NONE',  ( -2.870721577664869351, -1.799218864078162117, -2.038938680912825596 ) ) ;
#29564=ORIENTED_EDGE ( 'NONE', *, *, #24164, .T. ) ;
#29567=CARTESIAN_POINT ( 'NONE',  ( -1.194090705995999979, -61.24031658870000427, -12.43436538493000043 ) ) ;
#29568=EDGE_CURVE ( 'NONE', #52988, #36311, #11540, .T. ) ;
#29571=CARTESIAN_POINT ( 'NONE',  ( 10.31986335554000078, -24.28918510737999981, -7.753844818030001029 ) ) ;
#29574=CARTESIAN_POINT ( 'NONE',  ( -1.250000000000000000, -55.54999999966999980, -12.50000000000000000 ) ) ;
#29575=DIRECTION ( 'NONE',  ( -0.7071067811865475727, 0.000000000000000000, 0.7071067811865475727 ) ) ;
#29576=ORIENTED_EDGE ( 'NONE', *, *, #15348, .T. ) ;
#29580=CARTESIAN_POINT ( 'NONE',  ( 1.568318300085000120E-14, -0.05000000003700048185, 0.000000000000000000 ) ) ;
#29581=CARTESIAN_POINT ( 'NONE',  ( 1.538071403319964281, -77.66458333333333997, 11.75000000000000711 ) ) ;
#29582=CARTESIAN_POINT ( 'NONE',  ( -12.76303204298000082, -60.06485150663000638, 1.980584515756000030 ) ) ;
#29584=ADVANCED_FACE ( 'NONE', ( #18464 ), #31128, .F. ) ;
#29587=DIRECTION ( 'NONE',  ( -0.7071067811865475727, 0.000000000000000000, 0.7071067811865475727 ) ) ;
#29591=ORIENTED_EDGE ( 'NONE', *, *, #48653, .T. ) ;
#29592=CARTESIAN_POINT ( 'NONE',  ( -12.68625206992999921, -55.03580249152999926, -1.886949102778999965 ) ) ;
#29593=ORIENTED_EDGE ( 'NONE', *, *, #54091, .T. ) ;
#29594=ORIENTED_EDGE ( 'NONE', *, *, #1218, .F. ) ;
#29596=CARTESIAN_POINT ( 'NONE',  ( 10.35398566681999988, -23.40788276239999988, 7.619388279076999559 ) ) ;
#29599=B_SPLINE_CURVE_WITH_KNOTS ( 'NONE', 3,
 ( #38968, #17399, #52841, #7674, #48423, #26833 ),
 .UNSPECIFIED., .F., .F.,
 ( 4, 2, 4 ),
 ( 0.000000000000000000, 0.5000000000000000000, 1.000000000000000000 ),
 .UNSPECIFIED. ) ;
#29600=CARTESIAN_POINT ( 'NONE',  ( 0.000000000000000000, -39.30476017083000073, 0.000000000000000000 ) ) ;
#29606=VERTEX_POINT ( 'NONE', #4292 ) ;
#29608=DIRECTION ( 'NONE',  ( -0.3090169943748909409, 0.000000000000000000, -0.9510565162951719609 ) ) ;
#29610=DIRECTION ( 'NONE',  ( 0.000000000000000000, 1.000000000000000000, 0.000000000000000000 ) ) ;
#29612=CARTESIAN_POINT ( 'NONE',  ( 7.668936932623999780, -22.77152778045000048, 10.21380041493000057 ) ) ;
#29613=CARTESIAN_POINT ( 'NONE',  ( 12.50000000000000000, -51.86282895648000135, 0.000000000000000000 ) ) ;
#29615=DIRECTION ( 'NONE',  ( 0.7071067811865475727, 0.000000000000000000, -0.7071067811865475727 ) ) ;
#29624=CARTESIAN_POINT ( 'NONE',  ( 2.062597299672999540, -22.78485473281999774, -12.87022657272000004 ) ) ;
#29625=FACE_OUTER_BOUND ( 'NONE', #41508, .T. ) ;
#29626=CARTESIAN_POINT ( 'NONE',  ( 13.98934701301999972, -32.57813015402999923, 1.420884290714999950E-05 ) ) ;
#29630=LINE ( 'NONE', #55644, #53479 ) ;
#29631=CARTESIAN_POINT ( 'NONE',  ( 2.859635500329999580, -0.9504959227639564467, -2.056314849297946612 ) ) ;
#29632=ORIENTED_EDGE ( 'NONE', *, *, #57353, .F. ) ;
#29634=DIRECTION ( 'NONE',  ( -2.493024943570999650E-13, -1.000000000000000000, 2.029372555462999773E-12 ) ) ;
#29635=CARTESIAN_POINT ( 'NONE',  ( 10.06692933833339687, -18.29657287078697792, -7.655995045172042879 ) ) ;
#29639=CARTESIAN_POINT ( 'NONE',  ( 0.000000000000000000, 4.040000000000000036, 0.000000000000000000 ) ) ;
#29640=CARTESIAN_POINT ( 'NONE',  ( 0.4254240051736215000, -3.135416666666666075, -3.250000000000000000 ) ) ;
#29641=DIRECTION ( 'NONE',  ( 0.7071067811865475727, 0.000000000000000000, 0.7071067811865475727 ) ) ;
#29644=AXIS2_PLACEMENT_3D ( 'NONE', #43822, #31072, #49110 ) ;
#29645=CARTESIAN_POINT ( 'NONE',  ( 0.5211352025712173708, -76.32812523379961078, -11.74973435454385040 ) ) ;
#29649=CARTESIAN_POINT ( 'NONE',  ( -3.027333896924861101, -1.068427606005047048, 1.360419436555698969 ) ) ;
#29657=AXIS2_PLACEMENT_3D ( 'NONE', #16397, #3679, #30242 ) ;
#29659=( BOUNDED_SURFACE ( )  B_SPLINE_SURFACE ( 3, 3, ( 
 ( #29033, #55914, #15466, #51496 ),
 ( #6601, #24612, #42627, #11624 ),
 ( #14477, #28633, #27757, #1222 ),
 ( #28926, #46683, #45801, #6203 ),
 ( #23919, #937, #28335, #46969 ),
 ( #41937, #32468, #42235, #46386 ),
 ( #10946, #33356, #5910, #650 ) ),
 .UNSPECIFIED., .F., .F., .F. ) 
 B_SPLINE_SURFACE_WITH_KNOTS ( ( 4, 3, 4 ),
 ( 4, 4 ),
 ( 0.000000000000000000, 1.000000000000000000, 2.000000000000000000 ),
 ( 0.000000000000000000, 1.000000000000000000 ),
 .UNSPECIFIED. ) 
 GEOMETRIC_REPRESENTATION_ITEM ( )  RATIONAL_B_SPLINE_SURFACE ( (
 ( 1.196373642248999891, 1.184225762575999985, 1.184225762575999985, 1.196373642248999891),
 ( 0.9447739570234999773, 0.9351807998836999536, 0.9351807998836999536, 0.9447739570234999773),
 ( 0.9447739570234999773, 0.9351807998836999536, 0.9351807998836999536, 0.9447739570234999773),
 ( 1.196373642248999891, 1.184225762575999985, 1.184225762575999985, 1.196373642248999891),
 ( 0.9447739570234999773, 0.9351807998836999536, 0.9351807998836999536, 0.9447739570234999773),
 ( 0.9447739570234999773, 0.9351807998836999536, 0.9351807998836999536, 0.9447739570234999773),
 ( 1.196373642248999891, 1.184225762575999985, 1.184225762575999985, 1.196373642248999891) ) ) 
 REPRESENTATION_ITEM ( '' )  SURFACE ( )  );
#29662=CARTESIAN_POINT ( 'NONE',  ( 1.495357591751715010, -24.55876337363582707, 12.70444646759489693 ) ) ;
#29666=CARTESIAN_POINT ( 'NONE',  ( 3.415507079190750250, -3.499999999999999556, -0.9241186193027908224 ) ) ;
#29667=ORIENTED_EDGE ( 'NONE', *, *, #16117, .T. ) ;
#29672=ORIENTED_EDGE ( 'NONE', *, *, #8769, .T. ) ;
#29682=CARTESIAN_POINT ( 'NONE',  ( -11.44417895085272008, -77.27916666666668277, 3.075537641221497420 ) ) ;
#29684=CONICAL_SURFACE ( 'NONE', #35356, 0.6999999997695030007, 0.7853981633972997312 ) ;
#29686=B_SPLINE_CURVE_WITH_KNOTS ( 'NONE', 3,
 ( #56398, #51979, #7093, #43115, #20669, #49278 ),
 .UNSPECIFIED., .F., .F.,
 ( 4, 2, 4 ),
 ( 0.000000000000000000, 0.5000000000000000000, 1.000000000000000000 ),
 .UNSPECIFIED. ) ;
#29689=CIRCLE ( 'NONE', #23083, 1.750000000000001998 ) ;
#29690=DIRECTION ( 'NONE',  ( 0.000000000000000000, -1.000000000000000000, 0.000000000000000000 ) ) ;
#29696=CARTESIAN_POINT ( 'NONE',  ( -12.50000000000000000, -49.87071422276000021, 0.000000000000000000 ) ) ;
#29697=CARTESIAN_POINT ( 'NONE',  ( 1.980584515752000119, -60.06485146591000301, -12.76303204605000197 ) ) ;
#29698=CARTESIAN_POINT ( 'NONE',  ( -7.633403016722000167, -60.18650073818000124, -10.18126993295000027 ) ) ;
#29701=B_SPLINE_CURVE_WITH_KNOTS ( 'NONE', 3,
 ( #7718, #7432, #22155, #8290, #8582, #25434, #57591, #26570, #43449, #3863, #21005, #35425, #21291, #53168, #48461, #44603, #34567, #57020, #16581, #53455, #30136, #57883, #26294, #25721, #39870, #57309, #12999, #30429, #52599, #12151, #48186, #43746, #3298, #48747, #12717, #21863, #52883, #21581, #8004, #30997, #12436, #26001, #44026, #3577, #44307, #8877, #50207, #36322, #41342, #9175, #26871, #10054, #58, #28036, #23615, #36899, #350, #46081, #49331, #32455, #40466, #27453, #13587, #14464, #9757, #5605, #44898, #4451, #5034, #13294, #36613, #18329, #9468, #22452, #50500, #49627, #54346, #54912, #27742, #18033, #41628, #36026, #54052, #45491, #13885, #40756, #31880, #31287, #49923, #45789, #23036, #54635, #31582, #14171, #1208, #27159, #926, #41052, #45198, #32168, #5325, #19200, #23332, #37191, #4745, #639, #22746, #18622, #18906, #29486, #42800, #46664, #42509, #47543, #51088, #51953, #11221, #15349, #41923, #20077, #10637, #2362, #6191, #43092, #55798, #33041, #23905, #20359, #37777, #28619, #7067, #47245, #33914, #1787, #15049, #24785, #38354, #24204, #56376, #15927, #38069, #37478, #25069, #33342, #11509, #28913, #2650, #20644, #55205, #14748, #51673, #42221, #6777, #19783, #32748, #51375, #50796, #19485, #55501, #10341, #28320, #46372, #10932, #5896, #56089, #46957, #6484, #24495, #1495, #2079, #15635, #33631, #29200, #34196, #17074, #3222, #8214, #34487, #52234, #35349, #25352, #12074, #29765 ),
 .UNSPECIFIED., .F., .F.,
 ( 4, 2, 1, 1, 1, 1, 2, 2, 2, 2, 1, 1, 1, 1, 1, 1, 2, 2, 2, 2, 2, 1, 1, 1, 1, 1, 2, 2, 2, 1, 1, 1, 1, 2, 2, 2, 2, 1, 1, 1, 1, 2, 2, 2, 2, 2, 2, 2, 1, 1, 1, 1, 2, 2, 2, 2, 2, 1, 1, 1, 1, 2, 2, 2, 2, 1, 1, 1, 1, 1, 1, 2, 2, 2, 2, 2, 2, 2, 2, 2, 1, 1, 1, 1, 1, 2, 2, 2, 2, 1, 1, 2, 2, 2, 2, 1, 1, 1, 2, 2, 2, 2, 2, 1, 1, 1, 1, 1, 2, 2, 2, 2, 2, 1, 1, 1, 2, 2, 4 ),
 ( 0.000000000000000000, 0.03125000000005081352, 0.04687500000007623763, 0.05468750000008895662, 0.05859375000009531265, 0.06054687500009849760, 0.06152343750010012130, 0.06250000000010175194, 0.09375000000015386303, 0.1093750000001798978, 0.1171875000001929429, 0.1210937500001994238, 0.1230468750002026851, 0.1240234375002043643, 0.1245117187502051553, 0.1247558593752055855, 0.1248779296877058076, 0.1250000000002060296, 0.1562500000002606804, 0.1718750000002879919, 0.1796875000003016198, 0.1835937500003083644, 0.1855468750003117229, 0.1865234375003133049, 0.1870117187503139711, 0.1872558593753144152, 0.1873779296878145262, 0.1875000000003146650, 0.2031250000003272105, 0.2109375000003335388, 0.2148437500003366751, 0.2167968750003382850, 0.2177734375003390621, 0.2182617187503395062, 0.2187500000003399225, 0.2343750000003542444, 0.2421875000003613498, 0.2460937500003649026, 0.2480468750003666512, 0.2490234375003675393, 0.2495117187503679834, 0.2497558593753683165, 0.2500000000003685940, 0.2812500000004109491, 0.3125000000004533041, 0.3437500000004956036, 0.3593750000005168088, 0.3671875000005274114, 0.3710937500005328515, 0.3730468750005358491, 0.3740234375005368483, 0.3745117187505374035, 0.3747558593755371814, 0.3750000000005369594, 0.4062500000005068168, 0.4218750000004917178, 0.4296875000004841127, 0.4335937500004803935, 0.4355468750004785061, 0.4365234375004776179, 0.4370117187504771183, 0.4372558593754768963, 0.4375000000004766743, 0.4687500000004548029, 0.4843750000004438117, 0.4921875000004383716, 0.4960937500004356515, 0.4980468750004342637, 0.4990234375004335421, 0.4995117187504332645, 0.4997558593754330980, 0.4998779296879329870, 0.5000000000004328760, 0.5625000000003597123, 0.6250000000002866596, 0.6562500000002500222, 0.6875000000002134959, 0.7187500000001769696, 0.7343750000001587619, 0.7421875000001495470, 0.7460937500001449951, 0.7480468750001427747, 0.7490234375001416645, 0.7495117187501411093, 0.7497558593751408873, 0.7498779296876407763, 0.7500000000001405542, 0.7656250000001202372, 0.7734375000001100231, 0.7773437500001049161, 0.7792968750001023626, 0.7802734375001010303, 0.7812500000000996980, 0.7968750000000796030, 0.8046875000000695000, 0.8085937500000645040, 0.8105468750000618394, 0.8115234375000606182, 0.8120117187500600631, 0.8125000000000595080, 0.8437500000000257572, 0.8593750000000086597, 0.8671875000000003331, 0.8710937499999961142, 0.8730468749999940048, 0.8740234374999928946, 0.8745117187499923395, 0.8747558593749921174, 0.8748779296874918954, 0.8749999999999917843, 0.9062499999999941158, 0.9218749999999952260, 0.9296874999999957812, 0.9335937499999960032, 0.9355468749999962252, 0.9365234374999962252, 0.9370117187499962252, 0.9374999999999963363, 1.000000000000000000 ),
 .UNSPECIFIED. ) ;
#29703=CARTESIAN_POINT ( 'NONE',  ( -12.50745077490000057, -17.00005551713000074, 2.011909873286000185E-09 ) ) ;
#29706=DIRECTION ( 'NONE',  ( -0.7071067811865969777, 0.7071067811864980568, -6.623700168368979662E-09 ) ) ;
#29708=CARTESIAN_POINT ( 'NONE',  ( 1.501534314719157326, -24.55152951663309224, -12.70455943739907845 ) ) ;
#29709=CARTESIAN_POINT ( 'NONE',  ( 10.65858277789999953, -75.78824986905000571, 6.553927674015000093 ) ) ;
#29710=ORIENTED_EDGE ( 'NONE', *, *, #40776, .F. ) ;
#29712=CARTESIAN_POINT ( 'NONE',  ( 12.72397319118000070, -60.02144180272999563, 1.930910316632999946 ) ) ;
#29713=CARTESIAN_POINT ( 'NONE',  ( -12.63427402858000015, -78.67048691447000408, -0.3091878550698000105 ) ) ;
#29714=CARTESIAN_POINT ( 'NONE',  ( 12.59682398755999877, -55.41262488626999527, -1.801644812721000077 ) ) ;
#29720=DIRECTION ( 'NONE',  ( -0.7071067811865475727, 0.000000000000000000, -0.7071067811865475727 ) ) ;
#29721=ADVANCED_FACE ( 'NONE', ( #19748 ), #14134, .F. ) ;
#29723=EDGE_LOOP ( 'NONE', ( #4393, #43486, #6434, #14349 ) ) ;
#29726=CARTESIAN_POINT ( 'NONE',  ( -7.401770473315045784, -55.34844303569003898, -8.137215171343788356 ) ) ;
#29728=ORIENTED_EDGE ( 'NONE', *, *, #40709, .F. ) ;
#29731=EDGE_CURVE ( 'NONE', #8867, #19870, #53140, .T. ) ;
#29733=EDGE_CURVE ( 'NONE', #46351, #31027, #21396, .T. ) ;
#29736=ORIENTED_EDGE ( 'NONE', *, *, #1245, .T. ) ;
#29739=CARTESIAN_POINT ( 'NONE',  ( 8.813891479047955002, -25.01010130368346296, 8.872963530592734571 ) ) ;
#29740=CARTESIAN_POINT ( 'NONE',  ( 8.541162059860999634, -53.79199348416999982, 9.205819316548000231 ) ) ;
#29743=CARTESIAN_POINT ( 'NONE',  ( 0.000000000000000000, -5.899999999999999467, 0.000000000000000000 ) ) ;
#29747=CARTESIAN_POINT ( 'NONE',  ( -7.633501923154999425, -23.20104675770999947, 10.36289748052999826 ) ) ;
#29750=CARTESIAN_POINT ( 'NONE',  ( 9.778543098509999254, -61.84857981670000271, -8.284584910426000093 ) ) ;
#29752=DIRECTION ( 'NONE',  ( 0.9999999999999992228, 4.158392524217991108E-08, 7.906211575362985062E-12 ) ) ;
#29753=DIRECTION ( 'NONE',  ( 0.9859154929577472748, 0.1672442547470080754, 0.000000000000000000 ) ) ;
#29755=AXIS2_PLACEMENT_3D ( 'NONE', #23543, #5827, #50728 ) ;
#29757=CARTESIAN_POINT ( 'NONE',  ( 12.83836863002999884, -60.00626272179999887, -2.062146390631000248 ) ) ;
#29760=ADVANCED_FACE ( 'NONE', ( #10308 ), #23294, .F. ) ;
#29761=CARTESIAN_POINT ( 'NONE',  ( -3.098209881784000252, -2.427646227706999671, 1.748874889861999904 ) ) ;
#29765=CARTESIAN_POINT ( 'NONE',  ( -11.75000000000000000, -76.20000000000000284, -1.391479524197000231E-14 ) ) ;
#29768=CARTESIAN_POINT ( 'NONE',  ( -7.686918321221999584, -20.24439829127999957, 10.48771805383000100 ) ) ;
#29769=VECTOR ( 'NONE', #49277, 1000.000000000000000 ) ;
#29770=VERTEX_POINT ( 'NONE', #37157 ) ;
#29771=CARTESIAN_POINT ( 'NONE',  ( -10.55910102244999926, -19.21514526754999963, -7.642147947538999730 ) ) ;
#29775=CARTESIAN_POINT ( 'NONE',  ( -7.760939450761999758, -61.03085356300000086, 10.15321588361999972 ) ) ;
#29778=CARTESIAN_POINT ( 'NONE',  ( 8.485281374238999419, -59.94999999967000548, -8.485281374238999419 ) ) ;
#29784=ADVANCED_FACE ( 'NONE', ( #14426 ), #31869, .F. ) ;
#29786=EDGE_CURVE ( 'NONE', #51185, #15436, #12968, .T. ) ;
#29791=CARTESIAN_POINT ( 'NONE',  ( 1.799501877760999902, -55.51082434643999619, -12.60552522433000000 ) ) ;
#29792=CARTESIAN_POINT ( 'NONE',  ( -12.82904109066000053, -60.12452273675999947, 2.062673488410000200 ) ) ;
#29794=EDGE_CURVE ( 'NONE', #456, #47003, #47533, .T. ) ;
#29797=ORIENTED_EDGE ( 'NONE', *, *, #4570, .T. ) ;
#29801=ORIENTED_EDGE ( 'NONE', *, *, #1146, .F. ) ;
#29802=CARTESIAN_POINT ( 'NONE',  ( 7.765024210423000284, -17.90905971384000139, 9.830784063418001040 ) ) ;
#29805=CARTESIAN_POINT ( 'NONE',  ( 14.00000000000000000, -6.100000000000000533, 0.000000000000000000 ) ) ;
#29808=CARTESIAN_POINT ( 'NONE',  ( -9.186177604835998878, -78.22983485330000519, -8.911975928459002105 ) ) ;
#29809=VECTOR ( 'NONE', #32177, 1000.000000000000000 ) ;
#29810=CARTESIAN_POINT ( 'NONE',  ( -11.19999999999999929, -74.80000000000001137, 0.000000000000000000 ) ) ;
#29814=EDGE_CURVE ( 'NONE', #26014, #18217, #49517, .T. ) ;
#29816=CIRCLE ( 'NONE', #32641, 5.000000000000000888 ) ;
#29817=VERTEX_POINT ( 'NONE', #21474 ) ;
#29827=FACE_OUTER_BOUND ( 'NONE', #16303, .T. ) ;
#29829=CARTESIAN_POINT ( 'NONE',  ( -12.58338334675000070, -20.25199022618999933, -1.667961445601999992 ) ) ;
#29830=CARTESIAN_POINT ( 'NONE',  ( -5.866053559275163032, -78.43233687970867152, 10.46067059907391439 ) ) ;
#29832=CARTESIAN_POINT ( 'NONE',  ( -9.931052045577779097, -24.12278631289421682, -7.764003813950841604 ) ) ;
#29834=CARTESIAN_POINT ( 'NONE',  ( -12.52134121561647895, -60.72745484868465127, -1.618935178750646742 ) ) ;
#29835=EDGE_LOOP ( 'NONE', ( #29039, #29728, #40878 ) ) ;
#29838=CARTESIAN_POINT ( 'NONE',  ( 17.50000000000000000, -49.87071424677999687, 2.026612384852999926E-13 ) ) ;
#29840=CARTESIAN_POINT ( 'NONE',  ( -12.70556836347999941, -16.77227722772000007, 1.774192816106000118E-09 ) ) ;
#29842=CARTESIAN_POINT ( 'NONE',  ( 2.685641878552820661, -1.943966194794985336, -2.278905777910877006 ) ) ;
#29845=CARTESIAN_POINT ( 'NONE',  ( 12.00000000000000000, -23.15000000000000213, 0.8000000000000000444 ) ) ;
#29848=LINE ( 'NONE', #4156, #43037 ) ;
#29857=CARTESIAN_POINT ( 'NONE',  ( 1.318114156663148018, -17.26427522804863912, 12.70261578162694427 ) ) ;
#29859=CARTESIAN_POINT ( 'NONE',  ( 11.24215158465786324, -78.47224147109442072, 3.414609402431842522 ) ) ;
#29860=CARTESIAN_POINT ( 'NONE',  ( -7.610436523699135591, -60.32540704675938059, 10.41144397134750221 ) ) ;
#29861=EDGE_LOOP ( 'NONE', ( #34521, #26572, #31870, #44040 ) ) ;
#29870=DIRECTION ( 'NONE',  ( 1.000000000000000000, -3.446666965303000135E-11, 0.000000000000000000 ) ) ;
#29874=CARTESIAN_POINT ( 'NONE',  ( 1.799501877760999902, -23.28917565320000094, 12.60552522436000089 ) ) ;
#29878=ORIENTED_EDGE ( 'NONE', *, *, #48767, .F. ) ;
#29879=CARTESIAN_POINT ( 'NONE',  ( -12.44180763921999855, -54.70743932605000026, -1.459474665415000150 ) ) ;
#29880=ORIENTED_EDGE ( 'NONE', *, *, #36593, .F. ) ;
#29882=CARTESIAN_POINT ( 'NONE',  ( 10.18948929998999908, -23.21532694344000092, 7.645397820736000050 ) ) ;
#29887=EDGE_CURVE ( 'NONE', #16917, #38582, #6619, .T. ) ;
#29888=ORIENTED_EDGE ( 'NONE', *, *, #190, .T. ) ;
#29893=CARTESIAN_POINT ( 'NONE',  ( -12.77651047021000075, -62.10895689102999739, 0.04321256188116000263 ) ) ;
#29895=CARTESIAN_POINT ( 'NONE',  ( 7.612971540274999782, -18.67547726287999765, 10.53003236233000095 ) ) ;
#29896=CARTESIAN_POINT ( 'NONE',  ( 9.433548213746519195, -61.92797454583810435, 8.532643227366113692 ) ) ;
#29897=CARTESIAN_POINT ( 'NONE',  ( -10.04116292118000153, -19.23537109840999904, 7.682344222590000271 ) ) ;
#29899=DIRECTION ( 'NONE',  ( -1.000000000000000000, 0.000000000000000000, 0.000000000000000000 ) ) ;
#29901=AXIS2_PLACEMENT_3D ( 'NONE', #22561, #53863, #41149 ) ;
#29903=FACE_OUTER_BOUND ( 'NONE', #33461, .T. ) ;
#29907=CARTESIAN_POINT ( 'NONE',  ( -12.70228545259607955, -61.62820680317611277, 1.205254117661766600 ) ) ;
#29909=CARTESIAN_POINT ( 'NONE',  ( -1.798368564625000054, -18.80363242954000214, -12.61278090841000044 ) ) ;
#29910=VECTOR ( 'NONE', #51025, 1000.000000000000000 ) ;
#29913=CARTESIAN_POINT ( 'NONE',  ( 12.80088938722999892, -22.76256651757000071, 1.980532758767000301 ) ) ;
#29915=CARTESIAN_POINT ( 'NONE',  ( 2.050740132903084323, -3.500000000000000444, 2.700322267406692234 ) ) ;
#29916=CARTESIAN_POINT ( 'NONE',  ( -2.270853409273421608, -1.678612695437378122, 2.807048657911480394 ) ) ;
#29918=CARTESIAN_POINT ( 'NONE',  ( -11.75000000000000000, -75.80000000000001137, -9.948686767780999254E-14 ) ) ;
#29919=CYLINDRICAL_SURFACE ( 'NONE', #26671, 10.20000000000000107 ) ;
#29922=CARTESIAN_POINT ( 'NONE',  ( -0.9150818714851000069, -2.526649131856000263, 3.529087875733000423 ) ) ;
#29925=DIRECTION ( 'NONE',  ( 0.000000000000000000, 0.000000000000000000, -1.000000000000000000 ) ) ;
#29929=CARTESIAN_POINT ( 'NONE',  ( 0.000000000000000000, 0.000000000000000000, 0.000000000000000000 ) ) ;
#29931=CARTESIAN_POINT ( 'NONE',  ( 8.229676248979066244, -76.38669349085955673, -8.386630946024894229 ) ) ;
#29934=CARTESIAN_POINT ( 'NONE',  ( 7.674627477122999863, -19.24922971947000150, 10.14950121128000049 ) ) ;
#29937=CARTESIAN_POINT ( 'NONE',  ( 2.661813197064093472, -3.400464207879271950, 1.930198727209918363 ) ) ;
#29939=CARTESIAN_POINT ( 'NONE',  ( 13.94827586207000003, -45.69638659094999866, 8.082388075971999052E-06 ) ) ;
#29942=EDGE_CURVE ( 'NONE', #39794, #18938, #44073, .T. ) ;
#29947=ORIENTED_EDGE ( 'NONE', *, *, #40763, .F. ) ;
#29948=ADVANCED_FACE ( 'NONE', ( #4931 ), #42113, .T. ) ;
#29949=CARTESIAN_POINT ( 'NONE',  ( 0.5999999999999999778, -18.84999999999000053, 11.79999999999999893 ) ) ;
#29952=VECTOR ( 'NONE', #28568, 1000.000000000000114 ) ;
#29954=ORIENTED_EDGE ( 'NONE', *, *, #37347, .T. ) ;
#29958=CARTESIAN_POINT ( 'NONE',  ( 7.648026768024999811, -18.75000001589999954, -10.12290050218000026 ) ) ;
#29961=CARTESIAN_POINT ( 'NONE',  ( 10.36289662403999756, -60.00106470408999826, 7.633500902345000227 ) ) ;
#29962=ORIENTED_EDGE ( 'NONE', *, *, #7171, .F. ) ;
#29965=CARTESIAN_POINT ( 'NONE',  ( -10.98384528668754712, -18.77109020607789347, 0.5959859912294981354 ) ) ;
#29968=DIRECTION ( 'NONE',  ( -0.7071067811865475727, 0.000000000000000000, -0.7071067811865475727 ) ) ;
#29971=CARTESIAN_POINT ( 'NONE',  ( 12.64769468388000107, -77.23434608859999173, -3.464320626314000062 ) ) ;
#29977=CARTESIAN_POINT ( 'NONE',  ( 1.238562849883346084, -2.945020736201496181, 3.003986674293444015 ) ) ;
#29980=VECTOR ( 'NONE', #21842, 1000.000000000000000 ) ;
#29981=DIRECTION ( 'NONE',  ( 0.000000000000000000, 0.000000000000000000, -1.000000000000000000 ) ) ;
#29983=CARTESIAN_POINT ( 'NONE',  ( -8.333327861477410892, -76.26168058832676877, -8.283105682464439568 ) ) ;
#29984=CARTESIAN_POINT ( 'NONE',  ( 10.18589226631999978, -18.71082276572999703, 7.641012305223999768 ) ) ;
#29985=CARTESIAN_POINT ( 'NONE',  ( -9.770427757074999775, -61.85529868422999300, -8.292768371773000524 ) ) ;
#29989=CARTESIAN_POINT ( 'NONE',  ( -10.55511172854000002, -78.00228514651000467, 7.611100925114999249 ) ) ;
#29990=EDGE_CURVE ( 'NONE', #16041, #55326, #15078, .T. ) ;
#29993=CARTESIAN_POINT ( 'NONE',  ( 1.003693376009385796, -24.96223992107688971, -12.70247752664816510 ) ) ;
#29994=CARTESIAN_POINT ( 'NONE',  ( -10.48773066565999912, -76.04028235578000761, -6.823991308961000257 ) ) ;
#29995=ORIENTED_EDGE ( 'NONE', *, *, #38712, .F. ) ;
#29999=CARTESIAN_POINT ( 'NONE',  ( 12.43359700621999941, -61.50705514136999597, 0.8500729763766999847 ) ) ;
#30000=CARTESIAN_POINT ( 'NONE',  ( -11.27056218971000057, -79.04223899011000753, 6.053064779036000154 ) ) ;
#30001=DIRECTION ( 'NONE',  ( -0.0001230612157847738313, 0.000000000000000000, 0.9999999924279686647 ) ) ;
#30006=ORIENTED_EDGE ( 'NONE', *, *, #40270, .F. ) ;
#30012=CARTESIAN_POINT ( 'NONE',  ( 12.71798280852999952, -55.50221404479999876, 1.931086388455000025 ) ) ;
#30015=EDGE_CURVE ( 'NONE', #28471, #14201, #10528, .T. ) ;
#30017=EDGE_LOOP ( 'NONE', ( #45802, #4334, #3396, #11898 ) ) ;
#30019=CIRCLE ( 'NONE', #19679, 12.50000000000000000 ) ;
#30021=CARTESIAN_POINT ( 'NONE',  ( 1.750000000001000089, -60.05000000958000328, 12.56594317859000043 ) ) ;
#30023=VERTEX_POINT ( 'NONE', #36795 ) ;
#30029=CARTESIAN_POINT ( 'NONE',  ( 9.835237363953000411, -54.71864156536999957, 7.760968332694998750 ) ) ;
#30031=DIRECTION ( 'NONE',  ( -0.7071067811865969777, -0.7071067811864980568, -3.873916144559985708E-09 ) ) ;
#30032=FACE_OUTER_BOUND ( 'NONE', #52186, .T. ) ;
#30035=CARTESIAN_POINT ( 'NONE',  ( 9.369164850722000892, -60.04999999966999980, -7.601397897754999633 ) ) ;
#30036=CARTESIAN_POINT ( 'NONE',  ( -10.62397638184999948, -75.99013970749000180, -6.218250916117999516 ) ) ;
#30038=CARTESIAN_POINT ( 'NONE',  ( -1.081559480311999888, -0.7500000000000000000, 3.328697807033000000 ) ) ;
#30040=CARTESIAN_POINT ( 'NONE',  ( -12.54238283046690405, -23.52853599825456499, 1.749799162367805305 ) ) ;
#30041=CARTESIAN_POINT ( 'NONE',  ( 2.624826629463999694, -78.80583510652000712, 11.97953966613999910 ) ) ;
#30044=CARTESIAN_POINT ( 'NONE',  ( -4.697272406144668011, -78.45677523852745594, 11.11871297001820302 ) ) ;
#30049=FACE_OUTER_BOUND ( 'NONE', #33212, .T. ) ;
#30050=CARTESIAN_POINT ( 'NONE',  ( -0.2809113064957999839, -2.587250604645999985, -3.546626096927000038 ) ) ;
#30055=CARTESIAN_POINT ( 'NONE',  ( -11.35771826322349476, -75.79999999999999716, 3.694658569866112074 ) ) ;
#30060=EDGE_CURVE ( 'NONE', #525, #38648, #38291, .T. ) ;
#30061=CARTESIAN_POINT ( 'NONE',  ( -10.21380041495000057, -19.22847221992000044, -7.668936932643000581 ) ) ;
#30066=CARTESIAN_POINT ( 'NONE',  ( -2.599785613040999976, -0.9850476590665998566, 2.400557175927000131 ) ) ;
#30068=LINE ( 'NONE', #52529, #22975 ) ;
#30070=VERTEX_POINT ( 'NONE', #29958 ) ;
#30075=CARTESIAN_POINT ( 'NONE',  ( -10.01332844635999919, -55.51943307300000185, -7.654537085013999764 ) ) ;
#30078=VERTEX_POINT ( 'NONE', #28804 ) ;
#30082=CARTESIAN_POINT ( 'NONE',  ( -11.19999999861000006, -74.79999999860999083, -9.230037863942000436E-09 ) ) ;
#30091=EDGE_CURVE ( 'NONE', #15955, #43107, #25257, .T. ) ;
#30092=ORIENTED_EDGE ( 'NONE', *, *, #21561, .T. ) ;
#30096=CARTESIAN_POINT ( 'NONE',  ( 1.980610890454014283, -55.27926110484507660, 12.74374574604364341 ) ) ;
#30097=CARTESIAN_POINT ( 'NONE',  ( -1.184344363998000027, -77.19917510722000031, -12.90193715879000003 ) ) ;
#30099=CARTESIAN_POINT ( 'NONE',  ( -5.747123378374999980, -78.21567021303999923, 10.24856442990000005 ) ) ;
#30100=CARTESIAN_POINT ( 'NONE',  ( 0.000000000000000000, -0.1000000007601000024, 0.000000000000000000 ) ) ;
#30103=ORIENTED_EDGE ( 'NONE', *, *, #57529, .F. ) ;
#30104=CARTESIAN_POINT ( 'NONE',  ( -4.227801413918860145E-27, -6.000000000000000000, -13.89999999999999680 ) ) ;
#30105=ORIENTED_EDGE ( 'NONE', *, *, #27194, .T. ) ;
#30111=CARTESIAN_POINT ( 'NONE',  ( 9.090775133877240677, -76.50427104666793809, 7.448072922064946866 ) ) ;
#30114=VECTOR ( 'NONE', #35555, 1000.000000000000227 ) ;
#30115=EDGE_CURVE ( 'NONE', #10285, #15955, #47720, .T. ) ;
#30120=ADVANCED_FACE ( 'NONE', ( #56558 ), #28121, .F. ) ;
#30121=CARTESIAN_POINT ( 'NONE',  ( 10.59548767697000038, -21.75736537952000305, -7.678667886032999768 ) ) ;
#30125=ORIENTED_EDGE ( 'NONE', *, *, #21885, .T. ) ;
#30130=CARTESIAN_POINT ( 'NONE',  ( -12.71536175402382973, -17.87444297184845254, 1.781227265987796571 ) ) ;
#30136=CARTESIAN_POINT ( 'NONE',  ( 10.86177173228253956, -75.98064620389800439, 4.480746983072430467 ) ) ;
#30138=ORIENTED_EDGE ( 'NONE', *, *, #45220, .F. ) ;
#30141=CARTESIAN_POINT ( 'NONE',  ( 1.635689433014386296, -2.268028125413032559, -2.840897925314485928 ) ) ;
#30142=CARTESIAN_POINT ( 'NONE',  ( 1.876038030996965977, -78.83715597219580218, -11.74176995800102574 ) ) ;
#30143=DIRECTION ( 'NONE',  ( 0.000000000000000000, -1.000000000000000000, 0.000000000000000000 ) ) ;
#30146=CARTESIAN_POINT ( 'NONE',  ( 10.36222489919000012, -23.22120223852000009, -7.631889817950999522 ) ) ;
#30155=EDGE_CURVE ( 'NONE', #21348, #27676, #49742, .T. ) ;
#30157=CARTESIAN_POINT ( 'NONE',  ( -7.326354731301396583, -79.17057289994376390, -9.531881770301540158 ) ) ;
#30158=CARTESIAN_POINT ( 'NONE',  ( -1.538071403320043551, -77.68541666666666856, 11.74999999999999467 ) ) ;
#30159=DIRECTION ( 'NONE',  ( -1.000000000000000000, 0.000000000000000000, 0.000000000000000000 ) ) ;
#30163=AXIS2_PLACEMENT_3D ( 'NONE', #9200, #30739, #4185 ) ;
#30165=CARTESIAN_POINT ( 'NONE',  ( -1.232226824161543277, -61.32290911199032735, 12.50408896753025445 ) ) ;
#30166=CARTESIAN_POINT ( 'NONE',  ( -10.42531125072000009, -55.53514854654000032, -7.624341767124000135 ) ) ;
#30167=CARTESIAN_POINT ( 'NONE',  ( -12.57354097141999993, -23.72384125742000194, 1.757953070309000054 ) ) ;
#30168=ORIENTED_EDGE ( 'NONE', *, *, #47250, .F. ) ;
#30170=CARTESIAN_POINT ( 'NONE',  ( -12.54983130235000033, -53.74901607425999828, -0.1356732392833999989 ) ) ;
#30171=EDGE_LOOP ( 'NONE', ( #48070, #31630, #51163, #36654 ) ) ;
#30172=CARTESIAN_POINT ( 'NONE',  ( 0.4482635754052999855, -78.67990936191000628, -12.25553529036999834 ) ) ;
#30177=CARTESIAN_POINT ( 'NONE',  ( -12.50000000000000000, -60.04999999966999980, 1.250000000000000000 ) ) ;
#30178=ORIENTED_EDGE ( 'NONE', *, *, #27932, .F. ) ;
#30179=CONICAL_SURFACE ( 'NONE', #19843, 13.89999999994999946, 0.7853981633972997312 ) ;
#30184=CARTESIAN_POINT ( 'NONE',  ( -12.82230166705999963, -60.22260937973999972, -2.065916748305000272 ) ) ;
#30186=CARTESIAN_POINT ( 'NONE',  ( 7.682344222590000271, -19.23537109840999904, 10.04116292118000153 ) ) ;
#30188=CARTESIAN_POINT ( 'NONE',  ( -12.70556836352000118, -62.02772277195000328, -2.424224025342999716E-09 ) ) ;
#30191=CARTESIAN_POINT ( 'NONE',  ( 12.77301916226999978, -16.94808379552999966, -1.052060437765000023 ) ) ;
#30192=CARTESIAN_POINT ( 'NONE',  ( 1.980532758766000212, -56.03743349309000621, 12.80088938803999810 ) ) ;
#30193=CARTESIAN_POINT ( 'NONE',  ( -10.52337198490644710, -76.66276897022568448, 5.229864349995584583 ) ) ;
#30194=B_SPLINE_CURVE_WITH_KNOTS ( 'NONE', 3,
 ( #5915, #1804, #46098, #5054, #45508, #50518 ),
 .UNSPECIFIED., .F., .F.,
 ( 4, 2, 4 ),
 ( 0.000000000000000000, 0.5000000000000000000, 1.000000000000000000 ),
 .UNSPECIFIED. ) ;
#30195=EDGE_LOOP ( 'NONE', ( #54638, #55975, #19772, #56710 ) ) ;
#30196=CARTESIAN_POINT ( 'NONE',  ( -7.633403241802001027, -55.41350283619000550, 10.18127013546999926 ) ) ;
#30198=CARTESIAN_POINT ( 'NONE',  ( -8.958657468039000094, -16.79887336309000290, -8.950049500644999156 ) ) ;
#30200=DIRECTION ( 'NONE',  ( 0.000000000000000000, 1.433665241479999788E-08, -0.9999999999999998890 ) ) ;
#30202=AXIS2_PLACEMENT_3D ( 'NONE', #39522, #48973, #13232 ) ;
#30203=CARTESIAN_POINT ( 'NONE',  ( 3.162950201720829746, -1.330633240748065660, -0.8520949969437336957 ) ) ;
#30207=CARTESIAN_POINT ( 'NONE',  ( 12.52785920744742398, -23.79405666946011166, 1.668536824485531200 ) ) ;
#30211=EDGE_CURVE ( 'NONE', #2137, #25757, #15806, .T. ) ;
#30212=CARTESIAN_POINT ( 'NONE',  ( -12.50728630770449001, -24.99975539312151795, 0.1757873578728431363 ) ) ;
#30213=CARTESIAN_POINT ( 'NONE',  ( -12.49306764015999960, -23.28056535155999995, 1.667917367065999912 ) ) ;
#30214=CARTESIAN_POINT ( 'NONE',  ( 3.801730483759000023, -3.472300407297999936, 0.1797210791774999927 ) ) ;
#30219=DIRECTION ( 'NONE',  ( 0.7071067811865475727, 0.000000000000000000, 0.7071067811865475727 ) ) ;
#30222=B_SPLINE_CURVE_WITH_KNOTS ( 'NONE', 3,
 ( #44871, #30682, #8264, #25972, #43999, #49301, #39556, #17716, #35106, #48720, #53141, #53729, #26264, #3836, #57854, #17411, #53426, #12969, #26544, #22125, #10319, #5874, #54319, #13859 ),
 .UNSPECIFIED., .F., .F.,
 ( 4, 2, 2, 2, 2, 2, 2, 2, 2, 2, 2, 4 ),
 ( 0.000000000000000000, 0.1250000000000002498, 0.2500000000000004996, 0.3750000000000007772, 0.4375000000000011657, 0.5000000000000015543, 0.6250000000000028866, 0.7500000000000043299, 0.8125000000000045519, 0.8437500000000038858, 0.8750000000000033307, 1.000000000000000000 ),
 .UNSPECIFIED. ) ;
#30227=CARTESIAN_POINT ( 'NONE',  ( 10.81612714324542779, -76.41779430387406080, -4.590319906461707511 ) ) ;
#30235=DIRECTION ( 'NONE',  ( 0.000000000000000000, 1.000000000000000000, 0.000000000000000000 ) ) ;
#30241=ORIENTED_EDGE ( 'NONE', *, *, #209, .F. ) ;
#30242=DIRECTION ( 'NONE',  ( 0.000000000000000000, -1.000000000000000000, 0.000000000000000000 ) ) ;
#30243=AXIS2_PLACEMENT_3D ( 'NONE', #23341, #23047, #8889 ) ;
#30251=ORIENTED_EDGE ( 'NONE', *, *, #48146, .F. ) ;
#30252=CARTESIAN_POINT ( 'NONE',  ( -11.47456978792000015, -79.03590068956999914, -4.589774320666000662 ) ) ;
#30259=LINE ( 'NONE', #16706, #41884 ) ;
#30262=CARTESIAN_POINT ( 'NONE',  ( 12.62753648294000008, -77.73388785726000094, -3.537092078510000182 ) ) ;
#30268=FACE_OUTER_BOUND ( 'NONE', #11824, .T. ) ;
#30269=CARTESIAN_POINT ( 'NONE',  ( 1.233621921305137370, -2.945159437469935693, 3.006013160803045814 ) ) ;
#30271=B_SPLINE_CURVE_WITH_KNOTS ( 'NONE', 3,
 ( #27659, #50128, #45996, #18823, #9381, #1125 ),
 .UNSPECIFIED., .F., .F.,
 ( 4, 1, 1, 4 ),
 ( 0.000000000000000000, 0.3333333333333000081, 0.6666666666667000474, 1.000000000000000000 ),
 .UNSPECIFIED. ) ;
#30274=CARTESIAN_POINT ( 'NONE',  ( -1.209804193477999945, -2.347258720801999932, -3.608664049297999998 ) ) ;
#30276=CARTESIAN_POINT ( 'NONE',  ( -7.601397897754999633, -55.55000000209000177, -10.07627163191000008 ) ) ;
#30281=CIRCLE ( 'NONE', #15210, 12.05000000000000071 ) ;
#30283=CARTESIAN_POINT ( 'NONE',  ( 12.55073801092999908, -77.28072481401001426, -3.437763296274999991 ) ) ;
#30284=AXIS2_PLACEMENT_3D ( 'NONE', #12524, #24947, #20806 ) ;
#30286=CARTESIAN_POINT ( 'NONE',  ( 1.722320549971293024, -24.23663688827699403, -12.71171904436489797 ) ) ;
#30287=CARTESIAN_POINT ( 'NONE',  ( 4.917835995879999977, -76.82652295158999323, -11.17807926867999946 ) ) ;
#30291=EDGE_CURVE ( 'NONE', #3967, #13029, #48792, .T. ) ;
#30292=CARTESIAN_POINT ( 'NONE',  ( 12.83838776462000020, -60.00596988455000513, 2.062170466182000172 ) ) ;
#30293=CARTESIAN_POINT ( 'NONE',  ( 7.682331425195999763, -19.23513569609999863, -10.04115011120000034 ) ) ;
#30303=CARTESIAN_POINT ( 'NONE',  ( 12.80896991324999945, -58.55453807205000061, 1.930989179114000143 ) ) ;
#30309=EDGE_LOOP ( 'NONE', ( #18372, #55171, #48782, #12326, #57334 ) ) ;
#30311=CYLINDRICAL_SURFACE ( 'NONE', #28571, 1.750000000000000000 ) ;
#30312=CARTESIAN_POINT ( 'NONE',  ( 3.985185646092895606, -1.087326648717707789, -0.5301898958182351684 ) ) ;
#30313=ORIENTED_EDGE ( 'NONE', *, *, #17520, .F. ) ;
#30314=CARTESIAN_POINT ( 'NONE',  ( -12.71005379439038663, -24.29489531516004064, -1.687596143068920140 ) ) ;
#30316=CARTESIAN_POINT ( 'NONE',  ( 2.624826629463999694, -78.90783571398633001, 11.97953966613999910 ) ) ;
#30318=EDGE_CURVE ( 'NONE', #30070, #16697, #46801, .T. ) ;
#30319=VECTOR ( 'NONE', #24673, 1000.000000000000000 ) ;
#30320=CARTESIAN_POINT ( 'NONE',  ( 9.778561352688999619, -53.75143577336000078, 8.284566532368000225 ) ) ;
#30324=CARTESIAN_POINT ( 'NONE',  ( 12.71106812367828454, -61.05135172934481602, -1.717582538848928309 ) ) ;
#30327=CARTESIAN_POINT ( 'NONE',  ( -7.961052042448998556, -24.53567435024999810, 9.783216378915000178 ) ) ;
#30330=CARTESIAN_POINT ( 'NONE',  ( -12.50686498856104478, -24.30484291404696151, 1.423095204833915384 ) ) ;
#30332=CARTESIAN_POINT ( 'NONE',  ( -7.601397897754999633, -23.25000000000000000, -9.369164850722000892 ) ) ;
#30333=CARTESIAN_POINT ( 'NONE',  ( 0.000000000000000000, -13.07071424677999971, 0.000000000000000000 ) ) ;
#30334=DIRECTION ( 'NONE',  ( 0.000000000000000000, 1.000000000000000000, 0.000000000000000000 ) ) ;
#30341=CARTESIAN_POINT ( 'NONE',  ( -2.042632565901000063, -3.544876866276999827, -2.913050207213999876 ) ) ;
#30345=CARTESIAN_POINT ( 'NONE',  ( -5.376030604968692117, -75.79999999999999716, 10.62656574052478753 ) ) ;
#30353=EDGE_CURVE ( 'NONE', #15969, #16250, #46928, .T. ) ;
#30356=VECTOR ( 'NONE', #46502, 1000.000000000000114 ) ;
#30357=CARTESIAN_POINT ( 'NONE',  ( -2.373463140952000394, -1.290903522605000076, -3.049005324064999911 ) ) ;
#30359=CARTESIAN_POINT ( 'NONE',  ( 12.46083365854999769, -23.68341615479999973, -1.628972628240999976 ) ) ;
#30360=DIRECTION ( 'NONE',  ( 1.000000000000000000, 0.000000000000000000, 0.000000000000000000 ) ) ;
#30363=CARTESIAN_POINT ( 'NONE',  ( -12.60354432324999863, -56.04899162853999428, 1.750000000000000000 ) ) ;
#30364=PLANE ( 'NONE',  #6375 ) ;
#30367=CIRCLE ( 'NONE', #4939, 0.5000000000000004441 ) ;
#30370=DIRECTION ( 'NONE',  ( 0.000000000000000000, -1.000000000000000000, 0.000000000000000000 ) ) ;
#30372=AXIS2_PLACEMENT_3D ( 'NONE', #12665, #8525, #26518 ) ;
#30374=B_SPLINE_CURVE_WITH_KNOTS ( 'NONE', 3,
 ( #48901, #44459, #22015, #40023, #17597, #28184 ),
 .UNSPECIFIED., .F., .F.,
 ( 4, 2, 4 ),
 ( 0.000000000000000000, 0.5000000000000000000, 1.000000000000000000 ),
 .UNSPECIFIED. ) ;
#30375=CARTESIAN_POINT ( 'NONE',  ( -12.69616050746999925, -57.04828923575999511, 1.799475304559999822 ) ) ;
#30376=CARTESIAN_POINT ( 'NONE',  ( -8.652389292562999046, -53.53734871844999788, -9.414476472778000371 ) ) ;
#30385=DIRECTION ( 'NONE',  ( 0.9999433559010179051, 0.000000000000000000, 0.01064354214585019887 ) ) ;
#30388=CARTESIAN_POINT ( 'NONE',  ( 11.75000000000000000, -76.05000000000001137, 0.000000000000000000 ) ) ;
#30389=CARTESIAN_POINT ( 'NONE',  ( 12.15305909882999913, -78.48342962590999150, -3.479748152880000056 ) ) ;
#30390=EDGE_CURVE ( 'NONE', #7685, #7374, #747, .T. ) ;
#30392=CARTESIAN_POINT ( 'NONE',  ( 13.63885489310999510, -19.21421830981000056, 7.254376133916000668 ) ) ;
#30396=CARTESIAN_POINT ( 'NONE',  ( 1.980584515756000030, -55.53514849873000259, -12.76303204337999908 ) ) ;
#30397=ORIENTED_EDGE ( 'NONE', *, *, #33002, .T. ) ;
#30401=FACE_OUTER_BOUND ( 'NONE', #7099, .T. ) ;
#30405=DIRECTION ( 'NONE',  ( 0.000000000000000000, -1.000000000000000000, 0.000000000000000000 ) ) ;
#30408=CARTESIAN_POINT ( 'NONE',  ( -1.335477334469999862E-14, -72.70000000000000284, 0.000000000000000000 ) ) ;
#30411=CARTESIAN_POINT ( 'NONE',  ( 10.98362417419999915, -18.84999999999999787, 0.5999999999999999778 ) ) ;
#30414=CONICAL_SURFACE ( 'NONE', #45534, 13.94999999994999840, 0.7853981633972997312 ) ;
#30416=B_SPLINE_CURVE_WITH_KNOTS ( 'NONE', 3,
 ( #54924, #10067, #28047, #46093 ),
 .UNSPECIFIED., .F., .F.,
 ( 4, 4 ),
 ( 0.000000000000000000, 1.000000000000000000 ),
 .UNSPECIFIED. ) ;
#30417=EDGE_LOOP ( 'NONE', ( #24895, #35606, #54872, #46072 ) ) ;
#30423=CARTESIAN_POINT ( 'NONE',  ( -12.70249541838816576, -17.03496187199482392, 0.9988462570818790187 ) ) ;
#30424=CIRCLE ( 'NONE', #34213, 1.250000000000000444 ) ;
#30426=CARTESIAN_POINT ( 'NONE',  ( -2.513431698483562293, -2.188227315379490445, 2.466895036164149957 ) ) ;
#30428=CARTESIAN_POINT ( 'NONE',  ( -0.005119011380322999356, -53.86186137778000216, -12.43705489340000092 ) ) ;
#30429=CARTESIAN_POINT ( 'NONE',  ( 10.06040271365206529, -75.99314077920472243, 6.073823502367483584 ) ) ;
#30431=AXIS2_PLACEMENT_3D ( 'NONE', #15273, #50003, #36112 ) ;
#30432=CARTESIAN_POINT ( 'NONE',  ( -7.488678058322025599, -78.62828703116568363, 9.109634963579681610 ) ) ;
#30433=CARTESIAN_POINT ( 'NONE',  ( -0.4259899833590489737, -2.215981609665019558, -3.248268024827842826 ) ) ;
#30434=CARTESIAN_POINT ( 'NONE',  ( 10.50046875551768366, -78.91200283610369581, -5.354272345414459622 ) ) ;
#30440=CARTESIAN_POINT ( 'NONE',  ( 1.103931348481366204, -17.37916251880048080, -12.50298439258972039 ) ) ;
#30443=DIRECTION ( 'NONE',  ( 1.000000000000000000, 0.000000000000000000, 0.000000000000000000 ) ) ;
#30448=CARTESIAN_POINT ( 'NONE',  ( -11.44417895085272008, -77.77916666666666856, 3.075537641221497420 ) ) ;
#30450=AXIS2_PLACEMENT_3D ( 'NONE', #25633, #56940, #42503 ) ;
#30454=ORIENTED_EDGE ( 'NONE', *, *, #19768, .T. ) ;
#30455=EDGE_CURVE ( 'NONE', #36484, #19156, #9520, .T. ) ;
#30456=CARTESIAN_POINT ( 'NONE',  ( -1.749899258079942843, -60.18716848725600954, 12.55433901293707599 ) ) ;
#30457=CARTESIAN_POINT ( 'NONE',  ( 2.062502994258999856, -21.75648180056000314, 12.92181194095000052 ) ) ;
#30459=CIRCLE ( 'NONE', #1294, 13.94827586206999825 ) ;
#30460=CARTESIAN_POINT ( 'NONE',  ( 7.220923959705223716, -76.12291666666662593, 9.396085398178630754 ) ) ;
#30461=VERTEX_POINT ( 'NONE', #5093 ) ;
#30463=FACE_OUTER_BOUND ( 'NONE', #28927, .T. ) ;
#30466=ORIENTED_EDGE ( 'NONE', *, *, #9903, .T. ) ;
#30469=AXIS2_PLACEMENT_3D ( 'NONE', #39736, #49188, #22906 ) ;
#30473=CIRCLE ( 'NONE', #31438, 0.8000000000000000444 ) ;
#30476=VERTEX_POINT ( 'NONE', #20909 ) ;
#30482=CARTESIAN_POINT ( 'NONE',  ( 7.705119999407000542, -21.75171076523999858, 10.24996238026999862 ) ) ;
#30486=CARTESIAN_POINT ( 'NONE',  ( -7.919595949288999570, -59.94999999446000771, 8.768124086549999419 ) ) ;
#30487=DIRECTION ( 'NONE',  ( -1.000000000000000000, 0.000000000000000000, 0.000000000000000000 ) ) ;
#30488=CARTESIAN_POINT ( 'NONE',  ( -11.52087155025212972, -76.68407063598148454, 2.308491139881042375 ) ) ;
#30489=EDGE_LOOP ( 'NONE', ( #12539, #30683, #28739, #14860, #5438, #32724 ) ) ;
#30491=CARTESIAN_POINT ( 'NONE',  ( -7.658894278873999539, -55.59060682883999505, 10.01676917980999981 ) ) ;
#30493=CARTESIAN_POINT ( 'NONE',  ( -10.00844281758000065, -18.63109810616999695, -7.647097920691000361 ) ) ;
#30494=CARTESIAN_POINT ( 'NONE',  ( -12.76303204298000082, -60.06485150663000638, 1.980584515756000030 ) ) ;
#30495=CARTESIAN_POINT ( 'NONE',  ( -1.056237665594999875, -16.95133986302000295, -12.77256098197999989 ) ) ;
#30496=DIRECTION ( 'NONE',  ( -1.000000000000000000, 0.000000000000000000, 0.000000000000000000 ) ) ;
#30500=CARTESIAN_POINT ( 'NONE',  ( 3.500000000000000000, -3.500000000000000000, 1.049058100190999900E-13 ) ) ;
#30503=DIRECTION ( 'NONE',  ( 0.000000000000000000, -1.000000000000000000, 0.000000000000000000 ) ) ;
#30504=AXIS2_PLACEMENT_3D ( 'NONE', #37864, #37274, #14838 ) ;
#30505=CARTESIAN_POINT ( 'NONE',  ( -0.5045596072235000173, -53.66471086928999767, 12.66210649705999991 ) ) ;
#30506=CARTESIAN_POINT ( 'NONE',  ( -12.92181194095000052, -21.75648180056000314, 2.062502994258999856 ) ) ;
#30507=CARTESIAN_POINT ( 'NONE',  ( -0.5150151199216000952, -3.104341653420000124, 3.771016058666000426 ) ) ;
#30511=DIRECTION ( 'NONE',  ( 0.7071067811865475727, 0.000000000000000000, 0.7071067811865475727 ) ) ;
#30512=CARTESIAN_POINT ( 'NONE',  ( -8.485281374238999419, -60.04999999966999980, -8.485281374238999419 ) ) ;
#30516=CARTESIAN_POINT ( 'NONE',  ( -4.229409687621918934, -76.85652762026346352, 11.31572571056822341 ) ) ;
#30517=CARTESIAN_POINT ( 'NONE',  ( 10.77656672099982949, -76.41708097615209283, -4.682833356338025332 ) ) ;
#30520=CARTESIAN_POINT ( 'NONE',  ( -2.188064519153326781, -1.035140800317944532, 2.430261573971487010 ) ) ;
#30523=DIRECTION ( 'NONE',  ( 0.000000000000000000, 0.000000000000000000, -1.000000000000000000 ) ) ;
#30526=CARTESIAN_POINT ( 'NONE',  ( -7.635939924820385194, -18.22474192285963923, -10.36595855977485137 ) ) ;
#30527=EDGE_CURVE ( 'NONE', #57635, #42021, #16490, .T. ) ;
#30530=CARTESIAN_POINT ( 'NONE',  ( -12.50000000000000000, -23.24999999758999536, 1.750000000000000000 ) ) ;
#30531=DIRECTION ( 'NONE',  ( 0.6562721000521710701, 0.7545243075561669510, -7.880219195195659585E-10 ) ) ;
#30532=ORIENTED_EDGE ( 'NONE', *, *, #25893, .T. ) ;
#30534=CARTESIAN_POINT ( 'NONE',  ( 12.50728617052612357, -17.00024476466254342, 0.1757991157707580188 ) ) ;
#30536=FACE_OUTER_BOUND ( 'NONE', #28805, .T. ) ;
#30537=ORIENTED_EDGE ( 'NONE', *, *, #6888, .T. ) ;
#30544=ORIENTED_EDGE ( 'NONE', *, *, #2671, .F. ) ;
#30546=CARTESIAN_POINT ( 'NONE',  ( -12.11584633110999931, -78.48982704611999850, 2.436790123298999688 ) ) ;
#30548=VERTEX_POINT ( 'NONE', #46138 ) ;
#30549=DIRECTION ( 'NONE',  ( 0.7071067812087692417, 2.829528277810876343E-07, -0.7071067811642691714 ) ) ;
#30550=LINE ( 'NONE', #48582, #2008 ) ;
#30556=CARTESIAN_POINT ( 'NONE',  ( 12.66594527011999816, -76.73480431993999673, -3.392478259704000187 ) ) ;
#30557=CARTESIAN_POINT ( 'NONE',  ( 6.694424008027000106, -76.41805712980000465, -9.543441777632999390 ) ) ;
#30558=EDGE_CURVE ( 'NONE', #48463, #21680, #34616, .T. ) ;
#30563=CARTESIAN_POINT ( 'NONE',  ( -1.273994397749967256, -3.008312834910695788, 2.989085386252882781 ) ) ;
#30567=CARTESIAN_POINT ( 'NONE',  ( -0.4587696627765999735, -3.432718315767000039, -3.778272981138000031 ) ) ;
#30569=VERTEX_POINT ( 'NONE', #50348 ) ;
#30571=PLANE ( 'NONE',  #44922 ) ;
#30572=AXIS2_PLACEMENT_3D ( 'NONE', #24825, #25110, #43135 ) ;
#30574=CARTESIAN_POINT ( 'NONE',  ( -12.77297374713000089, -17.27184670111999765, -1.476174539902000094 ) ) ;
#30575=CARTESIAN_POINT ( 'NONE',  ( -10.64207148833999916, -77.00320160920000490, 7.489034475093999887 ) ) ;
#30576=B_SPLINE_CURVE_WITH_KNOTS ( 'NONE', 3,
 ( #57823, #48977, #3803, #4093, #21806, #12376, #53112, #26812 ),
 .UNSPECIFIED., .F., .F.,
 ( 4, 2, 2, 4 ),
 ( 0.000000000000000000, 0.5000000000000026645, 0.7500000000000013323, 1.000000000000000000 ),
 .UNSPECIFIED. ) ;
#30578=DIRECTION ( 'NONE',  ( -0.7071067811864980568, 1.531837635818995070E-11, 0.7071067811865969777 ) ) ;
#30579=CARTESIAN_POINT ( 'NONE',  ( 9.424223717388999333, -76.77544674281999448, -8.000359493957999391 ) ) ;
#30581=CIRCLE ( 'NONE', #19316, 0.5000000000000004441 ) ;
#30582=DIRECTION ( 'NONE',  ( -1.000000000000000000, 0.000000000000000000, 0.000000000000000000 ) ) ;
#30583=DIRECTION ( 'NONE',  ( 1.894056204930980603E-11, 1.538483568841980365E-07, -0.9999999999999882316 ) ) ;
#30584=CARTESIAN_POINT ( 'NONE',  ( -10.98675469975087182, -18.58582062461403339, -0.5398555193318074208 ) ) ;
#30585=CARTESIAN_POINT ( 'NONE',  ( -1.667961430005999945, -20.25111654322000021, -12.58335110166999904 ) ) ;
#30595=ORIENTED_EDGE ( 'NONE', *, *, #10366, .F. ) ;
#30597=CARTESIAN_POINT ( 'NONE',  ( 12.87024489158000051, -56.01538333533000014, 2.062597265787999845 ) ) ;
#30599=ORIENTED_EDGE ( 'NONE', *, *, #41362, .F. ) ;
#30606=VERTEX_POINT ( 'NONE', #55937 ) ;
#30608=ORIENTED_EDGE ( 'NONE', *, *, #22891, .F. ) ;
#30609=CARTESIAN_POINT ( 'NONE',  ( -10.61911868076999887, -78.59168781514685520, -6.134606423928000041 ) ) ;
#30610=VECTOR ( 'NONE', #6382, 1000.000000000000000 ) ;
#30612=CARTESIAN_POINT ( 'NONE',  ( 7.647736468613000049, -55.07704514418999509, 10.13404651203999940 ) ) ;
#30613=CARTESIAN_POINT ( 'NONE',  ( -7.612971540274999782, -18.67547726287999765, -10.53003236233000095 ) ) ;
#30614=DIRECTION ( 'NONE',  ( 0.7071067811865475727, 0.000000000000000000, -0.7071067811865475727 ) ) ;
#30615=AXIS2_PLACEMENT_3D ( 'NONE', #55640, #47384, #24923 ) ;
#30616=CARTESIAN_POINT ( 'NONE',  ( 12.70556836326691119, -62.02772277412548618, -0.2597962961632950818 ) ) ;
#30617=ADVANCED_FACE ( 'NONE', ( #28756 ), #39857, .F. ) ;
#30620=CARTESIAN_POINT ( 'NONE',  ( -8.541150802303999257, -25.00800189280999675, 9.205830468593999782 ) ) ;
#30625=DIRECTION ( 'NONE',  ( 0.000000000000000000, 1.000000000000000000, 0.000000000000000000 ) ) ;
#30627=DIRECTION ( 'NONE',  ( 0.000000000000000000, -1.000000000000000000, -1.480297366168000156E-13 ) ) ;
#30630=CARTESIAN_POINT ( 'NONE',  ( 8.485281374238999419, -23.25000000000000000, 8.485281374238999419 ) ) ;
#30632=CARTESIAN_POINT ( 'NONE',  ( 0.000000000000000000, -26.30294702885999669, -12.53545825868000207 ) ) ;
#30633=EDGE_CURVE ( 'NONE', #1462, #39052, #33180, .T. ) ;
#30635=CARTESIAN_POINT ( 'NONE',  ( -1.980464483675000054, -58.55560170709000545, 12.85140862643000048 ) ) ;
#30636=CARTESIAN_POINT ( 'NONE',  ( 0.000000000000000000, -3.000000000000000000, 0.000000000000000000 ) ) ;
#30646=VECTOR ( 'NONE', #13270, 1000.000000000000114 ) ;
#30649=CARTESIAN_POINT ( 'NONE',  ( 12.61271904360000029, -23.19692351046000311, -1.798332623270999964 ) ) ;
#30652=LINE ( 'NONE', #57821, #34261 ) ;
#30654=CARTESIAN_POINT ( 'NONE',  ( 9.722718241315000398, -18.75000000000000000, 7.954951288349001004 ) ) ;
#30658=DIRECTION ( 'NONE',  ( 0.000000000000000000, 1.000000000000000000, 0.000000000000000000 ) ) ;
#30659=CARTESIAN_POINT ( 'NONE',  ( -5.915435705384207488, -77.78186773030601842, -10.26011948101617755 ) ) ;
#30660=DIRECTION ( 'NONE',  ( -0.7071067811865473507, -1.433670265776094594E-08, 0.7071067811865473507 ) ) ;
#30662=CARTESIAN_POINT ( 'NONE',  ( -7.659225706216000518, -55.11732795990999989, -9.963487823480999594 ) ) ;
#30668=CARTESIAN_POINT ( 'NONE',  ( 8.485281374238999419, -59.94999999967000548, 8.485281374238999419 ) ) ;
#30669=EDGE_CURVE ( 'NONE', #40915, #20424, #42647, .T. ) ;
#30671=EDGE_LOOP ( 'NONE', ( #25315, #44236, #33045, #15931 ) ) ;
#30674=CARTESIAN_POINT ( 'NONE',  ( 11.89999999977000122, -23.15000000000000213, 0.000000000000000000 ) ) ;
#30675=CARTESIAN_POINT ( 'NONE',  ( -9.194628130165000357, -77.14367046626000501, -9.128060447331000304 ) ) ;
#30678=CARTESIAN_POINT ( 'NONE',  ( -7.624341764926000131, -23.26485149464000202, 10.42531124853000080 ) ) ;
#30682=CARTESIAN_POINT ( 'NONE',  ( 7.610436392416016105, -18.47459049295285993, 10.41144384038989656 ) ) ;
#30683=ORIENTED_EDGE ( 'NONE', *, *, #52060, .T. ) ;
#30685=FACE_OUTER_BOUND ( 'NONE', #7538, .T. ) ;
#30687=CARTESIAN_POINT ( 'NONE',  ( -12.65375411752000012, -20.25022861081000158, -1.750000000000000000 ) ) ;
#30688=CIRCLE ( 'NONE', #36489, 0.8000000000000011546 ) ;
#30689=CARTESIAN_POINT ( 'NONE',  ( 1.733997378035627035, -60.32383216727249930, -12.54437956615601202 ) ) ;
#30691=CARTESIAN_POINT ( 'NONE',  ( 12.80896991324000034, -21.75453807238000081, 1.930989179114000143 ) ) ;
#30692=CARTESIAN_POINT ( 'NONE',  ( -5.917523019358107206, -76.71666666666662593, 10.26699006316250795 ) ) ;
#30693=FACE_OUTER_BOUND ( 'NONE', #459, .T. ) ;
#30696=AXIS2_PLACEMENT_3D ( 'NONE', #50621, #28738, #41749 ) ;
#30697=CARTESIAN_POINT ( 'NONE',  ( 10.38645071867999903, -22.77819125662999866, -7.655542440070999710 ) ) ;
#30699=CARTESIAN_POINT ( 'NONE',  ( -7.342331066867000544, -55.64999999967000122, -8.190859204290999784 ) ) ;
#30700=ORIENTED_EDGE ( 'NONE', *, *, #22178, .F. ) ;
#30703=CARTESIAN_POINT ( 'NONE',  ( -13.99999999996999911, -5.900000000026950353, 3.874891027003000340E-10 ) ) ;
#30709=CARTESIAN_POINT ( 'NONE',  ( -0.005928781627726999008, -53.59886949703999903, -12.66336824414000084 ) ) ;
#30711=DIRECTION ( 'NONE',  ( 0.000000000000000000, 1.000000000000000000, 0.000000000000000000 ) ) ;
#30714=CARTESIAN_POINT ( 'NONE',  ( 2.599382155498818570, -2.299256034861846043, -1.997070427629134448 ) ) ;
#30715=CARTESIAN_POINT ( 'NONE',  ( -0.01679078366784302057, -78.82468149487773701, -11.88860714937941054 ) ) ;
#30720=CARTESIAN_POINT ( 'NONE',  ( 1.811016405462505530, -17.93826444626764172, 12.71771640064008579 ) ) ;
#30722=CARTESIAN_POINT ( 'NONE',  ( -3.845786535788662253, -78.59967399330191995, 11.15268554086950559 ) ) ;
#30723=CARTESIAN_POINT ( 'NONE',  ( 10.07627163191000008, -60.04999999657000131, -7.601397897754999633 ) ) ;
#30725=ADVANCED_FACE ( 'NONE', ( #38782 ), #30891, .F. ) ;
#30728=CARTESIAN_POINT ( 'NONE',  ( 3.679515170149685765, -75.79999999999999716, -11.28544018175951358 ) ) ;
#30735=AXIS2_PLACEMENT_3D ( 'NONE', #49035, #3010, #35729 ) ;
#30737=CARTESIAN_POINT ( 'NONE',  ( 9.102137320399311449, -17.02814024880371591, -8.583672455337429952 ) ) ;
#30738=TOROIDAL_SURFACE ( 'NONE', #46814, 1.250000000000000000, 0.5000000000000000000 ) ;
#30739=DIRECTION ( 'NONE',  ( 0.000000000000000000, 1.000000000000000000, 0.000000000000000000 ) ) ;
#30744=DIRECTION ( 'NONE',  ( 0.000000000000000000, -1.000000000000000000, 0.000000000000000000 ) ) ;
#30745=EDGE_CURVE ( 'NONE', #51037, #56909, #9335, .T. ) ;
#30747=CYLINDRICAL_SURFACE ( 'NONE', #5667, 12.50000000000000000 ) ;
#30748=ORIENTED_EDGE ( 'NONE', *, *, #35119, .F. ) ;
#30749=CARTESIAN_POINT ( 'NONE',  ( 10.01749676170999948, -23.19181054693000021, 7.660430254659999605 ) ) ;
#30754=EDGE_CURVE ( 'NONE', #36961, #26860, #10119, .T. ) ;
#30756=EDGE_LOOP ( 'NONE', ( #51441, #38836, #48138, #39980 ) ) ;
#30759=EDGE_CURVE ( 'NONE', #8704, #7685, #49483, .T. ) ;
#30761=CARTESIAN_POINT ( 'NONE',  ( 6.037385872459999803, -75.75138372272999732, 10.30991454870999924 ) ) ;
#30765=FACE_OUTER_BOUND ( 'NONE', #53883, .T. ) ;
#30767=CARTESIAN_POINT ( 'NONE',  ( -11.51760730114658848, -76.68396387802945924, 2.324764085046806983 ) ) ;
#30768=ORIENTED_EDGE ( 'NONE', *, *, #43060, .T. ) ;
#30769=B_SPLINE_CURVE_WITH_KNOTS ( 'NONE', 3,
 ( #23475, #1073, #33193, #50656, #51239, #10202, #46821, #37926 ),
 .UNSPECIFIED., .F., .F.,
 ( 4, 2, 2, 4 ),
 ( 0.000000000000000000, 0.5000000000000026645, 0.7500000000000013323, 1.000000000000000000 ),
 .UNSPECIFIED. ) ;
#30773=CARTESIAN_POINT ( 'NONE',  ( -10.01752115541999899, -18.80828330197000042, -7.660412752602000275 ) ) ;
#30774=AXIS2_PLACEMENT_3D ( 'NONE', #37751, #55773, #33314 ) ;
#30775=CARTESIAN_POINT ( 'NONE',  ( 7.641012386020999969, -55.51082434643999619, 10.18589234707000202 ) ) ;
#30778=CARTESIAN_POINT ( 'NONE',  ( 5.939680743703000668E-14, -6.000000000000000000, 0.000000000000000000 ) ) ;
#30779=CARTESIAN_POINT ( 'NONE',  ( 10.01332844639000008, -60.08056692637000396, -7.654537085048000122 ) ) ;
#30780=LINE ( 'NONE', #48814, #16936 ) ;
#30782=DIRECTION ( 'NONE',  ( 0.7071067811705838979, 1.925102962605954398E-07, 0.7071067812024849353 ) ) ;
#30784=VECTOR ( 'NONE', #14667, 1000.000000000000227 ) ;
#30785=ORIENTED_EDGE ( 'NONE', *, *, #3191, .F. ) ;
#30786=CARTESIAN_POINT ( 'NONE',  ( -1.995597954366113980, -1.528831350911639575, 2.597155843134357323 ) ) ;
#30787=CYLINDRICAL_SURFACE ( 'NONE', #10807, 0.5999999999999999778 ) ;
#30789=VECTOR ( 'NONE', #10177, 1000.000000000000114 ) ;
#30790=CARTESIAN_POINT ( 'NONE',  ( 2.492987828166000064, -3.446546016549000058, 2.660538423215999870 ) ) ;
#30794=DIRECTION ( 'NONE',  ( 0.7592504785507936393, 0.04890181649399957808, 0.6489586451877946693 ) ) ;
#30795=CARTESIAN_POINT ( 'NONE',  ( -1.667269374592999842, -60.00939883451999890, 12.49858097732999873 ) ) ;
#30796=CARTESIAN_POINT ( 'NONE',  ( 12.43569863939999998, -17.11799904157000185, 0.4278707626186000201 ) ) ;
#30800=CARTESIAN_POINT ( 'NONE',  ( 11.73832436745839836, -77.18564631431473799, -2.604929631990708483 ) ) ;
#30806=CARTESIAN_POINT ( 'NONE',  ( -12.77306367233000017, -61.85881314422999822, 1.040970605966999862 ) ) ;
#30808=DIRECTION ( 'NONE',  ( 0.000000000000000000, -1.000000000000000000, 0.000000000000000000 ) ) ;
#30809=CARTESIAN_POINT ( 'NONE',  ( 11.80573474569990644, -75.80000000000001137, 2.494142706669169041 ) ) ;
#30812=CARTESIAN_POINT ( 'NONE',  ( 1.247385803315000041, -61.27722255996999934, 12.50301438880000049 ) ) ;
#30815=ORIENTED_EDGE ( 'NONE', *, *, #20837, .T. ) ;
#30818=ORIENTED_EDGE ( 'NONE', *, *, #49807, .F. ) ;
#30819=CARTESIAN_POINT ( 'NONE',  ( 10.06692933812901636, -55.09657286943566845, -7.655995045250127085 ) ) ;
#30820=AXIS2_PLACEMENT_3D ( 'NONE', #20416, #17939, #21270 ) ;
#30822=FACE_OUTER_BOUND ( 'NONE', #25989, .T. ) ;
#30825=CARTESIAN_POINT ( 'NONE',  ( 1.698401934077000019, -24.22014045903999957, -12.66748707612999958 ) ) ;
#30830=CARTESIAN_POINT ( 'NONE',  ( 4.786724983033999514, -78.66227135457999964, -11.39381604551999772 ) ) ;
#30835=ADVANCED_FACE ( 'NONE', ( #13656 ), #22812, .F. ) ;
#30840=CARTESIAN_POINT ( 'NONE',  ( -13.07887593023000150, -78.01141106207001030, -0.9532572298037998992 ) ) ;
#30841=CARTESIAN_POINT ( 'NONE',  ( 12.15305909882999913, -77.97218707672999471, -3.479748152880000056 ) ) ;
#30844=DIRECTION ( 'NONE',  ( 0.000000000000000000, -1.000000000000000000, 0.000000000000000000 ) ) ;
#30845=CARTESIAN_POINT ( 'NONE',  ( 0.2546300289211099743, -2.969716266808483773, 3.249428101292205717 ) ) ;
#30847=EDGE_CURVE ( 'NONE', #52194, #51486, #43849, .T. ) ;
#30848=CYLINDRICAL_SURFACE ( 'NONE', #58105, 1.750000000000000000 ) ;
#30850=CARTESIAN_POINT ( 'NONE',  ( 0.07399134906894000441, -2.156119551551000324, 3.805339572302000040 ) ) ;
#30852=ORIENTED_EDGE ( 'NONE', *, *, #9852, .F. ) ;
#30854=ADVANCED_FACE ( 'NONE', ( #9533 ), #54530, .F. ) ;
#30857=PLANE ( 'NONE',  #19890 ) ;
#30858=CARTESIAN_POINT ( 'NONE',  ( -3.274010471232999819, -77.37790540356000690, 12.59444704299999884 ) ) ;
#30860=CARTESIAN_POINT ( 'NONE',  ( -8.114920487416192429, -61.62884529303471481, -9.847900218127630723 ) ) ;
#30861=CARTESIAN_POINT ( 'NONE',  ( 12.53239398062000198, -19.23513569609999863, -1.667936688463999895 ) ) ;
#30862=VERTEX_POINT ( 'NONE', #14817 ) ;
#30865=CARTESIAN_POINT ( 'NONE',  ( 8.385806979662810079, -53.91189752975327565, -9.298530586697486555 ) ) ;
#30870=TOROIDAL_SURFACE ( 'NONE', #41136, 17.50000000000000000, 5.000000000000000000 ) ;
#30874=ORIENTED_EDGE ( 'NONE', *, *, #47629, .T. ) ;
#30877=VECTOR ( 'NONE', #29104, 1000.000000000000000 ) ;
#30881=EDGE_CURVE ( 'NONE', #23208, #8867, #13610, .T. ) ;
#30882=CARTESIAN_POINT ( 'NONE',  ( 12.83044039271999992, -55.49360374314999689, 2.062670899148999926 ) ) ;
#30887=VERTEX_POINT ( 'NONE', #34846 ) ;
#30888=ORIENTED_EDGE ( 'NONE', *, *, #11689, .F. ) ;
#30891=B_SPLINE_SURFACE_WITH_KNOTS ( 'NONE', 3, 3, ( 
 ( #50931, #10479, #11358, #56224 ),
 ( #28464, #15774, #46513, #33766 ),
 ( #37620, #6037, #51804, #42940 ),
 ( #24046, #42063, #51226, #34630 ),
 ( #21923, #25783, #57081, #26634 ),
 ( #25491, #34340, #39932, #16645 ),
 ( #44668, #8648, #3638, #21351 ),
 ( #57948, #57653, #12211, #17209 ),
 ( #43809, #30198, #17502, #34913 ),
 ( #35197, #16933, #48522, #52657 ),
 ( #26350, #16359, #48246, #3354 ),
 ( #40230, #26061, #4221, #53229 ),
 ( #21641, #39366, #7783, #7494 ),
 ( #3073, #57373, #44088, #8066 ),
 ( #52945, #39647, #12495, #30493 ),
 ( #43512, #12778, #21067, #39072 ),
 ( #35491, #47961, #22219, #30773 ) ),
 .UNSPECIFIED., .F., .F., .F.,
 ( 4, 1, 1, 1, 1, 1, 1, 1, 1, 1, 1, 1, 1, 1, 4 ),
 ( 4, 4 ),
 ( -0.01011837001263999995, 0.000000000000000000, 0.08333333333333001192, 0.1666666666667000196, 0.2500000000000000000, 0.3333333333333000081, 0.4166666666666999919, 0.5000000000000000000, 0.5833333333333000637, 0.6666666666667000474, 0.7500000000000000000, 0.8333333333333000637, 0.9166666666667000474, 1.000000000000000000, 1.010372850415000023 ),
 ( -0.3559705548695000221, 1.357613361108999994 ),
 .UNSPECIFIED. ) ;
#30894=ORIENTED_EDGE ( 'NONE', *, *, #13958, .F. ) ;
#30898=CARTESIAN_POINT ( 'NONE',  ( -0.4515105396358876089, -18.45278097531891959, 10.99076531923741840 ) ) ;
#30900=CARTESIAN_POINT ( 'NONE',  ( 11.75000000000000000, -78.54999999999999716, 0.000000000000000000 ) ) ;
#30901=CARTESIAN_POINT ( 'NONE',  ( 7.682344222584999827, -59.56462890159999546, -10.04116292117000064 ) ) ;
#30903=CARTESIAN_POINT ( 'NONE',  ( -10.15831671671000080, -24.21991983044000207, 7.756223511073000232 ) ) ;
#30907=VECTOR ( 'NONE', #11583, 1000.000000000000114 ) ;
#30908=CARTESIAN_POINT ( 'NONE',  ( 10.48771805366000009, -21.75560171527000008, -7.686918321049000191 ) ) ;
#30909=CARTESIAN_POINT ( 'NONE',  ( -1.669724228656999987, -23.36897676534000112, 12.48434610067999984 ) ) ;
#30912=FACE_OUTER_BOUND ( 'NONE', #24097, .T. ) ;
#30914=CARTESIAN_POINT ( 'NONE',  ( 12.44180635032999938, -60.89260544892000127, -1.459447571596000026 ) ) ;
#30919=LINE ( 'NONE', #3782, #11834 ) ;
#30924=CARTESIAN_POINT ( 'NONE',  ( -10.42272502865000128, -20.24546192895000019, -7.691893942754999713 ) ) ;
#30930=FACE_OUTER_BOUND ( 'NONE', #19740, .T. ) ;
#30932=CARTESIAN_POINT ( 'NONE',  ( 12.43640309385000009, -24.91747517602999906, 0.05224034426415000154 ) ) ;
#30934=ORIENTED_EDGE ( 'NONE', *, *, #6029, .T. ) ;
#30935=CARTESIAN_POINT ( 'NONE',  ( -12.74365836111545391, -55.27810168844658278, 1.980611005600371399 ) ) ;
#30936=CARTESIAN_POINT ( 'NONE',  ( 8.179414028892216137, -24.74093020614164473, -9.502908389697516611 ) ) ;
#30938=CARTESIAN_POINT ( 'NONE',  ( -2.316740560951787486, -1.663670436995591473, -2.311895541344660909 ) ) ;
#30939=CARTESIAN_POINT ( 'NONE',  ( -10.55910102243999837, -56.01514526721999943, -7.642147947524999374 ) ) ;
#30942=VERTEX_POINT ( 'NONE', #25713 ) ;
#30944=DIRECTION ( 'NONE',  ( 1.000000000000000000, 0.000000000000000000, 0.000000000000000000 ) ) ;
#30945=CARTESIAN_POINT ( 'NONE',  ( -0.8506806241676574398, -1.104166666666666963, -3.165411199172027068 ) ) ;
#30947=ORIENTED_EDGE ( 'NONE', *, *, #31613, .T. ) ;
#30948=CARTESIAN_POINT ( 'NONE',  ( -9.778561352688999619, -53.75143577336000078, -8.284566532368000225 ) ) ;
#30953=CARTESIAN_POINT ( 'NONE',  ( 0.000000000000000000, -60.04999999966999980, 12.00000000000000000 ) ) ;
#30957=CARTESIAN_POINT ( 'NONE',  ( 10.01752115541999899, -18.80828330197000042, 7.660412752602000275 ) ) ;
#30960=CARTESIAN_POINT ( 'NONE',  ( -3.187445619818999987, -77.97624008069000467, 12.55797944092000051 ) ) ;
#30963=CARTESIAN_POINT ( 'NONE',  ( -7.714303428875997959, -15.69705297113999443, 12.53545825868000385 ) ) ;
#30968=VERTEX_POINT ( 'NONE', #25135 ) ;
#30970=CARTESIAN_POINT ( 'NONE',  ( 9.569482281372000188, -76.74786216769000191, -7.743360016082000641 ) ) ;
#30973=CARTESIAN_POINT ( 'NONE',  ( -0.1607120884409986850, -2.970659796132148589, -3.515337033079625417 ) ) ;
#30975=CARTESIAN_POINT ( 'NONE',  ( -10.10712711932128549, -17.53345760874380588, 7.860996423953121592 ) ) ;
#30976=DIRECTION ( 'NONE',  ( -1.000000000000000000, 0.000000000000000000, 0.000000000000000000 ) ) ;
#30977=CARTESIAN_POINT ( 'NONE',  ( -8.130811096204000776, -61.48523690322999613, -9.546858433459998849 ) ) ;
#30980=DIRECTION ( 'NONE',  ( -0.7071067811865475727, 0.000000000000000000, -0.7071067811865475727 ) ) ;
#30984=ORIENTED_EDGE ( 'NONE', *, *, #53645, .F. ) ;
#30986=B_SPLINE_CURVE_WITH_KNOTS ( 'NONE', 3,
 ( #24021, #11050, #19020, #55319, #14574, #32568, #42036, #29031 ),
 .UNSPECIFIED., .F., .F.,
 ( 4, 2, 2, 4 ),
 ( 0.000000000000000000, 0.5000000000000000000, 0.7500000000000000000, 1.000000000000000000 ),
 .UNSPECIFIED. ) ;
#30992=VECTOR ( 'NONE', #32870, 1000.000000000000114 ) ;
#30996=CARTESIAN_POINT ( 'NONE',  ( -1.295048492664000017, -54.27106480841000291, -12.54716442233000073 ) ) ;
#30997=CARTESIAN_POINT ( 'NONE',  ( 9.770618005419288821, -75.99681979438835810, 6.526589924811744936 ) ) ;
#30999=EDGE_LOOP ( 'NONE', ( #35732, #40511, #32348, #8529 ) ) ;
#31001=EDGE_CURVE ( 'NONE', #5420, #5785, #26287, .T. ) ;
#31002=CARTESIAN_POINT ( 'NONE',  ( -11.28059581212394846, -77.17303457489015273, 3.843385645491329772 ) ) ;
#31007=CARTESIAN_POINT ( 'NONE',  ( 0.2678032734880190224, -16.78567224710744199, 12.70526550769191410 ) ) ;
#31009=CARTESIAN_POINT ( 'NONE',  ( -5.747123378374999980, -78.61567021304000491, 10.24856442990000005 ) ) ;
#31011=EDGE_LOOP ( 'NONE', ( #11472, #3116, #26972, #9029, #21118, #317 ) ) ;
#31014=CARTESIAN_POINT ( 'NONE',  ( 0.7999999999999001243, -23.15000000002000036, -12.00000000000000000 ) ) ;
#31016=EDGE_CURVE ( 'NONE', #17140, #12818, #16865, .T. ) ;
#31018=CARTESIAN_POINT ( 'NONE',  ( -12.50239399162999909, -54.11640749821000185, 1.003653728895000041 ) ) ;
#31021=AXIS2_PLACEMENT_3D ( 'NONE', #57136, #34684, #3694 ) ;
#31025=FACE_OUTER_BOUND ( 'NONE', #24557, .T. ) ;
#31026=EDGE_LOOP ( 'NONE', ( #5560, #43863, #14826, #10811, #4774, #26599 ) ) ;
#31027=VERTEX_POINT ( 'NONE', #12712 ) ;
#31029=CIRCLE ( 'NONE', #29159, 5.000000000000000000 ) ;
#31030=ORIENTED_EDGE ( 'NONE', *, *, #19517, .F. ) ;
#31031=DIRECTION ( 'NONE',  ( -1.000000000000000000, 0.000000000000000000, 0.000000000000000000 ) ) ;
#31032=ORIENTED_EDGE ( 'NONE', *, *, #8416, .T. ) ;
#31033=CARTESIAN_POINT ( 'NONE',  ( -7.919595949288999570, -59.94999999446000771, 8.768124086549999419 ) ) ;
#31045=EDGE_CURVE ( 'NONE', #44782, #29606, #37562, .T. ) ;
#31047=CARTESIAN_POINT ( 'NONE',  ( 11.36243170732000074, -76.64353223351000111, -3.693170977796000010 ) ) ;
#31051=CARTESIAN_POINT ( 'NONE',  ( 12.89999999994999769, -2.999999999951000085, 1.886268220167000189E-09 ) ) ;
#31053=CARTESIAN_POINT ( 'NONE',  ( -10.19019669286999985, -23.19643762568000156, -7.646965578493999161 ) ) ;
#31060=CARTESIAN_POINT ( 'NONE',  ( -12.70395504303452761, -61.40679290093079601, 1.447100708791914769 ) ) ;
#31061=CARTESIAN_POINT ( 'NONE',  ( 7.641012305241000391, -60.08917723397000543, 10.18589226633000067 ) ) ;
#31062=CARTESIAN_POINT ( 'NONE',  ( -0.5506765233279000693, -16.74045707756000212, -12.77514798311000099 ) ) ;
#31063=CARTESIAN_POINT ( 'NONE',  ( -0.9356112496366845166, -54.05892169592745233, 12.50329130245003206 ) ) ;
#31069=ORIENTED_EDGE ( 'NONE', *, *, #9126, .T. ) ;
#31070=CARTESIAN_POINT ( 'NONE',  ( 0.000000000000000000, -32.88214388149999934, 0.000000000000000000 ) ) ;
#31071=CARTESIAN_POINT ( 'NONE',  ( -1.044910384896000188, -53.74473505772000692, 12.77260826194999943 ) ) ;
#31072=DIRECTION ( 'NONE',  ( -0.0001178721535674749112, 0.000000000000000000, 0.9999999930530777403 ) ) ;
#31073=CARTESIAN_POINT ( 'NONE',  ( 1.522081929427000047, -1.790731624101999930, -3.312820992749999860 ) ) ;
#31075=CARTESIAN_POINT ( 'NONE',  ( 1.250000000000000000, -18.75000000000000000, -12.50000000000000000 ) ) ;
#31077=CARTESIAN_POINT ( 'NONE',  ( -2.065394024360999836, -60.22161432612999477, 12.82193048530000112 ) ) ;
#31078=LINE ( 'NONE', #40551, #9675 ) ;
#31082=CARTESIAN_POINT ( 'NONE',  ( 9.101979256333937229, -77.14561836503926884, -8.015291124465097283 ) ) ;
#31083=CARTESIAN_POINT ( 'NONE',  ( -5.417662631175000243, -78.99125755395999704, 11.58939433055000023 ) ) ;
#31090=CARTESIAN_POINT ( 'NONE',  ( -12.44180635032999938, -60.89260544892000127, 1.459447571596000026 ) ) ;
#31097=CARTESIAN_POINT ( 'NONE',  ( 7.342377162853147787, -55.56980390652891799, 8.190817883596530180 ) ) ;
#31101=CARTESIAN_POINT ( 'NONE',  ( 12.50000000000000000, -60.04999999966999980, 1.250000000000000000 ) ) ;
#31106=CARTESIAN_POINT ( 'NONE',  ( -0.4356486348715999934, -24.88064955810000001, -12.43591427121000237 ) ) ;
#31109=ORIENTED_EDGE ( 'NONE', *, *, #57827, .F. ) ;
#31110=DIRECTION ( 'NONE',  ( 1.158066155992000047E-14, 0.000000000000000000, -1.000000000000000000 ) ) ;
#31111=CARTESIAN_POINT ( 'NONE',  ( 6.740316367734999758, -78.83471566304000078, 10.35856724650999894 ) ) ;
#31113=EDGE_LOOP ( 'NONE', ( #33144, #29710, #53238, #33075 ) ) ;
#31117=AXIS2_PLACEMENT_3D ( 'NONE', #48853, #53869, #26110 ) ;
#31119=CIRCLE ( 'NONE', #13214, 13.89999999999999858 ) ;
#31122=CARTESIAN_POINT ( 'NONE',  ( -9.767718346792999995, -78.45544818976000556, 7.129174073149000534 ) ) ;
#31124=CARTESIAN_POINT ( 'NONE',  ( -12.60796396291999955, -77.75016851287999486, -0.9189346901731000328 ) ) ;
#31126=CARTESIAN_POINT ( 'NONE',  ( 8.485281374238999419, -60.04999999966999980, 8.485281374238999419 ) ) ;
#31128=CYLINDRICAL_SURFACE ( 'NONE', #12011, 0.6000000000000008660 ) ;
#31129=CARTESIAN_POINT ( 'NONE',  ( -8.556714653534148951, -76.76008902517540378, -8.154008032208290402 ) ) ;
#31133=CARTESIAN_POINT ( 'NONE',  ( 2.113064247614999669, -3.489169774745999764, -3.165785623842000351 ) ) ;
#31135=ORIENTED_EDGE ( 'NONE', *, *, #2786, .T. ) ;
#31136=CARTESIAN_POINT ( 'NONE',  ( 0.3116081091750318444, -23.68684619778880673, 10.99615594221777215 ) ) ;
#31137=DIRECTION ( 'NONE',  ( 1.000000000000000000, 0.000000000000000000, 0.000000000000000000 ) ) ;
#31139=CONICAL_SURFACE ( 'NONE', #24605, 12.84999999995999964, 0.7853981633972997312 ) ;
#31140=B_SPLINE_CURVE_WITH_KNOTS ( 'NONE', 3,
 ( #57206, #38907, #7047, #16486, #30324, #7903, #12052, #25905, #3476, #21482, #39489, #57490, #53070, #12619, #30616, #17934 ),
 .UNSPECIFIED., .F., .F.,
 ( 4, 2, 2, 2, 2, 2, 2, 4 ),
 ( 0.000000000000000000, 0.2500000000000038303, 0.3750000000000026090, 0.4375000000000021094, 0.5000000000000015543, 0.6250000000000005551, 0.7499999999999995559, 1.000000000000000000 ),
 .UNSPECIFIED. ) ;
#31141=CARTESIAN_POINT ( 'NONE',  ( -12.54673279573000144, -17.17202488779000191, -0.9078290272348999990 ) ) ;
#31142=CARTESIAN_POINT ( 'NONE',  ( 12.51033564907000084, -78.24514168465999830, -3.582046052171000028 ) ) ;
#31144=CARTESIAN_POINT ( 'NONE',  ( 12.69616050747999836, -20.24828923609000242, -1.799475304559999822 ) ) ;
#31145=EDGE_LOOP ( 'NONE', ( #18304, #22612, #57417, #27432 ) ) ;
#31146=CARTESIAN_POINT ( 'NONE',  ( -13.94241845804000057, -69.26002936526001008, -4.312607201944000624E-05 ) ) ;
#31147=FACE_OUTER_BOUND ( 'NONE', #3270, .T. ) ;
#31150=CARTESIAN_POINT ( 'NONE',  ( -2.062502994258999856, -21.75648180056000314, -12.92181194095000052 ) ) ;
#31151=AXIS2_PLACEMENT_3D ( 'NONE', #43181, #51755, #11020 ) ;
#31153=EDGE_CURVE ( 'NONE', #5887, #4102, #53778, .T. ) ;
#31155=CARTESIAN_POINT ( 'NONE',  ( -3.754890333716000228, -1.276863097741000042, -1.424957469106999941 ) ) ;
#31164=EDGE_LOOP ( 'NONE', ( #51636, #47422, #13636, #26678 ) ) ;
#31168=VERTEX_POINT ( 'NONE', #40752 ) ;
#31170=ORIENTED_EDGE ( 'NONE', *, *, #44498, .T. ) ;
#31171=ORIENTED_EDGE ( 'NONE', *, *, #37817, .T. ) ;
#31172=CARTESIAN_POINT ( 'NONE',  ( 7.356278612544861595, -60.10416868444998784, 8.178338515874330028 ) ) ;
#31173=EDGE_CURVE ( 'NONE', #9948, #41659, #29689, .T. ) ;
#31175=CARTESIAN_POINT ( 'NONE',  ( 2.630134112433684113, -1.666103305045204319, 3.040499453435629995 ) ) ;
#31176=ORIENTED_EDGE ( 'NONE', *, *, #8069, .F. ) ;
#31177=CARTESIAN_POINT ( 'NONE',  ( 11.00000000000000178, -18.25000000000000355, 0.1607611550154312841 ) ) ;
#31178=ORIENTED_EDGE ( 'NONE', *, *, #17446, .T. ) ;
#31180=DIRECTION ( 'NONE',  ( 0.000000000000000000, 0.000000000000000000, -1.000000000000000000 ) ) ;
#31183=CARTESIAN_POINT ( 'NONE',  ( 7.247844507162001015, -18.75000000000000000, 9.722718241315000398 ) ) ;
#31184=CARTESIAN_POINT ( 'NONE',  ( 11.37984331015203487, -77.42617268424514521, -3.047297811426050718 ) ) ;
#31186=DIRECTION ( 'NONE',  ( 4.222607431054999479E-09, 0.9999999999999998890, -1.485891339405999759E-08 ) ) ;
#31189=CARTESIAN_POINT ( 'NONE',  ( -9.523353692535000192, -24.81947015623000041, 8.220363114681999761 ) ) ;
#31191=TOROIDAL_SURFACE ( 'NONE', #7662, 1.250000000000000000, 0.5000000000000000000 ) ;
#31194=CARTESIAN_POINT ( 'NONE',  ( -12.54980553589999914, -16.95222688865000293, -0.05649961219507999843 ) ) ;
#31198=CARTESIAN_POINT ( 'NONE',  ( -12.54435915808567970, -60.32412882177197844, -1.733925320397640357 ) ) ;
#31199=CARTESIAN_POINT ( 'NONE',  ( 3.950759981329000414, -1.627363918999999992, -0.2034811876873000025 ) ) ;
#31201=B_SPLINE_CURVE_WITH_KNOTS ( 'NONE', 3,
 ( #33175, #51221, #10774, #6620, #46802, #24344, #20209, #15483, #2209, #38200 ),
 .UNSPECIFIED., .F., .F.,
 ( 4, 2, 2, 2, 4 ),
 ( 0.000000000000000000, 0.09375005742280677346, 0.1875001148456135469, 0.2812501722684203065, 0.3750002296912270938 ),
 .UNSPECIFIED. ) ;
#31218=LINE ( 'NONE', #27682, #43590 ) ;
#31221=CARTESIAN_POINT ( 'NONE',  ( -10.15831671673000081, -61.01991983010999832, 7.756223511098000678 ) ) ;
#31224=CARTESIAN_POINT ( 'NONE',  ( -12.50000000000000000, -23.24999999688999708, -1.750000000000000000 ) ) ;
#31225=CARTESIAN_POINT ( 'NONE',  ( -11.89999999977000122, -18.84999999999999787, 0.000000000000000000 ) ) ;
#31226=CARTESIAN_POINT ( 'NONE',  ( -2.062597299672999540, -59.58485473249000108, 12.87022657274000004 ) ) ;
#31227=EDGE_LOOP ( 'NONE', ( #17394, #17462, #4439, #56783 ) ) ;
#31231=CARTESIAN_POINT ( 'NONE',  ( -10.21381326473999884, -59.57129148919000272, -7.668949790015999746 ) ) ;
#31236=CARTESIAN_POINT ( 'NONE',  ( -9.722718241315000398, -23.25000000000000000, -7.954951288349001004 ) ) ;
#31237=CARTESIAN_POINT ( 'NONE',  ( -3.250000000000001332, -1.010416666666666963, -0.4254240051736181139 ) ) ;
#31239=EDGE_CURVE ( 'NONE', #13029, #6729, #36020, .T. ) ;
#31240=CARTESIAN_POINT ( 'NONE',  ( -7.631896578914999729, -55.57877526445999905, -10.36221705163000095 ) ) ;
#31252=CARTESIAN_POINT ( 'NONE',  ( -12.91626791057999846, -77.58770759395000027, -1.016208772393999871 ) ) ;
#31255=ADVANCED_FACE ( 'NONE', ( #15345 ), #35615, .F. ) ;
#31262=CARTESIAN_POINT ( 'NONE',  ( 10.54796701376999835, -75.84510257978999448, 6.346365727669000201 ) ) ;
#31264=CARTESIAN_POINT ( 'NONE',  ( 3.529139221787363390, -2.612568796686050909, 0.6082355383969471063 ) ) ;
#31265=CARTESIAN_POINT ( 'NONE',  ( -8.266608573609707022, -17.02766203690127966, 9.697383820329660509 ) ) ;
#31271=CARTESIAN_POINT ( 'NONE',  ( 6.487909909861338420, -77.22037378120354845, -10.11762090100198819 ) ) ;
#31273=CARTESIAN_POINT ( 'NONE',  ( -9.945248159053452497, -76.00840104940344588, -8.414435792164686845 ) ) ;
#31280=AXIS2_PLACEMENT_3D ( 'NONE', #24339, #54751, #5736 ) ;
#31282=CARTESIAN_POINT ( 'NONE',  ( 12.50000000000000000, -55.54999999966999980, 0.000000000000000000 ) ) ;
#31283=AXIS2_PLACEMENT_3D ( 'NONE', #57036, #21592, #57601 ) ;
#31286=CARTESIAN_POINT ( 'NONE',  ( -0.4802748259363999739, -53.79473092685000069, -12.54896097830000024 ) ) ;
#31287=CARTESIAN_POINT ( 'NONE',  ( 2.491388965909014708, -76.05772791729621929, 11.48290208440257665 ) ) ;
#31289=CARTESIAN_POINT ( 'NONE',  ( -8.485281374238999419, 0.000000000000000000, -8.485281374238999419 ) ) ;
#31290=VERTEX_POINT ( 'NONE', #24968 ) ;
#31291=CARTESIAN_POINT ( 'NONE',  ( -7.342331066867000544, -59.94999999967000548, 8.190859204290999784 ) ) ;
#31294=CARTESIAN_POINT ( 'NONE',  ( -13.94241847916999966, -46.33997059779999717, -4.312626734219999997E-05 ) ) ;
#31295=CARTESIAN_POINT ( 'NONE',  ( -6.528377880799854260, -76.27803772958627349, -9.769420381365502948 ) ) ;
#31298=EDGE_CURVE ( 'NONE', #45201, #15410, #42115, .T. ) ;
#31302=ORIENTED_EDGE ( 'NONE', *, *, #25293, .F. ) ;
#31304=AXIS2_PLACEMENT_3D ( 'NONE', #33209, #28494, #10809 ) ;
#31307=DIRECTION ( 'NONE',  ( 1.000000000000000000, 0.000000000000000000, 0.000000000000000000 ) ) ;
#31311=CARTESIAN_POINT ( 'NONE',  ( 11.07343986574985450, -76.91880255752919027, -4.079208564647556656 ) ) ;
#31312=DIRECTION ( 'NONE',  ( 0.000000000000000000, 0.000000000000000000, -1.000000000000000000 ) ) ;
#31313=DIRECTION ( 'NONE',  ( 1.194281197986999840E-10, 1.000000000000000000, 5.211300245735000371E-10 ) ) ;
#31314=CARTESIAN_POINT ( 'NONE',  ( -12.74366183110831052, -60.32185227186467102, -1.980611001123811388 ) ) ;
#31316=CARTESIAN_POINT ( 'NONE',  ( -12.43410103865999972, -24.44137177768999791, 1.192638008239000014 ) ) ;
#31320=AXIS2_PLACEMENT_3D ( 'NONE', #43426, #2414, #37830 ) ;
#31321=ORIENTED_EDGE ( 'NONE', *, *, #58078, .T. ) ;
#31323=VERTEX_POINT ( 'NONE', #34098 ) ;
#31324=CARTESIAN_POINT ( 'NONE',  ( 9.963467980702999327, -23.68274967071999981, 7.659239661648999942 ) ) ;
#31325=CARTESIAN_POINT ( 'NONE',  ( 8.150146600852352208, -55.38467666605773587, -7.387512494710277267 ) ) ;
#31327=ADVANCED_FACE ( 'NONE', ( #33529 ), #36601, .F. ) ;
#31329=CIRCLE ( 'NONE', #46476, 1.750000000000001332 ) ;
#31331=DIRECTION ( 'NONE',  ( -1.000000000000000000, 0.000000000000000000, 0.000000000000000000 ) ) ;
#31332=ORIENTED_EDGE ( 'NONE', *, *, #20652, .T. ) ;
#31340=CIRCLE ( 'NONE', #23820, 0.5999999999999999778 ) ;
#31341=CARTESIAN_POINT ( 'NONE',  ( 12.38384620286000093, -76.22877954592999572, -4.343081969281999299 ) ) ;
#31345=VECTOR ( 'NONE', #34069, 1000.000000000000000 ) ;
#31346=CARTESIAN_POINT ( 'NONE',  ( 12.46164872708000004, -18.32834420040999746, -1.631615798668999862 ) ) ;
#31348=EDGE_CURVE ( 'NONE', #38883, #48634, #4197, .T. ) ;
#31349=CARTESIAN_POINT ( 'NONE',  ( -11.17196203841501756, -76.67470515005034315, 3.660625636545362660 ) ) ;
#31356=DIRECTION ( 'NONE',  ( 0.000000000000000000, 0.000000000000000000, 1.000000000000000000 ) ) ;
#31359=CARTESIAN_POINT ( 'NONE',  ( 10.35747158360999975, -55.48415522678000400, -7.626500902197000720 ) ) ;
#31364=ORIENTED_EDGE ( 'NONE', *, *, #28267, .F. ) ;
#31365=DIRECTION ( 'NONE',  ( 1.000000000000000000, -6.386278974555000074E-09, 1.411448851650999890E-10 ) ) ;
#31366=CARTESIAN_POINT ( 'NONE',  ( 1.632307027713000069, -55.13072810409999391, 12.46200249210000166 ) ) ;
#31368=CARTESIAN_POINT ( 'NONE',  ( 0.7674396588794000218, -2.946116667230000097, -3.891291548070999973 ) ) ;
#31371=CARTESIAN_POINT ( 'NONE',  ( 3.165411199172027512, -1.729166666666666519, -0.8506806241676553304 ) ) ;
#31375=CARTESIAN_POINT ( 'NONE',  ( 12.61112375831999977, -18.78433928967000099, 1.798929377342999736 ) ) ;
#31378=AXIS2_PLACEMENT_3D ( 'NONE', #48638, #56915, #39477 ) ;
#31379=CARTESIAN_POINT ( 'NONE',  ( 12.50000000000000000, -55.55000000278000272, -1.750000000000000000 ) ) ;
#31380=CARTESIAN_POINT ( 'NONE',  ( -10.31240102133999947, -78.61950547832000780, 7.304110959076998810 ) ) ;
#31381=B_SPLINE_SURFACE_WITH_KNOTS ( 'NONE', 3, 3, ( 
 ( #42438, #27952, #33260, #46588 ),
 ( #1420, #20002, #15562, #23535 ),
 ( #24122, #41548, #28830, #19702 ),
 ( #10857, #37109, #47172, #14669 ),
 ( #11152, #46878, #6408, #32667 ),
 ( #6704, #10259, #43016, #48039 ),
 ( #29985, #7858, #24995, #20854 ),
 ( #2572, #7569, #53020, #12006 ),
 ( #44169, #52447, #25569, #34123 ),
 ( #3716, #3153, #21141, #56586 ),
 ( #43589, #38858, #2857, #34418 ),
 ( #38572, #56879, #16435, #33841 ),
 ( #7281, #39149, #25857, #51878 ),
 ( #16146, #11722, #11433, #8149 ),
 ( #12573, #21719, #29698, #43886 ),
 ( #17008, #57157, #29415, #57449 ),
 ( #39724, #16722, #34705, #25283 ) ),
 .UNSPECIFIED., .F., .F., .F.,
 ( 4, 1, 1, 1, 1, 1, 1, 1, 1, 1, 1, 1, 1, 1, 4 ),
 ( 4, 4 ),
 ( -0.01011400514355000058, 0.000000000000000000, 0.08333333333333001192, 0.1666666666667000196, 0.2500000000000000000, 0.3333333333333000081, 0.4166666666666999919, 0.5000000000000000000, 0.5833333333333000637, 0.6666666666667000474, 0.7500000000000000000, 0.8333333333333000637, 0.9166666666667000474, 1.000000000000000000, 1.010365328128000062 ),
 ( -0.3559705546945999832, 1.357612395640000136 ),
 .UNSPECIFIED. ) ;
#31383=DIRECTION ( 'NONE',  ( 0.7071067811865969777, 0.7071067811864980568, 1.033971025369995989E-10 ) ) ;
#31385=CARTESIAN_POINT ( 'NONE',  ( 1.718598680008210700, -61.04962933004735959, 12.71111582771794701 ) ) ;
#31387=CARTESIAN_POINT ( 'NONE',  ( -12.83675988122999989, -60.02754371127999633, 2.062832873794000044 ) ) ;
#31389=EDGE_CURVE ( 'NONE', #21891, #33033, #47421, .T. ) ;
#31390=CARTESIAN_POINT ( 'NONE',  ( -5.747123378374999980, -78.61567021304000491, 10.24856442990000005 ) ) ;
#31392=AXIS2_PLACEMENT_3D ( 'NONE', #6717, #12300, #43028 ) ;
#31393=VECTOR ( 'NONE', #22537, 1000.000000000000000 ) ;
#31397=DIRECTION ( 'NONE',  ( 0.000000000000000000, -1.000000000000000000, 0.000000000000000000 ) ) ;
#31398=ORIENTED_EDGE ( 'NONE', *, *, #18627, .F. ) ;
#31399=VERTEX_POINT ( 'NONE', #54089 ) ;
#31402=LINE ( 'NONE', #58289, #36788 ) ;
#31403=ORIENTED_EDGE ( 'NONE', *, *, #2566, .T. ) ;
#31404=CARTESIAN_POINT ( 'NONE',  ( 10.42531125070999920, -60.06485145371000556, -7.624341767111000756 ) ) ;
#31405=CARTESIAN_POINT ( 'NONE',  ( 1.980584515752000119, -18.73514853375999678, 12.76303204602000108 ) ) ;
#31408=CARTESIAN_POINT ( 'NONE',  ( -0.8445585116435000428, -24.71040443242999984, -12.43380736237000050 ) ) ;
#31413=CARTESIAN_POINT ( 'NONE',  ( 6.659420128180999932, -78.74763481331000037, 10.23424531685000005 ) ) ;
#31414=ORIENTED_EDGE ( 'NONE', *, *, #49397, .F. ) ;
#31415=ORIENTED_EDGE ( 'NONE', *, *, #28885, .T. ) ;
#31416=EDGE_CURVE ( 'NONE', #11901, #23950, #13639, .T. ) ;
#31419=CARTESIAN_POINT ( 'NONE',  ( -1.980584515756000030, -60.06485150062000145, -12.76303204342999997 ) ) ;
#31423=CARTESIAN_POINT ( 'NONE',  ( 11.74505801343999956, -76.70322811118001027, 5.470698999298999610 ) ) ;
#31427=CARTESIAN_POINT ( 'NONE',  ( -12.50000000000000000, -60.04999999966999980, 0.000000000000000000 ) ) ;
#31432=CARTESIAN_POINT ( 'NONE',  ( -0.5536213250151708065, -76.82071496306311076, -11.80762683626677401 ) ) ;
#31435=CARTESIAN_POINT ( 'NONE',  ( -26.50000000000000000, -39.49523982883999906, -1.535553829236000105E-05 ) ) ;
#31438=AXIS2_PLACEMENT_3D ( 'NONE', #26510, #17678, #25942 ) ;
#31440=CARTESIAN_POINT ( 'NONE',  ( 12.00000000000000000, -18.84999999997999964, -0.7999999999999001243 ) ) ;
#31441=CARTESIAN_POINT ( 'NONE',  ( -9.546819346760001324, -61.48527546573999558, 8.130850182904000079 ) ) ;
#31443=CARTESIAN_POINT ( 'NONE',  ( -12.57354471038000021, -18.27622323986999930, -1.757967544833999973 ) ) ;
#31444=CARTESIAN_POINT ( 'NONE',  ( 12.53073434187000146, -77.74559991600001752, -3.509976885708000260 ) ) ;
#31445=CARTESIAN_POINT ( 'NONE',  ( -10.10713367727843881, -61.26653151295378308, -7.860990029236842425 ) ) ;
#31446=CARTESIAN_POINT ( 'NONE',  ( 12.83044039274999903, -23.30639625649999758, -2.062670899148999926 ) ) ;
#31447=ORIENTED_EDGE ( 'NONE', *, *, #37279, .F. ) ;
#31448=DIRECTION ( 'NONE',  ( 1.000000000000000000, 0.000000000000000000, 0.000000000000000000 ) ) ;
#31449=LINE ( 'NONE', #9039, #43681 ) ;
#31454=CARTESIAN_POINT ( 'NONE',  ( 4.010845454633999552, -1.597904343863999932, -0.2065758488482999922 ) ) ;
#31455=CARTESIAN_POINT ( 'NONE',  ( -1.931043742978000077, -59.57795407677000554, -12.75763395697999947 ) ) ;
#31461=ORIENTED_EDGE ( 'NONE', *, *, #19630, .F. ) ;
#31462=ORIENTED_EDGE ( 'NONE', *, *, #37223, .F. ) ;
#31465=ORIENTED_EDGE ( 'NONE', *, *, #21803, .F. ) ;
#31470=CARTESIAN_POINT ( 'NONE',  ( 0.1070836934507127802, -2.728288973199432199, -3.247988223077748593 ) ) ;
#31472=CARTESIAN_POINT ( 'NONE',  ( 4.014948207387869061, -1.593756223004204609, -0.2067871583196793928 ) ) ;
#31475=ADVANCED_FACE ( 'NONE', ( #52424 ), #12634, .F. ) ;
#31477=DIRECTION ( 'NONE',  ( 2.273768121930269862E-11, -5.258082751534180400E-20, -1.000000000000000000 ) ) ;
#31480=CARTESIAN_POINT ( 'NONE',  ( 7.220923959705223716, -77.12291666666664014, 9.396085398178630754 ) ) ;
#31484=EDGE_CURVE ( 'NONE', #44555, #52418, #15675, .T. ) ;
#31486=CARTESIAN_POINT ( 'NONE',  ( -9.213114944024999531, -25.00524898755999814, 8.533795138592999763 ) ) ;
#31487=ADVANCED_FACE ( 'NONE', ( #11259 ), #33382, .F. ) ;
#31488=DIRECTION ( 'NONE',  ( 0.000000000000000000, 1.000000000000000000, 0.000000000000000000 ) ) ;
#31492=CARTESIAN_POINT ( 'NONE',  ( 17.49999999998999911, -65.72928575305999743, 1.613072089394999983E-05 ) ) ;
#31493=LINE ( 'NONE', #58085, #21029 ) ;
#31496=CARTESIAN_POINT ( 'NONE',  ( 3.921473243360999561, -1.120934344713000019, -0.5217135850094999361 ) ) ;
#31498=CIRCLE ( 'NONE', #6074, 0.8000000000000011546 ) ;
#31503=CARTESIAN_POINT ( 'NONE',  ( 13.63885489310999510, -19.21421830981000056, -7.254376133916000668 ) ) ;
#31507=CARTESIAN_POINT ( 'NONE',  ( -1.980464439859999981, -57.04527982639000072, 12.85144117157999943 ) ) ;
#31508=ADVANCED_FACE ( 'NONE', ( #29240 ), #28728, .F. ) ;
#31509=CYLINDRICAL_SURFACE ( 'NONE', #36405, 1.750000000000000000 ) ;
#31512=ORIENTED_EDGE ( 'NONE', *, *, #35189, .F. ) ;
#31517=CARTESIAN_POINT ( 'NONE',  ( 5.694538069269999623E-14, -72.89999999999999147, -14.00000000000097877 ) ) ;
#31519=CARTESIAN_POINT ( 'NONE',  ( 11.45970853605999906, -77.04030896091001068, 5.337786833297999856 ) ) ;
#31521=CARTESIAN_POINT ( 'NONE',  ( -3.164582902296511069, -3.121138013161445457, -0.8488383203591168824 ) ) ;
#31522=CARTESIAN_POINT ( 'NONE',  ( -1.931086388578000079, -60.09778754156999980, 12.71798269388000158 ) ) ;
#31525=CARTESIAN_POINT ( 'NONE',  ( 1.208267227088423823, -53.97409317822796027, -12.70228502419097794 ) ) ;
#31527=DIRECTION ( 'NONE',  ( 0.000000000000000000, 0.000000000000000000, -1.000000000000000000 ) ) ;
#31533=ORIENTED_EDGE ( 'NONE', *, *, #57406, .T. ) ;
#31535=CARTESIAN_POINT ( 'NONE',  ( -0.7699595307336942751, -77.81793362728524244, -11.75325798414018941 ) ) ;
#31537=CARTESIAN_POINT ( 'NONE',  ( 11.99999999979999821, -23.14999999072999870, -0.7999999997951999786 ) ) ;
#31538=ORIENTED_EDGE ( 'NONE', *, *, #14140, .F. ) ;
#31539=ORIENTED_EDGE ( 'NONE', *, *, #22302, .T. ) ;
#31540=CARTESIAN_POINT ( 'NONE',  ( -10.52693198617000014, -55.37847693893999690, -7.606025555747000233 ) ) ;
#31541=AXIS2_PLACEMENT_3D ( 'NONE', #52689, #30235, #34083 ) ;
#31543=ORIENTED_EDGE ( 'NONE', *, *, #7086, .T. ) ;
#31547=VERTEX_POINT ( 'NONE', #29810 ) ;
#31549=DIRECTION ( 'NONE',  ( 0.7071067811865475727, 0.000000000000000000, -0.7071067811865475727 ) ) ;
#31550=CARTESIAN_POINT ( 'NONE',  ( 12.66594527011999816, -76.72356177075999994, -3.392478259704000187 ) ) ;
#31560=B_SPLINE_SURFACE_WITH_KNOTS ( 'NONE', 3, 3, ( 
 ( #6226, #56699, #7103, #43130 ),
 ( #2686, #28657, #24821, #42545 ),
 ( #46705, #1824, #11545, #46993 ),
 ( #51706, #52271, #38391, #20679 ),
 ( #37812, #33379, #33079, #29802 ),
 ( #11255, #16257, #20112, #11825 ),
 ( #47857, #10967, #6812, #24243 ),
 ( #43403, #28951, #7387, #29522 ),
 ( #15083, #33951, #6521, #42259 ),
 ( #2964, #56123, #24531, #15669 ),
 ( #25388, #38678, #20963, #25103 ),
 ( #19820, #51124, #10677, #56410 ),
 ( #33667, #55833, #2113, #38103 ),
 ( #29234, #47284, #42837, #2396 ),
 ( #20393, #15960, #51990, #34814 ),
 ( #8541, #48143, #44561, #12960 ),
 ( #58137, #17704, #21825, #30957 ) ),
 .UNSPECIFIED., .F., .F., .F.,
 ( 4, 1, 1, 1, 1, 1, 1, 1, 1, 1, 1, 1, 1, 1, 4 ),
 ( 4, 4 ),
 ( -0.01011837001263999995, 0.000000000000000000, 0.08333333333333001192, 0.1666666666667000196, 0.2500000000000000000, 0.3333333333333000081, 0.4166666666666999919, 0.5000000000000000000, 0.5833333333333000637, 0.6666666666667000474, 0.7500000000000000000, 0.8333333333333000637, 0.9166666666667000474, 1.000000000000000000, 1.010372850415000023 ),
 ( -0.3559705548695000221, 1.357613361108999994 ),
 .UNSPECIFIED. ) ;
#31561=CARTESIAN_POINT ( 'NONE',  ( -2.185466470362367630, -3.277594938514446277, 2.760202041691888208 ) ) ;
#31562=CARTESIAN_POINT ( 'NONE',  ( -8.610991514544377168, -16.82512235768486875, 9.355860133801421341 ) ) ;
#31565=CARTESIAN_POINT ( 'NONE',  ( -9.723174507563001612, -61.27697503937000079, -7.958760295438001009 ) ) ;
#31567=CARTESIAN_POINT ( 'NONE',  ( 11.28168611626732698, -76.82899490262227005, 4.307594075494947106 ) ) ;
#31569=AXIS2_PLACEMENT_3D ( 'NONE', #36475, #4614, #49187 ) ;
#31573=AXIS2_PLACEMENT_3D ( 'NONE', #35323, #21761, #4046 ) ;
#31575=CYLINDRICAL_SURFACE ( 'NONE', #50290, 1.750000000000000000 ) ;
#31576=DIRECTION ( 'NONE',  ( -0.7071067811864970576, -3.534300184300985629E-08, -0.7071067811865970887 ) ) ;
#31577=DIRECTION ( 'NONE',  ( -0.7071067812088192017, 2.829527200303080525E-07, 0.7071067811642192114 ) ) ;
#31578=VECTOR ( 'NONE', #27082, 1000.000000000000000 ) ;
#31582=CARTESIAN_POINT ( 'NONE',  ( 2.299484790252942723, -76.05912199685272412, 11.52265691577497897 ) ) ;
#31585=ORIENTED_EDGE ( 'NONE', *, *, #33943, .T. ) ;
#31586=B_SPLINE_CURVE_WITH_KNOTS ( 'NONE', 3,
 ( #29480, #7634, #2357, #52229, #21498, #16500 ),
 .UNSPECIFIED., .F., .F.,
 ( 4, 2, 4 ),
 ( 0.000000000000000000, 0.5000000000000000000, 1.000000000000000000 ),
 .UNSPECIFIED. ) ;
#31587=DIRECTION ( 'NONE',  ( 0.7071067811865475727, 0.000000000000000000, 0.7071067811865475727 ) ) ;
#31588=AXIS2_PLACEMENT_3D ( 'NONE', #55348, #55938, #29055 ) ;
#31589=ADVANCED_FACE ( 'NONE', ( #29526 ), #36277, .F. ) ;
#31592=CARTESIAN_POINT ( 'NONE',  ( -6.192097496234715059, -76.28079615762941046, -9.993622780947980289 ) ) ;
#31596=CARTESIAN_POINT ( 'NONE',  ( -1.370379768245999841E-14, -74.59999999999999432, 0.000000000000000000 ) ) ;
#31597=DIRECTION ( 'NONE',  ( 0.000000000000000000, -1.000000000000000000, 0.000000000000000000 ) ) ;
#31598=ORIENTED_EDGE ( 'NONE', *, *, #4478, .F. ) ;
#31600=CARTESIAN_POINT ( 'NONE',  ( 12.70228549156958486, -53.97187149228901859, 1.205357499425017132 ) ) ;
#31603=EDGE_CURVE ( 'NONE', #40579, #39052, #19348, .T. ) ;
#31607=DIRECTION ( 'NONE',  ( 0.000000000000000000, 0.000000000000000000, -1.000000000000000000 ) ) ;
#31608=CARTESIAN_POINT ( 'NONE',  ( -10.19999999921000011, -0.2000000007865999907, 1.811583764860000079E-09 ) ) ;
#31610=EDGE_CURVE ( 'NONE', #3043, #2890, #20116, .T. ) ;
#31613=EDGE_CURVE ( 'NONE', #30461, #55907, #28344, .T. ) ;
#31615=CARTESIAN_POINT ( 'NONE',  ( -12.77649794757999935, -25.30831393477999924, -0.06464137375187999079 ) ) ;
#31622=CARTESIAN_POINT ( 'NONE',  ( 7.631889049354000143, -23.22121504852000129, 10.36222434949000082 ) ) ;
#31630=ORIENTED_EDGE ( 'NONE', *, *, #47775, .T. ) ;
#31637=CARTESIAN_POINT ( 'NONE',  ( -1.871685860826000081, -76.53201366967000752, -12.83051903312999897 ) ) ;
#31642=CARTESIAN_POINT ( 'NONE',  ( -10.35398566681999988, -23.40788276239999988, -7.619388279076999559 ) ) ;
#31643=CARTESIAN_POINT ( 'NONE',  ( -10.84978627008842444, -76.66831054839785509, 4.509941008725813383 ) ) ;
#31650=CARTESIAN_POINT ( 'NONE',  ( -10.01749678875999905, -18.80819056997000160, 7.660430392568000180 ) ) ;
#31652=CARTESIAN_POINT ( 'NONE',  ( 12.50000000000000000, -49.87071422276000021, 0.000000000000000000 ) ) ;
#31653=LINE ( 'NONE', #4224, #12883 ) ;
#31655=DIRECTION ( 'NONE',  ( 0.000000000000000000, 1.000000000000000000, 0.000000000000000000 ) ) ;
#31657=DIRECTION ( 'NONE',  ( -1.000000000000000000, 0.000000000000000000, 0.000000000000000000 ) ) ;
#31660=CARTESIAN_POINT ( 'NONE',  ( 1.669724228661999987, -55.43102323432999867, 12.48434610065999983 ) ) ;
#31663=CARTESIAN_POINT ( 'NONE',  ( 3.261288468347999903, -3.007443126209999651, -2.257235270949999872 ) ) ;
#31667=DIRECTION ( 'NONE',  ( 0.000000000000000000, -1.000000000000000000, 0.000000000000000000 ) ) ;
#31668=CARTESIAN_POINT ( 'NONE',  ( -1.405334850318079587, -24.31492947778725977, -12.50716844834618868 ) ) ;
#31670=VECTOR ( 'NONE', #48958, 1000.000000000000000 ) ;
#31675=CARTESIAN_POINT ( 'NONE',  ( 9.783235115916999902, -54.26434390361999505, -7.961033122292000108 ) ) ;
#31679=CARTESIAN_POINT ( 'NONE',  ( -1.782734487945632607, -60.92245368521469828, 12.71547286929785514 ) ) ;
#31681=CARTESIAN_POINT ( 'NONE',  ( -12.61271904362000029, -59.99692351013000291, 1.798332623270000097 ) ) ;
#31690=ORIENTED_EDGE ( 'NONE', *, *, #19352, .T. ) ;
#31699=CARTESIAN_POINT ( 'NONE',  ( 12.04999999926000243, -79.29999999926000953, 5.384918141074000180E-09 ) ) ;
#31700=CARTESIAN_POINT ( 'NONE',  ( 1.798368564625000054, -23.19636757045999786, -12.61278090841000044 ) ) ;
#31704=CARTESIAN_POINT ( 'NONE',  ( 2.549865490971999549, -78.60221383193000122, 11.63742185847999977 ) ) ;
#31706=EDGE_LOOP ( 'NONE', ( #48079, #32751, #49378, #50453 ) ) ;
#31713=AXIS2_PLACEMENT_3D ( 'NONE', #40906, #58030, #35577 ) ;
#31715=CARTESIAN_POINT ( 'NONE',  ( 12.34410331423999985, -77.06018438914000512, -3.381164140480000135 ) ) ;
#31716=CARTESIAN_POINT ( 'NONE',  ( -3.110005734825000090, -77.63915923096000427, 12.25287980954000133 ) ) ;
#31718=VECTOR ( 'NONE', #56804, 1000.000000000000000 ) ;
#31719=LINE ( 'NONE', #770, #32059 ) ;
#31724=CARTESIAN_POINT ( 'NONE',  ( -6.652173553828778729, -78.22269769528665506, 9.741036272413309050 ) ) ;
#31727=PLANE ( 'NONE',  #56274 ) ;
#31729=CARTESIAN_POINT ( 'NONE',  ( -3.750250575282000121, -2.303689136176000130, 0.6493866540274000343 ) ) ;
#31731=ORIENTED_EDGE ( 'NONE', *, *, #51109, .F. ) ;
#31732=CARTESIAN_POINT ( 'NONE',  ( 0.4764073897457280493, -23.51691643868322856, 10.98970030907948114 ) ) ;
#31735=B_SPLINE_CURVE_WITH_KNOTS ( 'NONE', 3,
 ( #45322, #22870, #45026, #9882, #14005, #1045, #32002, #4579 ),
 .UNSPECIFIED., .F., .F.,
 ( 4, 2, 2, 4 ),
 ( 0.000000000000000000, 0.4999999999999973355, 0.7499999999999986677, 1.000000000000000000 ),
 .UNSPECIFIED. ) ;
#31736=CARTESIAN_POINT ( 'NONE',  ( 1.667916687244999974, -55.50150862742999891, 12.49168433577000137 ) ) ;
#31737=CARTESIAN_POINT ( 'NONE',  ( 5.715297388934000189, -78.35615096658000311, 11.69132169264999987 ) ) ;
#31742=EDGE_CURVE ( 'NONE', #57621, #19974, #46053, .T. ) ;
#31746=CARTESIAN_POINT ( 'NONE',  ( 7.626500902217000721, -23.31584477285000290, -10.35747158362999976 ) ) ;
#31749=CARTESIAN_POINT ( 'NONE',  ( -1.182840957218999955, -1.418543513115000154, -3.838043326965000279 ) ) ;
#31751=DIRECTION ( 'NONE',  ( -0.7071067811865475727, 0.000000000000000000, -0.7071067811865475727 ) ) ;
#31752=EDGE_LOOP ( 'NONE', ( #13042, #36977, #6885 ) ) ;
#31755=LINE ( 'NONE', #19078, #55865 ) ;
#31758=ORIENTED_EDGE ( 'NONE', *, *, #9886, .F. ) ;
#31761=ADVANCED_FACE ( 'NONE', ( #55179 ), #52347, .T. ) ;
#31763=CIRCLE ( 'NONE', #39319, 0.8000000000000011546 ) ;
#31766=VECTOR ( 'NONE', #34930, 1000.000000000000000 ) ;
#31767=ORIENTED_EDGE ( 'NONE', *, *, #43956, .T. ) ;
#31769=CARTESIAN_POINT ( 'NONE',  ( 7.342331066867000544, -59.94999999967000548, 8.190859204290999784 ) ) ;
#31773=CARTESIAN_POINT ( 'NONE',  ( -8.179400488414586334, -54.05908162288749708, -9.502921777750872323 ) ) ;
#31775=VERTEX_POINT ( 'NONE', #36872 ) ;
#31778=CARTESIAN_POINT ( 'NONE',  ( 10.19022281664999952, -55.60366258855000154, 7.646946378492000207 ) ) ;
#31779=CARTESIAN_POINT ( 'NONE',  ( -7.678667886032999768, -21.75736537952000305, -10.59548767697000038 ) ) ;
#31780=CARTESIAN_POINT ( 'NONE',  ( 1.538071403319964281, -77.16458333333332575, 11.75000000000000711 ) ) ;
#31781=CARTESIAN_POINT ( 'NONE',  ( 11.75000000000000000, -76.55000000000001137, 0.000000000000000000 ) ) ;
#31784=CARTESIAN_POINT ( 'NONE',  ( -10.13694968398000107, -23.70834319340999841, 7.646073915527999532 ) ) ;
#31785=CARTESIAN_POINT ( 'NONE',  ( 2.425729133266999670E-14, -6.000000000000000000, 0.000000000000000000 ) ) ;
#31786=CARTESIAN_POINT ( 'NONE',  ( -11.44417895085272008, -76.77916666666666856, 3.075537641221497420 ) ) ;
#31787=VECTOR ( 'NONE', #35914, 1000.000000000000000 ) ;
#31793=CARTESIAN_POINT ( 'NONE',  ( 1.382886570147999983, -24.63098219832000169, 12.65982054476000052 ) ) ;
#31795=B_SPLINE_SURFACE_WITH_KNOTS ( 'NONE', 3, 3, ( 
 ( #18522, #53355, #54540, #14081 ),
 ( #40365, #48936, #27062, #26769 ),
 ( #255, #39769, #35624, #57783 ),
 ( #44797, #26197, #4349, #44215 ),
 ( #22350, #58373, #8478, #3763 ),
 ( #17935, #53956, #12901, #30901 ),
 ( #13193, #49227, #45100, #21763 ),
 ( #26473, #19103, #41830, #23812 ) ),
 .UNSPECIFIED., .F., .F., .F.,
 ( 4, 1, 1, 1, 1, 4 ),
 ( 4, 4 ),
 ( -0.01200407345747999885, 0.000000000000000000, 0.3333333333333000081, 0.6666666666667000474, 1.000000000000000000, 1.011997855551999947 ),
 ( -0.3559705542741999906, 1.355970554273999928 ),
 .UNSPECIFIED. ) ;
#31796=CARTESIAN_POINT ( 'NONE',  ( -3.066224723149000297, -0.9186268662769999649, 2.224133471770000092 ) ) ;
#31798=TOROIDAL_SURFACE ( 'NONE', #36532, 17.50000000000000000, 5.000000000000000000 ) ;
#31799=CARTESIAN_POINT ( 'NONE',  ( 10.01332844635999919, -55.51943307300000185, 7.654537085013999764 ) ) ;
#31802=CARTESIAN_POINT ( 'NONE',  ( 14.00000000000000000, -69.50420297070000686, 0.000000000000000000 ) ) ;
#31804=DIRECTION ( 'NONE',  ( 0.000000000000000000, -1.000000000000000000, 0.000000000000000000 ) ) ;
#31818=DIRECTION ( 'NONE',  ( 0.000000000000000000, 0.000000000000000000, -1.000000000000000000 ) ) ;
#31819=CARTESIAN_POINT ( 'NONE',  ( -11.75000000000000000, -77.70000000000000284, 0.000000000000000000 ) ) ;
#31820=LINE ( 'NONE', #40990, #51243 ) ;
#31822=DIRECTION ( 'NONE',  ( -4.762546956201999894E-11, 1.000000000000000000, 4.762495317921000031E-11 ) ) ;
#31824=CARTESIAN_POINT ( 'NONE',  ( -9.546819346760001324, -61.48527546573999558, 8.130850182904000079 ) ) ;
#31826=ORIENTED_EDGE ( 'NONE', *, *, #40075, .F. ) ;
#31827=CARTESIAN_POINT ( 'NONE',  ( -1.722320550011157581, -54.56336311145560103, -12.71171904433065691 ) ) ;
#31829=CARTESIAN_POINT ( 'NONE',  ( 8.335705697175322726, -75.88712408948835275, -8.333479323607702938 ) ) ;
#31835=CARTESIAN_POINT ( 'NONE',  ( 10.42531125070999920, -60.06485145371000556, -7.624341767111000756 ) ) ;
#31842=ORIENTED_EDGE ( 'NONE', *, *, #13441, .F. ) ;
#31844=CARTESIAN_POINT ( 'NONE',  ( 10.36745710147586230, -23.76601929542621150, -7.635228183621981302 ) ) ;
#31846=VERTEX_POINT ( 'NONE', #34174 ) ;
#31848=CIRCLE ( 'NONE', #33756, 1.250000000000000000 ) ;
#31850=CARTESIAN_POINT ( 'NONE',  ( 5.554685856605999561, -76.83457105268000475, 11.87889705760999881 ) ) ;
#31855=CARTESIAN_POINT ( 'NONE',  ( -1.423904377506350016, -24.30512805201053084, 12.50677628656577056 ) ) ;
#31857=DIRECTION ( 'NONE',  ( 0.000000000000000000, 0.000000000000000000, 1.000000000000000000 ) ) ;
#31858=CARTESIAN_POINT ( 'NONE',  ( -11.84062247810999935, -76.52995468096000309, 3.366775603358000080 ) ) ;
#31861=CARTESIAN_POINT ( 'NONE',  ( 2.033676212217215618, -3.175283224387012826, 2.872998029602974679 ) ) ;
#31862=CARTESIAN_POINT ( 'NONE',  ( 7.948089776799000639, -61.24033979686999629, -9.636757666110000287 ) ) ;
#31863=CARTESIAN_POINT ( 'NONE',  ( -4.802691730569000228, -78.39023052333000408, 11.09149278351999968 ) ) ;
#31867=CARTESIAN_POINT ( 'NONE',  ( 10.05087014954224500, -76.84678485164965878, 6.687395104276451008 ) ) ;
#31869=B_SPLINE_SURFACE_WITH_KNOTS ( 'NONE', 3, 3, ( 
 ( #55465, #54598, #14713, #23578 ),
 ( #15312, #19454, #37447, #33305 ),
 ( #50467, #27708, #46922, #32711 ),
 ( #23871, #51341, #28287, #27997 ),
 ( #5570, #28586, #41594, #1174 ),
 ( #55172, #50763, #46336, #5862 ),
 ( #46630, #6160, #24168, #42185 ),
 ( #1753, #10900, #28876, #38035 ),
 ( #7607, #2330, #29450, #25607 ),
 ( #15604, #21181, #56918, #39183 ),
 ( #56628, #47787, #38613, #20893 ) ),
 .UNSPECIFIED., .F., .F., .F.,
 ( 4, 1, 1, 1, 1, 1, 1, 1, 4 ),
 ( 4, 4 ),
 ( -0.02001211456242000045, 0.000000000000000000, 0.1666666666667000196, 0.3333333333333000081, 0.5000000000000000000, 0.6666666666667000474, 0.8333333333333000637, 1.000000000000000000, 1.020273719995999917 ),
 ( -0.3582002740308999900, 1.358863140970000050 ),
 .UNSPECIFIED. ) ;
#31870=ORIENTED_EDGE ( 'NONE', *, *, #50508, .F. ) ;
#31872=CARTESIAN_POINT ( 'NONE',  ( -12.00000000000000000, -60.04999999966999980, 0.000000000000000000 ) ) ;
#31879=AXIS2_PLACEMENT_3D ( 'NONE', #30408, #25982, #30976 ) ;
#31880=CARTESIAN_POINT ( 'NONE',  ( 2.574494627908628264, -76.05712420562880993, 11.46441856251786717 ) ) ;
#31884=CARTESIAN_POINT ( 'NONE',  ( 1.623944433304999935, -76.18552953598467070, -12.20239005717999881 ) ) ;
#31888=CARTESIAN_POINT ( 'NONE',  ( 12.50000000000000000, -17.31640971966000109, -1.003652782652999953 ) ) ;
#31893=CARTESIAN_POINT ( 'NONE',  ( 12.70722357733919949, -17.58971352782045017, 1.610228312194780687 ) ) ;
#31895=LINE ( 'NONE', #18639, #28262 ) ;
#31899=EDGE_CURVE ( 'NONE', #45259, #35427, #22146, .T. ) ;
#31902=CARTESIAN_POINT ( 'NONE',  ( 1.911540947291000103, -3.081127687535999637, 3.291214574437999918 ) ) ;
#31903=ADVANCED_FACE ( 'NONE', ( #37752, #47516 ), #10909, .F. ) ;
#31905=CARTESIAN_POINT ( 'NONE',  ( 7.624341764906000130, -55.53514850498000044, 10.42531124851000079 ) ) ;
#31907=CARTESIAN_POINT ( 'NONE',  ( -12.77656765293000163, -25.31198129913999750, 0.1555235816856000153 ) ) ;
#31908=VERTEX_POINT ( 'NONE', #51646 ) ;
#31909=ORIENTED_EDGE ( 'NONE', *, *, #13062, .T. ) ;
#31912=EDGE_LOOP ( 'NONE', ( #7310, #7129, #16827, #43397 ) ) ;
#31914=CARTESIAN_POINT ( 'NONE',  ( 7.647093862755999893, -23.36895637638999901, 10.00844027276999881 ) ) ;
#31915=CONICAL_SURFACE ( 'NONE', #6483, 0.6999999997694995590, 0.7853981633972997312 ) ;
#31916=EDGE_CURVE ( 'NONE', #11190, #9459, #3136, .T. ) ;
#31917=CARTESIAN_POINT ( 'NONE',  ( 9.770427757074999775, -61.85529868422999300, 8.292768371773000524 ) ) ;
#31922=ORIENTED_EDGE ( 'NONE', *, *, #20329, .F. ) ;
#31923=CARTESIAN_POINT ( 'NONE',  ( 7.634645133894655267, -60.27584427251623111, -10.10912661257307477 ) ) ;
#31924=ORIENTED_EDGE ( 'NONE', *, *, #46695, .F. ) ;
#31929=CARTESIAN_POINT ( 'NONE',  ( 3.629361671790999999, -75.76997015003999536, 11.72003014384999986 ) ) ;
#31936=CARTESIAN_POINT ( 'NONE',  ( 1.799502287743000029, -60.10716934574000447, -12.60413652834999887 ) ) ;
#31937=CARTESIAN_POINT ( 'NONE',  ( -8.188331488387625257, -60.02841244176944713, 7.345153731672212416 ) ) ;
#31939=ORIENTED_EDGE ( 'NONE', *, *, #44540, .F. ) ;
#31944=CARTESIAN_POINT ( 'NONE',  ( 1.636761686205415067, -3.333333333333333481, 2.839805762151342616 ) ) ;
#31945=CARTESIAN_POINT ( 'NONE',  ( -12.00000000000000000, -23.25000000000000000, -1.250000000000000000 ) ) ;
#31946=DIRECTION ( 'NONE',  ( 0.000000000000000000, -1.000000000000000000, 0.000000000000000000 ) ) ;
#31957=CARTESIAN_POINT ( 'NONE',  ( 3.549182112775000064, -1.939138932809999938, -1.374451376799000091 ) ) ;
#31962=CARTESIAN_POINT ( 'NONE',  ( 0.000000000000000000, 4.040000000000000036, 0.000000000000000000 ) ) ;
#31963=DIRECTION ( 'NONE',  ( 0.000000000000000000, -1.000000000000000000, 0.000000000000000000 ) ) ;
#31964=CARTESIAN_POINT ( 'NONE',  ( 12.54983130239999944, -16.94901607458999848, 0.1356732392833999989 ) ) ;
#31966=AXIS2_PLACEMENT_3D ( 'NONE', #20965, #12110, #8255 ) ;
#31968=CARTESIAN_POINT ( 'NONE',  ( 9.389188763448000685, -54.08956227294000740, -8.194870530143999687 ) ) ;
#31972=CARTESIAN_POINT ( 'NONE',  ( 1.930860503475322121, -60.57417505891291398, 12.72930866334770705 ) ) ;
#31974=AXIS2_PLACEMENT_3D ( 'NONE', #50947, #55068, #36760 ) ;
#31975=CARTESIAN_POINT ( 'NONE',  ( -12.77651065753999937, -62.10896598063000340, -0.04308629978602999955 ) ) ;
#31977=CARTESIAN_POINT ( 'NONE',  ( 5.940599228801999379E-14, -5.899999999999999467, -13.99999999999886491 ) ) ;
#31978=CARTESIAN_POINT ( 'NONE',  ( -12.70556836347999941, -16.77227722772000007, 1.774192816106000118E-09 ) ) ;
#31981=CARTESIAN_POINT ( 'NONE',  ( 9.298479816477872362, -53.91187382742512568, 8.385858173805548432 ) ) ;
#31985=ORIENTED_EDGE ( 'NONE', *, *, #14180, .F. ) ;
#31989=CARTESIAN_POINT ( 'NONE',  ( -1.370379768245999841E-14, -74.59999999999999432, 0.000000000000000000 ) ) ;
#31991=FACE_OUTER_BOUND ( 'NONE', #13733, .T. ) ;
#31994=DIRECTION ( 'NONE',  ( 0.000000000000000000, 1.000000000000000000, 0.000000000000000000 ) ) ;
#31995=CARTESIAN_POINT ( 'NONE',  ( 0.9212224518303999687, -24.81954101839000160, -12.54670315981999984 ) ) ;
#31997=CARTESIAN_POINT ( 'NONE',  ( 11.99999999979999821, -18.85000000927000130, 0.7999999997951999786 ) ) ;
#31998=CARTESIAN_POINT ( 'NONE',  ( -5.373789810023999358, -78.83213957653998705, -10.63267532885000044 ) ) ;
#32000=ORIENTED_EDGE ( 'NONE', *, *, #9972, .F. ) ;
#32002=CARTESIAN_POINT ( 'NONE',  ( -1.749899258077675324, -18.61283151237003963, -12.55433901290727405 ) ) ;
#32006=DIRECTION ( 'NONE',  ( 0.000000000000000000, -1.000000000000000000, 0.000000000000000000 ) ) ;
#32008=CARTESIAN_POINT ( 'NONE',  ( 12.36191581903000092, -76.56064262049000035, -3.311046255921999748 ) ) ;
#32009=EDGE_CURVE ( 'NONE', #43036, #38390, #41933, .T. ) ;
#32011=CARTESIAN_POINT ( 'NONE',  ( -12.49306752634999995, -23.28056692670000061, -1.667917367010000040 ) ) ;
#32012=CARTESIAN_POINT ( 'NONE',  ( -0.6999999999999999556, -21.00000000000000000, 11.90000000000000036 ) ) ;
#32016=CARTESIAN_POINT ( 'NONE',  ( -11.75000000000000178, -78.29297251775329869, 1.037641870170390002 ) ) ;
#32022=ADVANCED_FACE ( 'NONE', ( #44212 ), #7119, .F. ) ;
#32026=CARTESIAN_POINT ( 'NONE',  ( -0.5999999999999999778, -18.84999999999999787, -10.98362417419999915 ) ) ;
#32027=ADVANCED_FACE ( 'NONE', ( #30032 ), #45782, .F. ) ;
#32030=CARTESIAN_POINT ( 'NONE',  ( 1.667961430005999945, -57.05111654290000445, 12.58335110165999993 ) ) ;
#32031=CARTESIAN_POINT ( 'NONE',  ( 5.647598101448999763, -77.85660919792000811, 11.72364604052000203 ) ) ;
#32033=CARTESIAN_POINT ( 'NONE',  ( 9.850513606030963487, -17.69492088480771841, 7.836738268704446675 ) ) ;
#32036=CIRCLE ( 'NONE', #33937, 14.00000000000000000 ) ;
#32041=CARTESIAN_POINT ( 'NONE',  ( 4.010845454633999552, -1.493904343864000062, -0.2065758488482999922 ) ) ;
#32043=CYLINDRICAL_SURFACE ( 'NONE', #45326, 1.750000000000001332 ) ;
#32045=ORIENTED_EDGE ( 'NONE', *, *, #26796, .F. ) ;
#32049=ORIENTED_EDGE ( 'NONE', *, *, #57492, .F. ) ;
#32050=ORIENTED_EDGE ( 'NONE', *, *, #43438, .T. ) ;
#32056=ORIENTED_EDGE ( 'NONE', *, *, #31001, .F. ) ;
#32059=VECTOR ( 'NONE', #8717, 1000.000000000000000 ) ;
#32060=VECTOR ( 'NONE', #9693, 1000.000000000000000 ) ;
#32061=CARTESIAN_POINT ( 'NONE',  ( -1.192446808648067735, -2.695995745449793812, -3.022765882159190731 ) ) ;
#32075=CARTESIAN_POINT ( 'NONE',  ( 3.075537641221509411, -78.65416666666668277, 11.44417895085272008 ) ) ;
#32078=CARTESIAN_POINT ( 'NONE',  ( 11.48655120864317425, -76.46745349848808360, 2.565345163985293553 ) ) ;
#32079=CIRCLE ( 'NONE', #27410, 14.00000000000000000 ) ;
#32080=EDGE_CURVE ( 'NONE', #17178, #33530, #14362, .T. ) ;
#32081=CARTESIAN_POINT ( 'NONE',  ( -0.5847500590555335664, -23.30655143820058228, -10.98448857562232028 ) ) ;
#32084=CARTESIAN_POINT ( 'NONE',  ( 10.50409585618203501, -78.24416319518880414, 5.966360771605526025 ) ) ;
#32089=CARTESIAN_POINT ( 'NONE',  ( -13.79999999994999982, 4.699973049637762301E-11, -2.072309110287000051E-09 ) ) ;
#32090=CARTESIAN_POINT ( 'NONE',  ( -1.761265949708000100, -23.70858218785999938, 12.57448205042999945 ) ) ;
#32091=CARTESIAN_POINT ( 'NONE',  ( 11.80100040496257563, -79.25000000000001421, -2.513071059627543846 ) ) ;
#32093=CARTESIAN_POINT ( 'NONE',  ( -1.116072162164000181, -1.569750604645999914, -3.621394142857999654 ) ) ;
#32096=CARTESIAN_POINT ( 'NONE',  ( 10.04115011118999945, -56.03513569577999931, 7.682331425181999407 ) ) ;
#32098=DIRECTION ( 'NONE',  ( -1.000000000000000000, 0.000000000000000000, 0.000000000000000000 ) ) ;
#32099=DIRECTION ( 'NONE',  ( 3.788597347406000047E-11, 1.000000000000000000, 0.000000000000000000 ) ) ;
#32101=CARTESIAN_POINT ( 'NONE',  ( -14.00000000000000000, -9.295797029142999435, 3.101241903103999638E-11 ) ) ;
#32105=VERTEX_POINT ( 'NONE', #54538 ) ;
#32109=CARTESIAN_POINT ( 'NONE',  ( -1.980584515752000119, -55.53514853344000102, -12.76303204600000107 ) ) ;
#32112=CARTESIAN_POINT ( 'NONE',  ( 9.546819346421999697, -24.68527546640000025, -8.130850183241999929 ) ) ;
#32113=DIRECTION ( 'NONE',  ( 1.000000000000000000, 0.000000000000000000, 0.000000000000000000 ) ) ;
#32117=ORIENTED_EDGE ( 'NONE', *, *, #29786, .T. ) ;
#32118=CARTESIAN_POINT ( 'NONE',  ( -1.318114156661947423, -54.06427522772299454, -12.70261578158667248 ) ) ;
#32122=CARTESIAN_POINT ( 'NONE',  ( -12.64502302235999842, -56.02870851050000311, -1.799490220168999954 ) ) ;
#32123=CARTESIAN_POINT ( 'NONE',  ( 10.98362417419999915, -23.15000000000000213, 0.5999999999999999778 ) ) ;
#32127=VERTEX_POINT ( 'NONE', #1401 ) ;
#32133=DIRECTION ( 'NONE',  ( 0.000000000000000000, 1.000000000000000000, 0.000000000000000000 ) ) ;
#32135=B_SPLINE_CURVE_WITH_KNOTS ( 'NONE', 3,
 ( #5467, #5754, #41776, #9905, #14897, #32604, #32895, #46816, #27886, #10487, #1067, #14608, #45934, #51526, #37629, #37920, #11083, #28472 ),
 .UNSPECIFIED., .F., .F.,
 ( 4, 2, 2, 2, 2, 2, 2, 2, 4 ),
 ( 0.000000000000000000, 0.1250000000000000000, 0.2500000000000000000, 0.3750000000000000000, 0.5000000000000000000, 0.6250000000000000000, 0.7500000000000000000, 0.8750000000000000000, 1.000000000000000000 ),
 .UNSPECIFIED. ) ;
#32139=B_SPLINE_CURVE_WITH_KNOTS ( 'NONE', 3,
 ( #36395, #33915, #6192, #49999 ),
 .UNSPECIFIED., .F., .F.,
 ( 4, 4 ),
 ( 0.000000000000000000, 1.000000000000000000 ),
 .UNSPECIFIED. ) ;
#32140=CIRCLE ( 'NONE', #40638, 12.50000000000000000 ) ;
#32142=CARTESIAN_POINT ( 'NONE',  ( -9.359366689070000689, -77.55613138518998539, -9.185202947203000790 ) ) ;
#32146=ORIENTED_EDGE ( 'NONE', *, *, #21764, .F. ) ;
#32148=EDGE_CURVE ( 'NONE', #27639, #5204, #53845, .T. ) ;
#32149=CARTESIAN_POINT ( 'NONE',  ( 5.894077591580000330, -76.64739919339000096, -10.80721126921000064 ) ) ;
#32151=CARTESIAN_POINT ( 'NONE',  ( 0.8323291101560614802, -2.493205130203935749, -3.480095087541390519 ) ) ;
#32152=CARTESIAN_POINT ( 'NONE',  ( 7.658900562732000594, -60.00940503048000352, -10.01676248783999945 ) ) ;
#32153=CARTESIAN_POINT ( 'NONE',  ( 12.21456857099000004, -78.76020556754998836, -1.096995930408000142 ) ) ;
#32155=CARTESIAN_POINT ( 'NONE',  ( 7.648026768008000076, -55.55000001556999933, -10.12290050216000026 ) ) ;
#32157=CARTESIAN_POINT ( 'NONE',  ( 9.229604799106443380, -76.85567982616369420, 7.771863644200966981 ) ) ;
#32162=CARTESIAN_POINT ( 'NONE',  ( -12.50000000000000000, -18.75000000310999937, 1.750000000000000000 ) ) ;
#32163=CARTESIAN_POINT ( 'NONE',  ( -1.750000000001000089, -56.04899163641999849, -12.60354432391000046 ) ) ;
#32168=CARTESIAN_POINT ( 'NONE',  ( 0.3917937483749863725, -76.07213746520410780, 11.74425345321102299 ) ) ;
#32172=CARTESIAN_POINT ( 'NONE',  ( 1.980584515756000030, -18.73514849905999924, -12.76303204340999997 ) ) ;
#32174=CARTESIAN_POINT ( 'NONE',  ( -14.00000000000000000, -46.13782243168999742, -5.544480864478000239E-06 ) ) ;
#32177=DIRECTION ( 'NONE',  ( 0.000000000000000000, 1.000000000000000000, 0.000000000000000000 ) ) ;
#32179=PLANE ( 'NONE',  #30243 ) ;
#32180=CARTESIAN_POINT ( 'NONE',  ( 9.389188763474001220, -17.28956227326999695, -8.194870530173000489 ) ) ;
#32181=DIRECTION ( 'NONE',  ( 0.7071067812087692417, 2.829525585096875613E-07, -0.7071067811642691714 ) ) ;
#32185=FACE_BOUND ( 'NONE', #39286, .T. ) ;
#32189=CARTESIAN_POINT ( 'NONE',  ( 12.50659871789738276, -61.77347219457124083, -0.3508073943565040431 ) ) ;
#32190=DIRECTION ( 'NONE',  ( 0.9999476293090542312, 0.000000000000000000, 0.01023418971888952027 ) ) ;
#32191=EDGE_CURVE ( 'NONE', #6077, #11225, #14648, .T. ) ;
#32193=CARTESIAN_POINT ( 'NONE',  ( 0.000000000000000000, -3.749999999256000027, 0.000000000000000000 ) ) ;
#32194=EDGE_CURVE ( 'NONE', #42541, #3955, #27836, .T. ) ;
#32197=ORIENTED_EDGE ( 'NONE', *, *, #29942, .T. ) ;
#32198=ORIENTED_EDGE ( 'NONE', *, *, #2631, .T. ) ;
#32206=CARTESIAN_POINT ( 'NONE',  ( 7.646092217304000904, -60.50851177880000620, 10.13691708059000085 ) ) ;
#32207=CARTESIAN_POINT ( 'NONE',  ( 12.50000000000000000, -55.54999999966999980, 0.000000000000000000 ) ) ;
#32211=EDGE_LOOP ( 'NONE', ( #57424, #44335, #57536, #31690 ) ) ;
#32212=CARTESIAN_POINT ( 'NONE',  ( -10.36745710147586230, -23.76601929542621150, 7.635228183621981302 ) ) ;
#32213=VERTEX_POINT ( 'NONE', #27060 ) ;
#32214=EDGE_CURVE ( 'NONE', #25015, #26696, #18422, .T. ) ;
#32218=VECTOR ( 'NONE', #42099, 999.9999999999998863 ) ;
#32225=CARTESIAN_POINT ( 'NONE',  ( 2.062670899361999766, -60.10639784916000394, -12.83044027763000017 ) ) ;
#32226=CARTESIAN_POINT ( 'NONE',  ( 12.83044039277999993, -60.10639625617000092, -2.062670899148999926 ) ) ;
#32227=ADVANCED_FACE ( 'NONE', ( #28224 ), #50702, .F. ) ;
#32229=ORIENTED_EDGE ( 'NONE', *, *, #35938, .F. ) ;
#32233=ADVANCED_FACE ( 'NONE', ( #18520 ), #8036, .F. ) ;
#32234=CARTESIAN_POINT ( 'NONE',  ( -10.47513558174000003, -18.19636614430000066, 7.624778818008999259 ) ) ;
#32235=LINE ( 'NONE', #31652, #714 ) ;
#32242=EDGE_LOOP ( 'NONE', ( #7114, #4565, #45153, #24586 ) ) ;
#32244=CARTESIAN_POINT ( 'NONE',  ( 1.540744644154000031, -2.148872700496999855, 3.654751654090000024 ) ) ;
#32247=CARTESIAN_POINT ( 'NONE',  ( 8.227501432777001966, -24.82538814609000255, -9.516269854983999466 ) ) ;
#32248=LINE ( 'NONE', #45577, #21317 ) ;
#32249=CARTESIAN_POINT ( 'NONE',  ( 0.8522304910899691777, -1.955669459018320122, 3.167342208975652440 ) ) ;
#32251=B_SPLINE_CURVE_WITH_KNOTS ( 'NONE', 3,
 ( #34270, #20997, #16863, #34844 ),
 .UNSPECIFIED., .F., .F.,
 ( 4, 4 ),
 ( 0.000000000000000000, 1.000000000000000000 ),
 .UNSPECIFIED. ) ;
#32255=DIRECTION ( 'NONE',  ( 0.000000000000000000, 1.000000000000000000, 0.000000000000000000 ) ) ;
#32265=EDGE_CURVE ( 'NONE', #42393, #5429, #57396, .T. ) ;
#32266=ORIENTED_EDGE ( 'NONE', *, *, #38780, .F. ) ;
#32267=EDGE_CURVE ( 'NONE', #17032, #23858, #539, .T. ) ;
#32273=ORIENTED_EDGE ( 'NONE', *, *, #56086, .T. ) ;
#32275=VERTEX_POINT ( 'NONE', #11707 ) ;
#32276=ORIENTED_EDGE ( 'NONE', *, *, #42593, .T. ) ;
#32278=VECTOR ( 'NONE', #45956, 1000.000000000000000 ) ;
#32281=AXIS2_PLACEMENT_3D ( 'NONE', #15134, #23993, #54710 ) ;
#32283=CARTESIAN_POINT ( 'NONE',  ( 0.000000000000000000, -23.25000000000000000, -12.00000000000000000 ) ) ;
#32284=ORIENTED_EDGE ( 'NONE', *, *, #33310, .F. ) ;
#32285=ORIENTED_EDGE ( 'NONE', *, *, #7335, .T. ) ;
#32287=DIRECTION ( 'NONE',  ( 0.000000000000000000, 0.000000000000000000, 1.000000000000000000 ) ) ;
#32288=DIRECTION ( 'NONE',  ( -1.000000000000000000, 0.000000000000000000, 0.000000000000000000 ) ) ;
#32291=CARTESIAN_POINT ( 'NONE',  ( -10.53101990620000095, -23.30639784948999704, 7.613962745608000127 ) ) ;
#32292=CARTESIAN_POINT ( 'NONE',  ( 12.32442898454999813, -77.55972615780000012, -3.452188809138999837 ) ) ;
#32295=CARTESIAN_POINT ( 'NONE',  ( -5.178558594642320934, -76.61041601060691164, 10.57677830698726851 ) ) ;
#32298=AXIS2_PLACEMENT_3D ( 'NONE', #29838, #25710, #47890 ) ;
#32300=CARTESIAN_POINT ( 'NONE',  ( 3.249790610657787848, -2.854537099176947201, 0.1710447749874229040 ) ) ;
#32301=DIRECTION ( 'NONE',  ( -0.009503199022040095811, 0.000000000000000000, 0.9999548435846228323 ) ) ;
#32306=CARTESIAN_POINT ( 'NONE',  ( -0.8385792221450999451, -2.924655184951000297, -3.712528424878000166 ) ) ;
#32308=ORIENTED_EDGE ( 'NONE', *, *, #24040, .T. ) ;
#32309=CARTESIAN_POINT ( 'NONE',  ( 9.243123480653681057, -61.71653773532028708, 8.441201026288084108 ) ) ;
#32310=CARTESIAN_POINT ( 'NONE',  ( 7.452378523309729275, -60.34721902435785523, -8.090910852015744226 ) ) ;
#32311=CARTESIAN_POINT ( 'NONE',  ( 1.537589725670525764, -77.56258520800980705, 11.74337905373031532 ) ) ;
#32312=CARTESIAN_POINT ( 'NONE',  ( 1.930989144707000005, -58.55365779174999830, 12.80900240954000147 ) ) ;
#32313=CARTESIAN_POINT ( 'NONE',  ( 12.55073801092999908, -77.17672481401000084, -3.437763296274999991 ) ) ;
#32316=ADVANCED_FACE ( 'NONE', ( #15247 ), #28815, .F. ) ;
#32318=CARTESIAN_POINT ( 'NONE',  ( 9.609171231144982173, -78.49653939831271998, 6.760579772709885304 ) ) ;
#32320=AXIS2_PLACEMENT_3D ( 'NONE', #10279, #41570, #41278 ) ;
#32321=DIRECTION ( 'NONE',  ( -0.6489586469986102779, 0.04890178910784081373, -0.7592504787669123179 ) ) ;
#32325=DIRECTION ( 'NONE',  ( 0.7071067811705344930, 1.925105116903093482E-07, 0.7071067812025343402 ) ) ;
#32328=CARTESIAN_POINT ( 'NONE',  ( 3.981113306789000106, -1.056808102910000047, -0.5296481109823999445 ) ) ;
#32329=CARTESIAN_POINT ( 'NONE',  ( -1.667961445601999992, -58.54800977479000323, -12.58338334669999981 ) ) ;
#32333=LINE ( 'NONE', #27907, #42828 ) ;
#32338=CARTESIAN_POINT ( 'NONE',  ( 0.000000000000000000, -9.295797029142999435, 0.000000000000000000 ) ) ;
#32345=ORIENTED_EDGE ( 'NONE', *, *, #2842, .T. ) ;
#32346=CARTESIAN_POINT ( 'NONE',  ( -0.7260205774406525148, -2.708476618800434998, -3.168507982638361309 ) ) ;
#32348=ORIENTED_EDGE ( 'NONE', *, *, #38954, .T. ) ;
#32349=CIRCLE ( 'NONE', #339, 1.750000000000000000 ) ;
#32351=CARTESIAN_POINT ( 'NONE',  ( 10.45205659047999980, -59.56232685193999998, 7.651160337235999975 ) ) ;
#32352=ADVANCED_FACE ( 'NONE', ( #38843 ), #33492, .F. ) ;
#32361=CARTESIAN_POINT ( 'NONE',  ( -8.096452064242996016, -22.78578169018999944, 13.15643568217000769 ) ) ;
#32363=DIRECTION ( 'NONE',  ( 0.000000000000000000, 1.000000000000000000, 0.000000000000000000 ) ) ;
#32365=CARTESIAN_POINT ( 'NONE',  ( -7.718368845804999268, -57.05199022587000002, -10.07722254368999870 ) ) ;
#32367=CARTESIAN_POINT ( 'NONE',  ( 6.792517171462394643, -76.52567734522683907, 9.587677660702928151 ) ) ;
#32368=CARTESIAN_POINT ( 'NONE',  ( 1.980584515752000119, -23.26485146623999967, -12.76303204602000108 ) ) ;
#32371=CARTESIAN_POINT ( 'NONE',  ( 2.256974249120885290, -78.09294649791769416, -11.85744693861532539 ) ) ;
#32374=CARTESIAN_POINT ( 'NONE',  ( -12.46164872708000004, -18.32834420040999746, 1.631615798668999862 ) ) ;
#32379=CARTESIAN_POINT ( 'NONE',  ( -3.562349398201000383, -1.892636553150000012, -0.5356682315460999932 ) ) ;
#32381=CARTESIAN_POINT ( 'NONE',  ( 10.21381326473999884, -59.57129148919000272, 7.668949790015999746 ) ) ;
#32382=CARTESIAN_POINT ( 'NONE',  ( -1.194090705999000024, -24.44031658902999737, -12.43436538489999954 ) ) ;
#32384=CARTESIAN_POINT ( 'NONE',  ( 1.722652182756000183, -2.378241823149000123, 3.030129174318000107 ) ) ;
#32385=CARTESIAN_POINT ( 'NONE',  ( 1.382886570148999850, -54.16901780135000166, -12.65982054472000051 ) ) ;
#32386=DIRECTION ( 'NONE',  ( -1.000000000000000000, 0.000000000000000000, 0.000000000000000000 ) ) ;
#32390=CARTESIAN_POINT ( 'NONE',  ( 4.857361268487999872, -76.91360380131999364, -11.04062220482000001 ) ) ;
#32391=EDGE_LOOP ( 'NONE', ( #29020, #9218, #12861, #2039 ) ) ;
#32393=AXIS2_PLACEMENT_3D ( 'NONE', #43484, #56771, #16903 ) ;
#32395=CARTESIAN_POINT ( 'NONE',  ( -7.958763980599000476, -17.52301961032999955, -9.723170659105999647 ) ) ;
#32398=CARTESIAN_POINT ( 'NONE',  ( 12.43652237957999951, -53.87935153028999480, -0.1283967009859000308 ) ) ;
#32399=FACE_OUTER_BOUND ( 'NONE', #36588, .T. ) ;
#32400=CARTESIAN_POINT ( 'NONE',  ( -3.500000000146000101, -0.7499999998540000101, 2.054632350152999929E-08 ) ) ;
#32407=CARTESIAN_POINT ( 'NONE',  ( -0.002438198160231863729, -75.82452515419292638, -11.78599345671029752 ) ) ;
#32409=EDGE_CURVE ( 'NONE', #56909, #17250, #36313, .T. ) ;
#32410=CARTESIAN_POINT ( 'NONE',  ( -12.83044039271999992, -55.49360374314999689, -2.062670899148999926 ) ) ;
#32415=CARTESIAN_POINT ( 'NONE',  ( 7.624341764943999955, -60.06485149430999826, -10.42531124854999902 ) ) ;
#32416=EDGE_LOOP ( 'NONE', ( #25707, #43564, #57457, #1800 ) ) ;
#32417=CARTESIAN_POINT ( 'NONE',  ( 12.50659871785095589, -24.97347219492458592, -0.3508073941908030347 ) ) ;
#32419=EDGE_CURVE ( 'NONE', #48994, #42771, #48212, .T. ) ;
#32420=AXIS2_PLACEMENT_3D ( 'NONE', #57141, #17270, #3697 ) ;
#32421=ORIENTED_EDGE ( 'NONE', *, *, #40763, .T. ) ;
#32422=CARTESIAN_POINT ( 'NONE',  ( -7.678655902623767737, -55.00623020231261506, 10.03844298032656823 ) ) ;
#32424=CARTESIAN_POINT ( 'NONE',  ( -12.54987272477000104, -25.05113590135999857, -0.1385846084899000075 ) ) ;
#32427=CARTESIAN_POINT ( 'NONE',  ( 1.980611416588510032, -18.47402268194409203, -12.74335092663070057 ) ) ;
#32429=B_SPLINE_CURVE_WITH_KNOTS ( 'NONE', 3,
 ( #15127, #56455, #28997, #55878, #28110, #11299 ),
 .UNSPECIFIED., .F., .F.,
 ( 4, 1, 1, 4 ),
 ( 0.000000000000000000, 0.3333333333333000081, 0.6666666666667000474, 1.000000000000000000 ),
 .UNSPECIFIED. ) ;
#32430=VECTOR ( 'NONE', #41213, 1000.000000000000000 ) ;
#32435=CARTESIAN_POINT ( 'NONE',  ( 3.007117222848000093, -75.83802852838000774, 11.93703523519999976 ) ) ;
#32437=ADVANCED_FACE ( 'NONE', ( #21127 ), #6474, .F. ) ;
#32438=CARTESIAN_POINT ( 'NONE',  ( -3.004631399418401294, -2.305633654303593350, 1.836342379236549860 ) ) ;
#32439=DIRECTION ( 'NONE',  ( 0.000000000000000000, 1.000000000000000000, 0.000000000000000000 ) ) ;
#32440=CARTESIAN_POINT ( 'NONE',  ( -12.10179013622999911, -78.49561315626999658, -1.986401539992999954 ) ) ;
#32444=CARTESIAN_POINT ( 'NONE',  ( 11.00000000000000000, -23.75000000000000000, -1.203259120426999909E-14 ) ) ;
#32445=CARTESIAN_POINT ( 'NONE',  ( -4.227663776733128209, -76.95352454581043844, 11.31097848705637965 ) ) ;
#32447=VERTEX_POINT ( 'NONE', #8417 ) ;
#32455=CARTESIAN_POINT ( 'NONE',  ( 8.318892879164591747, -76.01180963423074388, 8.297585421471344702 ) ) ;
#32458=ORIENTED_EDGE ( 'NONE', *, *, #34985, .T. ) ;
#32461=CARTESIAN_POINT ( 'NONE',  ( 10.42531124905999995, -23.26485148473999942, 7.624341765453999997 ) ) ;
#32464=FACE_OUTER_BOUND ( 'NONE', #6667, .T. ) ;
#32467=CARTESIAN_POINT ( 'NONE',  ( 7.622784390062999904, -18.21288991773999655, -10.47836615826999918 ) ) ;
#32468=CARTESIAN_POINT ( 'NONE',  ( 13.63885489310999510, -56.01421830980998351, -7.254376133916000668 ) ) ;
#32469=ORIENTED_EDGE ( 'NONE', *, *, #10165, .F. ) ;
#32471=CARTESIAN_POINT ( 'NONE',  ( 12.70255494770093918, -54.05391159002875412, 1.306413223725076067 ) ) ;
#32474=CARTESIAN_POINT ( 'NONE',  ( -8.425436799864590043, -77.01663941737371033, -8.658731487823875028 ) ) ;
#32479=EDGE_CURVE ( 'NONE', #12183, #26753, #41043, .T. ) ;
#32481=CARTESIAN_POINT ( 'NONE',  ( 10.42531125074000009, -18.73514854687000053, 7.624341767140999870 ) ) ;
#32486=ADVANCED_FACE ( 'NONE', ( #34334 ), #52368, .F. ) ;
#32490=VERTEX_POINT ( 'NONE', #30486 ) ;
#32491=CARTESIAN_POINT ( 'NONE',  ( 0.000000000000000000, 4.040000000000000036, 0.000000000000000000 ) ) ;
#32493=CARTESIAN_POINT ( 'NONE',  ( 8.643979526188999785, -62.05953772878000052, 9.422807787405000468 ) ) ;
#32499=EDGE_LOOP ( 'NONE', ( #19665, #32996, #53567, #1325 ) ) ;
#32500=FACE_OUTER_BOUND ( 'NONE', #33403, .T. ) ;
#32501=EDGE_LOOP ( 'NONE', ( #45305, #54647, #20310, #12044 ) ) ;
#32505=CARTESIAN_POINT ( 'NONE',  ( 8.485281374238999419, -23.25000000000000000, -8.485281374238999419 ) ) ;
#32507=CARTESIAN_POINT ( 'NONE',  ( -9.102137320389529052, -17.02814024879980792, 8.583672455348743568 ) ) ;
#32508=CARTESIAN_POINT ( 'NONE',  ( -3.206516299415000049, -2.013032031398999777, -0.5298615117031000299 ) ) ;
#32512=AXIS2_PLACEMENT_3D ( 'NONE', #6492, #41634, #2086 ) ;
#32513=CARTESIAN_POINT ( 'NONE',  ( -7.969039355681999837, -24.62377467844000023, -9.934746417635000881 ) ) ;
#32514=CARTESIAN_POINT ( 'NONE',  ( 12.80896991328000034, -57.04546192861999998, -1.930989179114000143 ) ) ;
#32516=EDGE_LOOP ( 'NONE', ( #47507, #49630 ) ) ;
#32522=ADVANCED_FACE ( 'NONE', ( #30765 ), #44660, .F. ) ;
#32524=DIRECTION ( 'NONE',  ( 4.762546956201999894E-11, -1.000000000000000000, 4.762495317921000031E-11 ) ) ;
#32525=CARTESIAN_POINT ( 'NONE',  ( 3.534803853715930089, -2.486768684982593847, -0.6079085174694663918 ) ) ;
#32532=ORIENTED_EDGE ( 'NONE', *, *, #47427, .F. ) ;
#32534=CARTESIAN_POINT ( 'NONE',  ( -3.607726709122000219, -2.271525618455999762, 1.647853588899000021 ) ) ;
#32539=CARTESIAN_POINT ( 'NONE',  ( -1.532229594837823505, -24.12298963131021168, -12.51228690880890682 ) ) ;
#32540=CARTESIAN_POINT ( 'NONE',  ( -8.894932048704164984, -53.57190732453712201, -9.073469156659786705 ) ) ;
#32541=B_SPLINE_SURFACE_WITH_KNOTS ( 'NONE', 3, 3, ( 
 ( #16921, #16631, #33754, #34617 ),
 ( #29893, #57358, #47665, #43796 ),
 ( #38192, #47083, #52644, #29323 ),
 ( #51793, #11346, #43498, #6612 ),
 ( #24910, #42927, #57071, #56211 ),
 ( #3059, #47950, #48233, #7769 ),
 ( #21055, #47371, #34900, #52930 ),
 ( #39056, #29042, #2482, #12199 ),
 ( #30184, #25772, #3343, #20486 ),
 ( #21339, #15759, #39351, #24623 ),
 ( #7191, #2201, #34038, #6901 ) ),
 .UNSPECIFIED., .F., .F., .F.,
 ( 4, 1, 1, 1, 1, 1, 1, 1, 4 ),
 ( 4, 4 ),
 ( -0.01994534136800000038, 0.000000000000000000, 0.1666666666667000196, 0.3333333333333000081, 0.5000000000000000000, 0.6666666666667000474, 0.8333333333333000637, 1.000000000000000000, 1.020519780480000138 ),
 ( -0.3582002740342999925, 1.358566136078000142 ),
 .UNSPECIFIED. ) ;
#32543=CARTESIAN_POINT ( 'NONE',  ( -7.686941364964000378, -58.55472017773000459, 10.48774103561000182 ) ) ;
#32544=CARTESIAN_POINT ( 'NONE',  ( 12.90058126069000011, -78.75123239577999357, 1.113827872717999989 ) ) ;
#32545=VECTOR ( 'NONE', #19926, 1000.000000000000000 ) ;
#32547=EDGE_CURVE ( 'NONE', #14715, #19368, #54240, .T. ) ;
#32551=CARTESIAN_POINT ( 'NONE',  ( -1.811016405462463119, -60.86173555340016605, 12.71771640067393605 ) ) ;
#32559=DIRECTION ( 'NONE',  ( 4.762557283857999921E-11, 1.000000000000000000, -4.762495317921000031E-11 ) ) ;
#32560=ORIENTED_EDGE ( 'NONE', *, *, #28194, .T. ) ;
#32561=ADVANCED_FACE ( 'NONE', ( #48798 ), #38541, .F. ) ;
#32562=ORIENTED_EDGE ( 'NONE', *, *, #29375, .T. ) ;
#32565=ORIENTED_EDGE ( 'NONE', *, *, #656, .T. ) ;
#32567=CARTESIAN_POINT ( 'NONE',  ( 2.019183793707000074, -18.21279722757000030, 12.79944116704999857 ) ) ;
#32568=CARTESIAN_POINT ( 'NONE',  ( -10.09635500651677553, -55.27627834093888026, -7.644087038098057896 ) ) ;
#32573=B_SPLINE_CURVE_WITH_KNOTS ( 'NONE', 3,
 ( #1330, #50917, #28156, #45620, #55331, #46207, #1047, #23161, #14876, #10466 ),
 .UNSPECIFIED., .F., .F.,
 ( 4, 2, 2, 2, 4 ),
 ( 0.000000000000000000, 0.2500000000000000000, 0.5000000000000000000, 0.7500000000000000000, 1.000000000000000000 ),
 .UNSPECIFIED. ) ;
#32575=EDGE_LOOP ( 'NONE', ( #12773, #35678, #15384, #22996 ) ) ;
#32576=EDGE_LOOP ( 'NONE', ( #28139, #5668, #2712, #6887 ) ) ;
#32582=CARTESIAN_POINT ( 'NONE',  ( 8.130811096541000538, -24.68523690389000080, 9.546858433121998999 ) ) ;
#32583=CARTESIAN_POINT ( 'NONE',  ( -10.35747145892000098, -23.31584731985000047, 7.626500777234999973 ) ) ;
#32584=CARTESIAN_POINT ( 'NONE',  ( 5.622921568558999716, -77.75781628945000534, 11.67242091225999978 ) ) ;
#32589=CARTESIAN_POINT ( 'NONE',  ( -9.022574137301845099, -76.64453523234787724, 7.529641841958728321 ) ) ;
#32598=CARTESIAN_POINT ( 'NONE',  ( 0.000000000000000000, -32.88214388149999934, 0.000000000000000000 ) ) ;
#32600=CARTESIAN_POINT ( 'NONE',  ( -2.809159726167000048, -3.410933523454000138, -2.568020482856000264 ) ) ;
#32602=EDGE_CURVE ( 'NONE', #39052, #43853, #35236, .T. ) ;
#32604=CARTESIAN_POINT ( 'NONE',  ( -8.782705133629537642, -78.85833333333333428, -7.901937437515731411 ) ) ;
#32605=CARTESIAN_POINT ( 'NONE',  ( 0.5847500590554981503, -18.69344856180424941, -10.98448857562232028 ) ) ;
#32608=DIRECTION ( 'NONE',  ( 1.000000000000000000, 0.000000000000000000, 0.000000000000000000 ) ) ;
#32610=DIRECTION ( 'NONE',  ( 0.000000000000000000, 1.000000000000000000, 0.000000000000000000 ) ) ;
#32611=LINE ( 'NONE', #36763, #13677 ) ;
#32619=DIRECTION ( 'NONE',  ( 0.000000000000000000, 1.000000000000000000, 0.000000000000000000 ) ) ;
#32626=DIRECTION ( 'NONE',  ( 0.000000000000000000, -1.000000000000000000, 0.000000000000000000 ) ) ;
#32630=ADVANCED_FACE ( 'NONE', ( #9442 ), #22723, .F. ) ;
#32631=VERTEX_POINT ( 'NONE', #18009 ) ;
#32632=TOROIDAL_SURFACE ( 'NONE', #8127, 17.50000000000000000, 5.000000000000000000 ) ;
#32633=ORIENTED_EDGE ( 'NONE', *, *, #7027, .F. ) ;
#32636=AXIS2_PLACEMENT_3D ( 'NONE', #11565, #48167, #25125 ) ;
#32638=CARTESIAN_POINT ( 'NONE',  ( 11.79999999999999893, -18.84999999999000053, -0.5999999999999999778 ) ) ;
#32641=AXIS2_PLACEMENT_3D ( 'NONE', #13360, #36387, #48812 ) ;
#32649=CARTESIAN_POINT ( 'NONE',  ( -9.546819346421999697, -24.68527546640000025, 8.130850183241999929 ) ) ;
#32651=ADVANCED_FACE ( 'NONE', ( #45468 ), #36298, .F. ) ;
#32653=CARTESIAN_POINT ( 'NONE',  ( -7.654537165450999936, -55.51943464808999806, -10.01332852686999964 ) ) ;
#32655=CARTESIAN_POINT ( 'NONE',  ( 4.774437967263952309, -76.54142007752965071, 10.73626118653558947 ) ) ;
#32656=CARTESIAN_POINT ( 'NONE',  ( -0.1577469407028221082, -23.75042584457683148, -11.00002392222777381 ) ) ;
#32657=DIRECTION ( 'NONE',  ( -0.9999999999995751176, 0.000000000000000000, -9.217549095371770968E-07 ) ) ;
#32666=EDGE_CURVE ( 'NONE', #37266, #30862, #4427, .T. ) ;
#32667=CARTESIAN_POINT ( 'NONE',  ( -9.830801209645999350, -60.89088557979000171, -7.765011064359000237 ) ) ;
#32670=CARTESIAN_POINT ( 'NONE',  ( 14.00000000000000000, -69.46217755556000384, 5.544640311636000234E-06 ) ) ;
#32671=CARTESIAN_POINT ( 'NONE',  ( 3.346724862759000274, -2.316915364169000124, 0.9739846248380000793 ) ) ;
#32675=DIRECTION ( 'NONE',  ( -0.7071067811865475727, 0.000000000000000000, -0.7071067811865475727 ) ) ;
#32676=DIRECTION ( 'NONE',  ( 0.000000000000000000, -1.000000000000000000, 0.000000000000000000 ) ) ;
#32678=CARTESIAN_POINT ( 'NONE',  ( -8.570684284043998957, -76.19351098207999939, 8.487147852098999579 ) ) ;
#32683=B_SPLINE_CURVE_WITH_KNOTS ( 'NONE', 3,
 ( #53496, #49073, #8623, #4199, #8920, #58218 ),
 .UNSPECIFIED., .F., .F.,
 ( 4, 2, 4 ),
 ( 0.000000000000000000, 0.5000000000000000000, 1.000000000000000000 ),
 .UNSPECIFIED. ) ;
#32685=VECTOR ( 'NONE', #418, 1000.000000000000000 ) ;
#32687=CARTESIAN_POINT ( 'NONE',  ( 8.121706841766027196, -53.96372996663640009, 9.841114038326725932 ) ) ;
#32691=AXIS2_PLACEMENT_3D ( 'NONE', #33793, #30523, #52687 ) ;
#32696=CARTESIAN_POINT ( 'NONE',  ( -3.237754142234346322, -0.9583333333332144655, 0.6872744716274413745 ) ) ;
#32699=CARTESIAN_POINT ( 'NONE',  ( 1.081559480311999888, -3.500000000000000000, -3.328697807033000000 ) ) ;
#32700=ORIENTED_EDGE ( 'NONE', *, *, #1866, .T. ) ;
#32701=DIRECTION ( 'NONE',  ( -1.000000000000000000, 0.000000000000000000, 0.000000000000000000 ) ) ;
#32702=LINE ( 'NONE', #50750, #22760 ) ;
#32705=CARTESIAN_POINT ( 'NONE',  ( 7.635939347835848601, -60.57525282293972424, -10.36595956260653217 ) ) ;
#32706=ORIENTED_EDGE ( 'NONE', *, *, #55969, .T. ) ;
#32710=ORIENTED_EDGE ( 'NONE', *, *, #4344, .F. ) ;
#32711=CARTESIAN_POINT ( 'NONE',  ( 12.48375942314000042, -55.42730665069999674, 1.669542353228000042 ) ) ;
#32714=CARTESIAN_POINT ( 'NONE',  ( -12.66232158686000098, -25.13482640580999927, -0.5080765942055999185 ) ) ;
#32716=ADVANCED_FACE ( 'NONE', ( #54889 ), #6392, .T. ) ;
#32718=LINE ( 'NONE', #10315, #19511 ) ;
#32721=AXIS2_PLACEMENT_3D ( 'NONE', #27359, #4348, #40955 ) ;
#32724=ORIENTED_EDGE ( 'NONE', *, *, #54272, .F. ) ;
#32725=CARTESIAN_POINT ( 'NONE',  ( 6.153863461931999623, -76.14932493800000657, -10.66140155521000032 ) ) ;
#32728=CARTESIAN_POINT ( 'NONE',  ( -0.7965256724932753274, -1.956068631034633798, -3.427793819624585403 ) ) ;
#32729=CARTESIAN_POINT ( 'NONE',  ( 12.60413670420000010, -18.69283319134000010, 1.799502287691000069 ) ) ;
#32730=VECTOR ( 'NONE', #8904, 1000.000000000000114 ) ;
#32731=CARTESIAN_POINT ( 'NONE',  ( 0.4482635754052999855, -78.61057602857999882, -12.25553529036999834 ) ) ;
#32736=CARTESIAN_POINT ( 'NONE',  ( -5.598612431920771293, -78.13655615605678406, -10.68738653231515201 ) ) ;
#32742=DIRECTION ( 'NONE',  ( 0.7071067811865474617, 0.000000000000000000, 0.7071067811865474617 ) ) ;
#32744=CARTESIAN_POINT ( 'NONE',  ( 3.481453347827000222, -2.659774131856000423, 1.293805899609000054 ) ) ;
#32748=CARTESIAN_POINT ( 'NONE',  ( -10.33041713801597972, -76.16000623662056057, 5.601055854838120851 ) ) ;
#32751=ORIENTED_EDGE ( 'NONE', *, *, #56017, .T. ) ;
#32752=CARTESIAN_POINT ( 'NONE',  ( 11.99950779401364187, -75.80399128148174270, 0.6018682196318532185 ) ) ;
#32754=CARTESIAN_POINT ( 'NONE',  ( 10.24628572959450779, -79.02087622563911395, -5.923537098732725603 ) ) ;
#32755=CARTESIAN_POINT ( 'NONE',  ( -9.396085398178614767, -76.85208333333332575, -7.220923959705254802 ) ) ;
#32759=CARTESIAN_POINT ( 'NONE',  ( 8.188285776315000319, -17.29506253989999820, -9.395726099566001466 ) ) ;
#32760=CARTESIAN_POINT ( 'NONE',  ( 7.624341764906000130, -55.53514850498000044, 10.42531124851000079 ) ) ;
#32761=ORIENTED_EDGE ( 'NONE', *, *, #27660, .F. ) ;
#32762=AXIS2_PLACEMENT_3D ( 'NONE', #27926, #1681, #19093 ) ;
#32764=CARTESIAN_POINT ( 'NONE',  ( 12.70305331333692855, -16.96853698854184245, 0.8727610012103214077 ) ) ;
#32767=CARTESIAN_POINT ( 'NONE',  ( -1.336644981821593081, -77.33686301158515164, 12.00120481110041659 ) ) ;
#32772=CARTESIAN_POINT ( 'NONE',  ( 10.98362417419999915, -23.15000000000000213, -0.5999999999999999778 ) ) ;
#32773=EDGE_CURVE ( 'NONE', #14039, #52988, #7557, .T. ) ;
#32778=ORIENTED_EDGE ( 'NONE', *, *, #1233, .T. ) ;
#32779=ORIENTED_EDGE ( 'NONE', *, *, #8159, .T. ) ;
#32782=ORIENTED_EDGE ( 'NONE', *, *, #19684, .T. ) ;
#32786=CARTESIAN_POINT ( 'NONE',  ( 8.478749451788999636, -61.67812788887000153, 9.108222796200001525 ) ) ;
#32790=ORIENTED_EDGE ( 'NONE', *, *, #22137, .F. ) ;
#32791=CARTESIAN_POINT ( 'NONE',  ( 1.568318300085000120E-14, -0.05000000003700048185, -12.84999999995999964 ) ) ;
#32797=DIRECTION ( 'NONE',  ( 0.7071067811865475727, 0.000000000000000000, -0.7071067811865475727 ) ) ;
#32798=CARTESIAN_POINT ( 'NONE',  ( -12.00000000000000000, -23.15000000000000213, 0.000000000000000000 ) ) ;
#32801=AXIS2_PLACEMENT_3D ( 'NONE', #19122, #22965, #50723 ) ;
#32805=CARTESIAN_POINT ( 'NONE',  ( -7.761030428335000231, -24.08151201375000028, -9.835168816226998345 ) ) ;
#32806=CARTESIAN_POINT ( 'NONE',  ( 12.49306764019000049, -60.08056535122999975, -1.667917367065999912 ) ) ;
#32817=CARTESIAN_POINT ( 'NONE',  ( 2.800339161470473570, -2.948150801642311691, -2.132651805043404902 ) ) ;
#32820=B_SPLINE_CURVE_WITH_KNOTS ( 'NONE', 3,
 ( #16024, #42896, #24593, #7161, #30157, #2742, #42607, #2170, #20171, #38159 ),
 .UNSPECIFIED., .F., .F.,
 ( 4, 2, 2, 2, 4 ),
 ( 0.3750002296912270938, 0.5312501722684203065, 0.6875001148456134636, 0.8437500574228067318, 1.000000000000000000 ),
 .UNSPECIFIED. ) ;
#32825=ORIENTED_EDGE ( 'NONE', *, *, #57618, .F. ) ;
#32826=CARTESIAN_POINT ( 'NONE',  ( -1.798336774605999944, -59.99644498018999883, -12.61277771568000006 ) ) ;
#32837=CARTESIAN_POINT ( 'NONE',  ( 10.36289663187000087, -55.59893657650000165, -7.633501051906999457 ) ) ;
#32845=CARTESIAN_POINT ( 'NONE',  ( -1.980584515756000030, -23.26485150094000076, -12.76303204340999997 ) ) ;
#32846=VECTOR ( 'NONE', #51931, 1000.000000000000000 ) ;
#32848=ORIENTED_EDGE ( 'NONE', *, *, #39847, .F. ) ;
#32855=ORIENTED_EDGE ( 'NONE', *, *, #4587, .F. ) ;
#32857=ADVANCED_FACE ( 'NONE', ( #10263 ), #33331, .F. ) ;
#32859=LINE ( 'NONE', #42625, #42417 ) ;
#32865=LINE ( 'NONE', #18446, #50827 ) ;
#32867=B_SPLINE_CURVE_WITH_KNOTS ( 'NONE', 3,
 ( #43178, #42887, #2159, #21015, #20160, #15719 ),
 .UNSPECIFIED., .F., .F.,
 ( 4, 1, 1, 4 ),
 ( 0.000000000000000000, 0.3333333333333000081, 0.6666666666667000474, 1.000000000000000000 ),
 .UNSPECIFIED. ) ;
#32868=EDGE_LOOP ( 'NONE', ( #2187, #57593, #54066, #8853 ) ) ;
#32870=DIRECTION ( 'NONE',  ( -0.7071067811864970576, 3.544461080512985563E-08, 0.7071067811865970887 ) ) ;
#32872=B_SPLINE_CURVE_WITH_KNOTS ( 'NONE', 3,
 ( #17459, #35447, #58198, #17761, #13020, #31018 ),
 .UNSPECIFIED., .F., .F.,
 ( 4, 2, 4 ),
 ( 0.000000000000000000, 0.5000000000000000000, 1.000000000000000000 ),
 .UNSPECIFIED. ) ;
#32873=CARTESIAN_POINT ( 'NONE',  ( 0.6484536762478674277, -61.92402982684195933, -12.70397497895977601 ) ) ;
#32875=DIRECTION ( 'NONE',  ( 0.000000000000000000, 1.000000000000000000, 0.000000000000000000 ) ) ;
#32879=DIRECTION ( 'NONE',  ( 0.7071067811865475727, 0.000000000000000000, 0.7071067811865475727 ) ) ;
#32880=CARTESIAN_POINT ( 'NONE',  ( 0.05508875196996424611, -76.57451616085182877, 11.74980235316340682 ) ) ;
#32883=VECTOR ( 'NONE', #45613, 999.9999999999998863 ) ;
#32891=DIRECTION ( 'NONE',  ( 0.000000000000000000, 1.000000000000000000, 0.000000000000000000 ) ) ;
#32892=CARTESIAN_POINT ( 'NONE',  ( 2.534829140202000008, -2.169001425904999891, 2.839140403360000509 ) ) ;
#32894=EDGE_LOOP ( 'NONE', ( #20548, #23574, #50028, #19591, #2767, #45164 ) ) ;
#32895=CARTESIAN_POINT ( 'NONE',  ( -7.901937437514109597, -78.86666666666667425, -8.782705133630996031 ) ) ;
#32898=CARTESIAN_POINT ( 'NONE',  ( 12.54673349189000042, -61.62806887777999520, -0.9076721992841999542 ) ) ;
#32901=CARTESIAN_POINT ( 'NONE',  ( 11.85869973992999959, -77.73177122362999114, 5.358216250391999225 ) ) ;
#32904=DIRECTION ( 'NONE',  ( -0.7071067811865474617, -3.445410891336226740E-11, -0.7071067811865474617 ) ) ;
#32905=DIRECTION ( 'NONE',  ( 0.000000000000000000, 1.000000000000000000, 0.000000000000000000 ) ) ;
#32908=DIRECTION ( 'NONE',  ( 0.000000000000000000, 0.000000000000000000, 1.000000000000000000 ) ) ;
#32910=CARTESIAN_POINT ( 'NONE',  ( -3.453171399369999950, -1.763032031398999999, -0.5706200895263999762 ) ) ;
#32916=ORIENTED_CLOSED_SHELL ( 'NONE', *, #50346, .F. );
#32918=ORIENTED_EDGE ( 'NONE', *, *, #39325, .F. ) ;
#32920=DIRECTION ( 'NONE',  ( -0.9999999923520045408, 0.000000000000000000, -0.0001236769620559006555 ) ) ;
#32921=DIRECTION ( 'NONE',  ( 0.7071067811865969777, -0.7071067811864980568, -1.459345738583993741E-08 ) ) ;
#32922=ORIENTED_EDGE ( 'NONE', *, *, #54959, .F. ) ;
#32926=EDGE_LOOP ( 'NONE', ( #36914, #4031, #26906, #23618, #39600 ) ) ;
#32927=EDGE_CURVE ( 'NONE', #57120, #34348, #19343, .T. ) ;
#32929=AXIS2_PLACEMENT_3D ( 'NONE', #9320, #53310, #48891 ) ;
#32933=DIRECTION ( 'NONE',  ( -3.957428551341999799E-14, -1.534448722697999916E-11, 1.000000000000000000 ) ) ;
#32935=CARTESIAN_POINT ( 'NONE',  ( -9.298479816475882842, -53.91187382742327827, -8.385858173807932303 ) ) ;
#32938=CARTESIAN_POINT ( 'NONE',  ( 1.232226823824853712, -17.47709088732368343, 12.50408896749734566 ) ) ;
#32940=AXIS2_PLACEMENT_3D ( 'NONE', #34650, #12232, #39389 ) ;
#32941=B_SPLINE_CURVE_WITH_KNOTS ( 'NONE', 3,
 ( #31565, #49614, #18016, #40, #26852, #8273, #40449, #57865, #13574, #30977 ),
 .UNSPECIFIED., .F., .F.,
 ( 4, 2, 2, 2, 4 ),
 ( 0.000000000000000000, 0.2500000000000000000, 0.5000000000000000000, 0.7500000000000000000, 1.000000000000000000 ),
 .UNSPECIFIED. ) ;
#32943=DIRECTION ( 'NONE',  ( 0.7071067812863980340, 6.386292029988980325E-09, 0.7071067810866970005 ) ) ;
#32947=CARTESIAN_POINT ( 'NONE',  ( -10.26699006316255591, -77.25833333333333997, 5.917523019358029934 ) ) ;
#32948=CARTESIAN_POINT ( 'NONE',  ( -7.612971540256999958, -55.47547726255000100, -10.53003236230999917 ) ) ;
#32950=CARTESIAN_POINT ( 'NONE',  ( 6.529670873989093849, -76.52793616002254851, 9.768490878051002468 ) ) ;
#32951=CARTESIAN_POINT ( 'NONE',  ( 0.3135214471715045415, -23.68581381184938195, -10.99610567419499318 ) ) ;
#32955=CARTESIAN_POINT ( 'NONE',  ( -1.103931350765845476, -61.42083747905900282, -12.50298439261660199 ) ) ;
#32963=CARTESIAN_POINT ( 'NONE',  ( -8.485281374238999419, -59.94999999967000548, -8.485281374238999419 ) ) ;
#32964=CARTESIAN_POINT ( 'NONE',  ( 12.56594317989000054, -23.24999999414999863, 1.750000000001000089 ) ) ;
#32965=EDGE_CURVE ( 'NONE', #26186, #36137, #34408, .T. ) ;
#32966=CARTESIAN_POINT ( 'NONE',  ( 12.70305380112397309, -25.03154493769342182, -0.8725910145142433683 ) ) ;
#32967=CARTESIAN_POINT ( 'NONE',  ( -2.015551294784000191, -23.80347704843999779, -12.79857978895000059 ) ) ;
#32968=CYLINDRICAL_SURFACE ( 'NONE', #24838, 1.750000000000001332 ) ;
#32970=ADVANCED_FACE ( 'NONE', ( #36650 ), #42263, .F. ) ;
#32971=CARTESIAN_POINT ( 'NONE',  ( -7.792426477851446265, -24.29102098708791857, -10.18245125506949300 ) ) ;
#32973=CARTESIAN_POINT ( 'NONE',  ( -0.8804656548073503952, -25.02803394707816054, -12.70299681151469606 ) ) ;
#32974=CARTESIAN_POINT ( 'NONE',  ( 3.706103181433999971, -75.90547385439001005, -11.47841872256999984 ) ) ;
#32975=ORIENTED_EDGE ( 'NONE', *, *, #12591, .T. ) ;
#32979=CARTESIAN_POINT ( 'NONE',  ( 14.00000000000000000, -72.70000000000000284, 0.000000000000000000 ) ) ;
#32984=DIRECTION ( 'NONE',  ( -0.7071067811865475727, 0.000000000000000000, -0.7071067811865475727 ) ) ;
#32986=VERTEX_POINT ( 'NONE', #19527 ) ;
#32987=DIRECTION ( 'NONE',  ( -1.000000000000000000, 0.000000000000000000, 0.000000000000000000 ) ) ;
#32988=VECTOR ( 'NONE', #33001, 999.9999999999998863 ) ;
#32996=ORIENTED_EDGE ( 'NONE', *, *, #40173, .F. ) ;
#32999=CARTESIAN_POINT ( 'NONE',  ( -1.799501877760999902, -18.71082434677000350, 12.60552522436000089 ) ) ;
#33001=DIRECTION ( 'NONE',  ( 0.5000000000000744960, -0.7071067811864422126, 0.5000000000000744960 ) ) ;
#33002=EDGE_CURVE ( 'NONE', #19, #47968, #10891, .T. ) ;
#33005=ORIENTED_EDGE ( 'NONE', *, *, #3630, .T. ) ;
#33010=CARTESIAN_POINT ( 'NONE',  ( -12.82230166703000052, -23.42260938006999993, -2.065916748305000272 ) ) ;
#33012=CYLINDRICAL_SURFACE ( 'NONE', #55549, 1.750000000000000000 ) ;
#33014=CARTESIAN_POINT ( 'NONE',  ( -0.8898229088992634095, -16.97675468815732103, -12.70296869045118626 ) ) ;
#33016=CARTESIAN_POINT ( 'NONE',  ( -12.70722357733599495, -17.58971352776233132, -1.610228312168085818 ) ) ;
#33019=APPLICATION_CONTEXT ( 'automotive_design' ) ;
#33021=CARTESIAN_POINT ( 'NONE',  ( 11.88049207238000093, -76.21158421993000331, -3.223263369271999856 ) ) ;
#33023=B_SPLINE_SURFACE_WITH_KNOTS ( 'NONE', 3, 3, ( 
 ( #11071, #47380, #6621, #19619 ),
 ( #20496, #50927, #28461, #47675 ),
 ( #24632, #51222, #1630, #46803 ),
 ( #6330, #7199, #24345, #6911 ),
 ( #24919, #52085, #20210, #42936 ),
 ( #2490, #38201, #56221, #15771 ),
 ( #33763, #38492, #51801, #56508 ),
 ( #34047, #52654, #7781, #3352 ),
 ( #34628, #25488, #44366, #39364 ),
 ( #8645, #48805, #35487, #21349 ),
 ( #26348, #3918, #25780, #39068 ),
 ( #3069, #7491, #16356, #21921 ),
 ( #53517, #26630, #49094, #44086 ),
 ( #43807, #39929, #39644, #12209 ),
 ( #57371, #16930, #30196, #57945 ),
 ( #11926, #57651, #34911, #30491 ),
 ( #8350, #17499, #56797, #48244 ) ),
 .UNSPECIFIED., .F., .F., .F.,
 ( 4, 1, 1, 1, 1, 1, 1, 1, 1, 1, 1, 1, 1, 1, 4 ),
 ( 4, 4 ),
 ( -0.01011398171657000057, 0.000000000000000000, 0.08333333333333001192, 0.1666666666667000196, 0.2500000000000000000, 0.3333333333333000081, 0.4166666666666999919, 0.5000000000000000000, 0.5833333333333000637, 0.6666666666667000474, 0.7500000000000000000, 0.8333333333333000637, 0.9166666666667000474, 1.000000000000000000, 1.010365777941000021 ),
 ( -0.3559705546970000078, 1.357612346708999995 ),
 .UNSPECIFIED. ) ;
#33026=CARTESIAN_POINT ( 'NONE',  ( 7.765022563386000165, -60.89093562068000409, -9.830785949133000301 ) ) ;
#33027=CARTESIAN_POINT ( 'NONE',  ( -9.042566447131001439, -79.11102013304999048, -8.284387575507999202 ) ) ;
#33029=CARTESIAN_POINT ( 'NONE',  ( -3.451066577810062874, -1.829698698065413964, -0.5702761658243397092 ) ) ;
#33030=CARTESIAN_POINT ( 'NONE',  ( 3.034193154433733941, -2.821981570262439565, -1.163058261055952558 ) ) ;
#33031=CARTESIAN_POINT ( 'NONE',  ( 11.22958103806566932, -78.26998077374973661, -4.439356378266488434 ) ) ;
#33033=VERTEX_POINT ( 'NONE', #1249 ) ;
#33035=CARTESIAN_POINT ( 'NONE',  ( -7.220923959705244144, -77.87291666666665435, -9.396085398178621872 ) ) ;
#33038=CARTESIAN_POINT ( 'NONE',  ( -3.532530677088999926, -1.827872856414999969, -1.580970727500000006 ) ) ;
#33041=CARTESIAN_POINT ( 'NONE',  ( -8.251448334410120822, -76.13695544466607146, 8.365207622121904052 ) ) ;
#33045=ORIENTED_EDGE ( 'NONE', *, *, #29377, .T. ) ;
#33046=CARTESIAN_POINT ( 'NONE',  ( 12.70259419118077915, -24.73882758529050463, 1.314635108442414602 ) ) ;
#33048=CARTESIAN_POINT ( 'NONE',  ( 0.000000000000000000, 4.040000000000000036, 0.000000000000000000 ) ) ;
#33050=DIRECTION ( 'NONE',  ( 0.000000000000000000, -1.000000000000000000, 0.000000000000000000 ) ) ;
#33054=CARTESIAN_POINT ( 'NONE',  ( 9.992014434680999813, -17.83915351714000153, -7.762970980311999725 ) ) ;
#33056=ORIENTED_EDGE ( 'NONE', *, *, #429, .T. ) ;
#33057=FACE_OUTER_BOUND ( 'NONE', #7022, .T. ) ;
#33060=EDGE_CURVE ( 'NONE', #8180, #29038, #453, .T. ) ;
#33061=CARTESIAN_POINT ( 'NONE',  ( 5.457687247930513408, -77.79051310338437020, 10.71434849429115310 ) ) ;
#33062=CARTESIAN_POINT ( 'NONE',  ( 12.50000000000000000, -17.31640971966000109, -1.003652782652999953 ) ) ;
#33066=LINE ( 'NONE', #659, #41133 ) ;
#33067=FACE_OUTER_BOUND ( 'NONE', #49286, .T. ) ;
#33068=AXIS2_PLACEMENT_3D ( 'NONE', #41528, #45982, #14360 ) ;
#33072=EDGE_CURVE ( 'NONE', #16168, #30569, #42860, .T. ) ;
#33073=CARTESIAN_POINT ( 'NONE',  ( -12.50728630775810402, -61.79975539279641339, 0.1757873579563377919 ) ) ;
#33075=ORIENTED_EDGE ( 'NONE', *, *, #53719, .F. ) ;
#33079=CARTESIAN_POINT ( 'NONE',  ( 7.762982794245000484, -17.83910040287999621, 9.991998894192999359 ) ) ;
#33080=FACE_OUTER_BOUND ( 'NONE', #47605, .T. ) ;
#33081=EDGE_CURVE ( 'NONE', #19448, #52807, #18947, .T. ) ;
#33082=CARTESIAN_POINT ( 'NONE',  ( -11.75618103724999841, -78.25732521500999894, -1.929672871034000092 ) ) ;
#33083=CARTESIAN_POINT ( 'NONE',  ( 9.310177428715999071, -61.93531023604000296, 8.596745825462999591 ) ) ;
#33088=EDGE_LOOP ( 'NONE', ( #43916, #38897, #8618, #10226 ) ) ;
#33089=CARTESIAN_POINT ( 'NONE',  ( -10.25201842917796924, -24.12180395215443696, 7.730408553586223697 ) ) ;
#33091=VERTEX_POINT ( 'NONE', #2400 ) ;
#33094=CARTESIAN_POINT ( 'NONE',  ( 0.000000000000000000, -6.100000000000000533, -13.99999999999798383 ) ) ;
#33096=CARTESIAN_POINT ( 'NONE',  ( -9.713030931998421380, -17.47705886690323140, -7.970419576809637974 ) ) ;
#33097=CARTESIAN_POINT ( 'NONE',  ( -1.316790939146709416, -2.092021354265999999, -2.998527993510658352 ) ) ;
#33099=B_SPLINE_CURVE_WITH_KNOTS ( 'NONE', 3,
 ( #28260, #1439, #54576, #9695 ),
 .UNSPECIFIED., .F., .F.,
 ( 4, 4 ),
 ( 0.000000000000000000, 1.000000000000000000 ),
 .UNSPECIFIED. ) ;
#33101=CARTESIAN_POINT ( 'NONE',  ( -8.284635637485001425, -25.04861451557999885, -9.778492910169999774 ) ) ;
#33102=CARTESIAN_POINT ( 'NONE',  ( 12.60413670423000099, -60.10716680829000325, -1.799502287691000069 ) ) ;
#33106=CIRCLE ( 'NONE', #14232, 30.49999999999999289 ) ;
#33110=EDGE_CURVE ( 'NONE', #237, #58179, #56705, .T. ) ;
#33111=CARTESIAN_POINT ( 'NONE',  ( -9.029856014872001069, -16.66737842935999936, 9.038878718683999836 ) ) ;
#33114=CARTESIAN_POINT ( 'NONE',  ( -0.3640064567607090296, -2.866730428114151685, -3.502711746507367163 ) ) ;
#33121=ORIENTED_EDGE ( 'NONE', *, *, #28961, .T. ) ;
#33123=CARTESIAN_POINT ( 'NONE',  ( -3.047436688878264466, -77.09406694292110274, 11.37773063511170157 ) ) ;
#33124=CARTESIAN_POINT ( 'NONE',  ( 1.698401934075999931, -61.02014045872000025, -12.66748707616000047 ) ) ;
#33125=CARTESIAN_POINT ( 'NONE',  ( -8.190859204290999784, -55.64999999967000122, 7.342331066867000544 ) ) ;
#33128=CARTESIAN_POINT ( 'NONE',  ( -12.80088938719999803, -19.23743348210000192, 1.980532758767000301 ) ) ;
#33131=CARTESIAN_POINT ( 'NONE',  ( -10.20679554288753010, -54.56427274255051429, -7.770327721632001250 ) ) ;
#33133=CARTESIAN_POINT ( 'NONE',  ( -7.624341766639000539, -23.26485146254000114, -10.42531125024000005 ) ) ;
#33134=CARTESIAN_POINT ( 'NONE',  ( 7.647094085174999556, -55.43104695408000282, -10.00844048069000003 ) ) ;
#33141=ORIENTED_EDGE ( 'NONE', *, *, #9213, .T. ) ;
#33143=DIRECTION ( 'NONE',  ( -0.7071067811864980568, -1.534448722697995070E-11, -0.7071067811865969777 ) ) ;
#33144=ORIENTED_EDGE ( 'NONE', *, *, #31001, .T. ) ;
#33146=ADVANCED_FACE ( 'NONE', ( #12114 ), #29241, .F. ) ;
#33149=VERTEX_POINT ( 'NONE', #25395 ) ;
#33154=VERTEX_POINT ( 'NONE', #38974 ) ;
#33156=CARTESIAN_POINT ( 'NONE',  ( 1.056237665594999875, -16.95133986302000295, 12.77256098197999989 ) ) ;
#33161=DIRECTION ( 'NONE',  ( -1.674928520677000026E-10, 1.000000000000000000, 2.004066721390000047E-09 ) ) ;
#33162=ADVANCED_FACE ( 'NONE', ( #20401 ), #7681, .F. ) ;
#33163=VERTEX_POINT ( 'NONE', #56417 ) ;
#33164=VERTEX_POINT ( 'NONE', #3264 ) ;
#33166=CARTESIAN_POINT ( 'NONE',  ( 8.343860018000999190, -55.64999999967000122, -8.343860018000999190 ) ) ;
#33168=CARTESIAN_POINT ( 'NONE',  ( -1.208267226910347603, -61.62590682120529806, -12.70228502427989881 ) ) ;
#33175=CARTESIAN_POINT ( 'NONE',  ( 9.708203932502000200, -79.25000000000000000, -7.053423027506000587 ) ) ;
#33180=LINE ( 'NONE', #25206, #20275 ) ;
#33182=CARTESIAN_POINT ( 'NONE',  ( -0.006333666751268000016, -16.66737355700000123, -12.77652491955999992 ) ) ;
#33185=LINE ( 'NONE', #20786, #2594 ) ;
#33186=CARTESIAN_POINT ( 'NONE',  ( 2.444312764923342485, -1.435907104546281898, -2.543885789726834545 ) ) ;
#33188=CARTESIAN_POINT ( 'NONE',  ( -0.5999663639301134888, -18.81035107904876469, -10.98362601162690844 ) ) ;
#33189=CARTESIAN_POINT ( 'NONE',  ( 7.216788504278100369, -77.52047868913132334, 9.394654730084591066 ) ) ;
#33193=CARTESIAN_POINT ( 'NONE',  ( 12.50679926050277047, -17.69581646371715422, -1.424414840275272542 ) ) ;
#33195=EDGE_CURVE ( 'NONE', #38791, #47867, #12663, .T. ) ;
#33196=LINE ( 'NONE', #15502, #15003 ) ;
#33198=VECTOR ( 'NONE', #24827, 1000.000000000000114 ) ;
#33202=DIRECTION ( 'NONE',  ( 0.000000000000000000, 0.000000000000000000, -1.000000000000000000 ) ) ;
#33204=CARTESIAN_POINT ( 'NONE',  ( -12.90000000000000036, -3.000000000000000000, 0.000000000000000000 ) ) ;
#33206=CARTESIAN_POINT ( 'NONE',  ( -3.500000000146000101, -0.7499999998540000101, 2.054632350152999929E-08 ) ) ;
#33208=CARTESIAN_POINT ( 'NONE',  ( -1.750000000000000000, -55.55000000209000177, 12.50000000000000000 ) ) ;
#33209=CARTESIAN_POINT ( 'NONE',  ( -7.954951288349001004, -18.75000000000000000, -9.722718241315000398 ) ) ;
#33212=EDGE_LOOP ( 'NONE', ( #12491, #42679, #54525, #50198 ) ) ;
#33213=CIRCLE ( 'NONE', #32281, 3.799999999999999822 ) ;
#33215=ADVANCED_FACE ( 'NONE', ( #39261 ), #57274, .F. ) ;
#33217=FACE_OUTER_BOUND ( 'NONE', #49150, .T. ) ;
#33219=EDGE_CURVE ( 'NONE', #52418, #29475, #20234, .T. ) ;
#33221=ORIENTED_EDGE ( 'NONE', *, *, #1068, .T. ) ;
#33223=CARTESIAN_POINT ( 'NONE',  ( 8.190859204290999784, -59.94999999967000548, 7.342331066867000544 ) ) ;
#33227=ORIENTED_EDGE ( 'NONE', *, *, #27610, .F. ) ;
#33230=VERTEX_POINT ( 'NONE', #30099 ) ;
#33231=CARTESIAN_POINT ( 'NONE',  ( 1.767510878348000247, -2.887137290291999836, 2.906076978666999988 ) ) ;
#33232=EDGE_LOOP ( 'NONE', ( #49201, #44571, #43332, #55602, #28552, #12120 ) ) ;
#33235=AXIS2_PLACEMENT_3D ( 'NONE', #13199, #53076, #43934 ) ;
#33238=CARTESIAN_POINT ( 'NONE',  ( 1.021160424422173252, -0.9687499998052564454, 3.160415270357120221 ) ) ;
#33241=CARTESIAN_POINT ( 'NONE',  ( -9.396085398178650294, -77.24791666666668277, 7.220923959705211281 ) ) ;
#33242=AXIS2_PLACEMENT_3D ( 'NONE', #26755, #40046, #35612 ) ;
#33245=CARTESIAN_POINT ( 'NONE',  ( 2.448098496330775919, -76.55784816645272883, 11.49200783961538797 ) ) ;
#33246=B_SPLINE_CURVE_WITH_KNOTS ( 'NONE', 3,
 ( #19461, #56068, #15612, #10317, #55476, #33016, #46348, #42777, #28594, #2340, #5872, #23881, #20334, #16773, #34754, #11769 ),
 .UNSPECIFIED., .F., .F.,
 ( 4, 2, 2, 2, 2, 2, 2, 4 ),
 ( 0.000000000000000000, 0.2499999999999964473, 0.3749999999999946709, 0.4374999999999952816, 0.4999999999999958922, 0.6249999999999968914, 0.7499999999999978906, 1.000000000000000000 ),
 .UNSPECIFIED. ) ;
#33248=DIRECTION ( 'NONE',  ( -0.9999999929803531362, 0.000000000000000000, -0.0001184875252605944247 ) ) ;
#33253=CIRCLE ( 'NONE', #7816, 3.249999999999999556 ) ;
#33257=CARTESIAN_POINT ( 'NONE',  ( -7.474083310498281563, -76.26977652102928573, -9.069810220831756808 ) ) ;
#33260=CARTESIAN_POINT ( 'NONE',  ( -10.19019669288000074, -59.99643762534999780, -7.646965578510999784 ) ) ;
#33261=DIRECTION ( 'NONE',  ( 0.000000000000000000, 0.000000000000000000, -1.000000000000000000 ) ) ;
#33265=CARTESIAN_POINT ( 'NONE',  ( 12.43646124688000043, -24.91751819622000141, -0.05236837568997999848 ) ) ;
#33269=CARTESIAN_POINT ( 'NONE',  ( -1.705971691335000040, -75.78238836370000797, -12.09219208115999855 ) ) ;
#33270=EDGE_LOOP ( 'NONE', ( #53285, #52422, #14064, #28433 ) ) ;
#33274=CARTESIAN_POINT ( 'NONE',  ( -4.842945234633629248, -76.29082827606781336, -10.70557031532286274 ) ) ;
#33275=CARTESIAN_POINT ( 'NONE',  ( 12.43646124691999866, -61.71751819588999410, -0.05236837569004999804 ) ) ;
#33283=ORIENTED_EDGE ( 'NONE', *, *, #51247, .T. ) ;
#33284=DIRECTION ( 'NONE',  ( 0.000000000000000000, 0.000000000000000000, -1.000000000000000000 ) ) ;
#33287=ORIENTED_EDGE ( 'NONE', *, *, #2589, .F. ) ;
#33290=CIRCLE ( 'NONE', #47492, 0.8000000000000011546 ) ;
#33291=CARTESIAN_POINT ( 'NONE',  ( 12.49168433582000226, -60.09849137196000157, 1.667916687244999974 ) ) ;
#33293=ORIENTED_EDGE ( 'NONE', *, *, #27149, .T. ) ;
#33294=ADVANCED_FACE ( 'NONE', ( #47583 ), #11830, .F. ) ;
#33299=ORIENTED_EDGE ( 'NONE', *, *, #43573, .F. ) ;
#33301=VECTOR ( 'NONE', #41138, 1000.000000000000000 ) ;
#33305=CARTESIAN_POINT ( 'NONE',  ( 12.49830607526000037, -55.59028586401999661, 1.666977523254999927 ) ) ;
#33308=ORIENTED_EDGE ( 'NONE', *, *, #35686, .F. ) ;
#33309=CARTESIAN_POINT ( 'NONE',  ( -12.55486071735000131, -24.15393633008000407, -1.580832792524999864 ) ) ;
#33310=EDGE_CURVE ( 'NONE', #3300, #3351, #28955, .T. ) ;
#33314=DIRECTION ( 'NONE',  ( -0.9999999924279686647, 0.000000000000000000, -0.0001230612157847738313 ) ) ;
#33316=CARTESIAN_POINT ( 'NONE',  ( 13.86363625866555438, -46.43897132165000130, 0.001706075946107717383 ) ) ;
#33319=CARTESIAN_POINT ( 'NONE',  ( -3.151328970204000157, -76.08706565608000005, -11.89977497056000111 ) ) ;
#33320=CARTESIAN_POINT ( 'NONE',  ( -1.419761472987663975, -2.442049273140185939, -3.284178234334656832 ) ) ;
#33321=ADVANCED_FACE ( 'NONE', ( #46997, #38685, #47863, #7392 ), #43640, .T. ) ;
#33322=CARTESIAN_POINT ( 'NONE',  ( 1.250000000000000000, -18.75000000000000000, -12.00000000000000000 ) ) ;
#33323=CARTESIAN_POINT ( 'NONE',  ( 10.82405698390000026, -79.27161254432999726, 5.765268246940999930 ) ) ;
#33327=CARTESIAN_POINT ( 'NONE',  ( 2.800996926600495041, -2.807707601517177132, -1.662906485826789016 ) ) ;
#33328=CARTESIAN_POINT ( 'NONE',  ( 12.01270605470693731, -77.80744209907201991, 1.121883719411586267 ) ) ;
#33329=CARTESIAN_POINT ( 'NONE',  ( -12.49999990534960226, -13.07071424677999971, -0.001538265197309672755 ) ) ;
#33331=B_SPLINE_SURFACE_WITH_KNOTS ( 'NONE', 3, 3, ( 
 ( #50722, #46592, #5822, #23254 ),
 ( #23829, #28243, #4957, #27954 ),
 ( #18832, #14099, #18542, #1424 ),
 ( #32967, #22963, #54558, #36824 ),
 ( #46296, #54839, #14382, #41846 ),
 ( #19413, #37403, #55424, #32382 ),
 ( #50426, #40583, #58296, #31408 ),
 ( #49747, #27279, #57703, #31106 ),
 ( #53279, #54163, #22269, #45315 ),
 ( #12825, #54461, #44419, #13997 ),
 ( #22864, #44719, #31995, #35248 ),
 ( #8401, #49451, #57998, #50036 ),
 ( #9583, #30825, #53575, #26983 ),
 ( #21973, #4273, #53876, #26398 ),
 ( #35546, #40285, #40873, #13705 ),
 ( #27567, #4865, #45611, #45017 ),
 ( #180, #4571, #31700, #22571 ) ),
 .UNSPECIFIED., .F., .F., .F.,
 ( 4, 1, 1, 1, 1, 1, 1, 1, 1, 1, 1, 1, 1, 1, 4 ),
 ( 4, 4 ),
 ( -0.01011408452870000106, 0.000000000000000000, 0.08333333333333001192, 0.1666666666667000196, 0.2500000000000000000, 0.3333333333333000081, 0.4166666666666999919, 0.5000000000000000000, 0.5833333333333000637, 0.6666666666667000474, 0.7500000000000000000, 0.8333333333333000637, 0.9166666666667000474, 1.000000000000000000, 1.010362559107000013 ),
 ( -0.3559705546267999954, 1.357612419602000076 ),
 .UNSPECIFIED. ) ;
#33337=CARTESIAN_POINT ( 'NONE',  ( -1.309998969828999993, -2.891902036004999843, -3.642009152241000081 ) ) ;
#33338=EDGE_CURVE ( 'NONE', #43980, #54533, #25859, .T. ) ;
#33339=VECTOR ( 'NONE', #49917, 1000.000000000000000 ) ;
#33342=CARTESIAN_POINT ( 'NONE',  ( -9.525237058298714032, -76.14974714360452879, 6.880006712239788769 ) ) ;
#33346=ORIENTED_EDGE ( 'NONE', *, *, #39681, .F. ) ;
#33347=EDGE_CURVE ( 'NONE', #24905, #22759, #54152, .T. ) ;
#33350=CARTESIAN_POINT ( 'NONE',  ( 3.075537641221555596, -76.94583333333332575, -11.44417895085270587 ) ) ;
#33351=CARTESIAN_POINT ( 'NONE',  ( -9.038948602551000633, -62.13262223832000331, 9.029786144045999663 ) ) ;
#33353=CARTESIAN_POINT ( 'NONE',  ( -8.909545442949999838, -59.94999999967000548, -8.061017305527000687 ) ) ;
#33355=CARTESIAN_POINT ( 'NONE',  ( 10.07615509326000058, -17.27367739700000016, -7.986954869189998973 ) ) ;
#33356=CARTESIAN_POINT ( 'NONE',  ( 13.13047446164998711, -56.01421830981000483, 0.8260994316375004365 ) ) ;
#33359=DIRECTION ( 'NONE',  ( 0.7071067811865475727, 0.000000000000000000, -0.7071067811865475727 ) ) ;
#33361=CARTESIAN_POINT ( 'NONE',  ( -2.677643855409316043, -77.34575811142462953, 11.78110567705964762 ) ) ;
#33362=LINE ( 'NONE', #51691, #7249 ) ;
#33363=B_SPLINE_CURVE_WITH_KNOTS ( 'NONE', 3,
 ( #47966, #44096, #39080, #48529, #30207, #37401, #55421, #32964 ),
 .UNSPECIFIED., .F., .F.,
 ( 4, 2, 2, 4 ),
 ( 0.000000000000000000, 0.4999999999999998890, 0.7499999999999998890, 1.000000000000000000 ),
 .UNSPECIFIED. ) ;
#33365=DIRECTION ( 'NONE',  ( 0.000000000000000000, 1.000000000000000000, 0.000000000000000000 ) ) ;
#33366=CARTESIAN_POINT ( 'NONE',  ( 1.799490225533999732, -59.57152778012000027, -12.64500484464999808 ) ) ;
#33369=CARTESIAN_POINT ( 'NONE',  ( -12.82904091336000008, -55.47547470607999998, 2.062673488738000049 ) ) ;
#33373=ORIENTED_EDGE ( 'NONE', *, *, #3399, .F. ) ;
#33378=ORIENTED_EDGE ( 'NONE', *, *, #56263, .T. ) ;
#33379=CARTESIAN_POINT ( 'NONE',  ( 7.760941378066999796, -17.76914109191999813, 10.15321372496999963 ) ) ;
#33381=CARTESIAN_POINT ( 'NONE',  ( 4.614376373661000841, -78.40102880538998420, -10.98357556630999987 ) ) ;
#33382=PLANE ( 'NONE',  #18375 ) ;
#33387=CARTESIAN_POINT ( 'NONE',  ( 4.112279070415571169, -78.14664095760667806, 11.05398264717377188 ) ) ;
#33390=CARTESIAN_POINT ( 'NONE',  ( -17.50000000000000000, -21.00000000000000000, 0.000000000000000000 ) ) ;
#33394=EDGE_CURVE ( 'NONE', #12948, #11806, #41529, .T. ) ;
#33398=EDGE_CURVE ( 'NONE', #41458, #43521, #4481, .T. ) ;
#33401=CARTESIAN_POINT ( 'NONE',  ( -7.648026768036999989, -60.04999998387000204, -10.12290050219000115 ) ) ;
#33403=EDGE_LOOP ( 'NONE', ( #39641, #53396, #19976, #32825, #40197 ) ) ;
#33408=CARTESIAN_POINT ( 'NONE',  ( -9.502921958796708424, -54.05907999824894716, 8.179400290910178839 ) ) ;
#33410=CARTESIAN_POINT ( 'NONE',  ( 3.164729434338774183, -3.463813167320636932, -1.543632381241692109 ) ) ;
#33413=FACE_OUTER_BOUND ( 'NONE', #54303, .T. ) ;
#33418=EDGE_CURVE ( 'NONE', #1462, #33666, #26941, .T. ) ;
#33420=CIRCLE ( 'NONE', #43846, 1.750000000000001332 ) ;
#33421=CARTESIAN_POINT ( 'NONE',  ( 1.056237665594999875, -61.84866013665000395, -12.77256098201999990 ) ) ;
#33422=CARTESIAN_POINT ( 'NONE',  ( -7.429974109827198525, -55.28385402668402548, 8.111636311575601610 ) ) ;
#33425=CARTESIAN_POINT ( 'NONE',  ( 7.636246406686000299, -23.76323123101999713, -10.30460653225000023 ) ) ;
#33427=CARTESIAN_POINT ( 'NONE',  ( -9.713032445802920023, -61.32293762623282163, 7.970418356084342904 ) ) ;
#33428=CARTESIAN_POINT ( 'NONE',  ( 9.716210726936424180, -78.49548457799500056, 6.605226190989496260 ) ) ;
#33430=EDGE_LOOP ( 'NONE', ( #44789, #55060, #43198, #27847 ) ) ;
#33433=CARTESIAN_POINT ( 'NONE',  ( 7.753900686106000251, -54.51068035512000165, -10.31980286347000053 ) ) ;
#33435=B_SPLINE_CURVE_WITH_KNOTS ( 'NONE', 3,
 ( #47008, #33096, #14515, #28671, #5374, #55255, #6538, #19537 ),
 .UNSPECIFIED., .F., .F.,
 ( 4, 2, 2, 4 ),
 ( 0.000000000000000000, 0.4999999999999977796, 0.7499999999999988898, 1.000000000000000000 ),
 .UNSPECIFIED. ) ;
#33443=ORIENTED_EDGE ( 'NONE', *, *, #5295, .F. ) ;
#33446=DIRECTION ( 'NONE',  ( 0.7071067811864980568, -0.7071067811865969777, -4.786443936370980024E-09 ) ) ;
#33454=CARTESIAN_POINT ( 'NONE',  ( 1.669724228656999987, -18.63102323466000243, 12.48434610067999984 ) ) ;
#33458=AXIS2_PLACEMENT_3D ( 'NONE', #2495, #37331, #37913 ) ;
#33461=EDGE_LOOP ( 'NONE', ( #52072, #19736, #6304, #39168 ) ) ;
#33462=ORIENTED_EDGE ( 'NONE', *, *, #2676, .T. ) ;
#33468=CARTESIAN_POINT ( 'NONE',  ( 0.000000000000000000, 4.040000000000000036, 0.000000000000000000 ) ) ;
#33469=DIRECTION ( 'NONE',  ( 0.000000000000000000, 0.000000000000000000, -1.000000000000000000 ) ) ;
#33472=CARTESIAN_POINT ( 'NONE',  ( -8.307389487175075971, -76.63738348406045020, 8.309511392601589108 ) ) ;
#33476=FACE_OUTER_BOUND ( 'NONE', #7780, .T. ) ;
#33477=CARTESIAN_POINT ( 'NONE',  ( 1.667936697358999965, -19.23537109840999904, -12.53241208775999915 ) ) ;
#33478=CARTESIAN_POINT ( 'NONE',  ( -7.919595949288999570, -57.79999999967000690, -8.909545442949999838 ) ) ;
#33479=CARTESIAN_POINT ( 'NONE',  ( 1.382886570147999983, -17.36901780168000187, -12.65982054476000052 ) ) ;
#33480=CARTESIAN_POINT ( 'NONE',  ( 1.980584515752000119, -23.26485146623999967, -12.76303204602000108 ) ) ;
#33483=CARTESIAN_POINT ( 'NONE',  ( 0.3644735108981210225, -1.383145019569959056, -3.562971877919846264 ) ) ;
#33486=ADVANCED_FACE ( 'NONE', ( #24402 ), #42820, .F. ) ;
#33487=DIRECTION ( 'NONE',  ( 0.7071067811865475727, 0.000000000000000000, -0.7071067811865475727 ) ) ;
#33488=CARTESIAN_POINT ( 'NONE',  ( -1.929975092519000013, -55.59892743702999240, 12.72537404207999856 ) ) ;
#33492=TOROIDAL_SURFACE ( 'NONE', #6150, 1.250000000000000000, 0.5000000000000000000 ) ;
#33494=CARTESIAN_POINT ( 'NONE',  ( -12.77651047528000028, -53.49104280904999342, -0.04320343284637000181 ) ) ;
#33495=CARTESIAN_POINT ( 'NONE',  ( -9.050966799188000067, -55.64999999964999233, -7.919595949288999570 ) ) ;
#33501=EDGE_CURVE ( 'NONE', #53336, #44757, #30259, .T. ) ;
#33506=DIRECTION ( 'NONE',  ( -0.9859154929577472748, 0.1672442547470080754, 0.000000000000000000 ) ) ;
#33510=LINE ( 'NONE', #14629, #27717 ) ;
#33512=CARTESIAN_POINT ( 'NONE',  ( -1.818468715484000065E-14, -79.29999999999999716, -12.04999999999996874 ) ) ;
#33514=ORIENTED_EDGE ( 'NONE', *, *, #30211, .F. ) ;
#33518=ORIENTED_EDGE ( 'NONE', *, *, #32479, .F. ) ;
#33520=ADVANCED_FACE ( 'NONE', ( #20555 ), #52145, .T. ) ;
#33521=VERTEX_POINT ( 'NONE', #52430 ) ;
#33523=ORIENTED_EDGE ( 'NONE', *, *, #30754, .F. ) ;
#33526=AXIS2_PLACEMENT_3D ( 'NONE', #43662, #44819, #34776 ) ;
#33527=VERTEX_POINT ( 'NONE', #3134 ) ;
#33528=CARTESIAN_POINT ( 'NONE',  ( -10.45205659047999980, -59.56232685193999998, -7.651160337235999975 ) ) ;
#33529=FACE_OUTER_BOUND ( 'NONE', #39974, .T. ) ;
#33530=VERTEX_POINT ( 'NONE', #21124 ) ;
#33536=CARTESIAN_POINT ( 'NONE',  ( 3.335937506701805777, -0.9140624994645799584, 0.5252349859688600908 ) ) ;
#33543=CARTESIAN_POINT ( 'NONE',  ( 8.138070855479238475, -76.51354002294402790, 8.478431565815370163 ) ) ;
#33546=CARTESIAN_POINT ( 'NONE',  ( -2.373398577992831271, -3.040439981628704214, 2.220387636506996554 ) ) ;
#33552=CARTESIAN_POINT ( 'NONE',  ( -2.098469896607999926E-14, 0.000000000000000000, 0.000000000000000000 ) ) ;
#33554=CARTESIAN_POINT ( 'NONE',  ( 10.07722254365999959, -21.74800977511999989, 7.718368845776000242 ) ) ;
#33555=DIRECTION ( 'NONE',  ( 0.7071067811865474617, 0.000000000000000000, 0.7071067811865474617 ) ) ;
#33556=ADVANCED_FACE ( 'NONE', ( #56858 ), #57889, .F. ) ;
#33557=CARTESIAN_POINT ( 'NONE',  ( 10.01235002625000092, -60.09848884406000025, 7.653559626114000203 ) ) ;
#33564=CARTESIAN_POINT ( 'NONE',  ( 9.938819120173999266, -76.55355739169999651, 6.834338467449999399 ) ) ;
#33571=CARTESIAN_POINT ( 'NONE',  ( 10.25203062048420399, -54.67822876341044491, 7.730397977249435115 ) ) ;
#33573=DIRECTION ( 'NONE',  ( 0.000000000000000000, 1.000000000000000000, 0.000000000000000000 ) ) ;
#33576=DIRECTION ( 'NONE',  ( 1.000000000000000000, 0.000000000000000000, 0.000000000000000000 ) ) ;
#33579=VECTOR ( 'NONE', #21209, 999.9999999999998863 ) ;
#33581=CARTESIAN_POINT ( 'NONE',  ( 1.250000000000000000, -23.25000000000000000, 12.00000000000000000 ) ) ;
#33585=CARTESIAN_POINT ( 'NONE',  ( 0.000000000000000000, 4.040000000000000036, 0.000000000000000000 ) ) ;
#33588=ORIENTED_EDGE ( 'NONE', *, *, #33712, .F. ) ;
#33598=CARTESIAN_POINT ( 'NONE',  ( -12.70610460582424750, -24.45512899796313633, -1.580683094053911830 ) ) ;
#33600=ORIENTED_EDGE ( 'NONE', *, *, #29794, .T. ) ;
#33601=CARTESIAN_POINT ( 'NONE',  ( -12.43571054526000097, -24.87980566418999828, -0.4385525234354999968 ) ) ;
#33604=CARTESIAN_POINT ( 'NONE',  ( 1.250000000000000000, -55.54999999966999980, 12.00000000000000000 ) ) ;
#33605=CARTESIAN_POINT ( 'NONE',  ( -8.485281374238999419, -55.54999999966999980, 8.485281374238999419 ) ) ;
#33610=B_SPLINE_CURVE_WITH_KNOTS ( 'NONE', 3,
 ( #55653, #19637, #41782, #5759, #15202, #14319 ),
 .UNSPECIFIED., .F., .F.,
 ( 4, 1, 1, 4 ),
 ( 0.000000000000000000, 0.3333333333333000081, 0.6666666666667000474, 1.000000000000000000 ),
 .UNSPECIFIED. ) ;
#33611=CARTESIAN_POINT ( 'NONE',  ( 11.05577208806000122, -76.66461526165998919, -4.921212746988999243 ) ) ;
#33615=CARTESIAN_POINT ( 'NONE',  ( 10.82405698390000026, -79.23694587766000552, 5.765268246940999930 ) ) ;
#33617=DIRECTION ( 'NONE',  ( 0.000000000000000000, -1.000000000000000000, 0.000000000000000000 ) ) ;
#33618=CARTESIAN_POINT ( 'NONE',  ( -12.01171088695212852, -78.04760641092620688, 0.3579334955698593168 ) ) ;
#33625=DIRECTION ( 'NONE',  ( 0.000000000000000000, -1.000000000000000000, 0.000000000000000000 ) ) ;
#33628=CARTESIAN_POINT ( 'NONE',  ( -3.690989959373000229, -2.872579967774000487, 0.4135749490274999718 ) ) ;
#33631=CARTESIAN_POINT ( 'NONE',  ( -11.39055364300875262, -76.18003226433557984, 2.885907805895131961 ) ) ;
#33632=CARTESIAN_POINT ( 'NONE',  ( 10.18499221077999906, -20.25022860214999909, -7.710118476625000383 ) ) ;
#33636=DIRECTION ( 'NONE',  ( 0.000000000000000000, -1.000000000000000000, 0.000000000000000000 ) ) ;
#33640=CARTESIAN_POINT ( 'NONE',  ( -7.619389973917000347, -60.20786254198000620, 10.35398617735999949 ) ) ;
#33644=LINE ( 'NONE', #51684, #375 ) ;
#33645=CARTESIAN_POINT ( 'NONE',  ( -12.70455814331304190, -54.23992875941976877, -1.489882837218519773 ) ) ;
#33646=ORIENTED_EDGE ( 'NONE', *, *, #19243, .T. ) ;
#33648=CARTESIAN_POINT ( 'NONE',  ( 7.648026766735999793, -23.25000000582000226, -10.12290050089000104 ) ) ;
#33655=CIRCLE ( 'NONE', #38379, 3.799999999999999822 ) ;
#33657=FACE_BOUND ( 'NONE', #40721, .T. ) ;
#33661=VECTOR ( 'NONE', #51579, 1000.000000000000000 ) ;
#33666=VERTEX_POINT ( 'NONE', #8129 ) ;
#33667=CARTESIAN_POINT ( 'NONE',  ( 10.31988039474999930, -17.71085245535000396, 7.753829094184000681 ) ) ;
#33670=CARTESIAN_POINT ( 'NONE',  ( -10.22174476410000032, -78.28692462859000045, 6.403415649647000052 ) ) ;
#33671=EDGE_CURVE ( 'NONE', #8523, #56093, #48299, .T. ) ;
#33672=CARTESIAN_POINT ( 'NONE',  ( 7.660411271065999728, -59.99173735459000056, 10.01752031416000044 ) ) ;
#33676=EDGE_LOOP ( 'NONE', ( #53337, #32146, #56406, #38708 ) ) ;
#33677=CARTESIAN_POINT ( 'NONE',  ( 2.147427714508652663, -78.16044680869335082, 11.59697916390112837 ) ) ;
#33687=CARTESIAN_POINT ( 'NONE',  ( -7.613962827179999948, -23.30639625649999758, 10.53101998747000145 ) ) ;
#33690=DIRECTION ( 'NONE',  ( 0.000000000000000000, 0.000000000000000000, -1.000000000000000000 ) ) ;
#33697=CARTESIAN_POINT ( 'NONE',  ( -7.753900686131000697, -17.71068035545000185, 10.31980286348999876 ) ) ;
#33700=DIRECTION ( 'NONE',  ( 0.000000000000000000, 0.000000000000000000, -1.000000000000000000 ) ) ;
#33703=CARTESIAN_POINT ( 'NONE',  ( 1.667260628947000001, -55.59057987493000041, -12.49858003893000102 ) ) ;
#33708=CARTESIAN_POINT ( 'NONE',  ( -6.650956564739962218, -78.62112206211111243, 9.738045520853518155 ) ) ;
#33709=CARTESIAN_POINT ( 'NONE',  ( 1.801614160555000010, -60.18652261871999798, -12.59687422890000086 ) ) ;
#33712=EDGE_CURVE ( 'NONE', #16171, #9567, #19255, .T. ) ;
#33716=CARTESIAN_POINT ( 'NONE',  ( 10.18127202938000053, -23.38645218951999993, -7.633406483298000644 ) ) ;
#33717=EDGE_CURVE ( 'NONE', #40044, #39806, #1360, .T. ) ;
#33720=CARTESIAN_POINT ( 'NONE',  ( 5.954976958736712511, -78.53219957205278945, 10.12882962619908866 ) ) ;
#33721=CARTESIAN_POINT ( 'NONE',  ( -7.624341766639000539, -23.26485146254000114, -10.42531125024000005 ) ) ;
#33728=DIRECTION ( 'NONE',  ( 0.000000000000000000, -1.000000000000000000, 0.000000000000000000 ) ) ;
#33729=CARTESIAN_POINT ( 'NONE',  ( -7.686941364987999847, -57.04527982297999955, -10.48774103564000093 ) ) ;
#33734=ORIENTED_EDGE ( 'NONE', *, *, #4570, .F. ) ;
#33735=CARTESIAN_POINT ( 'NONE',  ( 1.667917367010000040, -18.71943307332999851, 12.49306752634999995 ) ) ;
#33737=CARTESIAN_POINT ( 'NONE',  ( -12.61271904360000029, -23.19692351046000311, 1.798332623270999964 ) ) ;
#33738=ORIENTED_EDGE ( 'NONE', *, *, #10077, .F. ) ;
#33740=CARTESIAN_POINT ( 'NONE',  ( -12.54977952612999914, -53.75167110003000204, 0.03756586072996999370 ) ) ;
#33744=CARTESIAN_POINT ( 'NONE',  ( 0.005523896503811000225, -16.93036543774000080, 12.55021156880999911 ) ) ;
#33746=CARTESIAN_POINT ( 'NONE',  ( 1.750000000001000089, -60.05000000958000328, 12.56594317859000043 ) ) ;
#33750=EDGE_LOOP ( 'NONE', ( #30006, #23606, #14871, #32421, #6819 ) ) ;
#33751=EDGE_LOOP ( 'NONE', ( #19017, #37156, #50098, #27860 ) ) ;
#33753=CARTESIAN_POINT ( 'NONE',  ( -10.07627163191000008, -18.75000000240999753, 7.601397897754999633 ) ) ;
#33754=CARTESIAN_POINT ( 'NONE',  ( -12.54980660771999901, -61.84777352133000505, 0.05651102257804999779 ) ) ;
#33756=AXIS2_PLACEMENT_3D ( 'NONE', #5395, #18691, #36684 ) ;
#33757=CARTESIAN_POINT ( 'NONE',  ( 9.164385193176935118, -62.01567483104246037, 8.803702037067671071 ) ) ;
#33758=CARTESIAN_POINT ( 'NONE',  ( 1.750000000000000000, -21.74977139337000054, 12.65375411739000100 ) ) ;
#33763=CARTESIAN_POINT ( 'NONE',  ( -9.770419344647999438, -53.74469452534000169, 8.292776877908002220 ) ) ;
#33766=CARTESIAN_POINT ( 'NONE',  ( -7.658900723009000266, -18.79059707833999937, -10.01676258974000078 ) ) ;
#33768=CARTESIAN_POINT ( 'NONE',  ( 2.062312494845999655, -18.77284340107000205, -12.83634740209000036 ) ) ;
#33769=CARTESIAN_POINT ( 'NONE',  ( 0.4254080272216657077, -1.236984628861461655, -3.253004618393738223 ) ) ;
#33771=DIRECTION ( 'NONE',  ( 0.000000000000000000, -1.000000000000000000, 0.000000000000000000 ) ) ;
#33773=CARTESIAN_POINT ( 'NONE',  ( 0.9972398994228051095, -0.8977338377876618036, -3.382366038698053412 ) ) ;
#33775=CARTESIAN_POINT ( 'NONE',  ( 1.750000000000000000, -55.55000000278000272, 12.50000000000000000 ) ) ;
#33776=CARTESIAN_POINT ( 'NONE',  ( 9.837774000986101441, -17.68535604389086657, -7.850041800329745634 ) ) ;
#33780=EDGE_CURVE ( 'NONE', #22759, #46129, #6057, .T. ) ;
#33781=CARTESIAN_POINT ( 'NONE',  ( 1.288488638071999981, -61.33564939335000332, 12.54709296486000092 ) ) ;
#33787=CARTESIAN_POINT ( 'NONE',  ( 9.724363994122649402, -76.40209226852219615, -6.594912342232487568 ) ) ;
#33791=CARTESIAN_POINT ( 'NONE',  ( 7.958763982157000427, -54.32301960771999916, 9.723170657500999070 ) ) ;
#33793=CARTESIAN_POINT ( 'NONE',  ( 0.000000000000000000, -23.15000000000000213, 12.00000000000000000 ) ) ;
#33804=ORIENTED_EDGE ( 'NONE', *, *, #16020, .F. ) ;
#33805=ORIENTED_EDGE ( 'NONE', *, *, #50522, .F. ) ;
#33807=CARTESIAN_POINT ( 'NONE',  ( -7.220923959705244144, -77.37291666666664014, -9.396085398178621872 ) ) ;
#33811=EDGE_LOOP ( 'NONE', ( #50546, #10173, #24687, #18782, #25030 ) ) ;
#33814=CARTESIAN_POINT ( 'NONE',  ( -0.4143223953128999937, -2.940338749271000029, 3.376050216419999916 ) ) ;
#33816=LINE ( 'NONE', #47437, #30877 ) ;
#33823=EDGE_CURVE ( 'NONE', #58122, #15888, #38972, .T. ) ;
#33824=DIRECTION ( 'NONE',  ( 0.000000000000000000, 1.000000000000000000, 0.000000000000000000 ) ) ;
#33832=CARTESIAN_POINT ( 'NONE',  ( -12.60356226360999798, -56.04922971106000062, -1.750000000000000000 ) ) ;
#33836=AXIS2_PLACEMENT_3D ( 'NONE', #10023, #1179, #5291 ) ;
#33839=CARTESIAN_POINT ( 'NONE',  ( -7.046594079837121605, -76.27358058460355039, -9.403470532666203141 ) ) ;
#33840=CARTESIAN_POINT ( 'NONE',  ( -7.601397897754999633, -23.24999999688999708, -10.07627163191000008 ) ) ;
#33841=CARTESIAN_POINT ( 'NONE',  ( -7.943805570375999991, -61.23402324491999593, -9.641149735098998974 ) ) ;
#33844=CARTESIAN_POINT ( 'NONE',  ( -12.72554264791999934, -18.79839278105999867, -1.930240062458999928 ) ) ;
#33845=CARTESIAN_POINT ( 'NONE',  ( 12.66008999772000010, -24.62705329347999950, 1.387101471715999956 ) ) ;
#33848=DIRECTION ( 'NONE',  ( -1.000000000000000000, 0.000000000000000000, 0.000000000000000000 ) ) ;
#33850=CARTESIAN_POINT ( 'NONE',  ( 4.978310723272000082, -76.73944210185999282, -11.31553633254000069 ) ) ;
#33851=ORIENTED_EDGE ( 'NONE', *, *, #32009, .T. ) ;
#33853=CARTESIAN_POINT ( 'NONE',  ( 10.42531125072000009, -55.53514854654000032, 7.624341767124000135 ) ) ;
#33854=CARTESIAN_POINT ( 'NONE',  ( 9.444446661605001125, -78.97637553138000044, 8.397347097585999620 ) ) ;
#33855=CARTESIAN_POINT ( 'NONE',  ( -2.062597299672999540, -19.21514526754999963, -12.87022657274000004 ) ) ;
#33863=CARTESIAN_POINT ( 'NONE',  ( 7.601397897754999633, -23.24999999758999536, -10.07627163191000008 ) ) ;
#33864=ORIENTED_EDGE ( 'NONE', *, *, #2842, .F. ) ;
#33868=ORIENTED_EDGE ( 'NONE', *, *, #37309, .F. ) ;
#33871=AXIS2_PLACEMENT_3D ( 'NONE', #44111, #40254, #3661 ) ;
#33873=ORIENTED_EDGE ( 'NONE', *, *, #28413, .F. ) ;
#33879=ORIENTED_EDGE ( 'NONE', *, *, #18203, .F. ) ;
#33880=CARTESIAN_POINT ( 'NONE',  ( -12.71759155191110757, -24.06493881575022087, -1.809604648260982662 ) ) ;
#33883=ORIENTED_EDGE ( 'NONE', *, *, #54248, .T. ) ;
#33886=CARTESIAN_POINT ( 'NONE',  ( 9.346058021984571695, -16.83471832412213232, -8.620905970628376380 ) ) ;
#33891=CARTESIAN_POINT ( 'NONE',  ( -10.98362417419999915, -18.84999999999999787, 0.5999999999999999778 ) ) ;
#33893=CARTESIAN_POINT ( 'NONE',  ( -8.194866293440998817, -24.71043252651000088, 9.389192598794000588 ) ) ;
#33901=CARTESIAN_POINT ( 'NONE',  ( -9.416161903791310905, -77.49611799111114863, 7.561431734142661121 ) ) ;
#33903=EDGE_LOOP ( 'NONE', ( #37234, #42258, #17596, #25436, #9935, #29801 ) ) ;
#33905=FACE_OUTER_BOUND ( 'NONE', #16618, .T. ) ;
#33906=LINE ( 'NONE', #15342, #11608 ) ;
#33907=VECTOR ( 'NONE', #39102, 1000.000000000000000 ) ;
#33910=CARTESIAN_POINT ( 'NONE',  ( 3.334892075843000292, -2.746854981583999766, 1.239339612286000092 ) ) ;
#33914=CARTESIAN_POINT ( 'NONE',  ( -8.511625900046547955, -76.13945263819573483, 8.102560346989390538 ) ) ;
#33915=CARTESIAN_POINT ( 'NONE',  ( 10.21045785712752796, -76.85731980684688835, -5.980552670349623234 ) ) ;
#33921=CARTESIAN_POINT ( 'NONE',  ( 1.636761686205415067, -2.333333333333333037, 2.839805762151342616 ) ) ;
#33922=CARTESIAN_POINT ( 'NONE',  ( -7.646966600034999395, -59.99642081684000061, 10.19019745249000053 ) ) ;
#33926=DIRECTION ( 'NONE',  ( 0.000000000000000000, -1.000000000000000000, 0.000000000000000000 ) ) ;
#33928=ORIENTED_EDGE ( 'NONE', *, *, #27766, .F. ) ;
#33932=CARTESIAN_POINT ( 'NONE',  ( -3.161392481395000065, -1.783292672027000147, -1.501864700490999960 ) ) ;
#33937=AXIS2_PLACEMENT_3D ( 'NONE', #20343, #38338, #56362 ) ;
#33939=CARTESIAN_POINT ( 'NONE',  ( 10.18499221076999994, -57.05022860182000244, -7.710118476618999850 ) ) ;
#33940=CARTESIAN_POINT ( 'NONE',  ( 1.667917367065999912, -55.51943464808999806, -12.49306764013999960 ) ) ;
#33943=EDGE_CURVE ( 'NONE', #41659, #37958, #15699, .T. ) ;
#33946=ORIENTED_EDGE ( 'NONE', *, *, #17624, .F. ) ;
#33949=ADVANCED_FACE ( 'NONE', ( #37543 ), #1554, .T. ) ;
#33950=ORIENTED_EDGE ( 'NONE', *, *, #20193, .F. ) ;
#33951=CARTESIAN_POINT ( 'NONE',  ( 8.958657468039000094, -16.79887336309000290, 8.950049500644999156 ) ) ;
#33955=CARTESIAN_POINT ( 'NONE',  ( -10.26699006316252749, -75.84166666666666856, -5.917523019358070790 ) ) ;
#33956=CARTESIAN_POINT ( 'NONE',  ( -10.42426601462999969, -77.61928380272000538, 7.425889537758000536 ) ) ;
#33958=CARTESIAN_POINT ( 'NONE',  ( -8.485281374238999419, -23.25000000000000000, -8.485281374238999419 ) ) ;
#33961=EDGE_CURVE ( 'NONE', #1186, #41874, #7033, .T. ) ;
#33966=CARTESIAN_POINT ( 'NONE',  ( 12.50240681836000078, -61.48234730679999416, -1.005418944265000114 ) ) ;
#33970=FACE_OUTER_BOUND ( 'NONE', #20474, .T. ) ;
#33971=CARTESIAN_POINT ( 'NONE',  ( -10.36597025940959327, -18.22476146848570977, 7.635927901519359295 ) ) ;
#33973=FACE_OUTER_BOUND ( 'NONE', #32576, .T. ) ;
#33976=CARTESIAN_POINT ( 'NONE',  ( -7.919595949288999570, -55.65000000488999632, -8.768124086549999419 ) ) ;
#33978=AXIS2_PLACEMENT_3D ( 'NONE', #16603, #34590, #24880 ) ;
#33984=CARTESIAN_POINT ( 'NONE',  ( -9.414496040451998837, -16.73736394015000073, 8.652369398713998905 ) ) ;
#33986=CARTESIAN_POINT ( 'NONE',  ( 3.449524682386059471, -2.016339860153205876, 0.7156992932775020355 ) ) ;
#33989=CARTESIAN_POINT ( 'NONE',  ( 1.691611010928999903, -54.56917308736999672, -12.66722148965999928 ) ) ;
#33991=CARTESIAN_POINT ( 'NONE',  ( -13.89999999928999941, -5.999999999291000030, -8.437402497311000243E-09 ) ) ;
#33994=ORIENTED_EDGE ( 'NONE', *, *, #17890, .F. ) ;
#33996=CARTESIAN_POINT ( 'NONE',  ( 1.666727925310000025, -59.99174481743000342, -12.50018462905999961 ) ) ;
#33999=CIRCLE ( 'NONE', #8538, 0.5000000000000006661 ) ;
#34002=FACE_OUTER_BOUND ( 'NONE', #5864, .T. ) ;
#34005=CARTESIAN_POINT ( 'NONE',  ( 11.00358534011910017, -78.47804174058605042, 4.128363279570725908 ) ) ;
#34006=ORIENTED_EDGE ( 'NONE', *, *, #32080, .T. ) ;
#34008=CONICAL_SURFACE ( 'NONE', #42535, 12.74999999937999995, 0.7853981633972997312 ) ;
#34014=CARTESIAN_POINT ( 'NONE',  ( -1.817320609109999873E-14, -79.15000000008998882, 0.000000000000000000 ) ) ;
#34015=CARTESIAN_POINT ( 'NONE',  ( -10.14948852600999984, -59.55100835476999777, 7.674614791855999485 ) ) ;
#34018=ORIENTED_EDGE ( 'NONE', *, *, #14827, .F. ) ;
#34019=CARTESIAN_POINT ( 'NONE',  ( 1.799490225533999732, -19.22847221992000044, 12.64500484465999897 ) ) ;
#34020=CARTESIAN_POINT ( 'NONE',  ( -10.26699006316255591, -76.25833333333333997, 5.917523019358029934 ) ) ;
#34023=CARTESIAN_POINT ( 'NONE',  ( -12.77649795258999887, -53.49168567723999956, 0.06462540730615000395 ) ) ;
#34025=ORIENTED_EDGE ( 'NONE', *, *, #45387, .F. ) ;
#34029=FACE_BOUND ( 'NONE', #12959, .T. ) ;
#34032=EDGE_CURVE ( 'NONE', #58285, #11409, #5888, .T. ) ;
#34034=ORIENTED_EDGE ( 'NONE', *, *, #48052, .F. ) ;
#34037=ADVANCED_FACE ( 'NONE', ( #37770 ), #55791, .F. ) ;
#34038=CARTESIAN_POINT ( 'NONE',  ( -12.61277705616999967, -59.99666672496000075, -1.798399175679000095 ) ) ;
#34039=VECTOR ( 'NONE', #6682, 999.9999999999998863 ) ;
#34041=CARTESIAN_POINT ( 'NONE',  ( 7.653559502275999016, -23.29849137228000444, 10.01234990228999955 ) ) ;
#34042=DIRECTION ( 'NONE',  ( 0.000000000000000000, -1.000000000000000000, 0.000000000000000000 ) ) ;
#34043=CARTESIAN_POINT ( 'NONE',  ( -10.53003236233000095, -18.67547726287999765, 7.612971540274999782 ) ) ;
#34046=CARTESIAN_POINT ( 'NONE',  ( -1.342463812738999916E-14, -80.70000000000000284, -13.99999999999935874 ) ) ;
#34047=CARTESIAN_POINT ( 'NONE',  ( -9.414496040419999545, -53.53736393982000408, 8.652369398681999613 ) ) ;
#34050=CARTESIAN_POINT ( 'NONE',  ( 1.931087888049999979, -18.68415522710999710, -12.71658889741000031 ) ) ;
#34052=CARTESIAN_POINT ( 'NONE',  ( 13.94241845804000057, -32.46002936525999871, 4.312607202007000224E-05 ) ) ;
#34058=CARTESIAN_POINT ( 'NONE',  ( 3.236072848700317639, -1.467564355532075648, -1.392980727198947166 ) ) ;
#34059=B_SPLINE_CURVE_WITH_KNOTS ( 'NONE', 3,
 ( #5027, #9461, #40155, #41917, #20351, #33035, #10333, #1201, #20070, #15042, #28313, #42792, #24487, #11214, #37472, #50789, #2073, #38061 ),
 .UNSPECIFIED., .F., .F.,
 ( 4, 2, 2, 2, 2, 2, 2, 2, 4 ),
 ( 0.000000000000000000, 0.1249999999999999722, 0.2499999999999999445, 0.3749999999999998890, 0.4999999999999998890, 0.6249999999999998890, 0.7499999999999997780, 0.8749999999999998890, 1.000000000000000000 ),
 .UNSPECIFIED. ) ;
#34061=CARTESIAN_POINT ( 'NONE',  ( -3.167843140252689427, -1.581004088418222597, 0.8520282484494562381 ) ) ;
#34062=CARTESIAN_POINT ( 'NONE',  ( -12.50485692589189490, -24.86593462704853863, 0.6924071800263524867 ) ) ;
#34069=DIRECTION ( 'NONE',  ( 1.894056205636980548E-11, 1.538483569415980182E-07, -0.9999999999999882316 ) ) ;
#34071=FACE_OUTER_BOUND ( 'NONE', #20320, .T. ) ;
#34072=ADVANCED_FACE ( 'NONE', ( #24043 ), #33023, .F. ) ;
#34075=CARTESIAN_POINT ( 'NONE',  ( 8.269121427749986708, -76.38708047178403149, -8.347674621122058269 ) ) ;
#34078=CARTESIAN_POINT ( 'NONE',  ( 7.648026766733999615, -18.74999999413999774, 10.12290050089000104 ) ) ;
#34081=CARTESIAN_POINT ( 'NONE',  ( -2.122304942052989585, -0.7955729038712460177, -2.762992850480189055 ) ) ;
#34083=DIRECTION ( 'NONE',  ( 1.000000000000000000, 0.000000000000000000, 0.000000000000000000 ) ) ;
#34089=EDGE_LOOP ( 'NONE', ( #14186, #18553, #37367, #56343 ) ) ;
#34090=FACE_OUTER_BOUND ( 'NONE', #41221, .T. ) ;
#34091=ORIENTED_EDGE ( 'NONE', *, *, #28006, .F. ) ;
#34093=VERTEX_POINT ( 'NONE', #52943 ) ;
#34096=EDGE_LOOP ( 'NONE', ( #51423, #33646, #1671, #16583 ) ) ;
#34097=CARTESIAN_POINT ( 'NONE',  ( -10.48774103543000180, -58.55472018357999531, -7.686941364784000363 ) ) ;
#34098=CARTESIAN_POINT ( 'NONE',  ( -1.750000000000000000, -55.55000000209000177, 12.50000000000000000 ) ) ;
#34099=ORIENTED_EDGE ( 'NONE', *, *, #48543, .T. ) ;
#34102=DIRECTION ( 'NONE',  ( 0.7071067811865475727, 0.000000000000000000, -0.7071067811865475727 ) ) ;
#34111=AXIS2_PLACEMENT_3D ( 'NONE', #19613, #28454, #1050 ) ;
#34115=AXIS2_PLACEMENT_3D ( 'NONE', #50742, #6724, #15581 ) ;
#34118=CARTESIAN_POINT ( 'NONE',  ( 0.000000000000000000, -0.09999999995300053179, 0.000000000000000000 ) ) ;
#34119=CARTESIAN_POINT ( 'NONE',  ( -3.250000000000000000, -1.600000000000000089, 0.000000000000000000 ) ) ;
#34121=CARTESIAN_POINT ( 'NONE',  ( -11.16685539660449322, -76.22546096737708865, -3.732204631842894305 ) ) ;
#34122=CARTESIAN_POINT ( 'NONE',  ( 10.04116292115999975, -22.76462890193000277, 7.682344222570999470 ) ) ;
#34123=CARTESIAN_POINT ( 'NONE',  ( -8.790688707576000738, -61.73813493216999859, -8.797962936864001549 ) ) ;
#34127=CARTESIAN_POINT ( 'NONE',  ( -12.61112375831999977, -18.78433928967000099, -1.798929377342999736 ) ) ;
#34128=CARTESIAN_POINT ( 'NONE',  ( 7.349802007153999561, -77.72476194169999530, -10.73869877321999944 ) ) ;
#34131=CARTESIAN_POINT ( 'NONE',  ( 9.392096872483362446, -78.39518815251655326, -7.218040555448557605 ) ) ;
#34132=CARTESIAN_POINT ( 'NONE',  ( 1.811016405462519963, -24.06173555371950457, -12.71771640064136655 ) ) ;
#34133=CARTESIAN_POINT ( 'NONE',  ( -0.4693628207621999837, -76.70343746089999115, -12.35326893399999904 ) ) ;
#34137=CARTESIAN_POINT ( 'NONE',  ( 9.723199427898999048, -54.32306055827000080, -7.958735709912999390 ) ) ;
#34139=CARTESIAN_POINT ( 'NONE',  ( 12.72558241039000038, -60.00131830475000072, 1.930284820929999867 ) ) ;
#34140=CARTESIAN_POINT ( 'NONE',  ( -3.351075299998999668, -78.68536893705000068, -12.34648790642000016 ) ) ;
#34141=DIRECTION ( 'NONE',  ( -1.000000000000000000, 0.000000000000000000, 0.000000000000000000 ) ) ;
#34149=ADVANCED_FACE ( 'NONE', ( #29903 ), #53227, .F. ) ;
#34158=AXIS2_PLACEMENT_3D ( 'NONE', #20063, #25337, #15332 ) ;
#34159=ORIENTED_EDGE ( 'NONE', *, *, #11105, .T. ) ;
#34160=ORIENTED_EDGE ( 'NONE', *, *, #12341, .F. ) ;
#34166=CARTESIAN_POINT ( 'NONE',  ( 0.8519719440434405655, -2.455349913743563040, 3.164316409633407989 ) ) ;
#34167=ORIENTED_EDGE ( 'NONE', *, *, #48931, .F. ) ;
#34168=CARTESIAN_POINT ( 'NONE',  ( -8.031111192612954142, -78.48262027226905957, 9.095921368955231401 ) ) ;
#34170=CIRCLE ( 'NONE', #22860, 1.250000000000000444 ) ;
#34171=CARTESIAN_POINT ( 'NONE',  ( 8.798041828522000785, -53.86186490677999927, 8.790609562984000647 ) ) ;
#34174=CARTESIAN_POINT ( 'NONE',  ( -1.247385798842000071, -54.32277743483000165, 12.50301438874000048 ) ) ;
#34175=AXIS2_PLACEMENT_3D ( 'NONE', #21660, #6933, #25225 ) ;
#34179=CARTESIAN_POINT ( 'NONE',  ( -7.660431276880000695, -23.19179487662999861, 10.01749742441000102 ) ) ;
#34182=CARTESIAN_POINT ( 'NONE',  ( 10.30767511324000019, -60.54763733864000130, -7.634418707071000121 ) ) ;
#34189=DIRECTION ( 'NONE',  ( 0.7071067811865475727, 0.000000000000000000, 0.7071067811865475727 ) ) ;
#34190=CARTESIAN_POINT ( 'NONE',  ( -12.50000000000000000, -55.35321828636000419, 1.250000000000000000 ) ) ;
#34191=VECTOR ( 'NONE', #43737, 1000.000000000000000 ) ;
#34193=CARTESIAN_POINT ( 'NONE',  ( 0.6621380763940999392, -2.108437473830000464, -3.495547994364999855 ) ) ;
#34196=CARTESIAN_POINT ( 'NONE',  ( -11.45922444272926732, -76.18195732767712514, 2.597715832044583451 ) ) ;
#34199=CARTESIAN_POINT ( 'NONE',  ( -7.624341764926000131, -23.26485149464000202, 10.42531124853000080 ) ) ;
#34201=EDGE_CURVE ( 'NONE', #44710, #37950, #7990, .T. ) ;
#34207=CARTESIAN_POINT ( 'NONE',  ( -8.878335097444999491, -61.86963071710999884, 8.870344075662000449 ) ) ;
#34211=CARTESIAN_POINT ( 'NONE',  ( -12.70722357730239871, -54.38971352745738841, -1.610228312160249864 ) ) ;
#34212=EDGE_LOOP ( 'NONE', ( #53270, #29435, #14857, #11407 ) ) ;
#34213=AXIS2_PLACEMENT_3D ( 'NONE', #10787, #33487, #19931 ) ;
#34214=CARTESIAN_POINT ( 'NONE',  ( 10.40000000000000036, 0.000000000000000000, 0.000000000000000000 ) ) ;
#34216=CARTESIAN_POINT ( 'NONE',  ( 0.5999999998848000171, -23.14999999478999726, 11.79999999988000070 ) ) ;
#34217=VECTOR ( 'NONE', #3723, 1000.000000000000227 ) ;
#34220=EDGE_CURVE ( 'NONE', #45201, #21891, #20426, .T. ) ;
#34221=ORIENTED_EDGE ( 'NONE', *, *, #45263, .T. ) ;
#34222=B_SPLINE_CURVE_WITH_KNOTS ( 'NONE', 3,
 ( #5526, #15854, #1708, #56299, #51301, #2289, #55719, #51593, #20284, #46001 ),
 .UNSPECIFIED., .F., .F.,
 ( 4, 2, 2, 2, 4 ),
 ( 0.000000000000000000, 0.2500000000000000000, 0.5000000000000000000, 0.7500000000000000000, 1.000000000000000000 ),
 .UNSPECIFIED. ) ;
#34225=CARTESIAN_POINT ( 'NONE',  ( -7.970414252932341626, -24.52292089079958615, -9.713036876646134132 ) ) ;
#34229=ORIENTED_EDGE ( 'NONE', *, *, #51329, .T. ) ;
#34236=DIRECTION ( 'NONE',  ( 0.000000000000000000, -1.000000000000000000, 0.000000000000000000 ) ) ;
#34238=CARTESIAN_POINT ( 'NONE',  ( -1.495357591690006815, -54.24123662602505647, 12.70444646756156537 ) ) ;
#34239=CARTESIAN_POINT ( 'NONE',  ( -10.59557217617999925, -77.03266118433998599, 7.456311996931999531 ) ) ;
#34240=DIRECTION ( 'NONE',  ( 6.735242868878000753E-11, 1.000000000000000000, 0.000000000000000000 ) ) ;
#34246=CARTESIAN_POINT ( 'NONE',  ( 0.000000000000000000, 4.040000000000000036, 0.000000000000000000 ) ) ;
#34247=EDGE_LOOP ( 'NONE', ( #5489, #3979, #6498, #7082, #47887 ) ) ;
#34259=CARTESIAN_POINT ( 'NONE',  ( -12.82904109062999964, -18.67547726287999765, -2.062673488410000200 ) ) ;
#34260=CARTESIAN_POINT ( 'NONE',  ( -7.612971414716000140, -18.67547470641000018, 10.53003223724000037 ) ) ;
#34261=VECTOR ( 'NONE', #48686, 1000.000000000000000 ) ;
#34265=CYLINDRICAL_SURFACE ( 'NONE', #47953, 9.000000000000000000 ) ;
#34267=VERTEX_POINT ( 'NONE', #22443 ) ;
#34270=CARTESIAN_POINT ( 'NONE',  ( -3.206516299415000049, -2.013032031398999777, -0.5298615117031000299 ) ) ;
#34274=CARTESIAN_POINT ( 'NONE',  ( 1.183291175563982778, -2.097760233681444486, 3.314621515608663582 ) ) ;
#34283=ADVANCED_FACE ( 'NONE', ( #27150 ), #44751, .F. ) ;
#34285=CARTESIAN_POINT ( 'NONE',  ( 8.959429364845298949, -78.89329112012718781, -7.653857676387937126 ) ) ;
#34287=EDGE_CURVE ( 'NONE', #26450, #52133, #53749, .T. ) ;
#34290=CARTESIAN_POINT ( 'NONE',  ( 10.35410175339000105, -23.40399325350999860, -7.619715687203000520 ) ) ;
#34293=CARTESIAN_POINT ( 'NONE',  ( 11.30151105938903733, -78.47057225285870175, 3.216226699527826138 ) ) ;
#34294=CARTESIAN_POINT ( 'NONE',  ( -10.04567131166087357, -61.35088387338642946, 7.921299640537585951 ) ) ;
#34295=ORIENTED_EDGE ( 'NONE', *, *, #54826, .F. ) ;
#34298=DIRECTION ( 'NONE',  ( -0.7071067811865475727, 0.000000000000000000, -0.7071067811865475727 ) ) ;
#34299=CONICAL_SURFACE ( 'NONE', #25793, 12.94999999994000106, 0.7853981633972997312 ) ;
#34303=CARTESIAN_POINT ( 'NONE',  ( -12.82904091341000097, -60.12452529330000317, -2.062673488738000049 ) ) ;
#34304=FACE_OUTER_BOUND ( 'NONE', #27910, .T. ) ;
#34308=CARTESIAN_POINT ( 'NONE',  ( -13.99999999996999911, -5.900000000026950353, 3.874891027003000340E-10 ) ) ;
#34310=CARTESIAN_POINT ( 'NONE',  ( -12.55458806505999902, -24.16283916848999880, 1.575041344316999936 ) ) ;
#34313=DIRECTION ( 'NONE',  ( -1.000000000000000000, 0.000000000000000000, 0.000000000000000000 ) ) ;
#34315=EDGE_LOOP ( 'NONE', ( #2828, #21442, #19016, #32848, #20263 ) ) ;
#34324=ORIENTED_EDGE ( 'NONE', *, *, #48742, .T. ) ;
#34327=ADVANCED_FACE ( 'NONE', ( #18322 ), #36314, .F. ) ;
#34330=CARTESIAN_POINT ( 'NONE',  ( 7.705142895619999877, -20.24916621771999914, 10.24998526317999925 ) ) ;
#34331=CARTESIAN_POINT ( 'NONE',  ( 8.114920487424473805, -61.62884529302247216, 9.847900218122900284 ) ) ;
#34334=FACE_OUTER_BOUND ( 'NONE', #48254, .T. ) ;
#34335=AXIS2_PLACEMENT_3D ( 'NONE', #54082, #380, #18359 ) ;
#34336=CARTESIAN_POINT ( 'NONE',  ( 1.980532734072999901, -59.56232686814000488, 12.80090744966000038 ) ) ;
#34340=CARTESIAN_POINT ( 'NONE',  ( -7.974020021247000933, -17.36898233693000293, -9.929669236791999865 ) ) ;
#34341=CARTESIAN_POINT ( 'NONE',  ( 7.613962745625999062, -60.10639784916000394, 10.53101990622000095 ) ) ;
#34342=CARTESIAN_POINT ( 'NONE',  ( 0.8445585116436000739, -17.28959556757000016, -12.43380736237000050 ) ) ;
#34346=CARTESIAN_POINT ( 'NONE',  ( 2.674705653217700263, -3.500000000000001332, 2.124395908964210822 ) ) ;
#34347=CARTESIAN_POINT ( 'NONE',  ( -3.521517461832780693, -1.752479614403898323, -0.1112614230686466144 ) ) ;
#34348=VERTEX_POINT ( 'NONE', #49914 ) ;
#34353=CARTESIAN_POINT ( 'NONE',  ( -1.265915941616999829, -1.948956610291999736, 3.247563974725000246 ) ) ;
#34354=EDGE_CURVE ( 'NONE', #19523, #54307, #34059, .T. ) ;
#34357=CYLINDRICAL_SURFACE ( 'NONE', #12022, 1.750000000000000000 ) ;
#34361=DIRECTION ( 'NONE',  ( -1.000000000000000000, 0.000000000000000000, 0.000000000000000000 ) ) ;
#34364=EDGE_CURVE ( 'NONE', #34267, #22190, #5183, .T. ) ;
#34365=CARTESIAN_POINT ( 'NONE',  ( 1.105002574708906726, -76.33194444570602855, -11.71518713480698715 ) ) ;
#34369=ADVANCED_FACE ( 'NONE', ( #2355 ), #52297, .F. ) ;
#34370=CARTESIAN_POINT ( 'NONE',  ( 10.18499221075000172, -58.54977139891999371, 7.710118476601000026 ) ) ;
#34382=DIRECTION ( 'NONE',  ( 5.794542751510810980E-07, -1.853100651952265483E-20, -0.9999999999998322453 ) ) ;
#34383=ORIENTED_EDGE ( 'NONE', *, *, #48486, .T. ) ;
#34385=CARTESIAN_POINT ( 'NONE',  ( -0.4254240051736287720, -1.385416666666666297, 3.249999999999998224 ) ) ;
#34387=VERTEX_POINT ( 'NONE', #11784 ) ;
#34392=ORIENTED_EDGE ( 'NONE', *, *, #37434, .F. ) ;
#34397=CARTESIAN_POINT ( 'NONE',  ( -10.99609774599787215, -18.31447404869839701, 0.3135602106493823316 ) ) ;
#34398=ADVANCED_FACE ( 'NONE', ( #33905 ), #52511, .F. ) ;
#34402=CARTESIAN_POINT ( 'NONE',  ( 9.246161438659999732, -76.69780122596999661, -8.285323839175999794 ) ) ;
#34407=CARTESIAN_POINT ( 'NONE',  ( -10.14950121162999963, -19.24922972541000021, 7.674627477474999182 ) ) ;
#34408=CIRCLE ( 'NONE', #16516, 1.750000000000000000 ) ;
#34410=CARTESIAN_POINT ( 'NONE',  ( 2.294724576751220990, -2.913169622022151906, 2.300959236491029181 ) ) ;
#34413=CARTESIAN_POINT ( 'NONE',  ( -3.250000000000000000, -2.500000000000000000, 0.000000000000000000 ) ) ;
#34414=CARTESIAN_POINT ( 'NONE',  ( -13.13047446164998711, -56.01421830981000483, -0.8260994316375004365 ) ) ;
#34418=CARTESIAN_POINT ( 'NONE',  ( -8.188293269190999979, -61.50494400535999517, -9.395718629102999486 ) ) ;
#34419=AXIS2_PLACEMENT_3D ( 'NONE', #33478, #51805, #10480 ) ;
#34423=CARTESIAN_POINT ( 'NONE',  ( 12.72397319114999981, -23.22144180305999939, 1.930910316632999946 ) ) ;
#34425=CARTESIAN_POINT ( 'NONE',  ( 1.668607604570599312, -23.79381631241117390, -12.52787843850908978 ) ) ;
#34426=CARTESIAN_POINT ( 'NONE',  ( -12.41568479072999942, -76.00427771482000594, -1.552457108973999800 ) ) ;
#34427=EDGE_LOOP ( 'NONE', ( #34383, #19731, #20025, #27343, #38469, #26333 ) ) ;
#34430=CARTESIAN_POINT ( 'NONE',  ( 12.77301895554999867, -61.85186686341000240, 1.052127376138000114 ) ) ;
#34431=CARTESIAN_POINT ( 'NONE',  ( -6.116358872417999137, -78.49843700449001460, 10.57564232554000050 ) ) ;
#34432=CARTESIAN_POINT ( 'NONE',  ( 12.61277494327999982, -55.60332099621999902, -1.798398135845999946 ) ) ;
#34434=ADVANCED_FACE ( 'NONE', ( #43942 ), #1477, .F. ) ;
#34443=DIRECTION ( 'NONE',  ( 0.000000000000000000, 1.000000000000000000, 0.000000000000000000 ) ) ;
#34445=ORIENTED_EDGE ( 'NONE', *, *, #7435, .T. ) ;
#34447=ORIENTED_EDGE ( 'NONE', *, *, #52799, .F. ) ;
#34453=CARTESIAN_POINT ( 'NONE',  ( 11.44598977081988345, -77.96780392635157853, 3.079303880734496790 ) ) ;
#34456=CARTESIAN_POINT ( 'NONE',  ( 3.250000000000000000, -2.350000000000000089, 0.000000000000000000 ) ) ;
#34458=CARTESIAN_POINT ( 'NONE',  ( -1.777672186646999997, -78.93657643206628904, 12.13420648597999829 ) ) ;
#34460=CARTESIAN_POINT ( 'NONE',  ( 10.31988039472999930, -54.51085245502000021, 7.753829094159000235 ) ) ;
#34461=CARTESIAN_POINT ( 'NONE',  ( 8.114915067892086498, -17.17115967855345104, -9.847905526149444810 ) ) ;
#34466=DIRECTION ( 'NONE',  ( 0.000000000000000000, -1.000000000000000000, 0.000000000000000000 ) ) ;
#34468=CARTESIAN_POINT ( 'NONE',  ( -11.91862232004000077, -75.92788042555999084, 3.079279237876999531 ) ) ;
#34471=CARTESIAN_POINT ( 'NONE',  ( 10.18127202940000053, -60.18645218919000683, -7.633406483317000557 ) ) ;
#34472=CARTESIAN_POINT ( 'NONE',  ( -1.777672186646999997, -78.86924249125999609, 12.13420648597999829 ) ) ;
#34475=DIRECTION ( 'NONE',  ( 0.000000000000000000, -1.000000000000000000, 0.000000000000000000 ) ) ;
#34476=CARTESIAN_POINT ( 'NONE',  ( 8.485281374238999419, -60.74999999967048581, -8.485281374238999419 ) ) ;
#34477=EDGE_CURVE ( 'NONE', #25833, #4267, #11757, .T. ) ;
#34478=AXIS2_PLACEMENT_3D ( 'NONE', #40979, #22969, #32675 ) ;
#34481=CARTESIAN_POINT ( 'NONE',  ( 11.89999999977000122, -18.84999999999999787, 0.000000000000000000 ) ) ;
#34483=CARTESIAN_POINT ( 'NONE',  ( 0.4885402653841000031, -3.419151880086999995, 3.366111076004999703 ) ) ;
#34487=CARTESIAN_POINT ( 'NONE',  ( -11.51771691073675186, -76.18376931278361042, 2.323585216717103386 ) ) ;
#34491=VECTOR ( 'NONE', #57329, 1000.000000000000114 ) ;
#34493=CARTESIAN_POINT ( 'NONE',  ( -10.35845608625999859, -18.70221245812999911, -7.627487525417000036 ) ) ;
#34498=CARTESIAN_POINT ( 'NONE',  ( -2.884990931743999898, -1.577671397434999845, -1.282714777154000174 ) ) ;
#34500=FACE_OUTER_BOUND ( 'NONE', #16266, .T. ) ;
#34503=DIRECTION ( 'NONE',  ( 0.7071067811865475727, 0.000000000000000000, 0.7071067811865475727 ) ) ;
#34511=CARTESIAN_POINT ( 'NONE',  ( -9.722718241315000398, -55.54999999966999980, -7.954951288349001004 ) ) ;
#34512=B_SPLINE_CURVE_WITH_KNOTS ( 'NONE', 3,
 ( #15378, #51408, #14199, #10961, #51983, #38097, #20956, #7097, #12102, #38383, #56117, #39244, #29227, #57259, #52833, #7668 ),
 .UNSPECIFIED., .F., .F.,
 ( 4, 2, 2, 2, 2, 2, 2, 4 ),
 ( 0.000000000000000000, 0.2500000000000002220, 0.3749999999999991118, 0.4999999999999980016, 0.6249999999999968914, 0.6874999999999963363, 0.7499999999999958922, 1.000000000000000000 ),
 .UNSPECIFIED. ) ;
#34513=EDGE_CURVE ( 'NONE', #16536, #55676, #43801, .T. ) ;
#34516=ORIENTED_EDGE ( 'NONE', *, *, #43234, .F. ) ;
#34517=ORIENTED_EDGE ( 'NONE', *, *, #25889, .T. ) ;
#34521=ORIENTED_EDGE ( 'NONE', *, *, #35748, .T. ) ;
#34525=CARTESIAN_POINT ( 'NONE',  ( -10.25367346088999909, -78.20590642111000079, 7.393739220494000008 ) ) ;
#34526=AXIS2_PLACEMENT_3D ( 'NONE', #22755, #36329, #18045 ) ;
#34527=CARTESIAN_POINT ( 'NONE',  ( -9.050966798898000931, -59.94999999040999938, -7.919595949288999570 ) ) ;
#34530=DIRECTION ( 'NONE',  ( -1.000000000000000000, 0.000000000000000000, 0.000000000000000000 ) ) ;
#34535=CARTESIAN_POINT ( 'NONE',  ( -4.858114519317477509, -78.20876728749668416, 10.74709704218741813 ) ) ;
#34540=FACE_OUTER_BOUND ( 'NONE', #10224, .T. ) ;
#34541=CARTESIAN_POINT ( 'NONE',  ( 9.762347760324658452, -76.49685047353065670, 6.553835441005383622 ) ) ;
#34543=DIRECTION ( 'NONE',  ( -1.411442051944999995E-10, 6.386283326366000088E-09, -1.000000000000000000 ) ) ;
#34547=PLANE ( 'NONE',  #1748 ) ;
#34548=CARTESIAN_POINT ( 'NONE',  ( -7.668949790003000366, -22.77129148951999937, 10.21381326472000062 ) ) ;
#34550=CARTESIAN_POINT ( 'NONE',  ( 10.01332852689000141, -18.71943464842000182, -7.654537165467999671 ) ) ;
#34551=DIRECTION ( 'NONE',  ( -0.7071067811865475727, 0.000000000000000000, 0.7071067811865475727 ) ) ;
#34552=EDGE_CURVE ( 'NONE', #26739, #26014, #14566, .T. ) ;
#34562=CARTESIAN_POINT ( 'NONE',  ( -1.042351935971276067, -2.351068062435671902, -3.365055153995229809 ) ) ;
#34567=CARTESIAN_POINT ( 'NONE',  ( 10.95939905454414109, -75.97881982022552450, 4.237625572471915625 ) ) ;
#34569=EDGE_LOOP ( 'NONE', ( #51618, #8450, #34954, #53182 ) ) ;
#34576=CARTESIAN_POINT ( 'NONE',  ( 10.01676948373000009, -23.20938276584000093, -7.658894993369000481 ) ) ;
#34577=CARTESIAN_POINT ( 'NONE',  ( -1.718598679952006991, -17.75037066954035225, 12.71111582768095438 ) ) ;
#34578=EDGE_CURVE ( 'NONE', #53199, #27284, #6099, .T. ) ;
#34582=ORIENTED_EDGE ( 'NONE', *, *, #25263, .F. ) ;
#34583=AXIS2_PLACEMENT_3D ( 'NONE', #10019, #32133, #50174 ) ;
#34586=CARTESIAN_POINT ( 'NONE',  ( 12.56594317819999951, -55.54999998572999687, 1.750000000000000000 ) ) ;
#34590=DIRECTION ( 'NONE',  ( 0.000000000000000000, 1.000000000000000000, 0.000000000000000000 ) ) ;
#34592=LINE ( 'NONE', #52621, #53871 ) ;
#34597=CARTESIAN_POINT ( 'NONE',  ( 1.667936697358999965, -22.76462890193000277, 12.53241208773999915 ) ) ;
#34598=CARTESIAN_POINT ( 'NONE',  ( -9.396085398178650294, -76.24791666666668277, 7.220923959705211281 ) ) ;
#34599=EDGE_LOOP ( 'NONE', ( #55387, #43703, #41915, #26389 ) ) ;
#34600=ORIENTED_EDGE ( 'NONE', *, *, #45523, .T. ) ;
#34601=B_SPLINE_CURVE_WITH_KNOTS ( 'NONE', 3,
 ( #22690, #53992, #40702, #18274, #17975, #12935 ),
 .UNSPECIFIED., .F., .F.,
 ( 4, 2, 4 ),
 ( 0.000000000000000000, 0.5000000000000000000, 1.000000000000000000 ),
 .UNSPECIFIED. ) ;
#34602=CARTESIAN_POINT ( 'NONE',  ( -12.43356773662999970, -54.08739070985000552, -0.8411682846950000458 ) ) ;
#34604=ORIENTED_EDGE ( 'NONE', *, *, #19989, .F. ) ;
#34605=FACE_OUTER_BOUND ( 'NONE', #36419, .T. ) ;
#34612=ADVANCED_FACE ( 'NONE', ( #40244 ), #42009, .F. ) ;
#34616=CIRCLE ( 'NONE', #16729, 0.5000000000000001110 ) ;
#34617=CARTESIAN_POINT ( 'NONE',  ( -12.43646124691999866, -61.71751819588999410, 0.05236837569004999804 ) ) ;
#34619=CARTESIAN_POINT ( 'NONE',  ( 9.346069275303429791, -61.96527745656915442, 8.620894635631328740 ) ) ;
#34620=CARTESIAN_POINT ( 'NONE',  ( 9.073547343405500953, -53.57191135162067752, -8.894853367357773877 ) ) ;
#34622=CARTESIAN_POINT ( 'NONE',  ( -9.722718241315000398, -60.04999999966999980, -7.247844507162001015 ) ) ;
#34623=CARTESIAN_POINT ( 'NONE',  ( -7.648026768008000076, -55.55000001556999933, 10.12290050216000026 ) ) ;
#34625=VECTOR ( 'NONE', #30531, 1000.000000000000000 ) ;
#34626=EDGE_LOOP ( 'NONE', ( #47294, #46890, #8432, #30785 ) ) ;
#34627=AXIS2_PLACEMENT_3D ( 'NONE', #11034, #55597, #55895 ) ;
#34628=CARTESIAN_POINT ( 'NONE',  ( -9.029856014839001688, -53.46737842902999915, 9.038878718651000455 ) ) ;
#34630=CARTESIAN_POINT ( 'NONE',  ( -7.659225706236999720, -18.31732796024000010, -9.963487823496000928 ) ) ;
#34632=CARTESIAN_POINT ( 'NONE',  ( -1.933504092460000212, -18.59593152724999854, -12.70940235707999832 ) ) ;
#34635=DIRECTION ( 'NONE',  ( 0.000000000000000000, -1.000000000000000000, 0.000000000000000000 ) ) ;
#34637=CARTESIAN_POINT ( 'NONE',  ( 2.851043015753209176, -3.499999999999999112, 1.899452699823827029 ) ) ;
#34640=CARTESIAN_POINT ( 'NONE',  ( -2.941324361237704910, -3.499999999999999556, -1.526268571259735252 ) ) ;
#34641=B_SPLINE_CURVE_WITH_KNOTS ( 'NONE', 3,
 ( #14920, #48842, #30526, #17243, #43543, #56834, #8103, #44124, #47993, #20809, #8384, #16681, #3673, #12245, #57686, #35231, #26099, #21674, #52979, #16390, #48557, #21102, #2816, #53261 ),
 .UNSPECIFIED., .F., .F.,
 ( 4, 2, 2, 2, 2, 2, 2, 2, 2, 2, 2, 4 ),
 ( 0.000000000000000000, 0.1249999999999996114, 0.2499999999999992228, 0.3749999999999988343, 0.4374999999999983347, 0.4999999999999977796, 0.6249999999999967804, 0.7499999999999956701, 0.8124999999999947820, 0.8437499999999948930, 0.8749999999999951150, 1.000000000000000000 ),
 .UNSPECIFIED. ) ;
#34642=DIRECTION ( 'NONE',  ( 1.000000000000000000, 0.000000000000000000, 0.000000000000000000 ) ) ;
#34643=CARTESIAN_POINT ( 'NONE',  ( 2.852847297332000043, -3.410973948317999938, -2.519339706139999802 ) ) ;
#34646=DIRECTION ( 'NONE',  ( 1.000000000000000000, 0.000000000000000000, 0.000000000000000000 ) ) ;
#34650=CARTESIAN_POINT ( 'NONE',  ( -12.00000000000000000, -18.75000000000000000, 0.000000000000000000 ) ) ;
#34653=CARTESIAN_POINT ( 'NONE',  ( 10.67369879590530424, -76.41529813363538892, -4.913311340196373500 ) ) ;
#34659=CARTESIAN_POINT ( 'NONE',  ( -0.4479237788617201899, -0.8216145633097318157, -3.428385239426285480 ) ) ;
#34663=CARTESIAN_POINT ( 'NONE',  ( 3.708203932500000022, -75.80000000000001137, 11.41267819554000162 ) ) ;
#34664=CARTESIAN_POINT ( 'NONE',  ( 8.060167321886254399, -54.17936585327868215, 9.621722524767893248 ) ) ;
#34670=CARTESIAN_POINT ( 'NONE',  ( -1.217390015647338064, -24.81893024926236890, 12.70229597940998012 ) ) ;
#34672=ORIENTED_EDGE ( 'NONE', *, *, #25374, .F. ) ;
#34673=DIRECTION ( 'NONE',  ( 0.000000000000000000, 0.000000000000000000, -1.000000000000000000 ) ) ;
#34674=ORIENTED_EDGE ( 'NONE', *, *, #9705, .T. ) ;
#34678=ORIENTED_EDGE ( 'NONE', *, *, #10441, .F. ) ;
#34679=CARTESIAN_POINT ( 'NONE',  ( 12.16119841297000015, -78.66141265907999980, -1.092202732365999962 ) ) ;
#34682=ORIENTED_EDGE ( 'NONE', *, *, #3432, .T. ) ;
#34684=DIRECTION ( 'NONE',  ( 0.000000000000000000, 0.000000000000000000, -1.000000000000000000 ) ) ;
#34685=CARTESIAN_POINT ( 'NONE',  ( 12.49999990534960226, -13.07071424677999971, 0.001538265197309672755 ) ) ;
#34686=B_SPLINE_SURFACE_WITH_KNOTS ( 'NONE', 3, 3, ( 
 ( #45583, #32837, #18996, #45878 ),
 ( #1295, #5697, #727, #41430 ),
 ( #23706, #4838, #41718, #19289 ),
 ( #5989, #36700, #55295, #22834 ),
 ( #147, #14842, #440, #54137 ),
 ( #18416, #13676, #31675, #49720 ),
 ( #54437, #9263, #27249, #31968 ),
 ( #1015, #50011, #9557, #27541 ),
 ( #5129, #23127, #41135, #54716 ),
 ( #36989, #9850, #37869, #10733 ),
 ( #29011, #24299, #1583, #46761 ),
 ( #42605, #19573, #28710, #37573 ),
 ( #33433, #55589, #6283, #15139 ),
 ( #6578, #19875, #2168, #42312 ),
 ( #1880, #51177, #55889, #33134 ),
 ( #15441, #51470, #11027, #47050 ),
 ( #24590, #20169, #23996, #42013 ) ),
 .UNSPECIFIED., .F., .F., .F.,
 ( 4, 1, 1, 1, 1, 1, 1, 1, 1, 1, 1, 1, 1, 1, 4 ),
 ( 4, 4 ),
 ( -0.01011398171657000057, 0.000000000000000000, 0.08333333333333001192, 0.1666666666667000196, 0.2500000000000000000, 0.3333333333333000081, 0.4166666666666999919, 0.5000000000000000000, 0.5833333333333000637, 0.6666666666667000474, 0.7500000000000000000, 0.8333333333333000637, 0.9166666666667000474, 1.000000000000000000, 1.010365777941000021 ),
 ( -0.3559705546970000078, 1.357612346710000084 ),
 .UNSPECIFIED. ) ;
#34691=CARTESIAN_POINT ( 'NONE',  ( -13.07317008567999927, -77.51186929341000109, -1.028553310913000063 ) ) ;
#34698=CARTESIAN_POINT ( 'NONE',  ( 2.837645820808837982, -2.891962703774921373, 1.585247691945158577 ) ) ;
#34703=CARTESIAN_POINT ( 'NONE',  ( -3.370587613551000228, -1.726292672027000208, 0.9429417476038000068 ) ) ;
#34705=CARTESIAN_POINT ( 'NONE',  ( -7.646944885454000307, -59.99635956511999524, -10.19022188675999985 ) ) ;
#34708=CARTESIAN_POINT ( 'NONE',  ( 1.931087888240000217, -55.48415267986000288, 12.71658872082999814 ) ) ;
#34709=CARTESIAN_POINT ( 'NONE',  ( 12.56884868898000107, -76.74651637867998488, -3.366471670097000324 ) ) ;
#34713=CARTESIAN_POINT ( 'NONE',  ( -1.726950059272000182, -75.69530751397000756, -12.24089000852000098 ) ) ;
#34714=VERTEX_POINT ( 'NONE', #37267 ) ;
#34716=CARTESIAN_POINT ( 'NONE',  ( -3.250000000000000000, 4.040000000000000036, 0.000000000000000000 ) ) ;
#34718=CARTESIAN_POINT ( 'NONE',  ( 12.78037829250999913, -61.09316779356999660, 1.812823010630000065 ) ) ;
#34729=ORIENTED_EDGE ( 'NONE', *, *, #28413, .T. ) ;
#34730=ADVANCED_FACE ( 'NONE', ( #23695 ), #28301, .F. ) ;
#34732=CARTESIAN_POINT ( 'NONE',  ( -8.188331488387619927, -55.57158755757377122, -7.345153731672218633 ) ) ;
#34734=ORIENTED_EDGE ( 'NONE', *, *, #33219, .T. ) ;
#34736=EDGE_LOOP ( 'NONE', ( #27712, #40573, #13590, #210 ) ) ;
#34737=ORIENTED_EDGE ( 'NONE', *, *, #23477, .T. ) ;
#34738=CIRCLE ( 'NONE', #9314, 5.000000000000000888 ) ;
#34742=DIRECTION ( 'NONE',  ( 0.000000000000000000, 1.000000000000000000, 0.000000000000000000 ) ) ;
#34744=CARTESIAN_POINT ( 'NONE',  ( 3.250377508590382991, -2.361707286923234950, 0.4258434008466360221 ) ) ;
#34746=EDGE_CURVE ( 'NONE', #39067, #42771, #9290, .T. ) ;
#34749=B_SPLINE_CURVE_WITH_KNOTS ( 'NONE', 3,
 ( #14083, #39563, #26269, #32078, #23238, #16558, #41244, #34541, #52574, #30111, #1406, #55113, #11139, #51288, #56000, #19397, #19105, #28819, #6395, #28230, #33543, #24111, #41535, #18815, #55704, #42128, #32367, #46868, #15253, #37097, #10843, #14953, #42426, #32950, #36806, #24410, #47161, #6691, #50994, #10543, #32655, #54825, #1694, #28527, #46576, #14657, #1995, #19988, #14367, #6102, #19687, #27940, #37688, #33245, #15547, #51582, #45988, #24700, #23524, #1118, #55630, #1922, #54759, #45920, #37325, #41762, #1339, #5455, #32880, #46214, #15184, #50925, #36741, #51220, #14302, #32295, #10773, #50638, #23457, #19916, #1627, #28751, #50342, #55931, #15482, #10473, #55047, #46507, #33472, #19040, #14595, #32589, #5741, #28164, #23748, #57368, #24630, #52371, #42641, #16062, #39065, #20208, #12207, #38199, #56219, #47674, #30193, #56507, #48242, #51799, #26627, #35483, #40523, #31643, #13350, #31349, #49686, #49390, #17204, #48515, #407, #4512, #30767, #30488, #27217, #22805, #12771, #22512, #17496, #21918, #45255, #12490 ),
 .UNSPECIFIED., .F., .F.,
 ( 4, 2, 2, 2, 2, 2, 1, 1, 1, 1, 1, 2, 2, 2, 2, 2, 1, 1, 1, 1, 2, 2, 2, 2, 2, 1, 1, 1, 2, 2, 2, 2, 1, 1, 1, 1, 1, 2, 2, 2, 2, 2, 1, 1, 1, 2, 2, 2, 2, 2, 1, 1, 1, 1, 1, 1, 2, 2, 2, 2, 2, 1, 1, 1, 1, 2, 2, 2, 2, 1, 1, 1, 2, 2, 2, 2, 1, 1, 1, 1, 1, 2, 2, 2, 4 ),
 ( 0.000000000000000000, 0.06250000000000682787, 0.1250000000000136557, 0.1875000000000204559, 0.2187500000000238420, 0.2343750000000255629, 0.2421875000000264511, 0.2460937500000268674, 0.2480468750000270617, 0.2490234375000272560, 0.2495117187500273392, 0.2497558593750273392, 0.2500000000000273670, 0.2812500000000348610, 0.2968750000000385247, 0.3046875000000404121, 0.3085937500000413003, 0.3105468750000417999, 0.3115234375000421330, 0.3120117187500422995, 0.3122558593750424105, 0.3125000000000424660, 0.3437500000000606182, 0.3593750000000696665, 0.3671875000000742739, 0.3710937500000765499, 0.3730468750000777156, 0.3740234375000782707, 0.3745117187500785483, 0.3750000000000788258, 0.4062500000000975331, 0.4218750000001068035, 0.4296875000001114664, 0.4335937500001137423, 0.4355468750001149081, 0.4365234375001154632, 0.4370117187501157408, 0.4372558593751158518, 0.4375000000001159073, 0.4687500000001304512, 0.4843750000001376677, 0.4921875000001413314, 0.4960937500001431077, 0.4980468750001439959, 0.4990234375001444400, 0.4995117187501446621, 0.5000000000001448841, 0.6250000000002021716, 0.6875000000002308154, 0.7187500000002450262, 0.7343750000002522427, 0.7421875000002557954, 0.7460937500002575717, 0.7480468750002584599, 0.7490234375002589040, 0.7495117187502592371, 0.7497558593752592371, 0.7500000000002592371, 0.7812500000002334799, 0.7968750000002204903, 0.8046875000002140510, 0.8085937500002108314, 0.8105468750002091660, 0.8115234375002082778, 0.8120117187502078338, 0.8122558593752075007, 0.8125000000002072786, 0.8437500000001729727, 0.8593750000001559863, 0.8671875000001473266, 0.8710937500001431077, 0.8730468750001408873, 0.8740234375001398881, 0.8750000000001388889, 0.9062500000001064704, 0.9218750000000902611, 0.9296875000000821565, 0.9335937500000780487, 0.9355468750000760503, 0.9365234375000750511, 0.9370117187500744960, 0.9372558593750741629, 0.9375000000000738298, 0.9687500000000369704, 1.000000000000000000 ),
 .UNSPECIFIED. ) ;
#34750=CARTESIAN_POINT ( 'NONE',  ( 7.948094694382998426, -54.35965255578000210, 9.636752590464999102 ) ) ;
#34751=AXIS2_PLACEMENT_3D ( 'NONE', #471, #9881, #14291 ) ;
#34753=CARTESIAN_POINT ( 'NONE',  ( -3.044681358458452003, -77.30245510314006196, -11.37321520970169431 ) ) ;
#34754=CARTESIAN_POINT ( 'NONE',  ( -12.70556836324321281, -16.77227722580009939, -0.2598513551437900415 ) ) ;
#34756=EDGE_CURVE ( 'NONE', #47867, #36570, #39591, .T. ) ;
#34758=CARTESIAN_POINT ( 'NONE',  ( 1.328206530128999807, -76.58160288575999175, -12.23810562210000086 ) ) ;
#34762=CARTESIAN_POINT ( 'NONE',  ( -12.77301916226999978, -16.94808379552999966, 1.052060437765000023 ) ) ;
#34766=CARTESIAN_POINT ( 'NONE',  ( -0.8031675853856999892, -1.684977233352999981, 4.044120181570000305 ) ) ;
#34769=CARTESIAN_POINT ( 'NONE',  ( 1.906446389314999879, -1.641372700497000015, 3.546581172111999525 ) ) ;
#34773=DIRECTION ( 'NONE',  ( 0.000000000000000000, -1.000000000000000000, 0.000000000000000000 ) ) ;
#34774=CARTESIAN_POINT ( 'NONE',  ( 2.891311992273000175, -2.268041850768999890, 2.073108726819999692 ) ) ;
#34776=DIRECTION ( 'NONE',  ( -1.000000000000000000, 0.000000000000000000, 0.000000000000000000 ) ) ;
#34778=EDGE_CURVE ( 'NONE', #11225, #37628, #21179, .T. ) ;
#34779=CARTESIAN_POINT ( 'NONE',  ( -9.696018661907480407, -75.80000000000001137, 6.813282359576399827 ) ) ;
#34783=ORIENTED_EDGE ( 'NONE', *, *, #10734, .T. ) ;
#34784=CARTESIAN_POINT ( 'NONE',  ( -10.53101990620000095, -18.69360215052999763, -7.613962745610000304 ) ) ;
#34787=CARTESIAN_POINT ( 'NONE',  ( 11.44417895085271475, -77.02916666666666856, -3.075537641221520069 ) ) ;
#34790=CARTESIAN_POINT ( 'NONE',  ( 3.237649453555000001, -1.422597686686999818, -2.108892360458999971 ) ) ;
#34793=CARTESIAN_POINT ( 'NONE',  ( 0.000000000000000000, -46.09579702914000165, 0.000000000000000000 ) ) ;
#34794=VERTEX_POINT ( 'NONE', #44826 ) ;
#34796=AXIS2_PLACEMENT_3D ( 'NONE', #14283, #39981, #8398 ) ;
#34797=CARTESIAN_POINT ( 'NONE',  ( -14.00000000000000000, -72.70000000000000284, 0.000000000000000000 ) ) ;
#34798=FACE_OUTER_BOUND ( 'NONE', #33751, .T. ) ;
#34802=ORIENTED_EDGE ( 'NONE', *, *, #16639, .F. ) ;
#34806=CARTESIAN_POINT ( 'NONE',  ( -12.60413670423000099, -60.10716680829000325, 1.799502287691000069 ) ) ;
#34813=ORIENTED_EDGE ( 'NONE', *, *, #41370, .T. ) ;
#34814=CARTESIAN_POINT ( 'NONE',  ( 10.00844281758000065, -18.63109810616999695, 7.647097920691000361 ) ) ;
#34816=AXIS2_PLACEMENT_3D ( 'NONE', #53527, #44674, #4227 ) ;
#34817=LINE ( 'NONE', #7966, #22334 ) ;
#34818=CARTESIAN_POINT ( 'NONE',  ( 7.228795249850000104, -77.84130236656999102, -10.56189739613000000 ) ) ;
#34820=CARTESIAN_POINT ( 'NONE',  ( 7.714303428875997959, -26.30294702886003222, 12.53545825868000385 ) ) ;
#34824=DIRECTION ( 'NONE',  ( -0.9999999999999693578, 2.479738203407925921E-07, -1.117914101428966396E-12 ) ) ;
#34830=LINE ( 'NONE', #48163, #42665 ) ;
#34832=FACE_OUTER_BOUND ( 'NONE', #37082, .T. ) ;
#34834=CYLINDRICAL_SURFACE ( 'NONE', #27158, 3.600000000000000089 ) ;
#34835=CARTESIAN_POINT ( 'NONE',  ( -7.654537085030999499, -18.71943307332999851, 10.01332844637000008 ) ) ;
#34837=CARTESIAN_POINT ( 'NONE',  ( 10.21380041493000057, -22.77152778045000048, -7.668936932623999780 ) ) ;
#34841=EDGE_LOOP ( 'NONE', ( #5727, #24390, #17104, #18951, #22158, #44929 ) ) ;
#34844=CARTESIAN_POINT ( 'NONE',  ( -3.250000000000000000, -2.000000000000000000, 0.000000000000000000 ) ) ;
#34846=CARTESIAN_POINT ( 'NONE',  ( -12.76303204294999993, -23.26485150694999859, 1.980584515756000030 ) ) ;
#34850=CARTESIAN_POINT ( 'NONE',  ( -0.006333666751428999701, -53.46737355666999747, -12.77652491951000080 ) ) ;
#34855=VERTEX_POINT ( 'NONE', #12299 ) ;
#34856=FACE_OUTER_BOUND ( 'NONE', #3813, .T. ) ;
#34857=CARTESIAN_POINT ( 'NONE',  ( -2.841500632089049017, -2.143116487617794608, -1.636193441488569267 ) ) ;
#34864=CARTESIAN_POINT ( 'NONE',  ( 1.583004792647870307, -17.54790758843439491, 12.70616254411041801 ) ) ;
#34867=CARTESIAN_POINT ( 'NONE',  ( 0.000000000000000000, -6.000000000000000000, 0.000000000000000000 ) ) ;
#34868=ORIENTED_EDGE ( 'NONE', *, *, #12944, .T. ) ;
#34874=DIRECTION ( 'NONE',  ( 0.000000000000000000, 0.000000000000000000, -1.000000000000000000 ) ) ;
#34878=CARTESIAN_POINT ( 'NONE',  ( 11.61659281346613781, -76.93273162705501989, -2.077594685895145066 ) ) ;
#34879=CIRCLE ( 'NONE', #29236, 0.8000000000000000444 ) ;
#34880=ADVANCED_FACE ( 'NONE', ( #48049 ), #43897, .F. ) ;
#34881=CARTESIAN_POINT ( 'NONE',  ( -1.001315002657000131, -61.48522411647999775, 12.50000000000000000 ) ) ;
#34882=CARTESIAN_POINT ( 'NONE',  ( -12.70249480710866230, -61.76498603269881471, -0.9989402950384759228 ) ) ;
#34883=EDGE_CURVE ( 'NONE', #46040, #57635, #26858, .T. ) ;
#34884=CARTESIAN_POINT ( 'NONE',  ( 1.538071403319964281, -76.16458333333332575, 11.75000000000000711 ) ) ;
#34887=CARTESIAN_POINT ( 'NONE',  ( -12.77651065919999951, -53.49103388577999851, 0.04307580168117999125 ) ) ;
#34888=ORIENTED_EDGE ( 'NONE', *, *, #52060, .F. ) ;
#34889=FACE_OUTER_BOUND ( 'NONE', #13466, .T. ) ;
#34895=ORIENTED_EDGE ( 'NONE', *, *, #27890, .T. ) ;
#34896=ORIENTED_EDGE ( 'NONE', *, *, #33394, .T. ) ;
#34900=CARTESIAN_POINT ( 'NONE',  ( -12.55486071739000131, -60.95393632975000031, -1.580832792523999775 ) ) ;
#34902=CARTESIAN_POINT ( 'NONE',  ( 7.678690995240000206, -20.24351820077000141, 10.59551070215999857 ) ) ;
#34905=DIRECTION ( 'NONE',  ( 0.4045837981834735086, 0.8201365133286462328, 0.4045837981834735086 ) ) ;
#34907=FACE_OUTER_BOUND ( 'NONE', #51273, .T. ) ;
#34909=ORIENTED_EDGE ( 'NONE', *, *, #11133, .T. ) ;
#34911=CARTESIAN_POINT ( 'NONE',  ( -7.645391692591000599, -55.58469634128999814, 10.18949678826999872 ) ) ;
#34913=CARTESIAN_POINT ( 'NONE',  ( -8.798041828550999810, -17.06186490710999948, -8.790609563012999672 ) ) ;
#34915=LINE ( 'NONE', #30494, #38184 ) ;
#34916=CARTESIAN_POINT ( 'NONE',  ( 12.76303204291999904, -55.53514849259999409, 1.980584515756000030 ) ) ;
#34917=LINE ( 'NONE', #21071, #52478 ) ;
#34921=FACE_OUTER_BOUND ( 'NONE', #46448, .T. ) ;
#34923=ORIENTED_EDGE ( 'NONE', *, *, #26958, .F. ) ;
#34925=CARTESIAN_POINT ( 'NONE',  ( 2.061649843245999758, -55.59438692379999480, 12.83797346712000120 ) ) ;
#34926=CARTESIAN_POINT ( 'NONE',  ( 7.651147547633000201, -19.23743349724999874, -10.45204383579999963 ) ) ;
#34927=CARTESIAN_POINT ( 'NONE',  ( 3.129541869639000051, -2.920362276481999864, -2.166049510376999887 ) ) ;
#34929=CARTESIAN_POINT ( 'NONE',  ( 1.750000000001000089, -23.24999998674999802, -12.56594318051000059 ) ) ;
#34930=DIRECTION ( 'NONE',  ( -1.194297873234000201E-10, 1.000000000000000000, -5.211291098350999982E-10 ) ) ;
#34931=DIRECTION ( 'NONE',  ( -1.000000000000000000, 0.000000000000000000, 0.000000000000000000 ) ) ;
#34932=CARTESIAN_POINT ( 'NONE',  ( 1.636761686205427058, -3.166666666666666519, -2.839805762151336399 ) ) ;
#34934=CARTESIAN_POINT ( 'NONE',  ( -9.000000000000000000, -0.2000000000000000111, 0.000000000000000000 ) ) ;
#34935=EDGE_CURVE ( 'NONE', #37820, #46551, #57972, .T. ) ;
#34936=CARTESIAN_POINT ( 'NONE',  ( -1.873308010621101083, -77.06556246648871422, -11.87619401410840325 ) ) ;
#34938=CARTESIAN_POINT ( 'NONE',  ( -0.03884788386675075422, -76.32452440415889328, -11.74979495016792796 ) ) ;
#34941=CARTESIAN_POINT ( 'NONE',  ( 1.750000000001000089, -59.55100836327999758, -12.60354432391999957 ) ) ;
#34944=CARTESIAN_POINT ( 'NONE',  ( 3.251229025254284366, -3.362671771015649291, 0.5096591584606244840 ) ) ;
#34953=CARTESIAN_POINT ( 'NONE',  ( -12.00000000000000000, -18.84999999999999787, -0.5999999999999999778 ) ) ;
#34954=ORIENTED_EDGE ( 'NONE', *, *, #12181, .F. ) ;
#34955=B_SPLINE_CURVE_WITH_KNOTS ( 'NONE', 3,
 ( #12701, #40148, #52295, #29832, #47883, #7415 ),
 .UNSPECIFIED., .F., .F.,
 ( 4, 2, 4 ),
 ( 0.000000000000000000, 0.5000000000000000000, 1.000000000000000000 ),
 .UNSPECIFIED. ) ;
#34956=CARTESIAN_POINT ( 'NONE',  ( 7.709155920934510853, -60.72747430363504151, 9.998700314201467876 ) ) ;
#34957=CONICAL_SURFACE ( 'NONE', #52892, 0.6999999997695030007, 0.7853981633972997312 ) ;
#34958=VERTEX_POINT ( 'NONE', #53918 ) ;
#34959=VERTEX_POINT ( 'NONE', #22613 ) ;
#34967=CARTESIAN_POINT ( 'NONE',  ( 7.135759946468999360, -79.17960427995001282, -10.09022804928999939 ) ) ;
#34968=VERTEX_POINT ( 'NONE', #53614 ) ;
#34969=FACE_OUTER_BOUND ( 'NONE', #10655, .T. ) ;
#34971=ADVANCED_FACE ( 'NONE', ( #22905 ), #50079, .F. ) ;
#34975=CARTESIAN_POINT ( 'NONE',  ( -10.19999999921000011, -0.2000000007865999907, 1.811583764860000079E-09 ) ) ;
#34976=CARTESIAN_POINT ( 'NONE',  ( -10.31502378008536880, -79.09895833336493354, 5.961239727259085797 ) ) ;
#34979=CARTESIAN_POINT ( 'NONE',  ( -1.250000000000000000, -18.55321828668999729, -12.50000000000000000 ) ) ;
#34980=CIRCLE ( 'NONE', #4839, 0.5000000000000004441 ) ;
#34982=LINE ( 'NONE', #25561, #49694 ) ;
#34983=CARTESIAN_POINT ( 'NONE',  ( -2.298892750299144083, -3.037928567523061396, 2.296935490278543490 ) ) ;
#34985=EDGE_CURVE ( 'NONE', #26753, #7317, #5114, .T. ) ;
#34988=CARTESIAN_POINT ( 'NONE',  ( -0.8385792221450999451, -2.889988518283999941, -3.712528424878000166 ) ) ;
#34995=CARTESIAN_POINT ( 'NONE',  ( 12.61117499582000079, -23.21550664553999965, 1.798980867984000032 ) ) ;
#34996=CIRCLE ( 'NONE', #21816, 1.750000000000001332 ) ;
#34998=CARTESIAN_POINT ( 'NONE',  ( 1.782734487911076027, -24.12245368561141490, -12.71547286926152864 ) ) ;
#34999=CARTESIAN_POINT ( 'NONE',  ( -9.216780614190000165, -76.52341425608999259, 8.238619774073001167 ) ) ;
#35001=EDGE_CURVE ( 'NONE', #48492, #31399, #55156, .T. ) ;
#35003=DIRECTION ( 'NONE',  ( 0.000000000000000000, 0.000000000000000000, 1.000000000000000000 ) ) ;
#35004=EDGE_CURVE ( 'NONE', #47059, #48866, #54363, .T. ) ;
#35005=CARTESIAN_POINT ( 'NONE',  ( 12.61277705616999967, -59.99666672496000075, 1.798399175679000095 ) ) ;
#35006=CARTESIAN_POINT ( 'NONE',  ( -2.062597265787999845, -22.78461666469000235, -12.87024489156999962 ) ) ;
#35013=B_SPLINE_CURVE_WITH_KNOTS ( 'NONE', 3,
 ( #11496, #21773, #30908, #3770, #22360, #26482 ),
 .UNSPECIFIED., .F., .F.,
 ( 4, 1, 1, 4 ),
 ( 0.000000000000000000, 0.3333333333333000081, 0.6666666666667000474, 1.000000000000000000 ),
 .UNSPECIFIED. ) ;
#35015=ORIENTED_EDGE ( 'NONE', *, *, #3364, .T. ) ;
#35016=CARTESIAN_POINT ( 'NONE',  ( -8.178338515874335357, -55.49583131490307153, -7.356278612544859818 ) ) ;
#35017=ADVANCED_FACE ( 'NONE', ( #13743 ), #29684, .F. ) ;
#35023=ORIENTED_EDGE ( 'NONE', *, *, #37434, .T. ) ;
#35025=CARTESIAN_POINT ( 'NONE',  ( -3.453171399369999950, -1.863032031399000088, -0.5706200895263999762 ) ) ;
#35027=CARTESIAN_POINT ( 'NONE',  ( 10.98449626305583671, -18.69382183571523726, 0.5845794248139535298 ) ) ;
#35028=ORIENTED_EDGE ( 'NONE', *, *, #20538, .F. ) ;
#35029=CARTESIAN_POINT ( 'NONE',  ( 9.708203932502000200, -79.25000000000000000, -7.053423027506000587 ) ) ;
#35031=CIRCLE ( 'NONE', #8632, 1.749999999999999334 ) ;
#35032=CARTESIAN_POINT ( 'NONE',  ( 7.658900722992000532, -55.59059707800999917, 10.01676258972999989 ) ) ;
#35033=CARTESIAN_POINT ( 'NONE',  ( -7.718346056094000041, -21.74888345808999901, -10.07719973192000040 ) ) ;
#35038=CARTESIAN_POINT ( 'NONE',  ( -9.934814764470999648, -24.62368287829000124, 7.968971842743999723 ) ) ;
#35046=PLANE ( 'NONE',  #53638 ) ;
#35051=CARTESIAN_POINT ( 'NONE',  ( -8.096452064242996016, -22.78578169018999944, -13.15643568217000769 ) ) ;
#35052=CARTESIAN_POINT ( 'NONE',  ( 0.9838624519628998977, -2.321243309748000083, 3.418988675016000123 ) ) ;
#35055=LINE ( 'NONE', #43948, #25970 ) ;
#35056=DIRECTION ( 'NONE',  ( 1.000000000000000000, 1.534883903844000000E-11, -3.930229729684000008E-14 ) ) ;
#35060=VERTEX_POINT ( 'NONE', #53318 ) ;
#35064=EDGE_CURVE ( 'NONE', #56422, #23208, #30374, .T. ) ;
#35065=CARTESIAN_POINT ( 'NONE',  ( 11.75000000000000000, -77.04999999999999716, 0.000000000000000000 ) ) ;
#35067=AXIS2_PLACEMENT_3D ( 'NONE', #21342, #15761, #11349 ) ;
#35070=CARTESIAN_POINT ( 'NONE',  ( 12.54977961484000026, -25.04832888628999754, 0.03757501521676000211 ) ) ;
#35071=DIRECTION ( 'NONE',  ( 0.000000000000000000, 1.000000000000000000, 0.000000000000000000 ) ) ;
#35072=ORIENTED_EDGE ( 'NONE', *, *, #12669, .F. ) ;
#35076=FACE_OUTER_BOUND ( 'NONE', #1378, .T. ) ;
#35079=EDGE_CURVE ( 'NONE', #42463, #9508, #14619, .T. ) ;
#35083=CARTESIAN_POINT ( 'NONE',  ( -1.232226823489766199, -54.27709088663590364, -12.50408896745906340 ) ) ;
#35084=EDGE_CURVE ( 'NONE', #52197, #49440, #14325, .T. ) ;
#35085=ORIENTED_EDGE ( 'NONE', *, *, #22404, .T. ) ;
#35087=CARTESIAN_POINT ( 'NONE',  ( 1.001315001700999963, -54.11477588220000001, 12.50000000000000000 ) ) ;
#35088=CARTESIAN_POINT ( 'NONE',  ( -9.038965287750000854, -53.46737759073999996, -9.029769469428000406 ) ) ;
#35089=CIRCLE ( 'NONE', #11587, 12.80000000000000071 ) ;
#35092=ORIENTED_EDGE ( 'NONE', *, *, #48052, .T. ) ;
#35095=ORIENTED_EDGE ( 'NONE', *, *, #32965, .T. ) ;
#35097=DIRECTION ( 'NONE',  ( 0.7071067811865475727, 0.000000000000000000, -0.7071067811865475727 ) ) ;
#35100=CARTESIAN_POINT ( 'NONE',  ( -1.930860503447785925, -55.02582494032501614, 12.72930866328045418 ) ) ;
#35101=CARTESIAN_POINT ( 'NONE',  ( -9.082935096011000908, -77.23075131599000542, -9.017176053435999705 ) ) ;
#35106=CARTESIAN_POINT ( 'NONE',  ( 8.620934061286547490, -16.83470696674769229, 9.346030177879564249 ) ) ;
#35110=LINE ( 'NONE', #39561, #11657 ) ;
#35114=ADVANCED_FACE ( 'NONE', ( #5763 ), #37348, .T. ) ;
#35115=CARTESIAN_POINT ( 'NONE',  ( 12.64500484462999985, -22.77152778045000048, 1.799490225533999732 ) ) ;
#35116=CARTESIAN_POINT ( 'NONE',  ( 11.44417895085270054, -76.57083333333333997, 3.075537641221564922 ) ) ;
#35117=CARTESIAN_POINT ( 'NONE',  ( -1.750000000000000000, -23.24999999688999708, 12.50000000000000000 ) ) ;
#35119=EDGE_CURVE ( 'NONE', #23138, #46623, #32611, .T. ) ;
#35121=DIRECTION ( 'NONE',  ( 0.000000000000000000, -1.000000000000000000, 0.000000000000000000 ) ) ;
#35124=CIRCLE ( 'NONE', #1251, 13.89999999999999858 ) ;
#35126=ORIENTED_EDGE ( 'NONE', *, *, #40364, .F. ) ;
#35129=CARTESIAN_POINT ( 'NONE',  ( 12.80000000000000071, -2.900000000000000355, 0.000000000000000000 ) ) ;
#35136=CARTESIAN_POINT ( 'NONE',  ( -2.061649843245999758, -55.59438692379999480, -12.83797346712000120 ) ) ;
#35139=EDGE_LOOP ( 'NONE', ( #28726, #7929, #34392, #58001, #7252, #40342 ) ) ;
#35140=CIRCLE ( 'NONE', #18236, 1.750000000000001332 ) ;
#35143=CARTESIAN_POINT ( 'NONE',  ( 11.73875605999435123, -78.93695179073836243, -1.874534623384944254 ) ) ;
#35146=CARTESIAN_POINT ( 'NONE',  ( 0.3664097479239993849, -17.02809982499870856, -12.50575740043519346 ) ) ;
#35150=ORIENTED_EDGE ( 'NONE', *, *, #2676, .F. ) ;
#35156=CARTESIAN_POINT ( 'NONE',  ( 1.569236785184999737E-14, 0.000000000000000000, 0.000000000000000000 ) ) ;
#35158=DIRECTION ( 'NONE',  ( -0.7071067811864980568, 0.7071067811865969777, 2.302416782339995233E-09 ) ) ;
#35161=CARTESIAN_POINT ( 'NONE',  ( 0.000000000000000000, 0.000000000000000000, 0.000000000000000000 ) ) ;
#35163=CARTESIAN_POINT ( 'NONE',  ( -12.77306367228999839, -25.05881314456000197, 1.040970605966999862 ) ) ;
#35165=EDGE_LOOP ( 'NONE', ( #25601, #17426, #44278, #12750, #17511, #57546, #4269 ) ) ;
#35168=VERTEX_POINT ( 'NONE', #50660 ) ;
#35170=ORIENTED_EDGE ( 'NONE', *, *, #8069, .T. ) ;
#35172=CONICAL_SURFACE ( 'NONE', #44642, 0.6999999997695030007, 0.7853981633972997312 ) ;
#35176=EDGE_CURVE ( 'NONE', #7317, #35168, #50490, .T. ) ;
#35179=EDGE_LOOP ( 'NONE', ( #6305, #39627, #7834, #36495, #55533, #15425, #46758 ) ) ;
#35180=ORIENTED_EDGE ( 'NONE', *, *, #51772, .F. ) ;
#35182=DIRECTION ( 'NONE',  ( 0.000000000000000000, 0.000000000000000000, -1.000000000000000000 ) ) ;
#35185=CARTESIAN_POINT ( 'NONE',  ( -10.23621640724999793, -76.45181667362000155, 8.212304960288999922 ) ) ;
#35187=CARTESIAN_POINT ( 'NONE',  ( 8.114915067887620737, -53.97115967817116200, -9.847905526091571105 ) ) ;
#35189=EDGE_CURVE ( 'NONE', #33163, #33164, #45943, .T. ) ;
#35190=CARTESIAN_POINT ( 'NONE',  ( 12.78037507862999966, -17.70670131430000183, -1.812742845510000089 ) ) ;
#35191=CARTESIAN_POINT ( 'NONE',  ( -9.783241737786999792, -24.53564621530999901, -7.961026681561000018 ) ) ;
#35193=VERTEX_POINT ( 'NONE', #50948 ) ;
#35197=CARTESIAN_POINT ( 'NONE',  ( -9.422860735135998311, -16.74048607655000254, -8.643926020477998406 ) ) ;
#35198=CARTESIAN_POINT ( 'NONE',  ( 7.691893942725999800, -58.55453807205000061, 10.42272502862000039 ) ) ;
#35200=DIRECTION ( 'NONE',  ( 0.7071067811865474617, 0.000000000000000000, -0.7071067811865474617 ) ) ;
#35201=CARTESIAN_POINT ( 'NONE',  ( 10.07722254368999870, -57.05199022587000002, -7.718368845804999268 ) ) ;
#35209=EDGE_CURVE ( 'NONE', #6714, #48625, #24979, .T. ) ;
#35210=CARTESIAN_POINT ( 'NONE',  ( 2.062323307449999810, -55.57286846775000555, 12.83634826441000065 ) ) ;
#35211=CARTESIAN_POINT ( 'NONE',  ( -12.87024489156999962, -22.78461666469000235, 2.062597265787999845 ) ) ;
#35212=CARTESIAN_POINT ( 'NONE',  ( 0.7054349844981000484, -2.771954967774000522, -3.576897754931000151 ) ) ;
#35217=CARTESIAN_POINT ( 'NONE',  ( -0.005928781627359999175, -62.00113050230000056, 12.66336824422999996 ) ) ;
#35218=CARTESIAN_POINT ( 'NONE',  ( -2.839805762151337731, -3.041666666666666963, -1.636761686205423949 ) ) ;
#35221=CARTESIAN_POINT ( 'NONE',  ( 6.490606146300518908, -77.12338061544191703, -10.12186978042076646 ) ) ;
#35223=DIRECTION ( 'NONE',  ( 0.7071067811865474617, 0.000000000000000000, 0.7071067811865474617 ) ) ;
#35229=ADVANCED_FACE ( 'NONE', ( #55657 ), #57051, .T. ) ;
#35231=CARTESIAN_POINT ( 'NONE',  ( -10.04568514502024357, -17.44913840261576610, -7.921286339709529223 ) ) ;
#35232=ORIENTED_EDGE ( 'NONE', *, *, #31153, .T. ) ;
#35233=CARTESIAN_POINT ( 'NONE',  ( 8.179400488428159477, -54.05908162287557417, 9.502921777737899589 ) ) ;
#35236=CIRCLE ( 'NONE', #39139, 3.600000000000000089 ) ;
#35238=ORIENTED_EDGE ( 'NONE', *, *, #1200, .F. ) ;
#35241=ORIENTED_EDGE ( 'NONE', *, *, #45471, .T. ) ;
#35242=DIRECTION ( 'NONE',  ( 0.000000000000000000, -1.000000000000000000, 0.000000000000000000 ) ) ;
#35243=VECTOR ( 'NONE', #9878, 1000.000000000000000 ) ;
#35244=ORIENTED_EDGE ( 'NONE', *, *, #31016, .F. ) ;
#35248=CARTESIAN_POINT ( 'NONE',  ( 0.8537148449481999357, -24.70498145908999987, -12.43377424872999981 ) ) ;
#35251=ORIENTED_EDGE ( 'NONE', *, *, #35515, .F. ) ;
#35253=CARTESIAN_POINT ( 'NONE',  ( 11.90545625444000066, -78.77723422687999744, 3.315402164377000194 ) ) ;
#35254=VERTEX_POINT ( 'NONE', #23771 ) ;
#35256=CARTESIAN_POINT ( 'NONE',  ( 12.85140862679999962, -57.04439829966000275, -1.980464483675000054 ) ) ;
#35257=CARTESIAN_POINT ( 'NONE',  ( -1.624989163556999772E-14, -74.69999999881999031, 0.000000000000000000 ) ) ;
#35263=CARTESIAN_POINT ( 'NONE',  ( -13.06702859930000038, -77.01232752474999188, -1.103813699724999875 ) ) ;
#35267=CYLINDRICAL_SURFACE ( 'NONE', #41636, 0.5000000000000004441 ) ;
#35269=DIRECTION ( 'NONE',  ( 0.7071067811865474617, 0.000000000000000000, 0.7071067811865474617 ) ) ;
#35270=CARTESIAN_POINT ( 'NONE',  ( -1.305255771447972224, -3.009187556855974943, 2.975616621677583673 ) ) ;
#35272=CARTESIAN_POINT ( 'NONE',  ( -0.3664097479317053319, -24.97190017499968206, -12.50575740043507800 ) ) ;
#35274=CARTESIAN_POINT ( 'NONE',  ( -3.750250575282000121, -2.269022469510000306, 0.6493866540274000343 ) ) ;
#35278=B_SPLINE_CURVE_WITH_KNOTS ( 'NONE', 3,
 ( #32123, #53191, #13541, #18861, #45149, #4701, #304, #49875, #54588, #9419 ),
 .UNSPECIFIED., .F., .F.,
 ( 4, 2, 2, 2, 4 ),
 ( 0.000000000000000000, 0.1249999999999971689, 0.2499999999999943379, 0.4999999999999988898, 1.000000000000000000 ),
 .UNSPECIFIED. ) ;
#35281=VECTOR ( 'NONE', #34240, 1000.000000000000000 ) ;
#35284=CARTESIAN_POINT ( 'NONE',  ( 12.53073434187000146, -77.78026658266999505, -3.509976885708000260 ) ) ;
#35285=CARTESIAN_POINT ( 'NONE',  ( -7.921335223431004380, -61.35094696582485341, -10.04563431751754621 ) ) ;
#35286=CARTESIAN_POINT ( 'NONE',  ( 12.37198840876000006, -76.25631020154999362, 1.869025070383000031 ) ) ;
#35287=ORIENTED_EDGE ( 'NONE', *, *, #8047, .F. ) ;
#35291=CARTESIAN_POINT ( 'NONE',  ( 7.641012305223999768, -18.71082276572999703, -10.18589226631999978 ) ) ;
#35296=EDGE_CURVE ( 'NONE', #2377, #48625, #21217, .T. ) ;
#35301=ORIENTED_EDGE ( 'NONE', *, *, #2197, .T. ) ;
#35304=DIRECTION ( 'NONE',  ( 1.000000000000000000, 0.000000000000000000, 0.000000000000000000 ) ) ;
#35306=ORIENTED_EDGE ( 'NONE', *, *, #5626, .T. ) ;
#35311=CARTESIAN_POINT ( 'NONE',  ( -1.539687499886083888, -78.08365330915714253, 11.67491192796933319 ) ) ;
#35314=ORIENTED_EDGE ( 'NONE', *, *, #1809, .F. ) ;
#35317=ORIENTED_EDGE ( 'NONE', *, *, #481, .F. ) ;
#35321=CARTESIAN_POINT ( 'NONE',  ( 9.317995624384998621, -53.66762134137999851, 8.588852713974999276 ) ) ;
#35323=CARTESIAN_POINT ( 'NONE',  ( 0.000000000000000000, -65.72928575305999743, 0.000000000000000000 ) ) ;
#35325=CIRCLE ( 'NONE', #22161, 1.749999999999998668 ) ;
#35326=DIRECTION ( 'NONE',  ( 0.000000000000000000, 1.000000000000000000, 0.000000000000000000 ) ) ;
#35335=AXIS2_PLACEMENT_3D ( 'NONE', #34793, #56103, #56959 ) ;
#35337=CARTESIAN_POINT ( 'NONE',  ( 2.015551294784000191, -23.80347704843999779, 12.79857978895000059 ) ) ;
#35339=CARTESIAN_POINT ( 'NONE',  ( 0.5786309740341742947, -78.42119534047722595, 12.05093123062573213 ) ) ;
#35345=CARTESIAN_POINT ( 'NONE',  ( -10.53003236233000095, -23.32452273707999879, -7.612971540276999960 ) ) ;
#35348=FACE_OUTER_BOUND ( 'NONE', #51119, .T. ) ;
#35349=CARTESIAN_POINT ( 'NONE',  ( -11.52285712076000834, -76.18393803225121985, 2.297929651431338982 ) ) ;
#35353=ORIENTED_EDGE ( 'NONE', *, *, #13970, .T. ) ;
#35354=CARTESIAN_POINT ( 'NONE',  ( -10.07719973196000041, -20.25111654322000021, -7.718346056127999510 ) ) ;
#35356=AXIS2_PLACEMENT_3D ( 'NONE', #44760, #220, #27323 ) ;
#35358=CARTESIAN_POINT ( 'NONE',  ( 11.75000000000000178, -77.03958333333331154, -1.538071403319980268 ) ) ;
#35359=CARTESIAN_POINT ( 'NONE',  ( -9.996770077891000028, -60.95065455317000414, 7.758602204140999881 ) ) ;
#35360=AXIS2_PLACEMENT_3D ( 'NONE', #544, #46278, #49526 ) ;
#35361=CARTESIAN_POINT ( 'NONE',  ( 0.6384810558836999661, -1.356750604646000058, -3.810785800737999995 ) ) ;
#35363=CARTESIAN_POINT ( 'NONE',  ( 12.54976804508999955, -25.04775476228000031, 0.05637402076006000490 ) ) ;
#35364=CARTESIAN_POINT ( 'NONE',  ( -2.062670899148999926, -55.49360374314999689, 12.83044039271999992 ) ) ;
#35368=DIRECTION ( 'NONE',  ( 0.000000000000000000, -1.000000000000000000, 0.000000000000000000 ) ) ;
#35369=CARTESIAN_POINT ( 'NONE',  ( -10.35747158364999976, -60.11584477251999203, -7.626500902235000545 ) ) ;
#35371=EDGE_LOOP ( 'NONE', ( #32560, #28504, #48974, #30748, #36333 ) ) ;
#35372=DIRECTION ( 'NONE',  ( 0.000000000000000000, -1.000000000000000000, 0.000000000000000000 ) ) ;
#35373=CARTESIAN_POINT ( 'NONE',  ( 7.764818829621773943, -77.87976087924900526, -8.854276815225853525 ) ) ;
#35375=EDGE_LOOP ( 'NONE', ( #9429, #28323, #15155 ) ) ;
#35376=EDGE_CURVE ( 'NONE', #30078, #2252, #3323, .T. ) ;
#35377=CARTESIAN_POINT ( 'NONE',  ( -8.878349648264999061, -53.73036913477000098, -8.870329531799001188 ) ) ;
#35387=CARTESIAN_POINT ( 'NONE',  ( -3.116139353062999717, -78.47578184934000944, 12.57467468523999976 ) ) ;
#35389=CARTESIAN_POINT ( 'NONE',  ( 12.99510751537000353, -15.69705297113999443, 6.911973076623003642 ) ) ;
#35392=AXIS2_PLACEMENT_3D ( 'NONE', #12355, #16794, #21784 ) ;
#35394=LINE ( 'NONE', #58148, #20896 ) ;
#35398=CARTESIAN_POINT ( 'NONE',  ( 3.007117222848000093, -75.87269519504999948, 11.93703523519999976 ) ) ;
#35400=AXIS2_PLACEMENT_3D ( 'NONE', #22523, #41114, #417 ) ;
#35402=CARTESIAN_POINT ( 'NONE',  ( -1.202166735308230372, -3.252017009982586249, 3.308099677556824769 ) ) ;
#35403=CARTESIAN_POINT ( 'NONE',  ( 12.71798269385000069, -23.29778754190000001, 1.931086388578000079 ) ) ;
#35404=CARTESIAN_POINT ( 'NONE',  ( -12.75763395699000036, -19.22204592323999961, -1.931043742978000077 ) ) ;
#35406=CARTESIAN_POINT ( 'NONE',  ( 9.050966799188000067, -55.64999999964999233, 7.919595949288999570 ) ) ;
#35413=EDGE_CURVE ( 'NONE', #10827, #8754, #17759, .T. ) ;
#35414=EDGE_LOOP ( 'NONE', ( #20648, #24746, #14638, #44349 ) ) ;
#35424=CARTESIAN_POINT ( 'NONE',  ( 1.044910384896000188, -53.74473505772000692, -12.77260826194999943 ) ) ;
#35425=CARTESIAN_POINT ( 'NONE',  ( 11.43430539595883388, -75.96832016884428640, 2.742965560814985881 ) ) ;
#35427=VERTEX_POINT ( 'NONE', #47979 ) ;
#35429=CARTESIAN_POINT ( 'NONE',  ( 12.00000000000000000, -60.04999999966999980, 1.250000000000000000 ) ) ;
#35430=CARTESIAN_POINT ( 'NONE',  ( -6.967078475965290174, -78.77478358560729532, -9.587638151555635702 ) ) ;
#35432=B_SPLINE_CURVE_WITH_KNOTS ( 'NONE', 3,
 ( #33401, #24846, #16286, #38416, #25128, #51439 ),
 .UNSPECIFIED., .F., .F.,
 ( 4, 1, 1, 4 ),
 ( 0.000000000000000000, 0.3333333333333000081, 0.6666666666667000474, 1.000000000000000000 ),
 .UNSPECIFIED. ) ;
#35438=CARTESIAN_POINT ( 'NONE',  ( 2.593824895836550404, -78.55428885352219481, 11.47171456603886419 ) ) ;
#35439=FACE_OUTER_BOUND ( 'NONE', #6020, .T. ) ;
#35440=ORIENTED_EDGE ( 'NONE', *, *, #25996, .F. ) ;
#35443=EDGE_CURVE ( 'NONE', #55458, #49604, #17467, .T. ) ;
#35444=DIRECTION ( 'NONE',  ( -0.9936845293270585300, 0.1122098755727947705, 0.000000000000000000 ) ) ;
#35447=CARTESIAN_POINT ( 'NONE',  ( -12.50728313511820922, -53.80024825451957327, 0.1773838729375966927 ) ) ;
#35452=CARTESIAN_POINT ( 'NONE',  ( -12.50000000000000000, -60.04999999966999980, -1.250000000000000000 ) ) ;
#35453=AXIS2_PLACEMENT_3D ( 'NONE', #50653, #55649, #46818 ) ;
#35454=CARTESIAN_POINT ( 'NONE',  ( 0.000000000000000000, -26.10094976978000147, 0.000000000000000000 ) ) ;
#35458=ORIENTED_EDGE ( 'NONE', *, *, #35189, .T. ) ;
#35460=ORIENTED_EDGE ( 'NONE', *, *, #45850, .F. ) ;
#35463=ORIENTED_EDGE ( 'NONE', *, *, #35758, .T. ) ;
#35464=DIRECTION ( 'NONE',  ( -1.000000000000000000, 0.000000000000000000, 0.000000000000000000 ) ) ;
#35465=ORIENTED_EDGE ( 'NONE', *, *, #19768, .F. ) ;
#35466=CARTESIAN_POINT ( 'NONE',  ( 9.516272955293000990, -24.82538765621999843, 8.227498559427999680 ) ) ;
#35467=CARTESIAN_POINT ( 'NONE',  ( -10.45205659049000069, -19.23767314807999895, 7.651160337241000420 ) ) ;
#35471=VERTEX_POINT ( 'NONE', #38226 ) ;
#35477=CARTESIAN_POINT ( 'NONE',  ( 12.26635331368000159, -76.28453882784999962, 4.664607203767999977 ) ) ;
#35479=CARTESIAN_POINT ( 'NONE',  ( 7.864797288573664780, -54.34877151149995456, -10.10445166985919840 ) ) ;
#35481=CARTESIAN_POINT ( 'NONE',  ( 12.77651047532000028, -16.69104280938000073, 0.04320343284647000515 ) ) ;
#35482=CARTESIAN_POINT ( 'NONE',  ( -10.07616267220999973, -24.72631139030000114, -7.986947465007999014 ) ) ;
#35483=CARTESIAN_POINT ( 'NONE',  ( -10.83564775471081099, -76.66805056338695579, 4.543779009287320925 ) ) ;
#35485=ORIENTED_EDGE ( 'NONE', *, *, #44213, .F. ) ;
#35487=CARTESIAN_POINT ( 'NONE',  ( -8.533817832752999877, -53.79473856423000200, 9.213092693279001821 ) ) ;
#35491=CARTESIAN_POINT ( 'NONE',  ( -10.53562613913999968, -18.79442116269000351, -7.620013630324000253 ) ) ;
#35493=CARTESIAN_POINT ( 'NONE',  ( 2.426647618366673645E-14, -5.899999999999999467, -12.90000000000000036 ) ) ;
#35495=CARTESIAN_POINT ( 'NONE',  ( 0.2494208075035535266, -53.80711039216215852, 12.50614183109565047 ) ) ;
#35497=PLANE ( 'NONE',  #34816 ) ;
#35499=CARTESIAN_POINT ( 'NONE',  ( 2.839805762151334179, -1.791666666666666519, 1.636761686205429056 ) ) ;
#35502=ORIENTED_EDGE ( 'NONE', *, *, #28645, .T. ) ;
#35503=CARTESIAN_POINT ( 'NONE',  ( 1.996848836733677857, -1.424485875898780618, 2.599776808039695908 ) ) ;
#35504=CARTESIAN_POINT ( 'NONE',  ( -1.801750019967000016, -55.40992573246000319, 12.59656967650999881 ) ) ;
#35507=CARTESIAN_POINT ( 'NONE',  ( 1.416261411028999939, -1.974711001041000280, 3.359468912789999706 ) ) ;
#35509=AXIS2_PLACEMENT_3D ( 'NONE', #28210, #36216, #9944 ) ;
#35511=LINE ( 'NONE', #57098, #9197 ) ;
#35512=CARTESIAN_POINT ( 'NONE',  ( -1.466594960155999994, -60.88158199018999994, 12.44238958335999889 ) ) ;
#35513=CARTESIAN_POINT ( 'NONE',  ( 12.43641395964999852, -17.08198970748000178, -0.03481089025434000450 ) ) ;
#35515=EDGE_CURVE ( 'NONE', #41301, #9760, #41706, .T. ) ;
#35518=CARTESIAN_POINT ( 'NONE',  ( 12.03307672610699441, -76.69641582315870210, -1.008565388800895191 ) ) ;
#35519=CARTESIAN_POINT ( 'NONE',  ( 10.74399384636999955, -78.87441265908000787, -6.654290843581000203 ) ) ;
#35523=CARTESIAN_POINT ( 'NONE',  ( 1.575772165441551964, -61.26154542760956900, 12.70597445621661059 ) ) ;
#35525=CARTESIAN_POINT ( 'NONE',  ( -3.250000000000000000, -2.500000000000000000, 0.000000000000000000 ) ) ;
#35530=EDGE_CURVE ( 'NONE', #44472, #8017, #15589, .T. ) ;
#35538=VERTEX_POINT ( 'NONE', #29216 ) ;
#35541=EDGE_LOOP ( 'NONE', ( #1599, #14493, #10460, #36673 ) ) ;
#35544=AXIS2_PLACEMENT_3D ( 'NONE', #8286, #39292, #16576 ) ;
#35546=CARTESIAN_POINT ( 'NONE',  ( 2.065394024360999836, -23.42161432646000208, -12.82193048528000112 ) ) ;
#35550=FACE_OUTER_BOUND ( 'NONE', #41079, .T. ) ;
#35551=CARTESIAN_POINT ( 'NONE',  ( 11.76256880100000046, -78.69015337716000147, 3.275611217918000140 ) ) ;
#35552=VECTOR ( 'NONE', #254, 1000.000000000000227 ) ;
#35553=VERTEX_POINT ( 'NONE', #34216 ) ;
#35555=DIRECTION ( 'NONE',  ( 0.7071067811865473507, -1.433669009702094715E-08, -0.7071067811865473507 ) ) ;
#35562=CARTESIAN_POINT ( 'NONE',  ( -3.372301964606999825, -76.90131824283000128, 12.67255275672000003 ) ) ;
#35563=CARTESIAN_POINT ( 'NONE',  ( 12.20990109347999919, -76.47356177075999994, -3.270330254029999661 ) ) ;
#35567=CARTESIAN_POINT ( 'NONE',  ( -10.18491068061999982, -60.10716934574000447, 7.640030139773000606 ) ) ;
#35568=CARTESIAN_POINT ( 'NONE',  ( 1.034282562214086543, -2.950585576526748355, 3.080402021841319726 ) ) ;
#35573=CARTESIAN_POINT ( 'NONE',  ( 3.171758640500000226, -3.602072692704999746, 1.479846994257000059 ) ) ;
#35577=DIRECTION ( 'NONE',  ( 1.000000000000000000, 0.000000000000000000, 0.000000000000000000 ) ) ;
#35579=CARTESIAN_POINT ( 'NONE',  ( 2.062673488738000049, -55.47547470607999998, 12.82904091336000008 ) ) ;
#35580=CARTESIAN_POINT ( 'NONE',  ( 7.411516475408999050, -77.15588683971000705, -10.69619859711000132 ) ) ;
#35581=AXIS2_PLACEMENT_3D ( 'NONE', #403, #53811, #17796 ) ;
#35583=CARTESIAN_POINT ( 'NONE',  ( -8.792818914796958651, -62.02696626408313563, -9.175540344859795638 ) ) ;
#35584=CARTESIAN_POINT ( 'NONE',  ( 11.94419429569000002, -76.22030556059000617, -3.727676827021999983 ) ) ;
#35586=LINE ( 'NONE', #53035, #13487 ) ;
#35589=CARTESIAN_POINT ( 'NONE',  ( -2.062673488410000200, -23.32452273707999879, -12.82904109062999964 ) ) ;
#35592=CARTESIAN_POINT ( 'NONE',  ( -3.249661007175000282, -0.7674197747463000763, 2.357191814219000037 ) ) ;
#35595=ORIENTED_EDGE ( 'NONE', *, *, #2605, .F. ) ;
#35600=ORIENTED_EDGE ( 'NONE', *, *, #13607, .F. ) ;
#35601=ORIENTED_EDGE ( 'NONE', *, *, #52437, .F. ) ;
#35606=ORIENTED_EDGE ( 'NONE', *, *, #8092, .F. ) ;
#35610=CARTESIAN_POINT ( 'NONE',  ( -12.00000000000000000, -18.84999999997999964, 0.7999999999999001243 ) ) ;
#35612=DIRECTION ( 'NONE',  ( -0.7071067811865475727, 0.000000000000000000, 0.7071067811865475727 ) ) ;
#35615=B_SPLINE_SURFACE_WITH_KNOTS ( 'NONE', 3, 3, ( 
 ( #55202, #1205, #10051, #15631, #50792, #29196, #20354, #42796, #37774, #55496, #37475, #56085, #33337, #46368, #51372, #19482, #1492, #5893, #51670, #10633, #5600, #10929, #51084, #24201, #28316, #42505, #2076, #50497, #23901, #15046, #46077, #28910, #33038, #20074, #41920 ),
 ( #55795, #28616, #46661, #41625, #46954, #37188, #10337, #1783, #42217, #19778, #6188, #6480, #24491, #38064, #33628, #19196, #11217, #14745, #32744, #47242, #6773, #23611, #38351, #24782, #2358, #56372, #15923, #28033, #39212, #38642, #29481, #53087, #12070, #17070, #25635 ),
 ( #2646, #43945, #57509, #30341, #25348, #21499, #51950, #7922, #43088, #7064, #16501, #56660, #48384, #21206, #3496, #11506, #25064, #52514, #33910, #57227, #20924, #30050, #20640, #39505, #29761, #56942, #35052, #34774, #16215, #47539, #34193, #52230, #25922, #11787, #47818 ),
 ( #43364, #16792, #7348, #52798, #2923, #48102, #38925, #34483, #7635, #43660, #3219, #12353, #47145, #29102, #2546, #56276, #33814, #33231, #46853, #20549, #38545, #24396, #56559, #15534, #37378, #15238, #55392, #15826, #23800, #10830, #16120, #47435, #6677, #24096, #42410 ) ),
 .UNSPECIFIED., .F., .F., .F.,
 ( 4, 4 ),
 ( 4, 1, 1, 1, 1, 1, 1, 1, 1, 1, 1, 1, 1, 1, 1, 1, 1, 1, 1, 1, 1, 1, 1, 1, 1, 1, 1, 1, 1, 1, 1, 1, 4 ),
 ( -0.3708084972812999980, 1.370808497280999960 ),
 ( 0.1624174856069000028, 0.1891051637615999981, 0.2157928419163000211, 0.2424805200710000164, 0.2691681982257000394, 0.2958558763803000313, 0.3225435545349999988, 0.3492312326897000219, 0.3759189108443999894, 0.4026065889991000124, 0.4292942671537000043, 0.4559819453084000274, 0.4826696234630999949, 0.5093573016178000179, 0.5360449797724999854, 0.5627326579270999218, 0.5894203360818000004, 0.6161080142365000789, 0.6427956923911999354, 0.6694833705459000139, 0.6961710487005999815, 0.7228587268552000289, 0.7495464050098999964, 0.7762340831645999639, 0.8029217613193000425, 0.8296094394739998990, 0.8562971176285999464, 0.8829847957833000249, 0.9096724739379999924, 0.9363601520926999600, 0.9630478302474000385, 0.9897355084019999749, 1.016423186556999925 ),
 .UNSPECIFIED. ) ;
#35617=VERTEX_POINT ( 'NONE', #17380 ) ;
#35621=CARTESIAN_POINT ( 'NONE',  ( -7.613962745608000127, -23.30639784948999704, -10.53101990620000095 ) ) ;
#35622=CARTESIAN_POINT ( 'NONE',  ( -1.537891305778452233, -77.31276490156547254, -11.67737886329171815 ) ) ;
#35623=CARTESIAN_POINT ( 'NONE',  ( -10.26699006316255591, -78.75833333333332575, 5.917523019358029934 ) ) ;
#35624=CARTESIAN_POINT ( 'NONE',  ( 7.668936932630000314, -56.02847221959000024, -10.21380041493999968 ) ) ;
#35625=CARTESIAN_POINT ( 'NONE',  ( -7.954951288349001004, -60.24678171298000251, -9.722718241315000398 ) ) ;
#35626=CARTESIAN_POINT ( 'NONE',  ( 0.5999999999999999778, -23.15000000000000213, -10.98362417419999915 ) ) ;
#35628=EDGE_CURVE ( 'NONE', #9567, #35617, #3627, .T. ) ;
#35632=CONICAL_SURFACE ( 'NONE', #38484, 12.74999999937999995, 0.7853981633972997312 ) ;
#35633=DIRECTION ( 'NONE',  ( 0.000000000000000000, 0.000000000000000000, -1.000000000000000000 ) ) ;
#35634=CARTESIAN_POINT ( 'NONE',  ( -1.056237665594999875, -25.04866013698000060, 12.77256098197999989 ) ) ;
#35635=DIRECTION ( 'NONE',  ( -1.000000000000000000, 0.000000000000000000, 0.000000000000000000 ) ) ;
#35637=CARTESIAN_POINT ( 'NONE',  ( 4.086558352703000274, -1.033853494985000010, -0.5436765409910000457 ) ) ;
#35642=DIRECTION ( 'NONE',  ( -0.7071067811814418791, 1.254535583516073644E-07, -0.7071067811916420531 ) ) ;
#35644=B_SPLINE_SURFACE_WITH_KNOTS ( 'NONE', 3, 3, ( 
 ( #44693, #26659, #58268, #52180, #47481, #52461, #17832, #20870, #53847, #38587, #35819, #16162, #7585, #25009, #51892, #4543, #11735, #13381, #13086 ),
 ( #4246, #22245, #31380, #29713, #7296, #2872, #49422, #35519, #43606, #33854, #8972, #40256, #16450, #3166, #22546, #26957, #2591, #56318, #11450 ),
 ( #29429, #34431, #43030, #20590, #56602, #34140, #47761, #43316, #38873, #56893, #12019, #31083, #30000, #48054, #25584, #21156, #39162, #57171, #16737 ),
 ( #53547, #49120, #8671, #23417, #14553, #40846, #10430, #28414, #32544, #50593, #40557, #13971, #10144, #45289, #55004, #28120, #46171, #36408, #36120 ) ),
 .UNSPECIFIED., .F., .F., .F.,
 ( 4, 4 ),
 ( 4, 1, 1, 1, 1, 1, 1, 1, 1, 1, 1, 1, 1, 1, 1, 1, 4 ),
 ( -0.3708084972814000291, 1.370808497280999960 ),
 ( -0.009185076287115999730, 0.02066642164601000323, 0.05051791957914000125, 0.08036941751227000275, 0.1102209154453999973, 0.1400724133785000158, 0.1699239113116000066, 0.1997754092448000007, 0.2296269071778999915, 0.2594784051110000100, 0.2893299030441999764, 0.3191814009773000227, 0.3490328989103999580, 0.3788843968435000042, 0.4087358947766999706, 0.4385873927098000169, 0.4684388906429000077 ),
 .UNSPECIFIED. ) ;
#35646=DIRECTION ( 'NONE',  ( -0.7071067811865475727, 0.000000000000000000, -0.7071067811865475727 ) ) ;
#35655=CARTESIAN_POINT ( 'NONE',  ( -8.343860018000999190, -59.94999999967000548, 8.343860018000999190 ) ) ;
#35659=DIRECTION ( 'NONE',  ( 0.000000000000000000, 1.000000000000000000, 0.000000000000000000 ) ) ;
#35660=CARTESIAN_POINT ( 'NONE',  ( 2.161125324972999806, -0.7216593309027000691, -2.801917336448000118 ) ) ;
#35661=CARTESIAN_POINT ( 'NONE',  ( 7.601397897754999633, -23.25000000000000000, 9.369164850722000892 ) ) ;
#35662=DIRECTION ( 'NONE',  ( -0.7071067811865475727, 0.000000000000000000, -0.7071067811865475727 ) ) ;
#35664=EDGE_LOOP ( 'NONE', ( #56266, #55325, #44748, #35301 ) ) ;
#35665=CARTESIAN_POINT ( 'NONE',  ( -12.71758670595631280, -54.73493368743210397, 1.809547514116643274 ) ) ;
#35675=CYLINDRICAL_SURFACE ( 'NONE', #29455, 11.75000000000000000 ) ;
#35676=CARTESIAN_POINT ( 'NONE',  ( 8.872958366224914073, -61.81010144656845995, -8.813896669730688416 ) ) ;
#35677=FACE_OUTER_BOUND ( 'NONE', #50688, .T. ) ;
#35678=ORIENTED_EDGE ( 'NONE', *, *, #54774, .F. ) ;
#35680=CONICAL_SURFACE ( 'NONE', #49834, 8.899999998586000771, 0.7853981633972997312 ) ;
#35681=CARTESIAN_POINT ( 'NONE',  ( -12.60552522438000089, -60.08917565288000162, 1.799501877759999813 ) ) ;
#35682=CARTESIAN_POINT ( 'NONE',  ( -7.658900722992000532, -55.59059707800999917, -10.01676258972999989 ) ) ;
#35685=VERTEX_POINT ( 'NONE', #34797 ) ;
#35686=EDGE_CURVE ( 'NONE', #11409, #56919, #38868, .T. ) ;
#35687=ORIENTED_EDGE ( 'NONE', *, *, #38456, .T. ) ;
#35691=ORIENTED_EDGE ( 'NONE', *, *, #8018, .T. ) ;
#35700=LINE ( 'NONE', #30396, #19015 ) ;
#35701=ORIENTED_EDGE ( 'NONE', *, *, #13836, .F. ) ;
#35707=CARTESIAN_POINT ( 'NONE',  ( -1.083132186409117459, -2.748984415522624403, 3.413444661446231265 ) ) ;
#35709=CARTESIAN_POINT ( 'NONE',  ( -9.433537730491899254, -16.87202052679777253, 8.532653828096353976 ) ) ;
#35714=CARTESIAN_POINT ( 'NONE',  ( -1.629306394757588539, -76.93573459678474080, 11.96328544387188941 ) ) ;
#35717=DIRECTION ( 'NONE',  ( -1.000000000000000000, 0.000000000000000000, 0.000000000000000000 ) ) ;
#35721=CARTESIAN_POINT ( 'NONE',  ( 7.674614791499999811, -56.04899163905999870, -10.14948852566000070 ) ) ;
#35724=DIRECTION ( 'NONE',  ( -1.000000000000000000, 0.000000000000000000, 0.000000000000000000 ) ) ;
#35728=CARTESIAN_POINT ( 'NONE',  ( 0.8445585116459000119, -54.08959556723999640, -12.43380736233000050 ) ) ;
#35729=DIRECTION ( 'NONE',  ( 0.7071067811864963915, 0.000000000000000000, -0.7071067811865987540 ) ) ;
#35732=ORIENTED_EDGE ( 'NONE', *, *, #19663, .F. ) ;
#35737=DIRECTION ( 'NONE',  ( 0.000000000000000000, -0.8191989533107670862, 0.5735094374938772832 ) ) ;
#35739=CARTESIAN_POINT ( 'NONE',  ( 0.1409072282368034335, -78.57076637647936934, 11.74721378579847020 ) ) ;
#35741=ORIENTED_EDGE ( 'NONE', *, *, #12623, .F. ) ;
#35744=CARTESIAN_POINT ( 'NONE',  ( 8.750272118727675519, -75.80000000000002558, -8.070589281326626008 ) ) ;
#35748=EDGE_CURVE ( 'NONE', #19884, #26170, #9415, .T. ) ;
#35749=DIRECTION ( 'NONE',  ( 1.000000000000000000, 0.000000000000000000, 0.000000000000000000 ) ) ;
#35752=VECTOR ( 'NONE', #57663, 1000.000000000000000 ) ;
#35753=CARTESIAN_POINT ( 'NONE',  ( -1.513302041220051630E-14, -80.79999999999999716, 13.90000000000000036 ) ) ;
#35756=CARTESIAN_POINT ( 'NONE',  ( -12.66313299633999812, -25.17803434852999800, -0.06050769725596999438 ) ) ;
#35757=EDGE_LOOP ( 'NONE', ( #33121, #45311, #15379, #58221 ) ) ;
#35758=EDGE_CURVE ( 'NONE', #11190, #5429, #27404, .T. ) ;
#35763=VERTEX_POINT ( 'NONE', #27107 ) ;
#35766=CARTESIAN_POINT ( 'NONE',  ( 9.770427757044000572, -25.05529868456000386, 8.292768371742001321 ) ) ;
#35769=DIRECTION ( 'NONE',  ( 0.000000000000000000, -1.000000000000000000, -1.213843840257000049E-13 ) ) ;
#35775=VERTEX_POINT ( 'NONE', #45144 ) ;
#35779=CARTESIAN_POINT ( 'NONE',  ( -9.657845603713999694, -75.80025915097000677, -8.171271387442999412 ) ) ;
#35783=CARTESIAN_POINT ( 'NONE',  ( 12.70956139859000089, -18.59498835749000278, -1.933780970936999966 ) ) ;
#35784=CARTESIAN_POINT ( 'NONE',  ( -10.36221643468999964, -23.22123873666000193, -7.631895748949999891 ) ) ;
#35786=VERTEX_POINT ( 'NONE', #54861 ) ;
#35791=CARTESIAN_POINT ( 'NONE',  ( -3.250000000000001776, -3.489583333333332593, 0.4254240051736045136 ) ) ;
#35793=CARTESIAN_POINT ( 'NONE',  ( 0.000000000000000000, -49.87071424677999687, 0.000000000000000000 ) ) ;
#35794=CARTESIAN_POINT ( 'NONE',  ( -0.9212224518303999687, -17.18045898161000196, -12.54670315981999984 ) ) ;
#35796=CARTESIAN_POINT ( 'NONE',  ( 10.18589234707000202, -55.51082434643999619, -7.641012386020999969 ) ) ;
#35800=CARTESIAN_POINT ( 'NONE',  ( 0.4254240051736071226, -1.864583333333333259, 3.250000000000001776 ) ) ;
#35802=VERTEX_POINT ( 'NONE', #13534 ) ;
#35803=FACE_OUTER_BOUND ( 'NONE', #37413, .T. ) ;
#35804=CARTESIAN_POINT ( 'NONE',  ( 1.466594960164000039, -54.71841800914999965, 12.44238958329999889 ) ) ;
#35806=CARTESIAN_POINT ( 'NONE',  ( 3.654409531031999947, -2.491077063625000143, 1.063528925157000149 ) ) ;
#35811=CARTESIAN_POINT ( 'NONE',  ( -0.4802748259342999870, -61.80526907249000601, 12.54896097838000024 ) ) ;
#35812=CARTESIAN_POINT ( 'NONE',  ( 12.77297374713000089, -17.27184670111999765, 1.476174539902000094 ) ) ;
#35813=B_SPLINE_CURVE_WITH_KNOTS ( 'NONE', 3,
 ( #16871, #12716, #8289, #26000, #22154, #26293, #4155, #40161, #58175, #15271, #19707, #10865, #24127, #42730, #37115, #46596, #1137, #32971, #27957, #42145, #1427, #28836, #19416, #56016 ),
 .UNSPECIFIED., .F., .F.,
 ( 4, 2, 2, 2, 2, 2, 2, 2, 2, 2, 2, 4 ),
 ( 0.000000000000000000, 0.1250000000000006939, 0.2500000000000013878, 0.3750000000000016653, 0.4375000000000018319, 0.5000000000000018874, 0.6250000000000022204, 0.7500000000000025535, 0.8125000000000027756, 0.8437500000000022204, 0.8750000000000017764, 1.000000000000000000 ),
 .UNSPECIFIED. ) ;
#35818=CARTESIAN_POINT ( 'NONE',  ( 1.083751753440150623, -76.82094722090765515, 12.16865443235956512 ) ) ;
#35819=CARTESIAN_POINT ( 'NONE',  ( 2.521041396662000000, -79.11443781726001134, 12.22511922822000052 ) ) ;
#35824=CARTESIAN_POINT ( 'NONE',  ( 0.5135400120715946093, -61.97868533818393644, 12.70453250103551035 ) ) ;
#35833=CARTESIAN_POINT ( 'NONE',  ( 7.434020715870143903, -55.28308356097522847, 8.107762507646580019 ) ) ;
#35835=EDGE_CURVE ( 'NONE', #7896, #39052, #46614, .T. ) ;
#35836=VERTEX_POINT ( 'NONE', #19437 ) ;
#35837=VECTOR ( 'NONE', #45409, 1000.000000000000000 ) ;
#35840=ORIENTED_EDGE ( 'NONE', *, *, #3, .F. ) ;
#35841=DIRECTION ( 'NONE',  ( 0.000000000000000000, -0.8191989531316805628, 0.5735094377496839924 ) ) ;
#35843=CARTESIAN_POINT ( 'NONE',  ( -1.807051837523000026, -17.69921584757000232, 12.77977401834999860 ) ) ;
#35851=CARTESIAN_POINT ( 'NONE',  ( 10.11803007844999946, -79.12126414830001409, -6.834701957643000370 ) ) ;
#35852=B_SPLINE_CURVE_WITH_KNOTS ( 'NONE', 3,
 ( #44697, #13977, #31972, #40260, #31385, #35523, #13091, #4252, #58273, #45293, #54141, #35824, #9561, #27545, #53853, #45589, #49426, #5134, #26962, #44992, #4548, #22550, #13682, #40561, #154, #31679, #32551, #37577, #55301, #28419 ),
 .UNSPECIFIED., .F., .F.,
 ( 4, 2, 2, 2, 2, 2, 2, 2, 2, 2, 2, 2, 2, 2, 4 ),
 ( 0.000000000000000000, 0.1250000000000012768, 0.1875000000000003608, 0.2499999999999994449, 0.3124999999999985012, 0.3749999999999976130, 0.4999999999999957256, 0.5624999999999947820, 0.6249999999999937828, 0.6874999999999928946, 0.7499999999999920064, 0.8124999999999911182, 0.8437499999999921174, 0.8749999999999930056, 1.000000000000000000 ),
 .UNSPECIFIED. ) ;
#35855=DIRECTION ( 'NONE',  ( 0.000000000000000000, 1.000000000000000000, 0.000000000000000000 ) ) ;
#35856=DIRECTION ( 'NONE',  ( 0.000000000000000000, -1.000000000000000000, 0.000000000000000000 ) ) ;
#35857=CARTESIAN_POINT ( 'NONE',  ( -1.930860503577499721, -60.57417505875993413, -12.72930866334836253 ) ) ;
#35858=CIRCLE ( 'NONE', #40594, 12.57042253521000141 ) ;
#35863=CARTESIAN_POINT ( 'NONE',  ( -10.42426601462999969, -77.28220295299000497, 7.425889537758000536 ) ) ;
#35869=CARTESIAN_POINT ( 'NONE',  ( -10.04115011118999945, -59.56486430393999854, 7.682331425190000118 ) ) ;
#35870=CARTESIAN_POINT ( 'NONE',  ( -7.611782534905008113, -76.76874987344496049, -9.041039793178395456 ) ) ;
#35875=CARTESIAN_POINT ( 'NONE',  ( 0.07399134906894000441, -2.121452884883999968, 3.805339572302000040 ) ) ;
#35878=VERTEX_POINT ( 'NONE', #46226 ) ;
#35880=CARTESIAN_POINT ( 'NONE',  ( -7.601397897754999633, -23.24999999688999708, -10.07627163191000008 ) ) ;
#35882=CARTESIAN_POINT ( 'NONE',  ( -12.77649795263000065, -16.69168567756999977, 0.06462540730615000395 ) ) ;
#35884=CARTESIAN_POINT ( 'NONE',  ( -1.264141272797000060, -77.59992396741000675, -12.95149364859999963 ) ) ;
#35886=CARTESIAN_POINT ( 'NONE',  ( 12.75763395695999947, -22.77795407709999864, -1.931043742978000077 ) ) ;
#35890=CARTESIAN_POINT ( 'NONE',  ( 9.546819346760999636, -61.48527546573999558, -8.130850182902999990 ) ) ;
#35894=CARTESIAN_POINT ( 'NONE',  ( -3.587712099295000012, -1.745612256652999905, 1.801380527025000067 ) ) ;
#35895=CARTESIAN_POINT ( 'NONE',  ( -1.930989179114000143, -57.04546192861999998, -12.80896991328000034 ) ) ;
#35899=DIRECTION ( 'NONE',  ( 0.000000000000000000, -1.000000000000000000, -6.032211767129999953E-14 ) ) ;
#35900=CIRCLE ( 'NONE', #33068, 0.5000000000000004441 ) ;
#35901=ORIENTED_EDGE ( 'NONE', *, *, #32666, .F. ) ;
#35906=ORIENTED_EDGE ( 'NONE', *, *, #34354, .T. ) ;
#35908=VERTEX_POINT ( 'NONE', #10194 ) ;
#35909=ORIENTED_EDGE ( 'NONE', *, *, #31613, .F. ) ;
#35910=CARTESIAN_POINT ( 'NONE',  ( -10.07627163191000008, -60.04999999657000131, 7.601397897754999633 ) ) ;
#35914=DIRECTION ( 'NONE',  ( 0.000000000000000000, 1.000000000000000000, 0.000000000000000000 ) ) ;
#35915=AXIS2_PLACEMENT_3D ( 'NONE', #29372, #6367, #55378 ) ;
#35916=B_SPLINE_CURVE_WITH_KNOTS ( 'NONE', 3,
 ( #1614, #51791, #38189, #55922, #14872, #15170 ),
 .UNSPECIFIED., .F., .F.,
 ( 4, 1, 1, 4 ),
 ( 0.000000000000000000, 0.3333333333333000081, 0.6666666666667000474, 1.000000000000000000 ),
 .UNSPECIFIED. ) ;
#35920=CARTESIAN_POINT ( 'NONE',  ( 1.250000000000000000, -60.04999999966999980, 12.50000000000000000 ) ) ;
#35922=CARTESIAN_POINT ( 'NONE',  ( -7.626500902215000544, -18.68415522710999710, -10.35747158362999976 ) ) ;
#35924=EDGE_CURVE ( 'NONE', #38791, #11586, #37335, .T. ) ;
#35925=CARTESIAN_POINT ( 'NONE',  ( 10.13881649148000008, -76.50783510652000530, -5.938594122520999719 ) ) ;
#35928=CARTESIAN_POINT ( 'NONE',  ( -10.52693147740000157, -23.42153431750000436, 7.606024891108000396 ) ) ;
#35930=DIRECTION ( 'NONE',  ( -1.000000000000000000, 0.000000000000000000, 0.000000000000000000 ) ) ;
#35933=CARTESIAN_POINT ( 'NONE',  ( -12.79971535686000017, -18.20965922269000004, 2.019101350716999921 ) ) ;
#35934=CARTESIAN_POINT ( 'NONE',  ( 12.85144117163000033, -21.75472017028999971, -1.980464439859999981 ) ) ;
#35935=CARTESIAN_POINT ( 'NONE',  ( -0.005523896503821000906, -25.06963456225999920, 12.55021156880999911 ) ) ;
#35938=EDGE_CURVE ( 'NONE', #43521, #13888, #26100, .T. ) ;
#35939=CARTESIAN_POINT ( 'NONE',  ( -3.379948544607000116, -1.337975590836000039, 2.055725249092000162 ) ) ;
#35943=CARTESIAN_POINT ( 'NONE',  ( 12.43646324850000084, -61.72048514535000407, -0.1256879863178999857 ) ) ;
#35945=CARTESIAN_POINT ( 'NONE',  ( 7.714303428875997959, -26.30294702886003222, -12.53545825868000385 ) ) ;
#35949=EDGE_CURVE ( 'NONE', #34348, #17562, #23758, .T. ) ;
#35950=CARTESIAN_POINT ( 'NONE',  ( -13.94827576517086065, -33.10361340872000113, -0.001644113314415235816 ) ) ;
#35953=VERTEX_POINT ( 'NONE', #41771 ) ;
#35956=EDGE_CURVE ( 'NONE', #24318, #23895, #51230, .T. ) ;
#35962=CARTESIAN_POINT ( 'NONE',  ( -12.76303204291999904, -55.53514849259999409, -1.980584515756000030 ) ) ;
#35966=CARTESIAN_POINT ( 'NONE',  ( 12.54902678210999944, -25.00971938212000012, -0.4616712539285000028 ) ) ;
#35969=CARTESIAN_POINT ( 'NONE',  ( -1.980610890453999851, -55.27926110487717182, -12.74374574604606281 ) ) ;
#35973=CARTESIAN_POINT ( 'NONE',  ( -12.92177931905999877, -58.55736537918999574, -2.062503053667999797 ) ) ;
#35974=ORIENTED_EDGE ( 'NONE', *, *, #15009, .T. ) ;
#35975=DIRECTION ( 'NONE',  ( -1.000000000000000000, 0.000000000000000000, 0.000000000000000000 ) ) ;
#35976=AXIS2_PLACEMENT_3D ( 'NONE', #13268, #40136, #8552 ) ;
#35978=CARTESIAN_POINT ( 'NONE',  ( 3.165411199172027512, -1.229166666666666741, -0.8506806241676553304 ) ) ;
#35979=ADVANCED_FACE ( 'NONE', ( #28760 ), #13720, .F. ) ;
#35980=ORIENTED_EDGE ( 'NONE', *, *, #47517, .T. ) ;
#35981=VECTOR ( 'NONE', #32921, 1000.000000000000114 ) ;
#35982=ORIENTED_EDGE ( 'NONE', *, *, #53777, .T. ) ;
#35983=FACE_OUTER_BOUND ( 'NONE', #27024, .T. ) ;
#35985=ORIENTED_EDGE ( 'NONE', *, *, #48048, .F. ) ;
#35991=FACE_OUTER_BOUND ( 'NONE', #13929, .T. ) ;
#35992=CARTESIAN_POINT ( 'NONE',  ( -1.198731353186000215, -77.11209425748999990, -13.05866524906999970 ) ) ;
#35994=B_SPLINE_CURVE_WITH_KNOTS ( 'NONE', 3,
 ( #11590, #38436, #56453, #16008, #47621, #20726, #47905, #7437, #37560, #55576, #15125, #33123, #58181, #8295, #16585, #44310, #13299, #43750, #31002, #8008, #21010 ),
 .UNSPECIFIED., .F., .F.,
 ( 4, 2, 2, 2, 2, 2, 2, 2, 2, 1, 4 ),
 ( 0.000000000000000000, 0.1249999999999998612, 0.2499999999999998335, 0.3749999999999997780, 0.4999999999999997780, 0.5624999999999997780, 0.6249999999999997780, 0.7499999999999997780, 0.8124999999999998890, 0.8749999999999998890, 1.000000000000000000 ),
 .UNSPECIFIED. ) ;
#36002=CARTESIAN_POINT ( 'NONE',  ( -6.024415200221000077, -76.46769539903000634, 10.73507988388000101 ) ) ;
#36005=CARTESIAN_POINT ( 'NONE',  ( -0.3992292757334167108, -3.465166414414809992, -3.497470143203500026 ) ) ;
#36006=CARTESIAN_POINT ( 'NONE',  ( -9.164374456839587069, -16.78432317405038532, 8.803712804485032350 ) ) ;
#36010=ADVANCED_FACE ( 'NONE', ( #1347, #6337 ), #5463, .T. ) ;
#36012=PLANE ( 'NONE',  #46118 ) ;
#36015=ORIENTED_EDGE ( 'NONE', *, *, #14140, .T. ) ;
#36020=LINE ( 'NONE', #54047, #7994 ) ;
#36025=CARTESIAN_POINT ( 'NONE',  ( 1.750000000000000000, -23.24999999688999708, -12.50000000000000000 ) ) ;
#36026=CARTESIAN_POINT ( 'NONE',  ( 3.900131474043036839, -76.04750243334697757, 11.09005429771401197 ) ) ;
#36037=CARTESIAN_POINT ( 'NONE',  ( 1.980584515756000030, -55.53514849873000259, -12.76303204337999908 ) ) ;
#36039=DIRECTION ( 'NONE',  ( -0.7071067811865475727, 0.000000000000000000, 0.7071067811865475727 ) ) ;
#36040=DIRECTION ( 'NONE',  ( -0.7071067811865474617, 0.000000000000000000, 0.7071067811865474617 ) ) ;
#36041=VERTEX_POINT ( 'NONE', #19340 ) ;
#36051=LINE ( 'NONE', #13613, #17654 ) ;
#36053=DIRECTION ( 'NONE',  ( 0.000000000000000000, 1.000000000000000000, 0.000000000000000000 ) ) ;
#36054=DIRECTION ( 'NONE',  ( -0.7071067811865474617, 0.000000000000000000, 0.7071067811865474617 ) ) ;
#36055=CARTESIAN_POINT ( 'NONE',  ( -12.71759155194429347, -60.86493881542617146, -1.809604648260207727 ) ) ;
#36058=ORIENTED_EDGE ( 'NONE', *, *, #14909, .F. ) ;
#36059=VERTEX_POINT ( 'NONE', #9901 ) ;
#36060=DIRECTION ( 'NONE',  ( -1.000000000000000000, 0.000000000000000000, 0.000000000000000000 ) ) ;
#36063=ORIENTED_EDGE ( 'NONE', *, *, #44473, .T. ) ;
#36064=CARTESIAN_POINT ( 'NONE',  ( -12.10179013622999911, -78.56494648961000848, -1.986401539992999954 ) ) ;
#36066=CARTESIAN_POINT ( 'NONE',  ( 7.969039355681999837, -24.62377467844000023, 9.934746417635000881 ) ) ;
#36068=CARTESIAN_POINT ( 'NONE',  ( 8.107762507645121630, -55.28308356097012677, -7.434020715871730189 ) ) ;
#36081=CARTESIAN_POINT ( 'NONE',  ( -10.01856959424999971, -76.06150170016000800, -8.476471298849000746 ) ) ;
#36084=CARTESIAN_POINT ( 'NONE',  ( 7.710095619854000937, -20.24935285776999905, -10.18496935401000059 ) ) ;
#36088=CARTESIAN_POINT ( 'NONE',  ( -10.52682159650000138, -23.42567232067999683, -7.605689092050000433 ) ) ;
#36089=CARTESIAN_POINT ( 'NONE',  ( 11.79999999988000070, -18.85000000520999919, 0.5999999998848000171 ) ) ;
#36097=CARTESIAN_POINT ( 'NONE',  ( -10.35398565887000011, -18.59211376270000216, 7.619387877927000119 ) ) ;
#36099=CARTESIAN_POINT ( 'NONE',  ( -8.485281374238999419, -55.64999999967000122, -8.485281374238999419 ) ) ;
#36104=CARTESIAN_POINT ( 'NONE',  ( -1.997276839918484148, -1.927083333333333037, 2.598917237794077018 ) ) ;
#36107=CARTESIAN_POINT ( 'NONE',  ( -0.4701041210481999855, -53.79203065542999695, 12.54901038410999980 ) ) ;
#36108=CARTESIAN_POINT ( 'NONE',  ( -1.933650113854000097, -60.20786252993000431, -12.70909635757000089 ) ) ;
#36109=EDGE_CURVE ( 'NONE', #38390, #17250, #7113, .T. ) ;
#36110=CARTESIAN_POINT ( 'NONE',  ( -1.682691453581999896, -2.307097686686999882, -3.413847142597000062 ) ) ;
#36112=DIRECTION ( 'NONE',  ( -0.5721800009715952706, 0.8201280671261930166, 0.000000000000000000 ) ) ;
#36116=CARTESIAN_POINT ( 'NONE',  ( -1.200170490667999967, -61.23405701964999537, 12.43444080554000131 ) ) ;
#36117=FACE_OUTER_BOUND ( 'NONE', #25791, .T. ) ;
#36119=DIRECTION ( 'NONE',  ( 0.7071067811865474617, 0.7071067811865474617, 4.569532939869306191E-09 ) ) ;
#36120=CARTESIAN_POINT ( 'NONE',  ( 10.98582032482000059, -79.21006532114999743, -5.054225604206000533 ) ) ;
#36127=CARTESIAN_POINT ( 'NONE',  ( -12.49830695671999869, -60.00970582242000262, 1.666977511085999897 ) ) ;
#36129=DIRECTION ( 'NONE',  ( 0.7071067811865475727, 0.000000000000000000, 0.7071067811865475727 ) ) ;
#36130=DIRECTION ( 'NONE',  ( 0.6562721000522208081, -0.7545243075561237633, 7.874468564641248377E-10 ) ) ;
#36132=AXIS2_PLACEMENT_3D ( 'NONE', #55075, #14622, #27326 ) ;
#36134=CARTESIAN_POINT ( 'NONE',  ( -0.04193593510302838501, -61.81009741308654526, 12.50649570009192679 ) ) ;
#36136=LINE ( 'NONE', #13694, #58234 ) ;
#36137=VERTEX_POINT ( 'NONE', #54767 ) ;
#36138=ORIENTED_EDGE ( 'NONE', *, *, #18704, .T. ) ;
#36142=CARTESIAN_POINT ( 'NONE',  ( 9.723199427898999048, -54.32306055827000080, -7.958735709912999390 ) ) ;
#36143=ORIENTED_EDGE ( 'NONE', *, *, #45897, .T. ) ;
#36146=CARTESIAN_POINT ( 'NONE',  ( -12.00000000000000000, 0.000000000000000000, 0.000000000000000000 ) ) ;
#36148=CARTESIAN_POINT ( 'NONE',  ( -13.99936781018472232, -32.88214388149999934, -0.1330447863085613691 ) ) ;
#36152=CARTESIAN_POINT ( 'NONE',  ( 8.197900261343999517, -78.42976952347000008, -8.644410496647001452 ) ) ;
#36153=EDGE_LOOP ( 'NONE', ( #3851, #52996, #28695 ) ) ;
#36155=FACE_OUTER_BOUND ( 'NONE', #52701, .T. ) ;
#36157=CARTESIAN_POINT ( 'NONE',  ( -1.779623408236357784, -60.93630868993977856, -12.71471627660551285 ) ) ;
#36161=CARTESIAN_POINT ( 'NONE',  ( -12.75337166745000061, -76.83816582529999550, -1.077318095482000082 ) ) ;
#36162=CARTESIAN_POINT ( 'NONE',  ( -9.533257042556000371, -78.28128649030999497, 6.958047573390000018 ) ) ;
#36166=ADVANCED_FACE ( 'NONE', ( #13361 ), #28352, .F. ) ;
#36169=CARTESIAN_POINT ( 'NONE',  ( -10.21381326472999795, -56.02870851050000311, 7.668949790007999923 ) ) ;
#36170=CARTESIAN_POINT ( 'NONE',  ( 2.956485620267946590, -2.885265340294828729, 1.348054739062900742 ) ) ;
#36172=TOROIDAL_SURFACE ( 'NONE', #11703, 1.250000000000000000, 0.5000000000000000000 ) ;
#36177=CARTESIAN_POINT ( 'NONE',  ( -3.593558748265999636, -1.814443158354000163, 0.1459214154804999997 ) ) ;
#36180=CARTESIAN_POINT ( 'NONE',  ( -0.1610657711387516733, -23.74946977292809080, 10.99997582743960756 ) ) ;
#36183=PLANE ( 'NONE',  #43468 ) ;
#36184=CARTESIAN_POINT ( 'NONE',  ( 1.667961445601999992, -58.54800977479000323, 12.58338334669999981 ) ) ;
#36186=CARTESIAN_POINT ( 'NONE',  ( 5.579996517577999526, -77.35706742927000334, 11.75597208960999929 ) ) ;
#36187=CARTESIAN_POINT ( 'NONE',  ( -7.792426477875908475, -61.09102098674076586, -10.18245125509822380 ) ) ;
#36188=CARTESIAN_POINT ( 'NONE',  ( 12.49168451098999988, -23.29848884437999956, -1.667916687331000070 ) ) ;
#36190=CARTESIAN_POINT ( 'NONE',  ( 8.666925696308020122, -53.80708316136156100, -9.019429295813042202 ) ) ;
#36191=B_SPLINE_CURVE_WITH_KNOTS ( 'NONE', 3,
 ( #52298, #38997, #2711, #52013 ),
 .UNSPECIFIED., .F., .F.,
 ( 4, 4 ),
 ( 0.000000000000000000, 1.000000000000000000 ),
 .UNSPECIFIED. ) ;
#36193=CARTESIAN_POINT ( 'NONE',  ( 7.640030264156999706, -23.30716680861999990, -10.18491080493000212 ) ) ;
#36196=CARTESIAN_POINT ( 'NONE',  ( -3.754890333716000228, -1.380863097740999912, -1.424957469106999941 ) ) ;
#36201=CARTESIAN_POINT ( 'NONE',  ( -11.75000000000000000, -78.70000000000000284, -1.701764645356999850E-14 ) ) ;
#36203=ORIENTED_EDGE ( 'NONE', *, *, #30390, .F. ) ;
#36204=DIRECTION ( 'NONE',  ( 1.000000000000000000, 0.000000000000000000, 0.000000000000000000 ) ) ;
#36205=VECTOR ( 'NONE', #52897, 1000.000000000000000 ) ;
#36213=FACE_OUTER_BOUND ( 'NONE', #35179, .T. ) ;
#36216=DIRECTION ( 'NONE',  ( 0.000000000000000000, 1.000000000000000000, 0.000000000000000000 ) ) ;
#36217=ORIENTED_EDGE ( 'NONE', *, *, #5405, .T. ) ;
#36222=CARTESIAN_POINT ( 'NONE',  ( -0.5999999999999999778, -18.84999999999999787, 10.98362417419999915 ) ) ;
#36224=CARTESIAN_POINT ( 'NONE',  ( -11.75000000000000711, -78.78958333333332575, 1.538071403319954955 ) ) ;
#36225=AXIS2_PLACEMENT_3D ( 'NONE', #23945, #1534, #55838 ) ;
#36230=CARTESIAN_POINT ( 'NONE',  ( 3.075537641221509411, -76.65416666666669698, 11.44417895085272008 ) ) ;
#36232=AXIS2_PLACEMENT_3D ( 'NONE', #46958, #51376, #38070 ) ;
#36235=DIRECTION ( 'NONE',  ( 0.7071067811865475727, 0.000000000000000000, -0.7071067811865475727 ) ) ;
#36236=CARTESIAN_POINT ( 'NONE',  ( -1.389926494651000155, -24.62381336254999908, 12.65988803923000106 ) ) ;
#36238=CARTESIAN_POINT ( 'NONE',  ( 2.426647618366999603E-14, -5.949999999936550488, -12.94999999994000106 ) ) ;
#36239=CARTESIAN_POINT ( 'NONE',  ( -0.7707219435497000282, -1.772058083081000213, 3.880749451301000352 ) ) ;
#36240=DIRECTION ( 'NONE',  ( -0.9999999930530777403, 0.000000000000000000, -0.0001178721535689973885 ) ) ;
#36242=EDGE_CURVE ( 'NONE', #34959, #17250, #19383, .T. ) ;
#36243=DIRECTION ( 'NONE',  ( 0.000000000000000000, 0.000000000000000000, -1.000000000000000000 ) ) ;
#36245=CARTESIAN_POINT ( 'NONE',  ( 12.66313299637999989, -61.97803434819999779, 0.06050769725595000342 ) ) ;
#36247=CARTESIAN_POINT ( 'NONE',  ( -8.096452064242996016, -19.21421830981000056, -13.15643568217000769 ) ) ;
#36252=CARTESIAN_POINT ( 'NONE',  ( 0.000000000000000000, -55.54999999966999980, 12.00000000000000000 ) ) ;
#36255=ORIENTED_EDGE ( 'NONE', *, *, #36357, .T. ) ;
#36264=CARTESIAN_POINT ( 'NONE',  ( -10.07627163191000008, -23.24999999688999708, 7.601397897754999633 ) ) ;
#36265=CARTESIAN_POINT ( 'NONE',  ( 12.66001556632000025, -24.63260856943000121, -1.381621105852999909 ) ) ;
#36267=ORIENTED_EDGE ( 'NONE', *, *, #5783, .T. ) ;
#36268=CARTESIAN_POINT ( 'NONE',  ( -0.5222397221871039052, -53.63701780567495092, -12.70447686579387003 ) ) ;
#36271=CARTESIAN_POINT ( 'NONE',  ( 7.653261585152177027, -75.88086419595920518, -8.963777150644636649 ) ) ;
#36277=TOROIDAL_SURFACE ( 'NONE', #27791, 1.250000000000000000, 0.5000000000000000000 ) ;
#36278=CARTESIAN_POINT ( 'NONE',  ( 8.532660243229310382, -61.92798380502804889, -9.433531203619960337 ) ) ;
#36279=VERTEX_POINT ( 'NONE', #26495 ) ;
#36280=ORIENTED_EDGE ( 'NONE', *, *, #18574, .T. ) ;
#36281=CARTESIAN_POINT ( 'NONE',  ( -8.292781013277000568, -53.74469293044000295, -9.770415148702999986 ) ) ;
#36282=EDGE_CURVE ( 'NONE', #33149, #38390, #51471, .T. ) ;
#36285=EDGE_LOOP ( 'NONE', ( #28853, #20826, #26345, #743 ) ) ;
#36287=CARTESIAN_POINT ( 'NONE',  ( 10.10447584118665887, -24.45118490549160484, -7.864774383118550816 ) ) ;
#36289=ORIENTED_EDGE ( 'NONE', *, *, #39686, .T. ) ;
#36292=CARTESIAN_POINT ( 'NONE',  ( 11.80688451001000061, -77.86523079875999542, 5.334804138346999736 ) ) ;
#36297=ORIENTED_EDGE ( 'NONE', *, *, #13935, .T. ) ;
#36298=CYLINDRICAL_SURFACE ( 'NONE', #12620, 1.750000000000000000 ) ;
#36301=CARTESIAN_POINT ( 'NONE',  ( 1.423904377723752779, -61.10512805135451941, -12.50677628660343110 ) ) ;
#36302=CARTESIAN_POINT ( 'NONE',  ( -1.552255264827246073, -3.260542986159845835, 3.161068809798809554 ) ) ;
#36303=CARTESIAN_POINT ( 'NONE',  ( 12.75763395699000036, -19.22204592323999961, 1.931043742978000077 ) ) ;
#36304=CARTESIAN_POINT ( 'NONE',  ( 10.82405698390000026, -79.34094587766000473, 5.765268246940999930 ) ) ;
#36308=CARTESIAN_POINT ( 'NONE',  ( 4.589427651721361023, -77.39382578420598691, 11.10760103527476517 ) ) ;
#36309=CARTESIAN_POINT ( 'NONE',  ( 10.42531125072000009, -55.53514854654000032, 7.624341767124000135 ) ) ;
#36310=AXIS2_PLACEMENT_3D ( 'NONE', #29929, #6937, #31307 ) ;
#36311=VERTEX_POINT ( 'NONE', #25637 ) ;
#36313=CIRCLE ( 'NONE', #28770, 30.50000000000000355 ) ;
#36314=CYLINDRICAL_SURFACE ( 'NONE', #17384, 1.750000000000000000 ) ;
#36318=AXIS2_PLACEMENT_3D ( 'NONE', #49845, #50427, #46298 ) ;
#36322=CARTESIAN_POINT ( 'NONE',  ( 9.096888433124238560, -76.00412923759679984, 7.436607333932903074 ) ) ;
#36326=CARTESIAN_POINT ( 'NONE',  ( 9.754023262367997660, -76.24778881791411322, -7.509630405475999915 ) ) ;
#36329=DIRECTION ( 'NONE',  ( 0.000000000000000000, 1.000000000000000000, 0.000000000000000000 ) ) ;
#36331=DIRECTION ( 'NONE',  ( 0.000000000000000000, -1.000000000000000000, 0.000000000000000000 ) ) ;
#36332=DIRECTION ( 'NONE',  ( 0.000000000000000000, 0.000000000000000000, -1.000000000000000000 ) ) ;
#36333=ORIENTED_EDGE ( 'NONE', *, *, #20105, .F. ) ;
#36335=CARTESIAN_POINT ( 'NONE',  ( 12.70556836319933858, -53.57227722548668680, 0.2598513551479147976 ) ) ;
#36338=ADVANCED_FACE ( 'NONE', ( #22375 ), #4070, .F. ) ;
#36339=CARTESIAN_POINT ( 'NONE',  ( 11.29148473951573450, -76.42758390997302342, -3.256410895415154716 ) ) ;
#36341=CARTESIAN_POINT ( 'NONE',  ( 12.05000000000000071, -74.80000000000001137, 0.000000000000000000 ) ) ;
#36346=EDGE_CURVE ( 'NONE', #15231, #23858, #30919, .T. ) ;
#36347=AXIS2_PLACEMENT_3D ( 'NONE', #50647, #36750, #24050 ) ;
#36348=PLANE ( 'NONE',  #4511 ) ;
#36349=EDGE_LOOP ( 'NONE', ( #30852, #12256, #53410, #48565 ) ) ;
#36350=ORIENTED_EDGE ( 'NONE', *, *, #2605, .T. ) ;
#36353=ORIENTED_EDGE ( 'NONE', *, *, #35001, .T. ) ;
#36355=CARTESIAN_POINT ( 'NONE',  ( 8.870414880995999951, -25.06963060262999932, 8.878264461096000204 ) ) ;
#36357=EDGE_CURVE ( 'NONE', #36570, #32986, #49561, .T. ) ;
#36358=DIRECTION ( 'NONE',  ( 0.000000000000000000, 1.000000000000000000, 0.000000000000000000 ) ) ;
#36363=EDGE_CURVE ( 'NONE', #55676, #16697, #35055, .T. ) ;
#36364=ORIENTED_EDGE ( 'NONE', *, *, #30558, .T. ) ;
#36365=CARTESIAN_POINT ( 'NONE',  ( -7.764217752274555018, -24.25600304964931198, 10.21028588416213800 ) ) ;
#36366=ORIENTED_EDGE ( 'NONE', *, *, #37862, .T. ) ;
#36369=CYLINDRICAL_SURFACE ( 'NONE', #23441, 1.750000000000001332 ) ;
#36371=CARTESIAN_POINT ( 'NONE',  ( -9.702684712557999802, -76.47625438773999917, -8.600453018952999074 ) ) ;
#36374=DIRECTION ( 'NONE',  ( 1.000000000000000000, 0.000000000000000000, 0.000000000000000000 ) ) ;
#36376=CARTESIAN_POINT ( 'NONE',  ( -9.963467980702999327, -23.68274967071999981, -7.659239661648999942 ) ) ;
#36377=CARTESIAN_POINT ( 'NONE',  ( 12.64502302236999931, -59.57129148919000272, -1.799490220168999954 ) ) ;
#36385=CARTESIAN_POINT ( 'NONE',  ( 0.000000000000000000, 4.040000000000000036, 0.000000000000000000 ) ) ;
#36386=CARTESIAN_POINT ( 'NONE',  ( -0.7999999999999001243, -18.84999999997999964, -12.00000000000000000 ) ) ;
#36387=DIRECTION ( 'NONE',  ( -1.147001872821000084E-14, 0.000000000000000000, 1.000000000000000000 ) ) ;
#36389=CARTESIAN_POINT ( 'NONE',  ( 10.35747145894000099, -60.11584731951999316, -7.626500777253000685 ) ) ;
#36390=B_SPLINE_CURVE_WITH_KNOTS ( 'NONE', 3,
 ( #43911, #21462, #16462, #25309, #26178, #7597 ),
 .UNSPECIFIED., .F., .F.,
 ( 4, 1, 1, 4 ),
 ( 0.000000000000000000, 0.3333333333333000081, 0.6666666666667000474, 1.000000000000000000 ),
 .UNSPECIFIED. ) ;
#36393=CARTESIAN_POINT ( 'NONE',  ( -12.50000000000000000, -55.54999999966999980, 0.000000000000000000 ) ) ;
#36394=ORIENTED_EDGE ( 'NONE', *, *, #47117, .F. ) ;
#36395=CARTESIAN_POINT ( 'NONE',  ( 10.13881649148000008, -76.90783510652001098, -5.938594122520999719 ) ) ;
#36397=DIRECTION ( 'NONE',  ( -0.7071067811865475727, 0.000000000000000000, -0.7071067811865475727 ) ) ;
#36404=CARTESIAN_POINT ( 'NONE',  ( 12.54673279573000144, -17.17202488779000191, 0.9078290272347999679 ) ) ;
#36405=AXIS2_PLACEMENT_3D ( 'NONE', #571, #22073, #22677 ) ;
#36408=CARTESIAN_POINT ( 'NONE',  ( 9.906487715838999009, -79.19307150910000814, -7.400253471101999381 ) ) ;
#36409=VECTOR ( 'NONE', #44164, 1000.000000000000000 ) ;
#36414=DIRECTION ( 'NONE',  ( 0.9999999924279686647, 0.000000000000000000, 0.0001230612157835738363 ) ) ;
#36415=CARTESIAN_POINT ( 'NONE',  ( -12.65989858210999941, -61.74344101100000159, 0.9743214026256999949 ) ) ;
#36417=CARTESIAN_POINT ( 'NONE',  ( 12.60354432325999952, -19.24899162885999715, -1.750000000000000000 ) ) ;
#36419=EDGE_LOOP ( 'NONE', ( #48802, #50271, #17628, #35232, #813, #7098 ) ) ;
#36421=ADVANCED_FACE ( 'NONE', ( #35348 ), #44827, .F. ) ;
#36424=CARTESIAN_POINT ( 'NONE',  ( 7.892048199458332469, -55.05053022673563135, 7.664266801482971125 ) ) ;
#36430=ORIENTED_EDGE ( 'NONE', *, *, #45794, .T. ) ;
#36431=CARTESIAN_POINT ( 'NONE',  ( -1.667260628941999778, -18.79057987526000062, 12.49858003894999925 ) ) ;
#36432=LINE ( 'NONE', #53570, #4649 ) ;
#36435=CARTESIAN_POINT ( 'NONE',  ( 9.722718241315000398, -55.54999999966999980, -7.954951288349001004 ) ) ;
#36436=CARTESIAN_POINT ( 'NONE',  ( -11.91126960539999935, -78.74591742231000069, -0.2303430570443000258 ) ) ;
#36438=EDGE_LOOP ( 'NONE', ( #20994, #26243, #40037, #53317 ) ) ;
#36439=EDGE_LOOP ( 'NONE', ( #44204, #29190, #2884, #18287, #35150, #2974 ) ) ;
#36440=CARTESIAN_POINT ( 'NONE',  ( -12.52582254647393611, -18.19059700816967151, -1.680974932933145816 ) ) ;
#36441=AXIS2_PLACEMENT_3D ( 'NONE', #33605, #16483, #20621 ) ;
#36447=CARTESIAN_POINT ( 'NONE',  ( -12.91626791057999846, -77.42478844368000068, -1.016208772393999871 ) ) ;
#36449=CARTESIAN_POINT ( 'NONE',  ( -12.82904091339000097, -23.32452529362999982, -2.062673488738000049 ) ) ;
#36451=DIRECTION ( 'NONE',  ( 0.000000000000000000, 0.000000000000000000, 1.000000000000000000 ) ) ;
#36453=CONICAL_SURFACE ( 'NONE', #10089, 0.6999999997695000031, 0.7853981633972997312 ) ;
#36456=CARTESIAN_POINT ( 'NONE',  ( -11.06835501100700014, -78.27189007101333118, 4.078077733570931507 ) ) ;
#36459=DIRECTION ( 'NONE',  ( -4.762546956201999894E-11, -1.000000000000000000, -4.762495317921000031E-11 ) ) ;
#36461=CARTESIAN_POINT ( 'NONE',  ( 3.594201416108000036, -3.094009561889999649, 1.252117639952999850 ) ) ;
#36464=CYLINDRICAL_SURFACE ( 'NONE', #4637, 14.00000000000000000 ) ;
#36465=CARTESIAN_POINT ( 'NONE',  ( 8.190859204290999784, -59.94999999967000548, -7.342331066867000544 ) ) ;
#36469=CARTESIAN_POINT ( 'NONE',  ( -1.189541931187000134, -77.10038219874999754, -12.95855809378999979 ) ) ;
#36473=CARTESIAN_POINT ( 'NONE',  ( 10.31003757212999972, -76.29231484251999973, 7.089603455708999746 ) ) ;
#36474=VERTEX_POINT ( 'NONE', #17073 ) ;
#36475=CARTESIAN_POINT ( 'NONE',  ( 0.000000000000000000, -13.07071424677999971, 0.000000000000000000 ) ) ;
#36478=CARTESIAN_POINT ( 'NONE',  ( 7.682344222570999470, -22.76462890193000277, -10.04116292115999975 ) ) ;
#36481=CARTESIAN_POINT ( 'NONE',  ( -3.161392481395000065, -1.817959338694000060, -1.501864700490999960 ) ) ;
#36482=DIRECTION ( 'NONE',  ( 0.000000000000000000, 1.000000000000000000, 0.000000000000000000 ) ) ;
#36484=VERTEX_POINT ( 'NONE', #57229 ) ;
#36489=AXIS2_PLACEMENT_3D ( 'NONE', #28100, #23398, #46150 ) ;
#36490=ORIENTED_EDGE ( 'NONE', *, *, #14, .F. ) ;
#36493=DIRECTION ( 'NONE',  ( -1.000000000000000000, 0.000000000000000000, 0.000000000000000000 ) ) ;
#36494=VECTOR ( 'NONE', #50115, 1000.000000000000114 ) ;
#36495=ORIENTED_EDGE ( 'NONE', *, *, #28273, .T. ) ;
#36496=EDGE_CURVE ( 'NONE', #6364, #9689, #44403, .T. ) ;
#36500=EDGE_LOOP ( 'NONE', ( #3184, #8006, #48349, #51854, #20451 ) ) ;
#36501=CARTESIAN_POINT ( 'NONE',  ( -0.8304832018632568591, -2.705794687591313252, -3.142888880824831421 ) ) ;
#36507=ADVANCED_FACE ( 'NONE', ( #41268 ), #36830, .F. ) ;
#36508=ORIENTED_EDGE ( 'NONE', *, *, #51824, .T. ) ;
#36519=CARTESIAN_POINT ( 'NONE',  ( -13.86363636363000218, -9.638971321655001034, -1.277887488715999925E-05 ) ) ;
#36522=DIRECTION ( 'NONE',  ( 1.000000000000000000, 0.000000000000000000, 0.000000000000000000 ) ) ;
#36526=CARTESIAN_POINT ( 'NONE',  ( -12.44209697062000153, -17.91557297456000342, 1.464771213333999844 ) ) ;
#36527=DIRECTION ( 'NONE',  ( 0.4045837979902123238, 0.8201365135193228184, 0.4045837979902123238 ) ) ;
#36528=CARTESIAN_POINT ( 'NONE',  ( 1.477284502223000118, -24.72631500296999718, 12.77254812468999923 ) ) ;
#36530=CARTESIAN_POINT ( 'NONE',  ( -3.335732572513999905, -0.7444651668207999951, 2.419625153821000296 ) ) ;
#36532=AXIS2_PLACEMENT_3D ( 'NONE', #12744, #377, #4187 ) ;
#36533=CARTESIAN_POINT ( 'NONE',  ( 12.72923908218245082, -23.77554307155166313, -1.930512971245056386 ) ) ;
#36542=CARTESIAN_POINT ( 'NONE',  ( 7.624341766639000539, -23.26485146254000114, 10.42531125024000005 ) ) ;
#36544=CARTESIAN_POINT ( 'NONE',  ( 0.000000000000000000, -46.09579702914000165, 0.000000000000000000 ) ) ;
#36551=FACE_OUTER_BOUND ( 'NONE', #47856, .T. ) ;
#36554=CARTESIAN_POINT ( 'NONE',  ( 12.66232176271000043, -53.66513311386999874, -0.5079086068997000769 ) ) ;
#36556=CARTESIAN_POINT ( 'NONE',  ( 3.849498977080000106, -0.9616681123999000214, -0.3332954958730999784 ) ) ;
#36562=CARTESIAN_POINT ( 'NONE',  ( 6.159268256616873494, -75.86834440890064002, -10.04771440447366615 ) ) ;
#36564=CARTESIAN_POINT ( 'NONE',  ( -12.71658889739000031, -55.48415522678000400, -1.931087888049999979 ) ) ;
#36569=CARTESIAN_POINT ( 'NONE',  ( -1.799475295154000065, -20.24916621771999914, 12.69619287815999975 ) ) ;
#36570=VERTEX_POINT ( 'NONE', #41851 ) ;
#36575=EDGE_CURVE ( 'NONE', #50457, #32275, #1139, .T. ) ;
#36576=CARTESIAN_POINT ( 'NONE',  ( 7.635939347796300680, -23.77525282322134359, -10.36595956260444673 ) ) ;
#36578=EDGE_CURVE ( 'NONE', #23569, #1101, #49601, .T. ) ;
#36581=AXIS2_PLACEMENT_3D ( 'NONE', #48185, #7431, #24860 ) ;
#36583=CARTESIAN_POINT ( 'NONE',  ( 5.555615362064000529, -77.42119367106998595, 11.70460571637999969 ) ) ;
#36586=B_SPLINE_CURVE_WITH_KNOTS ( 'NONE', 3,
 ( #10803, #37060, #55078, #32910 ),
 .UNSPECIFIED., .F., .F.,
 ( 4, 4 ),
 ( 0.000000000000000000, 1.000000000000000000 ),
 .UNSPECIFIED. ) ;
#36588=EDGE_LOOP ( 'NONE', ( #16693, #15649, #13034 ) ) ;
#36590=CARTESIAN_POINT ( 'NONE',  ( -3.438348731682000281, -76.58513991147000866, -11.82003900998999946 ) ) ;
#36592=CARTESIAN_POINT ( 'NONE',  ( 1.942972292769964193, -2.177744011644287436, 2.933851992493632821 ) ) ;
#36593=EDGE_CURVE ( 'NONE', #52871, #51923, #52421, .T. ) ;
#36594=CARTESIAN_POINT ( 'NONE',  ( 7.758897894450000443, -61.10081253415999925, -10.31443085085999911 ) ) ;
#36595=CARTESIAN_POINT ( 'NONE',  ( 11.93255069029000026, -79.24879777483999987, -2.830763026309000008 ) ) ;
#36597=CARTESIAN_POINT ( 'NONE',  ( 12.70556836347999941, -16.77227722772000007, -1.774194455291999869E-09 ) ) ;
#36599=DIRECTION ( 'NONE',  ( 0.000000000000000000, 1.000000000000000000, 0.000000000000000000 ) ) ;
#36600=CARTESIAN_POINT ( 'NONE',  ( -10.16130211225899771, -76.39871602286838481, 8.152202769023755735 ) ) ;
#36601=B_SPLINE_SURFACE_WITH_KNOTS ( 'NONE', 3, 3, ( 
 ( #51566, #14938, #28806, #2261 ),
 ( #1980, #50979, #52138, #10531 ),
 ( #5795, #28213, #28513, #20262 ),
 ( #38253, #42990, #46271, #41816 ),
 ( #1391, #19672, #19386, #46563 ),
 ( #6087, #1682, #19975, #37672 ),
 ( #55690, #37960, #55987, #16700 ),
 ( #49371, #40206, #52711, #12263 ) ),
 .UNSPECIFIED., .F., .F., .F.,
 ( 4, 1, 1, 1, 1, 4 ),
 ( 4, 4 ),
 ( -0.01200407345745999922, 0.000000000000000000, 0.3333333333333000081, 0.6666666666667000474, 1.000000000000000000, 1.011997855551999947 ),
 ( -0.3559705542741999906, 1.355970554273999928 ),
 .UNSPECIFIED. ) ;
#36608=EDGE_CURVE ( 'NONE', #40639, #15436, #54843, .T. ) ;
#36613=CARTESIAN_POINT ( 'NONE',  ( 4.556417092236462629, -76.04278103528405097, 10.83029532527294414 ) ) ;
#36616=ORIENTED_EDGE ( 'NONE', *, *, #34756, .T. ) ;
#36617=EDGE_CURVE ( 'NONE', #52202, #19448, #45901, .T. ) ;
#36618=CARTESIAN_POINT ( 'NONE',  ( 3.295079792876998592, -76.40343702272410553, 11.86077433336000020 ) ) ;
#36621=CARTESIAN_POINT ( 'NONE',  ( -5.157220473068041322, -76.28856089857794132, -10.55843506099110485 ) ) ;
#36626=CARTESIAN_POINT ( 'NONE',  ( 9.643342484277001248, -17.05965044154000054, -8.260141428683001052 ) ) ;
#36627=CARTESIAN_POINT ( 'NONE',  ( 1.247385803315000041, -61.27722255996999934, 12.50301438880000049 ) ) ;
#36635=FACE_OUTER_BOUND ( 'NONE', #19656, .T. ) ;
#36636=DIRECTION ( 'NONE',  ( 0.000000000000000000, 0.000000000000000000, 1.000000000000000000 ) ) ;
#36637=DIRECTION ( 'NONE',  ( 1.000000000000000000, 0.000000000000000000, 0.000000000000000000 ) ) ;
#36640=CARTESIAN_POINT ( 'NONE',  ( -11.75000000000000000, -76.70000000000000284, 1.487410190129999909E-14 ) ) ;
#36646=CYLINDRICAL_SURFACE ( 'NONE', #41596, 3.250000000000000000 ) ;
#36647=CARTESIAN_POINT ( 'NONE',  ( 10.47513974133999959, -23.80361494181999760, 7.624776006159999397 ) ) ;
#36648=VECTOR ( 'NONE', #50719, 1000.000000000000000 ) ;
#36649=CARTESIAN_POINT ( 'NONE',  ( 9.636781270596999960, -61.24031362749000351, 7.948066289865000300 ) ) ;
#36650=FACE_OUTER_BOUND ( 'NONE', #50614, .T. ) ;
#36654=ORIENTED_EDGE ( 'NONE', *, *, #17049, .F. ) ;
#36655=CARTESIAN_POINT ( 'NONE',  ( -7.635939347796300680, -23.77525282322134359, 10.36595956260444673 ) ) ;
#36662=CARTESIAN_POINT ( 'NONE',  ( -8.385806979697797203, -17.11189753004796898, 9.298530586711937218 ) ) ;
#36664=EDGE_CURVE ( 'NONE', #19368, #43853, #27961, .T. ) ;
#36665=DIRECTION ( 'NONE',  ( 0.000000000000000000, -1.000000000000000000, 0.000000000000000000 ) ) ;
#36667=CARTESIAN_POINT ( 'NONE',  ( 7.674627477105999240, -22.75077028084999853, -10.14950121126000049 ) ) ;
#36669=ADVANCED_FACE ( 'NONE', ( #54565 ), #9056, .F. ) ;
#36670=CARTESIAN_POINT ( 'NONE',  ( 12.71162862753478962, -61.03964265605992523, 1.720599174757304395 ) ) ;
#36671=FACE_OUTER_BOUND ( 'NONE', #34599, .T. ) ;
#36673=ORIENTED_EDGE ( 'NONE', *, *, #8641, .T. ) ;
#36677=CARTESIAN_POINT ( 'NONE',  ( -2.839805762151343949, -3.458333333333332593, 1.636761686205412181 ) ) ;
#36678=CARTESIAN_POINT ( 'NONE',  ( -1.749722766154200304, -60.27588992799915957, -12.54673760685751027 ) ) ;
#36679=CARTESIAN_POINT ( 'NONE',  ( -0.3094144670187705670, -2.631516015699587818, 3.770305080625714123 ) ) ;
#36684=DIRECTION ( 'NONE',  ( 1.000000000000000000, 0.000000000000000000, 0.000000000000000000 ) ) ;
#36687=EDGE_CURVE ( 'NONE', #37820, #42621, #10269, .T. ) ;
#36689=CARTESIAN_POINT ( 'NONE',  ( 3.808251865168000183, -2.578157913353000374, 1.108301075316999951 ) ) ;
#36692=CARTESIAN_POINT ( 'NONE',  ( 7.631896413330000684, -23.22122715205999555, -10.36221694966999962 ) ) ;
#36693=DIRECTION ( 'NONE',  ( 0.000000000000000000, 0.000000000000000000, -1.000000000000000000 ) ) ;
#36695=CARTESIAN_POINT ( 'NONE',  ( -7.635939924807771284, -55.02474192253894358, -10.36595855974767488 ) ) ;
#36697=TOROIDAL_SURFACE ( 'NONE', #15029, 13.50000000000000000, 0.5000000000000000000 ) ;
#36699=EDGE_CURVE ( 'NONE', #33164, #26175, #853, .T. ) ;
#36700=CARTESIAN_POINT ( 'NONE',  ( 10.30457855490000085, -55.03665569380999756, -7.636266480997000450 ) ) ;
#36708=DIRECTION ( 'NONE',  ( 0.9999999999995751176, 0.000000000000000000, 9.217554803169769657E-07 ) ) ;
#36718=ORIENTED_EDGE ( 'NONE', *, *, #38712, .T. ) ;
#36720=ORIENTED_EDGE ( 'NONE', *, *, #15787, .F. ) ;
#36721=ORIENTED_EDGE ( 'NONE', *, *, #47602, .F. ) ;
#36722=CARTESIAN_POINT ( 'NONE',  ( -1.801750019963999971, -18.60992573277999895, 12.59656967653999970 ) ) ;
#36727=DIRECTION ( 'NONE',  ( 0.000000000000000000, -1.000000000000000000, 0.000000000000000000 ) ) ;
#36728=CARTESIAN_POINT ( 'NONE',  ( 11.73609379742999970, -79.06292401665000114, -2.784157491330999878 ) ) ;
#36729=EDGE_LOOP ( 'NONE', ( #48188, #15526, #32285, #2894, #51490 ) ) ;
#36733=CARTESIAN_POINT ( 'NONE',  ( -12.76303204291999904, -55.53514849259999409, -1.980584515756000030 ) ) ;
#36735=DIRECTION ( 'NONE',  ( 0.000000000000000000, 0.000000000000000000, -1.000000000000000000 ) ) ;
#36736=CARTESIAN_POINT ( 'NONE',  ( -10.38646360831000059, -19.22204592323999961, 7.655555357453000198 ) ) ;
#36737=CARTESIAN_POINT ( 'NONE',  ( -9.186177604835998878, -77.89275400357000478, -8.911975928459002105 ) ) ;
#36741=CARTESIAN_POINT ( 'NONE',  ( 0.005922634313507149466, -76.57483508499620939, 11.74990209218339743 ) ) ;
#36744=CONICAL_SURFACE ( 'NONE', #29194, 11.96250000010999948, 0.7853981633972997312 ) ;
#36746=CARTESIAN_POINT ( 'NONE',  ( 2.994436520183920258, -2.882819031401844700, 1.261580605330494098 ) ) ;
#36750=DIRECTION ( 'NONE',  ( 0.000000000000000000, 1.000000000000000000, 0.000000000000000000 ) ) ;
#36752=ORIENTED_EDGE ( 'NONE', *, *, #24164, .F. ) ;
#36754=EDGE_CURVE ( 'NONE', #38883, #11264, #47265, .T. ) ;
#36756=CARTESIAN_POINT ( 'NONE',  ( 7.958763980604000032, -17.52301961031999866, 9.723170659100999202 ) ) ;
#36758=CARTESIAN_POINT ( 'NONE',  ( -12.97295173694999981, -77.45424801882001020, -1.020668466325000079 ) ) ;
#36760=DIRECTION ( 'NONE',  ( 0.000000000000000000, 0.000000000000000000, 1.000000000000000000 ) ) ;
#36761=CARTESIAN_POINT ( 'NONE',  ( 11.62735544928448483, -78.45878212527921391, 1.746294367094141764 ) ) ;
#36763=CARTESIAN_POINT ( 'NONE',  ( 12.76303204525000012, -60.06485147653999945, 1.980584515753000208 ) ) ;
#36765=EDGE_CURVE ( 'NONE', #49440, #39336, #40220, .T. ) ;
#36768=CARTESIAN_POINT ( 'NONE',  ( 7.718368845776000242, -21.74800977511999989, -10.07722254365999959 ) ) ;
#36771=CARTESIAN_POINT ( 'NONE',  ( -3.431352783032999731, -1.239182682365999932, 2.086989923523999924 ) ) ;
#36778=VERTEX_POINT ( 'NONE', #2865 ) ;
#36782=ORIENTED_EDGE ( 'NONE', *, *, #2056, .T. ) ;
#36784=ADVANCED_FACE ( 'NONE', ( #51600 ), #24429, .F. ) ;
#36785=ORIENTED_EDGE ( 'NONE', *, *, #19076, .F. ) ;
#36787=VERTEX_POINT ( 'NONE', #28838 ) ;
#36788=VECTOR ( 'NONE', #53273, 1000.000000000000000 ) ;
#36789=CARTESIAN_POINT ( 'NONE',  ( -0.9863005837836278378, -2.701660951675892708, -3.096296943042188499 ) ) ;
#36791=EDGE_LOOP ( 'NONE', ( #35306, #39913, #9348, #49024, #41041, #7143 ) ) ;
#36795=CARTESIAN_POINT ( 'NONE',  ( -10.12290050256999940, -18.75000002239000096, -7.648026768411000376 ) ) ;
#36797=CARTESIAN_POINT ( 'NONE',  ( 10.42531125068999920, -23.26485145404000221, -7.624341767093000044 ) ) ;
#36802=DIRECTION ( 'NONE',  ( -1.000000000000000000, 0.000000000000000000, 0.000000000000000000 ) ) ;
#36803=CARTESIAN_POINT ( 'NONE',  ( 13.89248035986000041, -46.40840747658999277, 2.632528379853999966E-05 ) ) ;
#36806=CARTESIAN_POINT ( 'NONE',  ( 6.299964168848140922, -76.52989574100779180, 9.922046080742738638 ) ) ;
#36807=AXIS2_PLACEMENT_3D ( 'NONE', #22388, #50154, #36842 ) ;
#36808=CARTESIAN_POINT ( 'NONE',  ( 0.1610657711267718117, -23.74946977292816186, -10.99997582743960578 ) ) ;
#36812=CARTESIAN_POINT ( 'NONE',  ( -1.538071403320043551, -76.68541666666665435, 11.74999999999999467 ) ) ;
#36815=DIRECTION ( 'NONE',  ( 0.000000000000000000, 1.000000000000000000, 0.000000000000000000 ) ) ;
#36818=LINE ( 'NONE', #55123, #57217 ) ;
#36820=CARTESIAN_POINT ( 'NONE',  ( -3.533965481030999722, -1.844405165121999923, 1.774394495578000219 ) ) ;
#36821=EDGE_CURVE ( 'NONE', #32447, #44781, #10697, .T. ) ;
#36823=CARTESIAN_POINT ( 'NONE',  ( 10.07722254367000048, -58.54800977479000323, 7.718368845781999887 ) ) ;
#36824=CARTESIAN_POINT ( 'NONE',  ( -1.629367637659999923, -23.68263643397999729, -12.46114270826000059 ) ) ;
#36825=EDGE_CURVE ( 'NONE', #53933, #17027, #13669, .T. ) ;
#36827=LINE ( 'NONE', #5250, #542 ) ;
#36828=CARTESIAN_POINT ( 'NONE',  ( -8.485281374238999419, -18.75000000000000000, -8.485281374238999419 ) ) ;
#36830=CYLINDRICAL_SURFACE ( 'NONE', #1521, 1.750000000000001332 ) ;
#36831=CARTESIAN_POINT ( 'NONE',  ( -7.624341766656999475, -60.06485146221000093, -10.42531125026000005 ) ) ;
#36841=CARTESIAN_POINT ( 'NONE',  ( 12.66316398243999863, -53.62133896622000151, 0.04044089952533000409 ) ) ;
#36842=DIRECTION ( 'NONE',  ( 1.000000000000000000, 0.000000000000000000, 0.000000000000000000 ) ) ;
#36843=CARTESIAN_POINT ( 'NONE',  ( -0.6556216971886000833, -0.8299739483179999766, -3.808213771107999968 ) ) ;
#36848=CARTESIAN_POINT ( 'NONE',  ( -11.75000000000000000, -77.20000000000000284, -1.435311119447000145E-14 ) ) ;
#36850=B_SPLINE_CURVE_WITH_KNOTS ( 'NONE', 3,
 ( #11599, #29860, #52328, #8016, #29287, #47632, #7155, #16313, #52613, #47336, #25156, #43182, #7447, #38734, #44039, #34294, #43466, #56753, #20164, #48200, #11883, #43758, #6865, #39312 ),
 .UNSPECIFIED., .F., .F.,
 ( 4, 2, 2, 2, 2, 2, 2, 2, 2, 2, 2, 4 ),
 ( 0.000000000000000000, 0.1249999999999986400, 0.2499999999999972800, 0.3749999999999958922, 0.4374999999999955036, 0.4999999999999951150, 0.6249999999999954481, 0.7499999999999956701, 0.8124999999999944489, 0.8437499999999938938, 0.8749999999999933387, 1.000000000000000000 ),
 .UNSPECIFIED. ) ;
#36851=CARTESIAN_POINT ( 'NONE',  ( -12.69619287815999975, -57.04916621739000249, -1.799475295154000065 ) ) ;
#36853=EDGE_LOOP ( 'NONE', ( #24329, #15592, #13915, #52667, #57855 ) ) ;
#36854=AXIS2_PLACEMENT_3D ( 'NONE', #4026, #34443, #35304 ) ;
#36857=CARTESIAN_POINT ( 'NONE',  ( -1.930989179114000143, -21.75453807238000081, 12.80896991324000034 ) ) ;
#36862=ORIENTED_EDGE ( 'NONE', *, *, #19623, .F. ) ;
#36863=CARTESIAN_POINT ( 'NONE',  ( -12.00000000000000000, -23.25000000000000000, 0.000000000000000000 ) ) ;
#36864=DIRECTION ( 'NONE',  ( -0.7071067811865474617, 0.000000000000000000, -0.7071067811865474617 ) ) ;
#36866=CARTESIAN_POINT ( 'NONE',  ( -12.57434559697999887, -23.71110719500000030, -1.760800161976000089 ) ) ;
#36867=ORIENTED_EDGE ( 'NONE', *, *, #22940, .F. ) ;
#36871=CARTESIAN_POINT ( 'NONE',  ( -0.1380878922993147850, -16.77265597675732423, -12.70555840932534508 ) ) ;
#36872=CARTESIAN_POINT ( 'NONE',  ( -9.546815224142999767, -17.31472046677999899, -8.130854305520999858 ) ) ;
#36873=B_SPLINE_CURVE_WITH_KNOTS ( 'NONE', 3,
 ( #48661, #49840, #270, #49240, #17949, #18540 ),
 .UNSPECIFIED., .F., .F.,
 ( 4, 1, 1, 4 ),
 ( 0.000000000000000000, 0.3333333333333000081, 0.6666666666667000474, 1.000000000000000000 ),
 .UNSPECIFIED. ) ;
#36879=CARTESIAN_POINT ( 'NONE',  ( -12.19234209666000091, -76.02834339985999179, -1.697737568323999913 ) ) ;
#36881=CARTESIAN_POINT ( 'NONE',  ( -2.606762920072624556, -2.407945368431018807, -2.366633524576750247 ) ) ;
#36882=CARTESIAN_POINT ( 'NONE',  ( 12.71658889741000031, -18.68415522710999710, 1.931087888049999979 ) ) ;
#36883=CARTESIAN_POINT ( 'NONE',  ( -7.421655993048999811, -78.40939100203998180, 9.763070719336001346 ) ) ;
#36884=CARTESIAN_POINT ( 'NONE',  ( -1.750000000001000089, -19.24922971542000028, 12.60356226396999979 ) ) ;
#36886=CARTESIAN_POINT ( 'NONE',  ( 9.998727717550137228, -60.72738947565300549, -7.709134076929346158 ) ) ;
#36887=CARTESIAN_POINT ( 'NONE',  ( 4.105073526112258619, -77.20258383217594655, -11.34720543678841231 ) ) ;
#36888=CARTESIAN_POINT ( 'NONE',  ( -9.931063219235598538, -17.87724209356603566, 7.763994033422829233 ) ) ;
#36890=CARTESIAN_POINT ( 'NONE',  ( 0.000000000000000000, -18.75000000000000000, 12.00000000000000000 ) ) ;
#36893=CARTESIAN_POINT ( 'NONE',  ( 7.712213536729100483, -24.06179137615005814, 10.27334987165781399 ) ) ;
#36899=CARTESIAN_POINT ( 'NONE',  ( 8.452817831826150652, -76.01051698363419007, 8.161467144352542391 ) ) ;
#36902=ORIENTED_EDGE ( 'NONE', *, *, #31899, .F. ) ;
#36903=CARTESIAN_POINT ( 'NONE',  ( 0.5999999999999999778, -18.84999999999999787, -10.98362417419999915 ) ) ;
#36905=EDGE_CURVE ( 'NONE', #378, #19974, #53069, .T. ) ;
#36909=CARTESIAN_POINT ( 'NONE',  ( 1.250000000000000000, -60.04999999966999980, -12.00000000000000000 ) ) ;
#36911=CARTESIAN_POINT ( 'NONE',  ( -1.750000000000000000, -55.55000000278000272, -12.50000000000000000 ) ) ;
#36912=CARTESIAN_POINT ( 'NONE',  ( 8.643969996075000495, -16.74046576158000121, -9.422817222712001950 ) ) ;
#36913=CARTESIAN_POINT ( 'NONE',  ( -12.70556836347999941, -25.22772277227999993, -2.424223956931999920E-09 ) ) ;
#36914=ORIENTED_EDGE ( 'NONE', *, *, #36687, .F. ) ;
#36915=AXIS2_PLACEMENT_3D ( 'NONE', #9707, #23283, #41292 ) ;
#36921=CARTESIAN_POINT ( 'NONE',  ( 11.48314430570033373, -76.43277512481758151, -2.489787879572519458 ) ) ;
#36923=CARTESIAN_POINT ( 'NONE',  ( 3.171758640500000226, -3.532739359372000010, 1.479846994257000059 ) ) ;
#36924=EDGE_CURVE ( 'NONE', #37143, #37146, #56885, .T. ) ;
#36928=ORIENTED_EDGE ( 'NONE', *, *, #7961, .T. ) ;
#36939=CARTESIAN_POINT ( 'NONE',  ( 10.30458248780999853, -60.56332651778999576, 7.636263891343999965 ) ) ;
#36944=VERTEX_POINT ( 'NONE', #15935 ) ;
#36946=ORIENTED_EDGE ( 'NONE', *, *, #39380, .T. ) ;
#36951=AXIS2_PLACEMENT_3D ( 'NONE', #14475, #51964, #20371 ) ;
#36954=CARTESIAN_POINT ( 'NONE',  ( -2.317157120869037801, -2.062400358190874083, -2.314279884217083971 ) ) ;
#36958=CARTESIAN_POINT ( 'NONE',  ( -7.943805570347999279, -24.43402324524999969, -9.641149735076000482 ) ) ;
#36959=CARTESIAN_POINT ( 'NONE',  ( -8.768124086712999699, -59.94999999967000548, 7.919595949288999570 ) ) ;
#36961=VERTEX_POINT ( 'NONE', #20936 ) ;
#36966=CARTESIAN_POINT ( 'NONE',  ( -10.15323015673999940, -17.76919784905000199, 7.760928569209999850 ) ) ;
#36968=CARTESIAN_POINT ( 'NONE',  ( 9.396085398178630754, -78.49791666666665435, -7.220923959705230821 ) ) ;
#36970=CARTESIAN_POINT ( 'NONE',  ( -3.388399644966007873, -2.776263346416080857, -1.176069256401409691 ) ) ;
#36977=ORIENTED_EDGE ( 'NONE', *, *, #16242, .F. ) ;
#36979=CARTESIAN_POINT ( 'NONE',  ( -3.409844804438999954, -1.755159555871000032, -1.689431510286000027 ) ) ;
#36982=CARTESIAN_POINT ( 'NONE',  ( 9.213114944024999531, -25.00524898755999814, -8.533795138592999763 ) ) ;
#36985=CARTESIAN_POINT ( 'NONE',  ( -1.247385801080000078, -24.47722256257000240, -12.50301438876999960 ) ) ;
#36986=CARTESIAN_POINT ( 'NONE',  ( 0.000000000000000000, -0.7781249991808000255, 0.000000000000000000 ) ) ;
#36988=CARTESIAN_POINT ( 'NONE',  ( -7.651147547606000465, -22.76256650325000308, -10.45204383577999963 ) ) ;
#36989=CARTESIAN_POINT ( 'NONE',  ( 8.643969996042999426, -53.54046576124999746, -9.422817222680000881 ) ) ;
#36991=LINE ( 'NONE', #50013, #33301 ) ;
#36998=EDGE_CURVE ( 'NONE', #4635, #26450, #35140, .T. ) ;
#37001=EDGE_CURVE ( 'NONE', #56208, #42344, #52167, .T. ) ;
#37002=TOROIDAL_SURFACE ( 'NONE', #21901, 17.50000000000000000, 5.000000000000000000 ) ;
#37005=ORIENTED_EDGE ( 'NONE', *, *, #55170, .F. ) ;
#37006=ORIENTED_EDGE ( 'NONE', *, *, #18945, .T. ) ;
#37008=ORIENTED_EDGE ( 'NONE', *, *, #18893, .F. ) ;
#37009=ORIENTED_EDGE ( 'NONE', *, *, #8705, .T. ) ;
#37010=CARTESIAN_POINT ( 'NONE',  ( -0.4701041210474999898, -16.99203065576000071, 12.54901038416000070 ) ) ;
#37015=ADVANCED_FACE ( 'NONE', ( #3231 ), #51021, .F. ) ;
#37016=AXIS2_PLACEMENT_3D ( 'NONE', #36986, #28705, #6275 ) ;
#37019=CARTESIAN_POINT ( 'NONE',  ( -1.250000000000000000, -55.54999999966999980, -12.00000000000000000 ) ) ;
#37025=DIRECTION ( 'NONE',  ( 0.000000000000000000, 1.000000000000000000, 0.000000000000000000 ) ) ;
#37027=CARTESIAN_POINT ( 'NONE',  ( 12.00000000000000000, -55.54999999966999980, 0.000000000000000000 ) ) ;
#37029=CARTESIAN_POINT ( 'NONE',  ( -1.316656843623999817, -77.94825864453000008, -12.73088833989999991 ) ) ;
#37032=CARTESIAN_POINT ( 'NONE',  ( -12.92181194099999963, -20.24351820077000141, -2.062502994258999856 ) ) ;
#37037=CARTESIAN_POINT ( 'NONE',  ( -11.75023268171679725, -76.70812393556080622, -1.278857244370948498 ) ) ;
#37041=CARTESIAN_POINT ( 'NONE',  ( -3.370587613551000228, -1.795626005361000033, 0.9429417476038000068 ) ) ;
#37045=CARTESIAN_POINT ( 'NONE',  ( 7.387512494710278155, -60.21532333328941888, -8.150146600852353984 ) ) ;
#37048=CARTESIAN_POINT ( 'NONE',  ( -1.264141272797000060, -77.56525730074000080, -12.95149364859999963 ) ) ;
#37050=AXIS2_PLACEMENT_3D ( 'NONE', #42591, #38143, #42881 ) ;
#37051=DIRECTION ( 'NONE',  ( 0.000000000000000000, 1.000000000000000000, 0.000000000000000000 ) ) ;
#37052=CARTESIAN_POINT ( 'NONE',  ( 11.23127327872411207, -78.47254254513119065, 3.450269100463493999 ) ) ;
#37053=CIRCLE ( 'NONE', #16341, 1.250000000000000444 ) ;
#37056=CARTESIAN_POINT ( 'NONE',  ( -3.815503583757167139, -76.29810812315825785, -11.11946675543801177 ) ) ;
#37060=CARTESIAN_POINT ( 'NONE',  ( -3.288006932140723038, -1.664267874433481786, -0.5432996569361712158 ) ) ;
#37062=DIRECTION ( 'NONE',  ( 0.7071067811865474617, 0.000000000000000000, 0.7071067811865474617 ) ) ;
#37066=EDGE_CURVE ( 'NONE', #12948, #24745, #19116, .T. ) ;
#37067=VERTEX_POINT ( 'NONE', #26504 ) ;
#37071=VERTEX_POINT ( 'NONE', #31517 ) ;
#37075=ORIENTED_EDGE ( 'NONE', *, *, #252, .F. ) ;
#37077=EDGE_LOOP ( 'NONE', ( #7302, #39083, #48217, #2196 ) ) ;
#37080=CARTESIAN_POINT ( 'NONE',  ( -8.768124086712999699, -55.64999999965999677, -7.919595949288999570 ) ) ;
#37082=EDGE_LOOP ( 'NONE', ( #3401, #47324, #42572, #4922 ) ) ;
#37084=VERTEX_POINT ( 'NONE', #49566 ) ;
#37085=CARTESIAN_POINT ( 'NONE',  ( 1.423904377506844954, -17.69487194798980667, 12.50677628656596774 ) ) ;
#37086=FACE_OUTER_BOUND ( 'NONE', #12319, .T. ) ;
#37088=AXIS2_PLACEMENT_3D ( 'NONE', #21869, #21587, #38726 ) ;
#37089=DIRECTION ( 'NONE',  ( -0.9957542217973148757, 0.04890179604796068835, 0.07798810240099117441 ) ) ;
#37092=CARTESIAN_POINT ( 'NONE',  ( -8.060180467139032245, -24.62064870851448006, 9.621709426110552243 ) ) ;
#37093=VECTOR ( 'NONE', #15651, 1000.000000000000000 ) ;
#37095=CARTESIAN_POINT ( 'NONE',  ( -7.682331425190000118, -59.56486430393999854, -10.04115011118999945 ) ) ;
#37097=CARTESIAN_POINT ( 'NONE',  ( 6.575652215500655373, -76.52754343095485012, 9.737607018781540447 ) ) ;
#37101=CARTESIAN_POINT ( 'NONE',  ( -11.51674459389547955, -77.97731020001086222, -3.622551337281552097 ) ) ;
#37106=CARTESIAN_POINT ( 'NONE',  ( 12.99510751537000353, -52.49705297113997204, 6.911973076623003642 ) ) ;
#37109=CARTESIAN_POINT ( 'NONE',  ( -10.30458248780999853, -60.56332651778999576, -7.636263891343999965 ) ) ;
#37111=CARTESIAN_POINT ( 'NONE',  ( 12.70457891999001987, -25.17873330329356918, -0.5105076820880790622 ) ) ;
#37114=CARTESIAN_POINT ( 'NONE',  ( 0.2672301082454999754, -3.175485789881999921, -3.475315813263000209 ) ) ;
#37115=CARTESIAN_POINT ( 'NONE',  ( -8.114920487384752690, -24.82884529334158685, -9.847900218102966008 ) ) ;
#37119=DIRECTION ( 'NONE',  ( 0.000000000000000000, 0.000000000000000000, 1.000000000000000000 ) ) ;
#37120=B_SPLINE_CURVE_WITH_KNOTS ( 'NONE', 3,
 ( #51698, #20103, #56115, #37804, #1814, #2388 ),
 .UNSPECIFIED., .F., .F.,
 ( 4, 1, 1, 4 ),
 ( 0.000000000000000000, 0.3333333333333000081, 0.6666666666667000474, 1.000000000000000000 ),
 .UNSPECIFIED. ) ;
#37121=CARTESIAN_POINT ( 'NONE',  ( 1.933650113854000097, -60.20786252993000431, 12.70909635757000089 ) ) ;
#37124=VERTEX_POINT ( 'NONE', #37131 ) ;
#37126=CONICAL_SURFACE ( 'NONE', #11691, 0.6999999997695030007, 0.7853981633972997312 ) ;
#37128=CARTESIAN_POINT ( 'NONE',  ( -7.764005369055772654, -17.87720632479159022, -9.931049915325859345 ) ) ;
#37131=CARTESIAN_POINT ( 'NONE',  ( -1.164828128805999992E-14, -72.70000000000000284, -13.99999999999998401 ) ) ;
#37133=CARTESIAN_POINT ( 'NONE',  ( 2.359810653458999763, -0.8958210303590000700, -3.059514552098999918 ) ) ;
#37135=VECTOR ( 'NONE', #49448, 1000.000000000000000 ) ;
#37137=ORIENTED_EDGE ( 'NONE', *, *, #33394, .F. ) ;
#37138=CARTESIAN_POINT ( 'NONE',  ( -3.270833333333188264, -0.9791666666665451713, 0.3403392041390183587 ) ) ;
#37139=AXIS2_PLACEMENT_3D ( 'NONE', #27008, #26711, #45926 ) ;
#37140=CARTESIAN_POINT ( 'NONE',  ( -1.931736162948558544, -55.03329604256487073, -12.72978979887498063 ) ) ;
#37142=PLANE ( 'NONE',  #4522 ) ;
#37143=VERTEX_POINT ( 'NONE', #9994 ) ;
#37144=CARTESIAN_POINT ( 'NONE',  ( 12.50000000000000000, -60.04999999966999980, -1.250000000000000000 ) ) ;
#37146=VERTEX_POINT ( 'NONE', #27973 ) ;
#37149=DIRECTION ( 'NONE',  ( 1.000000000000000000, 0.000000000000000000, 0.000000000000000000 ) ) ;
#37150=VERTEX_POINT ( 'NONE', #46023 ) ;
#37151=CARTESIAN_POINT ( 'NONE',  ( -10.36222501928999939, -55.57880030132999849, -7.631889976297999922 ) ) ;
#37152=EDGE_CURVE ( 'NONE', #39513, #2249, #33099, .T. ) ;
#37153=FILL_AREA_STYLE ('',( #9427 ) ) ;
#37156=ORIENTED_EDGE ( 'NONE', *, *, #47000, .T. ) ;
#37157=CARTESIAN_POINT ( 'NONE',  ( -3.500000000146000101, -0.7499999998540000101, 2.054632350152999929E-08 ) ) ;
#37158=CARTESIAN_POINT ( 'NONE',  ( 7.624341764926000131, -23.26485149464000202, -10.42531124853000080 ) ) ;
#37160=ORIENTED_EDGE ( 'NONE', *, *, #13970, .F. ) ;
#37161=CARTESIAN_POINT ( 'NONE',  ( -12.78037829248000001, -24.29316779390000036, -1.812823010630000065 ) ) ;
#37163=FACE_OUTER_BOUND ( 'NONE', #23195, .T. ) ;
#37165=CARTESIAN_POINT ( 'NONE',  ( -1.980610890452897399, -18.47926110518529441, -12.74374574607219834 ) ) ;
#37172=DIRECTION ( 'NONE',  ( -0.7071067811865474617, 0.000000000000000000, -0.7071067811865474617 ) ) ;
#37174=CARTESIAN_POINT ( 'NONE',  ( 7.568503529865000523, -76.33963980947999062, 9.708412483427999007 ) ) ;
#37175=CARTESIAN_POINT ( 'NONE',  ( -2.337444978021420372, -2.416471344608311256, -2.633833035016341473 ) ) ;
#37176=CARTESIAN_POINT ( 'NONE',  ( 7.659225027833000077, -60.48266641633000518, -9.963489011801000217 ) ) ;
#37177=CARTESIAN_POINT ( 'NONE',  ( -10.61911868076999887, -78.52435387434999825, -6.134606423928000041 ) ) ;
#37180=CARTESIAN_POINT ( 'NONE',  ( 10.03846658019363502, -60.59367507117051588, -7.678639819092057728 ) ) ;
#37181=CARTESIAN_POINT ( 'NONE',  ( 5.455390417367294020, -77.88749686968762376, 10.70987740487309559 ) ) ;
#37186=CARTESIAN_POINT ( 'NONE',  ( 8.266617305338565203, -24.97234527442468632, 9.697375114818715502 ) ) ;
#37188=CARTESIAN_POINT ( 'NONE',  ( -3.452134515939000003, -3.351393098589999564, 1.370126006426999998 ) ) ;
#37191=CARTESIAN_POINT ( 'NONE',  ( 0.02495217850030486892, -76.07451107435575466, 11.74976244630887479 ) ) ;
#37198=CARTESIAN_POINT ( 'NONE',  ( 2.839805762151335511, -2.291666666666666519, 1.636761686205429278 ) ) ;
#37202=FACE_OUTER_BOUND ( 'NONE', #31164, .T. ) ;
#37203=CARTESIAN_POINT ( 'NONE',  ( 7.756275637039999893, -17.77995361836999777, -10.15825999916999933 ) ) ;
#37206=EDGE_CURVE ( 'NONE', #48292, #52871, #27611, .T. ) ;
#37208=CARTESIAN_POINT ( 'NONE',  ( 12.70253230850417481, -17.02944272791701863, 0.9891673677968747525 ) ) ;
#37210=CARTESIAN_POINT ( 'NONE',  ( 8.054632438192243171, -77.27014976278788083, 9.064962413430851740 ) ) ;
#37211=AXIS2_PLACEMENT_3D ( 'NONE', #16680, #57407, #47992 ) ;
#37214=CARTESIAN_POINT ( 'NONE',  ( -0.4587696627765999735, -3.363384982433000214, -3.778272981138000031 ) ) ;
#37217=DIRECTION ( 'NONE',  ( -0.7071067811865474617, 0.000000000000000000, -0.7071067811865474617 ) ) ;
#37220=ORIENTED_EDGE ( 'NONE', *, *, #35443, .F. ) ;
#37223=EDGE_CURVE ( 'NONE', #35617, #15196, #5606, .T. ) ;
#37228=CARTESIAN_POINT ( 'NONE',  ( 7.634438871678000282, -60.54781730666999806, 10.30764054783999839 ) ) ;
#37232=AXIS2_PLACEMENT_3D ( 'NONE', #24367, #28482, #55955 ) ;
#37234=ORIENTED_EDGE ( 'NONE', *, *, #44074, .T. ) ;
#37235=CARTESIAN_POINT ( 'NONE',  ( -10.20678250197623882, -24.23575784472138039, 7.770339463571165339 ) ) ;
#37240=B_SPLINE_CURVE_WITH_KNOTS ( 'NONE', 3,
 ( #13021, #17460, #8604, #21603, #26591, #4476, #44626, #13315, #53192, #49353 ),
 .UNSPECIFIED., .F., .F.,
 ( 4, 2, 2, 2, 4 ),
 ( 0.000000000000000000, 0.5000000000000089928, 0.6250000000000092149, 0.7500000000000095479, 1.000000000000000000 ),
 .UNSPECIFIED. ) ;
#37243=CARTESIAN_POINT ( 'NONE',  ( -8.130813118010999929, -17.31476110167000115, 9.546856411653001473 ) ) ;
#37248=AXIS2_PLACEMENT_3D ( 'NONE', #24793, #1502, #33050 ) ;
#37249=CARTESIAN_POINT ( 'NONE',  ( -7.620012114214000043, -23.20560398649000078, -10.53562503194000044 ) ) ;
#37250=CARTESIAN_POINT ( 'NONE',  ( 12.71658889743999943, -60.11584477251999203, -1.931087888049999979 ) ) ;
#37252=ORIENTED_EDGE ( 'NONE', *, *, #52776, .T. ) ;
#37253=CARTESIAN_POINT ( 'NONE',  ( 12.50000000000000000, -55.55000000278000272, -1.750000000000000000 ) ) ;
#37257=CARTESIAN_POINT ( 'NONE',  ( -7.620012214426000519, -18.79439747922000237, 10.53562508625000049 ) ) ;
#37259=CARTESIAN_POINT ( 'NONE',  ( 1.739823320037857002, -3.083851424189317569, 3.063316470677002190 ) ) ;
#37266=VERTEX_POINT ( 'NONE', #23554 ) ;
#37267=CARTESIAN_POINT ( 'NONE',  ( -9.050966799188000067, -55.64999999964999233, -7.919595949288999570 ) ) ;
#37271=CARTESIAN_POINT ( 'NONE',  ( -12.85144117163000033, -21.75472017028999971, 1.980464439859999981 ) ) ;
#37273=CARTESIAN_POINT ( 'NONE',  ( 1.637338945544639213, -1.934839485303867290, 2.842420532304482883 ) ) ;
#37274=DIRECTION ( 'NONE',  ( 0.000000000000000000, 1.000000000000000000, 0.000000000000000000 ) ) ;
#37276=ADVANCED_FACE ( 'NONE', ( #9405 ), #18269, .F. ) ;
#37279=EDGE_CURVE ( 'NONE', #6154, #36787, #31820, .T. ) ;
#37281=AXIS2_PLACEMENT_3D ( 'NONE', #8212, #35646, #17659 ) ;
#37285=CARTESIAN_POINT ( 'NONE',  ( -7.958776492183998741, -24.47699850274999989, 9.723157982400998378 ) ) ;
#37299=ADVANCED_FACE ( 'NONE', ( #45730 ), #55230, .F. ) ;
#37300=ORIENTED_EDGE ( 'NONE', *, *, #41443, .T. ) ;
#37303=DIRECTION ( 'NONE',  ( 0.000000000000000000, -1.000000000000000000, 0.000000000000000000 ) ) ;
#37308=CARTESIAN_POINT ( 'NONE',  ( -8.768124086549999419, -55.65000000488999632, 7.919595949288999570 ) ) ;
#37309=EDGE_CURVE ( 'NONE', #48492, #6877, #48363, .T. ) ;
#37310=ORIENTED_EDGE ( 'NONE', *, *, #26760, .F. ) ;
#37311=ORIENTED_EDGE ( 'NONE', *, *, #11752, .F. ) ;
#37316=DIRECTION ( 'NONE',  ( 0.000000000000000000, 0.000000000000000000, -1.000000000000000000 ) ) ;
#37318=DIRECTION ( 'NONE',  ( 0.000000000000000000, -1.000000000000000000, 0.000000000000000000 ) ) ;
#37323=VECTOR ( 'NONE', #5533, 999.9999999999998863 ) ;
#37324=CARTESIAN_POINT ( 'NONE',  ( -12.49168433579000137, -23.29849137228000444, -1.667916687244999974 ) ) ;
#37325=CARTESIAN_POINT ( 'NONE',  ( 0.3436388712391041933, -76.57261070421138527, 11.74524196079921623 ) ) ;
#37329=CARTESIAN_POINT ( 'NONE',  ( 12.50000000000000000, -55.54999999966999980, 0.000000000000000000 ) ) ;
#37331=DIRECTION ( 'NONE',  ( 0.000000000000000000, 1.000000000000000000, 0.000000000000000000 ) ) ;
#37333=EDGE_CURVE ( 'NONE', #57192, #39540, #37053, .T. ) ;
#37335=LINE ( 'NONE', #15193, #32545 ) ;
#37336=CARTESIAN_POINT ( 'NONE',  ( 3.190249742999000215, -2.021431841278999553, -2.075671974272999876 ) ) ;
#37337=CIRCLE ( 'NONE', #47732, 1.750000000000000444 ) ;
#37338=FACE_OUTER_BOUND ( 'NONE', #14572, .T. ) ;
#37340=CARTESIAN_POINT ( 'NONE',  ( -2.730984724245073103, -3.499999999999999556, -1.917875800217215598 ) ) ;
#37342=CYLINDRICAL_SURFACE ( 'NONE', #35453, 1.750000000000001332 ) ;
#37343=CARTESIAN_POINT ( 'NONE',  ( 1.799475295154000065, -58.55083378327000077, 12.69619287811999797 ) ) ;
#37344=CARTESIAN_POINT ( 'NONE',  ( 1.750000000001000089, -55.54999998977000075, -12.56594317853999954 ) ) ;
#37347=EDGE_CURVE ( 'NONE', #35775, #2137, #56029, .T. ) ;
#37348=CYLINDRICAL_SURFACE ( 'NONE', #8030, 14.00000000000000000 ) ;
#37351=CARTESIAN_POINT ( 'NONE',  ( 7.642160924865000204, -22.78461666469000235, -10.55911395186000057 ) ) ;
#37352=DIRECTION ( 'NONE',  ( -0.7071067811865475727, 0.000000000000000000, -0.7071067811865475727 ) ) ;
#37358=DIRECTION ( 'NONE',  ( 0.000000000000000000, 1.000000000000000000, 0.000000000000000000 ) ) ;
#37360=ORIENTED_EDGE ( 'NONE', *, *, #11674, .T. ) ;
#37361=VERTEX_POINT ( 'NONE', #20591 ) ;
#37367=ORIENTED_EDGE ( 'NONE', *, *, #2194, .F. ) ;
#37369=ORIENTED_EDGE ( 'NONE', *, *, #31484, .T. ) ;
#37372=CIRCLE ( 'NONE', #26027, 0.5000000000000004441 ) ;
#37375=ORIENTED_EDGE ( 'NONE', *, *, #57042, .F. ) ;
#37377=AXIS2_PLACEMENT_3D ( 'NONE', #44372, #31946, #27228 ) ;
#37378=CARTESIAN_POINT ( 'NONE',  ( -2.962050278768000311, -2.514727077435000346, 1.672015632479999958 ) ) ;
#37379=ORIENTED_EDGE ( 'NONE', *, *, #52968, .T. ) ;
#37386=CARTESIAN_POINT ( 'NONE',  ( 9.396085398178598780, -77.10208333333331154, 7.220923959705271677 ) ) ;
#37387=CARTESIAN_POINT ( 'NONE',  ( -7.655555357438999842, -56.02204592290999585, -10.38646360829000059 ) ) ;
#37391=CARTESIAN_POINT ( 'NONE',  ( 17.50000000000000000, -26.93717104351999936, 4.519611351839000330E-10 ) ) ;
#37392=CARTESIAN_POINT ( 'NONE',  ( -12.65372179304999811, -58.55064713745999683, -1.750000000000000000 ) ) ;
#37396=EDGE_CURVE ( 'NONE', #47003, #34794, #15578, .T. ) ;
#37398=DIRECTION ( 'NONE',  ( -0.7071067811865969777, 1.533578360404995178E-11, -0.7071067811864980568 ) ) ;
#37399=CARTESIAN_POINT ( 'NONE',  ( -12.50000000000000000, -18.75000000310999937, 1.750000000000000000 ) ) ;
#37401=CARTESIAN_POINT ( 'NONE',  ( 12.54435915805012769, -23.52412882219289969, 1.733925320388620683 ) ) ;
#37403=CARTESIAN_POINT ( 'NONE',  ( -1.382886570147999983, -24.63098219832000169, -12.65982054476000052 ) ) ;
#37406=CARTESIAN_POINT ( 'NONE',  ( 12.59682790092999838, -23.38734115225999943, 1.801645751184999922 ) ) ;
#37408=CIRCLE ( 'NONE', #27959, 14.00000000000000000 ) ;
#37410=DIRECTION ( 'NONE',  ( -0.7071067811865475727, 0.000000000000000000, -0.7071067811865475727 ) ) ;
#37412=CARTESIAN_POINT ( 'NONE',  ( 10.85336555362000155, -76.97361153625999464, -4.603040914152999541 ) ) ;
#37413=EDGE_LOOP ( 'NONE', ( #1163, #30397, #41691, #47756, #56277 ) ) ;
#37418=VECTOR ( 'NONE', #31186, 1000.000000000000114 ) ;
#37420=DIRECTION ( 'NONE',  ( -0.7071067811865475727, 0.000000000000000000, 0.7071067811865475727 ) ) ;
#37424=VECTOR ( 'NONE', #14917, 1000.000000000000227 ) ;
#37426=CARTESIAN_POINT ( 'NONE',  ( -3.799999999999999822, 0.000000000000000000, 0.000000000000000000 ) ) ;
#37430=CARTESIAN_POINT ( 'NONE',  ( 11.21020301114814011, -75.92468345066387769, -3.640793229887494764 ) ) ;
#37431=EDGE_CURVE ( 'NONE', #18217, #8616, #40812, .T. ) ;
#37432=ORIENTED_EDGE ( 'NONE', *, *, #5903, .F. ) ;
#37434=EDGE_CURVE ( 'NONE', #4000, #8688, #7818, .T. ) ;
#37438=B_SPLINE_CURVE_WITH_KNOTS ( 'NONE', 3,
 ( #43507, #30192, #7778, #39064, #34336, #43220 ),
 .UNSPECIFIED., .F., .F.,
 ( 4, 1, 1, 4 ),
 ( 0.000000000000000000, 0.3333333333333000081, 0.6666666666667000474, 1.000000000000000000 ),
 .UNSPECIFIED. ) ;
#37441=CARTESIAN_POINT ( 'NONE',  ( -1.667961445601999992, -20.25199022618999933, 12.58338334675000070 ) ) ;
#37442=ORIENTED_EDGE ( 'NONE', *, *, #14909, .T. ) ;
#37443=ORIENTED_EDGE ( 'NONE', *, *, #5363, .F. ) ;
#37446=ORIENTED_EDGE ( 'NONE', *, *, #48486, .F. ) ;
#37447=CARTESIAN_POINT ( 'NONE',  ( 12.61112375829999976, -55.58433928934000079, 1.798929377343999825 ) ) ;
#37451=ADVANCED_FACE ( 'NONE', ( #52181 ), #27389, .F. ) ;
#37455=CARTESIAN_POINT ( 'NONE',  ( -0.6484536763576147500, -16.87597017290601897, -12.70397497891858052 ) ) ;
#37460=CARTESIAN_POINT ( 'NONE',  ( 11.50190934395000042, -76.74432514197999922, -3.421415122956000143 ) ) ;
#37462=CARTESIAN_POINT ( 'NONE',  ( 7.646966600034999395, -59.99642081684000061, -10.19019745249000053 ) ) ;
#37463=CARTESIAN_POINT ( 'NONE',  ( -12.02296678431999943, -78.46687243819999935, 2.418109797047000242 ) ) ;
#37466=CARTESIAN_POINT ( 'NONE',  ( -7.954951288349001004, -23.25000000000000000, 9.722718241315000398 ) ) ;
#37468=CARTESIAN_POINT ( 'NONE',  ( -1.720220533992320888, -77.93641922950823187, 11.89284491344992922 ) ) ;
#37470=VERTEX_POINT ( 'NONE', #35890 ) ;
#37472=CARTESIAN_POINT ( 'NONE',  ( 10.26699006316253637, -78.00833333333331154, -5.917523019358050362 ) ) ;
#37473=CARTESIAN_POINT ( 'NONE',  ( -1.750000000000000000, -57.04935285922000077, -12.65372179284000076 ) ) ;
#37475=CARTESIAN_POINT ( 'NONE',  ( 3.239642551180000218, -2.998304953963999875, -2.117792278697999908 ) ) ;
#37478=CARTESIAN_POINT ( 'NONE',  ( -9.226664435044119372, -76.14651772991450684, 7.278599119727092059 ) ) ;
#37486=EDGE_CURVE ( 'NONE', #36484, #37361, #46532, .T. ) ;
#37487=DIRECTION ( 'NONE',  ( 0.000000000000000000, 1.000000000000000000, 0.000000000000000000 ) ) ;
#37491=CARTESIAN_POINT ( 'NONE',  ( 10.13402152809999990, -18.27694524397999842, -7.647754144029000223 ) ) ;
#37492=CARTESIAN_POINT ( 'NONE',  ( 9.431004454607295528, -17.19940410572471023, 8.251853356785181504 ) ) ;
#37497=DIRECTION ( 'NONE',  ( 0.000000000000000000, 0.000000000000000000, 1.000000000000000000 ) ) ;
#37498=CARTESIAN_POINT ( 'NONE',  ( 6.047259872863349983, -77.78606555346475204, 10.39103189327145138 ) ) ;
#37500=B_SPLINE_CURVE_WITH_KNOTS ( 'NONE', 3,
 ( #12439, #33708, #30432, #21294, #16876, #47620, #57023, #29277 ),
 .UNSPECIFIED., .F., .F.,
 ( 4, 2, 2, 4 ),
 ( 0.000000000000000000, 0.2500000000000000000, 0.5000000000000000000, 1.000000000000000000 ),
 .UNSPECIFIED. ) ;
#37503=CARTESIAN_POINT ( 'NONE',  ( -12.50485633183174450, -53.93407854620129882, -0.6924329878416003448 ) ) ;
#37504=CARTESIAN_POINT ( 'NONE',  ( 13.86363636363000218, -9.638971321655001034, 1.277887488545999904E-05 ) ) ;
#37506=DIRECTION ( 'NONE',  ( 0.000000000000000000, 0.000000000000000000, -1.000000000000000000 ) ) ;
#37508=CARTESIAN_POINT ( 'NONE',  ( 1.749722766158709142, -18.52411007112894836, -12.54673760678543282 ) ) ;
#37515=VERTEX_POINT ( 'NONE', #12586 ) ;
#37516=ADVANCED_FACE ( 'NONE', ( #52749 ), #56216, .F. ) ;
#37519=CARTESIAN_POINT ( 'NONE',  ( 8.252521514740998043, -61.73405767862000459, 9.650901483168000894 ) ) ;
#37523=ORIENTED_EDGE ( 'NONE', *, *, #30015, .F. ) ;
#37524=CARTESIAN_POINT ( 'NONE',  ( -7.861032689861890077, -24.46660299217103329, 10.10708926022225107 ) ) ;
#37528=CYLINDRICAL_SURFACE ( 'NONE', #15899, 12.50000000000000000 ) ;
#37529=EDGE_CURVE ( 'NONE', #52707, #46363, #1362, .T. ) ;
#37532=TOROIDAL_SURFACE ( 'NONE', #42274, 1.250000000000000000, 0.5000000000000000000 ) ;
#37533=CARTESIAN_POINT ( 'NONE',  ( 10.35396498619769012, -76.72450177318867759, -6.064612950829413762 ) ) ;
#37536=VECTOR ( 'NONE', #40289, 1000.000000000000114 ) ;
#37539=CARTESIAN_POINT ( 'NONE',  ( -7.633403016703000254, -23.38650073851000144, -10.18126993294000115 ) ) ;
#37540=CARTESIAN_POINT ( 'NONE',  ( 12.64500484464000074, -56.02847221959000024, -1.799490225533999732 ) ) ;
#37543=FACE_OUTER_BOUND ( 'NONE', #8148, .T. ) ;
#37547=CARTESIAN_POINT ( 'NONE',  ( -8.790679651960999763, -17.06186536190000069, 8.797972003296999688 ) ) ;
#37549=AXIS2_PLACEMENT_3D ( 'NONE', #9165, #49023, #4144 ) ;
#37550=CARTESIAN_POINT ( 'NONE',  ( -0.1800737450312397958, -3.129084965038133603, 3.516770117047313349 ) ) ;
#37557=ORIENTED_EDGE ( 'NONE', *, *, #32265, .F. ) ;
#37559=EDGE_CURVE ( 'NONE', #30862, #26517, #19743, .T. ) ;
#37560=CARTESIAN_POINT ( 'NONE',  ( 1.537519735729477643, -77.06247989013436950, 11.74357244733737105 ) ) ;
#37561=CARTESIAN_POINT ( 'NONE',  ( -11.75000000000000000, -78.70000000000000284, -1.701764645356999850E-14 ) ) ;
#37562=B_SPLINE_CURVE_WITH_KNOTS ( 'NONE', 3,
 ( #29840, #43442, #12430, #57303, #30423, #25427, #7998, #3291, #21284, #57584, #47892, #30130, #3003, #20999, #39291, #44301 ),
 .UNSPECIFIED., .F., .F.,
 ( 4, 2, 2, 2, 2, 2, 2, 4 ),
 ( 0.000000000000000000, 0.2499999999999975575, 0.3749999999999970024, 0.4999999999999964473, 0.6249999999999958922, 0.6874999999999954481, 0.7499999999999951150, 1.000000000000000000 ),
 .UNSPECIFIED. ) ;
#37567=CARTESIAN_POINT ( 'NONE',  ( -12.76303204517000012, -18.73514852243999940, 1.980584515753000208 ) ) ;
#37569=CARTESIAN_POINT ( 'NONE',  ( -1.704789469149992298, -23.70346161524693684, -12.53199752960662394 ) ) ;
#37570=CARTESIAN_POINT ( 'NONE',  ( -10.10448976474953575, -54.34884052577077540, -7.864761218127002351 ) ) ;
#37572=CARTESIAN_POINT ( 'NONE',  ( -7.651147547618999845, -56.03743349692000209, 10.45204383579000051 ) ) ;
#37573=CARTESIAN_POINT ( 'NONE',  ( 7.943801774140000660, -54.36598212437999678, -9.641153612765998915 ) ) ;
#37577=CARTESIAN_POINT ( 'NONE',  ( -1.931736162949572622, -60.56670395678658281, 12.72978979893449392 ) ) ;
#37580=ORIENTED_EDGE ( 'NONE', *, *, #14100, .T. ) ;
#37581=CARTESIAN_POINT ( 'NONE',  ( 9.000000000000000000, -0.5000000000000000000, 0.000000000000000000 ) ) ;
#37582=TOROIDAL_SURFACE ( 'NONE', #12127, 17.50000000000000000, 5.000000000000000000 ) ;
#37584=EDGE_LOOP ( 'NONE', ( #28514, #47477 ) ) ;
#37592=EDGE_LOOP ( 'NONE', ( #55530, #50147, #24007, #55966, #4399, #46480, #35241, #6962, #32855, #52913, #17329 ) ) ;
#37596=CARTESIAN_POINT ( 'NONE',  ( 2.061649843245999758, -18.79438692412999856, 12.83797346714000120 ) ) ;
#37602=CARTESIAN_POINT ( 'NONE',  ( -11.75000000000000000, -77.29999999999999716, 0.000000000000000000 ) ) ;
#37604=VERTEX_POINT ( 'NONE', #9337 ) ;
#37606=CARTESIAN_POINT ( 'NONE',  ( -12.70457891999271283, -25.17873330329357273, 0.5105076820425886730 ) ) ;
#37608=EDGE_CURVE ( 'NONE', #31168, #58211, #11626, .T. ) ;
#37609=CARTESIAN_POINT ( 'NONE',  ( 1.501534314749353394, -61.35152951622894335, -12.70455943744364724 ) ) ;
#37611=FACE_OUTER_BOUND ( 'NONE', #55811, .T. ) ;
#37620=CARTESIAN_POINT ( 'NONE',  ( -7.605690612615000568, -18.57434870741999688, -10.52682230157000021 ) ) ;
#37621=DIRECTION ( 'NONE',  ( 0.7071067811865475727, 0.000000000000000000, -0.7071067811865475727 ) ) ;
#37622=CARTESIAN_POINT ( 'NONE',  ( 0.4701041210474000143, -16.99203065576000071, -12.54901038416000070 ) ) ;
#37627=CARTESIAN_POINT ( 'NONE',  ( -1.461856643173269132, -1.340935351588901758, -3.213633154597908437 ) ) ;
#37628=VERTEX_POINT ( 'NONE', #14911 ) ;
#37629=CARTESIAN_POINT ( 'NONE',  ( 5.911015991360685007, -78.96666666666666856, -10.22919423417961937 ) ) ;
#37633=EDGE_CURVE ( 'NONE', #44472, #49809, #5478, .T. ) ;
#37636=CARTESIAN_POINT ( 'NONE',  ( -10.64207148833999916, -76.89920160919999148, 7.489034475093999887 ) ) ;
#37637=CYLINDRICAL_SURFACE ( 'NONE', #10137, 0.5000000000000006661 ) ;
#37639=AXIS2_PLACEMENT_3D ( 'NONE', #53637, #814, #23505 ) ;
#37644=CARTESIAN_POINT ( 'NONE',  ( -1.885855158825846090, -76.31202484814713216, -11.60495004190995516 ) ) ;
#37647=CYLINDRICAL_SURFACE ( 'NONE', #1950, 0.6000000000000008660 ) ;
#37648=EDGE_CURVE ( 'NONE', #46028, #4126, #47467, .T. ) ;
#37650=CARTESIAN_POINT ( 'NONE',  ( -1.636761686205434607, -2.916666666666667407, 2.839805762151332402 ) ) ;
#37652=CARTESIAN_POINT ( 'NONE',  ( -3.630949683906000036, -75.80000000000001137, -11.17491406647000041 ) ) ;
#37654=CARTESIAN_POINT ( 'NONE',  ( 0.000000000000000000, 4.040000000000000036, 0.000000000000000000 ) ) ;
#37659=DIRECTION ( 'NONE',  ( -0.7071067811865475727, 0.000000000000000000, -0.7071067811865475727 ) ) ;
#37660=CARTESIAN_POINT ( 'NONE',  ( 7.764005369058246231, -17.87720632478401583, 9.931049915323967525 ) ) ;
#37661=EDGE_LOOP ( 'NONE', ( #21162, #5714, #48128, #50970 ) ) ;
#37664=VERTEX_POINT ( 'NONE', #50665 ) ;
#37665=ADVANCED_FACE ( 'NONE', ( #46241 ), #21958, .F. ) ;
#37666=EDGE_LOOP ( 'NONE', ( #56038, #42043, #867, #10641, #45449, #42684, #33287, #19747, #38478 ) ) ;
#37669=EDGE_LOOP ( 'NONE', ( #29260, #46414, #30178, #11307, #51264, #52745, #38021 ) ) ;
#37672=CARTESIAN_POINT ( 'NONE',  ( -7.682344222584999827, -59.56462890159999546, 10.04116292117000064 ) ) ;
#37678=ADVANCED_FACE ( 'NONE', ( #5767 ), #23775, .F. ) ;
#37679=CARTESIAN_POINT ( 'NONE',  ( 0.000000000000000000, -45.91785611817000046, 0.000000000000000000 ) ) ;
#37680=CARTESIAN_POINT ( 'NONE',  ( 2.361413772017329382, -0.9453124996592523477, 2.369150859468821313 ) ) ;
#37683=CARTESIAN_POINT ( 'NONE',  ( -7.220923959705292994, -77.22708333333335418, 9.396085398178589898 ) ) ;
#37688=CARTESIAN_POINT ( 'NONE',  ( 2.604752141441593505, -76.55672158594160237, 11.45797238997031720 ) ) ;
#37689=CARTESIAN_POINT ( 'NONE',  ( 1.980532758766000212, -22.76256650694000072, -12.80088938802999898 ) ) ;
#37690=CARTESIAN_POINT ( 'NONE',  ( 0.000000000000000000, -9.638971321655001034, 0.000000000000000000 ) ) ;
#37692=CARTESIAN_POINT ( 'NONE',  ( -3.004722042233088697, -3.070212179489009152, 1.236557240987053996 ) ) ;
#37697=CARTESIAN_POINT ( 'NONE',  ( 7.342331066867000544, -55.64999999967000122, 8.190859204290999784 ) ) ;
#37700=CARTESIAN_POINT ( 'NONE',  ( -3.480424184914000296, -1.078054798046000018, -1.007877577829999982 ) ) ;
#37703=CARTESIAN_POINT ( 'NONE',  ( 13.13047446164998711, -22.78578169018998878, 0.8260994316375004365 ) ) ;
#37705=CARTESIAN_POINT ( 'NONE',  ( 12.99999999992999911, -5.999999999934902739, 2.526608922016999658E-09 ) ) ;
#37710=DIRECTION ( 'NONE',  ( 0.000000000000000000, 1.000000000000000000, 0.000000000000000000 ) ) ;
#37717=DIRECTION ( 'NONE',  ( 0.000000000000000000, -1.000000000000000000, 0.000000000000000000 ) ) ;
#37719=AXIS2_PLACEMENT_3D ( 'NONE', #48208, #16892, #44048 ) ;
#37724=DIRECTION ( 'NONE',  ( 0.000000000000000000, 1.000000000000000000, 0.000000000000000000 ) ) ;
#37725=CIRCLE ( 'NONE', #12230, 14.00000000000000000 ) ;
#37735=ORIENTED_EDGE ( 'NONE', *, *, #50662, .F. ) ;
#37736=ORIENTED_EDGE ( 'NONE', *, *, #27660, .T. ) ;
#37737=EDGE_CURVE ( 'NONE', #49445, #28402, #22904, .T. ) ;
#37742=ORIENTED_EDGE ( 'NONE', *, *, #20574, .F. ) ;
#37745=VECTOR ( 'NONE', #18439, 1000.000000000000114 ) ;
#37747=DIRECTION ( 'NONE',  ( 1.000000000000000000, 0.000000000000000000, 0.000000000000000000 ) ) ;
#37749=B_SPLINE_CURVE_WITH_KNOTS ( 'NONE', 3,
 ( #16675, #34941, #15801, #29363, #52973, #44118 ),
 .UNSPECIFIED., .F., .F.,
 ( 4, 1, 1, 4 ),
 ( 0.000000000000000000, 0.3333333333333000081, 0.6666666666667000474, 1.000000000000000000 ),
 .UNSPECIFIED. ) ;
#37751=CARTESIAN_POINT ( 'NONE',  ( 17.49999986748943925, -49.87071424677999687, 0.002153571276233540773 ) ) ;
#37752=FACE_BOUND ( 'NONE', #16983, .T. ) ;
#37753=EDGE_CURVE ( 'NONE', #46987, #34267, #52078, .T. ) ;
#37757=CARTESIAN_POINT ( 'NONE',  ( -11.84062247810999935, -76.46062134762000539, 3.366775603358000080 ) ) ;
#37760=DIRECTION ( 'NONE',  ( 0.000000000000000000, 1.000000000000000000, 0.000000000000000000 ) ) ;
#37761=CARTESIAN_POINT ( 'NONE',  ( -11.55418265775999842, -78.92079797882001913, 4.110954701505000308 ) ) ;
#37764=CARTESIAN_POINT ( 'NONE',  ( 12.71005124797207131, -17.70500926711284606, -1.687536500540181228 ) ) ;
#37765=CARTESIAN_POINT ( 'NONE',  ( 1.971342833597536037, -2.778145728227555011, -2.591225479259308351 ) ) ;
#37766=CARTESIAN_POINT ( 'NONE',  ( 11.72382527513436656, -77.78075717553235791, -2.897248159155891400 ) ) ;
#37770=FACE_OUTER_BOUND ( 'NONE', #35375, .T. ) ;
#37774=CARTESIAN_POINT ( 'NONE',  ( 2.810448636938000178, -3.104707871922999907, 2.661147811754999370 ) ) ;
#37777=CARTESIAN_POINT ( 'NONE',  ( -8.300354423835440087, -76.13742599171457925, 8.316632957359784584 ) ) ;
#37780=DIRECTION ( 'NONE',  ( -0.7071067811865474617, 0.000000000000000000, -0.7071067811865474617 ) ) ;
#37781=ORIENTED_EDGE ( 'NONE', *, *, #2552, .T. ) ;
#37784=VECTOR ( 'NONE', #15868, 999.9999999999998863 ) ;
#37785=CARTESIAN_POINT ( 'NONE',  ( -11.75000000000000355, -76.81041666666668277, -1.538071403320004249 ) ) ;
#37788=CARTESIAN_POINT ( 'NONE',  ( 7.648026766733999615, -18.74999999413999774, 10.12290050089000104 ) ) ;
#37789=CARTESIAN_POINT ( 'NONE',  ( 9.205836503716000152, -16.99200673936999806, -8.541144771069001607 ) ) ;
#37793=CARTESIAN_POINT ( 'NONE',  ( 0.000000000000000000, -23.94999999999946994, -12.00000000000000000 ) ) ;
#37794=CARTESIAN_POINT ( 'NONE',  ( -11.90000000000000036, -21.00000000000000000, 0.6999999999999999556 ) ) ;
#37796=CARTESIAN_POINT ( 'NONE',  ( -11.65386922465466846, -77.47918460901016147, -3.926725210437132851 ) ) ;
#37798=CARTESIAN_POINT ( 'NONE',  ( -12.52133763467701755, -54.87246868424995938, 1.618901766958424027 ) ) ;
#37799=VECTOR ( 'NONE', #49263, 999.9999999999998863 ) ;
#37801=CARTESIAN_POINT ( 'NONE',  ( 3.542727183245000244, -2.968224769577000099, -1.391102635753999950 ) ) ;
#37804=CARTESIAN_POINT ( 'NONE',  ( -1.980464439859999981, -20.24527982672000093, 12.85144117157999943 ) ) ;
#37808=ORIENTED_EDGE ( 'NONE', *, *, #18235, .T. ) ;
#37811=ORIENTED_EDGE ( 'NONE', *, *, #44849, .T. ) ;
#37812=CARTESIAN_POINT ( 'NONE',  ( 7.758899961888999997, -17.69918178096000005, 10.31442855573999928 ) ) ;
#37814=CARTESIAN_POINT ( 'NONE',  ( -11.82502128560000010, -78.31566534667000212, 2.378298163336999949 ) ) ;
#37815=CARTESIAN_POINT ( 'NONE',  ( 13.97864847978000036, -33.03331574008000615, 0.0001086647257957000046 ) ) ;
#37817=EDGE_CURVE ( 'NONE', #22264, #50397, #6002, .T. ) ;
#37820=VERTEX_POINT ( 'NONE', #53253 ) ;
#37821=CARTESIAN_POINT ( 'NONE',  ( 7.648026768008000076, -55.55000001556999933, -10.12290050216000026 ) ) ;
#37822=VECTOR ( 'NONE', #21746, 1000.000000000000000 ) ;
#37829=CARTESIAN_POINT ( 'NONE',  ( -9.621742412363845531, -17.37938300088043775, 8.060146969363517044 ) ) ;
#37830=DIRECTION ( 'NONE',  ( 0.000000000000000000, 0.000000000000000000, -1.000000000000000000 ) ) ;
#37833=CARTESIAN_POINT ( 'NONE',  ( 1.250000000000000000, -60.04999999966999980, -12.00000000000000000 ) ) ;
#37834=FACE_OUTER_BOUND ( 'NONE', #56553, .T. ) ;
#37836=CARTESIAN_POINT ( 'NONE',  ( 0.000000000000000000, -9.295797029142999435, 0.000000000000000000 ) ) ;
#37840=AXIS2_PLACEMENT_3D ( 'NONE', #7011, #14987, #41573 ) ;
#37844=CARTESIAN_POINT ( 'NONE',  ( -9.205836503716000152, -16.99200673936999806, 8.541144771069001607 ) ) ;
#37847=CARTESIAN_POINT ( 'NONE',  ( -1.888659139779025997, -2.830543595434927173, -3.048522970863501769 ) ) ;
#37852=CARTESIAN_POINT ( 'NONE',  ( 2.944803976276252122, -0.8802083256670968359, -1.696304167215174630 ) ) ;
#37856=CARTESIAN_POINT ( 'NONE',  ( -1.477284502223000118, -61.52631500263999698, -12.77254812472999923 ) ) ;
#37857=CARTESIAN_POINT ( 'NONE',  ( -7.364280830344936746, -55.45989902437826657, 8.171144579305440914 ) ) ;
#37860=CARTESIAN_POINT ( 'NONE',  ( 8.485538010655998775, -24.88067982437999959, -9.101501073481999882 ) ) ;
#37862=EDGE_CURVE ( 'NONE', #2615, #37882, #18999, .T. ) ;
#37864=CARTESIAN_POINT ( 'NONE',  ( 0.000000000000000000, -9.638971321655001034, 0.000000000000000000 ) ) ;
#37869=CARTESIAN_POINT ( 'NONE',  ( 8.533817832752999877, -53.79473856423000200, -9.213092693279001821 ) ) ;
#37877=EDGE_LOOP ( 'NONE', ( #41855, #57054, #22530, #29086 ) ) ;
#37882=VERTEX_POINT ( 'NONE', #13383 ) ;
#37886=ORIENTED_EDGE ( 'NONE', *, *, #15325, .F. ) ;
#37888=CARTESIAN_POINT ( 'NONE',  ( -0.5390150933987999382, -16.73739108348000215, 12.77520261005000002 ) ) ;
#37889=DIRECTION ( 'NONE',  ( -1.000000000000000000, 0.000000000000000000, 0.000000000000000000 ) ) ;
#37892=EDGE_CURVE ( 'NONE', #57635, #37143, #36991, .T. ) ;
#37894=DIRECTION ( 'NONE',  ( 0.000000000000000000, -1.000000000000000000, 0.000000000000000000 ) ) ;
#37897=ORIENTED_EDGE ( 'NONE', *, *, #4311, .T. ) ;
#37899=CARTESIAN_POINT ( 'NONE',  ( -8.485281374238999419, -18.75000000000000000, -8.485281374238999419 ) ) ;
#37900=CARTESIAN_POINT ( 'NONE',  ( 0.2678032735957956989, -62.01432775256377283, -12.70526550773551833 ) ) ;
#37902=DIRECTION ( 'NONE',  ( 0.000000000000000000, 0.000000000000000000, 1.000000000000000000 ) ) ;
#37903=CARTESIAN_POINT ( 'NONE',  ( -8.190859204290999784, -55.64999999967000122, -7.342331066867000544 ) ) ;
#37906=CARTESIAN_POINT ( 'NONE',  ( 0.000000000000000000, -18.75000000000000000, 12.50000000000000000 ) ) ;
#37912=CARTESIAN_POINT ( 'NONE',  ( 1.667961430005999945, -21.74888345808999901, -12.58335110161999815 ) ) ;
#37913=DIRECTION ( 'NONE',  ( 0.7071067811865475727, 0.000000000000000000, 0.7071067811865475727 ) ) ;
#37918=LINE ( 'NONE', #20222, #49608 ) ;
#37920=CARTESIAN_POINT ( 'NONE',  ( 7.901937437517356777, -78.98333333333333428, -8.782705133628073924 ) ) ;
#37925=AXIS2_PLACEMENT_3D ( 'NONE', #29327, #43502, #52648 ) ;
#37926=CARTESIAN_POINT ( 'NONE',  ( 12.56594317984999876, -18.75000000536999778, -1.750000000000000000 ) ) ;
#37927=CARTESIAN_POINT ( 'NONE',  ( 1.980584515752000119, -60.06485146591000301, -12.76303204605000197 ) ) ;
#37930=CARTESIAN_POINT ( 'NONE',  ( 5.694538069269999623E-14, -72.84999999994899156, 0.000000000000000000 ) ) ;
#37932=CARTESIAN_POINT ( 'NONE',  ( -0.7276578379041465094, -76.32000254687065421, -11.72896174709909367 ) ) ;
#37937=CARTESIAN_POINT ( 'NONE',  ( 3.981113306789000106, -1.091474769576999959, -0.5296481109823999445 ) ) ;
#37941=ADVANCED_FACE ( 'NONE', ( #5127 ), #23124, .F. ) ;
#37943=CARTESIAN_POINT ( 'NONE',  ( 7.954951288349001004, -60.04999999966999980, 9.722718241315000398 ) ) ;
#37945=ORIENTED_EDGE ( 'NONE', *, *, #4982, .F. ) ;
#37946=AXIS2_PLACEMENT_3D ( 'NONE', #57100, #3091, #30219 ) ;
#37949=DIRECTION ( 'NONE',  ( 0.000000000000000000, -1.000000000000000000, 0.000000000000000000 ) ) ;
#37950=VERTEX_POINT ( 'NONE', #39028 ) ;
#37953=ORIENTED_EDGE ( 'NONE', *, *, #46771, .T. ) ;
#37958=VERTEX_POINT ( 'NONE', #16316 ) ;
#37960=CARTESIAN_POINT ( 'NONE',  ( -7.627487606627999739, -60.09778595451999905, 10.35845616728999907 ) ) ;
#37962=EDGE_LOOP ( 'NONE', ( #20819, #7258, #8182, #30125 ) ) ;
#37973=AXIS2_PLACEMENT_3D ( 'NONE', #28310, #5886, #23893 ) ;
#37975=EDGE_CURVE ( 'NONE', #55326, #23097, #38993, .T. ) ;
#37979=CARTESIAN_POINT ( 'NONE',  ( -2.472112973585029128, -3.044024123572891316, 2.111677630882527801 ) ) ;
#37985=CARTESIAN_POINT ( 'NONE',  ( -6.862679483819019488, -76.27517955669237892, -9.537716243547501804 ) ) ;
#37986=CARTESIAN_POINT ( 'NONE',  ( 10.38645071870000081, -19.22180874373999870, 7.655542440091000600 ) ) ;
#37987=AXIS2_PLACEMENT_3D ( 'NONE', #48616, #3167, #13155 ) ;
#37988=CARTESIAN_POINT ( 'NONE',  ( -1.064906745635000096, -0.9574763279779000547, 3.122496867089999739 ) ) ;
#37989=CARTESIAN_POINT ( 'NONE',  ( 10.18491080495000034, -60.10716680829000325, 7.640030264173999441 ) ) ;
#37991=CARTESIAN_POINT ( 'NONE',  ( 12.43422056531000131, -24.43655741434000106, 1.197404442627999943 ) ) ;
#37996=CARTESIAN_POINT ( 'NONE',  ( 8.784635449156001030, -76.44554346881000129, -8.265499852908000378 ) ) ;
#38003=CARTESIAN_POINT ( 'NONE',  ( 12.43359548531999970, -54.09290601346000216, -0.8500179128028999553 ) ) ;
#38005=AXIS2_PLACEMENT_3D ( 'NONE', #19480, #50790, #14165 ) ;
#38009=ORIENTED_EDGE ( 'NONE', *, *, #17656, .F. ) ;
#38019=CARTESIAN_POINT ( 'NONE',  ( 12.60552511012999943, -60.08917723397000543, 1.799501877793999949 ) ) ;
#38021=ORIENTED_EDGE ( 'NONE', *, *, #33338, .T. ) ;
#38026=ORIENTED_EDGE ( 'NONE', *, *, #17049, .T. ) ;
#38029=B_SPLINE_CURVE_WITH_KNOTS ( 'NONE', 3,
 ( #27470, #4760, #5053, #41939, #54649, #31893, #40771, #19215, #14188, #45507, #5914, #37208, #32764, #653, #13900, #14766 ),
 .UNSPECIFIED., .F., .F.,
 ( 4, 2, 2, 2, 2, 2, 2, 4 ),
 ( 0.000000000000000000, 0.2500000000000064948, 0.3750000000000097700, 0.4375000000000099365, 0.5000000000000101030, 0.6250000000000078826, 0.7500000000000056621, 1.000000000000000000 ),
 .UNSPECIFIED. ) ;
#38032=CARTESIAN_POINT ( 'NONE',  ( 9.708203932502000200, -79.25000000000000000, -7.053423027506000587 ) ) ;
#38035=CARTESIAN_POINT ( 'NONE',  ( 12.43569863936000175, -53.91799904124000165, 0.4278707626186999957 ) ) ;
#38037=VERTEX_POINT ( 'NONE', #40180 ) ;
#38038=CARTESIAN_POINT ( 'NONE',  ( -12.66761950490999844, -24.22355206198999866, -1.696827901577000031 ) ) ;
#38042=CARTESIAN_POINT ( 'NONE',  ( 1.575772165387015367, -17.53845457196653967, -12.70597445617457666 ) ) ;
#38044=CARTESIAN_POINT ( 'NONE',  ( -11.75000000000000000, -77.79999999999999716, 1.702919296826999607E-14 ) ) ;
#38048=CARTESIAN_POINT ( 'NONE',  ( 7.331368884251999951, -75.77223222076000297, 9.888700222343000945 ) ) ;
#38049=EDGE_CURVE ( 'NONE', #43600, #20895, #10070, .T. ) ;
#38051=CARTESIAN_POINT ( 'NONE',  ( 17.49999999998999911, -28.92928575306000383, 1.613072089683000333E-05 ) ) ;
#38052=CARTESIAN_POINT ( 'NONE',  ( -1.777672186646999997, -78.83457582460000879, 12.13420648597999829 ) ) ;
#38054=CARTESIAN_POINT ( 'NONE',  ( -9.369164850722000892, -23.25000000000000000, -7.601397897754999633 ) ) ;
#38055=CARTESIAN_POINT ( 'NONE',  ( 9.210801724128419465, -77.85636445889269908, 7.879641758992598000 ) ) ;
#38057=CIRCLE ( 'NONE', #43710, 1.749999999999999556 ) ;
#38058=B_SPLINE_CURVE_WITH_KNOTS ( 'NONE', 3,
 ( #26156, #44176, #44456, #4007, #31445, #54498, #13447, #4902, #45649, #53915, #49487, #35583, #788, #5189, #30860, #35285, #9035, #36187, #27022, #40322, #4307, #26434, #45354, #18480 ),
 .UNSPECIFIED., .F., .F.,
 ( 4, 2, 2, 2, 2, 2, 2, 2, 2, 2, 2, 4 ),
 ( 0.000000000000000000, 0.1249999999999988343, 0.2499999999999976685, 0.3749999999999960587, 0.4374999999999961142, 0.4999999999999962252, 0.6249999999999952260, 0.7499999999999943379, 0.8124999999999953371, 0.8437499999999955591, 0.8749999999999957812, 1.000000000000000000 ),
 .UNSPECIFIED. ) ;
#38059=ORIENTED_EDGE ( 'NONE', *, *, #47046, .F. ) ;
#38061=CARTESIAN_POINT ( 'NONE',  ( 11.75000000000000000, -78.04999999999999716, 0.000000000000000000 ) ) ;
#38062=DIRECTION ( 'NONE',  ( 0.000000000000000000, -1.000000000000000000, 0.000000000000000000 ) ) ;
#38063=CARTESIAN_POINT ( 'NONE',  ( 1.247385801072999900, -24.47722256257999973, 12.50301438876999960 ) ) ;
#38064=CARTESIAN_POINT ( 'NONE',  ( -3.152753737320999949, -2.925781426754000325, -1.963312250333000053 ) ) ;
#38065=VECTOR ( 'NONE', #920, 1000.000000000000000 ) ;
#38067=CARTESIAN_POINT ( 'NONE',  ( -17.50000000000000000, -63.73717104351998586, -4.519588592266999650E-10 ) ) ;
#38068=ADVANCED_FACE ( 'NONE', ( #32185, #9483, #9772, #28337 ), #55219, .F. ) ;
#38069=CARTESIAN_POINT ( 'NONE',  ( -9.073759183985567134, -76.14497163204748631, 7.464983690866247024 ) ) ;
#38070=DIRECTION ( 'NONE',  ( 0.000000000000000000, 1.000000000000000000, 0.000000000000000000 ) ) ;
#38076=CARTESIAN_POINT ( 'NONE',  ( -11.75000000000000000, -76.79999999999999716, -1.435311119447000145E-14 ) ) ;
#38077=DIRECTION ( 'NONE',  ( 0.000000000000000000, 0.8191944459020620295, 0.5735158758074736518 ) ) ;
#38080=CARTESIAN_POINT ( 'NONE',  ( -1.699273914700831334, -3.183575180134248228, -2.900848162400441854 ) ) ;
#38082=CARTESIAN_POINT ( 'NONE',  ( -9.369164850722000892, -18.75000000000000000, -7.601397897754999633 ) ) ;
#38084=CARTESIAN_POINT ( 'NONE',  ( 3.947555661861085863, -77.60371600676303672, -11.64414702256997458 ) ) ;
#38091=DIRECTION ( 'NONE',  ( 0.000000000000000000, -1.000000000000000000, 0.000000000000000000 ) ) ;
#38094=CARTESIAN_POINT ( 'NONE',  ( 1.750000000001000089, -18.74999999009000007, -12.56594317857000043 ) ) ;
#38096=AXIS2_PLACEMENT_3D ( 'NONE', #17, #57840, #12957 ) ;
#38097=CARTESIAN_POINT ( 'NONE',  ( 12.70228859449407111, -53.97803615207048011, -1.213484947631863875 ) ) ;
#38103=CARTESIAN_POINT ( 'NONE',  ( 9.835237363972000324, -17.91864156569999977, 7.760968332719999196 ) ) ;
#38105=CARTESIAN_POINT ( 'NONE',  ( 7.784308188539000639, -79.14914617087998749, 8.871412621384999753 ) ) ;
#38106=DIRECTION ( 'NONE',  ( 0.000000000000000000, 0.1122098755727947705, -0.9936845293270585300 ) ) ;
#38111=CARTESIAN_POINT ( 'NONE',  ( 11.75000000000000000, -78.05690292554332643, 1.019250468234808471 ) ) ;
#38117=CARTESIAN_POINT ( 'NONE',  ( -7.709155920934738226, -60.72747430363508414, -9.998700314201723671 ) ) ;
#38118=CARTESIAN_POINT ( 'NONE',  ( -1.750000000000000000, -23.24999999688999708, 12.50000000000000000 ) ) ;
#38120=CARTESIAN_POINT ( 'NONE',  ( -7.718368845776000242, -21.74800977511999989, 10.07722254365999959 ) ) ;
#38127=B_SPLINE_CURVE_WITH_KNOTS ( 'NONE', 3,
 ( #2200, #38480, #19607, #42045, #47081, #1913, #6610, #56498, #6022, #52075, #11633, #25190, #2769, #37606, #15172, #10763 ),
 .UNSPECIFIED., .F., .F.,
 ( 4, 2, 2, 2, 2, 2, 2, 4 ),
 ( 0.000000000000000000, 0.2499999999999962252, 0.3749999999999943379, 0.4374999999999947264, 0.4999999999999951150, 0.6249999999999960032, 0.7499999999999968914, 1.000000000000000000 ),
 .UNSPECIFIED. ) ;
#38131=CARTESIAN_POINT ( 'NONE',  ( -7.631889106325000505, -18.77878585407000145, 10.36222439674000029 ) ) ;
#38133=CARTESIAN_POINT ( 'NONE',  ( -3.134290163747470270, -2.287741105247256712, -1.607198584962695520 ) ) ;
#38136=CARTESIAN_POINT ( 'NONE',  ( 1.930628539546999978, -55.57875555881000196, -12.72375828102000028 ) ) ;
#38137=EDGE_CURVE ( 'NONE', #54879, #39417, #38029, .T. ) ;
#38141=EDGE_LOOP ( 'NONE', ( #50751, #39376, #41225, #24642 ) ) ;
#38143=DIRECTION ( 'NONE',  ( 0.000000000000000000, 0.000000000000000000, -1.000000000000000000 ) ) ;
#38144=CIRCLE ( 'NONE', #12672, 5.000000000000000888 ) ;
#38145=CARTESIAN_POINT ( 'NONE',  ( -0.4701041210467000186, -61.80796934391000264, -12.54901038419999892 ) ) ;
#38146=CARTESIAN_POINT ( 'NONE',  ( -7.356278612544860707, -55.49583131490852850, 8.178338515874328252 ) ) ;
#38152=CARTESIAN_POINT ( 'NONE',  ( 11.22740784686473248, -78.47264872320555185, 3.462864101539464112 ) ) ;
#38154=ORIENTED_EDGE ( 'NONE', *, *, #20365, .T. ) ;
#38155=DIRECTION ( 'NONE',  ( 0.000000000000000000, -1.000000000000000000, 0.000000000000000000 ) ) ;
#38156=CARTESIAN_POINT ( 'NONE',  ( 13.79999999994999982, 4.699973049637762301E-11, 2.072308546948999944E-09 ) ) ;
#38157=EDGE_CURVE ( 'NONE', #3036, #42393, #50810, .T. ) ;
#38159=CARTESIAN_POINT ( 'NONE',  ( -11.87500000004000000, -79.12500000004000356, -1.061343742159000057E-08 ) ) ;
#38165=ADVANCED_FACE ( 'NONE', ( #46389 ), #17288, .T. ) ;
#38167=CARTESIAN_POINT ( 'NONE',  ( 2.062670899361999766, -18.69360215052999763, 12.83044027761000017 ) ) ;
#38169=EDGE_CURVE ( 'NONE', #42100, #29817, #24654, .T. ) ;
#38171=CYLINDRICAL_SURFACE ( 'NONE', #10172, 11.75000000000000000 ) ;
#38174=FACE_OUTER_BOUND ( 'NONE', #26324, .T. ) ;
#38176=ORIENTED_EDGE ( 'NONE', *, *, #55632, .F. ) ;
#38179=CARTESIAN_POINT ( 'NONE',  ( 1.295048492660999973, -17.47106480873999956, 12.54716442236999896 ) ) ;
#38180=DIRECTION ( 'NONE',  ( 1.411455651355999932E-10, 6.386283326366000088E-09, 1.000000000000000000 ) ) ;
#38182=CARTESIAN_POINT ( 'NONE',  ( -7.648026766753000416, -60.05000000550000294, 10.12290050090999927 ) ) ;
#38184=VECTOR ( 'NONE', #26351, 1000.000000000000000 ) ;
#38188=VERTEX_POINT ( 'NONE', #37793 ) ;
#38189=CARTESIAN_POINT ( 'NONE',  ( 12.65372179304999811, -58.55064713745999683, 1.750000000000000000 ) ) ;
#38192=CARTESIAN_POINT ( 'NONE',  ( -12.77657007944999989, -62.11210281297999813, -0.1589025507403999948 ) ) ;
#38194=CARTESIAN_POINT ( 'NONE',  ( 1.750000000000000000, -60.04999999725999515, 12.50000000000000000 ) ) ;
#38195=CARTESIAN_POINT ( 'NONE',  ( -10.01332852689000141, -18.71943464842000182, 7.654537165467999671 ) ) ;
#38196=DIRECTION ( 'NONE',  ( 0.7071067811865474617, 0.000000000000000000, 0.7071067811865474617 ) ) ;
#38199=CARTESIAN_POINT ( 'NONE',  ( -9.968462051564484838, -76.65502326558416257, 6.229966083963330625 ) ) ;
#38200=CARTESIAN_POINT ( 'NONE',  ( -6.464912241513801260E-06, -79.20362641130290626, -11.95086305119197689 ) ) ;
#38201=CARTESIAN_POINT ( 'NONE',  ( -9.929695104576000020, -54.16901065014000238, 7.973993995727001405 ) ) ;
#38206=CARTESIAN_POINT ( 'NONE',  ( 1.801750019963999971, -18.60992573277999895, -12.59656967653999970 ) ) ;
#38211=CARTESIAN_POINT ( 'NONE',  ( -3.447531475110328092, -1.267068432622050933, -0.7497128906106725887 ) ) ;
#38213=LINE ( 'NONE', #33775, #53674 ) ;
#38214=CARTESIAN_POINT ( 'NONE',  ( 10.07627163191000008, -60.04999999725999515, 7.601397897754999633 ) ) ;
#38218=AXIS2_PLACEMENT_3D ( 'NONE', #27721, #54025, #53731 ) ;
#38220=CARTESIAN_POINT ( 'NONE',  ( -12.57433760364000008, -55.08878254084000048, 1.760777649351999985 ) ) ;
#38222=CARTESIAN_POINT ( 'NONE',  ( 1.691611010926999947, -61.03082691197000287, 12.66722148972999840 ) ) ;
#38224=CARTESIAN_POINT ( 'NONE',  ( -12.00000000000000000, -60.04999999966999980, 0.000000000000000000 ) ) ;
#38225=ADVANCED_FACE ( 'NONE', ( #33057 ), #25084, .F. ) ;
#38226=CARTESIAN_POINT ( 'NONE',  ( 0.7999999997951000585, -23.14999999072999870, 11.99999999979999821 ) ) ;
#38228=ADVANCED_FACE ( 'NONE', ( #47837 ), #11237, .T. ) ;
#38230=CARTESIAN_POINT ( 'NONE',  ( 0.000000000000000000, -52.69905023022000279, 0.000000000000000000 ) ) ;
#38239=EDGE_CURVE ( 'NONE', #16697, #9567, #57236, .T. ) ;
#38240=CARTESIAN_POINT ( 'NONE',  ( 7.648026766733999615, -18.74999999413999774, 10.12290050089000104 ) ) ;
#38241=ORIENTED_EDGE ( 'NONE', *, *, #10942, .T. ) ;
#38244=ORIENTED_EDGE ( 'NONE', *, *, #13813, .T. ) ;
#38246=VERTEX_POINT ( 'NONE', #2379 ) ;
#38250=VERTEX_POINT ( 'NONE', #34214 ) ;
#38252=ORIENTED_EDGE ( 'NONE', *, *, #46337, .F. ) ;
#38253=CARTESIAN_POINT ( 'NONE',  ( -7.678667886061999681, -57.04263462147999775, 10.59548767699999949 ) ) ;
#38254=ORIENTED_EDGE ( 'NONE', *, *, #53703, .F. ) ;
#38258=CIRCLE ( 'NONE', #27880, 12.05000000000000071 ) ;
#38260=CARTESIAN_POINT ( 'NONE',  ( 11.81453738175115120, -78.72182493446904061, 3.290083300416718259 ) ) ;
#38261=FACE_OUTER_BOUND ( 'NONE', #34096, .T. ) ;
#38264=VECTOR ( 'NONE', #36727, 1000.000000000000000 ) ;
#38270=CARTESIAN_POINT ( 'NONE',  ( -3.249521313392360167, -3.093723106175902515, 0.2889460297551491585 ) ) ;
#38276=CARTESIAN_POINT ( 'NONE',  ( 0.000000000000000000, -56.01421830981000483, 13.15643568216998638 ) ) ;
#38278=CARTESIAN_POINT ( 'NONE',  ( -8.311834820408467550, -76.26188411096713082, -8.304661350511205242 ) ) ;
#38280=CARTESIAN_POINT ( 'NONE',  ( -2.931470798466000005, -1.005707716004999863, 2.126387630743999946 ) ) ;
#38281=FACE_OUTER_BOUND ( 'NONE', #11750, .T. ) ;
#38284=CARTESIAN_POINT ( 'NONE',  ( 12.54981857173999948, -25.04836586201999893, -0.03768635776136000648 ) ) ;
#38287=CARTESIAN_POINT ( 'NONE',  ( 10.27481476821000150, -76.04949241823000250, 6.317949980592000969 ) ) ;
#38291=B_SPLINE_CURVE_WITH_KNOTS ( 'NONE', 3,
 ( #24683, #47143, #6381, #34097, #33528, #11122 ),
 .UNSPECIFIED., .F., .F.,
 ( 4, 1, 1, 4 ),
 ( 0.000000000000000000, 0.3333333333333000081, 0.6666666666667000474, 1.000000000000000000 ),
 .UNSPECIFIED. ) ;
#38292=EDGE_CURVE ( 'NONE', #54222, #52985, #13537, .T. ) ;
#38294=CARTESIAN_POINT ( 'NONE',  ( -4.621634366555106510, -76.29240483638720605, -10.80276227228939234 ) ) ;
#38295=CARTESIAN_POINT ( 'NONE',  ( 10.41172548049708801, -55.27988211096354121, 7.610718780864914379 ) ) ;
#38297=DIRECTION ( 'NONE',  ( 0.9999999924279686647, 0.000000000000000000, 0.0001230612157847738313 ) ) ;
#38300=DIRECTION ( 'NONE',  ( 0.7071067811865474617, 0.7071067811865474617, -1.545239644671104046E-10 ) ) ;
#38303=VECTOR ( 'NONE', #17959, 1000.000000000000000 ) ;
#38307=VERTEX_POINT ( 'NONE', #47558 ) ;
#38308=AXIS2_PLACEMENT_3D ( 'NONE', #5047, #50510, #13597 ) ;
#38310=EDGE_CURVE ( 'NONE', #5427, #24905, #28929, .T. ) ;
#38315=ORIENTED_EDGE ( 'NONE', *, *, #4415, .T. ) ;
#38321=CARTESIAN_POINT ( 'NONE',  ( -2.841169247956853106, -2.559397276877021010, 1.638755559622367519 ) ) ;
#38326=CARTESIAN_POINT ( 'NONE',  ( 7.624341766647000362, -18.73514853758999976, -10.42531125024999916 ) ) ;
#38328=CARTESIAN_POINT ( 'NONE',  ( -11.37187252477004940, -77.21997671573330990, -3.043002530333297262 ) ) ;
#38332=CARTESIAN_POINT ( 'NONE',  ( -8.227501432777001966, -24.82538814609000255, 9.516269854983999466 ) ) ;
#38333=AXIS2_PLACEMENT_3D ( 'NONE', #42007, #1575, #5984 ) ;
#38337=CARTESIAN_POINT ( 'NONE',  ( 10.15831671673000081, -61.01991983010999832, -7.756223511098000678 ) ) ;
#38338=DIRECTION ( 'NONE',  ( 0.000000000000000000, 1.000000000000000000, 0.000000000000000000 ) ) ;
#38343=CARTESIAN_POINT ( 'NONE',  ( 10.93030503950313026, -77.83412702261058769, 4.999052250161460265 ) ) ;
#38344=CARTESIAN_POINT ( 'NONE',  ( -13.86301033151699791, -46.43897132165000130, -0.1317488955328562361 ) ) ;
#38348=DIRECTION ( 'NONE',  ( 0.000000000000000000, 0.000000000000000000, -1.000000000000000000 ) ) ;
#38351=CARTESIAN_POINT ( 'NONE',  ( -2.525108350097000187, -2.446968295937999915, -2.723651764455000457 ) ) ;
#38354=CARTESIAN_POINT ( 'NONE',  ( -8.943869871800938398, -76.14366878628676716, 7.620587988577864458 ) ) ;
#38355=CARTESIAN_POINT ( 'NONE',  ( 10.18496935385000057, -21.75064714707999869, -7.710095619702999947 ) ) ;
#38362=FACE_OUTER_BOUND ( 'NONE', #43915, .T. ) ;
#38363=CARTESIAN_POINT ( 'NONE',  ( -7.620037246310000789, -60.00567269791999792, 10.53559750860999955 ) ) ;
#38368=ORIENTED_EDGE ( 'NONE', *, *, #20439, .F. ) ;
#38372=CARTESIAN_POINT ( 'NONE',  ( -14.00000000000000000, -45.91785611817000046, 0.000000000000000000 ) ) ;
#38377=CARTESIAN_POINT ( 'NONE',  ( -7.601397897754999633, -18.75000000240999753, -10.07627163191000008 ) ) ;
#38379=AXIS2_PLACEMENT_3D ( 'NONE', #54544, #50123, #43427 ) ;
#38381=AXIS2_PLACEMENT_3D ( 'NONE', #56727, #8789, #26780 ) ;
#38383=CARTESIAN_POINT ( 'NONE',  ( 12.71005124793928509, -54.50500926681596781, -1.687536500541976903 ) ) ;
#38390=VERTEX_POINT ( 'NONE', #21518 ) ;
#38391=CARTESIAN_POINT ( 'NONE',  ( 7.647736468634000140, -18.27704514451999884, 10.13404651205999940 ) ) ;
#38394=CARTESIAN_POINT ( 'NONE',  ( 7.220923959705269013, -75.97708333333335418, -9.396085398178609438 ) ) ;
#38395=CARTESIAN_POINT ( 'NONE',  ( 11.52003294054999927, -78.03939249822001045, 5.205193576094000463 ) ) ;
#38397=DIRECTION ( 'NONE',  ( 0.000000000000000000, -1.000000000000000000, 0.000000000000000000 ) ) ;
#38398=CARTESIAN_POINT ( 'NONE',  ( 10.18496935386999880, -20.24935285395000051, 7.710095619721000659 ) ) ;
#38408=EDGE_CURVE ( 'NONE', #38188, #21151, #30473, .T. ) ;
#38410=CARTESIAN_POINT ( 'NONE',  ( -8.485281374238999419, -18.75000000000000000, 8.485281374238999419 ) ) ;
#38412=CARTESIAN_POINT ( 'NONE',  ( -7.682344222570999470, -22.76462890193000277, 10.04116292115999975 ) ) ;
#38416=CARTESIAN_POINT ( 'NONE',  ( -7.710118476736999682, -57.05022860539000362, -10.18499221088999995 ) ) ;
#38418=ORIENTED_EDGE ( 'NONE', *, *, #4638, .F. ) ;
#38423=CARTESIAN_POINT ( 'NONE',  ( -7.633403241821000051, -18.61350283651999860, 10.18127013549000104 ) ) ;
#38424=AXIS2_PLACEMENT_3D ( 'NONE', #4038, #44788, #22341 ) ;
#38426=CARTESIAN_POINT ( 'NONE',  ( -3.446482552678597600, -2.233460856228320690, 0.7286176306159007909 ) ) ;
#38429=CARTESIAN_POINT ( 'NONE',  ( 1.629367637664000057, -55.11736356569000606, -12.46114270824000059 ) ) ;
#38436=CARTESIAN_POINT ( 'NONE',  ( 11.74484861916918277, -76.95718971417709042, 1.539165031385370863 ) ) ;
#38437=CARTESIAN_POINT ( 'NONE',  ( -0.5045596072229000528, -61.93528913004999481, -12.66210649714999903 ) ) ;
#38439=DIRECTION ( 'NONE',  ( -1.996569343957000276E-14, 1.000000000000000000, -1.048636824995000113E-10 ) ) ;
#38442=CARTESIAN_POINT ( 'NONE',  ( 9.395758989562999375, -24.70491532583000449, -8.188252216825999241 ) ) ;
#38445=CARTESIAN_POINT ( 'NONE',  ( 10.11501736609056579, -78.49136027514339276, 5.984602011854717851 ) ) ;
#38446=CARTESIAN_POINT ( 'NONE',  ( -10.41172548049582680, -55.27988211093989435, -7.610718780863655830 ) ) ;
#38447=VERTEX_POINT ( 'NONE', #53110 ) ;
#38449=CONICAL_SURFACE ( 'NONE', #764, 13.94999999997000018, 0.7853981633972997312 ) ;
#38453=FACE_OUTER_BOUND ( 'NONE', #17888, .T. ) ;
#38456=EDGE_CURVE ( 'NONE', #8613, #13664, #2970, .T. ) ;
#38459=CARTESIAN_POINT ( 'NONE',  ( -10.10712711931551944, -54.33345760842059491, 7.860996423901147168 ) ) ;
#38461=CARTESIAN_POINT ( 'NONE',  ( 1.931043742978000077, -22.77795407709999864, 12.75763395695999947 ) ) ;
#38463=CARTESIAN_POINT ( 'NONE',  ( -12.59651352881000008, -23.39056208384000257, 1.801710201210000140 ) ) ;
#38466=LINE ( 'NONE', #20184, #8849 ) ;
#38469=ORIENTED_EDGE ( 'NONE', *, *, #22102, .F. ) ;
#38478=ORIENTED_EDGE ( 'NONE', *, *, #30847, .F. ) ;
#38480=CARTESIAN_POINT ( 'NONE',  ( -12.74331206680846407, -23.52649290806275317, 1.980611467279653981 ) ) ;
#38484=AXIS2_PLACEMENT_3D ( 'NONE', #19438, #41870, #50451 ) ;
#38486=CARTESIAN_POINT ( 'NONE',  ( -10.35845616727999996, -18.70221404512000163, 7.627487606607999737 ) ) ;
#38488=EDGE_CURVE ( 'NONE', #49656, #48292, #30652, .T. ) ;
#38490=CARTESIAN_POINT ( 'NONE',  ( -7.919595949288999570, -55.65000000893999754, -9.050966798898000931 ) ) ;
#38492=CARTESIAN_POINT ( 'NONE',  ( -9.643342484248000446, -53.85965044121000034, 8.260141428653000162 ) ) ;
#38494=CARTESIAN_POINT ( 'NONE',  ( 12.56594317984999876, -18.75000000536999778, -1.750000000000000000 ) ) ;
#38495=CARTESIAN_POINT ( 'NONE',  ( 1.930989179114000143, -21.75453807238000081, -12.80896991324000034 ) ) ;
#38501=ADVANCED_FACE ( 'NONE', ( #44248 ), #21804, .F. ) ;
#38502=CARTESIAN_POINT ( 'NONE',  ( -2.422546195149999804, -2.281904343863999873, 2.935532677474999907 ) ) ;
#38503=CARTESIAN_POINT ( 'NONE',  ( -12.00000000000000000, -23.25000000000000000, 1.250000000000000000 ) ) ;
#38508=CARTESIAN_POINT ( 'NONE',  ( -12.50412785609311683, -61.31985834570146920, 1.235051470172120469 ) ) ;
#38513=CARTESIAN_POINT ( 'NONE',  ( 1.044910384896000188, -61.85526494161999977, 12.77260826204000033 ) ) ;
#38516=CARTESIAN_POINT ( 'NONE',  ( -17.50000000000000000, -15.06282895647999887, -3.979079565841000010E-10 ) ) ;
#38519=CARTESIAN_POINT ( 'NONE',  ( 6.822138660719681447, -76.37385742326372906, -9.577683154303922919 ) ) ;
#38525=CARTESIAN_POINT ( 'NONE',  ( 1.010606015627170340, -3.450854123697218334, 3.127970707052925015 ) ) ;
#38528=CARTESIAN_POINT ( 'NONE',  ( 7.316118016526345080, -75.80000000000001137, 9.517257946189689122 ) ) ;
#38533=ORIENTED_EDGE ( 'NONE', *, *, #14271, .F. ) ;
#38534=CARTESIAN_POINT ( 'NONE',  ( -1.722320549981885440, -24.23663688825939388, 12.71171904436535272 ) ) ;
#38536=ORIENTED_EDGE ( 'NONE', *, *, #53765, .T. ) ;
#38537=CARTESIAN_POINT ( 'NONE',  ( 8.414570695956999913, -59.94999999967000548, -8.414570695956999913 ) ) ;
#38538=CARTESIAN_POINT ( 'NONE',  ( -11.75000000000000355, -77.31041666666665435, -1.538071403320004249 ) ) ;
#38541=B_SPLINE_SURFACE_WITH_KNOTS ( 'NONE', 3, 3, ( 
 ( #52938, #22211, #57646, #12205 ),
 ( #35481, #8935, #4214, #40222 ),
 ( #53221, #26924, #44955, #3913 ),
 ( #21916, #43803, #21633, #3349 ),
 ( #30191, #17202, #4509, #53812 ),
 ( #13053, #48512, #21345, #3629 ),
 ( #35190, #12488, #39357, #17797 ),
 ( #26054, #22511, #26625, #31346 ),
 ( #39638, #35783, #49388, #12769 ),
 ( #40521, #39924, #114, #57939 ),
 ( #17494, #52651, #48240, #7777 ) ),
 .UNSPECIFIED., .F., .F., .F.,
 ( 4, 1, 1, 1, 1, 1, 1, 1, 4 ),
 ( 4, 4 ),
 ( -0.01994574723510000175, 0.000000000000000000, 0.1666666666667000196, 0.3333333333333000081, 0.5000000000000000000, 0.6666666666667000474, 0.8333333333333000637, 1.000000000000000000, 1.020511277925000071 ),
 ( -0.3582002740325999635, 1.358574366096999997 ),
 .UNSPECIFIED. ) ;
#38543=CARTESIAN_POINT ( 'NONE',  ( 7.601397897754999633, -55.55000000278000272, -10.07627163191000008 ) ) ;
#38544=ORIENTED_EDGE ( 'NONE', *, *, #17656, .T. ) ;
#38545=CARTESIAN_POINT ( 'NONE',  ( 1.891006765463000061, -2.727532913352999966, -2.827272806746000011 ) ) ;
#38551=DIRECTION ( 'NONE',  ( 0.000000000000000000, -1.000000000000000000, 0.000000000000000000 ) ) ;
#38552=CIRCLE ( 'NONE', #55535, 1.749999999999998446 ) ;
#38561=CYLINDRICAL_SURFACE ( 'NONE', #7286, 0.5000000000000006661 ) ;
#38562=CARTESIAN_POINT ( 'NONE',  ( 0.04193593510216304943, -61.81009741308703553, -12.50649570009237088 ) ) ;
#38566=AXIS2_PLACEMENT_3D ( 'NONE', #46792, #6316, #17193 ) ;
#38567=DIRECTION ( 'NONE',  ( 0.000000000000000000, -1.000000000000000000, -3.571217395878000445E-14 ) ) ;
#38568=DIRECTION ( 'NONE',  ( 0.000000000000000000, -1.000000000000000000, 0.000000000000000000 ) ) ;
#38570=CARTESIAN_POINT ( 'NONE',  ( -9.852011461280598681, -76.24562891425179600, -6.431142245721705564 ) ) ;
#38571=CARTESIAN_POINT ( 'NONE',  ( 10.21380041495000057, -19.22847221992000044, 7.668936932643000581 ) ) ;
#38572=CARTESIAN_POINT ( 'NONE',  ( -7.981656248376999940, -61.51865039470999363, -10.08154475893999980 ) ) ;
#38573=EDGE_CURVE ( 'NONE', #24315, #3549, #54436, .T. ) ;
#38575=CARTESIAN_POINT ( 'NONE',  ( 10.18589234709999936, -60.08917565288000162, 7.641012386057000505 ) ) ;
#38579=CARTESIAN_POINT ( 'NONE',  ( -11.75000000000000000, -78.20000000000000284, 1.702919296826999607E-14 ) ) ;
#38580=DIRECTION ( 'NONE',  ( 0.000000000000000000, -1.000000000000000000, 0.000000000000000000 ) ) ;
#38581=CARTESIAN_POINT ( 'NONE',  ( 12.22350170820999971, -76.34339105127999403, 1.846593319174999914 ) ) ;
#38582=VERTEX_POINT ( 'NONE', #50159 ) ;
#38586=CARTESIAN_POINT ( 'NONE',  ( 12.66322140213000047, -61.98161935699999958, 0.1487435796151000134 ) ) ;
#38587=CARTESIAN_POINT ( 'NONE',  ( 9.328308112513999717, -79.06345638111000085, 8.294084752732000965 ) ) ;
#38588=DIRECTION ( 'NONE',  ( 0.6489586469979888861, 0.04890178911492917835, 0.7592504787669867028 ) ) ;
#38590=DIRECTION ( 'NONE',  ( 0.000000000000000000, 0.000000000000000000, 1.000000000000000000 ) ) ;
#38596=FACE_OUTER_BOUND ( 'NONE', #27562, .T. ) ;
#38597=AXIS2_PLACEMENT_3D ( 'NONE', #8077, #52386, #30503 ) ;
#38599=EDGE_LOOP ( 'NONE', ( #51367, #17191, #50611, #30103 ) ) ;
#38600=CARTESIAN_POINT ( 'NONE',  ( -9.837756817742013382, -61.11467795346588616, -7.850057933508078456 ) ) ;
#38605=CIRCLE ( 'NONE', #7511, 14.00000000000000000 ) ;
#38606=ORIENTED_EDGE ( 'NONE', *, *, #22137, .T. ) ;
#38607=EDGE_LOOP ( 'NONE', ( #52774, #20183, #5147, #54793, #46017, #54771, #52098, #22038, #42698, #36350, #57234, #14313 ) ) ;
#38608=AXIS2_PLACEMENT_3D ( 'NONE', #462, #45609, #13407 ) ;
#38613=CARTESIAN_POINT ( 'NONE',  ( 12.54976795928000044, -53.75224499974000025, -0.05636009750360999881 ) ) ;
#38618=CARTESIAN_POINT ( 'NONE',  ( 7.633088938737000007, -55.40992532391999958, 10.18115029110999892 ) ) ;
#38619=DIRECTION ( 'NONE',  ( -0.7071067811865474617, 0.000000000000000000, -0.7071067811865474617 ) ) ;
#38621=CARTESIAN_POINT ( 'NONE',  ( -7.224190341809336502, -77.27152570786351760, -9.395875115591328708 ) ) ;
#38622=ADVANCED_FACE ( 'NONE', ( #55149 ), #50449, .F. ) ;
#38627=CARTESIAN_POINT ( 'NONE',  ( 10.69843650790000034, -76.23917683518000388, 6.089250768039999429 ) ) ;
#38630=CARTESIAN_POINT ( 'NONE',  ( 9.213114944054998645, -61.80524898723000149, -8.533795138624000742 ) ) ;
#38631=CARTESIAN_POINT ( 'NONE',  ( -11.38660623898999980, -79.01294608163999555, -4.554589311945999697 ) ) ;
#38633=CARTESIAN_POINT ( 'NONE',  ( -17.50000000000000000, -57.79999999999999716, 0.000000000000000000 ) ) ;
#38634=FACE_OUTER_BOUND ( 'NONE', #11043, .T. ) ;
#38640=DIRECTION ( 'NONE',  ( 1.000000000000000000, 0.000000000000000000, 0.000000000000000000 ) ) ;
#38642=CARTESIAN_POINT ( 'NONE',  ( 2.804370767623999949, -2.074558083080999982, -2.435155557110000313 ) ) ;
#38645=CARTESIAN_POINT ( 'NONE',  ( 12.00000000000000000, -18.84999999999999787, 0.000000000000000000 ) ) ;
#38648=VERTEX_POINT ( 'NONE', #27106 ) ;
#38649=CARTESIAN_POINT ( 'NONE',  ( 14.00000000000000000, -46.09579702914000165, -3.101615809226999909E-11 ) ) ;
#38653=CARTESIAN_POINT ( 'NONE',  ( -7.948089776799000639, -61.24033979686999629, 9.636757666110000287 ) ) ;
#38656=DIRECTION ( 'NONE',  ( -1.000000000000000000, 0.000000000000000000, 0.000000000000000000 ) ) ;
#38657=CARTESIAN_POINT ( 'NONE',  ( -12.70395600756426724, -54.19327811275147155, -1.447166682400345294 ) ) ;
#38658=ORIENTED_EDGE ( 'NONE', *, *, #44954, .T. ) ;
#38659=DIRECTION ( 'NONE',  ( 0.000000000000000000, 1.000000000000000000, 0.000000000000000000 ) ) ;
#38664=ORIENTED_EDGE ( 'NONE', *, *, #29472, .F. ) ;
#38668=CARTESIAN_POINT ( 'NONE',  ( 2.062673488410000200, -55.47547726255000100, -12.82904109059999875 ) ) ;
#38669=ADVANCED_FACE ( 'NONE', ( #45143 ), #57738, .T. ) ;
#38672=DIRECTION ( 'NONE',  ( -1.000000000000000000, 0.000000000000000000, 0.000000000000000000 ) ) ;
#38673=VERTEX_POINT ( 'NONE', #24735 ) ;
#38674=ORIENTED_EDGE ( 'NONE', *, *, #38831, .F. ) ;
#38677=ORIENTED_EDGE ( 'NONE', *, *, #52545, .T. ) ;
#38678=CARTESIAN_POINT ( 'NONE',  ( 9.650965486090999690, -17.06598967526999999, 8.252456812006998987 ) ) ;
#38680=DIRECTION ( 'NONE',  ( 0.000000000000000000, -0.7071067811866525998, -0.7071067811864425456 ) ) ;
#38681=CIRCLE ( 'NONE', #7467, 0.6000000000000008660 ) ;
#38682=CARTESIAN_POINT ( 'NONE',  ( 1.931736162948486379, -55.03329604253293184, 12.72978979887180095 ) ) ;
#38683=CARTESIAN_POINT ( 'NONE',  ( -9.533257042556000371, -78.61836734003000515, 6.958047573390000018 ) ) ;
#38685=FACE_BOUND ( 'NONE', #56059, .T. ) ;
#38695=CARTESIAN_POINT ( 'NONE',  ( 11.79999999999999893, -23.15000000000999947, 0.5999999999999999778 ) ) ;
#38699=DIRECTION ( 'NONE',  ( 0.000000000000000000, 0.000000000000000000, 1.000000000000000000 ) ) ;
#38701=CARTESIAN_POINT ( 'NONE',  ( 0.000000000000000000, -0.5000000000000000000, 0.000000000000000000 ) ) ;
#38705=CARTESIAN_POINT ( 'NONE',  ( 12.00000000000000000, -23.25000000000000000, -1.750000000000000000 ) ) ;
#38707=CARTESIAN_POINT ( 'NONE',  ( -12.50409240828718360, -61.32129362315841092, -1.233800930083493563 ) ) ;
#38708=ORIENTED_EDGE ( 'NONE', *, *, #26796, .T. ) ;
#38711=LINE ( 'NONE', #11861, #34191 ) ;
#38712=EDGE_CURVE ( 'NONE', #22044, #34387, #26619, .T. ) ;
#38714=DIRECTION ( 'NONE',  ( 0.7071067810866970005, 6.386292029988980325E-09, -0.7071067812863980340 ) ) ;
#38716=CARTESIAN_POINT ( 'NONE',  ( -0.9429918526208548313, -1.853499113097019979, -3.393197731231969438 ) ) ;
#38723=ORIENTED_EDGE ( 'NONE', *, *, #38239, .F. ) ;
#38725=CARTESIAN_POINT ( 'NONE',  ( 0.5154756746309999693, -61.93240599730000184, -12.66205448077000106 ) ) ;
#38726=DIRECTION ( 'NONE',  ( 0.7071067811865474617, 0.000000000000000000, -0.7071067811865474617 ) ) ;
#38730=CARTESIAN_POINT ( 'NONE',  ( 10.18949719146000099, -23.21529250218000229, -7.645392405660000001 ) ) ;
#38734=CARTESIAN_POINT ( 'NONE',  ( -9.697372265369081035, -61.77233735005969351, 8.266620275728032041 ) ) ;
#38735=ORIENTED_EDGE ( 'NONE', *, *, #9374, .T. ) ;
#38741=DIRECTION ( 'NONE',  ( -0.7071067812863980340, 6.386274622742979319E-09, -0.7071067810866970005 ) ) ;
#38742=FACE_OUTER_BOUND ( 'NONE', #1451, .T. ) ;
#38748=ADVANCED_FACE ( 'NONE', ( #38596 ), #14991, .T. ) ;
#38749=CARTESIAN_POINT ( 'NONE',  ( 2.062673488738000049, -18.67547470641000018, 12.82904091339000097 ) ) ;
#38751=CARTESIAN_POINT ( 'NONE',  ( 5.917523019358037040, -76.13333333333329733, 10.26699006316254525 ) ) ;
#38753=VERTEX_POINT ( 'NONE', #24148 ) ;
#38754=CONICAL_SURFACE ( 'NONE', #53849, 0.6999999997694995590, 0.7853981633972997312 ) ;
#38755=CARTESIAN_POINT ( 'NONE',  ( -12.49830607526000037, -55.59028586401999661, -1.666977523254999927 ) ) ;
#38756=ORIENTED_EDGE ( 'NONE', *, *, #38408, .F. ) ;
#38757=ORIENTED_EDGE ( 'NONE', *, *, #9374, .F. ) ;
#38758=CARTESIAN_POINT ( 'NONE',  ( 10.36221643468999964, -23.22123873666000193, 7.631895748949999891 ) ) ;
#38761=DIRECTION ( 'NONE',  ( 0.000000000000000000, 1.000000000000000000, 0.000000000000000000 ) ) ;
#38767=CIRCLE ( 'NONE', #37840, 1.750000000000000000 ) ;
#38769=CARTESIAN_POINT ( 'NONE',  ( -12.25000000000000000, -80.79999999999999716, 0.000000000000000000 ) ) ;
#38773=CARTESIAN_POINT ( 'NONE',  ( 8.611000705980396575, -61.97488119190063571, 9.355851007348242376 ) ) ;
#38774=CARTESIAN_POINT ( 'NONE',  ( 1.750000000001000089, -18.75000001325000198, 12.56594318051000059 ) ) ;
#38776=DIRECTION ( 'NONE',  ( 0.000000000000000000, -1.000000000000000000, 0.000000000000000000 ) ) ;
#38780=EDGE_CURVE ( 'NONE', #42403, #47034, #28855, .T. ) ;
#38782=FACE_OUTER_BOUND ( 'NONE', #46407, .T. ) ;
#38783=CARTESIAN_POINT ( 'NONE',  ( 7.655542440085000067, -59.57819125629999490, 10.38645071868999992 ) ) ;
#38784=CARTESIAN_POINT ( 'NONE',  ( 1.477284502223000118, -17.27368499703000282, -12.77254812468999923 ) ) ;
#38787=CARTESIAN_POINT ( 'NONE',  ( 12.85140862673999784, -21.75560170163999985, 1.980464483675000054 ) ) ;
#38789=CARTESIAN_POINT ( 'NONE',  ( 3.313572498374643072, -3.500000000000000888, 1.146852011088394852 ) ) ;
#38790=DIRECTION ( 'NONE',  ( 0.9999999999999693578, 2.479738742161926003E-07, 1.114546890279966179E-12 ) ) ;
#38791=VERTEX_POINT ( 'NONE', #20308 ) ;
#38795=CARTESIAN_POINT ( 'NONE',  ( -3.625242457524000095, -3.139913721651000245, -0.3865940047836999849 ) ) ;
#38798=CARTESIAN_POINT ( 'NONE',  ( -12.70956139856000000, -55.39498835716000258, 1.933780970937999832 ) ) ;
#38799=FACE_OUTER_BOUND ( 'NONE', #45722, .T. ) ;
#38801=CARTESIAN_POINT ( 'NONE',  ( -3.165411199172024848, -3.020833333333332593, -0.8506806241676611036 ) ) ;
#38804=CARTESIAN_POINT ( 'NONE',  ( 0.000000000000000000, -18.84999999999999787, 12.00000000000000000 ) ) ;
#38808=CARTESIAN_POINT ( 'NONE',  ( 8.288812145454857117, -76.38727426244473406, -8.328108146873651307 ) ) ;
#38817=CARTESIAN_POINT ( 'NONE',  ( 9.723174505952000501, -24.47697504198000118, 7.958760297001999717 ) ) ;
#38823=CARTESIAN_POINT ( 'NONE',  ( -1.501534314726683306, -24.55152951662029892, 12.70455943739977656 ) ) ;
#38825=ORIENTED_EDGE ( 'NONE', *, *, #10734, .F. ) ;
#38827=CARTESIAN_POINT ( 'NONE',  ( 1.081559480311999888, -3.500000000000000000, -3.328697807033000000 ) ) ;
#38831=EDGE_CURVE ( 'NONE', #40540, #49656, #34170, .T. ) ;
#38832=ORIENTED_EDGE ( 'NONE', *, *, #21070, .T. ) ;
#38836=ORIENTED_EDGE ( 'NONE', *, *, #8592, .F. ) ;
#38839=DIRECTION ( 'NONE',  ( 0.000000000000000000, -1.000000000000000000, 0.000000000000000000 ) ) ;
#38843=FACE_OUTER_BOUND ( 'NONE', #44635, .T. ) ;
#38849=DIRECTION ( 'NONE',  ( 0.7071067811814418791, 1.254535583516073644E-07, 0.7071067811916420531 ) ) ;
#38850=CARTESIAN_POINT ( 'NONE',  ( 2.231512935965016986, -2.915198822935428868, 2.362588882341296603 ) ) ;
#38853=CARTESIAN_POINT ( 'NONE',  ( 1.001315002179000047, -24.68522411714000242, -12.50000000000000000 ) ) ;
#38854=CARTESIAN_POINT ( 'NONE',  ( -12.51072239526000196, -63.10294702885996543, -0.7871079366006996647 ) ) ;
#38858=CARTESIAN_POINT ( 'NONE',  ( -8.252521514740998043, -61.73405767862000459, -9.650901483168000894 ) ) ;
#38862=CARTESIAN_POINT ( 'NONE',  ( -10.64207148833999916, -76.96853494252998473, 7.489034475093999887 ) ) ;
#38866=CARTESIAN_POINT ( 'NONE',  ( 0.1380878923104814915, -25.22734402325045977, -12.70555840932425085 ) ) ;
#38867=CARTESIAN_POINT ( 'NONE',  ( 1.430780206329000048, -75.86025915096999483, 12.43029443217000107 ) ) ;
#38868=B_SPLINE_CURVE_WITH_KNOTS ( 'NONE', 3,
 ( #40104, #30363, #4092, #16525, #53392, #52820 ),
 .UNSPECIFIED., .F., .F.,
 ( 4, 1, 1, 4 ),
 ( 0.000000000000000000, 0.3333333333333000081, 0.6666666666667000474, 1.000000000000000000 ),
 .UNSPECIFIED. ) ;
#38869=VERTEX_POINT ( 'NONE', #54220 ) ;
#38872=CARTESIAN_POINT ( 'NONE',  ( 12.54673765600000124, -61.62199238204999574, 0.9174244429637000708 ) ) ;
#38873=CARTESIAN_POINT ( 'NONE',  ( 12.74575047010000084, -78.83831324550000375, 1.100459882033999914 ) ) ;
#38874=CARTESIAN_POINT ( 'NONE',  ( -2.062670899361999766, -18.69360215052999763, -12.83044027761000017 ) ) ;
#38883=VERTEX_POINT ( 'NONE', #40338 ) ;
#38884=ADVANCED_FACE ( 'NONE', ( #802 ), #13163, .F. ) ;
#38886=CARTESIAN_POINT ( 'NONE',  ( 12.71658889739000031, -55.48415522678000400, 1.931087888049999979 ) ) ;
#38889=ORIENTED_EDGE ( 'NONE', *, *, #9007, .T. ) ;
#38896=EDGE_CURVE ( 'NONE', #9459, #41516, #14337, .T. ) ;
#38897=ORIENTED_EDGE ( 'NONE', *, *, #37648, .T. ) ;
#38898=CARTESIAN_POINT ( 'NONE',  ( 1.638719174300647730, -2.434540441116925358, 2.841788563852642557 ) ) ;
#38900=DIRECTION ( 'NONE',  ( 1.000000000000000000, 0.000000000000000000, 0.000000000000000000 ) ) ;
#38903=CARTESIAN_POINT ( 'NONE',  ( 9.641218323587999350, -54.36606991882000273, 7.943737929401001985 ) ) ;
#38904=CARTESIAN_POINT ( 'NONE',  ( 7.864797288620628990, -17.54877151179043793, -10.10445166986456123 ) ) ;
#38905=CARTESIAN_POINT ( 'NONE',  ( -7.612971414713999962, -23.32452529362999982, -10.53003223722999948 ) ) ;
#38907=CARTESIAN_POINT ( 'NONE',  ( 12.74331206683557660, -60.32649290773598239, -1.980611467281674365 ) ) ;
#38910=CARTESIAN_POINT ( 'NONE',  ( -7.605690822180000588, -23.42565082156999878, 10.52682217035000001 ) ) ;
#38911=ADVANCED_FACE ( 'NONE', ( #517 ), #41505, .F. ) ;
#38914=CARTESIAN_POINT ( 'NONE',  ( 8.541150802335000236, -61.80800189248000009, -9.205830468624000673 ) ) ;
#38915=CARTESIAN_POINT ( 'NONE',  ( -10.39285214024000048, -78.40346505345000594, 6.510605926401999533 ) ) ;
#38917=CARTESIAN_POINT ( 'NONE',  ( -7.364280830344099193, -60.14010097497214247, -8.171144579306195865 ) ) ;
#38918=CARTESIAN_POINT ( 'NONE',  ( -5.869402599192000025, -78.46567021303999923, 10.46661899222999992 ) ) ;
#38919=DIRECTION ( 'NONE',  ( 0.000000000000000000, 0.000000000000000000, -1.000000000000000000 ) ) ;
#38922=FACE_OUTER_BOUND ( 'NONE', #19888, .T. ) ;
#38925=CARTESIAN_POINT ( 'NONE',  ( -1.703108177512000054, -3.472353339067000277, 2.944283159703000141 ) ) ;
#38928=CARTESIAN_POINT ( 'NONE',  ( -6.577478410916997476, -75.79999999999999716, 9.905072954783767258 ) ) ;
#38931=CARTESIAN_POINT ( 'NONE',  ( -7.651147547633000201, -19.23743349724999874, 10.45204383579999963 ) ) ;
#38934=VECTOR ( 'NONE', #23508, 1000.000000000000000 ) ;
#38938=CARTESIAN_POINT ( 'NONE',  ( -7.633089125635001082, -60.19007426270999872, 10.18115018433999985 ) ) ;
#38939=CARTESIAN_POINT ( 'NONE',  ( -2.973381617294999835, -0.5899651668208000244, -1.916927929355999982 ) ) ;
#38941=CARTESIAN_POINT ( 'NONE',  ( 7.646944981223999349, -18.80364172516999943, -10.19022195330999914 ) ) ;
#38943=B_SPLINE_CURVE_WITH_KNOTS ( 'NONE', 3,
 ( #18983, #46156, #5974, #10414, #5681, #10715, #37852, #23978, #1565, #11006 ),
 .UNSPECIFIED., .F., .F.,
 ( 4, 2, 2, 2, 4 ),
 ( 0.4999998626202952212, 0.6249998969652212910, 0.7499999313101475273, 0.8749999656550737637, 1.000000000000000000 ),
 .UNSPECIFIED. ) ;
#38944=ORIENTED_EDGE ( 'NONE', *, *, #32191, .T. ) ;
#38946=DIRECTION ( 'NONE',  ( 0.7071067811865474617, 0.000000000000000000, -0.7071067811865474617 ) ) ;
#38949=VECTOR ( 'NONE', #38588, 1000.000000000000114 ) ;
#38950=EDGE_CURVE ( 'NONE', #19368, #52985, #45664, .T. ) ;
#38951=CARTESIAN_POINT ( 'NONE',  ( -10.53101990617999917, -55.49360215019999742, -7.613962745591999592 ) ) ;
#38953=ORIENTED_EDGE ( 'NONE', *, *, #57042, .T. ) ;
#38954=EDGE_CURVE ( 'NONE', #52059, #4183, #31755, .T. ) ;
#38961=ORIENTED_EDGE ( 'NONE', *, *, #44074, .F. ) ;
#38967=VERTEX_POINT ( 'NONE', #22916 ) ;
#38968=CARTESIAN_POINT ( 'NONE',  ( 12.56594317823000040, -18.74999998606000062, 1.750000000000000000 ) ) ;
#38970=CARTESIAN_POINT ( 'NONE',  ( -1.308715794756476702, -54.05595500772570716, 12.70256747352372351 ) ) ;
#38971=CARTESIAN_POINT ( 'NONE',  ( -12.75936573546999853, -77.67478844368000068, -1.003864233875000123 ) ) ;
#38972=B_SPLINE_CURVE_WITH_KNOTS ( 'NONE', 3,
 ( #22727, #18309, #36301, #39564, #57566, #30689, #26270, #21839 ),
 .UNSPECIFIED., .F., .F.,
 ( 4, 2, 2, 4 ),
 ( 0.000000000000000000, 0.4999999999999945599, 0.7499999999999972244, 1.000000000000000000 ),
 .UNSPECIFIED. ) ;
#38974=CARTESIAN_POINT ( 'NONE',  ( -1.750000000000000000, -23.24999999688999708, 12.50000000000000000 ) ) ;
#38975=CARTESIAN_POINT ( 'NONE',  ( 0.000000000000000000, 4.040000000000000036, 0.000000000000000000 ) ) ;
#38977=DIRECTION ( 'NONE',  ( -1.000000000000000000, 0.000000000000000000, 0.000000000000000000 ) ) ;
#38978=EDGE_LOOP ( 'NONE', ( #53882, #46815, #39041, #35353, #34091, #10687 ) ) ;
#38980=VERTEX_POINT ( 'NONE', #49198 ) ;
#38991=DIRECTION ( 'NONE',  ( -0.9936845293270585300, -0.1122098755727947705, 0.000000000000000000 ) ) ;
#38993=CIRCLE ( 'NONE', #27649, 1.749999999999999778 ) ;
#38995=CARTESIAN_POINT ( 'NONE',  ( 10.59551070215999857, -20.24351820077000141, -7.678690995240000206 ) ) ;
#38997=CARTESIAN_POINT ( 'NONE',  ( -3.370516864494922604, -1.912300517193705529, -0.5569799872951896047 ) ) ;
#38998=CARTESIAN_POINT ( 'NONE',  ( -12.52785920748594428, -60.59405666895369791, -1.668536824536160035 ) ) ;
#39007=CARTESIAN_POINT ( 'NONE',  ( -1.680220311666482003, -1.835405696757452132, -3.096472680378186570 ) ) ;
#39011=DIRECTION ( 'NONE',  ( -0.7071067812094167238, -2.924114041541068650E-07, -0.7071067811636178035 ) ) ;
#39013=ORIENTED_EDGE ( 'NONE', *, *, #25745, .F. ) ;
#39021=CARTESIAN_POINT ( 'NONE',  ( 10.13694968398000107, -23.70834319340999841, -7.646073915527999532 ) ) ;
#39024=CARTESIAN_POINT ( 'NONE',  ( 12.00000000000000000, -18.84999999997999964, -0.7999999999999001243 ) ) ;
#39025=CARTESIAN_POINT ( 'NONE',  ( -10.07627163191000008, -18.75000000240999753, 7.601397897754999633 ) ) ;
#39026=ORIENTED_EDGE ( 'NONE', *, *, #47978, .F. ) ;
#39028=CARTESIAN_POINT ( 'NONE',  ( -8.485281374238999419, -60.74999999967048581, 8.485281374238999419 ) ) ;
#39030=VECTOR ( 'NONE', #47915, 1000.000000000000000 ) ;
#39032=ADVANCED_FACE ( 'NONE', ( #27036 ), #49501, .T. ) ;
#39039=CARTESIAN_POINT ( 'NONE',  ( 1.034214221880000141E-14, 0.2999999999999999334, 0.000000000000000000 ) ) ;
#39040=CARTESIAN_POINT ( 'NONE',  ( -12.68624828429000040, -23.76426636002999970, 1.886933512377000133 ) ) ;
#39041=ORIENTED_EDGE ( 'NONE', *, *, #31899, .T. ) ;
#39042=ORIENTED_EDGE ( 'NONE', *, *, #36699, .T. ) ;
#39043=CARTESIAN_POINT ( 'NONE',  ( -12.77568125274000010, -53.53490786090000597, -0.5296379231473000715 ) ) ;
#39046=PLANE ( 'NONE',  #27346 ) ;
#39052=VERTEX_POINT ( 'NONE', #18210 ) ;
#39055=DIRECTION ( 'NONE',  ( 0.000000000000000000, 0.000000000000000000, 1.000000000000000000 ) ) ;
#39056=CARTESIAN_POINT ( 'NONE',  ( -12.79972228485999963, -60.59021513420999838, -2.019125729023000027 ) ) ;
#39059=CARTESIAN_POINT ( 'NONE',  ( 7.624341766656999475, -60.06485146221000093, 10.42531125026000005 ) ) ;
#39064=CARTESIAN_POINT ( 'NONE',  ( 1.980464439859999981, -58.55472017426999543, 12.85144117154000121 ) ) ;
#39065=CARTESIAN_POINT ( 'NONE',  ( -9.759527141425989427, -76.65258383443992329, 6.542760971238160472 ) ) ;
#39067=VERTEX_POINT ( 'NONE', #36201 ) ;
#39068=CARTESIAN_POINT ( 'NONE',  ( -8.188285776285999518, -54.09506253957000155, 9.395726099541001020 ) ) ;
#39070=AXIS2_PLACEMENT_3D ( 'NONE', #10756, #31994, #50034 ) ;
#39072=CARTESIAN_POINT ( 'NONE',  ( -10.01676960212000012, -18.79061945240999876, -7.658895148207999881 ) ) ;
#39074=CARTESIAN_POINT ( 'NONE',  ( 7.705142895613999343, -57.04916621739000249, 10.24998526317999925 ) ) ;
#39075=CARTESIAN_POINT ( 'NONE',  ( -0.005119011380219999283, -17.06186137810999881, -12.43705489344000092 ) ) ;
#39080=CARTESIAN_POINT ( 'NONE',  ( 12.50680023853920630, -24.30414033429958209, 1.424451025645361302 ) ) ;
#39082=EDGE_CURVE ( 'NONE', #25591, #52707, #12481, .T. ) ;
#39083=ORIENTED_EDGE ( 'NONE', *, *, #51017, .T. ) ;
#39085=CARTESIAN_POINT ( 'NONE',  ( -12.50659871785105892, -24.97347219492468540, 0.3508073941911192817 ) ) ;
#39086=CARTESIAN_POINT ( 'NONE',  ( -12.71658872085999903, -18.68415268018999953, 1.931087888240000217 ) ) ;
#39087=CARTESIAN_POINT ( 'NONE',  ( 3.596145366532999876, -2.894607885732999986, 0.5996453614708999735 ) ) ;
#39088=DIRECTION ( 'NONE',  ( 1.000000000000000000, 0.000000000000000000, 0.000000000000000000 ) ) ;
#39090=CARTESIAN_POINT ( 'NONE',  ( -12.77657003520000067, -53.48789974419999993, 0.1588669551757000142 ) ) ;
#39091=CARTESIAN_POINT ( 'NONE',  ( 2.062312494845999655, -60.02715659860000130, 12.83634740211000036 ) ) ;
#39093=CARTESIAN_POINT ( 'NONE',  ( 0.000000000000000000, -32.88214388149999934, 0.000000000000000000 ) ) ;
#39097=CARTESIAN_POINT ( 'NONE',  ( 10.11784875172895148, -76.40690788625481389, -5.985750144463405142 ) ) ;
#39100=CARTESIAN_POINT ( 'NONE',  ( 8.838834764832000701, -55.54999999966999980, -8.838834764832000701 ) ) ;
#39101=CARTESIAN_POINT ( 'NONE',  ( 7.710118476742000126, -20.25022860572000027, 10.18499221090000084 ) ) ;
#39102=DIRECTION ( 'NONE',  ( 0.000000000000000000, -1.000000000000000000, 0.000000000000000000 ) ) ;
#39106=CARTESIAN_POINT ( 'NONE',  ( -7.624341764923000753, -18.73514850530999709, -10.42531124853000080 ) ) ;
#39108=CARTESIAN_POINT ( 'NONE',  ( 7.958763982157000427, -54.32301960771999916, 9.723170657500999070 ) ) ;
#39113=EDGE_LOOP ( 'NONE', ( #9719, #24014, #44787, #363, #168, #25897 ) ) ;
#39114=ADVANCED_FACE ( 'NONE', ( #6947 ), #6656, .F. ) ;
#39115=CARTESIAN_POINT ( 'NONE',  ( -1.081559480311999888, -0.7500000000000000000, 3.328697807033000000 ) ) ;
#39118=ORIENTED_EDGE ( 'NONE', *, *, #37333, .T. ) ;
#39120=ORIENTED_EDGE ( 'NONE', *, *, #11118, .F. ) ;
#39127=CARTESIAN_POINT ( 'NONE',  ( 12.50000000000000000, -23.24999999688999708, 1.750000000000000000 ) ) ;
#39129=DIRECTION ( 'NONE',  ( 0.7026410690473250398, -0.1122098755728047209, -0.7026410690473250398 ) ) ;
#39130=EDGE_CURVE ( 'NONE', #36944, #20252, #56789, .T. ) ;
#39131=CARTESIAN_POINT ( 'NONE',  ( 0.000000000000000000, -49.87071424677999687, 0.000000000000000000 ) ) ;
#39133=DIRECTION ( 'NONE',  ( 0.000000000000000000, 0.000000000000000000, 1.000000000000000000 ) ) ;
#39137=FACE_OUTER_BOUND ( 'NONE', #29501, .T. ) ;
#39139=AXIS2_PLACEMENT_3D ( 'NONE', #22426, #45174, #54321 ) ;
#39141=CARTESIAN_POINT ( 'NONE',  ( 2.613303202534924541, -2.902163255836463840, 1.941981267590990656 ) ) ;
#39143=CARTESIAN_POINT ( 'NONE',  ( 3.250000000000000000, -1.250000000000000000, 0.000000000000000000 ) ) ;
#39146=CARTESIAN_POINT ( 'NONE',  ( -3.448863046786000197, -1.782744131007000021, -1.608907009436000068 ) ) ;
#39149=CARTESIAN_POINT ( 'NONE',  ( -7.756281347497000489, -61.02006031080999549, -10.15825374577000062 ) ) ;
#39153=B_SPLINE_CURVE_WITH_KNOTS ( 'NONE', 3,
 ( #11780, #43080, #48660, #52507, #57503, #12064 ),
 .UNSPECIFIED., .F., .F.,
 ( 4, 2, 4 ),
 ( 0.000000000000000000, 0.5000000000000000000, 1.000000000000000000 ),
 .UNSPECIFIED. ) ;
#39154=CARTESIAN_POINT ( 'NONE',  ( 12.57042253521000141, -26.10094976978000147, 0.000000000000000000 ) ) ;
#39155=CARTESIAN_POINT ( 'NONE',  ( 5.512103878356000131, -76.89219232727998588, 11.78783395355999986 ) ) ;
#39157=CARTESIAN_POINT ( 'NONE',  ( 1.980584515752000119, -23.26485146623999967, -12.76303204602000108 ) ) ;
#39158=CARTESIAN_POINT ( 'NONE',  ( -1.099509683757999845, -76.19937248742999714, -12.31320345612999922 ) ) ;
#39159=ORIENTED_EDGE ( 'NONE', *, *, #16105, .T. ) ;
#39161=CARTESIAN_POINT ( 'NONE',  ( 12.55486071739000131, -60.95393632975000031, 1.580832792523999775 ) ) ;
#39162=CARTESIAN_POINT ( 'NONE',  ( 6.122063361877000176, -79.24616473471999711, -11.23243970840999850 ) ) ;
#39163=CARTESIAN_POINT ( 'NONE',  ( 7.668936932643000581, -19.22847221992000044, -10.21380041495000057 ) ) ;
#39166=CARTESIAN_POINT ( 'NONE',  ( -12.56594317984999876, -18.75000000536999778, 1.750000000000000000 ) ) ;
#39168=ORIENTED_EDGE ( 'NONE', *, *, #3634, .T. ) ;
#39171=ORIENTED_EDGE ( 'NONE', *, *, #5160, .T. ) ;
#39173=CARTESIAN_POINT ( 'NONE',  ( -7.452378523310481562, -55.25278097498677710, -8.090910852015047894 ) ) ;
#39174=VECTOR ( 'NONE', #299, 1000.000000000000000 ) ;
#39176=EDGE_LOOP ( 'NONE', ( #172, #19741, #51343, #15879, #56627 ) ) ;
#39183=CARTESIAN_POINT ( 'NONE',  ( 12.43641395959999940, -53.88198970716000247, -0.03481089025435999545 ) ) ;
#39184=ORIENTED_EDGE ( 'NONE', *, *, #42515, .T. ) ;
#39185=CARTESIAN_POINT ( 'NONE',  ( -12.26143800982999998, -79.05153930436631526, -0.2371146996492999870 ) ) ;
#39187=CARTESIAN_POINT ( 'NONE',  ( 8.260145278118999457, -53.85964900942000355, 9.643338478971999805 ) ) ;
#39189=DIRECTION ( 'NONE',  ( 0.7071067811865475727, 0.000000000000000000, 0.7071067811865475727 ) ) ;
#39191=CARTESIAN_POINT ( 'NONE',  ( 7.765002223030514017, -77.37977859133056313, -8.854379362200837988 ) ) ;
#39193=CARTESIAN_POINT ( 'NONE',  ( -8.485281374238999419, -23.25000000000000000, 8.485281374238999419 ) ) ;
#39195=CARTESIAN_POINT ( 'NONE',  ( -7.659225027811000786, -23.68266641665999828, 9.963489011784998794 ) ) ;
#39198=CARTESIAN_POINT ( 'NONE',  ( -12.66315144086999922, -16.82197088188999601, -0.06064144874954999209 ) ) ;
#39203=CARTESIAN_POINT ( 'NONE',  ( -3.245126138204999844, -1.829671397435000069, -1.541643571398999990 ) ) ;
#39204=DIRECTION ( 'NONE',  ( 0.9999999924279685537, 0.000000000000000000, 0.0001230612157836962969 ) ) ;
#39208=CARTESIAN_POINT ( 'NONE',  ( 12.70926857202000093, -60.20841990675999966, -1.933876778424000076 ) ) ;
#39210=B_SPLINE_CURVE_WITH_KNOTS ( 'NONE', 3,
 ( #47465, #52445, #47746, #10855, #7279, #34121, #2570, #20282, #38570, #25281, #2855, #15264, #1705, #20852, #24421, #56876, #12004, #29983, #56584, #19699, #38278, #15851, #55717, #28828, #42435, #33257, #6112, #33839, #37985, #16144, #51299, #56010, #15560, #46087, #41635, #18913, #31295, #4459, #31592, #5045, #18629, #36621, #50215, #33274, #29140, #38294, #41567, #42667, #50370, #23482, #55365, #41495, #37056, #55073, #50663, #10500, #24067, #37644, #28779, #19943, #37932, #2807, #42962, #2519, #11953, #34938, #47408, #4471, #52399, #29645, #34365, #16095, #40483, #26891, #43534, #3098, #38519, #56534, #47983, #20801, #43251, #12236, #29931, #34075, #38808, #21376, #44914, #22471, #12520, #6939, #56826, #52111, #15798, #47697, #7227, #51829, #48547, #52681, #52971, #33787, #25518, #11384, #7521, #29359, #21093, #25231, #39097, #57106, #43835, #16672, #34653, #8094, #30517, #30227, #48270, #7806, #3382, #25807, #57398, #16956, #36339, #41070, #657, #45512, #36921, #23055, #28055, #54365, #54071, #55224 ),
 .UNSPECIFIED., .F., .F.,
 ( 4, 2, 2, 2, 2, 2, 2, 1, 1, 1, 1, 1, 2, 2, 2, 2, 2, 1, 1, 1, 1, 1, 2, 2, 2, 2, 2, 1, 1, 1, 1, 2, 2, 2, 2, 2, 2, 2, 1, 1, 1, 1, 2, 2, 2, 2, 2, 2, 2, 1, 1, 1, 1, 1, 1, 2, 2, 2, 2, 2, 2, 1, 1, 1, 1, 2, 2, 2, 2, 2, 1, 1, 1, 2, 2, 2, 2, 1, 2, 2, 4 ),
 ( 0.000000000000000000, 0.06250000000016037172, 0.1250000000003207434, 0.1875000000004811151, 0.2187500000005612733, 0.2343750000006013245, 0.2421875000006213918, 0.2460937500006314671, 0.2480468750006364631, 0.2490234375006390166, 0.2495117187506402379, 0.2497558593756408762, 0.2498779296881412093, 0.2500000000006415424, 0.2812500000006000755, 0.2968750000005794809, 0.3046875000005691003, 0.3085937500005638823, 0.3105468750005613288, 0.3115234375005599965, 0.3120117187505592748, 0.3122558593755589418, 0.3123779296880587197, 0.3125000000005585532, 0.3437500000004944378, 0.3593750000004624079, 0.3671875000004463652, 0.3710937500004383716, 0.3730468750004343748, 0.3740234375004323764, 0.3745117187504313216, 0.3747558593754308220, 0.3750000000004302669, 0.4062500000003576028, 0.4218750000003212985, 0.4375000000002849387, 0.4687500000002122746, 0.4843750000001759703, 0.4921875000001578182, 0.4960937500001487144, 0.4980468750001442180, 0.4990234375001419420, 0.4995117187501407763, 0.5000000000001396661, 0.5624999999999947820, 0.6249999999998500089, 0.6874999999997051248, 0.7187499999996328492, 0.7343749999995966560, 0.7421874999995784483, 0.7460937499995694555, 0.7480468749995650146, 0.7490234374995626832, 0.7495117187495616839, 0.7497558593745610178, 0.7498779296870606847, 0.7499999999995603517, 0.7812499999996209699, 0.7968749999996512789, 0.8046874999996664890, 0.8085937499996740385, 0.8105468749996778133, 0.8115234374996798117, 0.8120117187496806999, 0.8122558593746812550, 0.8123779296871814770, 0.8124999999996815880, 0.8437499999997338795, 0.8593749999997600808, 0.8671874999997730704, 0.8710937499997796207, 0.8730468749997828404, 0.8740234374997843947, 0.8745117187497852829, 0.8749999999997860600, 0.9062499999998396838, 0.9218749999998664402, 0.9296874999998798739, 0.9335937499998865352, 0.9374999999998931965, 1.000000000000000000 ),
 .UNSPECIFIED. ) ;
#39212=CARTESIAN_POINT ( 'NONE',  ( 3.710074744828999904, -2.127759542060999820, -0.1726258946814999695 ) ) ;
#39217=CARTESIAN_POINT ( 'NONE',  ( -8.485281374238999419, -59.94999999967000548, -8.485281374238999419 ) ) ;
#39218=CARTESIAN_POINT ( 'NONE',  ( -8.130813118010999929, -17.31476110167000115, 9.546856411653001473 ) ) ;
#39221=ORIENTED_EDGE ( 'NONE', *, *, #24128, .F. ) ;
#39227=CARTESIAN_POINT ( 'NONE',  ( -7.765022563386000165, -60.89093562068000409, 9.830785949133000301 ) ) ;
#39228=CARTESIAN_POINT ( 'NONE',  ( -3.544559805645000061, -1.685986014850999970, 1.535826592584000005 ) ) ;
#39230=PLANE ( 'NONE',  #15440 ) ;
#39231=CARTESIAN_POINT ( 'NONE',  ( -12.70305331329071485, -53.76853698820474392, -0.8727610012296372899 ) ) ;
#39232=ORIENTED_EDGE ( 'NONE', *, *, #42360, .F. ) ;
#39233=CARTESIAN_POINT ( 'NONE',  ( -12.70610308055483628, -54.34479009111368697, 1.580620443374196382 ) ) ;
#39234=CARTESIAN_POINT ( 'NONE',  ( -3.431352783032999731, -1.204516015699999887, 2.086989923523999924 ) ) ;
#39240=CARTESIAN_POINT ( 'NONE',  ( -12.56594317982999875, -55.55000000504000468, 1.750000000000000000 ) ) ;
#39241=CARTESIAN_POINT ( 'NONE',  ( -12.00000000000000000, -60.04999999966999980, -1.250000000000000000 ) ) ;
#39244=CARTESIAN_POINT ( 'NONE',  ( 12.71536175399091739, -54.67444297152277954, -1.781227265980894758 ) ) ;
#39249=B_SPLINE_CURVE_WITH_KNOTS ( 'NONE', 3,
 ( #9376, #40959, #45401, #550, #18527, #36519 ),
 .UNSPECIFIED., .F., .F.,
 ( 4, 1, 1, 4 ),
 ( 0.000000000000000000, 0.3333333311575783497, 0.6666666623152567306, 0.9999999934728349693 ),
 .UNSPECIFIED. ) ;
#39251=ORIENTED_EDGE ( 'NONE', *, *, #18963, .F. ) ;
#39253=B_SPLINE_CURVE_WITH_KNOTS ( 'NONE', 3,
 ( #11532, #29510, #25090, #52827, #11243, #57253, #43114, #12382, #29222, #47271 ),
 .UNSPECIFIED., .F., .F.,
 ( 4, 2, 2, 2, 4 ),
 ( 0.000000000000000000, 0.2500000000000000000, 0.5000000000000000000, 0.7500000000000000000, 1.000000000000000000 ),
 .UNSPECIFIED. ) ;
#39256=CARTESIAN_POINT ( 'NONE',  ( -11.75000000000000355, -75.81041666666666856, -1.538071403320004249 ) ) ;
#39257=AXIS2_PLACEMENT_3D ( 'NONE', #1939, #42075, #28767 ) ;
#39258=CARTESIAN_POINT ( 'NONE',  ( -9.416026390438000604, -78.70544818976000556, 6.872484323511000248 ) ) ;
#39259=CONICAL_SURFACE ( 'NONE', #15674, 13.94999999937999924, 0.7853981633972997312 ) ;
#39261=FACE_OUTER_BOUND ( 'NONE', #14063, .T. ) ;
#39265=CIRCLE ( 'NONE', #4384, 13.89999999999999858 ) ;
#39266=ORIENTED_EDGE ( 'NONE', *, *, #4461, .T. ) ;
#39268=ORIENTED_EDGE ( 'NONE', *, *, #52545, .F. ) ;
#39272=DIRECTION ( 'NONE',  ( -0.7071067812863980340, -6.386265919119980056E-09, 0.7071067810866970005 ) ) ;
#39273=CARTESIAN_POINT ( 'NONE',  ( 12.05000000000000071, -75.80000000000001137, 0.000000000000000000 ) ) ;
#39275=LINE ( 'NONE', #25695, #27553 ) ;
#39278=CARTESIAN_POINT ( 'NONE',  ( -12.60413670420000010, -18.69283319134000010, -1.799502287691000069 ) ) ;
#39283=CARTESIAN_POINT ( 'NONE',  ( 8.838834764832000701, -60.04999999966999980, 8.838834764832000701 ) ) ;
#39286=EDGE_LOOP ( 'NONE', ( #55451, #27466, #35238, #36289 ) ) ;
#39289=CARTESIAN_POINT ( 'NONE',  ( 7.919595949288999570, -55.64999999964999233, -9.050966799188000067 ) ) ;
#39291=CARTESIAN_POINT ( 'NONE',  ( -12.74365836115054407, -18.47810168887382076, 1.980611005600014574 ) ) ;
#39292=DIRECTION ( 'NONE',  ( 0.000000000000000000, -1.000000000000000000, 0.000000000000000000 ) ) ;
#39293=CARTESIAN_POINT ( 'NONE',  ( -3.001381142052446549, -2.206320731719022543, 1.838231690380543348 ) ) ;
#39296=LINE ( 'NONE', #36025, #1878 ) ;
#39300=ORIENTED_EDGE ( 'NONE', *, *, #26943, .T. ) ;
#39301=CARTESIAN_POINT ( 'NONE',  ( 10.99999999999999822, -18.25000000000000000, -0.1600933372615688799 ) ) ;
#39302=DIRECTION ( 'NONE',  ( -1.000000000000000000, 0.000000000000000000, 0.000000000000000000 ) ) ;
#39304=EDGE_CURVE ( 'NONE', #45130, #2960, #34641, .T. ) ;
#39309=CARTESIAN_POINT ( 'NONE',  ( 1.247385801071000166, -17.52277743742000027, -12.50301438876999960 ) ) ;
#39311=CARTESIAN_POINT ( 'NONE',  ( 1.312204302215017826, -78.56237777671691447, 11.67681704195204517 ) ) ;
#39312=CARTESIAN_POINT ( 'NONE',  ( -10.42531125070999920, -60.06485145371000556, 7.624341767111000756 ) ) ;
#39313=ORIENTED_EDGE ( 'NONE', *, *, #19684, .F. ) ;
#39319=AXIS2_PLACEMENT_3D ( 'NONE', #3526, #22101, #13244 ) ;
#39321=CARTESIAN_POINT ( 'NONE',  ( 11.75000000000000000, -76.95000000000000284, 0.000000000000000000 ) ) ;
#39325=EDGE_CURVE ( 'NONE', #51850, #53713, #14997, .T. ) ;
#39327=LINE ( 'NONE', #48772, #6626 ) ;
#39328=CARTESIAN_POINT ( 'NONE',  ( 1.799490220168999954, -22.77129148951999937, 12.64502302235000109 ) ) ;
#39329=CARTESIAN_POINT ( 'NONE',  ( 11.75000000000000000, -76.05000000000001137, 0.000000000000000000 ) ) ;
#39331=ORIENTED_EDGE ( 'NONE', *, *, #55271, .T. ) ;
#39334=EDGE_LOOP ( 'NONE', ( #9037, #16828, #24079, #26522 ) ) ;
#39336=VERTEX_POINT ( 'NONE', #38817 ) ;
#39348=DIRECTION ( 'NONE',  ( 1.000000000000000000, 0.000000000000000000, 0.000000000000000000 ) ) ;
#39349=CARTESIAN_POINT ( 'NONE',  ( 7.648026766735999793, -23.25000000582000226, -10.12290050089000104 ) ) ;
#39351=CARTESIAN_POINT ( 'NONE',  ( -12.61117499584999813, -60.01550664522000034, -1.798980867982999943 ) ) ;
#39353=CARTESIAN_POINT ( 'NONE',  ( 7.691893942719999266, -21.75453807238000081, 10.42272502862000039 ) ) ;
#39355=CARTESIAN_POINT ( 'NONE',  ( 10.10712711931551944, -54.33345760842059491, -7.860996423901147168 ) ) ;
#39357=CARTESIAN_POINT ( 'NONE',  ( 12.55485633994999795, -17.84594908780999845, -1.580761757392000089 ) ) ;
#39358=EDGE_CURVE ( 'NONE', #44782, #49641, #17537, .T. ) ;
#39360=CIRCLE ( 'NONE', #21445, 4.999999999999996447 ) ;
#39364=CARTESIAN_POINT ( 'NONE',  ( -8.790679651930998872, -53.86186536156999694, 8.797972003268000663 ) ) ;
#39366=CARTESIAN_POINT ( 'NONE',  ( -10.15833271782000047, -17.78011549213000109, -7.756208840363000512 ) ) ;
#39368=CARTESIAN_POINT ( 'NONE',  ( -9.722718241315000398, -60.04999999966999980, -7.954951288349001004 ) ) ;
#39369=AXIS2_PLACEMENT_3D ( 'NONE', #18649, #13318, #41367 ) ;
#39372=DIRECTION ( 'NONE',  ( -0.9999548435846228323, 0.000000000000000000, -0.009503199022040118363 ) ) ;
#39376=ORIENTED_EDGE ( 'NONE', *, *, #57513, .T. ) ;
#39378=DIRECTION ( 'NONE',  ( 0.9999548435846228323, 0.000000000000000000, 0.009503199022040218977 ) ) ;
#39379=CARTESIAN_POINT ( 'NONE',  ( -12.60413652832999887, -18.69283065396999888, 1.799502287743000029 ) ) ;
#39380=EDGE_CURVE ( 'NONE', #56557, #378, #6508, .T. ) ;
#39381=CARTESIAN_POINT ( 'NONE',  ( -2.996400371072000191, -3.165668112399999679, 2.346782378936000057 ) ) ;
#39384=CARTESIAN_POINT ( 'NONE',  ( -12.68702648024000190, -55.04922088160000015, 1.889939500033999797 ) ) ;
#39386=FACE_OUTER_BOUND ( 'NONE', #50968, .T. ) ;
#39389=DIRECTION ( 'NONE',  ( 0.000000000000000000, 0.000000000000000000, 1.000000000000000000 ) ) ;
#39390=CARTESIAN_POINT ( 'NONE',  ( -8.485281374238999419, -60.04999999966999980, -8.485281374238999419 ) ) ;
#39394=CARTESIAN_POINT ( 'NONE',  ( 10.18496935386999880, -57.04935285362000030, 7.710095619715000126 ) ) ;
#39398=DIRECTION ( 'NONE',  ( 0.000000000000000000, 0.000000000000000000, -1.000000000000000000 ) ) ;
#39400=CIRCLE ( 'NONE', #29034, 5.000000000000000888 ) ;
#39403=DIRECTION ( 'NONE',  ( 0.000000000000000000, 1.000000000000000000, 0.000000000000000000 ) ) ;
#39407=CARTESIAN_POINT ( 'NONE',  ( 7.836764916109974166, -61.10511429613130474, 9.850487231183253201 ) ) ;
#39408=ORIENTED_EDGE ( 'NONE', *, *, #43404, .F. ) ;
#39412=CARTESIAN_POINT ( 'NONE',  ( -3.250000000000002665, -1.489583333333333703, 0.4254240051736044581 ) ) ;
#39417=VERTEX_POINT ( 'NONE', #25376 ) ;
#39418=CARTESIAN_POINT ( 'NONE',  ( 7.975755774848001245, -79.32330787033001229, 9.089596497509001338 ) ) ;
#39419=B_SPLINE_CURVE_WITH_KNOTS ( 'NONE', 3,
 ( #14915, #29079, #1658, #19072, #11099, #33791 ),
 .UNSPECIFIED., .F., .F.,
 ( 4, 2, 4 ),
 ( 0.000000000000000000, 0.5000000000000000000, 1.000000000000000000 ),
 .UNSPECIFIED. ) ;
#39421=DIRECTION ( 'NONE',  ( 0.7071067811865474617, 0.000000000000000000, 0.7071067811865474617 ) ) ;
#39428=CARTESIAN_POINT ( 'NONE',  ( 9.505949683906999681, -79.00000000000000000, 6.906476714433999575 ) ) ;
#39435=CARTESIAN_POINT ( 'NONE',  ( -1.258617623430583476, -3.007881555714398303, 2.995588677545779621 ) ) ;
#39437=AXIS2_PLACEMENT_3D ( 'NONE', #8663, #3655, #17822 ) ;
#39438=LINE ( 'NONE', #34413, #6372 ) ;
#39440=CARTESIAN_POINT ( 'NONE',  ( 3.521688171515000132, -3.583255539711999837, 0.7298424208991000084 ) ) ;
#39446=CARTESIAN_POINT ( 'NONE',  ( -12.43646312222999839, -17.07951485557000026, -0.1257251053153000120 ) ) ;
#39447=EDGE_CURVE ( 'NONE', #47646, #11409, #16980, .T. ) ;
#39448=CARTESIAN_POINT ( 'NONE',  ( 12.61277705613999878, -23.19666672528000007, 1.798399175679999740 ) ) ;
#39449=DIRECTION ( 'NONE',  ( -1.000000000000000000, 0.000000000000000000, 0.000000000000000000 ) ) ;
#39451=CARTESIAN_POINT ( 'NONE',  ( 1.980610890452888295, -23.52073889484903546, -12.74374574606960486 ) ) ;
#39452=CARTESIAN_POINT ( 'NONE',  ( -12.17235636505000151, -76.59542353800999592, -2.158157603104000177 ) ) ;
#39453=EDGE_LOOP ( 'NONE', ( #35840, #4930, #18514, #46837 ) ) ;
#39454=DIRECTION ( 'NONE',  ( -1.000000000000000000, 0.000000000000000000, 0.000000000000000000 ) ) ;
#39456=CARTESIAN_POINT ( 'NONE',  ( 12.66008999775999833, -61.42705329315000284, 1.387101471715999956 ) ) ;
#39457=CARTESIAN_POINT ( 'NONE',  ( -1.931043742978000077, -22.77795407709999864, -12.75763395695999947 ) ) ;
#39469=CARTESIAN_POINT ( 'NONE',  ( 12.60413670417000098, -55.49283319101999723, 1.799502287691000069 ) ) ;
#39470=CARTESIAN_POINT ( 'NONE',  ( -1.750000000001000089, -55.54999998977000075, 12.56594317853999954 ) ) ;
#39472=ORIENTED_EDGE ( 'NONE', *, *, #45514, .F. ) ;
#39473=ORIENTED_EDGE ( 'NONE', *, *, #4869, .F. ) ;
#39474=EDGE_CURVE ( 'NONE', #43629, #22264, #48981, .T. ) ;
#39476=ADVANCED_FACE ( 'NONE', ( #3524 ), #35675, .F. ) ;
#39477=DIRECTION ( 'NONE',  ( 0.7071067811865474617, 0.000000000000000000, -0.7071067811865474617 ) ) ;
#39478=CARTESIAN_POINT ( 'NONE',  ( 8.414570695956999913, -60.64999999943950826, -8.414570695956999913 ) ) ;
#39479=ORIENTED_EDGE ( 'NONE', *, *, #12618, .F. ) ;
#39485=CARTESIAN_POINT ( 'NONE',  ( 7.633502222218000455, -55.59895684611999656, 10.36289759015999934 ) ) ;
#39487=FACE_OUTER_BOUND ( 'NONE', #21327, .T. ) ;
#39489=CARTESIAN_POINT ( 'NONE',  ( 12.70228545259539032, -61.62820680322044353, -1.205254117609577236 ) ) ;
#39492=CARTESIAN_POINT ( 'NONE',  ( -10.01676948373000009, -23.20938276584000093, 7.658894993369000481 ) ) ;
#39495=CARTESIAN_POINT ( 'NONE',  ( -12.66008925484999992, -17.37289997915000228, 1.387046028394999908 ) ) ;
#39496=DIRECTION ( 'NONE',  ( 0.7071067811865475727, 0.000000000000000000, 0.7071067811865475727 ) ) ;
#39499=CARTESIAN_POINT ( 'NONE',  ( -1.214170062781000148, -1.395588905189000029, -3.939698975434999362 ) ) ;
#39503=CARTESIAN_POINT ( 'NONE',  ( 1.980464439859999981, -57.04527982639000072, -12.85144117157999943 ) ) ;
#39505=CARTESIAN_POINT ( 'NONE',  ( -3.515269593969000184, -2.480847686686999953, -0.5480397081700000284 ) ) ;
#39509=DIRECTION ( 'NONE',  ( 0.000000000000000000, 0.000000000000000000, 1.000000000000000000 ) ) ;
#39513=VERTEX_POINT ( 'NONE', #26240 ) ;
#39519=CARTESIAN_POINT ( 'NONE',  ( 0.008649596124003998757, -1.093362276482000128, 3.863893329571999935 ) ) ;
#39521=CARTESIAN_POINT ( 'NONE',  ( 12.66736977981000045, -24.23307288772000234, -1.690635117038000068 ) ) ;
#39522=CARTESIAN_POINT ( 'NONE',  ( -12.00000000000000000, -55.54999999966999980, 0.000000000000000000 ) ) ;
#39524=CARTESIAN_POINT ( 'NONE',  ( -12.71162569430491551, -54.56025712730872357, 1.720540999418351369 ) ) ;
#39525=AXIS2_PLACEMENT_3D ( 'NONE', #56844, #26113, #34673 ) ;
#39527=EDGE_CURVE ( 'NONE', #6877, #14569, #2143, .T. ) ;
#39528=FACE_OUTER_BOUND ( 'NONE', #47278, .T. ) ;
#39529=CARTESIAN_POINT ( 'NONE',  ( -10.18589226629999978, -55.51082276539999327, -7.641012305206999145 ) ) ;
#39530=ADVANCED_FACE ( 'NONE', ( #39814 ), #43596, .F. ) ;
#39533=CARTESIAN_POINT ( 'NONE',  ( -12.52785477533552516, -55.00586572896404647, 1.668513102962560835 ) ) ;
#39534=CARTESIAN_POINT ( 'NONE',  ( 9.431008682120035402, -61.60059307736660372, -8.251849285864723882 ) ) ;
#39536=CARTESIAN_POINT ( 'NONE',  ( -7.986982684638000762, -54.07364722701999682, -10.07612755991999975 ) ) ;
#39539=ORIENTED_EDGE ( 'NONE', *, *, #48016, .T. ) ;
#39540=VERTEX_POINT ( 'NONE', #17386 ) ;
#39548=CARTESIAN_POINT ( 'NONE',  ( -1.538071403319991814, -75.91458333333332575, -11.75000000000000355 ) ) ;
#39549=CARTESIAN_POINT ( 'NONE',  ( -7.818192365797999699, -78.68694664278000062, 9.061685001942999307 ) ) ;
#39551=CARTESIAN_POINT ( 'NONE',  ( -12.76303204525000012, -60.06485147653999945, -1.980584515753000208 ) ) ;
#39556=CARTESIAN_POINT ( 'NONE',  ( 8.274781782206300562, -17.02110650128472358, 9.689260013783508541 ) ) ;
#39557=EDGE_LOOP ( 'NONE', ( #31585, #23577, #49049 ) ) ;
#39561=CARTESIAN_POINT ( 'NONE',  ( 7.601397897754999633, -23.24999999688999708, 10.07627163191000008 ) ) ;
#39563=CARTESIAN_POINT ( 'NONE',  ( 11.74981453461694869, -76.45368481813011385, 0.5897208236573105999 ) ) ;
#39564=CARTESIAN_POINT ( 'NONE',  ( 1.618935784732136174, -60.72751168617237028, -12.52134385804463967 ) ) ;
#39565=CARTESIAN_POINT ( 'NONE',  ( 3.520524516624752298, -3.098549438791605048, -0.03236223760434995406 ) ) ;
#39566=AXIS2_PLACEMENT_3D ( 'NONE', #41881, #50463, #18867 ) ;
#39568=CARTESIAN_POINT ( 'NONE',  ( 4.823394776896443581, -78.11073669759603888, -11.06826222629441148 ) ) ;
#39569=CARTESIAN_POINT ( 'NONE',  ( -7.601397897754999633, -60.04999999725999515, 10.07627163191000008 ) ) ;
#39571=CARTESIAN_POINT ( 'NONE',  ( 10.35747158362999976, -18.68415522710999710, -7.626500902215000544 ) ) ;
#39574=FACE_OUTER_BOUND ( 'NONE', #15277, .T. ) ;
#39575=VERTEX_POINT ( 'NONE', #53117 ) ;
#39585=CARTESIAN_POINT ( 'NONE',  ( 1.460729357743000056, -54.70908756765000192, -12.44211643236999976 ) ) ;
#39588=ORIENTED_EDGE ( 'NONE', *, *, #20521, .F. ) ;
#39589=CARTESIAN_POINT ( 'NONE',  ( 0.5999999998848000171, -18.85000000520999919, -11.79999999988000070 ) ) ;
#39590=CARTESIAN_POINT ( 'NONE',  ( -0.8522511841608177985, -2.205572306515419800, -3.165809400549076891 ) ) ;
#39591=LINE ( 'NONE', #21011, #40014 ) ;
#39592=CARTESIAN_POINT ( 'NONE',  ( 12.50000000000000000, -26.93717104351999936, 0.000000000000000000 ) ) ;
#39596=CARTESIAN_POINT ( 'NONE',  ( 0.6484536763431314466, -16.87597017290114820, 12.70397497891879190 ) ) ;
#39600=ORIENTED_EDGE ( 'NONE', *, *, #27194, .F. ) ;
#39607=LINE ( 'NONE', #31608, #23312 ) ;
#39608=CARTESIAN_POINT ( 'NONE',  ( 10.66387363228065155, -76.91183802276627546, -5.042381349153009396 ) ) ;
#39609=AXIS2_PLACEMENT_3D ( 'NONE', #17253, #35242, #8994 ) ;
#39610=AXIS2_PLACEMENT_3D ( 'NONE', #49446, #40580, #52768 ) ;
#39612=CARTESIAN_POINT ( 'NONE',  ( -12.71162862753614675, -61.03964265594247962, -1.720599174840216516 ) ) ;
#39613=ADVANCED_FACE ( 'NONE', ( #57829 ), #26818, .F. ) ;
#39614=DIRECTION ( 'NONE',  ( 0.000000000000000000, 1.000000000000000000, 0.000000000000000000 ) ) ;
#39618=ORIENTED_EDGE ( 'NONE', *, *, #7759, .F. ) ;
#39620=ORIENTED_EDGE ( 'NONE', *, *, #2276, .F. ) ;
#39621=CARTESIAN_POINT ( 'NONE',  ( -9.369164850722000892, -18.75000000000000000, 7.601397897754999633 ) ) ;
#39627=ORIENTED_EDGE ( 'NONE', *, *, #44691, .T. ) ;
#39634=CARTESIAN_POINT ( 'NONE',  ( 7.612971414713999962, -23.32452529362999982, 10.53003223722999948 ) ) ;
#39636=CARTESIAN_POINT ( 'NONE',  ( 8.266608573639034674, -53.82766203646255576, -9.697383820226121998 ) ) ;
#39638=CARTESIAN_POINT ( 'NONE',  ( 12.82229880959000035, -18.57735182838000298, -2.065917129154000165 ) ) ;
#39639=DIRECTION ( 'NONE',  ( 1.000000000000000000, 0.000000000000000000, 0.000000000000000000 ) ) ;
#39641=ORIENTED_EDGE ( 'NONE', *, *, #40364, .T. ) ;
#39644=CARTESIAN_POINT ( 'NONE',  ( -7.646091287746999754, -55.09149945095000334, 10.13691902390999999 ) ) ;
#39647=CARTESIAN_POINT ( 'NONE',  ( -10.35410226330999883, -18.59601732823000120, -7.619716344073999892 ) ) ;
#39649=CARTESIAN_POINT ( 'NONE',  ( 7.682331425190000118, -59.56486430393999854, 10.04115011120000034 ) ) ;
#39650=CARTESIAN_POINT ( 'NONE',  ( -10.98362417419999915, -18.84999999999999787, 0.5999999999999999778 ) ) ;
#39652=CARTESIAN_POINT ( 'NONE',  ( 10.07719973192999952, -58.54888345776999614, -7.718346056099999686 ) ) ;
#39653=DIRECTION ( 'NONE',  ( -1.000000000000000000, 0.000000000000000000, 0.000000000000000000 ) ) ;
#39658=CARTESIAN_POINT ( 'NONE',  ( 11.75000000000000000, -78.45000000000000284, 0.000000000000000000 ) ) ;
#39659=FACE_OUTER_BOUND ( 'NONE', #49211, .T. ) ;
#39661=CARTESIAN_POINT ( 'NONE',  ( 1.801839102376999957, -2.465322672876999910, 3.169418229746999938 ) ) ;
#39665=CARTESIAN_POINT ( 'NONE',  ( -1.582498447116000184, -60.95086122444999432, 12.55493832976000057 ) ) ;
#39666=CARTESIAN_POINT ( 'NONE',  ( 3.165411199172027512, -3.229166666666666519, -0.8506806241676553304 ) ) ;
#39669=CARTESIAN_POINT ( 'NONE',  ( 4.106769510331843342, -77.10559041576395600, -11.35196456917261543 ) ) ;
#39670=AXIS2_PLACEMENT_3D ( 'NONE', #11108, #37659, #6660 ) ;
#39674=CARTESIAN_POINT ( 'NONE',  ( 10.14948852603999896, -56.04899164556000102, 7.674614791885000287 ) ) ;
#39676=CARTESIAN_POINT ( 'NONE',  ( -12.55458806508999992, -60.96283916815999504, 1.575041344316999936 ) ) ;
#39681=EDGE_CURVE ( 'NONE', #19958, #46028, #50941, .T. ) ;
#39682=DIRECTION ( 'NONE',  ( 0.7071067811865475727, 0.000000000000000000, -0.7071067811865475727 ) ) ;
#39684=CARTESIAN_POINT ( 'NONE',  ( -10.98464796637059671, -23.30469563149750556, -0.5810037832618578646 ) ) ;
#39686=EDGE_CURVE ( 'NONE', #35836, #9708, #42404, .T. ) ;
#39687=CARTESIAN_POINT ( 'NONE',  ( -1.583004792618638135, -24.45209241160721803, 12.70616254410927937 ) ) ;
#39688=VECTOR ( 'NONE', #38839, 1000.000000000000000 ) ;
#39692=CIRCLE ( 'NONE', #126, 12.50000000000000000 ) ;
#39694=LINE ( 'NONE', #31699, #44729 ) ;
#39700=CARTESIAN_POINT ( 'NONE',  ( 10.99067476705999979, -78.63267194099999813, -5.319090318451999977 ) ) ;
#39703=CYLINDRICAL_SURFACE ( 'NONE', #29150, 11.00000000000000000 ) ;
#39704=CARTESIAN_POINT ( 'NONE',  ( -9.723199429427999974, -17.52306056076000118, 7.958735708429999889 ) ) ;
#39709=CARTESIAN_POINT ( 'NONE',  ( -10.68064082909000057, -77.45636465244999158, 7.608522161463999289 ) ) ;
#39710=CARTESIAN_POINT ( 'NONE',  ( 7.139902610388999982, -77.41714066711000442, -10.43201753306000157 ) ) ;
#39712=DIRECTION ( 'NONE',  ( 0.9999463328794432337, 0.000000000000000000, -0.01036008498777044214 ) ) ;
#39716=CARTESIAN_POINT ( 'NONE',  ( -10.01235002620999914, -55.50151115525000023, 7.653559626076999578 ) ) ;
#39717=CARTESIAN_POINT ( 'NONE',  ( -1.332907328585176687, -3.009958170327963867, 2.963254743748688025 ) ) ;
#39719=CARTESIAN_POINT ( 'NONE',  ( -12.00000000000000000, -18.75000000000000000, -1.250000000000000000 ) ) ;
#39721=CARTESIAN_POINT ( 'NONE',  ( -3.054513261463999818, -2.798870392637999860, -2.270689576097000284 ) ) ;
#39724=CARTESIAN_POINT ( 'NONE',  ( -7.620012114232000755, -60.00560398617000146, -10.53562503196000044 ) ) ;
#39728=CARTESIAN_POINT ( 'NONE',  ( -12.43641395964999852, -17.08198970748000178, 0.03481089025432999862 ) ) ;
#39729=CARTESIAN_POINT ( 'NONE',  ( -12.97295173694999981, -77.55824801881999520, -1.020668466325000079 ) ) ;
#39730=EDGE_CURVE ( 'NONE', #15955, #52954, #56835, .T. ) ;
#39731=AXIS2_PLACEMENT_3D ( 'NONE', #47924, #48483, #30159 ) ;
#39732=DIRECTION ( 'NONE',  ( 0.000000000000000000, 1.000000000000000000, 0.000000000000000000 ) ) ;
#39733=FACE_OUTER_BOUND ( 'NONE', #27037, .T. ) ;
#39736=CARTESIAN_POINT ( 'NONE',  ( -1.250000000000000000, -23.25000000000000000, 12.50000000000000000 ) ) ;
#39737=CARTESIAN_POINT ( 'NONE',  ( 12.77302471396000172, -61.52230123271999673, 1.481949986260999941 ) ) ;
#39743=ORIENTED_EDGE ( 'NONE', *, *, #36905, .F. ) ;
#39744=DIRECTION ( 'NONE',  ( 0.000000000000000000, -1.000000000000000000, 0.000000000000000000 ) ) ;
#39747=ORIENTED_EDGE ( 'NONE', *, *, #38950, .T. ) ;
#39748=ORIENTED_EDGE ( 'NONE', *, *, #4478, .T. ) ;
#39752=ORIENTED_EDGE ( 'NONE', *, *, #32194, .T. ) ;
#39753=EDGE_CURVE ( 'NONE', #48636, #1742, #13446, .T. ) ;
#39754=ORIENTED_EDGE ( 'NONE', *, *, #44361, .F. ) ;
#39755=ORIENTED_EDGE ( 'NONE', *, *, #41580, .T. ) ;
#39758=ORIENTED_EDGE ( 'NONE', *, *, #16251, .T. ) ;
#39759=EDGE_CURVE ( 'NONE', #25961, #56481, #14144, .T. ) ;
#39762=AXIS2_PLACEMENT_3D ( 'NONE', #55041, #18742, #36735 ) ;
#39765=CARTESIAN_POINT ( 'NONE',  ( 7.646788101807000082, -55.42771363232999704, 10.00831428589000005 ) ) ;
#39766=PLANE ( 'NONE',  #45910 ) ;
#39767=DIRECTION ( 'NONE',  ( 0.9903465037221068634, -0.1386138613754009652, 0.000000000000000000 ) ) ;
#39769=CARTESIAN_POINT ( 'NONE',  ( 7.655542440077000244, -56.02180874340999850, -10.38645071868999992 ) ) ;
#39770=CARTESIAN_POINT ( 'NONE',  ( 1.750000000000000000, -60.04999999657000131, -12.50000000000000000 ) ) ;
#39771=CARTESIAN_POINT ( 'NONE',  ( -10.53495260691999924, -23.22711197486000145, 7.618387230241999930 ) ) ;
#39779=CARTESIAN_POINT ( 'NONE',  ( -8.150146600852348655, -60.21532333328943309, -7.387512494710285260 ) ) ;
#39790=LINE ( 'NONE', #52517, #33579 ) ;
#39794=VERTEX_POINT ( 'NONE', #38214 ) ;
#39795=EDGE_CURVE ( 'NONE', #2615, #31027, #56237, .T. ) ;
#39801=CIRCLE ( 'NONE', #21893, 9.000000000000000000 ) ;
#39802=CARTESIAN_POINT ( 'NONE',  ( -2.719292624632000166, -1.072128508794999879, 2.510906049621999703 ) ) ;
#39804=CARTESIAN_POINT ( 'NONE',  ( 12.66313299633999812, -25.17803434852999800, 0.06050769725596999438 ) ) ;
#39805=CARTESIAN_POINT ( 'NONE',  ( -1.667961430005999945, -58.54888345776999614, 12.58335110162999904 ) ) ;
#39806=VERTEX_POINT ( 'NONE', #15786 ) ;
#39807=CARTESIAN_POINT ( 'NONE',  ( 8.485281374238999419, -23.25000000000000000, 8.485281374238999419 ) ) ;
#39808=CARTESIAN_POINT ( 'NONE',  ( 8.583677312638442913, -24.97185920791718061, -9.102132574100766149 ) ) ;
#39809=DIRECTION ( 'NONE',  ( -1.000000000000000000, 0.000000000000000000, 0.000000000000000000 ) ) ;
#39810=CARTESIAN_POINT ( 'NONE',  ( -10.01234990226999955, -55.50150862742999891, -7.653559502261000347 ) ) ;
#39814=FACE_OUTER_BOUND ( 'NONE', #35165, .T. ) ;
#39816=CARTESIAN_POINT ( 'NONE',  ( 0.8506806241676642122, -1.145833333333333481, -3.165411199172024848 ) ) ;
#39818=AXIS2_PLACEMENT_3D ( 'NONE', #47489, #55448, #15877 ) ;
#39819=CARTESIAN_POINT ( 'NONE',  ( -10.47840693000000023, -55.01310507149000273, -7.622759963108999948 ) ) ;
#39826=EDGE_CURVE ( 'NONE', #1567, #48012, #47460, .T. ) ;
#39828=EDGE_CURVE ( 'NONE', #44485, #18159, #30424, .T. ) ;
#39829=ORIENTED_EDGE ( 'NONE', *, *, #8641, .F. ) ;
#39833=CARTESIAN_POINT ( 'NONE',  ( 5.691226796558999546, -77.83365458999999476, 11.81421328157999895 ) ) ;
#39835=CARTESIAN_POINT ( 'NONE',  ( 7.714303428875997959, -15.69705297113999443, 12.53545825868000385 ) ) ;
#39840=ORIENTED_EDGE ( 'NONE', *, *, #6908, .F. ) ;
#39842=CARTESIAN_POINT ( 'NONE',  ( -12.19234209666000091, -76.06301006652999774, -1.697737568323999913 ) ) ;
#39844=AXIS2_PLACEMENT_3D ( 'NONE', #51948, #24488, #38062 ) ;
#39846=CARTESIAN_POINT ( 'NONE',  ( 1.020992902784864986, -3.200861152918981656, 3.368731490719146127 ) ) ;
#39847=EDGE_CURVE ( 'NONE', #25463, #28651, #31340, .T. ) ;
#39849=FACE_OUTER_BOUND ( 'NONE', #33232, .T. ) ;
#39850=LINE ( 'NONE', #35406, #57185 ) ;
#39853=CARTESIAN_POINT ( 'NONE',  ( 10.42272502862000039, -21.75453807238000081, -7.691893942719999266 ) ) ;
#39855=CARTESIAN_POINT ( 'NONE',  ( 6.322255100220510293, -76.28719745902344584, 11.39032443625401214 ) ) ;
#39857=B_SPLINE_SURFACE_WITH_KNOTS ( 'NONE', 3, 3, ( 
 ( #29336, #11647, #20780, #6915 ),
 ( #20499, #24348, #20215, #7203 ),
 ( #29624, #47383, #51514, #19622 ),
 ( #46805, #38495, #42359, #37912 ),
 ( #10778, #1633, #56512, #15487 ),
 ( #43225, #24922, #47678, #33477 ),
 ( #2493, #16068, #1929, #15189 ),
 ( #11074, #34050, #6624, #52088 ) ),
 .UNSPECIFIED., .F., .F., .F.,
 ( 4, 1, 1, 1, 1, 4 ),
 ( 4, 4 ),
 ( -0.01200407347464999865, 0.000000000000000000, 0.3333333333333000081, 0.6666666666667000474, 1.000000000000000000, 1.011997855551999947 ),
 ( -0.3559705542741999906, 1.355970554273999928 ),
 .UNSPECIFIED. ) ;
#39858=EDGE_LOOP ( 'NONE', ( #27996, #40404, #71, #43265, #2685 ) ) ;
#39869=CARTESIAN_POINT ( 'NONE',  ( -1.814305421036000121, -54.51058030636000495, -12.78003582248999948 ) ) ;
#39870=CARTESIAN_POINT ( 'NONE',  ( 10.85629140140682125, -75.98074698996606458, 4.494010003869360226 ) ) ;
#39872=ORIENTED_EDGE ( 'NONE', *, *, #34935, .F. ) ;
#39876=CARTESIAN_POINT ( 'NONE',  ( -9.534922033296867383, -78.74983463097288450, -6.929927095622216981 ) ) ;
#39880=CARTESIAN_POINT ( 'NONE',  ( 1.689459950990167547, -17.70811746100764950, 12.71013585610350383 ) ) ;
#39882=DIRECTION ( 'NONE',  ( 0.6489586447330936148, -0.04890182338522946343, 0.7592504784955924624 ) ) ;
#39891=DIRECTION ( 'NONE',  ( 0.7071067811704841999, -1.939413340559955448E-07, -0.7071067812025843002 ) ) ;
#39894=CARTESIAN_POINT ( 'NONE',  ( 9.243145382185367964, -17.08347263196495192, -8.441178780123935965 ) ) ;
#39896=TOROIDAL_SURFACE ( 'NONE', #49359, 26.50000000000000000, 14.00000000000000000 ) ;
#39897=DIRECTION ( 'NONE',  ( 0.000000000000000000, -1.000000000000000000, 0.000000000000000000 ) ) ;
#39898=EDGE_LOOP ( 'NONE', ( #9296, #20033, #35287, #35502 ) ) ;
#39899=ORIENTED_EDGE ( 'NONE', *, *, #52763, .F. ) ;
#39900=CARTESIAN_POINT ( 'NONE',  ( -8.414570695956999913, -59.94999999967000548, 8.414570695956999913 ) ) ;
#39904=ORIENTED_EDGE ( 'NONE', *, *, #43046, .T. ) ;
#39905=CARTESIAN_POINT ( 'NONE',  ( 7.646944885436999684, -23.19635956544000166, 10.19022188674999896 ) ) ;
#39906=CIRCLE ( 'NONE', #21998, 13.86363636363999952 ) ;
#39913=ORIENTED_EDGE ( 'NONE', *, *, #2918, .T. ) ;
#39919=CARTESIAN_POINT ( 'NONE',  ( -1.894422427200999959, -76.61909451939000348, -12.98637956171999974 ) ) ;
#39920=ADVANCED_FACE ( 'NONE', ( #16081 ), #46487, .T. ) ;
#39921=CARTESIAN_POINT ( 'NONE',  ( 2.117002802198683753, -2.180884342491374639, -2.498681180296688176 ) ) ;
#39924=CARTESIAN_POINT ( 'NONE',  ( 12.72397198033999999, -18.77854962937000138, -1.930909771329999858 ) ) ;
#39925=CARTESIAN_POINT ( 'NONE',  ( -9.389195554418000356, -24.71043214204999927, -8.194863653270999748 ) ) ;
#39927=ORIENTED_EDGE ( 'NONE', *, *, #33943, .F. ) ;
#39929=CARTESIAN_POINT ( 'NONE',  ( -7.634437838894000627, -55.05219468418000162, 10.30764259108000225 ) ) ;
#39932=CARTESIAN_POINT ( 'NONE',  ( -7.961057357828999592, -17.46431744651999907, -9.783210913639999617 ) ) ;
#39933=CARTESIAN_POINT ( 'NONE',  ( 7.691916945423999508, -57.04634220890999785, 10.42274798266000069 ) ) ;
#39934=CARTESIAN_POINT ( 'NONE',  ( -0.5668640707507043297, -53.88340304925345947, 12.50470739224864936 ) ) ;
#39937=DIRECTION ( 'NONE',  ( 1.000000000000000000, 0.000000000000000000, 0.000000000000000000 ) ) ;
#39939=CARTESIAN_POINT ( 'NONE',  ( 0.8506806241676508895, -1.854166666666666741, 3.165411199172028400 ) ) ;
#39942=CARTESIAN_POINT ( 'NONE',  ( -11.75000000000000000, -77.20000000000000284, -1.435311119447000145E-14 ) ) ;
#39943=ADVANCED_FACE ( 'NONE', ( #11084 ), #29919, .F. ) ;
#39947=CARTESIAN_POINT ( 'NONE',  ( -3.434418375904999987, -2.158690377978999653, -1.223358650580000040 ) ) ;
#39949=CARTESIAN_POINT ( 'NONE',  ( 5.694538069269999623E-14, -72.84999999994899156, -13.94999999994999840 ) ) ;
#39951=CIRCLE ( 'NONE', #55051, 12.05000000000000071 ) ;
#39952=CARTESIAN_POINT ( 'NONE',  ( -0.4260390295771080971, -1.986914419589991487, 3.249230163478797451 ) ) ;
#39958=CARTESIAN_POINT ( 'NONE',  ( -10.79518247106041251, -76.98995411785524823, -5.399136025279304363 ) ) ;
#39959=EDGE_CURVE ( 'NONE', #17731, #23873, #57777, .T. ) ;
#39964=CARTESIAN_POINT ( 'NONE',  ( -1.001315002179000047, -17.31477588286000113, -12.50000000000000000 ) ) ;
#39967=CARTESIAN_POINT ( 'NONE',  ( -12.56594317989000054, -23.24999999414999863, -1.750000000001000089 ) ) ;
#39969=ORIENTED_EDGE ( 'NONE', *, *, #21768, .T. ) ;
#39973=CARTESIAN_POINT ( 'NONE',  ( 7.353725627631192197, -55.49344856148322691, 8.180687091746198902 ) ) ;
#39974=EDGE_LOOP ( 'NONE', ( #45933, #28579, #55311, #47774 ) ) ;
#39976=CARTESIAN_POINT ( 'NONE',  ( -3.215437157339553487, -0.7500000000000000000, 1.430139912060602425 ) ) ;
#39977=EDGE_CURVE ( 'NONE', #3036, #11190, #35994, .T. ) ;
#39979=CARTESIAN_POINT ( 'NONE',  ( 10.10912542004786907, -55.32413588747969868, -7.634643956464879366 ) ) ;
#39980=ORIENTED_EDGE ( 'NONE', *, *, #3473, .T. ) ;
#39981=DIRECTION ( 'NONE',  ( 0.000000000000000000, 0.000000000000000000, 1.000000000000000000 ) ) ;
#39989=CARTESIAN_POINT ( 'NONE',  ( -10.57271965826999960, -78.46022763255000143, -6.107801963966000613 ) ) ;
#39991=EDGE_LOOP ( 'NONE', ( #10728, #38825, #52359, #38944 ) ) ;
#39993=FACE_BOUND ( 'NONE', #915, .T. ) ;
#39998=CARTESIAN_POINT ( 'NONE',  ( -3.153993092687999766, -78.39994354880001026, 12.72742730875000028 ) ) ;
#39999=CARTESIAN_POINT ( 'NONE',  ( -1.228039281160999918, -77.36163602614999490, -12.58161828305999919 ) ) ;
#40003=CARTESIAN_POINT ( 'NONE',  ( -10.38645071868999992, -59.57819125629999490, 7.655542440085000067 ) ) ;
#40004=CARTESIAN_POINT ( 'NONE',  ( -2.301383562795737969, -3.038008897241404327, 2.294446131325794891 ) ) ;
#40008=CARTESIAN_POINT ( 'NONE',  ( 3.383845406481000406, -2.494828305427999826, -1.742318191517000070 ) ) ;
#40010=VERTEX_POINT ( 'NONE', #31291 ) ;
#40011=DIRECTION ( 'NONE',  ( -1.000000000000000000, 0.000000000000000000, 0.000000000000000000 ) ) ;
#40014=VECTOR ( 'NONE', #7723, 1000.000000000000000 ) ;
#40016=ADVANCED_FACE ( 'NONE', ( #7722 ), #21296, .F. ) ;
#40017=CARTESIAN_POINT ( 'NONE',  ( 1.750000000000000000, -18.75000000000000000, -12.00000000000000000 ) ) ;
#40018=CARTESIAN_POINT ( 'NONE',  ( -10.55511172854000002, -77.93295181317999720, 7.611100925114999249 ) ) ;
#40020=CARTESIAN_POINT ( 'NONE',  ( 9.713030931998421380, -17.47705886690323140, 7.970419576809637974 ) ) ;
#40022=VECTOR ( 'NONE', #4552, 1000.000000000000000 ) ;
#40023=CARTESIAN_POINT ( 'NONE',  ( -9.931063218460421282, -54.67724209132310875, 7.763994034062362992 ) ) ;
#40024=CARTESIAN_POINT ( 'NONE',  ( 8.130813118348999780, -54.11476110100999648, -9.546856411313999757 ) ) ;
#40037=ORIENTED_EDGE ( 'NONE', *, *, #52776, .F. ) ;
#40041=VERTEX_POINT ( 'NONE', #57887 ) ;
#40043=EDGE_CURVE ( 'NONE', #8704, #22042, #43633, .T. ) ;
#40044=VERTEX_POINT ( 'NONE', #17443 ) ;
#40046=DIRECTION ( 'NONE',  ( 0.000000000000000000, 1.000000000000000000, 0.000000000000000000 ) ) ;
#40047=DIRECTION ( 'NONE',  ( -0.7071067811865954233, 0.7071067811864955033, 7.552239815522943575E-08 ) ) ;
#40049=VERTEX_POINT ( 'NONE', #35429 ) ;
#40054=EDGE_CURVE ( 'NONE', #15436, #26860, #57127, .T. ) ;
#40056=CARTESIAN_POINT ( 'NONE',  ( -0.1577469407266123835, -18.24957415542316141, 11.00002392222777381 ) ) ;
#40057=CARTESIAN_POINT ( 'NONE',  ( 11.75000000000000000, -77.45000000000000284, 1.043320980279999928E-14 ) ) ;
#40058=CIRCLE ( 'NONE', #55167, 14.00000000000000000 ) ;
#40059=CARTESIAN_POINT ( 'NONE',  ( -10.42531124908000173, -60.06485148440999922, -7.624341765471999821 ) ) ;
#40062=CARTESIAN_POINT ( 'NONE',  ( -10.00844230537000001, -23.36891112553000127, 7.647097279392999880 ) ) ;
#40068=CARTESIAN_POINT ( 'NONE',  ( -1.666727925315000025, -23.19174481776000007, 12.50018462903999961 ) ) ;
#40069=CARTESIAN_POINT ( 'NONE',  ( -12.50000000000000000, -55.54999999966999980, 0.000000000000000000 ) ) ;
#40071=CARTESIAN_POINT ( 'NONE',  ( -3.387230649729000120, -1.584484372332999769, -1.285432911469999828 ) ) ;
#40075=EDGE_CURVE ( 'NONE', #29038, #36778, #14469, .T. ) ;
#40077=CARTESIAN_POINT ( 'NONE',  ( 1.980584515756000030, -55.53514849873000259, -12.76303204337999908 ) ) ;
#40078=CARTESIAN_POINT ( 'NONE',  ( -7.601397897754999633, -55.55000000209000177, -10.07627163191000008 ) ) ;
#40085=ORIENTED_EDGE ( 'NONE', *, *, #35001, .F. ) ;
#40091=B_SPLINE_CURVE_WITH_KNOTS ( 'NONE', 3,
 ( #42981, #39412, #2538, #25251, #7826, #43270, #16113, #16401, #34385, #52417, #25826, #43855, #57418, #16977, #23151, #21970, #57994, #177 ),
 .UNSPECIFIED., .F., .F.,
 ( 4, 2, 2, 2, 2, 2, 2, 2, 4 ),
 ( 0.000000000000000000, 0.1250000000000001110, 0.2500000000000001665, 0.3750000000000001665, 0.5000000000000001110, 0.6250000000000001110, 0.7500000000000001110, 0.8750000000000001110, 1.000000000000000000 ),
 .UNSPECIFIED. ) ;
#40092=PLANE ( 'NONE',  #16284 ) ;
#40095=CARTESIAN_POINT ( 'NONE',  ( -12.76303204525000012, -60.06485147653999945, -1.980584515753000208 ) ) ;
#40096=AXIS2_PLACEMENT_3D ( 'NONE', #11921, #29899, #58232 ) ;
#40098=CARTESIAN_POINT ( 'NONE',  ( -1.214351151748000124, -1.533058083081000111, 3.496700174682000117 ) ) ;
#40100=FACE_OUTER_BOUND ( 'NONE', #48685, .T. ) ;
#40101=CARTESIAN_POINT ( 'NONE',  ( 1.980584515756000030, -18.73514849905999924, -12.76303204340999997 ) ) ;
#40104=CARTESIAN_POINT ( 'NONE',  ( -12.56594317982999875, -55.55000000504000468, 1.750000000000000000 ) ) ;
#40106=CARTESIAN_POINT ( 'NONE',  ( -10.18491068058999893, -55.49283065365000311, -7.640030139739999449 ) ) ;
#40108=CARTESIAN_POINT ( 'NONE',  ( 9.369164850722000892, -18.75000000000000000, -7.601397897754999633 ) ) ;
#40111=CARTESIAN_POINT ( 'NONE',  ( -11.75000000000000000, -77.70000000000000284, 0.000000000000000000 ) ) ;
#40112=CARTESIAN_POINT ( 'NONE',  ( -2.062673488738000049, -23.32452529362999982, 12.82904091339000097 ) ) ;
#40114=ORIENTED_EDGE ( 'NONE', *, *, #11634, .F. ) ;
#40115=CARTESIAN_POINT ( 'NONE',  ( -12.80900240954000147, -58.55365779174999830, 1.930989144707000005 ) ) ;
#40116=CARTESIAN_POINT ( 'NONE',  ( -7.624757993407000001, -54.99647951274999969, -10.47516388917000008 ) ) ;
#40118=VERTEX_POINT ( 'NONE', #32172 ) ;
#40119=ORIENTED_EDGE ( 'NONE', *, *, #15903, .T. ) ;
#40123=ORIENTED_EDGE ( 'NONE', *, *, #9903, .F. ) ;
#40128=DIRECTION ( 'NONE',  ( 0.000000000000000000, 0.000000000000000000, -1.000000000000000000 ) ) ;
#40131=CARTESIAN_POINT ( 'NONE',  ( -13.13047446164998711, -22.78578169018998878, -0.8260994316375004365 ) ) ;
#40134=VECTOR ( 'NONE', #5253, 1000.000000000000000 ) ;
#40136=DIRECTION ( 'NONE',  ( 0.7071067811865475727, 0.000000000000000000, -0.7071067811865475727 ) ) ;
#40139=CARTESIAN_POINT ( 'NONE',  ( 9.754023262367999436, -76.24978791229999331, -7.509630405475999915 ) ) ;
#40142=CARTESIAN_POINT ( 'NONE',  ( -2.263164996904851289, -2.919503939068432530, -2.771219827481139042 ) ) ;
#40143=CARTESIAN_POINT ( 'NONE',  ( -9.346058021984571695, -16.83471832412213232, 8.620905970628376380 ) ) ;
#40144=CARTESIAN_POINT ( 'NONE',  ( 0.5999999999999999778, -18.84999999999999787, -10.98362417419999915 ) ) ;
#40145=DIRECTION ( 'NONE',  ( 0.000000000000000000, 0.000000000000000000, -1.000000000000000000 ) ) ;
#40148=CARTESIAN_POINT ( 'NONE',  ( -10.10912517723439841, -23.47586858184963532, -7.634643689412396128 ) ) ;
#40152=ORIENTED_EDGE ( 'NONE', *, *, #30155, .F. ) ;
#40154=EDGE_CURVE ( 'NONE', #28360, #30070, #14882, .T. ) ;
#40155=CARTESIAN_POINT ( 'NONE',  ( -11.44417895085270942, -77.82083333333333997, -3.075537641221545826 ) ) ;
#40156=CARTESIAN_POINT ( 'NONE',  ( -12.00000000000000000, -18.75000000000000000, 0.000000000000000000 ) ) ;
#40157=LINE ( 'NONE', #18027, #15449 ) ;
#40161=CARTESIAN_POINT ( 'NONE',  ( -9.433548213854539455, -25.12797454612102754, -8.532643227186095913 ) ) ;
#40164=FACE_OUTER_BOUND ( 'NONE', #16039, .T. ) ;
#40167=CARTESIAN_POINT ( 'NONE',  ( -3.250000000000000000, -2.100000000000000089, 0.000000000000000000 ) ) ;
#40170=ADVANCED_FACE ( 'NONE', ( #4456 ), #11621, .F. ) ;
#40173=EDGE_CURVE ( 'NONE', #9708, #41885, #22750, .T. ) ;
#40174=LINE ( 'NONE', #21301, #43041 ) ;
#40176=CARTESIAN_POINT ( 'NONE',  ( 3.150470485466851933, -78.55114870413540018, 11.31836463120567160 ) ) ;
#40177=CARTESIAN_POINT ( 'NONE',  ( 26.50000000000000000, -39.30476017083000073, 1.155265119678999855E-13 ) ) ;
#40180=CARTESIAN_POINT ( 'NONE',  ( -2.099388381696000023E-14, 0.000000000000000000, -12.69999999999999929 ) ) ;
#40181=CARTESIAN_POINT ( 'NONE',  ( 9.370643039124985307, -75.80000000000003979, -7.368669060076848076 ) ) ;
#40195=ORIENTED_EDGE ( 'NONE', *, *, #13958, .T. ) ;
#40196=VECTOR ( 'NONE', #8070, 1000.000000000000000 ) ;
#40197=ORIENTED_EDGE ( 'NONE', *, *, #43625, .F. ) ;
#40198=CARTESIAN_POINT ( 'NONE',  ( -9.723174507563001612, -61.27697503937000079, -7.958760295438001009 ) ) ;
#40200=ORIENTED_EDGE ( 'NONE', *, *, #56315, .T. ) ;
#40201=CARTESIAN_POINT ( 'NONE',  ( -7.421655993048999811, -78.47872433538000791, 9.763070719336001346 ) ) ;
#40204=EDGE_CURVE ( 'NONE', #51850, #822, #52224, .T. ) ;
#40205=ADVANCED_FACE ( 'NONE', ( #43098 ), #309, .T. ) ;
#40206=CARTESIAN_POINT ( 'NONE',  ( -7.626500902235000545, -60.11584477251999203, 10.35747158364999976 ) ) ;
#40211=ORIENTED_EDGE ( 'NONE', *, *, #30155, .T. ) ;
#40217=CARTESIAN_POINT ( 'NONE',  ( 12.23521718689999993, -76.14169869620000952, -4.290956967987999526 ) ) ;
#40219=CARTESIAN_POINT ( 'NONE',  ( 12.80090744918999945, -56.03767312542999690, 1.980532734072999901 ) ) ;
#40220=B_SPLINE_CURVE_WITH_KNOTS ( 'NONE', 3,
 ( #11728, #47753, #7288, #25288, #47474, #51308 ),
 .UNSPECIFIED., .F., .F.,
 ( 4, 2, 4 ),
 ( 0.000000000000000000, 0.5000000000000000000, 1.000000000000000000 ),
 .UNSPECIFIED. ) ;
#40222=CARTESIAN_POINT ( 'NONE',  ( 12.43647099681000157, -17.08193128089000012, 0.03491583288331000234 ) ) ;
#40230=CARTESIAN_POINT ( 'NONE',  ( -10.08162962782999905, -17.28146287379999890, -7.981572332336000386 ) ) ;
#40232=DIRECTION ( 'NONE',  ( 0.000000000000000000, -1.000000000000000000, 0.000000000000000000 ) ) ;
#40233=CARTESIAN_POINT ( 'NONE',  ( -1.890224871707000043, -18.25210751985000002, -12.68696160873999901 ) ) ;
#40234=DIRECTION ( 'NONE',  ( -0.9999999930530776293, 0.000000000000000000, -0.0001178721535688749008 ) ) ;
#40235=CARTESIAN_POINT ( 'NONE',  ( 10.53101998745000145, -55.49360374314999689, -7.613962827161000035 ) ) ;
#40236=FACE_OUTER_BOUND ( 'NONE', #40783, .T. ) ;
#40238=CARTESIAN_POINT ( 'NONE',  ( -12.80088938717999980, -56.03743348177000172, 1.980532758767000301 ) ) ;
#40241=ORIENTED_EDGE ( 'NONE', *, *, #7612, .T. ) ;
#40242=CARTESIAN_POINT ( 'NONE',  ( 12.57042253521000141, -15.89905023022000030, 0.000000000000000000 ) ) ;
#40243=CARTESIAN_POINT ( 'NONE',  ( 1.389926494652000022, -54.17618663712000426, 12.65988803918999928 ) ) ;
#40244=FACE_OUTER_BOUND ( 'NONE', #29723, .T. ) ;
#40245=CIRCLE ( 'NONE', #3491, 12.50000000000000000 ) ;
#40246=CARTESIAN_POINT ( 'NONE',  ( 1.588974128205000058, -1.877812473829999940, -3.458412288513000199 ) ) ;
#40247=CIRCLE ( 'NONE', #11987, 1.750000000000000666 ) ;
#40249=EDGE_CURVE ( 'NONE', #33666, #4024, #33253, .T. ) ;
#40250=CARTESIAN_POINT ( 'NONE',  ( -13.99999999961999819, -72.70000000038000110, 1.691901337660000028E-09 ) ) ;
#40252=CARTESIAN_POINT ( 'NONE',  ( 12.66313295597999833, -16.82196533882000011, -0.06049275240486999550 ) ) ;
#40254=DIRECTION ( 'NONE',  ( 0.000000000000000000, -1.000000000000000000, 0.000000000000000000 ) ) ;
#40255=CARTESIAN_POINT ( 'NONE',  ( 9.233489274360861643, -76.75868152203480577, 7.775098440744370620 ) ) ;
#40256=CARTESIAN_POINT ( 'NONE',  ( -5.351850814891999875, -79.07833840369001166, 11.44861053826999964 ) ) ;
#40260=CARTESIAN_POINT ( 'NONE',  ( 1.779623408287325015, -60.93630868986362259, 12.71471627660582193 ) ) ;
#40267=CARTESIAN_POINT ( 'NONE',  ( 12.50000000000000000, -54.11640971901999819, -1.003652782195000093 ) ) ;
#40270=EDGE_CURVE ( 'NONE', #1025, #16006, #29491, .T. ) ;
#40274=VERTEX_POINT ( 'NONE', #19490 ) ;
#40278=CARTESIAN_POINT ( 'NONE',  ( 12.50000000000000000, -60.04999999966999980, 0.000000000000000000 ) ) ;
#40280=EDGE_LOOP ( 'NONE', ( #599, #56654 ) ) ;
#40281=DIRECTION ( 'NONE',  ( 0.000000000000000000, -1.433672777923999722E-08, 0.9999999999999998890 ) ) ;
#40282=LINE ( 'NONE', #9289, #37135 ) ;
#40285=CARTESIAN_POINT ( 'NONE',  ( 1.933504092460000212, -23.40406847274999791, -12.70940235707999832 ) ) ;
#40289=DIRECTION ( 'NONE',  ( 0.7071067811863970265, -3.534300182982984496E-08, 0.7071067811866971198 ) ) ;
#40290=CARTESIAN_POINT ( 'NONE',  ( 3.072533585156999703, -79.06378271215000098, -11.81724133653000131 ) ) ;
#40292=EDGE_LOOP ( 'NONE', ( #20387, #44727, #42255, #23863 ) ) ;
#40293=CARTESIAN_POINT ( 'NONE',  ( 10.19999999921000011, -0.2000000007865999907, -1.811584077144999807E-09 ) ) ;
#40295=VECTOR ( 'NONE', #55011, 1000.000000000000000 ) ;
#40296=CARTESIAN_POINT ( 'NONE',  ( -1.980611416589750817, -60.32597731777364203, -12.74335092665457303 ) ) ;
#40298=AXIS2_PLACEMENT_3D ( 'NONE', #17048, #12330, #38900 ) ;
#40302=CARTESIAN_POINT ( 'NONE',  ( 7.167851722631999323, -78.00376328549999982, -10.60335505485999974 ) ) ;
#40303=CARTESIAN_POINT ( 'NONE',  ( -9.416026390438000604, -78.19420564057999457, 6.872484323511000248 ) ) ;
#40304=EDGE_CURVE ( 'NONE', #50392, #14039, #5066, .T. ) ;
#40306=CARTESIAN_POINT ( 'NONE',  ( 8.485281374238999419, -60.04999999966999980, -8.485281374238999419 ) ) ;
#40308=CARTESIAN_POINT ( 'NONE',  ( 12.60356226362999976, -19.24922971138999728, 1.750000000000000000 ) ) ;
#40309=CARTESIAN_POINT ( 'NONE',  ( 0.000000000000000000, -46.09579702914000165, 0.000000000000000000 ) ) ;
#40311=DIRECTION ( 'NONE',  ( 0.000000000000000000, -1.000000000000000000, 0.000000000000000000 ) ) ;
#40314=CARTESIAN_POINT ( 'NONE',  ( 3.702420020526000055, -2.551279764406999995, 0.8821385418971999792 ) ) ;
#40316=ORIENTED_EDGE ( 'NONE', *, *, #20329, .T. ) ;
#40318=LINE ( 'NONE', #49778, #50591 ) ;
#40321=CARTESIAN_POINT ( 'NONE',  ( -8.048032176077001054, -78.41399203484999703, 9.328081102756000220 ) ) ;
#40322=CARTESIAN_POINT ( 'NONE',  ( -7.730443418336787609, -60.92191635792283222, -10.25197760567054317 ) ) ;
#40323=CARTESIAN_POINT ( 'NONE',  ( 12.58338334669999981, -21.74800977511999989, -1.667961445601999992 ) ) ;
#40325=CARTESIAN_POINT ( 'NONE',  ( -9.102117850481628025, -24.97186524166153276, -8.583692176905405091 ) ) ;
#40326=B_SPLINE_CURVE_WITH_KNOTS ( 'NONE', 3,
 ( #43452, #42880, #47325, #6855, #2729, #24864, #43749, #11873, #39301, #3301 ),
 .UNSPECIFIED., .F., .F.,
 ( 4, 2, 2, 2, 4 ),
 ( 0.000000000000000000, 0.1250000000000000278, 0.2500000000000000555, 0.5000000000000000000, 1.000000000000000000 ),
 .UNSPECIFIED. ) ;
#40333=CARTESIAN_POINT ( 'NONE',  ( -3.587712099295000012, -1.814945589986999952, 1.801380527025000067 ) ) ;
#40334=CARTESIAN_POINT ( 'NONE',  ( -2.062503053667999797, -57.04263462147999775, -12.92177931909999877 ) ) ;
#40336=EDGE_LOOP ( 'NONE', ( #11899, #18681, #9870, #8753 ) ) ;
#40338=CARTESIAN_POINT ( 'NONE',  ( -11.75000000000000000, -78.20000000000000284, 1.702919296826999607E-14 ) ) ;
#40342=ORIENTED_EDGE ( 'NONE', *, *, #13836, .T. ) ;
#40345=DIRECTION ( 'NONE',  ( 0.9999999999998321343, 0.000000000000000000, 5.794540611356191117E-07 ) ) ;
#40347=ORIENTED_EDGE ( 'NONE', *, *, #10820, .T. ) ;
#40351=CARTESIAN_POINT ( 'NONE',  ( 7.664266801486627756, -60.54946977258676100, 7.892048199454674062 ) ) ;
#40361=DIRECTION ( 'NONE',  ( 0.000000000000000000, 1.000000000000000000, 0.000000000000000000 ) ) ;
#40363=CARTESIAN_POINT ( 'NONE',  ( 11.44417895085270054, -78.57083333333332575, 3.075537641221564922 ) ) ;
#40364=EDGE_CURVE ( 'NONE', #1897, #53199, #22900, .T. ) ;
#40365=CARTESIAN_POINT ( 'NONE',  ( 7.613962745591999592, -55.49360215019999742, -10.53101990617999917 ) ) ;
#40366=DIRECTION ( 'NONE',  ( 0.000000000000000000, 1.000000000000000000, 0.000000000000000000 ) ) ;
#40367=CARTESIAN_POINT ( 'NONE',  ( -10.19022265128000093, -23.19634105642999700, 7.646946115745000050 ) ) ;
#40372=FACE_OUTER_BOUND ( 'NONE', #47714, .T. ) ;
#40375=CARTESIAN_POINT ( 'NONE',  ( -1.582498447119000229, -24.15086122477999808, 12.55493832972999968 ) ) ;
#40378=CARTESIAN_POINT ( 'NONE',  ( -2.982938763343999877, -2.003833096891999954, -1.417087710164999903 ) ) ;
#40381=CARTESIAN_POINT ( 'NONE',  ( 12.77568181207000109, -62.06511628600999586, -0.5294980821349999367 ) ) ;
#40395=CARTESIAN_POINT ( 'NONE',  ( -1.164828128805999992E-14, -72.79999999999999716, -13.89999999999999858 ) ) ;
#40398=CARTESIAN_POINT ( 'NONE',  ( -10.01676948373999920, -60.00938276551000428, 7.658894993385999328 ) ) ;
#40400=CARTESIAN_POINT ( 'NONE',  ( 8.913248419499998576, -76.94780122596999661, -7.987006294937000206 ) ) ;
#40401=CARTESIAN_POINT ( 'NONE',  ( -5.489373150238907151, -76.38659796104998634, -10.46729459822925534 ) ) ;
#40402=CARTESIAN_POINT ( 'NONE',  ( 12.49989425040000057, -23.19225390461999936, -1.666425739591000044 ) ) ;
#40403=CARTESIAN_POINT ( 'NONE',  ( -2.062673488410000200, -55.47547726255000100, 12.82904109059999875 ) ) ;
#40404=ORIENTED_EDGE ( 'NONE', *, *, #17231, .F. ) ;
#40408=CARTESIAN_POINT ( 'NONE',  ( 1.064406907239667577, -1.752651614945672565, -3.099959123880238199 ) ) ;
#40413=CARTESIAN_POINT ( 'NONE',  ( -11.75358435535890500, -77.70973593635036991, -1.536616025939224306 ) ) ;
#40414=CARTESIAN_POINT ( 'NONE',  ( -1.668607604520085719, -55.00618368707833383, -12.52787843847536919 ) ) ;
#40415=EDGE_LOOP ( 'NONE', ( #29667, #56325, #25399, #53126 ) ) ;
#40416=ORIENTED_EDGE ( 'NONE', *, *, #7612, .F. ) ;
#40417=MECHANICAL_DESIGN_GEOMETRIC_PRESENTATION_REPRESENTATION('',(#21528),#9287);
#40418=CARTESIAN_POINT ( 'NONE',  ( -9.996785040876998707, -54.64937852858999889, -7.758588586516999008 ) ) ;
#40422=ORIENTED_EDGE ( 'NONE', *, *, #55095, .F. ) ;
#40423=ORIENTED_EDGE ( 'NONE', *, *, #52390, .F. ) ;
#40426=ADVANCED_FACE ( 'NONE', ( #44237 ), #19423, .F. ) ;
#40428=ORIENTED_EDGE ( 'NONE', *, *, #4905, .F. ) ;
#40431=CARTESIAN_POINT ( 'NONE',  ( 5.623102978484999959, -77.33411282133998554, 11.84678905512000036 ) ) ;
#40437=ADVANCED_FACE ( 'NONE', ( #27084 ), #17069, .T. ) ;
#40440=DIRECTION ( 'NONE',  ( 0.000000000000000000, -1.000000000000000000, 0.000000000000000000 ) ) ;
#40445=CARTESIAN_POINT ( 'NONE',  ( 3.189660922236018603, -2.561412939622563112, -1.629070403506577724 ) ) ;
#40447=DIRECTION ( 'NONE',  ( 0.000000000000000000, 1.000000000000000000, 0.000000000000000000 ) ) ;
#40449=CARTESIAN_POINT ( 'NONE',  ( -8.666912951892083328, -61.79291380850746407, -9.019442092672255384 ) ) ;
#40451=CARTESIAN_POINT ( 'NONE',  ( 3.717789071696637304, -76.90015469873267762, 11.48706906119333304 ) ) ;
#40465=CARTESIAN_POINT ( 'NONE',  ( 1.477284502223000118, -54.07368499670000261, -12.77254812464999922 ) ) ;
#40466=CARTESIAN_POINT ( 'NONE',  ( 8.313575899745858422, -76.01186070635600345, 8.302913058421760084 ) ) ;
#40470=CARTESIAN_POINT ( 'NONE',  ( -1.771468677314999907, -75.93649240829408598, 12.18184739844999420 ) ) ;
#40475=FACE_OUTER_BOUND ( 'NONE', #13143, .T. ) ;
#40481=CARTESIAN_POINT ( 'NONE',  ( 6.227934374241346660, -75.79999999999999716, -10.14191869714119676 ) ) ;
#40483=CARTESIAN_POINT ( 'NONE',  ( 3.073856691126545915, -76.34527577747576288, -11.36762008860266171 ) ) ;
#40488=DIRECTION ( 'NONE',  ( 0.000000000000000000, 1.000000000000000000, 0.000000000000000000 ) ) ;
#40491=CARTESIAN_POINT ( 'NONE',  ( -12.43640309385000009, -24.91747517602999906, -0.05224034426415000154 ) ) ;
#40501=CARTESIAN_POINT ( 'NONE',  ( 7.645391636765999976, -23.21530450358000053, 10.18949673576000059 ) ) ;
#40509=EDGE_CURVE ( 'NONE', #6488, #22487, #58391, .T. ) ;
#40511=ORIENTED_EDGE ( 'NONE', *, *, #2589, .T. ) ;
#40515=DIRECTION ( 'NONE',  ( 0.7071067811865475727, 0.000000000000000000, -0.7071067811865475727 ) ) ;
#40517=CARTESIAN_POINT ( 'NONE',  ( 11.97191554488999898, -76.11037712840000324, 4.552639408432999524 ) ) ;
#40519=CARTESIAN_POINT ( 'NONE',  ( 9.164374456753368037, -53.58432317374141007, -8.803712804513708079 ) ) ;
#40521=CARTESIAN_POINT ( 'NONE',  ( 12.83677071377000090, -18.77261389757000032, -2.062839858857999698 ) ) ;
#40523=CARTESIAN_POINT ( 'NONE',  ( -10.84553603787253095, -76.66823218638354831, 4.520140657707524490 ) ) ;
#40525=VERTEX_POINT ( 'NONE', #49846 ) ;
#40530=CARTESIAN_POINT ( 'NONE',  ( -10.52682159591000044, -18.57432398260000284, 7.605688676868000542 ) ) ;
#40531=DIRECTION ( 'NONE',  ( 0.000000000000000000, 0.1122098755727947705, -0.9936845293270585300 ) ) ;
#40532=EDGE_CURVE ( 'NONE', #10595, #20949, #27380, .T. ) ;
#40533=DIRECTION ( 'NONE',  ( -0.7071067812094172789, -2.924114042631071410E-07, -0.7071067811636172484 ) ) ;
#40538=CARTESIAN_POINT ( 'NONE',  ( 3.250000000000000000, -1.750000000000000000, 0.000000000000000000 ) ) ;
#40540=VERTEX_POINT ( 'NONE', #44816 ) ;
#40542=CARTESIAN_POINT ( 'NONE',  ( 0.5506765233279000693, -53.54045707723000191, 12.77514798307000099 ) ) ;
#40543=CARTESIAN_POINT ( 'NONE',  ( -1.667260628937999867, -60.00942012442000362, -12.49858003896999925 ) ) ;
#40544=CARTESIAN_POINT ( 'NONE',  ( -3.420922791951000352, -1.780913946619999910, 1.097631908065999973 ) ) ;
#40547=AXIS2_PLACEMENT_3D ( 'NONE', #4470, #17457, #35444 ) ;
#40548=CARTESIAN_POINT ( 'NONE',  ( -3.165411199172024848, -1.520833333333333259, -0.8506806241676611036 ) ) ;
#40550=CARTESIAN_POINT ( 'NONE',  ( -1.814305421036000121, -61.08941969298000174, 12.78003582256000215 ) ) ;
#40551=CARTESIAN_POINT ( 'NONE',  ( -10.07627163191000008, -60.04999999725999515, -7.601397897754999633 ) ) ;
#40557=CARTESIAN_POINT ( 'NONE',  ( 2.615203195289000249, -78.85319526808000035, 12.68173180764000030 ) ) ;
#40561=CARTESIAN_POINT ( 'NONE',  ( -1.689459951007934224, -61.09188253860865814, 12.71013585614315922 ) ) ;
#40564=CARTESIAN_POINT ( 'NONE',  ( 1.247385801071000166, -17.52277743742000027, -12.50301438876999960 ) ) ;
#40565=LINE ( 'NONE', #13095, #40022 ) ;
#40567=CARTESIAN_POINT ( 'NONE',  ( 12.56594317982999875, -55.55000000504000468, -1.750000000000000000 ) ) ;
#40569=CARTESIAN_POINT ( 'NONE',  ( 0.000000000000000000, -80.70000000000000284, 0.000000000000000000 ) ) ;
#40572=CARTESIAN_POINT ( 'NONE',  ( 8.171144579309718381, -55.45989902438863339, 7.364280830340200978 ) ) ;
#40573=ORIENTED_EDGE ( 'NONE', *, *, #46589, .T. ) ;
#40576=CARTESIAN_POINT ( 'NONE',  ( -3.499999997848071587, -0.7500000000000000000, 0.3665191617529296453 ) ) ;
#40577=EDGE_LOOP ( 'NONE', ( #38674, #37075, #42863, #23677 ) ) ;
#40578=DIRECTION ( 'NONE',  ( 0.000000000000000000, 0.000000000000000000, 1.000000000000000000 ) ) ;
#40579=VERTEX_POINT ( 'NONE', #22966 ) ;
#40580=DIRECTION ( 'NONE',  ( 0.7071067811865475727, 0.000000000000000000, -0.7071067811865475727 ) ) ;
#40583=CARTESIAN_POINT ( 'NONE',  ( -0.9781264271452000392, -24.94031143877000289, -12.65967462879000038 ) ) ;
#40587=CARTESIAN_POINT ( 'NONE',  ( -3.320254015711999962, -78.14236234271000114, 11.17445779594999955 ) ) ;
#40588=ADVANCED_FACE ( 'NONE', ( #12919, #49244, #22372, #8495 ), #41854, .T. ) ;
#40589=ORIENTED_EDGE ( 'NONE', *, *, #19701, .T. ) ;
#40594=AXIS2_PLACEMENT_3D ( 'NONE', #54657, #9492, #27477 ) ;
#40596=PLANE ( 'NONE',  #48309 ) ;
#40598=CARTESIAN_POINT ( 'NONE',  ( -8.012867221502000703, -78.34986579304998600, 9.287323121044000374 ) ) ;
#40599=CARTESIAN_POINT ( 'NONE',  ( -7.915529793650001089, -78.26278494331999980, 9.174504061492999796 ) ) ;
#40601=DIRECTION ( 'NONE',  ( -1.000000000000000000, 0.000000000000000000, 0.000000000000000000 ) ) ;
#40604=CARTESIAN_POINT ( 'NONE',  ( -10.53003223724999948, -60.12452529330000317, 7.612971414731999786 ) ) ;
#40605=CARTESIAN_POINT ( 'NONE',  ( 2.997702459963058175, -2.882598562504878448, 1.253802824134951921 ) ) ;
#40608=EDGE_CURVE ( 'NONE', #17178, #5420, #50428, .T. ) ;
#40609=CARTESIAN_POINT ( 'NONE',  ( 0.000000000000000000, 4.040000000000000036, 0.000000000000000000 ) ) ;
#40612=ORIENTED_EDGE ( 'NONE', *, *, #21070, .F. ) ;
#40613=CARTESIAN_POINT ( 'NONE',  ( -0.5999999999999999778, -23.15000000000000213, 10.98362417419999915 ) ) ;
#40616=DIRECTION ( 'NONE',  ( 0.000000000000000000, -1.000000000000000000, 0.000000000000000000 ) ) ;
#40617=VECTOR ( 'NONE', #11673, 1000.000000000000000 ) ;
#40619=CARTESIAN_POINT ( 'NONE',  ( -12.96685733093999993, -77.02403958349000845, -1.095351912296000041 ) ) ;
#40621=CARTESIAN_POINT ( 'NONE',  ( 12.80896991329000123, -20.24546192895000019, -1.930989179114000143 ) ) ;
#40623=ADVANCED_FACE ( 'NONE', ( #42143 ), #5530, .F. ) ;
#40624=CARTESIAN_POINT ( 'NONE',  ( -9.243123479229344852, -24.91653773630011059, -8.441201027682305735 ) ) ;
#40625=CARTESIAN_POINT ( 'NONE',  ( 13.94764600793045517, -33.10361340872000113, 0.1325532415315603119 ) ) ;
#40631=CARTESIAN_POINT ( 'NONE',  ( 2.301364338783000285, -1.421557261823000129, -3.291430154679999998 ) ) ;
#40632=CARTESIAN_POINT ( 'NONE',  ( -1.667916687331000070, -60.09848884406000025, -12.49168451100999988 ) ) ;
#40634=ORIENTED_EDGE ( 'NONE', *, *, #18845, .T. ) ;
#40635=B_SPLINE_CURVE_WITH_KNOTS ( 'NONE', 3,
 ( #54001, #43975, #8526, #26520, #3525, #35676, #53707, #21526, #39534, #57539 ),
 .UNSPECIFIED., .F., .F.,
 ( 4, 2, 2, 2, 4 ),
 ( 0.000000000000000000, 0.2500000000000000000, 0.5000000000000000000, 0.7500000000000000000, 1.000000000000000000 ),
 .UNSPECIFIED. ) ;
#40638=AXIS2_PLACEMENT_3D ( 'NONE', #48464, #8007, #16584 ) ;
#40639=VERTEX_POINT ( 'NONE', #10863 ) ;
#40642=ADVANCED_FACE ( 'NONE', ( #50138 ), #32968, .F. ) ;
#40645=ORIENTED_EDGE ( 'NONE', *, *, #33195, .F. ) ;
#40648=ORIENTED_EDGE ( 'NONE', *, *, #24040, .F. ) ;
#40649=CARTESIAN_POINT ( 'NONE',  ( -2.996749445452521421, -2.632334343058801096, -1.256619453663492703 ) ) ;
#40650=B_SPLINE_SURFACE_WITH_KNOTS ( 'NONE', 3, 3, ( 
 ( #24361, #19350, #42375, #15500 ),
 ( #33494, #51532, #46234, #48263 ),
 ( #39090, #21083, #52962, #7798 ),
 ( #25798, #26082, #11947, #42956 ),
 ( #16664, #43825, #29352, #7220 ),
 ( #3374, #15791, #2799, #12511 ),
 ( #57097, #16085, #16374, #21368 ),
 ( #20228, #39384, #38220, #47399 ),
 ( #25222, #38798, #7512, #8084 ),
 ( #24934, #57389, #16949, #3089 ),
 ( #25510, #44106, #47973, #43528 ) ),
 .UNSPECIFIED., .F., .F., .F.,
 ( 4, 1, 1, 1, 1, 1, 1, 1, 4 ),
 ( 4, 4 ),
 ( -0.01994574723506000249, 0.000000000000000000, 0.1666666666667000196, 0.3333333333333000081, 0.5000000000000000000, 0.6666666666667000474, 0.8333333333333000637, 1.000000000000000000, 1.020511277925000071 ),
 ( -0.3582002740308999900, 1.358574366093000085 ),
 .UNSPECIFIED. ) ;
#40652=CARTESIAN_POINT ( 'NONE',  ( -3.434862764218605591, -1.304367894840707365, 2.089124736184700737 ) ) ;
#40653=ORIENTED_EDGE ( 'NONE', *, *, #56786, .F. ) ;
#40654=CIRCLE ( 'NONE', #57577, 14.00000000000000000 ) ;
#40655=ORIENTED_EDGE ( 'NONE', *, *, #51824, .F. ) ;
#40658=CARTESIAN_POINT ( 'NONE',  ( 10.53562613913000057, -55.59442116235999976, 7.620013630307000518 ) ) ;
#40659=CARTESIAN_POINT ( 'NONE',  ( -7.655555357453000198, -19.22204592323999961, -10.38646360831000059 ) ) ;
#40661=LINE ( 'NONE', #44496, #58196 ) ;
#40665=CARTESIAN_POINT ( 'NONE',  ( -8.798028344861998917, -24.93813495683999903, 8.790623041439999952 ) ) ;
#40666=VECTOR ( 'NONE', #38300, 1000.000000000000114 ) ;
#40670=AXIS2_PLACEMENT_3D ( 'NONE', #35156, #44049, #50456 ) ;
#40674=FACE_BOUND ( 'NONE', #30195, .T. ) ;
#40675=CARTESIAN_POINT ( 'NONE',  ( 0.9781264271452999592, -24.94031143877000289, 12.65967462879000038 ) ) ;
#40676=CARTESIAN_POINT ( 'NONE',  ( -12.50680023857786338, -61.10414033366070186, -1.424451025847738972 ) ) ;
#40677=CARTESIAN_POINT ( 'NONE',  ( -1.165121112472999876, -1.482669754918000127, -3.780546559146999996 ) ) ;
#40680=CARTESIAN_POINT ( 'NONE',  ( 10.35845608624000036, -55.50221245779999890, 7.627487525399000212 ) ) ;
#40684=CARTESIAN_POINT ( 'NONE',  ( -12.51072239526000196, -26.30294702885999669, 0.7871079366006996647 ) ) ;
#40695=DIRECTION ( 'NONE',  ( 0.000000000000000000, 1.000000000000000000, 0.000000000000000000 ) ) ;
#40698=DIRECTION ( 'NONE',  ( 1.000000000000000000, 0.000000000000000000, 0.000000000000000000 ) ) ;
#40699=CARTESIAN_POINT ( 'NONE',  ( -1.155570385622000096, -77.37333680668000113, -12.58848097821000067 ) ) ;
#40700=DIRECTION ( 'NONE',  ( 0.7071067811865475727, 0.000000000000000000, -0.7071067811865475727 ) ) ;
#40701=CARTESIAN_POINT ( 'NONE',  ( 12.78015149457000099, -24.30330660695999967, -1.806228889758999978 ) ) ;
#40702=CARTESIAN_POINT ( 'NONE',  ( -7.655983890325164687, -55.09663439856309708, -10.06694524866255946 ) ) ;
#40703=ORIENTED_EDGE ( 'NONE', *, *, #23172, .F. ) ;
#40704=CARTESIAN_POINT ( 'NONE',  ( -1.217390015646170554, -53.98106975039858924, -12.70229597936710420 ) ) ;
#40706=CARTESIAN_POINT ( 'NONE',  ( 5.348541196722845115, -75.86208451537127928, -10.50221102791410033 ) ) ;
#40707=ADVANCED_FACE ( 'NONE', ( #9978 ), #41562, .F. ) ;
#40709=EDGE_CURVE ( 'NONE', #5204, #51909, #19081, .T. ) ;
#40710=CARTESIAN_POINT ( 'NONE',  ( -12.75763395696999858, -56.02204592290999585, -1.931043742978000077 ) ) ;
#40712=EDGE_LOOP ( 'NONE', ( #9930, #22340, #38252, #22993 ) ) ;
#40714=CARTESIAN_POINT ( 'NONE',  ( 7.861032689965319342, -61.26660299192877801, -10.10708926017425924 ) ) ;
#40715=ORIENTED_EDGE ( 'NONE', *, *, #36825, .T. ) ;
#40717=EDGE_LOOP ( 'NONE', ( #16875, #3865, #22635 ) ) ;
#40718=CARTESIAN_POINT ( 'NONE',  ( -7.645398650953000086, -55.58468617124000133, -10.18948982067999864 ) ) ;
#40721=EDGE_LOOP ( 'NONE', ( #56899, #42400, #34737, #37006, #5328 ) ) ;
#40726=EDGE_CURVE ( 'NONE', #5887, #51923, #55015, .T. ) ;
#40729=CARTESIAN_POINT ( 'NONE',  ( -3.153993092687999766, -78.38870099961999927, 12.72742730875000028 ) ) ;
#40735=ORIENTED_EDGE ( 'NONE', *, *, #48767, .T. ) ;
#40739=CARTESIAN_POINT ( 'NONE',  ( -2.945092855005243315, -3.303172867046446193, 1.926994060853980839 ) ) ;
#40740=CARTESIAN_POINT ( 'NONE',  ( 7.660431276897000430, -59.99179487629999841, -10.01749742442000191 ) ) ;
#40744=CARTESIAN_POINT ( 'NONE',  ( -5.099558739856028922, -77.14031901058056917, -10.93429447588933634 ) ) ;
#40745=CARTESIAN_POINT ( 'NONE',  ( 9.367799907751061639, -76.64748953336749082, -7.737080272526681846 ) ) ;
#40749=CARTESIAN_POINT ( 'NONE',  ( -1.164828128805999992E-14, -72.75000000040999737, -13.94999999959000014 ) ) ;
#40752=CARTESIAN_POINT ( 'NONE',  ( 1.250000000000000000, -55.54999999966999980, -12.00000000000000000 ) ) ;
#40756=CARTESIAN_POINT ( 'NONE',  ( 2.738482428451646911, -76.05593295161513367, 11.42672558838834895 ) ) ;
#40760=EDGE_CURVE ( 'NONE', #47713, #19532, #39906, .T. ) ;
#40761=CARTESIAN_POINT ( 'NONE',  ( -10.62397638184999948, -76.09214061310410671, -6.218250916117999516 ) ) ;
#40763=EDGE_CURVE ( 'NONE', #18636, #41301, #55579, .T. ) ;
#40767=CYLINDRICAL_SURFACE ( 'NONE', #1044, 1.750000000000001332 ) ;
#40771=CARTESIAN_POINT ( 'NONE',  ( 12.70619604133367098, -17.53855724477478972, 1.571828507159243271 ) ) ;
#40772=CARTESIAN_POINT ( 'NONE',  ( 0.9382417441925061663, -75.80000000000001137, -11.80136876550232117 ) ) ;
#40774=VECTOR ( 'NONE', #22748, 1000.000000000000000 ) ;
#40776=EDGE_CURVE ( 'NONE', #32275, #5785, #43639, .T. ) ;
#40778=DIRECTION ( 'NONE',  ( 0.000000000000000000, -1.000000000000000000, 0.000000000000000000 ) ) ;
#40779=LINE ( 'NONE', #53781, #13864 ) ;
#40782=FACE_BOUND ( 'NONE', #49876, .T. ) ;
#40783=EDGE_LOOP ( 'NONE', ( #56912, #35982, #33283, #31176 ) ) ;
#40784=EDGE_LOOP ( 'NONE', ( #43623, #25533, #35691, #28039 ) ) ;
#40787=CIRCLE ( 'NONE', #50243, 30.49999999999998934 ) ;
#40788=ORIENTED_EDGE ( 'NONE', *, *, #2918, .F. ) ;
#40790=ORIENTED_EDGE ( 'NONE', *, *, #27348, .F. ) ;
#40791=CARTESIAN_POINT ( 'NONE',  ( 8.588902834690999910, -25.13240111580999780, 9.317946123639000433 ) ) ;
#40793=CARTESIAN_POINT ( 'NONE',  ( 8.180687091746211337, -55.49344856148323402, -7.353725627631179762 ) ) ;
#40804=CYLINDRICAL_SURFACE ( 'NONE', #55471, 0.6000000000000008660 ) ;
#40807=VECTOR ( 'NONE', #28918, 1000.000000000000000 ) ;
#40808=CARTESIAN_POINT ( 'NONE',  ( 11.50045843932000089, -76.73061308324000152, -3.738034289973000135 ) ) ;
#40812=CIRCLE ( 'NONE', #51204, 0.5000000000000004441 ) ;
#40823=CARTESIAN_POINT ( 'NONE',  ( -3.250000000000000000, -3.500000000000000000, -1.188926645705999921E-13 ) ) ;
#40825=FACE_OUTER_BOUND ( 'NONE', #49206, .T. ) ;
#40833=CARTESIAN_POINT ( 'NONE',  ( 1.798954018885000172, -55.58469026579999905, 12.61117007300000026 ) ) ;
#40835=CARTESIAN_POINT ( 'NONE',  ( 3.362739751829000312, -2.429750604645999790, -1.782634050134999981 ) ) ;
#40836=EDGE_CURVE ( 'NONE', #18440, #20752, #32429, .T. ) ;
#40839=AXIS2_PLACEMENT_3D ( 'NONE', #51810, #16938, #51520 ) ;
#40841=CARTESIAN_POINT ( 'NONE',  ( 12.80000000000000071, -0.1000000000000000056, 0.000000000000000000 ) ) ;
#40843=CARTESIAN_POINT ( 'NONE',  ( 12.50000000000000000, -49.87071424677999687, 0.000000000000000000 ) ) ;
#40846=CARTESIAN_POINT ( 'NONE',  ( -3.391782956974000118, -78.59828808732000027, -12.49646859905000085 ) ) ;
#40847=B_SPLINE_SURFACE_WITH_KNOTS ( 'NONE', 3, 3, ( 
 ( #51145, #55853, #31936, #14227 ),
 ( #32225, #27800, #45846, #23387 ),
 ( #41398, #48132, #33366, #29511 ),
 ( #51694, #51403, #7664, #52259 ),
 ( #25663, #25091, #52542, #3248 ),
 ( #43693, #2952, #6801, #2675 ),
 ( #11244, #12099, #29791, #33940 ),
 ( #38668, #29223, #20952, #24810 ) ),
 .UNSPECIFIED., .F., .F., .F.,
 ( 4, 1, 1, 1, 1, 4 ),
 ( 4, 4 ),
 ( -0.01200407347463999970, 0.000000000000000000, 0.3333333333333000081, 0.6666666666667000474, 1.000000000000000000, 1.011997855551999947 ),
 ( -0.3559705542741999906, 1.355970554273999928 ),
 .UNSPECIFIED. ) ;
#40854=CARTESIAN_POINT ( 'NONE',  ( -12.72554383682000001, -60.00159311597000311, 1.930239506950999884 ) ) ;
#40857=CARTESIAN_POINT ( 'NONE',  ( 12.65375411746000012, -21.74977139047000207, -1.750000000000000000 ) ) ;
#40859=CIRCLE ( 'NONE', #30469, 0.5000000000000004441 ) ;
#40863=DIRECTION ( 'NONE',  ( 0.000000000000000000, 1.000000000000000000, 0.000000000000000000 ) ) ;
#40868=CARTESIAN_POINT ( 'NONE',  ( 1.980584515752000119, -55.53514853344000102, 12.76303204600000107 ) ) ;
#40869=ORIENTED_EDGE ( 'NONE', *, *, #50452, .F. ) ;
#40870=CARTESIAN_POINT ( 'NONE',  ( -1.666698456700999920, -18.80818260160000222, 12.50018138921000066 ) ) ;
#40871=DIRECTION ( 'NONE',  ( -1.000000000000000000, 0.000000000000000000, 0.000000000000000000 ) ) ;
#40873=CARTESIAN_POINT ( 'NONE',  ( 1.801614160558000055, -23.38652261905000174, -12.59687422887999908 ) ) ;
#40876=CARTESIAN_POINT ( 'NONE',  ( -8.893690104282001130, -78.89047970819000000, -8.147993850101000746 ) ) ;
#40878=ORIENTED_EDGE ( 'NONE', *, *, #43410, .T. ) ;
#40879=CARTESIAN_POINT ( 'NONE',  ( -11.99999999979999821, -23.14999999072999870, 0.7999999997951999786 ) ) ;
#40883=FACE_OUTER_BOUND ( 'NONE', #15392, .T. ) ;
#40884=CARTESIAN_POINT ( 'NONE',  ( -10.07719973192000040, -21.74888345808999901, 7.718346056094000041 ) ) ;
#40885=CARTESIAN_POINT ( 'NONE',  ( -3.220107333416999840, -77.22669831202999546, 12.38709272308999942 ) ) ;
#40886=EDGE_CURVE ( 'NONE', #53933, #45259, #15428, .T. ) ;
#40890=DIRECTION ( 'NONE',  ( 0.000000000000000000, 0.000000000000000000, -1.000000000000000000 ) ) ;
#40893=CARTESIAN_POINT ( 'NONE',  ( 12.60354432327999952, -22.75100837100999840, 1.750000000001000089 ) ) ;
#40895=CARTESIAN_POINT ( 'NONE',  ( -9.614379562845476457, -78.25080762427336367, 6.833952463418961898 ) ) ;
#40901=CARTESIAN_POINT ( 'NONE',  ( -3.804208684430999909, -3.354482064474000325, -0.1186911049137999996 ) ) ;
#40904=CARTESIAN_POINT ( 'NONE',  ( -0.4820079653423386956, -23.51614597297864862, 10.98957811953314412 ) ) ;
#40906=CARTESIAN_POINT ( 'NONE',  ( 0.000000000000000000, 0.000000000000000000, 0.000000000000000000 ) ) ;
#40909=ADVANCED_FACE ( 'NONE', ( #24577 ), #47037, .F. ) ;
#40910=CARTESIAN_POINT ( 'NONE',  ( 1.667936697358999965, -59.56462890159999546, 12.53241208775999915 ) ) ;
#40911=CARTESIAN_POINT ( 'NONE',  ( -1.189541931187000134, -77.13504886542000349, -12.95855809378999979 ) ) ;
#40914=CARTESIAN_POINT ( 'NONE',  ( 11.71247802671000038, -76.72437053406000018, -3.008538372945000372 ) ) ;
#40915=VERTEX_POINT ( 'NONE', #39592 ) ;
#40917=CYLINDRICAL_SURFACE ( 'NONE', #2268, 0.5999999999999999778 ) ;
#40918=ADVANCED_FACE ( 'NONE', ( #7724 ), #57820, .T. ) ;
#40920=CARTESIAN_POINT ( 'NONE',  ( -1.405334850300460126, -17.68507052218669529, 12.50716844834726160 ) ) ;
#40924=CARTESIAN_POINT ( 'NONE',  ( -3.754890333716000228, -1.346196431073999999, -1.424957469106999941 ) ) ;
#40928=ORIENTED_EDGE ( 'NONE', *, *, #43021, .F. ) ;
#40932=ORIENTED_EDGE ( 'NONE', *, *, #45102, .T. ) ;
#40935=AXIS2_PLACEMENT_3D ( 'NONE', #27709, #4998, #36864 ) ;
#40936=DIRECTION ( 'NONE',  ( 0.000000000000000000, 1.000000000000000000, 0.000000000000000000 ) ) ;
#40938=EDGE_LOOP ( 'NONE', ( #45160, #54290, #52632, #40428 ) ) ;
#40941=ORIENTED_EDGE ( 'NONE', *, *, #27168, .F. ) ;
#40942=CARTESIAN_POINT ( 'NONE',  ( 0.1872937409654373275, -2.730135739282324003, -3.245155438500901379 ) ) ;
#40943=ADVANCED_FACE ( 'NONE', ( #56747 ), #27645, .F. ) ;
#40944=LINE ( 'NONE', #532, #38934 ) ;
#40945=LINE ( 'NONE', #50396, #18564 ) ;
#40946=ORIENTED_EDGE ( 'NONE', *, *, #13607, .T. ) ;
#40947=CARTESIAN_POINT ( 'NONE',  ( -9.019406120295011320, -53.80707871034554302, -8.666949038533088512 ) ) ;
#40948=ORIENTED_EDGE ( 'NONE', *, *, #1233, .F. ) ;
#40950=CARTESIAN_POINT ( 'NONE',  ( 10.18127254042999930, -55.41355771686999532, 7.633407132363999814 ) ) ;
#40951=FACE_OUTER_BOUND ( 'NONE', #52385, .T. ) ;
#40952=DIRECTION ( 'NONE',  ( -1.000000000000000000, 0.000000000000000000, 0.000000000000000000 ) ) ;
#40955=DIRECTION ( 'NONE',  ( -1.000000000000000000, 0.000000000000000000, 0.000000000000000000 ) ) ;
#40959=CARTESIAN_POINT ( 'NONE',  ( -14.00000000000000000, -9.337822431690000258, -5.544480866950999326E-06 ) ) ;
#40960=DIRECTION ( 'NONE',  ( 0.000000000000000000, -1.000000000000000000, 0.000000000000000000 ) ) ;
#40962=CARTESIAN_POINT ( 'NONE',  ( -11.90928090972364295, -77.96396755025240566, -1.649882979053847176 ) ) ;
#40965=CARTESIAN_POINT ( 'NONE',  ( -12.43421868118999818, -17.56340276631999942, 1.197355605037999871 ) ) ;
#40966=CARTESIAN_POINT ( 'NONE',  ( -8.838834764832000701, -55.54999999966999980, 8.838834764832000701 ) ) ;
#40967=CARTESIAN_POINT ( 'NONE',  ( 1.886823409076000102, -23.76319684362000118, 12.68610076205999881 ) ) ;
#40970=CARTESIAN_POINT ( 'NONE',  ( -3.854343565295000218, -1.323241823148999963, -1.462699350379000007 ) ) ;
#40971=DIRECTION ( 'NONE',  ( 1.000000000000000000, 0.000000000000000000, 0.000000000000000000 ) ) ;
#40972=CARTESIAN_POINT ( 'NONE',  ( 10.42272502865000128, -57.04546192861999998, 7.691893942748999180 ) ) ;
#40975=FACE_OUTER_BOUND ( 'NONE', #32575, .T. ) ;
#40976=CARTESIAN_POINT ( 'NONE',  ( 3.481642061040000069, -3.298138707841000272, 0.1645893813865000055 ) ) ;
#40979=CARTESIAN_POINT ( 'NONE',  ( 7.954951288349001004, -23.25000000000000000, 9.722718241315000398 ) ) ;
#40990=CARTESIAN_POINT ( 'NONE',  ( 1.750000000000000000, -60.04999999725999515, 12.50000000000000000 ) ) ;
#40991=DIRECTION ( 'NONE',  ( 0.000000000000000000, 0.000000000000000000, -1.000000000000000000 ) ) ;
#40992=CARTESIAN_POINT ( 'NONE',  ( -3.250880417296999614, -77.15131824283000128, 12.21627067396000044 ) ) ;
#40994=CARTESIAN_POINT ( 'NONE',  ( -8.060180465563279384, -61.42064870639099894, 9.621709427725253505 ) ) ;
#40999=CARTESIAN_POINT ( 'NONE',  ( 1.750000000000000000, -55.54999999966999980, -12.00000000000000000 ) ) ;
#41001=CARTESIAN_POINT ( 'NONE',  ( -12.64500484464999808, -59.57152778012000027, -1.799490225533999732 ) ) ;
#41003=FACE_OUTER_BOUND ( 'NONE', #25824, .T. ) ;
#41006=CARTESIAN_POINT ( 'NONE',  ( 0.000000000000000000, -4.000000000000000000, 0.000000000000000000 ) ) ;
#41012=ORIENTED_EDGE ( 'NONE', *, *, #6138, .T. ) ;
#41013=CARTESIAN_POINT ( 'NONE',  ( -7.836763323982935958, -54.49488832206737499, 9.850488778788085042 ) ) ;
#41020=CARTESIAN_POINT ( 'NONE',  ( 12.47598273373999866, -77.80972615780000012, -3.494640443823999743 ) ) ;
#41024=CARTESIAN_POINT ( 'NONE',  ( -1.749899258077674435, -23.38716848763002076, 12.55433901290729182 ) ) ;
#41025=ORIENTED_EDGE ( 'NONE', *, *, #18621, .F. ) ;
#41027=CARTESIAN_POINT ( 'NONE',  ( -1.771468677314999907, -75.93849150267999448, 12.18184739844999953 ) ) ;
#41029=B_SPLINE_SURFACE_WITH_KNOTS ( 'NONE', 3, 3, ( 
 ( #27103, #17376, #30649, #40402 ),
 ( #21799, #53106, #22689, #48972 ),
 ( #44533, #13529, #4691, #27239 ),
 ( #53991, #12934, #4391, #30359 ),
 ( #40701, #39521, #17974, #18273 ),
 ( #53693, #36265, #48400, #13231 ),
 ( #8815, #8513, #12655, #22391 ),
 ( #7937, #44245, #35966, #17087 ),
 ( #25939, #43964, #8227, #3514 ),
 ( #57526, #21515, #35070, #48683 ),
 ( #26229, #39804, #35363, #30932 ) ),
 .UNSPECIFIED., .F., .F., .F.,
 ( 4, 1, 1, 1, 1, 1, 1, 1, 4 ),
 ( 4, 4 ),
 ( -0.02001474922155999786, 0.000000000000000000, 0.1666666666667000196, 0.3333333333333000081, 0.5000000000000000000, 0.6666666666667000474, 0.8333333333333000637, 1.000000000000000000, 1.020283381528000133 ),
 ( -0.3582002740325999635, 1.358862457854000061 ),
 .UNSPECIFIED. ) ;
#41030=CARTESIAN_POINT ( 'NONE',  ( -1.839417067126238203, -1.930490702502749345, -3.003034272496980961 ) ) ;
#41031=CARTESIAN_POINT ( 'NONE',  ( 8.227501432806000992, -61.62538814575999879, -9.516269855012000178 ) ) ;
#41032=CARTESIAN_POINT ( 'NONE',  ( 2.624826629463999694, -78.87516843985000037, 11.97953966613999910 ) ) ;
#41034=CARTESIAN_POINT ( 'NONE',  ( -1.750000000001000089, -22.75100836360999779, 12.60354432389999957 ) ) ;
#41037=CARTESIAN_POINT ( 'NONE',  ( 8.051245500302858460, -77.36714086066730545, 9.061184720839335682 ) ) ;
#41039=ADVANCED_FACE ( 'NONE', ( #51381 ), #35172, .F. ) ;
#41041=ORIENTED_EDGE ( 'NONE', *, *, #49593, .F. ) ;
#41043=CIRCLE ( 'NONE', #17473, 14.00000000000000000 ) ;
#41052=CARTESIAN_POINT ( 'NONE',  ( 0.8678127655509034755, -76.06901340928149580, 11.71984293853029691 ) ) ;
#41055=EDGE_LOOP ( 'NONE', ( #6183, #32469, #51899, #24053 ) ) ;
#41056=CARTESIAN_POINT ( 'NONE',  ( 12.21199139565999481, -76.31004809983465975, 1.550091862394999298 ) ) ;
#41060=CARTESIAN_POINT ( 'NONE',  ( -0.6454797251260506741, -17.11193487860159479, -12.50471521368209871 ) ) ;
#41063=CARTESIAN_POINT ( 'NONE',  ( 7.647094085193999469, -18.63104695440999947, -10.00844048070000092 ) ) ;
#41064=CARTESIAN_POINT ( 'NONE',  ( 9.298479816476996618, -17.11187382770974352, 8.385858173856171049 ) ) ;
#41065=ORIENTED_EDGE ( 'NONE', *, *, #47000, .F. ) ;
#41067=DIRECTION ( 'NONE',  ( 0.000000000000000000, -1.000000000000000000, -5.033011044969999542E-14 ) ) ;
#41070=CARTESIAN_POINT ( 'NONE',  ( 11.34395419804827299, -76.42888099978775074, -3.068742979946195160 ) ) ;
#41072=CARTESIAN_POINT ( 'NONE',  ( -12.50386430447168351, -54.01495396579433361, -0.8574436029508151202 ) ) ;
#41073=LINE ( 'NONE', #28058, #46900 ) ;
#41074=FACE_OUTER_BOUND ( 'NONE', #54173, .T. ) ;
#41077=DIRECTION ( 'NONE',  ( -0.7071067811865474617, 0.000000000000000000, 0.7071067811865474617 ) ) ;
#41079=EDGE_LOOP ( 'NONE', ( #25958, #43311, #44415, #11630 ) ) ;
#41081=DIRECTION ( 'NONE',  ( -0.7071067811865475727, 0.000000000000000000, -0.7071067811865475727 ) ) ;
#41082=VERTEX_POINT ( 'NONE', #32461 ) ;
#41084=CARTESIAN_POINT ( 'NONE',  ( 7.758655887903000092, -24.15078616243999932, 9.996711280983999970 ) ) ;
#41086=CARTESIAN_POINT ( 'NONE',  ( 9.029867227928999540, -62.13262194258000193, 9.038867509651000276 ) ) ;
#41087=CARTESIAN_POINT ( 'NONE',  ( 0.000000000000000000, -18.75000000000000000, 12.50000000000000000 ) ) ;
#41088=ADVANCED_FACE ( 'NONE', ( #1793 ), #42516, .F. ) ;
#41094=ORIENTED_EDGE ( 'NONE', *, *, #13103, .F. ) ;
#41097=DIRECTION ( 'NONE',  ( 0.7071067811865474617, 0.000000000000000000, -0.7071067811865474617 ) ) ;
#41099=CARTESIAN_POINT ( 'NONE',  ( -2.177178839649999809, -75.72006215493000525, 12.62074446832999897 ) ) ;
#41104=CARTESIAN_POINT ( 'NONE',  ( -8.790688707546999936, -24.93813493249999880, -8.797962936834998970 ) ) ;
#41105=EDGE_CURVE ( 'NONE', #19974, #17032, #19197, .T. ) ;
#41106=CARTESIAN_POINT ( 'NONE',  ( -7.666647577129732660, -60.55042584425837049, 7.889735440113262221 ) ) ;
#41108=ORIENTED_EDGE ( 'NONE', *, *, #3721, .F. ) ;
#41113=CARTESIAN_POINT ( 'NONE',  ( -12.70253258979055389, -61.77063167632906726, 0.9890392131111367391 ) ) ;
#41114=DIRECTION ( 'NONE',  ( 0.000000000000000000, 0.000000000000000000, 1.000000000000000000 ) ) ;
#41119=CARTESIAN_POINT ( 'NONE',  ( -9.722718241315000398, -23.44678171330999916, 7.954951288349001004 ) ) ;
#41123=CARTESIAN_POINT ( 'NONE',  ( 2.972945683522000060, -3.498054798046000169, -2.625398180863999897 ) ) ;
#41126=CARTESIAN_POINT ( 'NONE',  ( 8.652376385601000308, -25.26264602966000083, -9.414489258817999584 ) ) ;
#41130=CIRCLE ( 'NONE', #10968, 14.00000000000000000 ) ;
#41132=CARTESIAN_POINT ( 'NONE',  ( -7.686941364994000381, -20.24527982330999976, -10.48774103564000093 ) ) ;
#41133=VECTOR ( 'NONE', #10955, 1000.000000000000000 ) ;
#41134=AXIS2_PLACEMENT_3D ( 'NONE', #26367, #53840, #53539 ) ;
#41135=CARTESIAN_POINT ( 'NONE',  ( 8.870405106233999248, -53.73036971739000478, -8.878274241729000593 ) ) ;
#41136=AXIS2_PLACEMENT_3D ( 'NONE', #8074, #26070, #52665 ) ;
#41138=DIRECTION ( 'NONE',  ( 0.000000000000000000, -1.000000000000000000, 0.000000000000000000 ) ) ;
#41145=VERTEX_POINT ( 'NONE', #19790 ) ;
#41149=DIRECTION ( 'NONE',  ( -0.7026410690473250398, 0.1122098755728047209, -0.7026410690473250398 ) ) ;
#41154=DIRECTION ( 'NONE',  ( 1.000000000000000000, 0.000000000000000000, 0.000000000000000000 ) ) ;
#41156=CARTESIAN_POINT ( 'NONE',  ( -1.929975092517999924, -18.79892743736000327, 12.72537404210999945 ) ) ;
#41161=CARTESIAN_POINT ( 'NONE',  ( -7.638406141627999801, -78.40188750088999825, -9.335002989230998693 ) ) ;
#41163=EDGE_CURVE ( 'NONE', #43521, #18438, #1419, .T. ) ;
#41166=CARTESIAN_POINT ( 'NONE',  ( -12.56594317991999965, -60.04999999381999487, -1.750000000001000089 ) ) ;
#41169=CARTESIAN_POINT ( 'NONE',  ( 0.000000000000000000, -2.900000000000000355, 0.000000000000000000 ) ) ;
#41172=CARTESIAN_POINT ( 'NONE',  ( -10.07722254369999959, -20.25199022618999933, 7.718368845809999712 ) ) ;
#41174=CARTESIAN_POINT ( 'NONE',  ( -10.38133291898000188, -77.78174472164999997, 7.485792156039000389 ) ) ;
#41178=AXIS2_PLACEMENT_3D ( 'NONE', #4961, #27383, #32386 ) ;
#41179=CARTESIAN_POINT ( 'NONE',  ( 0.000000000000000000, -18.84999999999999787, -12.00000000000000000 ) ) ;
#41181=TOROIDAL_SURFACE ( 'NONE', #46857, 13.50000000000000000, 0.5000000000000000000 ) ;
#41187=LINE ( 'NONE', #27011, #761 ) ;
#41188=CARTESIAN_POINT ( 'NONE',  ( 12.00000000000000000, -79.25000000000000000, 1.072514965728000067E-08 ) ) ;
#41189=CARTESIAN_POINT ( 'NONE',  ( 1.781953555039999859, -3.015773310596999934, -3.363141973650999983 ) ) ;
#41192=DIRECTION ( 'NONE',  ( 0.000000000000000000, -1.000000000000000000, 0.000000000000000000 ) ) ;
#41193=CARTESIAN_POINT ( 'NONE',  ( 8.171144579307879852, -60.14010097496868212, -7.364280830342240236 ) ) ;
#41196=CARTESIAN_POINT ( 'NONE',  ( -9.234979314279001983, -77.07954422446000819, -9.168119495123999485 ) ) ;
#41204=CARTESIAN_POINT ( 'NONE',  ( 7.653559626096999580, -23.29848884437999956, -10.01235002622999914 ) ) ;
#41207=CARTESIAN_POINT ( 'NONE',  ( -1.182840957218999955, -1.383876846447999798, -3.838043326965000279 ) ) ;
#41208=CARTESIAN_POINT ( 'NONE',  ( -1.799475295154000065, -58.55083378327000077, -12.69619287811999797 ) ) ;
#41213=DIRECTION ( 'NONE',  ( -1.000000000000000000, -6.386283326366000088E-09, -1.411440692003999935E-10 ) ) ;
#41215=CONICAL_SURFACE ( 'NONE', #35400, 0.6999999997694995590, 0.7853981633972997312 ) ;
#41216=ORIENTED_EDGE ( 'NONE', *, *, #4006, .T. ) ;
#41219=LINE ( 'NONE', #808, #57687 ) ;
#41221=EDGE_LOOP ( 'NONE', ( #31415, #22327, #56677, #25759 ) ) ;
#41225=ORIENTED_EDGE ( 'NONE', *, *, #40532, .T. ) ;
#41226=CARTESIAN_POINT ( 'NONE',  ( -2.991231916151877002, -2.632707418491854856, -1.269656187733815056 ) ) ;
#41229=EDGE_LOOP ( 'NONE', ( #34517, #41953, #49364, #8692, #46838 ) ) ;
#41233=CARTESIAN_POINT ( 'NONE',  ( 1.618935784642568265, -18.07248831326923977, 12.52134385800272121 ) ) ;
#41235=DIRECTION ( 'NONE',  ( 0.9936845293270585300, -0.1122098755727947705, 0.000000000000000000 ) ) ;
#41237=CARTESIAN_POINT ( 'NONE',  ( -13.63885489310999510, -19.21421830981000056, 7.254376133916000668 ) ) ;
#41240=CARTESIAN_POINT ( 'NONE',  ( -3.250000000000000000, -3.000000000000000000, 0.000000000000000000 ) ) ;
#41241=CARTESIAN_POINT ( 'NONE',  ( -7.641012305241000391, -60.08917723397000543, -10.18589226633000067 ) ) ;
#41244=CARTESIAN_POINT ( 'NONE',  ( 10.43984081968398492, -76.48826064512984146, 5.458517345968248335 ) ) ;
#41245=CARTESIAN_POINT ( 'NONE',  ( 0.5705388283887262713, -23.34010097528690508, -10.98520465578131677 ) ) ;
#41249=CARTESIAN_POINT ( 'NONE',  ( 11.55970134427844975, -78.22637299551007573, 3.502838489863109750 ) ) ;
#41255=CARTESIAN_POINT ( 'NONE',  ( -1.933504092460000212, -23.40406847274999791, 12.70940235707999832 ) ) ;
#41258=CARTESIAN_POINT ( 'NONE',  ( 3.784441966891999964, -1.714444768728000001, -0.1949150922344000114 ) ) ;
#41262=CARTESIAN_POINT ( 'NONE',  ( 10.24998526315000014, -58.55083378327000077, 7.705142895592000052 ) ) ;
#41264=CARTESIAN_POINT ( 'NONE',  ( -0.5999999999999999778, -18.84999999999000053, -11.79999999999999893 ) ) ;
#41266=CARTESIAN_POINT ( 'NONE',  ( -3.398324506668000122, -2.562221200086999939, -0.7749863891880000022 ) ) ;
#41268=FACE_OUTER_BOUND ( 'NONE', #14214, .T. ) ;
#41270=LINE ( 'NONE', #8800, #38303 ) ;
#41278=DIRECTION ( 'NONE',  ( 0.000000000000000000, -1.000000000000000000, 0.000000000000000000 ) ) ;
#41280=CARTESIAN_POINT ( 'NONE',  ( -1.228039281160999918, -77.87287857533000590, -12.58161828305999919 ) ) ;
#41283=ORIENTED_EDGE ( 'NONE', *, *, #7759, .T. ) ;
#41285=CARTESIAN_POINT ( 'NONE',  ( 1.930860503447785925, -55.02582494032501614, -12.72930866328045418 ) ) ;
#41286=CARTESIAN_POINT ( 'NONE',  ( -7.919595949288999570, -59.94999999969000015, -8.768124086712999699 ) ) ;
#41287=CARTESIAN_POINT ( 'NONE',  ( -2.753235971857820097, -75.80574547360328097, -11.46018561868001306 ) ) ;
#41288=ADVANCED_FACE ( 'NONE', ( #25582 ), #29427, .F. ) ;
#41290=CARTESIAN_POINT ( 'NONE',  ( -12.50386430450149433, -17.21495396633332575, -0.8574436033227620380 ) ) ;
#41291=B_SPLINE_CURVE_WITH_KNOTS ( 'NONE', 3,
 ( #19086, #55092, #39407, #34956, #43266, #25823, #56549, #16110 ),
 .UNSPECIFIED., .F., .F.,
 ( 4, 2, 2, 4 ),
 ( 0.000000000000000000, 0.4999999999999996669, 0.7499999999999997780, 1.000000000000000000 ),
 .UNSPECIFIED. ) ;
#41292=DIRECTION ( 'NONE',  ( 0.9936845293270585300, 0.1122098755727947705, 0.000000000000000000 ) ) ;
#41296=CARTESIAN_POINT ( 'NONE',  ( -1.931087888049999979, -18.68415522710999710, 12.71658889741000031 ) ) ;
#41297=ORIENTED_EDGE ( 'NONE', *, *, #30759, .F. ) ;
#41298=ORIENTED_EDGE ( 'NONE', *, *, #6663, .T. ) ;
#41301=VERTEX_POINT ( 'NONE', #17020 ) ;
#41302=DIRECTION ( 'NONE',  ( -0.7071067811865474617, 0.000000000000000000, -0.7071067811865474617 ) ) ;
#41303=CARTESIAN_POINT ( 'NONE',  ( 9.175573575508092716, -25.22695822358256024, -8.792784719773246493 ) ) ;
#41307=CARTESIAN_POINT ( 'NONE',  ( 0.000000000000000000, -52.69905023022000279, 0.000000000000000000 ) ) ;
#41309=CARTESIAN_POINT ( 'NONE',  ( 10.36597025940959327, -18.22476146848570977, -7.635927901519359295 ) ) ;
#41318=CARTESIAN_POINT ( 'NONE',  ( -6.024415200221000077, -76.39836206569999888, 10.73507988388000101 ) ) ;
#41321=CARTESIAN_POINT ( 'NONE',  ( 1.062462549644097143, -1.998698511921152665, -3.356897962585378092 ) ) ;
#41322=CARTESIAN_POINT ( 'NONE',  ( 12.71798280854999952, -18.70221404512000163, 1.931086388455000025 ) ) ;
#41323=CARTESIAN_POINT ( 'NONE',  ( 3.086017585447000222, -79.16257562062001796, -11.86910201801999953 ) ) ;
#41325=CARTESIAN_POINT ( 'NONE',  ( -10.18499221075000172, -58.54977139891999371, -7.710118476601000026 ) ) ;
#41327=CARTESIAN_POINT ( 'NONE',  ( 3.018310159408800875, -2.820852371859394747, -1.203481977088054489 ) ) ;
#41328=DIRECTION ( 'NONE',  ( -0.7071067811865475727, 0.000000000000000000, 0.7071067811865475727 ) ) ;
#41329=CARTESIAN_POINT ( 'NONE',  ( -10.10912542009497983, -18.52413588830296476, 7.634643956514072904 ) ) ;
#41341=EDGE_CURVE ( 'NONE', #1253, #30942, #26714, .T. ) ;
#41342=CARTESIAN_POINT ( 'NONE',  ( 9.089779753456481259, -76.00420051561397372, 7.445294846272284772 ) ) ;
#41347=EDGE_CURVE ( 'NONE', #3955, #8688, #51890, .T. ) ;
#41349=CARTESIAN_POINT ( 'NONE',  ( -13.86363636363000218, -46.43897132165000130, -1.277887489420000009E-05 ) ) ;
#41353=DIRECTION ( 'NONE',  ( 0.000000000000000000, 1.000000000000000000, 0.000000000000000000 ) ) ;
#41354=CARTESIAN_POINT ( 'NONE',  ( 10.15323015673999940, -17.76919784905000199, -7.760928569209999850 ) ) ;
#41355=LINE ( 'NONE', #9769, #42836 ) ;
#41358=DIRECTION ( 'NONE',  ( -1.000000000000000000, 0.000000000000000000, 0.000000000000000000 ) ) ;
#41361=CARTESIAN_POINT ( 'NONE',  ( -5.471496541426451365, -76.86542272010237298, 10.76143312585065459 ) ) ;
#41362=EDGE_CURVE ( 'NONE', #4024, #38980, #7005, .T. ) ;
#41365=CARTESIAN_POINT ( 'NONE',  ( -12.50659830543690099, -53.82653383338065112, -0.3508384617699890073 ) ) ;
#41366=CARTESIAN_POINT ( 'NONE',  ( -7.958763980599000476, -17.52301961032999955, -9.723170659105999647 ) ) ;
#41367=DIRECTION ( 'NONE',  ( -0.9999999999998321343, 0.000000000000000000, -5.794540613806191565E-07 ) ) ;
#41370=EDGE_CURVE ( 'NONE', #34387, #50040, #23865, .T. ) ;
#41373=ORIENTED_EDGE ( 'NONE', *, *, #34354, .F. ) ;
#41376=EDGE_LOOP ( 'NONE', ( #7642, #41387, #47843, #26109, #46229, #29564 ) ) ;
#41380=CARTESIAN_POINT ( 'NONE',  ( 10.18114973714999927, -60.19009320380000361, 7.633087466122999487 ) ) ;
#41381=DIRECTION ( 'NONE',  ( 0.5721800012456795814, 0.8201280669349721997, 0.000000000000000000 ) ) ;
#41384=CARTESIAN_POINT ( 'NONE',  ( 2.883152686262326458, -1.811972400245676962, -1.558099060999823537 ) ) ;
#41387=ORIENTED_EDGE ( 'NONE', *, *, #37975, .F. ) ;
#41393=CIRCLE ( 'NONE', #52691, 12.57042253521000141 ) ;
#41396=DIRECTION ( 'NONE',  ( 0.000000000000000000, 1.000000000000000000, 0.000000000000000000 ) ) ;
#41398=CARTESIAN_POINT ( 'NONE',  ( 2.062597299672999540, -59.58485473249000108, -12.87022657274000004 ) ) ;
#41400=CARTESIAN_POINT ( 'NONE',  ( 12.71798269383000068, -55.50221245779999890, -1.931086388578000079 ) ) ;
#41402=VERTEX_POINT ( 'NONE', #24725 ) ;
#41403=DIRECTION ( 'NONE',  ( -0.7071067811865475727, 0.000000000000000000, 0.7071067811865475727 ) ) ;
#41407=CARTESIAN_POINT ( 'NONE',  ( -10.31444587878999997, -17.69924218095000157, 7.758886158107999975 ) ) ;
#41408=DIRECTION ( 'NONE',  ( -1.000000000000000000, 0.000000000000000000, 0.000000000000000000 ) ) ;
#41409=DIRECTION ( 'NONE',  ( 0.7071067811865475727, 0.000000000000000000, 0.7071067811865475727 ) ) ;
#41410=CARTESIAN_POINT ( 'NONE',  ( 2.537261334626276010, -2.939104093472465706, -2.439294570458690803 ) ) ;
#41418=CARTESIAN_POINT ( 'NONE',  ( 2.712110641633999730, -3.620707716005000076, 2.894388207016999726 ) ) ;
#41422=CARTESIAN_POINT ( 'NONE',  ( 8.798028344861998917, -24.93813495683999903, -8.790623041439999952 ) ) ;
#41423=DIRECTION ( 'NONE',  ( -0.07798810159653808693, 0.04890177473153878990, 0.9957542229071758566 ) ) ;
#41424=CARTESIAN_POINT ( 'NONE',  ( -1.749722766158645193, -23.47588992886881343, -12.54673760678556782 ) ) ;
#41427=VECTOR ( 'NONE', #30549, 999.9999999999998863 ) ;
#41428=CARTESIAN_POINT ( 'NONE',  ( -10.48771805367000098, -20.24439828562999821, -7.686918321060999482 ) ) ;
#41430=CARTESIAN_POINT ( 'NONE',  ( 10.01676221090000141, -55.59058563439999290, -7.658899961832999814 ) ) ;
#41436=B_SPLINE_CURVE_WITH_KNOTS ( 'NONE', 3,
 ( #46358, #5882, #5309, #41325, #23890, #2350 ),
 .UNSPECIFIED., .F., .F.,
 ( 4, 1, 1, 4 ),
 ( 0.000000000000000000, 0.3333333333333000081, 0.6666666666667000474, 1.000000000000000000 ),
 .UNSPECIFIED. ) ;
#41440=VECTOR ( 'NONE', #45617, 1000.000000000000000 ) ;
#41441=EDGE_LOOP ( 'NONE', ( #28277, #48503, #47642, #49743, #55249, #6866 ) ) ;
#41442=CARTESIAN_POINT ( 'NONE',  ( -1.624989163556999772E-14, -74.80000000000001137, -11.19999999999998863 ) ) ;
#41443=EDGE_CURVE ( 'NONE', #50397, #4032, #47223, .T. ) ;
#41445=LINE ( 'NONE', #1029, #1670 ) ;
#41447=VERTEX_POINT ( 'NONE', #40625 ) ;
#41451=DIRECTION ( 'NONE',  ( 0.7071067811865475727, 0.000000000000000000, -0.7071067811865475727 ) ) ;
#41457=ORIENTED_EDGE ( 'NONE', *, *, #45118, .F. ) ;
#41458=VERTEX_POINT ( 'NONE', #13153 ) ;
#41459=CARTESIAN_POINT ( 'NONE',  ( -12.50686284816388749, -17.69510763146807264, -1.423064270789318631 ) ) ;
#41462=CARTESIAN_POINT ( 'NONE',  ( -0.5135400118900182997, -61.97868533827725912, -12.70453250103373044 ) ) ;
#41466=CARTESIAN_POINT ( 'NONE',  ( 7.379132703266000348, -77.09176059790999602, -10.64946278274999969 ) ) ;
#41468=FACE_OUTER_BOUND ( 'NONE', #58149, .T. ) ;
#41472=AXIS2_PLACEMENT_3D ( 'NONE', #6651, #42089, #33506 ) ;
#41474=CARTESIAN_POINT ( 'NONE',  ( 3.000494659939939801, -2.882409298795182373, 1.247127308777857824 ) ) ;
#41478=DIRECTION ( 'NONE',  ( 1.000000000000000000, 0.000000000000000000, 0.000000000000000000 ) ) ;
#41481=ORIENTED_EDGE ( 'NONE', *, *, #46522, .T. ) ;
#41483=CARTESIAN_POINT ( 'NONE',  ( 7.997114030225745296, -60.48581381149598002, -7.553727747507254620 ) ) ;
#41484=DIRECTION ( 'NONE',  ( 0.000000000000000000, -1.000000000000000000, 0.000000000000000000 ) ) ;
#41486=CARTESIAN_POINT ( 'NONE',  ( 5.579996517577999526, -77.28773409592999144, 11.75597208960999929 ) ) ;
#41489=CARTESIAN_POINT ( 'NONE',  ( 9.685201957684167695, -78.49578785308447948, 6.650675367548727124 ) ) ;
#41493=CIRCLE ( 'NONE', #19804, 4.999999999999996447 ) ;
#41494=EDGE_CURVE ( 'NONE', #28795, #15888, #31449, .T. ) ;
#41495=CARTESIAN_POINT ( 'NONE',  ( -4.165135875058396664, -76.29562521202450398, -10.99247644781376287 ) ) ;
#41497=CARTESIAN_POINT ( 'NONE',  ( 7.654537165468999760, -23.28056535155999995, -10.01332852689000141 ) ) ;
#41500=CARTESIAN_POINT ( 'NONE',  ( -1.180494763713999973, -0.7538550533857000246, 3.461421590595000097 ) ) ;
#41502=CARTESIAN_POINT ( 'NONE',  ( 0.000000000000000000, -0.1000000007601000024, 0.000000000000000000 ) ) ;
#41505=CYLINDRICAL_SURFACE ( 'NONE', #9669, 0.5999999999999999778 ) ;
#41508=EDGE_LOOP ( 'NONE', ( #14339, #11538, #2766, #1170 ) ) ;
#41510=FACE_OUTER_BOUND ( 'NONE', #24820, .T. ) ;
#41513=ORIENTED_EDGE ( 'NONE', *, *, #52861, .F. ) ;
#41516=VERTEX_POINT ( 'NONE', #54209 ) ;
#41517=CONICAL_SURFACE ( 'NONE', #56610, 12.74999999937999995, 0.7853981633972997312 ) ;
#41518=VECTOR ( 'NONE', #38580, 1000.000000000000000 ) ;
#41522=ORIENTED_EDGE ( 'NONE', *, *, #3805, .F. ) ;
#41524=ORIENTED_EDGE ( 'NONE', *, *, #45970, .T. ) ;
#41528=CARTESIAN_POINT ( 'NONE',  ( 12.50000000000000000, -23.25000000000000000, 1.250000000000000000 ) ) ;
#41529=LINE ( 'NONE', #39551, #43787 ) ;
#41532=CARTESIAN_POINT ( 'NONE',  ( -7.958776492183998741, -24.47699850274999989, 9.723157982400998378 ) ) ;
#41535=CARTESIAN_POINT ( 'NONE',  ( 7.472976412552629455, -76.51966548243302668, 9.068880097928863293 ) ) ;
#41537=CARTESIAN_POINT ( 'NONE',  ( -12.76303204525000012, -60.06485147653999945, -1.980584515753000208 ) ) ;
#41540=CARTESIAN_POINT ( 'NONE',  ( -6.771615370240408716, -78.03068079904456056, -9.996688553910448860 ) ) ;
#41542=EDGE_CURVE ( 'NONE', #50457, #32490, #35586, .T. ) ;
#41543=CARTESIAN_POINT ( 'NONE',  ( -12.66761570929000058, -17.77632520104999969, 1.696752301450999978 ) ) ;
#41546=CARTESIAN_POINT ( 'NONE',  ( -12.69999999929000012, 7.141125103605999188E-10, -6.699862062809000450E-09 ) ) ;
#41548=CARTESIAN_POINT ( 'NONE',  ( -10.35398566683000077, -60.20788276206999967, -7.619388279096000360 ) ) ;
#41549=DIRECTION ( 'NONE',  ( 1.000000000000000000, 0.000000000000000000, 0.000000000000000000 ) ) ;
#41551=CIRCLE ( 'NONE', #36951, 1.750000000000000444 ) ;
#41553=CARTESIAN_POINT ( 'NONE',  ( 12.51072239526000196, -15.69705297114000331, 0.7871079366006996647 ) ) ;
#41554=CARTESIAN_POINT ( 'NONE',  ( 12.68703394091000014, -23.75066116476999767, 1.889962945498999902 ) ) ;
#41557=CARTESIAN_POINT ( 'NONE',  ( -1.980584515756000030, -55.53514849873000259, 12.76303204337999908 ) ) ;
#41559=CARTESIAN_POINT ( 'NONE',  ( -1.575772165402021807, -24.46154542800653431, -12.70597445617581478 ) ) ;
#41560=CARTESIAN_POINT ( 'NONE',  ( 6.559616885195999281, -75.99841620946999399, 10.30072712123999956 ) ) ;
#41561=EDGE_LOOP ( 'NONE', ( #37379, #41957, #44198, #33378 ) ) ;
#41562=B_SPLINE_SURFACE_WITH_KNOTS ( 'NONE', 3, 3, ( 
 ( #27956, #23256, #46881, #7218, #40976, #54841, #37114, #55129, #567, #54561, #46299, #14102, #45715, #5251, #14674, #5824, #41266, #18834, #14384, #32384, #32671, #23831, #50724, #10265, #41847, #1425, #34353, #43238, #48823, #25508, #3934, #53535, #17516, #12508, #3086 ),
 ( #21936, #53242, #52391, #30790, #57666, #21081, #26363, #43823, #38795, #8081, #25796, #57387, #39087, #17223, #35212, #25218, #57093, #12791, #29922, #39661, #8364, #44382, #16662, #20792, #39947, #11945, #57962, #35507, #13076, #12224, #31073, #2795, #49112, #56815, #16372 ),
 ( #47972, #21365, #7509, #43525, #30214, #34643, #52959, #52671, #48260, #39381, #30507, #7795, #3370, #34927, #16946, #48535, #26078, #44102, #3652, #21654, #35806, #40835, #13667, #36110, #9254, #18695, #430, #13371, #23408, #31957, #40246, #9547, #36979, #8961, #54704 ),
 ( #49413, #44979, #44684, #41418, #26946, #41123, #49709, #5119, #45867, #54992, #717, #1002, #45277, #31663, #31368, #14541, #4534, #5400, #23116, #27238, #36689, #22534, #4236, #18987, #53836, #32534, #8661, #32244, #54126, #26647, #22234, #27820, #58259, #17819, #40544 ) ),
 .UNSPECIFIED., .F., .F., .F.,
 ( 4, 4 ),
 ( 4, 1, 1, 1, 1, 1, 1, 1, 1, 1, 1, 1, 1, 1, 1, 1, 1, 1, 1, 1, 1, 1, 1, 1, 1, 1, 1, 1, 1, 1, 1, 1, 4 ),
 ( -0.3708084972812999980, 1.370808497280999960 ),
 ( 0.03450073181895999680, 0.06526418889335999785, 0.09602764596774999994, 0.1267911030420999785, 0.1575545601164999865, 0.1883180171909000222, 0.2190814742653000025, 0.2498449313396999827, 0.2806083884140999629, 0.3113718454884999987, 0.3421353025628999789, 0.3728987596373000146, 0.4036622167116999949, 0.4344256737861000306, 0.4651891308605000108, 0.4959525879348999911, 0.5267160450093000268, 0.5574795020837000070, 0.5882429591580999872, 0.6190064162324999675, 0.6497698733068999477, 0.6805333303813000390, 0.7112967874557000192, 0.7420602445300999994, 0.7728237016044999796, 0.8035871586789000709, 0.8343506157532999401, 0.8651140728276000003, 0.8958775299019999805, 0.9266409869763999607, 0.9574044440508000520, 0.9881679011251999212, 1.018931358199999915 ),
 .UNSPECIFIED. ) ;
#41565=ADVANCED_FACE ( 'NONE', ( #31147 ), #18198, .F. ) ;
#41567=CARTESIAN_POINT ( 'NONE',  ( -4.559477187396880460, -76.29284459774818572, -10.82903768629202013 ) ) ;
#41570=DIRECTION ( 'NONE',  ( 0.7071067811865475727, 0.000000000000000000, 0.7071067811865475727 ) ) ;
#41572=CARTESIAN_POINT ( 'NONE',  ( -2.958306647813000012, -1.246290208250999898, 2.731603797012999824 ) ) ;
#41573=DIRECTION ( 'NONE',  ( 0.000000000000000000, 0.000000000000000000, 1.000000000000000000 ) ) ;
#41575=ORIENTED_EDGE ( 'NONE', *, *, #11187, .T. ) ;
#41579=ORIENTED_EDGE ( 'NONE', *, *, #32965, .F. ) ;
#41580=EDGE_CURVE ( 'NONE', #30569, #33154, #40859, .T. ) ;
#41581=CARTESIAN_POINT ( 'NONE',  ( 3.250000000000000000, -1.750000000000000000, 0.000000000000000000 ) ) ;
#41583=AXIS2_PLACEMENT_3D ( 'NONE', #33585, #42465, #32701 ) ;
#41589=VERTEX_POINT ( 'NONE', #17900 ) ;
#41591=CARTESIAN_POINT ( 'NONE',  ( -10.01752115540999988, -55.60828330164999755, -7.660412752583999563 ) ) ;
#41594=CARTESIAN_POINT ( 'NONE',  ( 12.55458938217999965, -54.63720883353000346, 1.575070636625000242 ) ) ;
#41596=AXIS2_PLACEMENT_3D ( 'NONE', #32491, #14205, #27779 ) ;
#41597=FACE_OUTER_BOUND ( 'NONE', #30309, .T. ) ;
#41605=CARTESIAN_POINT ( 'NONE',  ( -1.001315002179000047, -24.68522411714000242, 12.50000000000000000 ) ) ;
#41607=CARTESIAN_POINT ( 'NONE',  ( 12.21199139566000014, -76.27738052755999831, 1.550091862394999964 ) ) ;
#41608=ADVANCED_FACE ( 'NONE', ( #26161 ), #40917, .F. ) ;
#41609=LINE ( 'NONE', #55781, #9706 ) ;
#41610=CARTESIAN_POINT ( 'NONE',  ( 7.636246406707999590, -60.56323123069000047, -10.30460653227000023 ) ) ;
#41611=CARTESIAN_POINT ( 'NONE',  ( 0.4482635754052999855, -78.64524269524000033, -12.25553529036999834 ) ) ;
#41615=CARTESIAN_POINT ( 'NONE',  ( 12.50745077490000057, -24.99994448286999926, 2.662071812989000278E-09 ) ) ;
#41616=CARTESIAN_POINT ( 'NONE',  ( -11.26810403927533244, -78.02092148738429955, 4.317468151549603839 ) ) ;
#41617=FACE_OUTER_BOUND ( 'NONE', #46701, .T. ) ;
#41620=EDGE_LOOP ( 'NONE', ( #43383, #56975, #2665, #32532, #28791, #2747 ) ) ;
#41623=CARTESIAN_POINT ( 'NONE',  ( 10.10713367717059796, -24.46653151341558896, 7.860990029285546576 ) ) ;
#41625=CARTESIAN_POINT ( 'NONE',  ( -2.132401835864000006, -3.457796016549000040, -3.041072444219000470 ) ) ;
#41628=CARTESIAN_POINT ( 'NONE',  ( 4.220281262689746349, -76.04518811977419546, 10.96961518909428435 ) ) ;
#41631=EDGE_LOOP ( 'NONE', ( #11106, #25831, #6882, #13752, #52061, #6948 ) ) ;
#41632=CARTESIAN_POINT ( 'NONE',  ( 7.648026768024999811, -18.75000001589999954, -10.12290050218000026 ) ) ;
#41633=CARTESIAN_POINT ( 'NONE',  ( 11.89593388229870463, -79.14596860729264449, 1.243669055771579046 ) ) ;
#41634=DIRECTION ( 'NONE',  ( 0.000000000000000000, 1.000000000000000000, 0.000000000000000000 ) ) ;
#41635=CARTESIAN_POINT ( 'NONE',  ( -6.536760041025257095, -76.27796683842150571, -9.763812029757714228 ) ) ;
#41636=AXIS2_PLACEMENT_3D ( 'NONE', #34979, #17277, #27585 ) ;
#41641=CARTESIAN_POINT ( 'NONE',  ( 10.47513558174000003, -18.19636614430000066, -7.624778818008999259 ) ) ;
#41642=CARTESIAN_POINT ( 'NONE',  ( -0.5999999999999999778, -18.84999999999000053, -11.79999999999999893 ) ) ;
#41643=ORIENTED_EDGE ( 'NONE', *, *, #22297, .F. ) ;
#41646=DIRECTION ( 'NONE',  ( 0.000000000000000000, -1.000000000000000000, 0.000000000000000000 ) ) ;
#41650=CARTESIAN_POINT ( 'NONE',  ( 4.591369065251983628, -77.29683506230675505, 11.11224176324230228 ) ) ;
#41653=CARTESIAN_POINT ( 'NONE',  ( -7.919595949288999570, -59.94999999040999938, 9.050966798898000931 ) ) ;
#41656=LINE ( 'NONE', #31905, #54711 ) ;
#41658=FACE_OUTER_BOUND ( 'NONE', #26749, .T. ) ;
#41659=VERTEX_POINT ( 'NONE', #31379 ) ;
#41666=ADVANCED_FACE ( 'NONE', ( #4245 ), #48545, .F. ) ;
#41668=CARTESIAN_POINT ( 'NONE',  ( 10.52682159652000138, -60.22567232035000018, 7.605689092069000345 ) ) ;
#41677=AXIS2_PLACEMENT_3D ( 'NONE', #32798, #15100, #50846 ) ;
#41678=DIRECTION ( 'NONE',  ( -1.000000000000000000, 0.000000000000000000, 0.000000000000000000 ) ) ;
#41681=CARTESIAN_POINT ( 'NONE',  ( -8.666925696772263876, -17.00708316157611577, 9.019429295400886559 ) ) ;
#41682=DIRECTION ( 'NONE',  ( 0.7071067811865475727, 0.000000000000000000, 0.7071067811865475727 ) ) ;
#41687=CARTESIAN_POINT ( 'NONE',  ( 12.70610460585974621, -61.25512899773330133, 1.580683093980798315 ) ) ;
#41691=ORIENTED_EDGE ( 'NONE', *, *, #6625, .T. ) ;
#41696=CARTESIAN_POINT ( 'NONE',  ( -7.657744736620999859, -18.33080421803999727, 9.966195456754999071 ) ) ;
#41699=CARTESIAN_POINT ( 'NONE',  ( 1.483582653850644473, -3.409532918301972249, -3.194058075009992947 ) ) ;
#41706=B_SPLINE_CURVE_WITH_KNOTS ( 'NONE', 3,
 ( #38372, #28339, #1806, #56394, #10660, #42816 ),
 .UNSPECIFIED., .F., .F.,
 ( 4, 1, 1, 4 ),
 ( 0.000000000000000000, 0.3333333333333000081, 0.6666666666667000474, 0.9999998688569559091 ),
 .UNSPECIFIED. ) ;
#41708=CARTESIAN_POINT ( 'NONE',  ( -2.061613410425999771, -60.00570014443000133, -12.83797036857999885 ) ) ;
#41712=CARTESIAN_POINT ( 'NONE',  ( -12.76303204294999993, -23.26485150694999859, 1.980584515756000030 ) ) ;
#41715=CARTESIAN_POINT ( 'NONE',  ( 9.722718241315000398, -55.54999999966999980, 7.954951288349001004 ) ) ;
#41718=CARTESIAN_POINT ( 'NONE',  ( 10.18114972180999978, -55.40990354248999950, -7.633087078966999783 ) ) ;
#41721=CARTESIAN_POINT ( 'NONE',  ( -10.42531125068999920, -23.26485145404000221, 7.624341767093000044 ) ) ;
#41731=VECTOR ( 'NONE', #2694, 1000.000000000000000 ) ;
#41734=ORIENTED_EDGE ( 'NONE', *, *, #15574, .T. ) ;
#41739=ORIENTED_EDGE ( 'NONE', *, *, #9213, .F. ) ;
#41741=AXIS2_PLACEMENT_3D ( 'NONE', #45074, #23207, #17910 ) ;
#41743=SHAPE_DEFINITION_REPRESENTATION ( #17763, #7439 ) ;
#41744=EDGE_CURVE ( 'NONE', #39513, #41458, #11965, .T. ) ;
#41746=AXIS2_PLACEMENT_3D ( 'NONE', #31289, #49629, #49334 ) ;
#41749=DIRECTION ( 'NONE',  ( -1.000000000000000000, 0.000000000000000000, 0.000000000000000000 ) ) ;
#41755=DIRECTION ( 'NONE',  ( 0.9999999924279685537, 0.000000000000000000, 0.0001230612157836962969 ) ) ;
#41757=DIRECTION ( 'NONE',  ( 1.000000000000000000, 0.000000000000000000, 0.000000000000000000 ) ) ;
#41758=CARTESIAN_POINT ( 'NONE',  ( -10.21380041493000057, -22.77152778045000048, 7.668936932623999780 ) ) ;
#41760=EDGE_CURVE ( 'NONE', #38246, #37150, #22039, .T. ) ;
#41762=CARTESIAN_POINT ( 'NONE',  ( 0.2689332326338723100, -76.57310917009351670, 11.74710904988357640 ) ) ;
#41765=AXIS2_PLACEMENT_3D ( 'NONE', #15629, #33625, #20638 ) ;
#41771=CARTESIAN_POINT ( 'NONE',  ( -12.76303204294000082, -18.73514849292999784, -1.980584515756000030 ) ) ;
#41773=CARTESIAN_POINT ( 'NONE',  ( 2.534829140202000008, -2.134334759237999979, 2.839140403360000509 ) ) ;
#41775=ORIENTED_EDGE ( 'NONE', *, *, #15217, .T. ) ;
#41776=CARTESIAN_POINT ( 'NONE',  ( -11.55514622821841542, -78.81666666666667709, -2.460715419382146774 ) ) ;
#41777=CARTESIAN_POINT ( 'NONE',  ( 8.188331488387794010, -60.02841244177609070, -7.345153731672020569 ) ) ;
#41778=CIRCLE ( 'NONE', #31378, 0.8000000000000011546 ) ;
#41779=EDGE_CURVE ( 'NONE', #10966, #27787, #5684, .T. ) ;
#41781=CARTESIAN_POINT ( 'NONE',  ( 1.667936688463999895, -56.03513569577999931, 12.53239398060000021 ) ) ;
#41782=CARTESIAN_POINT ( 'NONE',  ( 1.750000000000000000, -21.75064714178000003, -12.65372179279999898 ) ) ;
#41790=DIRECTION ( 'NONE',  ( 0.000000000000000000, 0.000000000000000000, -1.000000000000000000 ) ) ;
#41795=CARTESIAN_POINT ( 'NONE',  ( -12.04999999926000243, -79.29999999926000953, -5.384918809984000181E-09 ) ) ;
#41803=B_SPLINE_CURVE_WITH_KNOTS ( 'NONE', 3,
 ( #20889, #16184, #34453, #53343, #7604, #43335, #25604, #17325, #21751, #8184, #35311, #57480, #44202, #12041, #25319, #53055, #12608, #52485, #47784, #12888, #43627 ),
 .UNSPECIFIED., .F., .F.,
 ( 4, 2, 2, 2, 2, 2, 2, 2, 2, 1, 4 ),
 ( 0.000000000000000000, 0.1249999999999999722, 0.2499999999999999445, 0.3750000000000000000, 0.5000000000000001110, 0.5625000000000001110, 0.6250000000000001110, 0.7500000000000001110, 0.8125000000000001110, 0.8750000000000001110, 1.000000000000000000 ),
 .UNSPECIFIED. ) ;
#41805=ORIENTED_EDGE ( 'NONE', *, *, #18771, .F. ) ;
#41809=CARTESIAN_POINT ( 'NONE',  ( 7.995796640822063317, -60.48684619742046920, 7.555116226629825071 ) ) ;
#41811=AXIS2_PLACEMENT_3D ( 'NONE', #2982, #56425, #42850 ) ;
#41813=CARTESIAN_POINT ( 'NONE',  ( -12.76303204522000101, -23.26485147686999966, -1.980584515753000208 ) ) ;
#41816=CARTESIAN_POINT ( 'NONE',  ( -7.718346056121999865, -57.05111654290000445, 10.07719973194999952 ) ) ;
#41817=ORIENTED_EDGE ( 'NONE', *, *, #31153, .F. ) ;
#41821=VECTOR ( 'NONE', #32099, 1000.000000000000000 ) ;
#41822=DIRECTION ( 'NONE',  ( 0.000000000000000000, 0.000000000000000000, -1.000000000000000000 ) ) ;
#41823=CARTESIAN_POINT ( 'NONE',  ( -9.356372444455999471, -78.89426924292401111, 7.928823137711024316 ) ) ;
#41828=ADVANCED_FACE ( 'NONE', ( #27656 ), #45698, .F. ) ;
#41830=CARTESIAN_POINT ( 'NONE',  ( 7.640030264173999441, -60.10716680829000325, -10.18491080495000034 ) ) ;
#41832=EDGE_CURVE ( 'NONE', #43717, #58122, #7776, .T. ) ;
#41839=DIRECTION ( 'NONE',  ( 1.000000000000000000, 0.000000000000000000, 0.000000000000000000 ) ) ;
#41843=CARTESIAN_POINT ( 'NONE',  ( 0.000000000000000000, -49.87071424677999687, 0.000000000000000000 ) ) ;
#41845=CARTESIAN_POINT ( 'NONE',  ( 12.70395504299397693, -24.60679290123844609, -1.447100708825584947 ) ) ;
#41846=CARTESIAN_POINT ( 'NONE',  ( -1.460729357738999923, -24.09091243203000232, -12.44211643240000065 ) ) ;
#41847=CARTESIAN_POINT ( 'NONE',  ( -3.283483138947000057, -2.071609528251000309, -1.169594691854000112 ) ) ;
#41848=CARTESIAN_POINT ( 'NONE',  ( 12.70956478397999945, -23.40497526616000101, 1.933781249744999986 ) ) ;
#41851=CARTESIAN_POINT ( 'NONE',  ( -0.5999999998848000171, -18.85000000520999919, 11.79999999988000070 ) ) ;
#41852=CARTESIAN_POINT ( 'NONE',  ( -1.208267226912113079, -24.82590682154043904, -12.70228502423716854 ) ) ;
#41853=CARTESIAN_POINT ( 'NONE',  ( -6.294415428860999917, -76.25044869620001009, -10.46488830663000158 ) ) ;
#41854=( BOUNDED_SURFACE ( )  B_SPLINE_SURFACE ( 3, 3, ( 
 ( #4066, #48952, #45123, #40684 ),
 ( #26491, #57508, #17953, #276 ),
 ( #18254, #36247, #35051, #53086 ),
 ( #44515, #9094, #12640, #30632 ),
 ( #3777, #48665, #8210, #35945 ),
 ( #53972, #31503, #14971, #18545 ),
 ( #41553, #46594, #37703, #19414 ) ),
 .UNSPECIFIED., .F., .F., .F. ) 
 B_SPLINE_SURFACE_WITH_KNOTS ( ( 4, 3, 4 ),
 ( 4, 4 ),
 ( 0.000000000000000000, 1.000000000000000000, 2.000000000000000000 ),
 ( 0.000000000000000000, 1.000000000000000000 ),
 .UNSPECIFIED. ) 
 GEOMETRIC_REPRESENTATION_ITEM ( )  RATIONAL_B_SPLINE_SURFACE ( (
 ( 1.196373642248999891, 1.184225762575999985, 1.184225762575999985, 1.196373642248999891),
 ( 0.9447739570234999773, 0.9351807998836999536, 0.9351807998836999536, 0.9447739570234999773),
 ( 0.9447739570234999773, 0.9351807998836999536, 0.9351807998836999536, 0.9447739570234999773),
 ( 1.196373642248999891, 1.184225762575999985, 1.184225762575999985, 1.196373642248999891),
 ( 0.9447739570234999773, 0.9351807998836999536, 0.9351807998836999536, 0.9447739570234999773),
 ( 0.9447739570234999773, 0.9351807998836999536, 0.9351807998836999536, 0.9447739570234999773),
 ( 1.196373642248999891, 1.184225762575999985, 1.184225762575999985, 1.196373642248999891) ) ) 
 REPRESENTATION_ITEM ( '' )  SURFACE ( )  );
#41855=ORIENTED_EDGE ( 'NONE', *, *, #25909, .T. ) ;
#41857=CIRCLE ( 'NONE', #30504, 13.86363636363999952 ) ;
#41860=CARTESIAN_POINT ( 'NONE',  ( 10.10448976474820704, -54.34884052575311841, 7.864761218125428499 ) ) ;
#41862=CARTESIAN_POINT ( 'NONE',  ( 12.43570956081999945, -53.92016029949000000, -0.4384071701244000030 ) ) ;
#41865=PLANE ( 'NONE',  #51056 ) ;
#41868=EDGE_LOOP ( 'NONE', ( #15680, #29386, #54805, #49911 ) ) ;
#41870=DIRECTION ( 'NONE',  ( 0.000000000000000000, -1.000000000000000000, 0.000000000000000000 ) ) ;
#41874=VERTEX_POINT ( 'NONE', #2281 ) ;
#41877=CARTESIAN_POINT ( 'NONE',  ( 9.848022987154569918, -61.62869493570521939, -8.114799025198223603 ) ) ;
#41878=ORIENTED_EDGE ( 'NONE', *, *, #19264, .T. ) ;
#41879=EDGE_CURVE ( 'NONE', #11806, #9508, #15518, .T. ) ;
#41880=ORIENTED_EDGE ( 'NONE', *, *, #29098, .F. ) ;
#41881=CARTESIAN_POINT ( 'NONE',  ( 0.000000000000000000, -6.049999999381999949, 0.000000000000000000 ) ) ;
#41884=VECTOR ( 'NONE', #25840, 1000.000000000000114 ) ;
#41885=VERTEX_POINT ( 'NONE', #51000 ) ;
#41886=CARTESIAN_POINT ( 'NONE',  ( 8.485281374238999419, -18.75000000000000000, -8.485281374238999419 ) ) ;
#41887=CARTESIAN_POINT ( 'NONE',  ( 8.894916816479799593, -25.22809132934175835, -9.073484344813371294 ) ) ;
#41888=ORIENTED_EDGE ( 'NONE', *, *, #53135, .F. ) ;
#41891=TOROIDAL_SURFACE ( 'NONE', #8892, 13.50000000000000000, 0.5000000000000000000 ) ;
#41892=PLANE ( 'NONE',  #13823 ) ;
#41895=EDGE_CURVE ( 'NONE', #32127, #4183, #10497, .T. ) ;
#41896=CIRCLE ( 'NONE', #31541, 12.50000000000000000 ) ;
#41899=CARTESIAN_POINT ( 'NONE',  ( -1.733997378023031111, -23.52383216769542074, 12.54437956612010296 ) ) ;
#41900=ORIENTED_EDGE ( 'NONE', *, *, #8799, .F. ) ;
#41901=ADVANCED_FACE ( 'NONE', ( #27878, #5173 ), #18751, .T. ) ;
#41902=CARTESIAN_POINT ( 'NONE',  ( 10.54796701376999835, -75.77576924646000123, 6.346365727669000201 ) ) ;
#41905=CARTESIAN_POINT ( 'NONE',  ( 2.364202589570008950, -2.032802416630155484, -2.609243845418832031 ) ) ;
#41906=CARTESIAN_POINT ( 'NONE',  ( 12.87024489160000051, -19.21538333566000034, 2.062597265787999845 ) ) ;
#41907=CARTESIAN_POINT ( 'NONE',  ( -1.307210027570999911, -79.16850156920999382, -12.19386267984000050 ) ) ;
#41910=CARTESIAN_POINT ( 'NONE',  ( 9.713032445803841952, -61.32293762623243083, -7.970418356083900591 ) ) ;
#41911=CARTESIAN_POINT ( 'NONE',  ( -11.02814366974847893, -78.08318630897967694, -4.893295640579582439 ) ) ;
#41913=B_SPLINE_CURVE_WITH_KNOTS ( 'NONE', 3,
 ( #331, #27139, #54326, #36005, #22728, #49011, #3842, #13571, #49609, #53433, #26271, #13866, #22133, #9157, #17721, #40739, #18310, #31561, #36302, #35402, #18013, #3556, #49902, #39846, #57862, #31861, #53148, #9449, #54030, #26848, #44006, #39565, #44880, #57567, #44285, #17130, #48727, #8270, #21840, #17416, #12976, #30973, #36, #8558, #40142, #26549, #4431, #44578, #49307, #4134, #58154, #35707, #22431, #53736, #13272, #31264, #8857, #40445, #18604, #54893, #32151, #23886, #33320, #37175, #36881, #23314, #1478, #55188, #14729, #50190, #54614, #1190, #32438, #14443, #28015, #19180, #14152, #23018, #50483, #50777, #621, #24184, #36592, #10034, #9737, #51358, #27725, #5303, #5014, #1769, #45769, #19468, #46062, #41905, #42201, #41321, #6174, #904, #32728, #18888, #41030, #10322, #5583, #23595, #19762, #46647, #27436 ),
 .UNSPECIFIED., .F., .F.,
 ( 4, 2, 2, 2, 2, 2, 1, 2, 2, 2, 2, 2, 2, 2, 2, 2, 2, 2, 2, 2, 2, 2, 2, 2, 2, 2, 2, 1, 2, 2, 2, 2, 2, 2, 2, 2, 2, 2, 2, 2, 2, 2, 2, 2, 2, 2, 2, 2, 1, 2, 2, 2, 2, 2, 4 ),
 ( 0.000000000000000000, 0.01562500000000000694, 0.03125000000000001388, 0.04687500000000002082, 0.06250000000000002776, 0.07812500000000002776, 0.09375000000000004163, 0.1093750000000000555, 0.1250000000000000555, 0.1406250000000000555, 0.1562500000000000555, 0.1718750000000000555, 0.1875000000000000278, 0.2031250000000000000, 0.2187499999999999722, 0.2343749999999999722, 0.2499999999999999445, 0.2656249999999999445, 0.2812499999999999445, 0.2968749999999999445, 0.3124999999999999445, 0.3281250000000000000, 0.3437500000000000000, 0.3750000000000000000, 0.4062499999999999445, 0.4374999999999998890, 0.4687499999999998890, 0.4999999999999998335, 0.5312499999999997780, 0.5624999999999997780, 0.5937499999999997780, 0.6249999999999997780, 0.6562499999999998890, 0.6718749999999998890, 0.6874999999999998890, 0.7031249999999998890, 0.7187499999999998890, 0.7343749999999998890, 0.7499999999999998890, 0.7656249999999998890, 0.7812499999999998890, 0.7968749999999998890, 0.8124999999999998890, 0.8281249999999998890, 0.8437499999999998890, 0.8593749999999998890, 0.8749999999999998890, 0.8906250000000000000, 0.9062500000000000000, 0.9218750000000000000, 0.9375000000000000000, 0.9531250000000000000, 0.9687500000000000000, 0.9843750000000000000, 1.000000000000000000 ),
 .UNSPECIFIED. ) ;
#41914=ADVANCED_FACE ( 'NONE', ( #5459 ), #3186, .T. ) ;
#41915=ORIENTED_EDGE ( 'NONE', *, *, #11253, .F. ) ;
#41917=CARTESIAN_POINT ( 'NONE',  ( -10.26699006316252749, -77.84166666666666856, -5.917523019358070790 ) ) ;
#41918=CARTESIAN_POINT ( 'NONE',  ( 10.36597333712761326, -23.77522429014145544, 7.635925938716360051 ) ) ;
#41920=CARTESIAN_POINT ( 'NONE',  ( -3.483093260015999615, -1.774671397434999909, 0.8806644628490999382 ) ) ;
#41923=CARTESIAN_POINT ( 'NONE',  ( -6.982274206190579591, -76.12553274448890761, 9.454767744417145181 ) ) ;
#41925=CARTESIAN_POINT ( 'NONE',  ( 7.624341766639000539, -23.26485146254000114, 10.42531125024000005 ) ) ;
#41927=ORIENTED_EDGE ( 'NONE', *, *, #8622, .T. ) ;
#41928=DIRECTION ( 'NONE',  ( -0.3090169943750105674, 0.000000000000000000, 0.9510565162951329921 ) ) ;
#41933=CIRCLE ( 'NONE', #25936, 30.50000000000000355 ) ;
#41934=DIRECTION ( 'NONE',  ( 1.000000000000000000, 0.000000000000000000, 0.000000000000000000 ) ) ;
#41936=CARTESIAN_POINT ( 'NONE',  ( 7.753900686131000697, -17.71068035545000185, -10.31980286348999876 ) ) ;
#41937=CARTESIAN_POINT ( 'NONE',  ( 12.99510751537000353, -52.49705297113997204, -6.911973076623003642 ) ) ;
#41939=CARTESIAN_POINT ( 'NONE',  ( 12.71466563516855786, -17.86210710705555726, 1.778810201872595975 ) ) ;
#41942=CARTESIAN_POINT ( 'NONE',  ( 10.79453853465248159, -77.66598170563767667, -5.411409766425476775 ) ) ;
#41947=CARTESIAN_POINT ( 'NONE',  ( 3.521688171515000132, -3.513922206379000102, 0.7298424208991000084 ) ) ;
#41949=AXIS2_PLACEMENT_3D ( 'NONE', #50808, #10352, #47259 ) ;
#41953=ORIENTED_EDGE ( 'NONE', *, *, #45034, .T. ) ;
#41957=ORIENTED_EDGE ( 'NONE', *, *, #30115, .F. ) ;
#41960=CARTESIAN_POINT ( 'NONE',  ( 8.790688707576000738, -61.73813493216999859, 8.797962936864001549 ) ) ;
#41964=ORIENTED_EDGE ( 'NONE', *, *, #23172, .T. ) ;
#41965=CARTESIAN_POINT ( 'NONE',  ( -10.18248259416120938, -24.29095036201641022, 7.792398156871034764 ) ) ;
#41967=EDGE_CURVE ( 'NONE', #21583, #18023, #18964, .T. ) ;
#41969=LINE ( 'NONE', #2408, #2758 ) ;
#41970=AXIS2_PLACEMENT_3D ( 'NONE', #44359, #8345, #26341 ) ;
#41980=CARTESIAN_POINT ( 'NONE',  ( 12.74366183109916939, -60.32185227198593935, 1.980611001123821158 ) ) ;
#41982=EDGE_CURVE ( 'NONE', #52202, #4102, #22593, .T. ) ;
#41988=EDGE_CURVE ( 'NONE', #33230, #48634, #26672, .T. ) ;
#41990=CARTESIAN_POINT ( 'NONE',  ( -9.723199427802001082, -54.32306055813000256, 7.958735710007999842 ) ) ;
#41992=CARTESIAN_POINT ( 'NONE',  ( 3.209891797385462375, -2.966244217981962805, -1.450742976519075800 ) ) ;
#41998=CARTESIAN_POINT ( 'NONE',  ( -3.250000000000000000, -2.100000000000000089, 0.000000000000000000 ) ) ;
#42001=CARTESIAN_POINT ( 'NONE',  ( 1.466594960155999994, -60.88158199018999994, -12.44238958335999889 ) ) ;
#42005=CARTESIAN_POINT ( 'NONE',  ( 7.658900562714999971, -23.20940503079999928, -10.01676248781999945 ) ) ;
#42007=CARTESIAN_POINT ( 'NONE',  ( 8.485281374238999419, -59.94999999967000548, -8.485281374238999419 ) ) ;
#42009=B_SPLINE_SURFACE_WITH_KNOTS ( 'NONE', 3, 3, ( 
 ( #58258, #39086, #39379, #57665 ),
 ( #49412, #57092, #25507, #3650 ),
 ( #44101, #25795, #43524, #3085 ),
 ( #53241, #7794, #52670, #17222 ),
 ( #30506, #21653, #16659, #8080 ),
 ( #35211, #48822, #12223, #26361 ),
 ( #3369, #8660, #12790, #30213 ),
 ( #44381, #16945, #26646, #44682 ) ),
 .UNSPECIFIED., .F., .F., .F.,
 ( 4, 1, 1, 1, 1, 4 ),
 ( 4, 4 ),
 ( -0.01200407345745999922, 0.000000000000000000, 0.3333333333333000081, 0.6666666666667000474, 1.000000000000000000, 1.011997855551999947 ),
 ( -0.3559705542741000150, 1.355970554273999928 ),
 .UNSPECIFIED. ) ;
#42011=EDGE_CURVE ( 'NONE', #1755, #9471, #9604, .T. ) ;
#42013=CARTESIAN_POINT ( 'NONE',  ( 7.660411364605000273, -55.60826384781999820, -10.01752038681999935 ) ) ;
#42015=DIRECTION ( 'NONE',  ( 1.000000000000000000, 0.000000000000000000, 0.000000000000000000 ) ) ;
#42021=VERTEX_POINT ( 'NONE', #38494 ) ;
#42023=EDGE_CURVE ( 'NONE', #22487, #36041, #50659, .T. ) ;
#42024=CARTESIAN_POINT ( 'NONE',  ( -10.36597025940859673, -55.02476146821044978, 7.635927901479407254 ) ) ;
#42025=EDGE_LOOP ( 'NONE', ( #17769, #6019, #45424, #17984, #37008 ) ) ;
#42026=ADVANCED_FACE ( 'NONE', ( #33476 ), #36172, .F. ) ;
#42030=VERTEX_POINT ( 'NONE', #19621 ) ;
#42031=ORIENTED_EDGE ( 'NONE', *, *, #31416, .T. ) ;
#42033=ORIENTED_EDGE ( 'NONE', *, *, #22014, .T. ) ;
#42034=EDGE_LOOP ( 'NONE', ( #39026, #39251, #16288, #27629 ) ) ;
#42036=CARTESIAN_POINT ( 'NONE',  ( -10.11462645678665417, -55.41287635801736400, -7.639895286212103009 ) ) ;
#42041=DIRECTION ( 'NONE',  ( -0.7071067811864970576, 3.544461081833985722E-08, 0.7071067811865970887 ) ) ;
#42042=ORIENTED_EDGE ( 'NONE', *, *, #31484, .F. ) ;
#42043=ORIENTED_EDGE ( 'NONE', *, *, #47769, .T. ) ;
#42045=CARTESIAN_POINT ( 'NONE',  ( -12.71466317164989590, -24.13795986741163802, 1.778778223973440209 ) ) ;
#42050=CARTESIAN_POINT ( 'NONE',  ( 0.000000000000000000, -0.7781249991808000255, 0.000000000000000000 ) ) ;
#42062=CARTESIAN_POINT ( 'NONE',  ( -1.750000000001000089, -22.75077028492999887, -12.60356226393999890 ) ) ;
#42063=CARTESIAN_POINT ( 'NONE',  ( -7.636247231030999671, -18.23676232879999759, -10.30460520062000107 ) ) ;
#42064=VECTOR ( 'NONE', #35056, 1000.000000000000000 ) ;
#42065=CYLINDRICAL_SURFACE ( 'NONE', #42919, 3.250000000000000000 ) ;
#42066=CARTESIAN_POINT ( 'NONE',  ( 1.886823409076000102, -18.23680315638000238, -12.68610076205999881 ) ) ;
#42068=DIRECTION ( 'NONE',  ( -0.9999999924279685537, 0.000000000000000000, -0.0001230612157848962919 ) ) ;
#42070=CONICAL_SURFACE ( 'NONE', #18507, 11.96250000010999948, 0.7853981633972997312 ) ;
#42072=ORIENTED_EDGE ( 'NONE', *, *, #16481, .T. ) ;
#42073=CARTESIAN_POINT ( 'NONE',  ( 9.502896619541301604, -61.54094210160239697, 8.179425867541981532 ) ) ;
#42075=DIRECTION ( 'NONE',  ( 0.7071067811865475727, 0.000000000000000000, -0.7071067811865475727 ) ) ;
#42078=CARTESIAN_POINT ( 'NONE',  ( -9.234979314279001983, -77.01021089112001050, -9.168119495123999485 ) ) ;
#42089=DIRECTION ( 'NONE',  ( 0.000000000000000000, 0.000000000000000000, 1.000000000000000000 ) ) ;
#42091=CARTESIAN_POINT ( 'NONE',  ( -3.493489587975783461, -0.7565104147135170987, -0.4581487814226765654 ) ) ;
#42093=DIRECTION ( 'NONE',  ( 0.000000000000000000, -1.000000000000000000, 0.000000000000000000 ) ) ;
#42094=DIRECTION ( 'NONE',  ( 0.000000000000000000, 1.000000000000000000, 0.000000000000000000 ) ) ;
#42098=DIRECTION ( 'NONE',  ( 0.000000000000000000, 0.000000000000000000, -1.000000000000000000 ) ) ;
#42099=DIRECTION ( 'NONE',  ( -0.5000000000000744960, -0.7071067811864422126, -0.5000000000000744960 ) ) ;
#42100=VERTEX_POINT ( 'NONE', #26349 ) ;
#42103=ORIENTED_EDGE ( 'NONE', *, *, #21807, .T. ) ;
#42105=ADVANCED_FACE ( 'NONE', ( #21066 ), #21640, .F. ) ;
#42107=ORIENTED_EDGE ( 'NONE', *, *, #44295, .F. ) ;
#42108=CONICAL_SURFACE ( 'NONE', #49653, 12.84999999995999964, 0.7853981633972997312 ) ;
#42112=VERTEX_POINT ( 'NONE', #8351 ) ;
#42113=CYLINDRICAL_SURFACE ( 'NONE', #32762, 12.50000000000000000 ) ;
#42114=AXIS2_PLACEMENT_3D ( 'NONE', #13065, #22815, #26637 ) ;
#42115=LINE ( 'NONE', #42697, #30610 ) ;
#42116=VERTEX_POINT ( 'NONE', #7201 ) ;
#42122=CARTESIAN_POINT ( 'NONE',  ( 4.750170009413166916, -78.60686206216392691, -11.30680443602648211 ) ) ;
#42125=DIRECTION ( 'NONE',  ( -1.000000000000000000, 0.000000000000000000, 0.000000000000000000 ) ) ;
#42128=CARTESIAN_POINT ( 'NONE',  ( 6.942576159420212889, -76.52437370351259460, 9.480114445733105910 ) ) ;
#42129=CARTESIAN_POINT ( 'NONE',  ( -0.4764073897330970420, -23.51691643869884629, -10.98970030908002649 ) ) ;
#42133=CARTESIAN_POINT ( 'NONE',  ( -3.013316066571108287, -3.070796228357301150, 1.215459137038311654 ) ) ;
#42140=LINE ( 'NONE', #51008, #27196 ) ;
#42141=CARTESIAN_POINT ( 'NONE',  ( 2.932093990090213875, -3.499999999999999556, 1.781698043337538451 ) ) ;
#42143=FACE_OUTER_BOUND ( 'NONE', #32499, .T. ) ;
#42145=CARTESIAN_POINT ( 'NONE',  ( -7.730443418312603399, -24.12191635826273739, -10.25197760564498140 ) ) ;
#42148=CARTESIAN_POINT ( 'NONE',  ( -11.43953470459854671, -78.22010116149509429, -3.071145924981994124 ) ) ;
#42150=CARTESIAN_POINT ( 'NONE',  ( 10.06255860416000125, -76.46647654196999611, 6.919426796868999752 ) ) ;
#42151=ORIENTED_EDGE ( 'NONE', *, *, #41982, .T. ) ;
#42155=AXIS2_PLACEMENT_3D ( 'NONE', #48365, #21762, #17054 ) ;
#42157=CARTESIAN_POINT ( 'NONE',  ( 9.175589925015314563, -53.57304466838621693, 8.792768277016460132 ) ) ;
#42158=DIRECTION ( 'NONE',  ( -1.000000000000000000, 0.000000000000000000, 0.000000000000000000 ) ) ;
#42163=CARTESIAN_POINT ( 'NONE',  ( 9.050966798898000931, -55.65000000893999754, -7.919595949288999570 ) ) ;
#42166=CARTESIAN_POINT ( 'NONE',  ( -10.12290050124000018, -23.24999999991999644, -7.648026767085999822 ) ) ;
#42172=CARTESIAN_POINT ( 'NONE',  ( 12.82904091341000097, -60.12452529330000317, 2.062673488738000049 ) ) ;
#42177=CARTESIAN_POINT ( 'NONE',  ( -10.99608688423689173, -23.68532521788583622, -0.3139246511471364132 ) ) ;
#42185=CARTESIAN_POINT ( 'NONE',  ( 12.43356773662999970, -54.08739070985000552, 0.8411682846950000458 ) ) ;
#42186=CARTESIAN_POINT ( 'NONE',  ( 17.49999986748943925, -13.07071424677999971, 0.002153571276233540773 ) ) ;
#42188=CARTESIAN_POINT ( 'NONE',  ( -12.00000000000000000, -55.54999999966999980, 0.000000000000000000 ) ) ;
#42190=AXIS2_PLACEMENT_3D ( 'NONE', #11640, #29615, #38196 ) ;
#42192=CARTESIAN_POINT ( 'NONE',  ( -1.931736162947161217, -18.23329604287648209, -12.72978979890375051 ) ) ;
#42197=CARTESIAN_POINT ( 'NONE',  ( 10.69843650790000034, -76.27384350184999562, 6.089250768039999429 ) ) ;
#42200=EDGE_CURVE ( 'NONE', #14405, #19870, #8576, .T. ) ;
#42201=CARTESIAN_POINT ( 'NONE',  ( 1.772203737798494716, -2.015750464275656739, -3.085565428039042324 ) ) ;
#42202=CARTESIAN_POINT ( 'NONE',  ( 8.485538010685999666, -61.68067982404999583, -9.101501073510000595 ) ) ;
#42203=VECTOR ( 'NONE', #22789, 1000.000000000000000 ) ;
#42204=CARTESIAN_POINT ( 'NONE',  ( -9.042566447131001439, -79.07635346639000318, -8.284387575507999202 ) ) ;
#42208=CARTESIAN_POINT ( 'NONE',  ( 2.412979349487003766, -2.792060389164095380, -2.177788168880055331 ) ) ;
#42209=CARTESIAN_POINT ( 'NONE',  ( -9.233096103937967314, -77.61175265977985305, -9.061282067808580365 ) ) ;
#42213=B_SPLINE_CURVE_WITH_KNOTS ( 'NONE', 3,
 ( #3602, #8029, #16612, #21318, #34882, #52910, #53786, #26595, #49062, #22182, #39612, #8610, #36055, #44631, #31314, #13320 ),
 .UNSPECIFIED., .F., .F.,
 ( 4, 2, 2, 2, 2, 2, 2, 4 ),
 ( 0.000000000000000000, 0.2500000000000023315, 0.3750000000000048295, 0.5000000000000073275, 0.6250000000000098810, 0.6875000000000082157, 0.7500000000000065503, 1.000000000000000000 ),
 .UNSPECIFIED. ) ;
#42215=CARTESIAN_POINT ( 'NONE',  ( 7.792426477851446265, -24.29102098708791857, 10.18245125506949300 ) ) ;
#42216=CARTESIAN_POINT ( 'NONE',  ( 0.000000000000000000, -3.749999999256000027, -8.749999999256001360 ) ) ;
#42217=CARTESIAN_POINT ( 'NONE',  ( 2.696914660303999955, -3.191788721650999694, 2.553645155592000116 ) ) ;
#42221=CARTESIAN_POINT ( 'NONE',  ( -9.767653574770797320, -76.15254633665146855, 6.530473456064795457 ) ) ;
#42226=EDGE_LOOP ( 'NONE', ( #55886, #16541, #48749, #33588, #27235, #31321 ) ) ;
#42227=CARTESIAN_POINT ( 'NONE',  ( 12.71759155191131185, -24.06493881574830951, 1.809604648260965343 ) ) ;
#42234=CARTESIAN_POINT ( 'NONE',  ( 7.758650587948999977, -17.84922688128999724, -9.996717134846999642 ) ) ;
#42235=CARTESIAN_POINT ( 'NONE',  ( 13.63885489310999510, -59.58578169018998949, -7.254376133916000668 ) ) ;
#42240=CARTESIAN_POINT ( 'NONE',  ( -8.505218648663506187, -77.39023361062031370, 8.570118173896835501 ) ) ;
#42244=EDGE_CURVE ( 'NONE', #19894, #42030, #40157, .T. ) ;
#42246=DIRECTION ( 'NONE',  ( 0.7071067811865475727, 0.000000000000000000, 0.7071067811865475727 ) ) ;
#42247=CARTESIAN_POINT ( 'NONE',  ( 3.594201416108000036, -3.024676228556000268, 1.252117639952999850 ) ) ;
#42248=VECTOR ( 'NONE', #53215, 1000.000000000000114 ) ;
#42250=FACE_OUTER_BOUND ( 'NONE', #7448, .T. ) ;
#42253=ORIENTED_EDGE ( 'NONE', *, *, #28555, .F. ) ;
#42254=EDGE_CURVE ( 'NONE', #21333, #44757, #17735, .T. ) ;
#42255=ORIENTED_EDGE ( 'NONE', *, *, #2552, .F. ) ;
#42258=ORIENTED_EDGE ( 'NONE', *, *, #27697, .T. ) ;
#42259=CARTESIAN_POINT ( 'NONE',  ( 8.798041828550999810, -17.06186490710999948, 8.790609563012999672 ) ) ;
#42261=CARTESIAN_POINT ( 'NONE',  ( 10.64585027366999981, -79.12040545280000003, 5.670349170909000591 ) ) ;
#42262=CARTESIAN_POINT ( 'NONE',  ( 9.992017125402000488, -60.96084086979999483, 7.762968460695000239 ) ) ;
#42263=PLANE ( 'NONE',  #57056 ) ;
#42273=CARTESIAN_POINT ( 'NONE',  ( 0.000000000000000000, -9.638971321655001034, 0.000000000000000000 ) ) ;
#42274=AXIS2_PLACEMENT_3D ( 'NONE', #37906, #11851, #38991 ) ;
#42275=DIRECTION ( 'NONE',  ( 0.000000000000000000, 0.000000000000000000, 1.000000000000000000 ) ) ;
#42279=CARTESIAN_POINT ( 'NONE',  ( -7.645391636765999976, -23.21530450358000053, -10.18949673576000059 ) ) ;
#42280=CARTESIAN_POINT ( 'NONE',  ( 12.49168451100999988, -60.09848884406000025, -1.667916687331000070 ) ) ;
#42282=ORIENTED_EDGE ( 'NONE', *, *, #10378, .F. ) ;
#42284=DIRECTION ( 'NONE',  ( -0.7071067811865969777, -1.536189447283994854E-11, 0.7071067811864980568 ) ) ;
#42288=CARTESIAN_POINT ( 'NONE',  ( -7.956418361382000981, -17.47110680143000039, 9.787952249849000808 ) ) ;
#42291=AXIS2_PLACEMENT_3D ( 'NONE', #37836, #2993, #55855 ) ;
#42292=CARTESIAN_POINT ( 'NONE',  ( 3.507528428923288200, -2.993384342491289818, -0.2940356736387945147 ) ) ;
#42298=DIRECTION ( 'NONE',  ( 0.000000000000000000, -1.000000000000000000, 0.000000000000000000 ) ) ;
#42301=DIRECTION ( 'NONE',  ( 0.000000000000000000, -1.000000000000000000, 0.000000000000000000 ) ) ;
#42302=CARTESIAN_POINT ( 'NONE',  ( -7.398464061241327272, -55.34839576621715906, 8.140250184786385290 ) ) ;
#42305=CARTESIAN_POINT ( 'NONE',  ( 7.974014308125999762, -24.63100890329999970, -9.929675091742000248 ) ) ;
#42309=ORIENTED_EDGE ( 'NONE', *, *, #57529, .T. ) ;
#42312=CARTESIAN_POINT ( 'NONE',  ( 7.657744736598999680, -55.13080421771999795, -9.966195456739999514 ) ) ;
#42320=CARTESIAN_POINT ( 'NONE',  ( -5.827782744364191636, -78.51269081667429361, 10.39236577010555607 ) ) ;
#42321=CIRCLE ( 'NONE', #18755, 12.80000000000000071 ) ;
#42325=B_SPLINE_CURVE_WITH_KNOTS ( 'NONE', 3,
 ( #46276, #5508, #55695, #15244, #11129, #6387 ),
 .UNSPECIFIED., .F., .F.,
 ( 4, 2, 4 ),
 ( 0.000000000000000000, 0.5000000000000001110, 1.000000000000000000 ),
 .UNSPECIFIED. ) ;
#42328=ORIENTED_EDGE ( 'NONE', *, *, #43127, .T. ) ;
#42333=ORIENTED_EDGE ( 'NONE', *, *, #33072, .T. ) ;
#42335=CARTESIAN_POINT ( 'NONE',  ( 0.005928781627485999947, -16.79886949736999924, 12.66336824419000173 ) ) ;
#42344=VERTEX_POINT ( 'NONE', #38063 ) ;
#42348=CARTESIAN_POINT ( 'NONE',  ( -1.575772165365692645, -61.26154542772368927, -12.70597445621287847 ) ) ;
#42350=DIRECTION ( 'NONE',  ( 0.000000000000000000, 0.000000000000000000, -1.000000000000000000 ) ) ;
#42354=AXIS2_PLACEMENT_3D ( 'NONE', #11666, #29641, #47694 ) ;
#42359=CARTESIAN_POINT ( 'NONE',  ( 1.799475304559999822, -21.75171076523999858, -12.69616050742999924 ) ) ;
#42360=EDGE_CURVE ( 'NONE', #50040, #54902, #51083, .T. ) ;
#42362=CARTESIAN_POINT ( 'NONE',  ( 1.669849926071999890, -18.62771399582999976, -12.48404299553000030 ) ) ;
#42364=CARTESIAN_POINT ( 'NONE',  ( -14.00000000000000000, -46.09579702914000165, 0.000000000000000000 ) ) ;
#42367=CARTESIAN_POINT ( 'NONE',  ( 2.086062294176650678, -1.425354687551017463, -2.850033995333124182 ) ) ;
#42368=EDGE_CURVE ( 'NONE', #42463, #27850, #27691, .T. ) ;
#42370=CARTESIAN_POINT ( 'NONE',  ( 8.130811096204000776, -61.48523690322999613, 9.546858433459998849 ) ) ;
#42371=CARTESIAN_POINT ( 'NONE',  ( -1.539691793600886482, -77.58363846744875048, 11.67469292510621948 ) ) ;
#42374=AXIS2_PLACEMENT_3D ( 'NONE', #39093, #12516, #25514 ) ;
#42375=CARTESIAN_POINT ( 'NONE',  ( -12.54980553584999825, -53.75222688831999562, -0.05649961219500999887 ) ) ;
#42385=CARTESIAN_POINT ( 'NONE',  ( -3.165411199172029288, -2.979166666666666075, 0.8506806241676482250 ) ) ;
#42391=CARTESIAN_POINT ( 'NONE',  ( -12.50000000000000000, -23.24999999758999536, 1.750000000000000000 ) ) ;
#42393=VERTEX_POINT ( 'NONE', #14744 ) ;
#42395=DIRECTION ( 'NONE',  ( -0.7026410690473252618, -0.1122098755728027641, -0.7026410690473252618 ) ) ;
#42396=DIRECTION ( 'NONE',  ( 0.000000000000000000, -1.000000000000000000, 0.000000000000000000 ) ) ;
#42397=ORIENTED_EDGE ( 'NONE', *, *, #40270, .T. ) ;
#42400=ORIENTED_EDGE ( 'NONE', *, *, #55187, .T. ) ;
#42402=AXIS2_PLACEMENT_3D ( 'NONE', #21646, #57953, #39653 ) ;
#42403=VERTEX_POINT ( 'NONE', #54907 ) ;
#42404=B_SPLINE_CURVE_WITH_KNOTS ( 'NONE', 3,
 ( #32026, #33188, #50067, #45643, #45345, #5755, #1644, #4896, #5181, #23472, #19633, #27600, #55648, #46231, #55062, #32605, #10198, #23763 ),
 .UNSPECIFIED., .F., .F.,
 ( 4, 2, 2, 2, 2, 2, 2, 2, 4 ),
 ( 0.000000000000000000, 0.06250000000000068001, 0.1250000000000013600, 0.2500000000000027200, 0.5000000000000014433, 0.7500000000000001110, 0.8124999999999988898, 0.8749999999999975575, 1.000000000000000000 ),
 .UNSPECIFIED. ) ;
#42407=ORIENTED_EDGE ( 'NONE', *, *, #37066, .T. ) ;
#42410=CARTESIAN_POINT ( 'NONE',  ( -3.060972652365999913, -2.035913946620000026, 0.7739355898497000119 ) ) ;
#42417=VECTOR ( 'NONE', #38180, 1000.000000000000000 ) ;
#42424=CARTESIAN_POINT ( 'NONE',  ( -7.678690995233999672, -57.04351820043999766, -10.59551070214999946 ) ) ;
#42426=CARTESIAN_POINT ( 'NONE',  ( 6.534747300401333447, -76.52789284558512861, 9.765094741288242730 ) ) ;
#42429=CARTESIAN_POINT ( 'NONE',  ( 12.00000000000000000, -60.04999999966999980, 0.000000000000000000 ) ) ;
#42435=CARTESIAN_POINT ( 'NONE',  ( -7.648802896946197194, -76.26817011481092834, -8.920997862297024739 ) ) ;
#42436=CARTESIAN_POINT ( 'NONE',  ( 1.250000000000000000, -18.55321828668999729, 12.50000000000000000 ) ) ;
#42438=CARTESIAN_POINT ( 'NONE',  ( -10.53559655518999882, -60.00569178284000316, -7.620036226177999694 ) ) ;
#42439=CARTESIAN_POINT ( 'NONE',  ( 0.07833262907167658218, -3.500000000000000444, 3.294754266843233470 ) ) ;
#42441=VECTOR ( 'NONE', #54550, 1000.000000000000000 ) ;
#42443=CARTESIAN_POINT ( 'NONE',  ( 12.54901606605999831, -25.00731603500000233, 0.4733145588205000531 ) ) ;
#42445=CARTESIAN_POINT ( 'NONE',  ( 11.74911438887889759, -78.44153470896613101, -0.7697094805160100695 ) ) ;
#42447=CARTESIAN_POINT ( 'NONE',  ( -11.41861126715999930, -76.22951562304000106, 3.886338190518000335 ) ) ;
#42448=ORIENTED_EDGE ( 'NONE', *, *, #49350, .T. ) ;
#42452=FACE_OUTER_BOUND ( 'NONE', #51120, .T. ) ;
#42454=CARTESIAN_POINT ( 'NONE',  ( 12.70956139856000000, -55.39498835716000258, -1.933780970937999832 ) ) ;
#42458=CARTESIAN_POINT ( 'NONE',  ( 13.86363636363000218, -9.638971321655001034, 1.277887488545999904E-05 ) ) ;
#42461=VECTOR ( 'NONE', #44641, 1000.000000000000000 ) ;
#42463=VERTEX_POINT ( 'NONE', #55201 ) ;
#42465=DIRECTION ( 'NONE',  ( 0.000000000000000000, -1.000000000000000000, 0.000000000000000000 ) ) ;
#42471=ORIENTED_EDGE ( 'NONE', *, *, #20840, .F. ) ;
#42472=ORIENTED_EDGE ( 'NONE', *, *, #19663, .T. ) ;
#42476=EDGE_LOOP ( 'NONE', ( #18804, #57662, #43778 ) ) ;
#42477=CARTESIAN_POINT ( 'NONE',  ( 1.997394009589563924, -2.424135704803565439, 2.599556423877257938 ) ) ;
#42479=AXIS2_PLACEMENT_3D ( 'NONE', #6060, #55662, #33202 ) ;
#42480=ORIENTED_EDGE ( 'NONE', *, *, #25745, .T. ) ;
#42481=CARTESIAN_POINT ( 'NONE',  ( -12.83838776459000108, -23.20596988487999823, -2.062170466181000528 ) ) ;
#42490=CARTESIAN_POINT ( 'NONE',  ( -6.282410744257000523, -75.90028781030999028, 10.58616248715999930 ) ) ;
#42493=CARTESIAN_POINT ( 'NONE',  ( 9.317978910689999950, -61.93238462986000314, -8.588869595475999930 ) ) ;
#42494=CARTESIAN_POINT ( 'NONE',  ( -12.10179013622999911, -78.46094648960999507, -1.986401539992999954 ) ) ;
#42496=CARTESIAN_POINT ( 'NONE',  ( -7.889735440110458242, -60.55042584425823549, -7.666647577132536640 ) ) ;
#42497=EDGE_CURVE ( 'NONE', #43600, #25463, #49283, .T. ) ;
#42498=CARTESIAN_POINT ( 'NONE',  ( 10.65229704191123616, -78.26108579923685227, -5.670296759119941576 ) ) ;
#42499=DIRECTION ( 'NONE',  ( 0.000000000000000000, -1.000000000000000000, 0.000000000000000000 ) ) ;
#42500=EDGE_LOOP ( 'NONE', ( #8910, #18862, #23014, #37375 ) ) ;
#42503=DIRECTION ( 'NONE',  ( 0.9999548435846228323, 0.000000000000000000, 0.009503199022040218977 ) ) ;
#42505=CARTESIAN_POINT ( 'NONE',  ( -1.465608348446000075, -2.200283069271000258, 3.582222755774000067 ) ) ;
#42509=CARTESIAN_POINT ( 'NONE',  ( -2.856588293545408774, -76.09423490609401597, 11.40386817198159441 ) ) ;
#42512=CARTESIAN_POINT ( 'NONE',  ( 1.026866341085000007E-14, -0.1000000000000002554, 0.000000000000000000 ) ) ;
#42515=EDGE_CURVE ( 'NONE', #53612, #56919, #15922, .T. ) ;
#42516=CYLINDRICAL_SURFACE ( 'NONE', #10692, 3.250000000000000000 ) ;
#42517=CIRCLE ( 'NONE', #36854, 9.000000000000000000 ) ;
#42518=CARTESIAN_POINT ( 'NONE',  ( 0.4254240051736068451, -2.364583333333333481, 3.250000000000001776 ) ) ;
#42519=CARTESIAN_POINT ( 'NONE',  ( -9.213114944054998645, -61.80524898723000149, 8.533795138624000742 ) ) ;
#42522=CARTESIAN_POINT ( 'NONE',  ( 1.695907231049564201, -3.266824736097686088, -2.897058440794695766 ) ) ;
#42527=DIRECTION ( 'NONE',  ( 0.000000000000000000, -1.000000000000000000, 0.000000000000000000 ) ) ;
#42529=CARTESIAN_POINT ( 'NONE',  ( -11.56793956631425502, -77.42581400997612207, 4.165594241877493609 ) ) ;
#42532=CARTESIAN_POINT ( 'NONE',  ( 10.14948852600999984, -59.55100835476999777, -7.674614791855999485 ) ) ;
#42533=DIRECTION ( 'NONE',  ( 0.000000000000000000, -1.000000000000000000, 0.000000000000000000 ) ) ;
#42534=ADVANCED_FACE ( 'NONE', ( #30049 ), #20922, .F. ) ;
#42535=AXIS2_PLACEMENT_3D ( 'NONE', #50425, #49841, #36243 ) ;
#42537=CYLINDRICAL_SURFACE ( 'NONE', #18887, 9.000000000000000000 ) ;
#42540=ORIENTED_EDGE ( 'NONE', *, *, #25162, .T. ) ;
#42541=VERTEX_POINT ( 'NONE', #11216 ) ;
#42545=CARTESIAN_POINT ( 'NONE',  ( 7.658900723009000266, -18.79059707833999937, 10.01676258974000078 ) ) ;
#42547=CARTESIAN_POINT ( 'NONE',  ( 11.96278553877000128, -79.09166473471999836, 1.542582301795999866 ) ) ;
#42549=CARTESIAN_POINT ( 'NONE',  ( 13.94827586207000003, -33.10361340872000113, 8.082385094115998871E-06 ) ) ;
#42550=CARTESIAN_POINT ( 'NONE',  ( 0.000000000000000000, -23.15000000000000213, 11.79999999999999893 ) ) ;
#42553=ORIENTED_EDGE ( 'NONE', *, *, #41443, .F. ) ;
#42555=AXIS2_PLACEMENT_3D ( 'NONE', #48844, #8389, #3958 ) ;
#42558=CARTESIAN_POINT ( 'NONE',  ( 12.52582323437067124, -60.60939730725227292, -1.680974276192610972 ) ) ;
#42560=UNCERTAINTY_MEASURE_WITH_UNIT (LENGTH_MEASURE( 1.000000000000000082E-05 ), #602, 'distance_accuracy_value', 'NONE');
#42562=CARTESIAN_POINT ( 'NONE',  ( 11.82469666049999901, -76.02329627867000283, 4.496655510765000585 ) ) ;
#42563=DIRECTION ( 'NONE',  ( -0.9859154929577472748, 0.1672442547470080754, 0.000000000000000000 ) ) ;
#42565=CARTESIAN_POINT ( 'NONE',  ( -7.705119999441000012, -20.24828923609000242, 10.24996238031000040 ) ) ;
#42568=CARTESIAN_POINT ( 'NONE',  ( 7.710118476736999682, -57.05022860539000362, 10.18499221088999995 ) ) ;
#42570=FILL_AREA_STYLE ('',( #29547 ) ) ;
#42572=ORIENTED_EDGE ( 'NONE', *, *, #23059, .F. ) ;
#42573=EDGE_CURVE ( 'NONE', #800, #42344, #31586, .T. ) ;
#42577=CARTESIAN_POINT ( 'NONE',  ( -1.247385801080000078, -24.47722256257000240, -12.50301438876999960 ) ) ;
#42579=CARTESIAN_POINT ( 'NONE',  ( -8.666925696261760237, -53.80708316137260994, 9.019429295859271889 ) ) ;
#42581=CARTESIAN_POINT ( 'NONE',  ( -2.105625082083603328, -2.323927937926350662, -2.820318438645454950 ) ) ;
#42589=EDGE_LOOP ( 'NONE', ( #39313, #42107, #26451, #50210 ) ) ;
#42591=CARTESIAN_POINT ( 'NONE',  ( 0.000000000000000000, -60.04999999966999980, 12.50000000000000000 ) ) ;
#42592=CARTESIAN_POINT ( 'NONE',  ( -0.4356486348705999601, -61.68064955776999625, -12.43591427125000060 ) ) ;
#42593=EDGE_CURVE ( 'NONE', #10368, #10966, #12069, .T. ) ;
#42594=CARTESIAN_POINT ( 'NONE',  ( -7.345153731672206199, -55.57158755757922108, 8.188331488387630586 ) ) ;
#42597=CARTESIAN_POINT ( 'NONE',  ( 10.19022265128000093, -23.19634105642999700, -7.646946115745000050 ) ) ;
#42600=CARTESIAN_POINT ( 'NONE',  ( 6.069819744066555778, -78.53115937559208248, 10.06047354936908178 ) ) ;
#42601=DIRECTION ( 'NONE',  ( -0.7071067811865475727, 0.000000000000000000, -0.7071067811865475727 ) ) ;
#42605=CARTESIAN_POINT ( 'NONE',  ( 7.981651535783000462, -54.08135615453999634, -10.08154952393999970 ) ) ;
#42607=CARTESIAN_POINT ( 'NONE',  ( -10.39929541389761702, -79.15104165712787676, -5.992801102062716545 ) ) ;
#42612=CARTESIAN_POINT ( 'NONE',  ( -8.114915067887620737, -53.97115967817116200, 9.847905526091571105 ) ) ;
#42613=ORIENTED_EDGE ( 'NONE', *, *, #21764, .T. ) ;
#42621=VERTEX_POINT ( 'NONE', #24781 ) ;
#42622=EDGE_CURVE ( 'NONE', #39417, #26558, #56941, .T. ) ;
#42623=TOROIDAL_SURFACE ( 'NONE', #36915, 1.250000000000000000, 0.5000000000000000000 ) ;
#42624=CARTESIAN_POINT ( 'NONE',  ( 1.890224871707000043, -18.25210751985000002, 12.68696160873999901 ) ) ;
#42625=CARTESIAN_POINT ( 'NONE',  ( 0.5999999998848000171, -18.85000000520999919, -11.79999999988000070 ) ) ;
#42627=CARTESIAN_POINT ( 'NONE',  ( -13.63885489310999510, -59.58578169018998949, -7.254376133916000668 ) ) ;
#42631=ORIENTED_EDGE ( 'NONE', *, *, #27677, .F. ) ;
#42636=CARTESIAN_POINT ( 'NONE',  ( 0.000000000000000000, 4.040000000000000036, 0.000000000000000000 ) ) ;
#42641=CARTESIAN_POINT ( 'NONE',  ( -9.734541936978917676, -76.65229327790524394, 6.579934271495913478 ) ) ;
#42647=LINE ( 'NONE', #2781, #24017 ) ;
#42649=CARTESIAN_POINT ( 'NONE',  ( 1.288488638074000159, -17.46435060632000003, -12.54709296483000003 ) ) ;
#42653=CARTESIAN_POINT ( 'NONE',  ( 3.110769248615221194, -0.9610483397592147758, -1.653932746071141935 ) ) ;
#42655=DIRECTION ( 'NONE',  ( 0.7071067812094172789, -2.924114041541070768E-07, 0.7071067811636172484 ) ) ;
#42656=CARTESIAN_POINT ( 'NONE',  ( 10.12290050124000018, -18.75000000007999645, -7.648026767085999822 ) ) ;
#42660=CARTESIAN_POINT ( 'NONE',  ( -3.274010471232999819, -77.34323873689000095, 12.59444704299999884 ) ) ;
#42661=CARTESIAN_POINT ( 'NONE',  ( 1.807051837523000026, -61.10078415209999747, 12.77977401837999949 ) ) ;
#42664=CARTESIAN_POINT ( 'NONE',  ( -12.50000000000000000, -55.55000000209000177, -1.750000000000000000 ) ) ;
#42665=VECTOR ( 'NONE', #34543, 1000.000000000000000 ) ;
#42667=CARTESIAN_POINT ( 'NONE',  ( -4.528061651730656223, -76.29306646779448897, -10.84218088047703965 ) ) ;
#42672=CARTESIAN_POINT ( 'NONE',  ( 0.4254240051736068451, -2.864583333333333925, 3.250000000000001776 ) ) ;
#42679=ORIENTED_EDGE ( 'NONE', *, *, #4113, .F. ) ;
#42680=VECTOR ( 'NONE', #56658, 1000.000000000000114 ) ;
#42682=DIRECTION ( 'NONE',  ( -0.7071067811865475727, 0.000000000000000000, 0.7071067811865475727 ) ) ;
#42684=ORIENTED_EDGE ( 'NONE', *, *, #22726, .F. ) ;
#42686=VERTEX_POINT ( 'NONE', #47902 ) ;
#42690=ORIENTED_EDGE ( 'NONE', *, *, #42368, .T. ) ;
#42691=ADVANCED_FACE ( 'NONE', ( #13589 ), #13296, .T. ) ;
#42697=CARTESIAN_POINT ( 'NONE',  ( 7.919595949288999570, -55.64999999965999677, -8.768124086712999699 ) ) ;
#42698=ORIENTED_EDGE ( 'NONE', *, *, #32191, .F. ) ;
#42699=DIRECTION ( 'NONE',  ( 0.000000000000000000, 0.000000000000000000, 1.000000000000000000 ) ) ;
#42703=DIRECTION ( 'NONE',  ( 0.000000000000000000, -1.000000000000000000, 0.000000000000000000 ) ) ;
#42712=ADVANCED_FACE ( 'NONE', ( #40164 ), #44900, .F. ) ;
#42714=CARTESIAN_POINT ( 'NONE',  ( -7.958763980599000476, -17.52301961032999955, -9.723170659105999647 ) ) ;
#42718=VECTOR ( 'NONE', #26787, 999.9999999999998863 ) ;
#42721=DIRECTION ( 'NONE',  ( 0.000000000000000000, -1.000000000000000000, 9.099419098363000178E-12 ) ) ;
#42722=CARTESIAN_POINT ( 'NONE',  ( 12.50745077490000057, -17.00005551713000074, -2.011911479242000131E-09 ) ) ;
#42723=VECTOR ( 'NONE', #37717, 1000.000000000000000 ) ;
#42724=DIRECTION ( 'NONE',  ( -1.147010004338000229E-14, 0.000000000000000000, 1.000000000000000000 ) ) ;
#42726=ADVANCED_FACE ( 'NONE', ( #53759 ), #8879, .T. ) ;
#42727=CARTESIAN_POINT ( 'NONE',  ( 10.01332852690999964, -60.08056535122999975, 7.654537165486999584 ) ) ;
#42729=EDGE_CURVE ( 'NONE', #20675, #26186, #4747, .T. ) ;
#42730=CARTESIAN_POINT ( 'NONE',  ( -8.266617305338565203, -24.97234527442468632, -9.697375114818715502 ) ) ;
#42731=B_SPLINE_CURVE_WITH_KNOTS ( 'NONE', 3,
 ( #43236, #47970, #52669, #7507, #38508, #6926 ),
 .UNSPECIFIED., .F., .F.,
 ( 4, 2, 4 ),
 ( 0.000000000000000000, 0.5000000000000000000, 1.000000000000000000 ),
 .UNSPECIFIED. ) ;
#42734=CARTESIAN_POINT ( 'NONE',  ( -1.980611416588520024, -23.52597731804367953, -12.74335092663162250 ) ) ;
#42735=CARTESIAN_POINT ( 'NONE',  ( 8.351130818052999061, -75.94147849534999750, -8.703251827980000854 ) ) ;
#42742=CARTESIAN_POINT ( 'NONE',  ( 12.55485633992000061, -54.64594908747999824, -1.580761757393000178 ) ) ;
#42744=VECTOR ( 'NONE', #3854, 1000.000000000000114 ) ;
#42746=CARTESIAN_POINT ( 'NONE',  ( -1.392423410630999929E-14, -75.80000000000001137, 0.000000000000000000 ) ) ;
#42754=CARTESIAN_POINT ( 'NONE',  ( 12.75761570869000039, -59.57819125629999490, 1.931043762602999925 ) ) ;
#42759=ORIENTED_EDGE ( 'NONE', *, *, #25360, .T. ) ;
#42762=ADVANCED_FACE ( 'NONE', ( #29489 ), #2082, .F. ) ;
#42765=EDGE_CURVE ( 'NONE', #12597, #54609, #8387, .T. ) ;
#42771=VERTEX_POINT ( 'NONE', #46960 ) ;
#42774=CARTESIAN_POINT ( 'NONE',  ( 9.841113773978118928, -17.16371975942079686, -8.121706172286355496 ) ) ;
#42777=CARTESIAN_POINT ( 'NONE',  ( -12.70455814334985511, -17.43992875973548706, -1.489882837223169387 ) ) ;
#42778=FACE_OUTER_BOUND ( 'NONE', #29835, .T. ) ;
#42780=CARTESIAN_POINT ( 'NONE',  ( -7.647735717248999698, -23.72294882383999948, 10.13404777202000062 ) ) ;
#42783=DIRECTION ( 'NONE',  ( 0.9999999924279685537, 0.000000000000000000, 0.0001230612157848962919 ) ) ;
#42784=CARTESIAN_POINT ( 'NONE',  ( 3.086017585447000222, -79.09324228728000605, -11.86910201801999953 ) ) ;
#42787=CARTESIAN_POINT ( 'NONE',  ( -9.188080731290124703, -77.99423656384304593, 7.746760052061067547 ) ) ;
#42789=AXIS2_PLACEMENT_3D ( 'NONE', #31225, #3797, #4088 ) ;
#42790=ORIENTED_EDGE ( 'NONE', *, *, #7357, .F. ) ;
#42792=CARTESIAN_POINT ( 'NONE',  ( 5.917523019358082337, -77.96666666666666856, -10.26699006316252394 ) ) ;
#42794=B_SPLINE_CURVE_WITH_KNOTS ( 'NONE', 3,
 ( #36597, #54897, #10623, #24189, #19767, #28604, #5018, #28021, #54619, #37764, #14157, #27729, #49907, #46651, #10327, #6178 ),
 .UNSPECIFIED., .F., .F.,
 ( 4, 2, 2, 2, 2, 2, 2, 4 ),
 ( 0.000000000000000000, 0.2499999999999970024, 0.3749999999999955036, 0.4999999999999940048, 0.6249999999999924505, 0.6874999999999932276, 0.7499999999999938938, 1.000000000000000000 ),
 .UNSPECIFIED. ) ;
#42796=CARTESIAN_POINT ( 'NONE',  ( 0.5559119596479000780, -3.157909330902999745, 3.830311516254000015 ) ) ;
#42797=VECTOR ( 'NONE', #18177, 1000.000000000000227 ) ;
#42800=CARTESIAN_POINT ( 'NONE',  ( -1.136237469166809122, -76.08235068074559138, 11.70153850263246298 ) ) ;
#42801=DIRECTION ( 'NONE',  ( 1.000000000000000000, 0.000000000000000000, 0.000000000000000000 ) ) ;
#42805=CARTESIAN_POINT ( 'NONE',  ( -6.024415200220997413, -76.46569630464409784, 10.73507988388000101 ) ) ;
#42808=CARTESIAN_POINT ( 'NONE',  ( -7.961052042476000068, -61.33567434991999789, 9.783216378940000624 ) ) ;
#42814=CARTESIAN_POINT ( 'NONE',  ( 7.634645133843636522, -23.47584427336935775, -10.10912661252998923 ) ) ;
#42816=CARTESIAN_POINT ( 'NONE',  ( -13.94827586207000003, -45.69638659094999866, -8.082388077679998639E-06 ) ) ;
#42820=TOROIDAL_SURFACE ( 'NONE', #47562, 1.250000000000000000, 0.5000000000000000000 ) ;
#42825=DIRECTION ( 'NONE',  ( -0.7071067811865475727, 0.000000000000000000, 0.7071067811865475727 ) ) ;
#42828=VECTOR ( 'NONE', #37358, 1000.000000000000000 ) ;
#42836=VECTOR ( 'NONE', #32181, 999.9999999999998863 ) ;
#42837=CARTESIAN_POINT ( 'NONE',  ( 10.13695543448000080, -18.29168900649999685, 7.646071007876000358 ) ) ;
#42840=CARTESIAN_POINT ( 'NONE',  ( -10.38133291898000188, -78.11882557138000038, 7.485792156039000389 ) ) ;
#42842=CARTESIAN_POINT ( 'NONE',  ( 9.722718241315000398, -55.35321828636000419, 7.954951288349001004 ) ) ;
#42844=ADVANCED_FACE ( 'NONE', ( #2929 ), #56836, .T. ) ;
#42845=ORIENTED_EDGE ( 'NONE', *, *, #42023, .T. ) ;
#42846=CARTESIAN_POINT ( 'NONE',  ( -3.903942181442680681, -78.20186436195335489, 11.12926803347593996 ) ) ;
#42850=DIRECTION ( 'NONE',  ( -0.7071067811865475727, 0.000000000000000000, 0.7071067811865475727 ) ) ;
#42854=CARTESIAN_POINT ( 'NONE',  ( -10.42531124905999995, -18.73514851523999880, 7.624341765453999997 ) ) ;
#42856=CARTESIAN_POINT ( 'NONE',  ( -7.691893942754999713, -20.24546192895000019, 10.42272502865000128 ) ) ;
#42860=CIRCLE ( 'NONE', #36225, 1.250000000000000000 ) ;
#42861=SURFACE_STYLE_FILL_AREA ( #42570 ) ;
#42863=ORIENTED_EDGE ( 'NONE', *, *, #37206, .F. ) ;
#42868=EDGE_CURVE ( 'NONE', #23950, #17469, #35089, .T. ) ;
#42869=CARTESIAN_POINT ( 'NONE',  ( -7.622784390062999904, -18.21288991773999655, 10.47836615826999918 ) ) ;
#42871=CARTESIAN_POINT ( 'NONE',  ( 2.226387500030236222, -2.070620109172146783, 2.730464303426434647 ) ) ;
#42874=CARTESIAN_POINT ( 'NONE',  ( 1.758095523371000057, -55.07708336086999878, -12.57362173513000059 ) ) ;
#42880=CARTESIAN_POINT ( 'NONE',  ( 10.98363359191198718, -18.81005173320433244, -0.5998275989260992702 ) ) ;
#42881=DIRECTION ( 'NONE',  ( -0.5721800015184017596, -0.8201280667447015116, 0.000000000000000000 ) ) ;
#42883=CARTESIAN_POINT ( 'NONE',  ( -0.5390150933989998894, -62.06260891619000120, -12.77520261008999825 ) ) ;
#42887=CARTESIAN_POINT ( 'NONE',  ( 10.45204383623999966, -59.56256649442000395, -7.651147548074000326 ) ) ;
#42889=DIRECTION ( 'NONE',  ( -0.7071067811813920301, 1.254536121801983732E-07, -0.7071067811916919021 ) ) ;
#42890=CARTESIAN_POINT ( 'NONE',  ( 11.34432545814875759, -78.46928195054157129, 3.060665140078473456 ) ) ;
#42891=DIRECTION ( 'NONE',  ( 0.7071067811865475727, 0.000000000000000000, -0.7071067811865475727 ) ) ;
#42892=ORIENTED_EDGE ( 'NONE', *, *, #24691, .T. ) ;
#42894=DIRECTION ( 'NONE',  ( 0.7071067811865969777, -0.7071067811864980568, -1.752031294627994831E-09 ) ) ;
#42896=CARTESIAN_POINT ( 'NONE',  ( -1.564666716807709523, -79.19661455703162289, -11.94661365431226230 ) ) ;
#42898=CARTESIAN_POINT ( 'NONE',  ( -10.18496935386000146, -58.55064714674999493, 7.710095619709000481 ) ) ;
#42902=B_SPLINE_CURVE_WITH_KNOTS ( 'NONE', 3,
 ( #13024, #17175, #3884, #39894, #30737, #8317, #12178, #4184, #53483, #49061 ),
 .UNSPECIFIED., .F., .F.,
 ( 4, 2, 2, 2, 4 ),
 ( 0.000000000000000000, 0.2500000000000000000, 0.5000000000000000000, 0.7500000000000000000, 1.000000000000000000 ),
 .UNSPECIFIED. ) ;
#42904=FACE_OUTER_BOUND ( 'NONE', #15524, .T. ) ;
#42906=AXIS2_PLACEMENT_3D ( 'NONE', #56439, #11283, #15110 ) ;
#42908=ORIENTED_EDGE ( 'NONE', *, *, #20538, .T. ) ;
#42910=CARTESIAN_POINT ( 'NONE',  ( -12.66235371494999917, -53.66260492101000068, -0.4957155363045000485 ) ) ;
#42911=VECTOR ( 'NONE', #38714, 1000.000000000000000 ) ;
#42912=ORIENTED_EDGE ( 'NONE', *, *, #40608, .T. ) ;
#42913=VERTEX_POINT ( 'NONE', #46529 ) ;
#42919=AXIS2_PLACEMENT_3D ( 'NONE', #43226, #19624, #51227 ) ;
#42922=EDGE_CURVE ( 'NONE', #26124, #8841, #24061, .T. ) ;
#42923=ORIENTED_EDGE ( 'NONE', *, *, #252, .T. ) ;
#42927=CARTESIAN_POINT ( 'NONE',  ( -12.65987830577000040, -61.73692962272999551, -0.9847759095506000149 ) ) ;
#42930=DIRECTION ( 'NONE',  ( 0.6562721000563372931, 0.7545243075525430720, -7.866585117886450344E-10 ) ) ;
#42936=CARTESIAN_POINT ( 'NONE',  ( -9.830798712606000578, -54.70910918491000530, 7.765013391389000041 ) ) ;
#42940=CARTESIAN_POINT ( 'NONE',  ( -7.646788101826000883, -18.62771363264999991, -10.00831428591000005 ) ) ;
#42942=CARTESIAN_POINT ( 'NONE',  ( 1.807051837523000026, -17.69921584757000232, -12.77977401834999860 ) ) ;
#42943=CARTESIAN_POINT ( 'NONE',  ( -3.251154051729839178, -1.100857096137070279, 2.995606203745920413E-05 ) ) ;
#42944=CARTESIAN_POINT ( 'NONE',  ( 13.86363625866319715, -9.638971321655001034, 0.001706075946107427251 ) ) ;
#42945=CARTESIAN_POINT ( 'NONE',  ( 3.383845406481000406, -2.564161638761000450, -1.742318191517000070 ) ) ;
#42946=CARTESIAN_POINT ( 'NONE',  ( -0.8613851204907587711, -0.8555241698066097245, -3.423604145181888825 ) ) ;
#42947=ORIENTED_EDGE ( 'NONE', *, *, #29731, .F. ) ;
#42948=CARTESIAN_POINT ( 'NONE',  ( -8.768124086549999419, -59.94999999446000771, -7.919595949288999570 ) ) ;
#42950=CARTESIAN_POINT ( 'NONE',  ( -1.667260628947000001, -55.59057987493000041, 12.49858003893000102 ) ) ;
#42953=B_SPLINE_CURVE_WITH_KNOTS ( 'NONE', 3,
 ( #11688, #43555, #29666, #12540, #20541, #3120, #57699, #44134, #21398, #38827 ),
 .UNSPECIFIED., .F., .F.,
 ( 4, 1, 1, 2, 2, 4 ),
 ( 0.000000000000000000, 0.2499999999999998890, 0.3749999999999998335, 0.4374999999999998890, 0.5000000000000000000, 1.000000000000000000 ),
 .UNSPECIFIED. ) ;
#42956=CARTESIAN_POINT ( 'NONE',  ( -12.43570956081999945, -53.92016029949000000, 0.4384071701245000341 ) ) ;
#42957=CARTESIAN_POINT ( 'NONE',  ( 12.00000000000000000, -23.25000000000000000, 0.000000000000000000 ) ) ;
#42958=CARTESIAN_POINT ( 'NONE',  ( 1.382886570147999983, -61.43098219798999793, 12.65982054480000052 ) ) ;
#42959=DIRECTION ( 'NONE',  ( -0.7071067811865475727, 0.000000000000000000, 0.7071067811865475727 ) ) ;
#42962=CARTESIAN_POINT ( 'NONE',  ( -0.3136163193838756302, -76.32274192230099175, -11.74634812822112373 ) ) ;
#42966=LINE ( 'NONE', #7810, #33907 ) ;
#42973=EDGE_CURVE ( 'NONE', #47711, #45259, #53033, .T. ) ;
#42975=CARTESIAN_POINT ( 'NONE',  ( 13.89999999928999941, -5.999999999291000030, 8.437407073926000296E-09 ) ) ;
#42978=CARTESIAN_POINT ( 'NONE',  ( 26.50000000000000000, -39.49523982883999906, 1.535553829149999833E-05 ) ) ;
#42981=CARTESIAN_POINT ( 'NONE',  ( -3.250000000000000000, -1.500000000000000000, 0.000000000000000000 ) ) ;
#42982=CARTESIAN_POINT ( 'NONE',  ( 7.220923959705269013, -77.47708333333335418, -9.396085398178609438 ) ) ;
#42985=VECTOR ( 'NONE', #590, 1000.000000000000000 ) ;
#42986=ORIENTED_EDGE ( 'NONE', *, *, #1218, .T. ) ;
#42989=ORIENTED_EDGE ( 'NONE', *, *, #2276, .T. ) ;
#42990=CARTESIAN_POINT ( 'NONE',  ( -7.691893942748999180, -57.04546192861999998, 10.42272502865000128 ) ) ;
#42995=AXIS2_PLACEMENT_3D ( 'NONE', #28263, #38590, #24731 ) ;
#43005=DIRECTION ( 'NONE',  ( 0.000000000000000000, -1.000000000000000000, 0.000000000000000000 ) ) ;
#43010=CARTESIAN_POINT ( 'NONE',  ( -13.95956770449999951, -33.08075762116000362, -5.182382777876000184E-05 ) ) ;
#43011=CARTESIAN_POINT ( 'NONE',  ( -12.99510751537000353, -63.10294702886003648, 6.911973076623003642 ) ) ;
#43013=B_SPLINE_CURVE_WITH_KNOTS ( 'NONE', 3,
 ( #7398, #38111, #29532, #19829, #6820, #56990, #43417, #24252, #2698, #20122, #33387, #33677, #48155, #24830, #2122, #42846, #34535, #16552 ),
 .UNSPECIFIED., .F., .F.,
 ( 4, 2, 2, 2, 2, 2, 2, 2, 4 ),
 ( 0.000000000000000000, 0.1250000000000000000, 0.2500000000000000000, 0.3750000000000000000, 0.5000000000000000000, 0.6250000000000000000, 0.7500000000000000000, 0.8750000000000000000, 1.000000000000000000 ),
 .UNSPECIFIED. ) ;
#43015=CARTESIAN_POINT ( 'NONE',  ( 10.53101990620000095, -18.69360215052999763, 7.613962745610000304 ) ) ;
#43016=CARTESIAN_POINT ( 'NONE',  ( -9.783241737811998462, -61.33564621498000946, -7.961026681588999843 ) ) ;
#43020=CARTESIAN_POINT ( 'NONE',  ( 5.715297388934000189, -78.39081763324999486, 11.69132169264999987 ) ) ;
#43021=EDGE_CURVE ( 'NONE', #54392, #43629, #1228, .T. ) ;
#43025=CARTESIAN_POINT ( 'NONE',  ( 11.80084191424000117, -76.30738641031999236, -3.682937823519999654 ) ) ;
#43028=DIRECTION ( 'NONE',  ( -1.000000000000000000, 0.000000000000000000, 0.000000000000000000 ) ) ;
#43029=CARTESIAN_POINT ( 'NONE',  ( -1.001315002179000047, -24.68522411714000242, 12.50000000000000000 ) ) ;
#43030=CARTESIAN_POINT ( 'NONE',  ( -10.43921282250999916, -78.53242462859000739, 7.393929757317000195 ) ) ;
#43031=CARTESIAN_POINT ( 'NONE',  ( 12.72397198031000087, -55.57854962903999763, -1.930909771329999858 ) ) ;
#43035=CARTESIAN_POINT ( 'NONE',  ( 10.35453599130000057, -76.75783510652000530, -6.064947188958000446 ) ) ;
#43036=VERTEX_POINT ( 'NONE', #21371 ) ;
#43037=VECTOR ( 'NONE', #39011, 1000.000000000000227 ) ;
#43041=VECTOR ( 'NONE', #58186, 1000.000000000000114 ) ;
#43044=AXIS2_PLACEMENT_3D ( 'NONE', #36393, #49701, #53529 ) ;
#43046=EDGE_CURVE ( 'NONE', #51486, #44855, #27748, .T. ) ;
#43058=EDGE_LOOP ( 'NONE', ( #32562, #19176, #8348, #58400 ) ) ;
#43059=CARTESIAN_POINT ( 'NONE',  ( 0.4482635754052999855, -78.67790996937631576, -12.25553529036999834 ) ) ;
#43060=EDGE_CURVE ( 'NONE', #54702, #53710, #46491, .T. ) ;
#43062=CARTESIAN_POINT ( 'NONE',  ( 7.605690612596999856, -55.37434870709000023, 10.52682230156000109 ) ) ;
#43063=CARTESIAN_POINT ( 'NONE',  ( 9.998734510692498745, -54.87263061026122557, 7.709128441167307777 ) ) ;
#43070=CARTESIAN_POINT ( 'NONE',  ( -7.762981007049000404, -24.16089459216999913, 9.992000916352999695 ) ) ;
#43071=VECTOR ( 'NONE', #30031, 1000.000000000000000 ) ;
#43075=CARTESIAN_POINT ( 'NONE',  ( 9.934814764497000183, -61.42368287795999748, -7.968971842771999547 ) ) ;
#43076=CARTESIAN_POINT ( 'NONE',  ( 4.750030159171999777, -78.60465007998999454, -11.30647155123999958 ) ) ;
#43077=DIRECTION ( 'NONE',  ( 0.000000000000000000, 0.000000000000000000, 1.000000000000000000 ) ) ;
#43080=CARTESIAN_POINT ( 'NONE',  ( 12.54238283046685076, -23.52853599825469644, -1.749799162367749794 ) ) ;
#43082=AXIS2_PLACEMENT_3D ( 'NONE', #57656, #12215, #30496 ) ;
#43085=DIRECTION ( 'NONE',  ( 0.7071067811865474617, 0.000000000000000000, -0.7071067811865474617 ) ) ;
#43086=CARTESIAN_POINT ( 'NONE',  ( 1.667260628941999778, -23.20942012473999938, 12.49858003894999925 ) ) ;
#43088=CARTESIAN_POINT ( 'NONE',  ( 2.583380683670000177, -3.278869571379000369, 2.446142499428999972 ) ) ;
#43089=EDGE_CURVE ( 'NONE', #7256, #10595, #3111, .T. ) ;
#43092=CARTESIAN_POINT ( 'NONE',  ( -8.079589622638239987, -76.13532046087181016, 8.532035202244687255 ) ) ;
#43098=FACE_OUTER_BOUND ( 'NONE', #21279, .T. ) ;
#43101=FACE_OUTER_BOUND ( 'NONE', #28497, .T. ) ;
#43102=CARTESIAN_POINT ( 'NONE',  ( -9.422842877325999567, -62.05952027250000214, 8.643944052328999206 ) ) ;
#43107=VERTEX_POINT ( 'NONE', #9260 ) ;
#43114=CARTESIAN_POINT ( 'NONE',  ( -0.2494208075201428676, -53.80711039216416225, -12.50614183109633260 ) ) ;
#43115=CARTESIAN_POINT ( 'NONE',  ( 12.50483465198240474, -61.66452578640149085, 0.6958747608065251056 ) ) ;
#43121=AXIS2_PLACEMENT_3D ( 'NONE', #34511, #42533, #24520 ) ;
#43127=EDGE_CURVE ( 'NONE', #48625, #23001, #18153, .T. ) ;
#43130=CARTESIAN_POINT ( 'NONE',  ( 7.660431561281999535, -18.80820826823000047, 10.01749754194999831 ) ) ;
#43132=CARTESIAN_POINT ( 'NONE',  ( 1.689459950984219860, -54.50811746068924180, 12.71013585606941376 ) ) ;
#43133=CARTESIAN_POINT ( 'NONE',  ( 7.167851722631999323, -78.34084413521999579, -10.60335505485999974 ) ) ;
#43135=DIRECTION ( 'NONE',  ( -1.000000000000000000, 0.000000000000000000, 0.000000000000000000 ) ) ;
#43146=EDGE_CURVE ( 'NONE', #49897, #19229, #31078, .T. ) ;
#43147=FACE_OUTER_BOUND ( 'NONE', #379, .T. ) ;
#43149=CARTESIAN_POINT ( 'NONE',  ( -7.640030139758000161, -18.69283065396999888, 10.18491068059999805 ) ) ;
#43153=CARTESIAN_POINT ( 'NONE',  ( 0.000000000000000000, 4.040000000000000036, 0.000000000000000000 ) ) ;
#43161=AXIS2_PLACEMENT_3D ( 'NONE', #49683, #9228, #27214 ) ;
#43163=CARTESIAN_POINT ( 'NONE',  ( 0.9301983931536133010, -2.396301603284799242, -3.396501321809576091 ) ) ;
#43168=CARTESIAN_POINT ( 'NONE',  ( -7.648026768024999811, -18.75000001589999954, 10.12290050218000026 ) ) ;
#43172=ADVANCED_FACE ( 'NONE', ( #4539 ), #57742, .F. ) ;
#43173=CARTESIAN_POINT ( 'NONE',  ( -10.07627163191000008, -60.04999999725999515, -7.601397897754999633 ) ) ;
#43178=CARTESIAN_POINT ( 'NONE',  ( 10.42531125070999920, -60.06485145371000556, -7.624341767111000756 ) ) ;
#43181=CARTESIAN_POINT ( 'NONE',  ( 7.247844507162001015, -60.04999999966999980, -9.722718241315000398 ) ) ;
#43182=CARTESIAN_POINT ( 'NONE',  ( -9.175573575496970946, -62.02695822328879416, 8.792784719842536845 ) ) ;
#43183=VERTEX_POINT ( 'NONE', #40843 ) ;
#43185=AXIS2_PLACEMENT_3D ( 'NONE', #28939, #54937, #37506 ) ;
#43186=CARTESIAN_POINT ( 'NONE',  ( 0.01090852172292994249, -75.80000000000002558, -11.82854724701027038 ) ) ;
#43187=ADVANCED_FACE ( 'NONE', ( #36117 ), #9447, .F. ) ;
#43189=LINE ( 'NONE', #20742, #23623 ) ;
#43190=CARTESIAN_POINT ( 'NONE',  ( 7.247844507162001015, -23.25000000000000000, -9.722718241315000398 ) ) ;
#43193=DIRECTION ( 'NONE',  ( -2.582621269620000094E-11, 0.000000000000000000, 1.000000000000000000 ) ) ;
#43196=CARTESIAN_POINT ( 'NONE',  ( -3.075537641221584018, -76.19583333333332575, 11.44417895085269876 ) ) ;
#43198=ORIENTED_EDGE ( 'NONE', *, *, #36664, .F. ) ;
#43199=CARTESIAN_POINT ( 'NONE',  ( -12.77656766269999977, -53.48801851230000182, -0.1555695072194999973 ) ) ;
#43200=EDGE_LOOP ( 'NONE', ( #27703, #56199, #24030, #31539 ) ) ;
#43204=FACE_OUTER_BOUND ( 'NONE', #1971, .T. ) ;
#43207=ORIENTED_EDGE ( 'NONE', *, *, #43545, .F. ) ;
#43211=CARTESIAN_POINT ( 'NONE',  ( 10.12290050124000018, -23.24999999991999644, 7.648026767085999822 ) ) ;
#43214=VECTOR ( 'NONE', #33143, 1000.000000000000000 ) ;
#43215=EDGE_CURVE ( 'NONE', #57279, #30548, #51164, .T. ) ;
#43216=CARTESIAN_POINT ( 'NONE',  ( 8.266617305387050862, -61.77234527411995657, 9.697375114829227982 ) ) ;
#43220=CARTESIAN_POINT ( 'NONE',  ( 1.980584515756000030, -60.06485150062000145, 12.76303204342999997 ) ) ;
#43225=CARTESIAN_POINT ( 'NONE',  ( 2.062597265787999845, -19.21538333566000034, -12.87024489160000051 ) ) ;
#43226=CARTESIAN_POINT ( 'NONE',  ( 0.000000000000000000, 4.040000000000000036, 0.000000000000000000 ) ) ;
#43227=CARTESIAN_POINT ( 'NONE',  ( 2.015551294784000191, -18.19652295155999866, -12.79857978895000059 ) ) ;
#43228=CARTESIAN_POINT ( 'NONE',  ( 3.250000000000000000, -1.350000000000000089, 0.000000000000000000 ) ) ;
#43230=CARTESIAN_POINT ( 'NONE',  ( -1.568660613942000071, -1.943195589986999927, -3.467930652269000102 ) ) ;
#43231=CARTESIAN_POINT ( 'NONE',  ( 3.440865526187972367, -0.9821531737497413150, -0.7873258519433958824 ) ) ;
#43232=ORIENTED_EDGE ( 'NONE', *, *, #2465, .F. ) ;
#43234=EDGE_CURVE ( 'NONE', #49658, #54222, #33213, .T. ) ;
#43235=CARTESIAN_POINT ( 'NONE',  ( 5.940599228801999379E-14, -5.950000000028910385, 0.000000000000000000 ) ) ;
#43236=CARTESIAN_POINT ( 'NONE',  ( -12.56594317825999951, -60.05000001354000005, 1.750000000000000000 ) ) ;
#43238=CARTESIAN_POINT ( 'NONE',  ( 1.354019794466000182, -1.887630151311999960, 3.211827542139999991 ) ) ;
#43251=CARTESIAN_POINT ( 'NONE',  ( 7.991295277419832921, -76.38438841642825139, -8.615442090525050389 ) ) ;
#43256=CARTESIAN_POINT ( 'NONE',  ( 12.76303204294999993, -23.26485150694999859, -1.980584515756000030 ) ) ;
#43257=CARTESIAN_POINT ( 'NONE',  ( -0.001508081476238588370, -3.476049081606229052, 3.262047271239970847 ) ) ;
#43260=CARTESIAN_POINT ( 'NONE',  ( 8.038883227244705054, -75.79999999999998295, 8.916086791020916280 ) ) ;
#43265=ORIENTED_EDGE ( 'NONE', *, *, #7728, .F. ) ;
#43266=CARTESIAN_POINT ( 'NONE',  ( 7.678657038161719406, -60.59377623463995377, 10.03844138482045523 ) ) ;
#43267=EDGE_CURVE ( 'NONE', #3300, #25746, #27827, .T. ) ;
#43268=ORIENTED_EDGE ( 'NONE', *, *, #37608, .F. ) ;
#43269=VERTEX_POINT ( 'NONE', #28117 ) ;
#43270=CARTESIAN_POINT ( 'NONE',  ( -1.997276839918484148, -1.427083333333333259, 2.598917237794077018 ) ) ;
#43275=ORIENTED_EDGE ( 'NONE', *, *, #42729, .F. ) ;
#43277=CARTESIAN_POINT ( 'NONE',  ( 1.026866341085000007E-14, -0.1000000000000002554, 0.000000000000000000 ) ) ;
#43278=ORIENTED_EDGE ( 'NONE', *, *, #11514, .T. ) ;
#43279=DIRECTION ( 'NONE',  ( 0.000000000000000000, -1.000000000000000000, 6.735201558252998979E-11 ) ) ;
#43281=CARTESIAN_POINT ( 'NONE',  ( -10.98465012826174281, -18.69514063119217795, 0.5809631169955963292 ) ) ;
#43284=VECTOR ( 'NONE', #22657, 1000.000000000000114 ) ;
#43291=CIRCLE ( 'NONE', #2753, 0.5000000000000006661 ) ;
#43293=CARTESIAN_POINT ( 'NONE',  ( 2.156866207458188356, -2.917591387413716486, 2.431545018423679316 ) ) ;
#43300=CARTESIAN_POINT ( 'NONE',  ( 10.35845616727999996, -23.29778595484999926, 7.627487606609999915 ) ) ;
#43302=ADVANCED_FACE ( 'NONE', ( #6574 ), #54932, .F. ) ;
#43303=CYLINDRICAL_SURFACE ( 'NONE', #17571, 1.750000000000001332 ) ;
#43307=CARTESIAN_POINT ( 'NONE',  ( -9.234979314279001983, -77.11421089111999549, -9.168119495123999485 ) ) ;
#43309=CARTESIAN_POINT ( 'NONE',  ( 0.000000000000000000, -46.43897132165000130, 0.000000000000000000 ) ) ;
#43310=CARTESIAN_POINT ( 'NONE',  ( -9.882566678146000427, -76.71850902869999800, -7.174148702167999936 ) ) ;
#43311=ORIENTED_EDGE ( 'NONE', *, *, #32265, .T. ) ;
#43316=CARTESIAN_POINT ( 'NONE',  ( 10.87611295313000070, -78.78733180935000746, -6.736118790891999275 ) ) ;
#43317=CARTESIAN_POINT ( 'NONE',  ( -1.667916687244999974, -18.70150862776000267, -12.49168433580000048 ) ) ;
#43320=CARTESIAN_POINT ( 'NONE',  ( -13.00000000000000000, -6.000000000000000000, 0.000000000000000000 ) ) ;
#43322=ORIENTED_EDGE ( 'NONE', *, *, #13088, .F. ) ;
#43324=VECTOR ( 'NONE', #25548, 1000.000000000000114 ) ;
#43328=CARTESIAN_POINT ( 'NONE',  ( -8.190859204290999784, -55.64999999967000122, -7.342331066867000544 ) ) ;
#43331=ORIENTED_EDGE ( 'NONE', *, *, #51494, .T. ) ;
#43332=ORIENTED_EDGE ( 'NONE', *, *, #49299, .F. ) ;
#43333=AXIS2_PLACEMENT_3D ( 'NONE', #52991, #8114, #16692 ) ;
#43335=CARTESIAN_POINT ( 'NONE',  ( 7.216918803465672383, -78.02046273671660970, 9.394863879516428540 ) ) ;
#43338=CARTESIAN_POINT ( 'NONE',  ( 0.4257466702800756231, -2.465754650056851904, 3.247861184464477802 ) ) ;
#43340=CARTESIAN_POINT ( 'NONE',  ( 11.03890801094999929, -78.76413212360631633, -5.342433469444999972 ) ) ;
#43342=ADVANCED_FACE ( 'NONE', ( #24292 ), #5985, .F. ) ;
#43343=CARTESIAN_POINT ( 'NONE',  ( 7.760941378042000238, -54.56914109158999793, 10.15321372494000052 ) ) ;
#43344=CARTESIAN_POINT ( 'NONE',  ( 10.03847181063950345, -55.00634590446509264, 7.678636148863391853 ) ) ;
#43345=CARTESIAN_POINT ( 'NONE',  ( 1.980584515756000030, -60.06485150062000145, 12.76303204342999997 ) ) ;
#43350=CARTESIAN_POINT ( 'NONE',  ( -1.771468677314999907, -75.83449150267999528, 12.18184739844999953 ) ) ;
#43353=DIRECTION ( 'NONE',  ( 9.217554798189211692E-07, 4.180954627647226425E-20, -0.9999999999995752287 ) ) ;
#43354=CARTESIAN_POINT ( 'NONE',  ( -12.26143800982999998, -78.94953869689999237, -0.2371146996492999870 ) ) ;
#43355=CARTESIAN_POINT ( 'NONE',  ( 12.50000000000000000, -54.11640971901999819, -1.003652782195000093 ) ) ;
#43357=CYLINDRICAL_SURFACE ( 'NONE', #23894, 1.750000000000000000 ) ;
#43359=EDGE_CURVE ( 'NONE', #25591, #17264, #5407, .T. ) ;
#43360=CARTESIAN_POINT ( 'NONE',  ( 12.61112459821999998, -60.01565178538000112, -1.798929298655999931 ) ) ;
#43362=AXIS2_PLACEMENT_3D ( 'NONE', #46830, #51832, #20238 ) ;
#43364=CARTESIAN_POINT ( 'NONE',  ( 2.095072722873000171, -3.738360633964000090, -2.362033056849000445 ) ) ;
#43365=AXIS2_PLACEMENT_3D ( 'NONE', #9494, #27184, #26318 ) ;
#43371=ORIENTED_EDGE ( 'NONE', *, *, #32547, .F. ) ;
#43372=CARTESIAN_POINT ( 'NONE',  ( -10.55911395186000057, -22.78461666469000235, -7.642160924865000204 ) ) ;
#43374=B_SPLINE_CURVE_WITH_KNOTS ( 'NONE', 3,
 ( #1889, #50309, #15448, #46471, #14851, #32845 ),
 .UNSPECIFIED., .F., .F.,
 ( 4, 1, 1, 4 ),
 ( 0.000000000000000000, 0.3333333333333000081, 0.6666666666667000474, 1.000000000000000000 ),
 .UNSPECIFIED. ) ;
#43376=EDGE_CURVE ( 'NONE', #891, #21680, #41857, .T. ) ;
#43378=CARTESIAN_POINT ( 'NONE',  ( -9.317978910689999950, -61.93238462986000314, 8.588869595475999930 ) ) ;
#43379=DIRECTION ( 'NONE',  ( -0.6562721000562879992, 0.7545243075525860377, 7.877492217643861041E-10 ) ) ;
#43381=CARTESIAN_POINT ( 'NONE',  ( -3.600000000000000089, -0.6500000000000000222, 0.000000000000000000 ) ) ;
#43383=ORIENTED_EDGE ( 'NONE', *, *, #738, .T. ) ;
#43384=CARTESIAN_POINT ( 'NONE',  ( 7.764010764699802891, -24.12280919934631029, -9.931043767183597382 ) ) ;
#43387=CARTESIAN_POINT ( 'NONE',  ( -10.01332852690999964, -60.08056535122999975, -7.654537165486999584 ) ) ;
#43390=AXIS2_PLACEMENT_3D ( 'NONE', #40278, #17852, #35841 ) ;
#43391=CARTESIAN_POINT ( 'NONE',  ( -12.50239399162999909, -54.11640749821000185, 1.003653728895000041 ) ) ;
#43394=EDGE_CURVE ( 'NONE', #34855, #525, #16470, .T. ) ;
#43397=ORIENTED_EDGE ( 'NONE', *, *, #27017, .F. ) ;
#43398=ORIENTED_EDGE ( 'NONE', *, *, #49858, .F. ) ;
#43403=CARTESIAN_POINT ( 'NONE',  ( 8.652389292596000203, -16.73734871878000163, 9.414476472810001439 ) ) ;
#43404=EDGE_CURVE ( 'NONE', #2471, #47498, #3213, .T. ) ;
#43406=LINE ( 'NONE', #3539, #18798 ) ;
#43409=CARTESIAN_POINT ( 'NONE',  ( 11.74505801343999956, -76.86614726144999565, 5.470698999298999610 ) ) ;
#43410=EDGE_CURVE ( 'NONE', #5204, #52919, #38057, .T. ) ;
#43417=CARTESIAN_POINT ( 'NONE',  ( 9.064753713361380250, -78.10522340434667399, 7.545303945706750781 ) ) ;
#43422=PLANE ( 'NONE',  #41811 ) ;
#43426=CARTESIAN_POINT ( 'NONE',  ( 0.000000000000000000, -0.09999999858569999511, 0.000000000000000000 ) ) ;
#43427=DIRECTION ( 'NONE',  ( -1.000000000000000000, 0.000000000000000000, 0.000000000000000000 ) ) ;
#43428=CARTESIAN_POINT ( 'NONE',  ( 0.000000000000000000, -4.000000000000000000, 0.000000000000000000 ) ) ;
#43429=CARTESIAN_POINT ( 'NONE',  ( -7.653559502277999194, -18.70150862776000267, 10.01234990228999955 ) ) ;
#43430=B_SPLINE_SURFACE_WITH_KNOTS ( 'NONE', 3, 3, ( 
 ( #11004, #47319, #28988, #51451 ),
 ( #2148, #38136, #15708, #33703 ),
 ( #56447, #51742, #11291, #29271 ),
 ( #6848, #24858, #42874, #38429 ),
 ( #16002, #33989, #52028, #39585 ),
 ( #40465, #32385, #21580, #13293 ),
 ( #35424, #50429, #18032, #35728 ),
 ( #52882, #57882, #44025, #44897 ),
 ( #34850, #30709, #12435, #30428 ),
 ( #4450, #21860, #31286, #54051 ),
 ( #3862, #3576, #9979, #14385 ),
 ( #53756, #49330, #30996, #53454 ),
 ( #39869, #57, #48460, #17438 ),
 ( #48746, #43744, #12998, #17150 ),
 ( #17740, #3297, #49034, #8875 ),
 ( #8581, #26569, #8003, #21289 ),
 ( #35136, #26870, #57589, #53167 ) ),
 .UNSPECIFIED., .F., .F., .F.,
 ( 4, 1, 1, 1, 1, 1, 1, 1, 1, 1, 1, 1, 1, 1, 4 ),
 ( 4, 4 ),
 ( -0.01011408452864000045, 0.000000000000000000, 0.08333333333333001192, 0.1666666666667000196, 0.2500000000000000000, 0.3333333333333000081, 0.4166666666666999919, 0.5000000000000000000, 0.5833333333333000637, 0.6666666666667000474, 0.7500000000000000000, 0.8333333333333000637, 0.9166666666667000474, 1.000000000000000000, 1.010362559107000013 ),
 ( -0.3559705546267999954, 1.357612419580000118 ),
 .UNSPECIFIED. ) ;
#43433=CARTESIAN_POINT ( 'NONE',  ( -3.250000000000000000, -1.500000000000000000, 0.000000000000000000 ) ) ;
#43435=CIRCLE ( 'NONE', #10447, 1.250000000000000000 ) ;
#43436=ORIENTED_EDGE ( 'NONE', *, *, #14, .T. ) ;
#43438=EDGE_CURVE ( 'NONE', #28634, #36787, #16017, .T. ) ;
#43442=CARTESIAN_POINT ( 'NONE',  ( -12.70556836329126504, -16.77227722666621901, 0.2641978056568241029 ) ) ;
#43444=CARTESIAN_POINT ( 'NONE',  ( 0.2474615858699362181, -1.880639237606296144, -3.511584093533194117 ) ) ;
#43449=CARTESIAN_POINT ( 'NONE',  ( 11.53347032108356451, -75.96504513096159883, 2.244556689769372948 ) ) ;
#43451=VERTEX_POINT ( 'NONE', #39025 ) ;
#43452=CARTESIAN_POINT ( 'NONE',  ( 10.98362417419999915, -18.84999999999999787, -0.5999999999999999778 ) ) ;
#43453=DIRECTION ( 'NONE',  ( 1.000000000000000000, 0.000000000000000000, 0.000000000000000000 ) ) ;
#43457=B_SPLINE_CURVE_WITH_KNOTS ( 'NONE', 3,
 ( #23470, #1351, #29063, #47105, #6341, #50651, #55355, #6637, #1642, #19055, #24643, #10197, #19345, #37340, #46521, #6046, #19632, #34640, #21361, #47686, #2505 ),
 .UNSPECIFIED., .F., .F.,
 ( 4, 2, 2, 1, 1, 2, 2, 1, 1, 1, 2, 2, 4 ),
 ( 0.000000000000000000, 0.1250000000000000278, 0.2500000000000000555, 0.3750000000000001110, 0.4375000000000001110, 0.4687500000000001110, 0.5000000000000001110, 0.6250000000000002220, 0.6875000000000002220, 0.7187500000000002220, 0.7343750000000001110, 0.7500000000000000000, 1.000000000000000000 ),
 .UNSPECIFIED. ) ;
#43461=CARTESIAN_POINT ( 'NONE',  ( 10.53562597589000127, -23.20558297624999966, -7.620013358880999732 ) ) ;
#43464=LINE ( 'NONE', #24291, #7245 ) ;
#43466=CARTESIAN_POINT ( 'NONE',  ( -10.10447584125107845, -61.25118490511745506, 7.864774383105175737 ) ) ;
#43467=EDGE_LOOP ( 'NONE', ( #53263, #58209, #48862 ) ) ;
#43468=AXIS2_PLACEMENT_3D ( 'NONE', #9325, #27316, #4898 ) ;
#43471=CARTESIAN_POINT ( 'NONE',  ( 10.13881649148000008, -76.50783510652000530, -5.938594122520999719 ) ) ;
#43473=CYLINDRICAL_SURFACE ( 'NONE', #33978, 0.5000000000000004441 ) ;
#43474=CARTESIAN_POINT ( 'NONE',  ( 3.075537641221509411, -77.65416666666668277, 11.44417895085272008 ) ) ;
#43479=FACE_OUTER_BOUND ( 'NONE', #15746, .T. ) ;
#43480=CARTESIAN_POINT ( 'NONE',  ( -12.50000000000000000, -39.30476017083000073, 0.000000000000000000 ) ) ;
#43481=ORIENTED_EDGE ( 'NONE', *, *, #50662, .T. ) ;
#43484=CARTESIAN_POINT ( 'NONE',  ( 0.000000000000000000, 0.000000000000000000, 0.000000000000000000 ) ) ;
#43485=ORIENTED_EDGE ( 'NONE', *, *, #49017, .F. ) ;
#43486=ORIENTED_EDGE ( 'NONE', *, *, #50654, .T. ) ;
#43490=EDGE_CURVE ( 'NONE', #37470, #43629, #16403, .T. ) ;
#43492=DIRECTION ( 'NONE',  ( 1.000000000000000000, 0.000000000000000000, 0.000000000000000000 ) ) ;
#43493=EDGE_LOOP ( 'NONE', ( #19440, #47209, #47131, #53906, #9220 ) ) ;
#43494=ORIENTED_EDGE ( 'NONE', *, *, #25360, .F. ) ;
#43496=AXIS2_PLACEMENT_3D ( 'NONE', #42746, #11454, #33576 ) ;
#43498=CARTESIAN_POINT ( 'NONE',  ( -12.54901606610000009, -61.80731603467000213, -0.4733145588201999598 ) ) ;
#43501=CARTESIAN_POINT ( 'NONE',  ( 14.00000000000000000, -32.70420297070000260, 0.000000000000000000 ) ) ;
#43502=DIRECTION ( 'NONE',  ( 0.000000000000000000, -1.000000000000000000, 0.000000000000000000 ) ) ;
#43503=CARTESIAN_POINT ( 'NONE',  ( -10.53101998747000145, -18.69360374348000065, 7.613962827178999859 ) ) ;
#43505=B_SPLINE_SURFACE_WITH_KNOTS ( 'NONE', 3, 3, ( 
 ( #39634, #11917, #8055, #34041 ),
 ( #11348, #16923, #52079, #26050 ),
 ( #3345, #11637, #29612, #16633 ),
 ( #47667, #39353, #30482, #16350 ),
 ( #34902, #52646, #34330, #57642 ),
 ( #7193, #17196, #29326, #30186 ),
 ( #47373, #21341, #52365, #57360 ),
 ( #29895, #6903, #12201, #7483 ) ),
 .UNSPECIFIED., .F., .F., .F.,
 ( 4, 1, 1, 1, 1, 4 ),
 ( 4, 4 ),
 ( -0.01200407347462999902, 0.000000000000000000, 0.3333333333333000081, 0.6666666666667000474, 1.000000000000000000, 1.011997855551999947 ),
 ( -0.3559705542741000150, 1.355970554273999928 ),
 .UNSPECIFIED. ) ;
#43507=CARTESIAN_POINT ( 'NONE',  ( 1.980584515752000119, -55.53514853344000102, 12.76303204600000107 ) ) ;
#43508=ORIENTED_EDGE ( 'NONE', *, *, #4383, .F. ) ;
#43512=CARTESIAN_POINT ( 'NONE',  ( -10.53495272788999948, -18.77289072628000355, -7.618387390369000478 ) ) ;
#43513=CARTESIAN_POINT ( 'NONE',  ( 7.678690995233999672, -57.04351820043999766, 10.59551070214999946 ) ) ;
#43514=CARTESIAN_POINT ( 'NONE',  ( -0.5154756746316999649, -16.86759400236999795, -12.66205448072999928 ) ) ;
#43519=CARTESIAN_POINT ( 'NONE',  ( -0.1115855426138554346, -3.500000000000000000, 3.288764228670495449 ) ) ;
#43520=CARTESIAN_POINT ( 'NONE',  ( 3.018788407823380648, -1.457011938536811657, -1.814601626188562689 ) ) ;
#43521=VERTEX_POINT ( 'NONE', #12164 ) ;
#43524=CARTESIAN_POINT ( 'NONE',  ( -12.64500484465999897, -19.22847221992000044, 1.799490225533999732 ) ) ;
#43525=CARTESIAN_POINT ( 'NONE',  ( 2.602549234900000119, -3.533626866276999845, 2.777463315117000064 ) ) ;
#43526=AXIS2_PLACEMENT_3D ( 'NONE', #45889, #10156, #14564 ) ;
#43528=CARTESIAN_POINT ( 'NONE',  ( -12.49996905247000001, -55.60797343434000339, 1.666511841116000037 ) ) ;
#43529=DIRECTION ( 'NONE',  ( 0.000000000000000000, 1.000000000000000000, 0.000000000000000000 ) ) ;
#43531=CYLINDRICAL_SURFACE ( 'NONE', #32940, 1.750000000000000000 ) ;
#43534=CARTESIAN_POINT ( 'NONE',  ( 5.291843864070292724, -76.36141765332132536, -10.52905727750688847 ) ) ;
#43537=CARTESIAN_POINT ( 'NONE',  ( 7.648026768019999366, -23.24999998419999869, 10.12290050217000115 ) ) ;
#43538=FACE_OUTER_BOUND ( 'NONE', #54730, .T. ) ;
#43540=CARTESIAN_POINT ( 'NONE',  ( -0.4254240051736147277, -2.614583333333332149, -3.250000000000000888 ) ) ;
#43542=CARTESIAN_POINT ( 'NONE',  ( 1.250000000000000000, -23.25000000000000000, -12.50000000000000000 ) ) ;
#43543=CARTESIAN_POINT ( 'NONE',  ( -7.861037107735485030, -17.53338873151346178, -10.10708465679509160 ) ) ;
#43545=EDGE_CURVE ( 'NONE', #55842, #57192, #57037, .T. ) ;
#43546=VERTEX_POINT ( 'NONE', #33721 ) ;
#43548=CARTESIAN_POINT ( 'NONE',  ( -9.722718241315000398, -55.54999999966999980, 7.954951288349001004 ) ) ;
#43553=ORIENTED_EDGE ( 'NONE', *, *, #46771, .F. ) ;
#43555=CARTESIAN_POINT ( 'NONE',  ( 3.500000000000000444, -3.500000000000000444, -0.3803866565412687417 ) ) ;
#43560=ORIENTED_EDGE ( 'NONE', *, *, #15032, .F. ) ;
#43563=B_SPLINE_CURVE_WITH_KNOTS ( 'NONE', 3,
 ( #55019, #50606, #10155, #5709, #19302, #16898 ),
 .UNSPECIFIED., .F., .F.,
 ( 4, 1, 1, 4 ),
 ( 0.000000000000000000, 0.3333333333333000081, 0.6666666666667000474, 0.9999998688569559091 ),
 .UNSPECIFIED. ) ;
#43564=ORIENTED_EDGE ( 'NONE', *, *, #8592, .T. ) ;
#43573=EDGE_CURVE ( 'NONE', #24318, #22028, #36850, .T. ) ;
#43574=CARTESIAN_POINT ( 'NONE',  ( -11.87500000004000000, -79.12500000004000356, -1.061343742159000057E-08 ) ) ;
#43582=CARTESIAN_POINT ( 'NONE',  ( -2.342324693664710189, -3.039369196919617711, 2.252836536559642333 ) ) ;
#43587=CARTESIAN_POINT ( 'NONE',  ( -0.6934022908089999548, -3.172245813181999718, 3.742362521638999961 ) ) ;
#43588=CARTESIAN_POINT ( 'NONE',  ( 10.01235002622999914, -23.29848884437999956, 7.653559626096999580 ) ) ;
#43589=CARTESIAN_POINT ( 'NONE',  ( -8.284635637516000628, -61.84861451525000575, -9.778492910201000754 ) ) ;
#43590=VECTOR ( 'NONE', #23270, 1000.000000000000000 ) ;
#43593=CARTESIAN_POINT ( 'NONE',  ( 7.342331066867000544, -59.94999999967000548, -8.190859204290999784 ) ) ;
#43594=CARTESIAN_POINT ( 'NONE',  ( 11.79660191402999914, -76.80202101964999883, 5.494707494196000575 ) ) ;
#43596=TOROIDAL_SURFACE ( 'NONE', #11576, 1.250000000000000000, 0.5000000000000000000 ) ;
#43598=CARTESIAN_POINT ( 'NONE',  ( 1.749899258077701747, -23.38716848762994616, -12.55433901290728826 ) ) ;
#43599=CARTESIAN_POINT ( 'NONE',  ( 3.798386035105999703, -75.73131215493000923, -11.76423408806999937 ) ) ;
#43600=VERTEX_POINT ( 'NONE', #49935 ) ;
#43604=B_SPLINE_CURVE_WITH_KNOTS ( 'NONE', 3,
 ( #20454, #56467, #16021, #52045, #25160, #43186, #40772, #366, #30728, #18346, #40481, #57607, #74, #22469, #35744, #12734, #40181, #52902, #22173, #53775, #44324, #13311, #48478, #18053, #49348, #48763 ),
 .UNSPECIFIED., .F., .F.,
 ( 4, 2, 2, 2, 2, 2, 1, 2, 2, 1, 2, 2, 2, 4 ),
 ( 0.000000000000000000, 0.06250000000000009714, 0.1250000000000001943, 0.2500000000000003331, 0.3750000000000004441, 0.5000000000000005551, 0.5625000000000005551, 0.5937500000000004441, 0.6250000000000004441, 0.6875000000000001110, 0.7187500000000000000, 0.7499999999999998890, 0.8750000000000000000, 1.000000000000000000 ),
 .UNSPECIFIED. ) ;
#43606=CARTESIAN_POINT ( 'NONE',  ( 12.59091967951000157, -78.92539409523000415, 1.087091891348999972 ) ) ;
#43607=CARTESIAN_POINT ( 'NONE',  ( -1.931043762602999925, -19.22180874373999870, -12.75761570870000128 ) ) ;
#43617=CARTESIAN_POINT ( 'NONE',  ( 12.49306764013999960, -55.51943464808999806, 1.667917367065999912 ) ) ;
#43619=ORIENTED_EDGE ( 'NONE', *, *, #57353, .T. ) ;
#43621=AXIS2_PLACEMENT_3D ( 'NONE', #55483, #32439, #19181 ) ;
#43623=ORIENTED_EDGE ( 'NONE', *, *, #50786, .F. ) ;
#43625=EDGE_CURVE ( 'NONE', #1897, #55907, #43764, .T. ) ;
#43627=CARTESIAN_POINT ( 'NONE',  ( -11.75000000000000000, -78.20000000000000284, 1.702919296826999607E-14 ) ) ;
#43629=VERTEX_POINT ( 'NONE', #30723 ) ;
#43633=CIRCLE ( 'NONE', #17244, 1.250000000000000000 ) ;
#43634=CARTESIAN_POINT ( 'NONE',  ( 10.13695543446000080, -55.09168900617999753, 7.646071007854999380 ) ) ;
#43635=CARTESIAN_POINT ( 'NONE',  ( 9.713030931733710460, -54.27705886621562570, 7.970419577022584967 ) ) ;
#43636=LINE ( 'NONE', #51645, #18546 ) ;
#43639=B_SPLINE_CURVE_WITH_KNOTS ( 'NONE', 3,
 ( #1284, #51749, #42594, #38146, #37857, #42302, #33422, #46749, #6858, #19563, #50578, #55282, #56168, #2441, #20443, #47328, #23696, #33125 ),
 .UNSPECIFIED., .F., .F.,
 ( 4, 2, 2, 2, 2, 2, 2, 2, 4 ),
 ( 0.000000000000000000, 0.06250000000000620337, 0.1250000000000124067, 0.2500000000000148215, 0.5000000000000133227, 0.7500000000000117684, 0.8125000000000111022, 0.8750000000000104361, 1.000000000000000000 ),
 .UNSPECIFIED. ) ;
#43640=( BOUNDED_SURFACE ( )  B_SPLINE_SURFACE ( 3, 3, ( 
 ( #58144, #3830, #26260, #8260 ),
 ( #35389, #30392, #17711, #17407 ),
 ( #39835, #8847, #26838, #34820 ),
 ( #57848, #12401, #53725, #53420 ),
 ( #30963, #48428, #32361, #3544 ),
 ( #27934, #41237, #49000, #45983 ),
 ( #5509, #8547, #40131, #7970 ) ),
 .UNSPECIFIED., .F., .F., .T. ) 
 B_SPLINE_SURFACE_WITH_KNOTS ( ( 4, 3, 4 ),
 ( 4, 4 ),
 ( 0.000000000000000000, 1.000000000000000000, 2.000000000000000000 ),
 ( 0.000000000000000000, 1.000000000000000000 ),
 .UNSPECIFIED. ) 
 GEOMETRIC_REPRESENTATION_ITEM ( )  RATIONAL_B_SPLINE_SURFACE ( (
 ( 1.196373642248999891, 1.184225762575999985, 1.184225762575999985, 1.196373642248999891),
 ( 0.9447739570234999773, 0.9351807998836999536, 0.9351807998836999536, 0.9447739570234999773),
 ( 0.9447739570234999773, 0.9351807998836999536, 0.9351807998836999536, 0.9447739570234999773),
 ( 1.196373642248999891, 1.184225762575999985, 1.184225762575999985, 1.196373642248999891),
 ( 0.9447739570234999773, 0.9351807998836999536, 0.9351807998836999536, 0.9447739570234999773),
 ( 0.9447739570234999773, 0.9351807998836999536, 0.9351807998836999536, 0.9447739570234999773),
 ( 1.196373642248999891, 1.184225762575999985, 1.184225762575999985, 1.196373642248999891) ) ) 
 REPRESENTATION_ITEM ( '' )  SURFACE ( )  );
#43645=CARTESIAN_POINT ( 'NONE',  ( 9.754023262367999436, -76.14578791229999410, -7.509630405475999915 ) ) ;
#43648=CARTESIAN_POINT ( 'NONE',  ( -12.77562786370999959, -16.73761952138000098, 0.5426593252874999385 ) ) ;
#43652=CARTESIAN_POINT ( 'NONE',  ( 7.601397897754999633, -55.55000000278000272, -10.07627163191000008 ) ) ;
#43655=CARTESIAN_POINT ( 'NONE',  ( 12.82202361519000000, -60.22627773000999696, -2.066043355638000012 ) ) ;
#43656=FACE_OUTER_BOUND ( 'NONE', #53019, .T. ) ;
#43658=CARTESIAN_POINT ( 'NONE',  ( 11.75000000000000000, -76.45000000000000284, 0.000000000000000000 ) ) ;
#43660=CARTESIAN_POINT ( 'NONE',  ( 3.387743934813999935, -3.312748962127999963, 0.3042514350666000178 ) ) ;
#43662=CARTESIAN_POINT ( 'NONE',  ( 0.000000000000000000, -18.84999999999999787, 11.79999999999999893 ) ) ;
#43663=DIRECTION ( 'NONE',  ( 0.000000000000000000, 1.000000000000000000, 0.000000000000000000 ) ) ;
#43668=CARTESIAN_POINT ( 'NONE',  ( -10.53101998747000145, -23.30639625649999758, -7.613962827179999948 ) ) ;
#43669=CIRCLE ( 'NONE', #18224, 12.80000000000000071 ) ;
#43674=CARTESIAN_POINT ( 'NONE',  ( -3.387669551781999910, -1.642803219816000082, -0.5093631002026000054 ) ) ;
#43679=B_SPLINE_CURVE_WITH_KNOTS ( 'NONE', 3,
 ( #53659, #30040, #44505, #30330, #17061, #17642 ),
 .UNSPECIFIED., .F., .F.,
 ( 4, 2, 4 ),
 ( 0.000000000000000000, 0.5000000000000000000, 1.000000000000000000 ),
 .UNSPECIFIED. ) ;
#43680=ADVANCED_FACE ( 'NONE', ( #13307 ), #13600, .T. ) ;
#43681=VECTOR ( 'NONE', #30583, 1000.000000000000000 ) ;
#43682=CARTESIAN_POINT ( 'NONE',  ( -12.70451796512396037, -53.62354927347614364, 0.5205401190852502191 ) ) ;
#43683=PLANE ( 'NONE',  #10372 ) ;
#43692=CARTESIAN_POINT ( 'NONE',  ( 10.14950121160999963, -56.04922972508000356, -7.674627477461999803 ) ) ;
#43693=CARTESIAN_POINT ( 'NONE',  ( 2.062597265787999845, -56.01538333533000014, -12.87024489158000051 ) ) ;
#43694=CARTESIAN_POINT ( 'NONE',  ( -12.80896991328000034, -57.04546192861999998, 1.930989179114000143 ) ) ;
#43699=EDGE_LOOP ( 'NONE', ( #5497, #40211 ) ) ;
#43703=ORIENTED_EDGE ( 'NONE', *, *, #50035, .T. ) ;
#43706=CARTESIAN_POINT ( 'NONE',  ( -3.110005734825000090, -78.15040178014000105, 12.25287980954000133 ) ) ;
#43707=DIRECTION ( 'NONE',  ( -0.7026410690473250398, -0.1122098755728047209, -0.7026410690473250398 ) ) ;
#43708=CARTESIAN_POINT ( 'NONE',  ( -9.050966799188000067, -59.94999999969999749, 7.919595949288999570 ) ) ;
#43710=AXIS2_PLACEMENT_3D ( 'NONE', #2737, #42891, #16886 ) ;
#43711=FACE_OUTER_BOUND ( 'NONE', #21473, .T. ) ;
#43713=ADVANCED_FACE ( 'NONE', ( #35439 ), #4171, .F. ) ;
#43717=VERTEX_POINT ( 'NONE', #13010 ) ;
#43723=AXIS2_PLACEMENT_3D ( 'NONE', #25205, #2780, #52087 ) ;
#43725=CARTESIAN_POINT ( 'NONE',  ( 12.50728313511535816, -53.80024825452284887, -0.1773837592813573005 ) ) ;
#43730=CARTESIAN_POINT ( 'NONE',  ( 10.35845608625999859, -23.29778754190000001, -7.627487525415999947 ) ) ;
#43734=ORIENTED_EDGE ( 'NONE', *, *, #11308, .T. ) ;
#43737=DIRECTION ( 'NONE',  ( 0.000000000000000000, -1.000000000000000000, 0.000000000000000000 ) ) ;
#43744=CARTESIAN_POINT ( 'NONE',  ( -1.890224871708999999, -55.05210751953000425, -12.68696160870999989 ) ) ;
#43745=CARTESIAN_POINT ( 'NONE',  ( -7.710095619854000937, -20.24935285776999905, 10.18496935401000059 ) ) ;
#43746=CARTESIAN_POINT ( 'NONE',  ( 9.815103194665955044, -75.99628344196712249, 6.459577566555076977 ) ) ;
#43749=CARTESIAN_POINT ( 'NONE',  ( 10.98961866300693657, -18.48267221962651163, -0.4810437121500372171 ) ) ;
#43750=CARTESIAN_POINT ( 'NONE',  ( -10.19670478072613307, -77.15724104849601872, 5.890804208869317549 ) ) ;
#43752=DIRECTION ( 'NONE',  ( 0.000000000000000000, 1.000000000000000000, 0.000000000000000000 ) ) ;
#43755=B_SPLINE_CURVE_WITH_KNOTS ( 'NONE', 3,
 ( #51644, #43635, #6752, #43063, #43344, #7042, #56349, #3197 ),
 .UNSPECIFIED., .F., .F.,
 ( 4, 2, 2, 4 ),
 ( 0.000000000000000000, 0.5000000000000000000, 0.7500000000000000000, 1.000000000000000000 ),
 .UNSPECIFIED. ) ;
#43757=CARTESIAN_POINT ( 'NONE',  ( 7.954951288349001004, -55.35321828636000419, -9.722718241315000398 ) ) ;
#43758=CARTESIAN_POINT ( 'NONE',  ( -10.36745710150462507, -60.56601929499609582, 7.635228183650350609 ) ) ;
#43759=ORIENTED_EDGE ( 'NONE', *, *, #17867, .F. ) ;
#43760=ADVANCED_FACE ( 'NONE', ( #45208 ), #45768, .F. ) ;
#43764=CIRCLE ( 'NONE', #55979, 14.00000000000000000 ) ;
#43767=DIRECTION ( 'NONE',  ( 0.000000000000000000, 1.000000000000000000, 0.000000000000000000 ) ) ;
#43772=CARTESIAN_POINT ( 'NONE',  ( 1.799475304559999822, -20.24828923609000242, 12.69616050747999836 ) ) ;
#43776=CARTESIAN_POINT ( 'NONE',  ( -12.43641395959999940, -53.88198970716000247, 0.03481089025435999545 ) ) ;
#43778=ORIENTED_EDGE ( 'NONE', *, *, #20521, .T. ) ;
#43787=VECTOR ( 'NONE', #49296, 1000.000000000000114 ) ;
#43788=ADVANCED_FACE ( 'NONE', ( #3234 ), #34299, .F. ) ;
#43789=EDGE_LOOP ( 'NONE', ( #26426, #36946, #56666, #12096, #38059, #58047 ) ) ;
#43790=ORIENTED_EDGE ( 'NONE', *, *, #55553, .T. ) ;
#43793=ADVANCED_FACE ( 'NONE', ( #34500 ), #51965, .F. ) ;
#43795=CIRCLE ( 'NONE', #18343, 12.50000000000000000 ) ;
#43796=CARTESIAN_POINT ( 'NONE',  ( -12.43647262256999930, -61.71807034702999317, 0.03492325570154000691 ) ) ;
#43800=CARTESIAN_POINT ( 'NONE',  ( -8.838834764832000701, -18.75000000000000000, 8.838834764832000701 ) ) ;
#43801=B_SPLINE_CURVE_WITH_KNOTS ( 'NONE', 3,
 ( #57386, #34926, #21080, #3933, #48534, #53534 ),
 .UNSPECIFIED., .F., .F.,
 ( 4, 1, 1, 4 ),
 ( 0.000000000000000000, 0.3333333333333000081, 0.6666666666667000474, 1.000000000000000000 ),
 .UNSPECIFIED. ) ;
#43803=CARTESIAN_POINT ( 'NONE',  ( 12.66232176275999954, -16.86513311418999805, -0.5079086068997000769 ) ) ;
#43807=CARTESIAN_POINT ( 'NONE',  ( -7.622784390041999814, -55.01288991740999990, 10.47836615824999917 ) ) ;
#43809=CARTESIAN_POINT ( 'NONE',  ( -9.038965287783000235, -16.66737759107000372, -9.029769469460999787 ) ) ;
#43810=CARTESIAN_POINT ( 'NONE',  ( 7.705119999413000187, -58.55171076491000548, 10.24996238027999951 ) ) ;
#43812=ADVANCED_FACE ( 'NONE', ( #7365 ), #47834, .T. ) ;
#43813=CARTESIAN_POINT ( 'NONE',  ( 0.8492415665292510907, -1.247390030182168541, -3.167727707052294228 ) ) ;
#43815=CARTESIAN_POINT ( 'NONE',  ( 12.76303204294000082, -18.73514849292999784, 1.980584515756000030 ) ) ;
#43817=CARTESIAN_POINT ( 'NONE',  ( 0.5420726531984851881, -3.499999999999999556, 3.280180941426340979 ) ) ;
#43819=ORIENTED_EDGE ( 'NONE', *, *, #19051, .T. ) ;
#43821=CARTESIAN_POINT ( 'NONE',  ( -1.374053708643000007E-14, -74.80000000000001137, 0.000000000000000000 ) ) ;
#43822=CARTESIAN_POINT ( 'NONE',  ( -26.49999981590656262, -39.30476017083000073, -0.003123612069538085796 ) ) ;
#43823=CARTESIAN_POINT ( 'NONE',  ( -2.331653612116000307, -3.201240180630999799, -2.802716395477999889 ) ) ;
#43825=CARTESIAN_POINT ( 'NONE',  ( -12.65987793659000005, -53.86302453462000273, 0.9847129294438998759 ) ) ;
#43827=CARTESIAN_POINT ( 'NONE',  ( -1.636740604697537016, -2.018159380161653083, 2.842028451810316270 ) ) ;
#43829=EDGE_CURVE ( 'NONE', #45130, #20752, #33644, .T. ) ;
#43831=DIRECTION ( 'NONE',  ( 0.000000000000000000, 0.000000000000000000, 1.000000000000000000 ) ) ;
#43833=CARTESIAN_POINT ( 'NONE',  ( -11.98222815316549905, -76.96326881833607558, -1.546144727786179951 ) ) ;
#43835=CARTESIAN_POINT ( 'NONE',  ( 10.48850619502800718, -76.41229039468936435, -5.300019550382959466 ) ) ;
#43838=AXIS2_PLACEMENT_3D ( 'NONE', #7108, #2692, #2116 ) ;
#43841=CARTESIAN_POINT ( 'NONE',  ( 3.250000000000000000, -3.350000000000000089, 0.000000000000000000 ) ) ;
#43843=FACE_OUTER_BOUND ( 'NONE', #47182, .T. ) ;
#43846=AXIS2_PLACEMENT_3D ( 'NONE', #45297, #36129, #26669 ) ;
#43849=B_SPLINE_CURVE_WITH_KNOTS ( 'NONE', 3,
 ( #40823, #35791, #18685, #36677, #50565, #27808, #23396, #415, #13947, #5673, #58243, #31944, #17805, #5104, #26933, #49988, #44964, #45855 ),
 .UNSPECIFIED., .F., .F.,
 ( 4, 2, 2, 2, 2, 2, 2, 2, 4 ),
 ( 0.000000000000000000, 0.1250000000000001665, 0.2500000000000002776, 0.3750000000000002776, 0.5000000000000002220, 0.6250000000000001110, 0.7500000000000001110, 0.8750000000000000000, 1.000000000000000000 ),
 .UNSPECIFIED. ) ;
#43852=CARTESIAN_POINT ( 'NONE',  ( -1.003693376014196836, -24.96223992107934109, 12.70247752664746521 ) ) ;
#43853=VERTEX_POINT ( 'NONE', #43381 ) ;
#43854=ORIENTED_EDGE ( 'NONE', *, *, #40836, .F. ) ;
#43855=CARTESIAN_POINT ( 'NONE',  ( 1.636761686205415067, -1.333333333333332815, 2.839805762151342616 ) ) ;
#43856=CARTESIAN_POINT ( 'NONE',  ( -12.50000000000000000, -18.75000000310999937, 1.750000000000000000 ) ) ;
#43859=ORIENTED_EDGE ( 'NONE', *, *, #24901, .T. ) ;
#43860=CARTESIAN_POINT ( 'NONE',  ( -7.826265407172001254, -78.57604920034999907, -9.564588425367000823 ) ) ;
#43861=ORIENTED_EDGE ( 'NONE', *, *, #23941, .T. ) ;
#43863=ORIENTED_EDGE ( 'NONE', *, *, #57812, .F. ) ;
#43867=CARTESIAN_POINT ( 'NONE',  ( 12.00000000000000000, -23.15000000002000036, 0.7999999999999001243 ) ) ;
#43870=CARTESIAN_POINT ( 'NONE',  ( 7.909383950897899140, -79.01041666666978358, 8.790170633244827059 ) ) ;
#43871=CARTESIAN_POINT ( 'NONE',  ( -3.040431873813000063, -78.13870099961999927, 12.26916943822000050 ) ) ;
#43872=VECTOR ( 'NONE', #5475, 1000.000000000000114 ) ;
#43876=AXIS2_PLACEMENT_3D ( 'NONE', #5078, #23370, #964 ) ;
#43878=CARTESIAN_POINT ( 'NONE',  ( -1.247739402645562823, -3.007575997018046454, 3.000140550506007919 ) ) ;
#43882=CARTESIAN_POINT ( 'NONE',  ( 0.04193593611180446157, -25.01009741336668313, -12.50649570005624334 ) ) ;
#43884=CARTESIAN_POINT ( 'NONE',  ( 3.190249742999000215, -1.986765174611999862, -2.075671974272999876 ) ) ;
#43886=CARTESIAN_POINT ( 'NONE',  ( -7.647093862774999806, -60.16895637605999525, -10.00844027277999970 ) ) ;
#43887=EDGE_CURVE ( 'NONE', #22028, #6729, #30068, .T. ) ;
#43890=CARTESIAN_POINT ( 'NONE',  ( -12.77306291386999959, -16.94129324301999873, -1.041150512314999999 ) ) ;
#43891=CARTESIAN_POINT ( 'NONE',  ( 11.85869973992999959, -77.83577122363000456, 5.358216250391999225 ) ) ;
#43892=CARTESIAN_POINT ( 'NONE',  ( 0.000000000000000000, -6.049999999381999949, -13.94999999937999924 ) ) ;
#43893=DIRECTION ( 'NONE',  ( 0.7071067811865975328, 0.7071067811864976127, -1.047750255310995327E-09 ) ) ;
#43894=CARTESIAN_POINT ( 'NONE',  ( -11.70293741273999899, -76.05535392359000468, 3.983108938927999443 ) ) ;
#43897=PLANE ( 'NONE',  #52342 ) ;
#43898=DIRECTION ( 'NONE',  ( 0.000000000000000000, 1.000000000000000000, 0.000000000000000000 ) ) ;
#43899=CARTESIAN_POINT ( 'NONE',  ( 12.66232158689999920, -61.93482640547999551, 0.5080765942054999984 ) ) ;
#43900=CARTESIAN_POINT ( 'NONE',  ( 7.655542440091000600, -19.22180874373999870, -10.38645071870000081 ) ) ;
#43903=CARTESIAN_POINT ( 'NONE',  ( -12.60356226360999798, -22.75077028889999653, 1.750000000000000000 ) ) ;
#43908=ORIENTED_EDGE ( 'NONE', *, *, #29229, .T. ) ;
#43910=ADVANCED_FACE ( 'NONE', ( #21225 ), #39230, .T. ) ;
#43911=CARTESIAN_POINT ( 'NONE',  ( -10.42531125070999920, -60.06485145371000556, 7.624341767111000756 ) ) ;
#43914=ORIENTED_EDGE ( 'NONE', *, *, #45725, .T. ) ;
#43915=EDGE_LOOP ( 'NONE', ( #21455, #54811, #42042, #45834 ) ) ;
#43916=ORIENTED_EDGE ( 'NONE', *, *, #50253, .T. ) ;
#43917=FACE_OUTER_BOUND ( 'NONE', #36439, .T. ) ;
#43918=DIRECTION ( 'NONE',  ( 0.000000000000000000, 0.000000000000000000, -1.000000000000000000 ) ) ;
#43919=LINE ( 'NONE', #8466, #55342 ) ;
#43922=ORIENTED_EDGE ( 'NONE', *, *, #50253, .F. ) ;
#43925=CARTESIAN_POINT ( 'NONE',  ( 8.292781013277000568, -53.74469293044000295, 9.770415148702999986 ) ) ;
#43931=CARTESIAN_POINT ( 'NONE',  ( 11.50190934395000042, -76.67499180864999175, -3.421415122956000143 ) ) ;
#43934=DIRECTION ( 'NONE',  ( -0.9999999999998321343, 0.000000000000000000, -5.794540613806191565E-07 ) ) ;
#43935=CARTESIAN_POINT ( 'NONE',  ( 12.85140862681000051, -20.24439829998999940, -1.980464483675000054 ) ) ;
#43937=CARTESIAN_POINT ( 'NONE',  ( -3.250000000000000000, -2.500000000000000000, 0.000000000000000000 ) ) ;
#43938=CARTESIAN_POINT ( 'NONE',  ( 2.697037849775999696, -1.612630151311999827, 3.117841812466000118 ) ) ;
#43942=FACE_OUTER_BOUND ( 'NONE', #7599, .T. ) ;
#43945=CARTESIAN_POINT ( 'NONE',  ( 1.640804023310000082, -3.633545964575999765, -2.958959333410000170 ) ) ;
#43946=AXIS2_PLACEMENT_3D ( 'NONE', #49249, #43529, #52674 ) ;
#43948=CARTESIAN_POINT ( 'NONE',  ( 7.624341764926000131, -23.26485149464000202, -10.42531124853000080 ) ) ;
#43953=AXIS2_PLACEMENT_3D ( 'NONE', #51402, #33365, #19220 ) ;
#43956=EDGE_CURVE ( 'NONE', #11972, #32127, #50990, .T. ) ;
#43960=CARTESIAN_POINT ( 'NONE',  ( -8.414570695956999913, -59.94999999967000548, -8.414570695956999913 ) ) ;
#43962=CARTESIAN_POINT ( 'NONE',  ( -2.838799636221999823, -1.159209358523000111, 2.621254923317000163 ) ) ;
#43964=CARTESIAN_POINT ( 'NONE',  ( 12.66319951811000166, -25.18148258132000095, -0.1455783832297000147 ) ) ;
#43968=CARTESIAN_POINT ( 'NONE',  ( 7.958776492191999452, -24.47699850276000078, -9.723157982392999443 ) ) ;
#43970=CARTESIAN_POINT ( 'NONE',  ( -10.18491080495000034, -60.10716680829000325, -7.640030264173999441 ) ) ;
#43972=ADVANCED_FACE ( 'NONE', ( #58113 ), #2255, .F. ) ;
#43975=CARTESIAN_POINT ( 'NONE',  ( 8.060180465568407726, -61.42064870639847385, -9.621709427723352803 ) ) ;
#43977=CARTESIAN_POINT ( 'NONE',  ( -7.624341766629000539, -55.53514853726999689, 10.42531125022999916 ) ) ;
#43979=ORIENTED_EDGE ( 'NONE', *, *, #10515, .T. ) ;
#43980=VERTEX_POINT ( 'NONE', #9117 ) ;
#43983=VERTEX_POINT ( 'NONE', #57817 ) ;
#43984=ADVANCED_FACE ( 'NONE', ( #295 ), #41029, .F. ) ;
#43988=CARTESIAN_POINT ( 'NONE',  ( 11.75000000000000178, -76.03958333333331154, -1.538071403319980268 ) ) ;
#43989=CARTESIAN_POINT ( 'NONE',  ( 5.488127745643000210, -77.50827452080000057, 11.56242237764000080 ) ) ;
#43993=CARTESIAN_POINT ( 'NONE',  ( -8.485281374238999419, -23.25000000000000000, -8.485281374238999419 ) ) ;
#43996=B_SPLINE_CURVE_WITH_KNOTS ( 'NONE', 3,
 ( #52860, #12126, #7406, #38117, #57285, #48441, #20699, #25411 ),
 .UNSPECIFIED., .F., .F.,
 ( 4, 2, 2, 4 ),
 ( 0.000000000000000000, 0.5000000000000049960, 0.7500000000000024425, 1.000000000000000000 ),
 .UNSPECIFIED. ) ;
#43998=CIRCLE ( 'NONE', #15728, 14.00000000000000355 ) ;
#43999=CARTESIAN_POINT ( 'NONE',  ( 7.861037107701863036, -17.53338873154977406, 10.10708465682759183 ) ) ;
#44003=CARTESIAN_POINT ( 'NONE',  ( 0.000000000000000000, -6.049999999381999949, 0.000000000000000000 ) ) ;
#44004=VECTOR ( 'NONE', #23877, 1000.000000000000000 ) ;
#44005=CARTESIAN_POINT ( 'NONE',  ( -12.60354432327999952, -22.75100837100999840, -1.750000000001000089 ) ) ;
#44006=CARTESIAN_POINT ( 'NONE',  ( 3.504452398293381510, -3.107075414968905491, 0.3467038912678755969 ) ) ;
#44007=CARTESIAN_POINT ( 'NONE',  ( 12.82904091339000097, -23.32452529362999982, 2.062673488738000049 ) ) ;
#44011=CARTESIAN_POINT ( 'NONE',  ( 10.42274798266999980, -20.24634220924000161, -7.691916945430000041 ) ) ;
#44014=ORIENTED_EDGE ( 'NONE', *, *, #25296, .F. ) ;
#44025=CARTESIAN_POINT ( 'NONE',  ( 0.4701041210481999855, -53.79203065542999695, -12.54901038410999980 ) ) ;
#44026=CARTESIAN_POINT ( 'NONE',  ( 9.368450651685826358, -76.00132557254696053, 7.092182908105610473 ) ) ;
#44029=DIRECTION ( 'NONE',  ( -0.7071067811864976127, -0.7071067811865975328, -8.872361892382962277E-10 ) ) ;
#44030=ADVANCED_FACE ( 'NONE', ( #40100 ), #27679, .F. ) ;
#44033=EDGE_CURVE ( 'NONE', #38753, #56422, #26507, .T. ) ;
#44038=CYLINDRICAL_SURFACE ( 'NONE', #19063, 0.5000000000000006661 ) ;
#44039=CARTESIAN_POINT ( 'NONE',  ( -9.848022987154569918, -61.62869493570523360, 8.114799025198225380 ) ) ;
#44040=ORIENTED_EDGE ( 'NONE', *, *, #21807, .F. ) ;
#44044=VECTOR ( 'NONE', #32524, 1000.000000000000000 ) ;
#44045=EDGE_CURVE ( 'NONE', #25757, #3967, #13629, .T. ) ;
#44046=AXIS2_PLACEMENT_3D ( 'NONE', #55038, #46206, #50331 ) ;
#44048=DIRECTION ( 'NONE',  ( 1.000000000000000000, 0.000000000000000000, 0.000000000000000000 ) ) ;
#44049=DIRECTION ( 'NONE',  ( 0.000000000000000000, 1.000000000000000000, 0.000000000000000000 ) ) ;
#44053=ORIENTED_EDGE ( 'NONE', *, *, #27026, .T. ) ;
#44056=CARTESIAN_POINT ( 'NONE',  ( 0.8000000000000000444, -23.15000000000000213, -12.00000000000000000 ) ) ;
#44057=ORIENTED_EDGE ( 'NONE', *, *, #19838, .T. ) ;
#44058=ORIENTED_EDGE ( 'NONE', *, *, #4982, .T. ) ;
#44060=ORIENTED_EDGE ( 'NONE', *, *, #15617, .T. ) ;
#44062=ORIENTED_EDGE ( 'NONE', *, *, #36242, .F. ) ;
#44069=ORIENTED_EDGE ( 'NONE', *, *, #21619, .F. ) ;
#44073=CIRCLE ( 'NONE', #38424, 1.750000000000001332 ) ;
#44074=EDGE_CURVE ( 'NONE', #4486, #36041, #38466, .T. ) ;
#44079=DIRECTION ( 'NONE',  ( 0.000000000000000000, 1.000000000000000000, 0.000000000000000000 ) ) ;
#44080=DIRECTION ( 'NONE',  ( 1.000000000000000000, 0.000000000000000000, 0.000000000000000000 ) ) ;
#44083=ORIENTED_EDGE ( 'NONE', *, *, #5058, .T. ) ;
#44085=AXIS2_PLACEMENT_3D ( 'NONE', #34118, #52161, #21136 ) ;
#44086=CARTESIAN_POINT ( 'NONE',  ( -7.761025538834000592, -54.71850014388999739, 9.835174270505000038 ) ) ;
#44088=CARTESIAN_POINT ( 'NONE',  ( -10.13695543448000080, -18.29168900649999685, -7.646071007876000358 ) ) ;
#44089=CYLINDRICAL_SURFACE ( 'NONE', #6156, 14.00000000000000000 ) ;
#44090=LINE ( 'NONE', #34916, #4418 ) ;
#44091=AXIS2_PLACEMENT_3D ( 'NONE', #20018, #37420, #51609 ) ;
#44096=CARTESIAN_POINT ( 'NONE',  ( 12.50409240825462120, -24.52129362382453692, 1.233800929768811283 ) ) ;
#44098=ORIENTED_EDGE ( 'NONE', *, *, #34477, .T. ) ;
#44099=DIRECTION ( 'NONE',  ( 0.000000000000000000, -1.000000000000000000, 0.000000000000000000 ) ) ;
#44100=CARTESIAN_POINT ( 'NONE',  ( 0.9212224518320000222, -53.98045898127999465, 12.54670315977999984 ) ) ;
#44101=CARTESIAN_POINT ( 'NONE',  ( -12.87022657274000004, -19.21514526754999963, 2.062597299672999540 ) ) ;
#44102=CARTESIAN_POINT ( 'NONE',  ( -3.251796736646000330, -2.675056440563999605, 1.977781782242000075 ) ) ;
#44103=EDGE_CURVE ( 'NONE', #57621, #15231, #24878, .T. ) ;
#44106=CARTESIAN_POINT ( 'NONE',  ( -12.72558083408000051, -55.59866855809999464, 1.930284430576000076 ) ) ;
#44108=CARTESIAN_POINT ( 'NONE',  ( -2.019183793707000074, -60.58720277209999949, 12.79944116707999946 ) ) ;
#44111=CARTESIAN_POINT ( 'NONE',  ( 2.426647618366999603E-14, -5.949999999936550488, 0.000000000000000000 ) ) ;
#44112=CARTESIAN_POINT ( 'NONE',  ( -10.12213620585348828, -76.99884921769482560, -6.582638106783194942 ) ) ;
#44115=ADVANCED_FACE ( 'NONE', ( #12462, #30463 ), #52346, .F. ) ;
#44118=CARTESIAN_POINT ( 'NONE',  ( 1.750000000001000089, -55.54999998977000075, -12.56594317853999954 ) ) ;
#44121=CARTESIAN_POINT ( 'NONE',  ( 3.250000000000000444, -2.739583333333333481, -0.4254240051736113415 ) ) ;
#44124=CARTESIAN_POINT ( 'NONE',  ( -8.532671860997186997, -16.87201063391398748, -9.433519686788320868 ) ) ;
#44130=CARTESIAN_POINT ( 'NONE',  ( 12.50485632864967123, -17.13407884568546891, 0.6924337387642888197 ) ) ;
#44133=ORIENTED_EDGE ( 'NONE', *, *, #15164, .F. ) ;
#44134=CARTESIAN_POINT ( 'NONE',  ( 2.380924776420011657, -3.499999999999999556, -2.674844963567099221 ) ) ;
#44140=ORIENTED_EDGE ( 'NONE', *, *, #5283, .F. ) ;
#44142=CARTESIAN_POINT ( 'NONE',  ( -1.791405018985999797, -78.89219709918999968, 12.22794537915999946 ) ) ;
#44143=VERTEX_POINT ( 'NONE', #48220 ) ;
#44145=DIRECTION ( 'NONE',  ( -0.7071067811865475727, 0.000000000000000000, 0.7071067811865475727 ) ) ;
#44146=FACE_BOUND ( 'NONE', #26332, .T. ) ;
#44149=ADVANCED_FACE ( 'NONE', ( #38174 ), #27344, .F. ) ;
#44154=CARTESIAN_POINT ( 'NONE',  ( 5.623102978484999959, -77.34535537052001075, 11.84678905512000036 ) ) ;
#44156=CARTESIAN_POINT ( 'NONE',  ( 8.913248419499998576, -76.43655867677999538, -7.987006294937000206 ) ) ;
#44158=CARTESIAN_POINT ( 'NONE',  ( -7.624341764926000131, -23.26485149464000202, 10.42531124853000080 ) ) ;
#44160=CARTESIAN_POINT ( 'NONE',  ( -10.35845616725999996, -55.50221404479999876, 7.627487606591000002 ) ) ;
#44161=CARTESIAN_POINT ( 'NONE',  ( -1.906216885303581243, -3.025969998097067570, 2.639459242746020617 ) ) ;
#44163=VECTOR ( 'NONE', #34466, 1000.000000000000000 ) ;
#44164=DIRECTION ( 'NONE',  ( 0.000000000000000000, 1.000000000000000000, 0.000000000000000000 ) ) ;
#44166=CARTESIAN_POINT ( 'NONE',  ( -3.054513261463999818, -2.833537059304999772, -2.270689576097000284 ) ) ;
#44168=ORIENTED_EDGE ( 'NONE', *, *, #8375, .T. ) ;
#44169=CARTESIAN_POINT ( 'NONE',  ( -9.029867227927999451, -62.13262194258000193, -9.038867509651000276 ) ) ;
#44170=DIRECTION ( 'NONE',  ( 0.000000000000000000, 1.000000000000000000, 0.000000000000000000 ) ) ;
#44172=CARTESIAN_POINT ( 'NONE',  ( -12.77656766273999978, -16.68801851262999847, -0.1555695072196000006 ) ) ;
#44173=CARTESIAN_POINT ( 'NONE',  ( 5.579996517577999526, -77.39173409593000486, 11.75597208960999929 ) ) ;
#44175=AXIS2_PLACEMENT_3D ( 'NONE', #49318, #13578, #49618 ) ;
#44176=CARTESIAN_POINT ( 'NONE',  ( -10.41144098944999463, -60.32546312031783486, -7.610433527982627844 ) ) ;
#44177=CARTESIAN_POINT ( 'NONE',  ( 6.099198899075000568, -76.41540033321001602, 10.75284491171999868 ) ) ;
#44182=CARTESIAN_POINT ( 'NONE',  ( 12.70956478401000034, -60.20497526583999814, 1.933781249744999986 ) ) ;
#44183=CARTESIAN_POINT ( 'NONE',  ( -1.667936697358999965, -22.76462890193000277, -12.53241208773999915 ) ) ;
#44185=EDGE_CURVE ( 'NONE', #4989, #44143, #53200, .T. ) ;
#44189=EDGE_LOOP ( 'NONE', ( #54957, #21552, #18357, #49580, #17314, #35460 ) ) ;
#44190=B_SPLINE_CURVE_WITH_KNOTS ( 'NONE', 3,
 ( #52620, #47923, #7162, #3317, #16025, #12172, #7456, #43474, #29581, #30158, #21311, #2456, #47638, #25166, #20460, #30448, #20743, #3595 ),
 .UNSPECIFIED., .F., .F.,
 ( 4, 2, 2, 2, 2, 2, 2, 2, 4 ),
 ( 0.000000000000000000, 0.1250000000000000833, 0.2500000000000001665, 0.3750000000000001110, 0.5000000000000001110, 0.6250000000000001110, 0.7500000000000000000, 0.8750000000000000000, 1.000000000000000000 ),
 .UNSPECIFIED. ) ;
#44196=CARTESIAN_POINT ( 'NONE',  ( -7.434020715871331397, -55.28308356097138443, -8.107762507645487560 ) ) ;
#44198=ORIENTED_EDGE ( 'NONE', *, *, #14702, .F. ) ;
#44200=ORIENTED_EDGE ( 'NONE', *, *, #18771, .T. ) ;
#44201=ADVANCED_FACE ( 'NONE', ( #12748 ), #37126, .F. ) ;
#44202=CARTESIAN_POINT ( 'NONE',  ( -3.785083400059697567, -78.09945095226758838, 11.15180688584555213 ) ) ;
#44204=ORIENTED_EDGE ( 'NONE', *, *, #51138, .T. ) ;
#44207=CARTESIAN_POINT ( 'NONE',  ( -12.10179013622999911, -78.56294709707631796, -1.986401539992999954 ) ) ;
#44209=CARTESIAN_POINT ( 'NONE',  ( 7.624757993407000001, -54.99647951274999969, 10.47516388917000008 ) ) ;
#44211=CARTESIAN_POINT ( 'NONE',  ( 0.5999999999999999778, -23.15000000000000213, -11.79999999999999893 ) ) ;
#44212=FACE_OUTER_BOUND ( 'NONE', #20892, .T. ) ;
#44213=EDGE_CURVE ( 'NONE', #35193, #23446, #4122, .T. ) ;
#44215=CARTESIAN_POINT ( 'NONE',  ( 7.718346056121999865, -57.05111654290000445, -10.07719973194999952 ) ) ;
#44216=CARTESIAN_POINT ( 'NONE',  ( 7.919595949288999570, -59.94999999967000548, 8.768124086712999699 ) ) ;
#44232=DIRECTION ( 'NONE',  ( 0.000000000000000000, 1.000000000000000000, 0.000000000000000000 ) ) ;
#44233=CARTESIAN_POINT ( 'NONE',  ( -7.709154088328800114, -18.07253195914548627, 9.998702477107983100 ) ) ;
#44236=ORIENTED_EDGE ( 'NONE', *, *, #51772, .T. ) ;
#44237=FACE_OUTER_BOUND ( 'NONE', #32868, .T. ) ;
#44243=CARTESIAN_POINT ( 'NONE',  ( 1.752416575730000092, -1.467211001040999996, 3.260037978519999768 ) ) ;
#44245=CARTESIAN_POINT ( 'NONE',  ( 12.66235429707000115, -25.13741783422999987, -0.4955846680316000619 ) ) ;
#44247=ORIENTED_EDGE ( 'NONE', *, *, #2689, .T. ) ;
#44248=FACE_OUTER_BOUND ( 'NONE', #11162, .T. ) ;
#44255=CARTESIAN_POINT ( 'NONE',  ( -12.54435570279974854, -55.27582218184407736, 1.733918077762378829 ) ) ;
#44258=ORIENTED_EDGE ( 'NONE', *, *, #27261, .T. ) ;
#44260=CARTESIAN_POINT ( 'NONE',  ( 1.232226823490451428, -54.27709088663625181, 12.50408896745931386 ) ) ;
#44261=CARTESIAN_POINT ( 'NONE',  ( -8.227509542961000122, -53.97460508840000415, -9.516261809240999625 ) ) ;
#44263=ORIENTED_EDGE ( 'NONE', *, *, #41370, .F. ) ;
#44264=ORIENTED_EDGE ( 'NONE', *, *, #17332, .F. ) ;
#44271=CARTESIAN_POINT ( 'NONE',  ( -9.247037010692000791, -77.64321223492000001, -9.074963555248000802 ) ) ;
#44278=ORIENTED_EDGE ( 'NONE', *, *, #50436, .F. ) ;
#44280=CARTESIAN_POINT ( 'NONE',  ( 7.331368884251999951, -75.84156555408999623, 9.888700222343000945 ) ) ;
#44282=VECTOR ( 'NONE', #26889, 1000.000000000000114 ) ;
#44285=CARTESIAN_POINT ( 'NONE',  ( 3.012546900933178673, -3.055919557904988260, -1.823338109451127620 ) ) ;
#44287=CARTESIAN_POINT ( 'NONE',  ( 12.92181194099999963, -20.24351820077000141, 2.062502994258999856 ) ) ;
#44289=CARTESIAN_POINT ( 'NONE',  ( -12.49168451098999988, -18.70151115557999688, -1.667916687331000070 ) ) ;
#44292=CARTESIAN_POINT ( 'NONE',  ( 10.35845616727999996, -18.70221404512000163, -7.627487606607999737 ) ) ;
#44293=CARTESIAN_POINT ( 'NONE',  ( 10.13881649148000008, -76.90783510652001098, -5.938594122520999719 ) ) ;
#44295=EDGE_CURVE ( 'NONE', #45569, #40274, #56024, .T. ) ;
#44299=CARTESIAN_POINT ( 'NONE',  ( 0.000000000000000000, -60.04999999966999980, -12.00000000000000000 ) ) ;
#44301=CARTESIAN_POINT ( 'NONE',  ( -12.76303204517000012, -18.73514852243999940, 1.980584515753000208 ) ) ;
#44306=CARTESIAN_POINT ( 'NONE',  ( -12.70556836343000029, -53.57227722738999631, 1.774192865971000122E-09 ) ) ;
#44307=CARTESIAN_POINT ( 'NONE',  ( 9.182347698127177438, -76.00326530161947858, 7.331077060909383825 ) ) ;
#44310=CARTESIAN_POINT ( 'NONE',  ( -8.852883971327290880, -77.14144752210202682, 7.763934591146516517 ) ) ;
#44311=CARTESIAN_POINT ( 'NONE',  ( 5.385928292795701289, -78.86210492683198936, -10.60790267139944021 ) ) ;
#44313=CIRCLE ( 'NONE', #12290, 11.00000000000000000 ) ;
#44319=CARTESIAN_POINT ( 'NONE',  ( 0.3141224841222575170, -78.56945284321614054, 11.74397421471209313 ) ) ;
#44324=CARTESIAN_POINT ( 'NONE',  ( 10.53393757967567090, -75.80000000000001137, -5.616035657633564604 ) ) ;
#44326=CARTESIAN_POINT ( 'NONE',  ( -11.79999999988000070, -23.14999999478999726, 0.5999999998848000171 ) ) ;
#44327=CARTESIAN_POINT ( 'NONE',  ( -10.07627163191000008, -55.55000000278000272, -7.601397897754999633 ) ) ;
#44330=CIRCLE ( 'NONE', #26410, 13.94827586206999825 ) ;
#44333=DIRECTION ( 'NONE',  ( 0.000000000000000000, -0.1122098755727947705, 0.9936845293270585300 ) ) ;
#44335=ORIENTED_EDGE ( 'NONE', *, *, #57513, .F. ) ;
#44339=CARTESIAN_POINT ( 'NONE',  ( 9.889431646000000242, -78.85235367036999321, 7.252463523969000292 ) ) ;
#44340=VERTEX_POINT ( 'NONE', #26600 ) ;
#44341=CARTESIAN_POINT ( 'NONE',  ( 7.657745562908000458, -23.66920625126000033, 9.966193613329998868 ) ) ;
#44346=VERTEX_POINT ( 'NONE', #40198 ) ;
#44347=AXIS2_PLACEMENT_3D ( 'NONE', #27397, #50443, #40991 ) ;
#44349=ORIENTED_EDGE ( 'NONE', *, *, #57533, .T. ) ;
#44355=CARTESIAN_POINT ( 'NONE',  ( 12.11913442928999984, -76.19745797811999921, 4.608623306100999351 ) ) ;
#44356=CARTESIAN_POINT ( 'NONE',  ( 3.174095336822680746, -2.230252669283250277, -0.8063667267729033306 ) ) ;
#44357=CARTESIAN_POINT ( 'NONE',  ( 7.610717068315568490, -55.27984996805254525, -10.41172376761247875 ) ) ;
#44359=CARTESIAN_POINT ( 'NONE',  ( 0.000000000000000000, -0.2000000000000000111, 0.000000000000000000 ) ) ;
#44361=EDGE_CURVE ( 'NONE', #14201, #2137, #49452, .T. ) ;
#44365=VECTOR ( 'NONE', #9184, 1000.000000000000000 ) ;
#44366=CARTESIAN_POINT ( 'NONE',  ( -8.870405106233999248, -53.73036971739000478, 8.878274241729000593 ) ) ;
#44368=CARTESIAN_POINT ( 'NONE',  ( -12.70619440583237214, -61.26151788281449484, 1.571771935835015510 ) ) ;
#44369=AXIS2_PLACEMENT_3D ( 'NONE', #54242, #23231, #13777 ) ;
#44371=CARTESIAN_POINT ( 'NONE',  ( -1.666727925315000025, -18.80825518223999993, -12.50018462903999961 ) ) ;
#44372=CARTESIAN_POINT ( 'NONE',  ( 0.000000000000000000, 4.040000000000000036, 0.000000000000000000 ) ) ;
#44374=FACE_BOUND ( 'NONE', #57753, .T. ) ;
#44379=DIRECTION ( 'NONE',  ( 0.7071067811864980568, -1.536189447283994854E-11, 0.7071067811865969777 ) ) ;
#44380=CARTESIAN_POINT ( 'NONE',  ( -1.576170184336000091, -54.63913032751000287, 12.55466896101999907 ) ) ;
#44381=CARTESIAN_POINT ( 'NONE',  ( -12.82904109062999964, -23.32452273707999879, 2.062673488410000200 ) ) ;
#44382=CARTESIAN_POINT ( 'NONE',  ( 3.221176052379999710, -2.342669754918000002, -1.707589208867000163 ) ) ;
#44384=CARTESIAN_POINT ( 'NONE',  ( -3.250000000000001332, -1.510416666666666741, -0.4254240051736181139 ) ) ;
#44386=EDGE_CURVE ( 'NONE', #38967, #45976, #51350, .T. ) ;
#44387=CARTESIAN_POINT ( 'NONE',  ( -1.930009203933999995, -60.00099032284000344, 12.72537718780000127 ) ) ;
#44388=CARTESIAN_POINT ( 'NONE',  ( 12.43646312222999839, -17.07951485557000026, 0.1257251053153000120 ) ) ;
#44391=CARTESIAN_POINT ( 'NONE',  ( 11.86339925601972922, -77.19009386423427088, -1.944120246756255943 ) ) ;
#44392=AXIS2_PLACEMENT_3D ( 'NONE', #47133, #42682, #42395 ) ;
#44397=FACE_OUTER_BOUND ( 'NONE', #8252, .T. ) ;
#44398=FACE_OUTER_BOUND ( 'NONE', #23935, .T. ) ;
#44401=CARTESIAN_POINT ( 'NONE',  ( -12.54435915805012414, -23.52412882219291035, -1.733925320388666202 ) ) ;
#44402=CARTESIAN_POINT ( 'NONE',  ( 8.728206860394864819, -75.80000000000001137, 8.278571939072135066 ) ) ;
#44403=B_SPLINE_CURVE_WITH_KNOTS ( 'NONE', 3,
 ( #53089, #12642, #30635, #31507, #4962, #41557 ),
 .UNSPECIFIED., .F., .F.,
 ( 4, 1, 1, 4 ),
 ( 0.000000000000000000, 0.3333333333333000081, 0.6666666666667000474, 1.000000000000000000 ),
 .UNSPECIFIED. ) ;
#44404=ORIENTED_EDGE ( 'NONE', *, *, #32547, .T. ) ;
#44408=DIRECTION ( 'NONE',  ( 0.7272727272724163194, -0.6863485850246158204, 6.703676216208155796E-07 ) ) ;
#44412=VECTOR ( 'NONE', #46415, 1000.000000000000000 ) ;
#44413=VERTEX_POINT ( 'NONE', #3535 ) ;
#44414=DIRECTION ( 'NONE',  ( 1.000000000000000000, 0.000000000000000000, 0.000000000000000000 ) ) ;
#44415=ORIENTED_EDGE ( 'NONE', *, *, #35758, .F. ) ;
#44417=CARTESIAN_POINT ( 'NONE',  ( -1.374053708643000007E-14, -74.80000000000001137, 0.000000000000000000 ) ) ;
#44419=CARTESIAN_POINT ( 'NONE',  ( 0.4802748259353999960, -25.00526907281999911, -12.54896097834000024 ) ) ;
#44424=CARTESIAN_POINT ( 'NONE',  ( -12.50000000000000000, -23.25000000000000000, 0.000000000000000000 ) ) ;
#44425=CARTESIAN_POINT ( 'NONE',  ( 12.25699876382000042, -79.26582643418001339, 1.580520632500000078 ) ) ;
#44427=ADVANCED_FACE ( 'NONE', ( #52838 ), #8249, .F. ) ;
#44428=ORIENTED_EDGE ( 'NONE', *, *, #56141, .T. ) ;
#44434=CARTESIAN_POINT ( 'NONE',  ( 5.554685856605999561, -76.84581360187000598, 11.87889705760999881 ) ) ;
#44435=CARTESIAN_POINT ( 'NONE',  ( 12.17287523535000027, -77.47264530806999971, -3.409737174454000375 ) ) ;
#44441=CARTESIAN_POINT ( 'NONE',  ( -10.55911395186000057, -56.01538333533000014, 7.642160924870000649 ) ) ;
#44442=CARTESIAN_POINT ( 'NONE',  ( 1.721677682318950575, -2.931119376536615917, 2.765314047765481398 ) ) ;
#44446=CARTESIAN_POINT ( 'NONE',  ( 3.702420020526000055, -2.516613097741000171, 0.8821385418971999792 ) ) ;
#44453=CARTESIAN_POINT ( 'NONE',  ( -12.55458938220999876, -17.83720883386000011, -1.575070636625000242 ) ) ;
#44454=CARTESIAN_POINT ( 'NONE',  ( 11.85869973992999959, -77.76643789029000686, 5.358216250391999225 ) ) ;
#44455=VECTOR ( 'NONE', #47134, 1000.000000000000000 ) ;
#44456=CARTESIAN_POINT ( 'NONE',  ( -10.36597333715949176, -60.57522428981332752, -7.635925938723863382 ) ) ;
#44457=CARTESIAN_POINT ( 'NONE',  ( 9.998734510784624163, -18.07263061081724942, 7.709128441133644927 ) ) ;
#44459=CARTESIAN_POINT ( 'NONE',  ( -10.10912542004608561, -55.32413588744719135, 7.634643956462955572 ) ) ;
#44460=CARTESIAN_POINT ( 'NONE',  ( 8.251806177857083924, -53.99944067038419604, -9.431051272625094128 ) ) ;
#44462=CARTESIAN_POINT ( 'NONE',  ( -2.062670899148999926, -23.30639625649999758, -12.83044039274999903 ) ) ;
#44465=CARTESIAN_POINT ( 'NONE',  ( -1.667936688463999895, -56.03513569577999931, -12.53239398060000021 ) ) ;
#44472=VERTEX_POINT ( 'NONE', #21537 ) ;
#44473=EDGE_CURVE ( 'NONE', #57766, #53695, #31498, .T. ) ;
#44476=CARTESIAN_POINT ( 'NONE',  ( 12.60552522433000000, -55.51082434643999619, 1.799501877760999902 ) ) ;
#44479=MECHANICAL_DESIGN_GEOMETRIC_PRESENTATION_REPRESENTATION('',(#57667),#1147);
#44485=VERTEX_POINT ( 'NONE', #50764 ) ;
#44487=ORIENTED_EDGE ( 'NONE', *, *, #35209, .F. ) ;
#44495=B_SPLINE_CURVE_WITH_KNOTS ( 'NONE', 3,
 ( #31419, #40296, #35857, #36157, #13714, #42348, #1619, #5733, #33168, #15174, #46794, #41462, #55039, #50628, #37900, #24034, #32873, #5161, #6319, #51213, #23741, #37609, #24336, #10178, #5445, #10765, #28743, #14588, #27864, #55924 ),
 .UNSPECIFIED., .F., .F.,
 ( 4, 2, 2, 2, 2, 2, 2, 2, 2, 2, 2, 2, 2, 2, 4 ),
 ( 0.000000000000000000, 0.1250000000000041633, 0.1875000000000046907, 0.2500000000000052180, 0.3125000000000057176, 0.3750000000000062728, 0.5000000000000072164, 0.5625000000000077716, 0.6250000000000082157, 0.6875000000000087708, 0.7500000000000093259, 0.8125000000000098810, 0.8437500000000087708, 0.8750000000000075495, 1.000000000000000000 ),
 .UNSPECIFIED. ) ;
#44496=CARTESIAN_POINT ( 'NONE',  ( 8.190859204290999784, -55.64999999967000122, -7.342331066867000544 ) ) ;
#44498=EDGE_CURVE ( 'NONE', #55676, #21570, #23094, .T. ) ;
#44499=CARTESIAN_POINT ( 'NONE',  ( 12.00000000000000000, -18.75000000000000000, -1.250000000000000000 ) ) ;
#44504=AXIS2_PLACEMENT_3D ( 'NONE', #23562, #9413, #27403 ) ;
#44505=CARTESIAN_POINT ( 'NONE',  ( -12.52582323433392197, -23.80939730775229890, 1.680974276152719771 ) ) ;
#44507=CARTESIAN_POINT ( 'NONE',  ( -1.798368564625000054, -23.19636757045999786, 12.61278090841000044 ) ) ;
#44508=DIRECTION ( 'NONE',  ( 0.000000000000000000, 0.8191944460894394764, 0.5735158755398287456 ) ) ;
#44510=CARTESIAN_POINT ( 'NONE',  ( -0.4165118319448999351, -1.439790208251000125, 3.598914716717999784 ) ) ;
#44513=CARTESIAN_POINT ( 'NONE',  ( 12.43640309388999832, -61.71747517570000241, 0.05224034426410999882 ) ) ;
#44515=CARTESIAN_POINT ( 'NONE',  ( 0.000000000000000000, -15.69705297114000331, -12.53545825868000207 ) ) ;
#44518=CARTESIAN_POINT ( 'NONE',  ( 0.000000000000000000, -26.93717104351999936, 0.000000000000000000 ) ) ;
#44526=CARTESIAN_POINT ( 'NONE',  ( -10.07627163191000008, -23.24999999688999708, 7.601397897754999633 ) ) ;
#44528=CARTESIAN_POINT ( 'NONE',  ( -10.35410175341000105, -60.20399325318000194, 7.619715687221999545 ) ) ;
#44529=LINE ( 'NONE', #14401, #7608 ) ;
#44531=CARTESIAN_POINT ( 'NONE',  ( 3.586056226710999884, -1.401363919000000013, 0.9161727453457999548 ) ) ;
#44533=CARTESIAN_POINT ( 'NONE',  ( 12.82202361517000000, -23.42627773034000427, -2.066043355638000012 ) ) ;
#44534=LINE ( 'NONE', #40101, #1012 ) ;
#44535=EDGE_LOOP ( 'NONE', ( #13919, #8515, #505, #53714 ) ) ;
#44540=EDGE_CURVE ( 'NONE', #53636, #8280, #25828, .T. ) ;
#44543=AXIS2_PLACEMENT_3D ( 'NONE', #43960, #3793, #3510 ) ;
#44546=DIRECTION ( 'NONE',  ( 0.000000000000000000, -1.000000000000000000, 0.000000000000000000 ) ) ;
#44547=CARTESIAN_POINT ( 'NONE',  ( 1.997276839918477265, -1.177083333333333481, -2.598917237794082791 ) ) ;
#44548=VERTEX_POINT ( 'NONE', #10309 ) ;
#44549=ORIENTED_EDGE ( 'NONE', *, *, #41879, .T. ) ;
#44550=AXIS2_PLACEMENT_3D ( 'NONE', #4694, #22987, #33284 ) ;
#44551=CARTESIAN_POINT ( 'NONE',  ( -12.60552511008000032, -55.51082276539999327, 1.799501877793999949 ) ) ;
#44552=CARTESIAN_POINT ( 'NONE',  ( -7.961057357800999768, -54.26431744618999886, -9.783210913615000948 ) ) ;
#44555=VERTEX_POINT ( 'NONE', #46046 ) ;
#44560=ORIENTED_EDGE ( 'NONE', *, *, #55472, .T. ) ;
#44561=CARTESIAN_POINT ( 'NONE',  ( 10.18949731070999931, -18.78470987703000006, 7.645392562261999814 ) ) ;
#44564=CARTESIAN_POINT ( 'NONE',  ( 5.759449073023001020, -78.33319635864999952, 11.78163922240000083 ) ) ;
#44566=DIRECTION ( 'NONE',  ( 0.7071067811865475727, 0.000000000000000000, 0.7071067811865475727 ) ) ;
#44571=ORIENTED_EDGE ( 'NONE', *, *, #33060, .F. ) ;
#44575=CIRCLE ( 'NONE', #41765, 9.000000000000000000 ) ;
#44576=ADVANCED_FACE ( 'NONE', ( #5571 ), #9431, .F. ) ;
#44578=CARTESIAN_POINT ( 'NONE',  ( -3.580942884975041984, -2.851296129650088496, -0.07958713964337410518 ) ) ;
#44579=CARTESIAN_POINT ( 'NONE',  ( -7.730439324435801396, -17.87809618957197699, 10.25198230928420173 ) ) ;
#44585=DIRECTION ( 'NONE',  ( 1.000000000000000000, 0.000000000000000000, 0.000000000000000000 ) ) ;
#44589=B_SPLINE_SURFACE_WITH_KNOTS ( 'NONE', 3, 3, ( 
 ( #25512, #7222, #56819, #16375 ),
 ( #39091, #2512, #10270, #29354 ),
 ( #1140, #37121, #57099, #50730 ),
 ( #47401, #28251, #5828, #23835 ),
 ( #42661, #38222, #56243, #24936 ),
 ( #15793, #42958, #33781, #20516 ),
 ( #38513, #17522, #12513, #16950 ),
 ( #53246, #17227, #48827, #7800 ),
 ( #4239, #35217, #13080, #21370 ),
 ( #18121, #48540, #35811, #12795 ),
 ( #8666, #49115, #22540, #17824 ),
 ( #143, #57967, #26950, #36116 ),
 ( #40550, #53841, #39665, #35512 ),
 ( #44108, #44983, #22238, #8369 ),
 ( #31077, #3657, #13376, #57671 ),
 ( #54133, #26652, #53540, #30795 ),
 ( #26368, #44387, #44688, #13672 ) ),
 .UNSPECIFIED., .F., .F., .F.,
 ( 4, 1, 1, 1, 1, 1, 1, 1, 1, 1, 1, 1, 1, 1, 4 ),
 ( 4, 4 ),
 ( -0.01011408452875999994, 0.000000000000000000, 0.08333333333333001192, 0.1666666666667000196, 0.2500000000000000000, 0.3333333333333000081, 0.4166666666666999919, 0.5000000000000000000, 0.5833333333333000637, 0.6666666666667000474, 0.7500000000000000000, 0.8333333333333000637, 0.9166666666667000474, 1.000000000000000000, 1.010362559108000102 ),
 ( -0.3559705546268999710, 1.357612419623000166 ),
 .UNSPECIFIED. ) ;
#44593=CYLINDRICAL_SURFACE ( 'NONE', #3131, 1.750000000000000000 ) ;
#44601=CARTESIAN_POINT ( 'NONE',  ( -12.50000000000000000, -18.75000000240999753, -1.750000000000000000 ) ) ;
#44603=CARTESIAN_POINT ( 'NONE',  ( 11.00423669942431104, -75.97794915958310469, 4.119231451974944669 ) ) ;
#44606=AXIS2_PLACEMENT_3D ( 'NONE', #19358, #32908, #9042 ) ;
#44607=CARTESIAN_POINT ( 'NONE',  ( 3.165057598945393291, -2.330483944310657307, -0.8521617472482003741 ) ) ;
#44608=EDGE_CURVE ( 'NONE', #31908, #11806, #14427, .T. ) ;
#44615=CARTESIAN_POINT ( 'NONE',  ( 4.598774055804255134, -78.54242297502504755, 10.81608457866212802 ) ) ;
#44624=DIRECTION ( 'NONE',  ( -1.000000000000000000, 0.000000000000000000, 0.000000000000000000 ) ) ;
#44625=CIRCLE ( 'NONE', #54995, 13.79999999999999893 ) ;
#44626=CARTESIAN_POINT ( 'NONE',  ( -10.98676125741665643, -23.41445108201299874, 0.5397229578417699347 ) ) ;
#44631=CARTESIAN_POINT ( 'NONE',  ( -12.72966770609339804, -60.56881200329789294, -1.931346186347923766 ) ) ;
#44634=FACE_OUTER_BOUND ( 'NONE', #40336, .T. ) ;
#44635=EDGE_LOOP ( 'NONE', ( #27842, #1098, #36394, #28368, #53049, #48327, #52176 ) ) ;
#44641=DIRECTION ( 'NONE',  ( 0.7071067812863980340, -6.386274622742979319E-09, -0.7071067810866970005 ) ) ;
#44642=AXIS2_PLACEMENT_3D ( 'NONE', #28626, #23622, #28041 ) ;
#44648=ORIENTED_EDGE ( 'NONE', *, *, #27677, .T. ) ;
#44654=CARTESIAN_POINT ( 'NONE',  ( 7.624341766647000362, -18.73514853758999976, -10.42531125024999916 ) ) ;
#44656=CARTESIAN_POINT ( 'NONE',  ( 5.890705889994000799, -75.57722202328000094, 10.05943228418000146 ) ) ;
#44660=PLANE ( 'NONE',  #50493 ) ;
#44661=CARTESIAN_POINT ( 'NONE',  ( -10.53494356938999843, -23.22715052988000295, -7.618393677165000710 ) ) ;
#44668=CARTESIAN_POINT ( 'NONE',  ( -8.292781013307999771, -16.94469293076999961, -9.770415148734000965 ) ) ;
#44669=CARTESIAN_POINT ( 'NONE',  ( -1.532229595825244761, -60.92298962908660087, -12.51228690890456541 ) ) ;
#44670=CARTESIAN_POINT ( 'NONE',  ( -1.930638663166000191, -18.77877936711000117, -12.72375916873000001 ) ) ;
#44671=CARTESIAN_POINT ( 'NONE',  ( 0.04193593712240011040, -53.78990258635192134, 12.50649570002414279 ) ) ;
#44673=CARTESIAN_POINT ( 'NONE',  ( 10.21381326472999795, -56.02870851050000311, -7.668949790007999923 ) ) ;
#44674=DIRECTION ( 'NONE',  ( 0.7071067811865475727, 0.000000000000000000, -0.7071067811865475727 ) ) ;
#44676=CARTESIAN_POINT ( 'NONE',  ( -12.76303204513999923, -55.53514852210999919, 1.980584515753000208 ) ) ;
#44680=AXIS2_PLACEMENT_3D ( 'NONE', #92, #57914, #36060 ) ;
#44681=CARTESIAN_POINT ( 'NONE',  ( 1.582498447120999963, -54.64913877488999816, 12.55493832969000145 ) ) ;
#44682=CARTESIAN_POINT ( 'NONE',  ( -12.49168451098999988, -23.29848884437999956, 1.667916687331000070 ) ) ;
#44684=CARTESIAN_POINT ( 'NONE',  ( -0.07105210834495999384, -3.682034174984999630, 3.964982828070999332 ) ) ;
#44686=CARTESIAN_POINT ( 'NONE',  ( 2.839805762151339952, -1.708333333333332815, -1.636761686205418176 ) ) ;
#44688=CARTESIAN_POINT ( 'NONE',  ( -1.798368564622000010, -59.99636757014000210, 12.61278090843000044 ) ) ;
#44691=EDGE_CURVE ( 'NONE', #4024, #47903, #8236, .T. ) ;
#44692=CARTESIAN_POINT ( 'NONE',  ( -10.34725804423785256, -76.90989821929815662, 6.236182828636385622 ) ) ;
#44693=CARTESIAN_POINT ( 'NONE',  ( -3.600020634850999546, -78.65560489188999327, 11.08749048210999888 ) ) ;
#44697=CARTESIAN_POINT ( 'NONE',  ( 1.980584515756000030, -60.06485150062000145, 12.76303204342999997 ) ) ;
#44698=CARTESIAN_POINT ( 'NONE',  ( -1.250000000000000000, -55.35321828636000419, -12.50000000000000000 ) ) ;
#44699=CARTESIAN_POINT ( 'NONE',  ( -12.66235429711000116, -61.93741783389999966, 0.4955846680318000130 ) ) ;
#44705=CARTESIAN_POINT ( 'NONE',  ( 0.3664097495389522785, -61.77190017435451352, 12.50575740046243922 ) ) ;
#44708=VECTOR ( 'NONE', #21415, 1000.000000000000000 ) ;
#44709=CARTESIAN_POINT ( 'NONE',  ( 7.555116226634262411, -55.11315380192718294, 7.995796640817951939 ) ) ;
#44710=VERTEX_POINT ( 'NONE', #6431 ) ;
#44711=EDGE_LOOP ( 'NONE', ( #28204, #43790, #37300, #11082, #29878, #15682 ) ) ;
#44714=CARTESIAN_POINT ( 'NONE',  ( 12.50000000000000000, -60.04999999966999980, 0.000000000000000000 ) ) ;
#44719=CARTESIAN_POINT ( 'NONE',  ( 0.9887300587124998597, -24.93410057768999977, -12.65963207090000076 ) ) ;
#44720=CIRCLE ( 'NONE', #23011, 13.94827586206999825 ) ;
#44723=ORIENTED_EDGE ( 'NONE', *, *, #7321, .F. ) ;
#44725=CARTESIAN_POINT ( 'NONE',  ( 8.402029934263000044, -78.60393122293001511, -8.859658380982999404 ) ) ;
#44726=ORIENTED_EDGE ( 'NONE', *, *, #41744, .F. ) ;
#44727=ORIENTED_EDGE ( 'NONE', *, *, #44884, .F. ) ;
#44728=FACE_OUTER_BOUND ( 'NONE', #23939, .T. ) ;
#44729=VECTOR ( 'NONE', #27277, 1000.000000000000000 ) ;
#44730=ADVANCED_FACE ( 'NONE', ( #46613 ), #23561, .F. ) ;
#44735=CARTESIAN_POINT ( 'NONE',  ( -2.472194872447494696, -79.05729166668488972, 11.61165635167936472 ) ) ;
#44737=B_SPLINE_CURVE_WITH_KNOTS ( 'NONE', 3,
 ( #56097, #51680, #51383, #55805, #46964, #1794, #29207, #10940, #28330, #42518, #47254, #33921, #51961, #2370, #37198, #46675, #5904, #29495 ),
 .UNSPECIFIED., .F., .F.,
 ( 4, 2, 2, 2, 2, 2, 2, 2, 4 ),
 ( 0.000000000000000000, 0.1250000000000001665, 0.2500000000000002776, 0.3750000000000002776, 0.5000000000000002220, 0.6250000000000001110, 0.7500000000000001110, 0.8750000000000000000, 1.000000000000000000 ),
 .UNSPECIFIED. ) ;
#44742=CARTESIAN_POINT ( 'NONE',  ( -1.842154520908950044, -76.81205411479356826, -11.67446096355657126 ) ) ;
#44744=DIRECTION ( 'NONE',  ( 0.000000000000000000, 0.000000000000000000, -1.000000000000000000 ) ) ;
#44746=CARTESIAN_POINT ( 'NONE',  ( -0.3113020967593000399, -2.629516015700000153, 3.793306396812999637 ) ) ;
#44748=ORIENTED_EDGE ( 'NONE', *, *, #37486, .F. ) ;
#44751=TOROIDAL_SURFACE ( 'NONE', #20272, 1.250000000000000000, 0.5000000000000000000 ) ;
#44754=CARTESIAN_POINT ( 'NONE',  ( 7.287838312904000304, -78.15497037702999705, -10.78085041437000058 ) ) ;
#44756=CARTESIAN_POINT ( 'NONE',  ( -10.12561891750000065, -76.54434732925000162, -7.350590001713999122 ) ) ;
#44757=VERTEX_POINT ( 'NONE', #42166 ) ;
#44758=EDGE_CURVE ( 'NONE', #3325, #42463, #28697, .T. ) ;
#44759=AXIS2_PLACEMENT_3D ( 'NONE', #7535, #3117, #21108 ) ;
#44760=CARTESIAN_POINT ( 'NONE',  ( 8.414570695956999913, -59.94999999967000548, 8.414570695956999913 ) ) ;
#44767=CARTESIAN_POINT ( 'NONE',  ( -3.161392481395000065, -1.887292672027000018, -1.501864700490999960 ) ) ;
#44768=CARTESIAN_POINT ( 'NONE',  ( -1.667917367010000040, -55.51943307300000185, -12.49306752631999906 ) ) ;
#44770=ORIENTED_EDGE ( 'NONE', *, *, #43127, .F. ) ;
#44772=DIRECTION ( 'NONE',  ( 1.000000000000000000, 0.000000000000000000, 0.000000000000000000 ) ) ;
#44779=ORIENTED_EDGE ( 'NONE', *, *, #3191, .T. ) ;
#44781=VERTEX_POINT ( 'NONE', #3173 ) ;
#44782=VERTEX_POINT ( 'NONE', #21456 ) ;
#44783=CARTESIAN_POINT ( 'NONE',  ( -2.288966405475738597, -2.663704043780092956, -2.306431892470109712 ) ) ;
#44784=CARTESIAN_POINT ( 'NONE',  ( 11.79999999999999893, -23.15000000000000213, 0.000000000000000000 ) ) ;
#44785=CYLINDRICAL_SURFACE ( 'NONE', #17620, 0.5000000000000004441 ) ;
#44786=AXIS2_PLACEMENT_3D ( 'NONE', #37930, #15206, #27896 ) ;
#44787=ORIENTED_EDGE ( 'NONE', *, *, #30881, .T. ) ;
#44788=DIRECTION ( 'NONE',  ( -0.7071067811865475727, 0.000000000000000000, -0.7071067811865475727 ) ) ;
#44789=ORIENTED_EDGE ( 'NONE', *, *, #35835, .T. ) ;
#44793=LINE ( 'NONE', #17931, #49098 ) ;
#44794=CARTESIAN_POINT ( 'NONE',  ( -7.626500777234999973, -23.31584731985000047, -10.35747145892000098 ) ) ;
#44795=CARTESIAN_POINT ( 'NONE',  ( 5.891554620702148526, -77.36431389369244016, -10.19904068193172719 ) ) ;
#44796=CARTESIAN_POINT ( 'NONE',  ( -12.50000000000000000, -18.75000000000000000, 0.000000000000000000 ) ) ;
#44797=CARTESIAN_POINT ( 'NONE',  ( 7.678667886061999681, -57.04263462147999775, -10.59548767699999949 ) ) ;
#44799=CARTESIAN_POINT ( 'NONE',  ( -9.108250977391000092, -24.87811334491999915, 8.478720681740998799 ) ) ;
#44800=LINE ( 'NONE', #4352, #43284 ) ;
#44806=CARTESIAN_POINT ( 'NONE',  ( -12.54981748964999966, -16.95163512371999914, -0.03767836620435000006 ) ) ;
#44807=DIRECTION ( 'NONE',  ( -0.7272727272724163194, -0.6863485850246158204, -6.703676215667153735E-07 ) ) ;
#44808=CARTESIAN_POINT ( 'NONE',  ( -1.930009203935999951, -23.20099032317000365, 12.72537718777000038 ) ) ;
#44809=CARTESIAN_POINT ( 'NONE',  ( -7.919595949288999570, -55.64999999964999233, 9.050966799188000067 ) ) ;
#44811=CARTESIAN_POINT ( 'NONE',  ( -3.236421654187000119, -2.018566864578999809, 1.624998546076000139 ) ) ;
#44814=CARTESIAN_POINT ( 'NONE',  ( 12.66736977985000046, -61.03307288738999858, -1.690635117038999935 ) ) ;
#44816=CARTESIAN_POINT ( 'NONE',  ( 7.601397897754999633, -18.75000000000000000, 9.369164850722000892 ) ) ;
#44819=DIRECTION ( 'NONE',  ( 0.000000000000000000, 0.000000000000000000, -1.000000000000000000 ) ) ;
#44826=CARTESIAN_POINT ( 'NONE',  ( -12.56594317989000054, -23.24999999414999863, -1.750000000001000089 ) ) ;
#44827=TOROIDAL_SURFACE ( 'NONE', #1486, 17.50000000000000000, 5.000000000000000000 ) ;
#44832=CARTESIAN_POINT ( 'NONE',  ( -10.36292431360000066, -60.00096201600999990, 7.633479737330000070 ) ) ;
#44833=DIRECTION ( 'NONE',  ( 0.000000000000000000, 1.000000000000000000, 0.000000000000000000 ) ) ;
#44834=DIRECTION ( 'NONE',  ( -0.7071067811864980568, 0.7071067811865969777, 4.151099656137985125E-09 ) ) ;
#44836=CARTESIAN_POINT ( 'NONE',  ( -10.42531124903999995, -55.53514851492000304, 7.624341765436000173 ) ) ;
#44837=CARTESIAN_POINT ( 'NONE',  ( -1.667916687244999974, -60.09849137196000157, 12.49168433582000226 ) ) ;
#44838=EDGE_LOOP ( 'NONE', ( #53747, #27778, #22088, #34604 ) ) ;
#44839=CARTESIAN_POINT ( 'NONE',  ( -12.70299804974076530, -53.77411689953881790, 0.8844418155833001505 ) ) ;
#44843=CARTESIAN_POINT ( 'NONE',  ( -12.49168451095999899, -55.50151115525000023, -1.667916687331000070 ) ) ;
#44847=CARTESIAN_POINT ( 'NONE',  ( -1.537993320270047315, -77.81278135628818404, -11.67747152160435142 ) ) ;
#44848=CARTESIAN_POINT ( 'NONE',  ( -2.062670899361999766, -23.30639784948999704, 12.83044027760000105 ) ) ;
#44849=EDGE_CURVE ( 'NONE', #45077, #9760, #44720, .T. ) ;
#44851=ORIENTED_EDGE ( 'NONE', *, *, #4905, .T. ) ;
#44852=CARTESIAN_POINT ( 'NONE',  ( -7.620037552694999938, -55.59433113521999559, -10.53559761426999764 ) ) ;
#44855=VERTEX_POINT ( 'NONE', #15876 ) ;
#44861=CARTESIAN_POINT ( 'NONE',  ( 0.000000000000000000, -63.73717104351998586, 0.000000000000000000 ) ) ;
#44864=CARTESIAN_POINT ( 'NONE',  ( 12.64769468388000107, -77.22310353941999495, -3.464320626314000062 ) ) ;
#44866=CARTESIAN_POINT ( 'NONE',  ( -6.354078923955547964, -78.36956649114314644, 10.19482050615332369 ) ) ;
#44871=CARTESIAN_POINT ( 'NONE',  ( 7.624341764923000753, -18.73514850530999709, 10.42531124853000080 ) ) ;
#44872=ORIENTED_EDGE ( 'NONE', *, *, #2197, .F. ) ;
#44874=B_SPLINE_CURVE_WITH_KNOTS ( 'NONE', 3,
 ( #39218, #21787, #21210, #44233, #53374, #3223, #57231, #2927 ),
 .UNSPECIFIED., .F., .F.,
 ( 4, 2, 2, 4 ),
 ( 0.000000000000000000, 0.4999999999999995559, 0.7499999999999997780, 1.000000000000000000 ),
 .UNSPECIFIED. ) ;
#44875=CARTESIAN_POINT ( 'NONE',  ( 7.568503529865000523, -76.37430647614999657, 9.708412483427999007 ) ) ;
#44880=CARTESIAN_POINT ( 'NONE',  ( 3.432017302438363338, -3.081497486436961530, -0.7773794206622555159 ) ) ;
#44881=CARTESIAN_POINT ( 'NONE',  ( 12.50745077485999879, -53.80005551680000053, -2.012158279073999839E-09 ) ) ;
#44884=EDGE_CURVE ( 'NONE', #47498, #37882, #33510, .T. ) ;
#44886=CARTESIAN_POINT ( 'NONE',  ( -10.11788549770072621, -77.09584413801610481, -6.579903885935526553 ) ) ;
#44888=DIRECTION ( 'NONE',  ( -0.7071067811865474617, 0.000000000000000000, -0.7071067811865474617 ) ) ;
#44889=ORIENTED_EDGE ( 'NONE', *, *, #30211, .T. ) ;
#44892=CARTESIAN_POINT ( 'NONE',  ( 7.674627477118999508, -59.55077028051999832, -10.14950121126999960 ) ) ;
#44897=CARTESIAN_POINT ( 'NONE',  ( 0.4356486348728999536, -53.91935044157000334, -12.43591427117000059 ) ) ;
#44898=CARTESIAN_POINT ( 'NONE',  ( 5.240463812692992107, -76.03770333581218210, 10.52392510242733259 ) ) ;
#44900=PLANE ( 'NONE',  #12487 ) ;
#44903=CARTESIAN_POINT ( 'NONE',  ( 7.331368884251999951, -75.87423312637412209, 9.888700222343000945 ) ) ;
#44908=CARTESIAN_POINT ( 'NONE',  ( 9.722718241315000398, -60.24678171298000251, -7.954951288349001004 ) ) ;
#44910=ORIENTED_EDGE ( 'NONE', *, *, #35376, .T. ) ;
#44914=CARTESIAN_POINT ( 'NONE',  ( 8.302863715705628422, -76.38741280764111252, -8.314095789455475227 ) ) ;
#44915=ADVANCED_FACE ( 'NONE', ( #51547 ), #6655, .F. ) ;
#44918=CARTESIAN_POINT ( 'NONE',  ( 11.00000000000000533, -23.75000000000000355, -0.1604995627819790494 ) ) ;
#44919=EDGE_CURVE ( 'NONE', #44548, #2890, #55668, .T. ) ;
#44921=FACE_OUTER_BOUND ( 'NONE', #25956, .T. ) ;
#44922=AXIS2_PLACEMENT_3D ( 'NONE', #2290, #56301, #52169 ) ;
#44925=CARTESIAN_POINT ( 'NONE',  ( 0.000000000000000000, -32.36102867817999851, 0.000000000000000000 ) ) ;
#44926=DIRECTION ( 'NONE',  ( 0.7071067811865475727, 0.000000000000000000, 0.7071067811865475727 ) ) ;
#44928=AXIS2_PLACEMENT_3D ( 'NONE', #40609, #40311, #45046 ) ;
#44929=ORIENTED_EDGE ( 'NONE', *, *, #33347, .T. ) ;
#44935=CARTESIAN_POINT ( 'NONE',  ( 9.389195554418000356, -24.71043214204999927, 8.194863653270999748 ) ) ;
#44938=CARTESIAN_POINT ( 'NONE',  ( 8.190859204290999784, -55.64999999967000122, -7.342331066867000544 ) ) ;
#44940=EDGE_CURVE ( 'NONE', #30569, #35193, #32333, .T. ) ;
#44950=CARTESIAN_POINT ( 'NONE',  ( 11.93795915497000060, -75.96753699673999449, -4.186706965401000069 ) ) ;
#44952=DIRECTION ( 'NONE',  ( 0.000000000000000000, -1.000000000000000000, 0.000000000000000000 ) ) ;
#44954=EDGE_CURVE ( 'NONE', #31323, #51555, #46247, .T. ) ;
#44955=CARTESIAN_POINT ( 'NONE',  ( 12.54987159816999842, -16.94886760191999997, -0.1385534523823999942 ) ) ;
#44956=CARTESIAN_POINT ( 'NONE',  ( 12.00000000000000000, -55.54999999966999980, 1.750000000000000000 ) ) ;
#44964=CARTESIAN_POINT ( 'NONE',  ( 3.250000000000000444, -3.260416666666665630, 0.4254240051736248862 ) ) ;
#44965=CIRCLE ( 'NONE', #14774, 1.749999999999998446 ) ;
#44966=CARTESIAN_POINT ( 'NONE',  ( 10.26699006316253637, -78.50833333333332575, -5.917523019358050362 ) ) ;
#44967=CARTESIAN_POINT ( 'NONE',  ( 12.50000000000000000, -23.25000000000000000, 0.000000000000000000 ) ) ;
#44969=CARTESIAN_POINT ( 'NONE',  ( 10.59548767697000038, -58.55736537918999574, -7.678667886039000301 ) ) ;
#44972=CARTESIAN_POINT ( 'NONE',  ( -0.8506806241676722058, -1.895833333333333037, 3.165411199172021739 ) ) ;
#44976=EDGE_CURVE ( 'NONE', #14764, #43451, #26783, .T. ) ;
#44977=CARTESIAN_POINT ( 'NONE',  ( -1.382886570148999850, -54.16901780135000166, 12.65982054472000051 ) ) ;
#44978=CARTESIAN_POINT ( 'NONE',  ( -1.798944584240000255, -60.01533228248000285, -12.61116916001999932 ) ) ;
#44979=CARTESIAN_POINT ( 'NONE',  ( -1.897426238260999876, -3.722918480970999866, 3.187324685277999947 ) ) ;
#44982=CARTESIAN_POINT ( 'NONE',  ( -0.7999999997951999786, -23.14999999072999870, -11.99999999979999821 ) ) ;
#44983=CARTESIAN_POINT ( 'NONE',  ( -1.890224871705999954, -60.54789247981999267, 12.68696160876999990 ) ) ;
#44984=CARTESIAN_POINT ( 'NONE',  ( 12.43640296266999989, -17.08252466130999991, -0.05222744260230000046 ) ) ;
#44986=CARTESIAN_POINT ( 'NONE',  ( 0.000000000000000000, -6.100000000000000533, 0.000000000000000000 ) ) ;
#44987=CARTESIAN_POINT ( 'NONE',  ( 12.06472673805143536, -76.70531092299836473, 0.3523124688570539731 ) ) ;
#44988=FACE_OUTER_BOUND ( 'NONE', #49005, .T. ) ;
#44992=CARTESIAN_POINT ( 'NONE',  ( -1.217390015640017253, -61.61893024898913040, 12.70229597944532252 ) ) ;
#44994=B_SPLINE_CURVE_WITH_KNOTS ( 'NONE', 3,
 ( #41366, #27475, #28348, #54935, #55523, #27769, #23058, #28644, #18647, #46694 ),
 .UNSPECIFIED., .F., .F.,
 ( 4, 2, 2, 2, 4 ),
 ( 0.000000000000000000, 0.2500000000000000000, 0.5000000000000000000, 0.7500000000000000000, 1.000000000000000000 ),
 .UNSPECIFIED. ) ;
#44995=CARTESIAN_POINT ( 'NONE',  ( -12.66319951814999989, -61.98148258098999719, 0.1455783832297999902 ) ) ;
#44996=CARTESIAN_POINT ( 'NONE',  ( 13.99999999996999911, -5.900000000026970781, -3.874887541704999824E-10 ) ) ;
#45005=VERTEX_POINT ( 'NONE', #14919 ) ;
#45007=ORIENTED_EDGE ( 'NONE', *, *, #41542, .F. ) ;
#45009=AXIS2_PLACEMENT_3D ( 'NONE', #49471, #30844, #4595 ) ;
#45011=DIRECTION ( 'NONE',  ( 0.000000000000000000, -1.000000000000000000, 0.000000000000000000 ) ) ;
#45015=CARTESIAN_POINT ( 'NONE',  ( 11.75000000000000000, -77.54999999999999716, 2.316376715183999699E-14 ) ) ;
#45017=CARTESIAN_POINT ( 'NONE',  ( 1.667269374596999976, -23.20939883484999910, -12.49858097730999873 ) ) ;
#45020=LINE ( 'NONE', #4867, #37536 ) ;
#45021=CARTESIAN_POINT ( 'NONE',  ( -9.112421873709999787, -79.06464140765000082, -8.348385936088000392 ) ) ;
#45022=AXIS2_PLACEMENT_3D ( 'NONE', #41006, #23573, #54869 ) ;
#45024=ORIENTED_EDGE ( 'NONE', *, *, #52773, .T. ) ;
#45025=CARTESIAN_POINT ( 'NONE',  ( -7.601397897754999633, -18.75000000310999937, 10.07627163191000008 ) ) ;
#45026=CARTESIAN_POINT ( 'NONE',  ( -1.423904377506317820, -17.69487194798944429, -12.50677628656574747 ) ) ;
#45027=CIRCLE ( 'NONE', #34627, 0.5000000000000000000 ) ;
#45033=CARTESIAN_POINT ( 'NONE',  ( 6.861116763436999832, -76.59221882925000102, -9.781075755418999762 ) ) ;
#45034=EDGE_CURVE ( 'NONE', #6045, #22190, #41896, .T. ) ;
#45038=DIRECTION ( 'NONE',  ( -0.7071067811865475727, 0.000000000000000000, -0.7071067811865475727 ) ) ;
#45041=CARTESIAN_POINT ( 'NONE',  ( -10.38646360829000059, -56.02204592290999585, 7.655555357438999842 ) ) ;
#45046=DIRECTION ( 'NONE',  ( -1.000000000000000000, 0.000000000000000000, 0.000000000000000000 ) ) ;
#45049=CARTESIAN_POINT ( 'NONE',  ( 0.07399134906894000441, -2.190786218217000147, 3.805339572302000040 ) ) ;
#45051=ORIENTED_EDGE ( 'NONE', *, *, #56017, .F. ) ;
#45052=CARTESIAN_POINT ( 'NONE',  ( 0.000000000000000000, 4.040000000000000036, 0.000000000000000000 ) ) ;
#45053=ADVANCED_FACE ( 'NONE', ( #43843 ), #465, .F. ) ;
#45056=DIRECTION ( 'NONE',  ( 1.000000000000000000, 0.000000000000000000, 0.000000000000000000 ) ) ;
#45057=CARTESIAN_POINT ( 'NONE',  ( 12.56884868898000107, -76.71184971201999758, -3.366471670097000324 ) ) ;
#45059=CARTESIAN_POINT ( 'NONE',  ( 12.60552522436000089, -23.28917565320000094, -1.799501877760999902 ) ) ;
#45060=EDGE_LOOP ( 'NONE', ( #52249, #20724, #17265, #15108 ) ) ;
#45061=CARTESIAN_POINT ( 'NONE',  ( -13.86363636363000218, -69.16102867818000277, -1.277888281761000050E-05 ) ) ;
#45062=DIRECTION ( 'NONE',  ( 0.7071067811865474617, 0.000000000000000000, -0.7071067811865474617 ) ) ;
#45065=DIRECTION ( 'NONE',  ( 0.000000000000000000, -1.000000000000000000, 0.000000000000000000 ) ) ;
#45068=CARTESIAN_POINT ( 'NONE',  ( -1.182840957218999955, -1.453210179782000067, -3.838043326965000279 ) ) ;
#45069=CARTESIAN_POINT ( 'NONE',  ( -2.062673488410000200, -60.12452273675999947, -12.82904109066000053 ) ) ;
#45074=CARTESIAN_POINT ( 'NONE',  ( -0.5999999999999999778, -23.15000000000000213, -12.00000000000000000 ) ) ;
#45076=ORIENTED_EDGE ( 'NONE', *, *, #49441, .T. ) ;
#45077=VERTEX_POINT ( 'NONE', #29939 ) ;
#45081=EDGE_LOOP ( 'NONE', ( #58335, #28578, #52587, #20941 ) ) ;
#45084=ORIENTED_EDGE ( 'NONE', *, *, #26314, .T. ) ;
#45085=CARTESIAN_POINT ( 'NONE',  ( 1.292332971236618944, -2.758531009554976876, -2.981824453458054691 ) ) ;
#45088=B_SPLINE_SURFACE_WITH_KNOTS ( 'NONE', 3, 3, ( 
 ( #34260, #47881, #43149, #43429 ),
 ( #51725, #52011, #52580, #34835 ),
 ( #52865, #20132, #29543, #11277 ),
 ( #29255, #42856, #42565, #12419 ),
 ( #47012, #2131, #52292, #38120 ),
 ( #20988, #15691, #34548, #38412 ),
 ( #33687, #2416, #6830, #2989 ),
 ( #20418, #7412, #56432, #12131 ) ),
 .UNSPECIFIED., .F., .F., .F.,
 ( 4, 1, 1, 1, 1, 4 ),
 ( 4, 4 ),
 ( -0.01200407345746999990, 0.000000000000000000, 0.3333333333333000081, 0.6666666666667000474, 1.000000000000000000, 1.011997855551999947 ),
 ( -0.3559705542741999906, 1.355970554273999928 ),
 .UNSPECIFIED. ) ;
#45089=ORIENTED_EDGE ( 'NONE', *, *, #35530, .T. ) ;
#45091=ORIENTED_EDGE ( 'NONE', *, *, #54291, .F. ) ;
#45092=CARTESIAN_POINT ( 'NONE',  ( 3.250000000000000000, -2.350000000000000089, 0.000000000000000000 ) ) ;
#45096=CARTESIAN_POINT ( 'NONE',  ( -7.655542440070999710, -22.77819125662999866, -10.38645071867999903 ) ) ;
#45097=CARTESIAN_POINT ( 'NONE',  ( 5.917523019358037040, -77.13333333333329733, 10.26699006316254525 ) ) ;
#45099=CARTESIAN_POINT ( 'NONE',  ( -1.704789468943344266, -55.09653838336419085, 12.53199752951682022 ) ) ;
#45100=CARTESIAN_POINT ( 'NONE',  ( 7.641012386057000505, -60.08917565288000162, -10.18589234709999936 ) ) ;
#45102=EDGE_CURVE ( 'NONE', #3351, #33164, #21190, .T. ) ;
#45103=CARTESIAN_POINT ( 'NONE',  ( -9.996770077869998161, -24.15065455350000079, 7.758602204116000323 ) ) ;
#45106=CARTESIAN_POINT ( 'NONE',  ( 7.220923959705223716, -76.62291666666662593, 9.396085398178630754 ) ) ;
#45110=AXIS2_PLACEMENT_3D ( 'NONE', #12704, #35717, #54556 ) ;
#45112=CARTESIAN_POINT ( 'NONE',  ( -0.8537148449481000156, -24.70498145908999987, 12.43377424872999981 ) ) ;
#45115=CARTESIAN_POINT ( 'NONE',  ( -3.960388868909999971, -0.8168122488617000077, -1.146868004699999943 ) ) ;
#45118=EDGE_CURVE ( 'NONE', #37124, #35685, #6115, .T. ) ;
#45121=CARTESIAN_POINT ( 'NONE',  ( 12.66319951814999989, -61.98148258098999719, -0.1455783832297999902 ) ) ;
#45123=CARTESIAN_POINT ( 'NONE',  ( -13.13047446164998711, -22.78578169018998878, 0.8260994316375004365 ) ) ;
#45130=VERTEX_POINT ( 'NONE', #39106 ) ;
#45136=CARTESIAN_POINT ( 'NONE',  ( -10.01752098898000121, -59.99172009619000079, 7.660412494194000388 ) ) ;
#45138=LINE ( 'NONE', #32400, #17607 ) ;
#45140=CARTESIAN_POINT ( 'NONE',  ( -2.836899952100275790, -3.141950402152397626, -1.634619481798827545 ) ) ;
#45141=CARTESIAN_POINT ( 'NONE',  ( -1.931043742978000077, -56.02204592290999585, 12.75763395696999858 ) ) ;
#45142=VERTEX_POINT ( 'NONE', #47416 ) ;
#45143=FACE_OUTER_BOUND ( 'NONE', #34089, .T. ) ;
#45144=CARTESIAN_POINT ( 'NONE',  ( -7.601397897754999633, -55.55000000278000272, 10.07627163191000008 ) ) ;
#45149=CARTESIAN_POINT ( 'NONE',  ( 10.98521615365917725, -23.34051012009622283, 0.5703160980905067623 ) ) ;
#45152=CARTESIAN_POINT ( 'NONE',  ( -2.062597299672999540, -22.78485473281999774, 12.87022657272000004 ) ) ;
#45153=ORIENTED_EDGE ( 'NONE', *, *, #34364, .F. ) ;
#45154=EDGE_CURVE ( 'NONE', #22042, #26124, #54207, .T. ) ;
#45155=EDGE_LOOP ( 'NONE', ( #12592, #53794, #10581, #45051 ) ) ;
#45157=CARTESIAN_POINT ( 'NONE',  ( -10.18127254042999930, -55.41355771686999532, -7.633407132363999814 ) ) ;
#45160=ORIENTED_EDGE ( 'NONE', *, *, #16825, .T. ) ;
#45164=ORIENTED_EDGE ( 'NONE', *, *, #44498, .F. ) ;
#45167=CARTESIAN_POINT ( 'NONE',  ( -9.306321164319999895, -77.05658961653000461, -9.238944841226000904 ) ) ;
#45173=ORIENTED_EDGE ( 'NONE', *, *, #55067, .F. ) ;
#45174=DIRECTION ( 'NONE',  ( 0.000000000000000000, -1.000000000000000000, 0.000000000000000000 ) ) ;
#45176=CARTESIAN_POINT ( 'NONE',  ( 11.65396969189999865, -75.74817663119999622, -2.860942225950000140 ) ) ;
#45180=AXIS2_PLACEMENT_3D ( 'NONE', #21077, #25214, #12221 ) ;
#45181=CARTESIAN_POINT ( 'NONE',  ( 12.82904109062999964, -18.67547726287999765, 2.062673488410000200 ) ) ;
#45185=CARTESIAN_POINT ( 'NONE',  ( 11.51565071235703464, -76.77562505554482186, -3.637760148594212151 ) ) ;
#45186=CARTESIAN_POINT ( 'NONE',  ( 12.17658135360961147, -76.23143817709451753, 4.630469027495792034 ) ) ;
#45190=FACE_OUTER_BOUND ( 'NONE', #29246, .T. ) ;
#45191=AXIS2_PLACEMENT_3D ( 'NONE', #38224, #7803, #43831 ) ;
#45196=CARTESIAN_POINT ( 'NONE',  ( 0.000000000000000000, -3.749999999256000027, 0.000000000000000000 ) ) ;
#45198=CARTESIAN_POINT ( 'NONE',  ( 0.5528049087483969393, -76.07108491924718408, 11.73740210370585579 ) ) ;
#45201=VERTEX_POINT ( 'NONE', #15807 ) ;
#45202=CARTESIAN_POINT ( 'NONE',  ( -12.19234209666000091, -76.06101097214411766, -1.697737568323999913 ) ) ;
#45207=CYLINDRICAL_SURFACE ( 'NONE', #5729, 0.5000000000000006661 ) ;
#45208=FACE_OUTER_BOUND ( 'NONE', #21182, .T. ) ;
#45211=DIRECTION ( 'NONE',  ( 0.000000000000000000, -1.000000000000000000, 0.000000000000000000 ) ) ;
#45216=CARTESIAN_POINT ( 'NONE',  ( 12.50680023857767154, -61.10414033366100739, 1.424451025847232044 ) ) ;
#45218=DIRECTION ( 'NONE',  ( -0.7071067811865475727, 0.000000000000000000, 0.7071067811865475727 ) ) ;
#45220=EDGE_CURVE ( 'NONE', #58165, #27335, #53222, .T. ) ;
#45227=ORIENTED_EDGE ( 'NONE', *, *, #16816, .T. ) ;
#45230=VECTOR ( 'NONE', #42894, 1000.000000000000000 ) ;
#45231=ORIENTED_EDGE ( 'NONE', *, *, #50804, .T. ) ;
#45234=CARTESIAN_POINT ( 'NONE',  ( 9.636781270573999691, -24.44031362782000016, 7.948066289838000564 ) ) ;
#45236=CARTESIAN_POINT ( 'NONE',  ( 7.342331066867000544, -55.64999999967000122, -8.190859204290999784 ) ) ;
#45241=ORIENTED_EDGE ( 'NONE', *, *, #18549, .T. ) ;
#45243=ORIENTED_EDGE ( 'NONE', *, *, #56248, .T. ) ;
#45247=DIRECTION ( 'NONE',  ( -1.000000000000000000, 0.000000000000000000, 0.000000000000000000 ) ) ;
#45249=CARTESIAN_POINT ( 'NONE',  ( -2.529679113815999969, -76.39605739169999765, 12.87721456411999910 ) ) ;
#45255=CARTESIAN_POINT ( 'NONE',  ( -11.74964429611623729, -76.69742914047841964, 0.2920691019370554309 ) ) ;
#45256=ADVANCED_FACE ( 'NONE', ( #12809 ), #18134, .F. ) ;
#45259=VERTEX_POINT ( 'NONE', #31977 ) ;
#45263=EDGE_CURVE ( 'NONE', #11057, #15123, #40565, .T. ) ;
#45265=DIRECTION ( 'NONE',  ( 0.000000000000000000, -1.000000000000000000, 0.000000000000000000 ) ) ;
#45267=CARTESIAN_POINT ( 'NONE',  ( -1.103931346216595166, -54.17916251667382710, 12.50298439255883665 ) ) ;
#45270=DIRECTION ( 'NONE',  ( 0.000000000000000000, 1.000000000000000000, 0.000000000000000000 ) ) ;
#45272=CARTESIAN_POINT ( 'NONE',  ( -2.598917237794094337, -1.947916666666666741, 1.997276839918461722 ) ) ;
#45275=CARTESIAN_POINT ( 'NONE',  ( 1.890224871708999999, -55.05210751953000425, 12.68696160870999989 ) ) ;
#45276=CARTESIAN_POINT ( 'NONE',  ( -1.801750019961000149, -60.19007426689000084, -12.59656967656000148 ) ) ;
#45277=CARTESIAN_POINT ( 'NONE',  ( 3.912230941219999369, -3.068769585190000093, 0.6523515869903999675 ) ) ;
#45281=CARTESIAN_POINT ( 'NONE',  ( -1.997276839918471714, -1.572916666666666741, -2.598917237794086788 ) ) ;
#45284=CARTESIAN_POINT ( 'NONE',  ( 12.66319948256999872, -16.81851729361000380, 0.1456213732515000137 ) ) ;
#45289=CARTESIAN_POINT ( 'NONE',  ( -12.80742885296000111, -79.00613957653999364, -1.906747295896999983 ) ) ;
#45293=CARTESIAN_POINT ( 'NONE',  ( 0.9935076047078643668, -61.76816187723569129, 12.70250268220879875 ) ) ;
#45297=CARTESIAN_POINT ( 'NONE',  ( -8.838834764832000701, -23.25000000000000000, -8.838834764832000701 ) ) ;
#45299=ORIENTED_EDGE ( 'NONE', *, *, #40532, .F. ) ;
#45300=EDGE_CURVE ( 'NONE', #42021, #37146, #27267, .T. ) ;
#45305=ORIENTED_EDGE ( 'NONE', *, *, #46337, .T. ) ;
#45306=ORIENTED_EDGE ( 'NONE', *, *, #16367, .T. ) ;
#45311=ORIENTED_EDGE ( 'NONE', *, *, #2760, .T. ) ;
#45312=CARTESIAN_POINT ( 'NONE',  ( 7.954951288349001004, -55.54999999966999980, -9.722718241315000398 ) ) ;
#45315=CARTESIAN_POINT ( 'NONE',  ( 0.005119011380242999981, -24.93813862189000119, -12.43705489344000092 ) ) ;
#45317=LINE ( 'NONE', #4574, #47942 ) ;
#45318=CARTESIAN_POINT ( 'NONE',  ( 12.01346855044000073, -78.57433180934999939, -1.078935046565000277 ) ) ;
#45320=VERTEX_POINT ( 'NONE', #8102 ) ;
#45321=LINE ( 'NONE', #40293, #26328 ) ;
#45322=CARTESIAN_POINT ( 'NONE',  ( -1.001315002179000047, -17.31477588286000113, -12.50000000000000000 ) ) ;
#45324=AXIS2_PLACEMENT_3D ( 'NONE', #54938, #46107, #46984 ) ;
#45326=AXIS2_PLACEMENT_3D ( 'NONE', #9632, #31751, #14628 ) ;
#45328=FACE_OUTER_BOUND ( 'NONE', #19605, .T. ) ;
#45329=CARTESIAN_POINT ( 'NONE',  ( -10.59557217617999925, -76.86974203406001038, 7.456311996931999531 ) ) ;
#45335=CARTESIAN_POINT ( 'NONE',  ( -10.01332844639000008, -60.08056692637000396, 7.654537085048000122 ) ) ;
#45336=CARTESIAN_POINT ( 'NONE',  ( -7.489529519948906255, -78.22972517753335353, 9.112965939832363915 ) ) ;
#45339=DIRECTION ( 'NONE',  ( 4.762495317921000031E-11, 1.000000000000000000, 4.762531464717999529E-11 ) ) ;
#45341=CARTESIAN_POINT ( 'NONE',  ( -0.4587696627765999735, -3.467384982432999863, -3.778272981138000031 ) ) ;
#45342=DIRECTION ( 'NONE',  ( -0.9999999924279685537, 0.000000000000000000, -0.0001230612157848962919 ) ) ;
#45343=ORIENTED_EDGE ( 'NONE', *, *, #27348, .T. ) ;
#45344=DIRECTION ( 'NONE',  ( -0.7071067811865474617, -3.445410891336226740E-11, 0.7071067811865474617 ) ) ;
#45345=CARTESIAN_POINT ( 'NONE',  ( -0.5705388283868735311, -18.65989902471411810, -10.98520465578141092 ) ) ;
#45348=AXIS2_PLACEMENT_3D ( 'NONE', #24709, #2286, #38568 ) ;
#45349=CARTESIAN_POINT ( 'NONE',  ( 1.931086388578000079, -55.50221245779999890, 12.71798269383000068 ) ) ;
#45350=CARTESIAN_POINT ( 'NONE',  ( -12.96685733093999993, -76.98937291683000694, -1.095351912296000041 ) ) ;
#45353=EDGE_CURVE ( 'NONE', #21333, #47059, #33420, .T. ) ;
#45354=CARTESIAN_POINT ( 'NONE',  ( -7.610716808857792337, -60.32015489447598355, -10.41172350879243780 ) ) ;
#45355=CARTESIAN_POINT ( 'NONE',  ( 12.75761570870000128, -19.22180874373999870, -1.931043762602999925 ) ) ;
#45359=CARTESIAN_POINT ( 'NONE',  ( 2.426647618366999603E-14, -5.949999999936550488, 0.000000000000000000 ) ) ;
#45360=TOROIDAL_SURFACE ( 'NONE', #24620, 17.50000000000000000, 5.000000000000000000 ) ;
#45363=CARTESIAN_POINT ( 'NONE',  ( -1.180494763713999973, -0.6845217200523000534, 3.461421590595000097 ) ) ;
#45364=CARTESIAN_POINT ( 'NONE',  ( -1.930989144707000005, -58.55365779174999830, -12.80900240954000147 ) ) ;
#45366=ORIENTED_EDGE ( 'NONE', *, *, #32927, .T. ) ;
#45369=AXIS2_PLACEMENT_3D ( 'NONE', #18831, #46591, #41549 ) ;
#45376=B_SPLINE_CURVE_WITH_KNOTS ( 'NONE', 3,
 ( #45, #5022, #49910, #629, #17728, #31273, #26857, #14160, #338, #45186, #39855, #18612, #36600, #18020, #22734, #9745, #49617, #40745, #49021 ),
 .UNSPECIFIED., .F., .F.,
 ( 4, 1, 1, 1, 1, 1, 1, 1, 1, 1, 1, 1, 1, 1, 1, 1, 4 ),
 ( 0.000000000000000000, 0.04500236217446485637, 0.1100020431571605006, 0.1750017241396574219, 0.2400014051223532952, 0.3050010861050493904, 0.3700007670877452637, 0.4350004480702421850, 0.5000001290529377806, 0.5649998100356339314, 0.6299994910183297492, 0.6949991720008267260, 0.7599988529835225437, 0.8249985339662186945, 0.8899982149487153382, 0.9549978959314112670, 1.000000000000000000 ),
 .UNSPECIFIED. ) ;
#45378=EDGE_LOOP ( 'NONE', ( #46908, #7059, #2254, #44560, #25768, #30700 ) ) ;
#45382=CARTESIAN_POINT ( 'NONE',  ( -1.960246996891127136, -2.673871147968344353, -2.594988089372104678 ) ) ;
#45385=CARTESIAN_POINT ( 'NONE',  ( 9.369164850722000892, -23.25000000000000000, 7.601397897754999633 ) ) ;
#45387=EDGE_CURVE ( 'NONE', #38967, #34794, #56767, .T. ) ;
#45391=ORIENTED_EDGE ( 'NONE', *, *, #12233, .F. ) ;
#45395=CARTESIAN_POINT ( 'NONE',  ( -7.682331425175999762, -22.76486430425999785, -10.04115011118000211 ) ) ;
#45396=CARTESIAN_POINT ( 'NONE',  ( -1.165746613897999928E-14, -72.79999999999999716, 0.000000000000000000 ) ) ;
#45397=CARTESIAN_POINT ( 'NONE',  ( 10.66325342011824162, -76.51486258876667534, -5.043235781625467595 ) ) ;
#45401=CARTESIAN_POINT ( 'NONE',  ( -13.98934701867000108, -9.421869816320000979, -1.420930503335999789E-05 ) ) ;
#45404=CARTESIAN_POINT ( 'NONE',  ( 12.50000000000000000, -60.04999999725999515, -1.750000000000000000 ) ) ;
#45405=CARTESIAN_POINT ( 'NONE',  ( 9.396085398178598780, -76.60208333333331154, 7.220923959705271677 ) ) ;
#45408=CARTESIAN_POINT ( 'NONE',  ( -12.55485633994999795, -17.84594908780999845, 1.580761757392000089 ) ) ;
#45409=DIRECTION ( 'NONE',  ( 0.000000000000000000, -1.000000000000000000, 0.000000000000000000 ) ) ;
#45410=CARTESIAN_POINT ( 'NONE',  ( -0.4450739772391999471, -24.87813214802000061, 12.43586747594999942 ) ) ;
#45412=CARTESIAN_POINT ( 'NONE',  ( -0.7058306598777001062, -1.946219782538000098, 3.554007990761999913 ) ) ;
#45415=CARTESIAN_POINT ( 'NONE',  ( 12.54705830253000087, -61.33699017322999936, -1.287129557046000183 ) ) ;
#45417=CARTESIAN_POINT ( 'NONE',  ( -10.01332852689000141, -23.28056535155999995, -7.654537165468999760 ) ) ;
#45420=CARTESIAN_POINT ( 'NONE',  ( 0.000000000000000000, -18.75000000000000000, -12.50000000000000000 ) ) ;
#45424=ORIENTED_EDGE ( 'NONE', *, *, #40760, .F. ) ;
#45427=B_SPLINE_CURVE_WITH_KNOTS ( 'NONE', 3,
 ( #13346, #22509, #8636, #8933, #40219, #26052 ),
 .UNSPECIFIED., .F., .F.,
 ( 4, 1, 1, 4 ),
 ( 0.000000000000000000, 0.3333333333333000081, 0.6666666666667000474, 1.000000000000000000 ),
 .UNSPECIFIED. ) ;
#45430=CARTESIAN_POINT ( 'NONE',  ( 12.66315144082999922, -53.62197088156000291, 0.06064144874944999569 ) ) ;
#45431=CARTESIAN_POINT ( 'NONE',  ( 0.000000000000000000, -63.73717104351998586, 0.000000000000000000 ) ) ;
#45433=CARTESIAN_POINT ( 'NONE',  ( -11.75000000000000178, -76.30865979610494776, -1.278660935777401475 ) ) ;
#45434=CARTESIAN_POINT ( 'NONE',  ( -9.019414221598461623, -61.79291943934574505, 8.666941069244513685 ) ) ;
#45442=CARTESIAN_POINT ( 'NONE',  ( -12.50745077490000057, -17.00005551713000074, 2.011909873286000185E-09 ) ) ;
#45443=DIRECTION ( 'NONE',  ( 0.7071067811865474617, 0.000000000000000000, 0.7071067811865474617 ) ) ;
#45446=CARTESIAN_POINT ( 'NONE',  ( 10.41172477450676581, -60.32013115014468951, -7.610718073431629094 ) ) ;
#45449=ORIENTED_EDGE ( 'NONE', *, *, #46589, .F. ) ;
#45450=CARTESIAN_POINT ( 'NONE',  ( -10.36292447788999915, -55.59904187545999577, -7.633480004398999874 ) ) ;
#45451=SURFACE_SIDE_STYLE ('',( #45750 ) ) ;
#45460=DIRECTION ( 'NONE',  ( 0.7272727272724163194, -0.6863485850246158204, 6.703676227819155323E-07 ) ) ;
#45462=CARTESIAN_POINT ( 'NONE',  ( 0.000000000000000000, -23.25000000000000000, 12.50000000000000000 ) ) ;
#45467=VERTEX_POINT ( 'NONE', #17840 ) ;
#45468=FACE_OUTER_BOUND ( 'NONE', #19830, .T. ) ;
#45469=CARTESIAN_POINT ( 'NONE',  ( -3.438348731682000281, -76.65447324480000191, -11.82003900998999946 ) ) ;
#45471=EDGE_CURVE ( 'NONE', #30968, #26684, #8866, .T. ) ;
#45473=CARTESIAN_POINT ( 'NONE',  ( 7.620037246310000789, -60.00567269791999792, -10.53559750860999955 ) ) ;
#45474=CARTESIAN_POINT ( 'NONE',  ( -1.777672186646999997, -78.90390915793000204, 12.13420648597999829 ) ) ;
#45476=CARTESIAN_POINT ( 'NONE',  ( -3.453171399369999950, -1.863032031399000088, -0.5706200895263999762 ) ) ;
#45478=CARTESIAN_POINT ( 'NONE',  ( 12.06634091025675204, -77.30042855182080075, 0.05712547007327853366 ) ) ;
#45479=CARTESIAN_POINT ( 'NONE',  ( 9.050966799188000067, -55.64999999964999233, 7.919595949288999570 ) ) ;
#45491=CARTESIAN_POINT ( 'NONE',  ( 3.155060921293558085, -76.05290718790978133, 11.32013784086210961 ) ) ;
#45494=VERTEX_POINT ( 'NONE', #6293 ) ;
#45496=CIRCLE ( 'NONE', #5901, 0.5000000000000004441 ) ;
#45500=FACE_OUTER_BOUND ( 'NONE', #55574, .T. ) ;
#45502=FACE_OUTER_BOUND ( 'NONE', #52280, .T. ) ;
#45503=CARTESIAN_POINT ( 'NONE',  ( 7.634437838915999919, -18.25219468451000182, -10.30764259110000047 ) ) ;
#45506=VECTOR ( 'NONE', #1352, 1000.000000000000000 ) ;
#45507=CARTESIAN_POINT ( 'NONE',  ( 12.70255494774207961, -17.25391159036992050, 1.306413223736588858 ) ) ;
#45508=CARTESIAN_POINT ( 'NONE',  ( 12.50728617048449465, -53.80024476432964065, 0.1757991156898129625 ) ) ;
#45512=CARTESIAN_POINT ( 'NONE',  ( 11.45098972023387240, -76.43180119005340600, -2.636752081925491265 ) ) ;
#45514=EDGE_CURVE ( 'NONE', #6488, #4486, #43374, .T. ) ;
#45521=CARTESIAN_POINT ( 'NONE',  ( -12.66001556632000025, -24.63260856943000121, 1.381621105852999909 ) ) ;
#45522=ORIENTED_EDGE ( 'NONE', *, *, #4777, .F. ) ;
#45523=EDGE_CURVE ( 'NONE', #51133, #47356, #51398, .T. ) ;
#45524=EDGE_LOOP ( 'NONE', ( #49868, #19964, #17111, #53602 ) ) ;
#45527=AXIS2_PLACEMENT_3D ( 'NONE', #38051, #43353, #2913 ) ;
#45528=EDGE_LOOP ( 'NONE', ( #34516, #6671, #23854 ) ) ;
#45529=FACE_OUTER_BOUND ( 'NONE', #11539, .T. ) ;
#45530=CARTESIAN_POINT ( 'NONE',  ( 7.753906807039999904, -24.28933445982999828, 10.31979621049999807 ) ) ;
#45531=CARTESIAN_POINT ( 'NONE',  ( 7.622785526051999661, -60.58712283452999259, 10.47836401508999948 ) ) ;
#45534=AXIS2_PLACEMENT_3D ( 'NONE', #28902, #42499, #46948 ) ;
#45538=CARTESIAN_POINT ( 'NONE',  ( -10.42531125068999920, -23.26485145404000221, 7.624341767093000044 ) ) ;
#45542=DIRECTION ( 'NONE',  ( 0.7071067811865475727, 0.000000000000000000, -0.7071067811865475727 ) ) ;
#45544=AXIS2_PLACEMENT_3D ( 'NONE', #494, #10488, #23187 ) ;
#45545=CARTESIAN_POINT ( 'NONE',  ( -12.96570439747000059, -75.91866156851000369, -0.01980505094338999919 ) ) ;
#45548=DIRECTION ( 'NONE',  ( 2.505275680394999719E-13, -1.000000000000000000, -2.029755673547999903E-12 ) ) ;
#45550=CARTESIAN_POINT ( 'NONE',  ( -7.631889049354000143, -23.22121504852000129, -10.36222434949000082 ) ) ;
#45551=CARTESIAN_POINT ( 'NONE',  ( -7.997114030248268612, -60.48581381147864988, 7.553727747482917643 ) ) ;
#45558=DIRECTION ( 'NONE',  ( 0.000000000000000000, -1.000000000000000000, 0.000000000000000000 ) ) ;
#45559=ADVANCED_FACE ( 'NONE', ( #9565 ), #55013, .F. ) ;
#45560=CARTESIAN_POINT ( 'NONE',  ( -1.750000000001000089, -60.05000000958000328, -12.56594317859000043 ) ) ;
#45561=CARTESIAN_POINT ( 'NONE',  ( 12.50000000000000000, -60.24678171298000251, 1.250000000000000000 ) ) ;
#45562=LINE ( 'NONE', #13950, #32685 ) ;
#45567=CYLINDRICAL_SURFACE ( 'NONE', #29044, 12.50000000000000000 ) ;
#45569=VERTEX_POINT ( 'NONE', #37581 ) ;
#45572=CARTESIAN_POINT ( 'NONE',  ( -10.11462613662204468, -23.38712935484990751, 7.639894945624773115 ) ) ;
#45575=CIRCLE ( 'NONE', #38005, 0.5000000000000004441 ) ;
#45576=CARTESIAN_POINT ( 'NONE',  ( 7.633501923154999425, -23.20104675770999947, -10.36289748052999826 ) ) ;
#45577=CARTESIAN_POINT ( 'NONE',  ( -7.624341766639000539, -23.26485146254000114, -10.42531125024000005 ) ) ;
#45579=CARTESIAN_POINT ( 'NONE',  ( 12.70926961119000076, -18.59159259619999816, 1.933875435151000133 ) ) ;
#45582=VECTOR ( 'NONE', #25406, 1000.000000000000114 ) ;
#45583=CARTESIAN_POINT ( 'NONE',  ( 10.53559655342999868, -55.59430957992999822, -7.620036381585000740 ) ) ;
#45586=EDGE_CURVE ( 'NONE', #38447, #42021, #10152, .T. ) ;
#45589=CARTESIAN_POINT ( 'NONE',  ( -0.5222397218926316809, -61.96298219375309912, 12.70447686588483194 ) ) ;
#45591=CARTESIAN_POINT ( 'NONE',  ( -12.54977961489000116, -61.84832888596000089, -0.03757501521675000317 ) ) ;
#45593=CARTESIAN_POINT ( 'NONE',  ( 12.76303204517000012, -18.73514852243999940, -1.980584515753000208 ) ) ;
#45597=CARTESIAN_POINT ( 'NONE',  ( 9.019406120300617502, -53.80707871034709200, 8.666949038527242521 ) ) ;
#45600=DIRECTION ( 'NONE',  ( 0.7592504788686188499, -0.04890177850593128983, 0.6489586476785169644 ) ) ;
#45602=EDGE_CURVE ( 'NONE', #14201, #14108, #10859, .T. ) ;
#45604=DIRECTION ( 'NONE',  ( -1.000000000000000000, 0.000000000000000000, 0.000000000000000000 ) ) ;
#45607=ORIENTED_EDGE ( 'NONE', *, *, #4587, .T. ) ;
#45608=PLANE ( 'NONE',  #39610 ) ;
#45609=DIRECTION ( 'NONE',  ( -1.000000000000000000, 0.000000000000000000, 0.000000000000000000 ) ) ;
#45610=CARTESIAN_POINT ( 'NONE',  ( 1.750000000001000089, -56.04899163641999849, 12.60354432391000046 ) ) ;
#45611=CARTESIAN_POINT ( 'NONE',  ( 1.798954018882000128, -23.21530973387000074, -12.61117007302000026 ) ) ;
#45613=DIRECTION ( 'NONE',  ( 0.07798810159604831205, 0.04890177472412891857, -0.9957542229075783125 ) ) ;
#45614=CARTESIAN_POINT ( 'NONE',  ( -7.299466235464000086, -78.25818391050999878, 9.602332031690000491 ) ) ;
#45615=ORIENTED_EDGE ( 'NONE', *, *, #9126, .F. ) ;
#45616=ORIENTED_EDGE ( 'NONE', *, *, #4113, .T. ) ;
#45617=DIRECTION ( 'NONE',  ( 0.000000000000000000, 1.000000000000000000, -8.313948728910000322E-11 ) ) ;
#45619=CARTESIAN_POINT ( 'NONE',  ( -3.600000000000000089, -0.2000000000000000111, 0.000000000000000000 ) ) ;
#45620=CARTESIAN_POINT ( 'NONE',  ( -0.5668640725916784806, -17.08340305018563399, 12.50470739227127304 ) ) ;
#45623=FACE_OUTER_BOUND ( 'NONE', #17993, .T. ) ;
#45624=CARTESIAN_POINT ( 'NONE',  ( -10.24998526317999925, -20.24916621771999914, 7.705142895619999877 ) ) ;
#45625=CARTESIAN_POINT ( 'NONE',  ( -3.148725677322000482, -77.72624008069000467, 12.40542962523000092 ) ) ;
#45627=CARTESIAN_POINT ( 'NONE',  ( -12.53239398059000109, -22.76486430425999785, -1.667936688463999895 ) ) ;
#45628=CARTESIAN_POINT ( 'NONE',  ( 9.722718241315000398, -23.25000000000000000, 7.247844507162001015 ) ) ;
#45634=EDGE_CURVE ( 'NONE', #38307, #36279, #38144, .T. ) ;
#45638=CARTESIAN_POINT ( 'NONE',  ( -2.963791440107999886, -3.298030605495000156, 2.387889716789000083 ) ) ;
#45640=EDGE_CURVE ( 'NONE', #18023, #3036, #27889, .T. ) ;
#45642=CYLINDRICAL_SURFACE ( 'NONE', #21558, 11.75000000000000000 ) ;
#45643=CARTESIAN_POINT ( 'NONE',  ( -0.5812841321855997112, -18.69583131523479480, -10.98463311464191605 ) ) ;
#45644=DIRECTION ( 'NONE',  ( -0.7071067811865475727, 0.000000000000000000, -0.7071067811865475727 ) ) ;
#45646=CARTESIAN_POINT ( 'NONE',  ( 1.799502287691000069, -60.10716680829000325, 12.60413670423000099 ) ) ;
#45647=CARTESIAN_POINT ( 'NONE',  ( -10.55511172854000002, -77.96761847984998894, 7.611100925114999249 ) ) ;
#45649=CARTESIAN_POINT ( 'NONE',  ( -9.346069275187129932, -61.96527745658262631, -8.620894635752145874 ) ) ;
#45652=CARTESIAN_POINT ( 'NONE',  ( -8.666912951382961694, -24.99291380871171597, -9.019442093130059845 ) ) ;
#45655=CARTESIAN_POINT ( 'NONE',  ( 7.678667886068000215, -20.24263462181000151, -10.59548767699999949 ) ) ;
#45658=CARTESIAN_POINT ( 'NONE',  ( -3.858199361241999803, -0.7704335234539000377, -1.117275487237999965 ) ) ;
#45659=FACE_OUTER_BOUND ( 'NONE', #56904, .T. ) ;
#45662=AXIS2_PLACEMENT_3D ( 'NONE', #9907, #5469, #41484 ) ;
#45664=LINE ( 'NONE', #23492, #53028 ) ;
#45669=LINE ( 'NONE', #13758, #11420 ) ;
#45671=ORIENTED_EDGE ( 'NONE', *, *, #58265, .F. ) ;
#45677=CARTESIAN_POINT ( 'NONE',  ( -1.605981818850155562, -2.684253276126684629, -2.834025076496387463 ) ) ;
#45680=EDGE_LOOP ( 'NONE', ( #52554, #36015, #8880, #9178 ) ) ;
#45682=ORIENTED_EDGE ( 'NONE', *, *, #44608, .F. ) ;
#45686=CARTESIAN_POINT ( 'NONE',  ( 10.01676960210999923, -55.59061945207999855, 7.658895148190000057 ) ) ;
#45690=ADVANCED_FACE ( 'NONE', ( #27915 ), #24026, .F. ) ;
#45692=AXIS2_PLACEMENT_3D ( 'NONE', #41087, #55246, #41381 ) ;
#45695=CARTESIAN_POINT ( 'NONE',  ( 0.5245219981381742391, -23.45160423346249701, -10.98753021428673904 ) ) ;
#45698=CYLINDRICAL_SURFACE ( 'NONE', #24885, 1.750000000000000000 ) ;
#45702=CARTESIAN_POINT ( 'NONE',  ( 12.00000000000000000, 0.000000000000000000, 0.000000000000000000 ) ) ;
#45704=CARTESIAN_POINT ( 'NONE',  ( 1.691611010928000036, -24.23082691229999952, 12.66722148969999928 ) ) ;
#45708=CARTESIAN_POINT ( 'NONE',  ( -1.404568169276999789, -1.063321030358999941, -3.519501389975000283 ) ) ;
#45711=CARTESIAN_POINT ( 'NONE',  ( 1.749722766162256304, -55.32411007028125738, -12.54673760671575877 ) ) ;
#45712=CARTESIAN_POINT ( 'NONE',  ( 12.70253258974613608, -24.97063167672577677, -0.9890392130105698509 ) ) ;
#45715=CARTESIAN_POINT ( 'NONE',  ( 3.438102579189000085, -2.807527036004999754, 0.5732922487111999921 ) ) ;
#45722=EDGE_LOOP ( 'NONE', ( #31403, #33946, #2391 ) ) ;
#45725=EDGE_CURVE ( 'NONE', #2185, #46363, #41291, .T. ) ;
#45730=FACE_OUTER_BOUND ( 'NONE', #2299, .T. ) ;
#45737=CARTESIAN_POINT ( 'NONE',  ( 0.9262492265155897186, -75.83078504772286976, -11.74884656353136947 ) ) ;
#45744=CARTESIAN_POINT ( 'NONE',  ( -1.931086388455000025, -18.70221404512000163, 12.71798280854999952 ) ) ;
#45745=ORIENTED_EDGE ( 'NONE', *, *, #8219, .F. ) ;
#45749=AXIS2_PLACEMENT_3D ( 'NONE', #1634, #56513, #37621 ) ;
#45750=SURFACE_STYLE_FILL_AREA ( #37153 ) ;
#45756=ORIENTED_EDGE ( 'NONE', *, *, #30669, .F. ) ;
#45758=FACE_OUTER_BOUND ( 'NONE', #43699, .T. ) ;
#45759=DIRECTION ( 'NONE',  ( 0.000000000000000000, 1.000000000000000000, 0.000000000000000000 ) ) ;
#45760=CARTESIAN_POINT ( 'NONE',  ( -1.689459950971515800, -17.70811746097506401, -12.71013585610241492 ) ) ;
#45764=ORIENTED_EDGE ( 'NONE', *, *, #10186, .T. ) ;
#45766=CARTESIAN_POINT ( 'NONE',  ( 11.65396969189999865, -75.67884329787000297, -2.860942225950000140 ) ) ;
#45768=B_SPLINE_SURFACE_WITH_KNOTS ( 'NONE', 3, 3, ( 
 ( #49048, #23342, #28046, #9768 ),
 ( #15060, #54645, #51102, #19496 ),
 ( #6202, #24215, #28334, #10945 ),
 ( #41641, #45800, #37491, #55513 ),
 ( #1506, #41354, #33054, #14184 ),
 ( #33355, #46385, #55809, #50807 ),
 ( #18918, #36626, #5909, #32180 ),
 ( #55215, #19211, #37789, #50220 ),
 ( #27756, #1221, #10653, #5335 ),
 ( #36912, #14762, #936, #15361 ),
 ( #10351, #14476, #51388, #32759 ),
 ( #23918, #54923, #46682, #28632 ),
 ( #41936, #37203, #42234, #1798 ),
 ( #32467, #45503, #50513, #19795 ),
 ( #5050, #23048, #10066, #41063 ),
 ( #649, #46092, #5618, #18634 ),
 ( #23629, #29499, #38941, #20657 ) ),
 .UNSPECIFIED., .F., .F., .F.,
 ( 4, 1, 1, 1, 1, 1, 1, 1, 1, 1, 1, 1, 1, 1, 4 ),
 ( 4, 4 ),
 ( -0.01011398171662000051, 0.000000000000000000, 0.08333333333333001192, 0.1666666666667000196, 0.2500000000000000000, 0.3333333333333000081, 0.4166666666666999919, 0.5000000000000000000, 0.5833333333333000637, 0.6666666666667000474, 0.7500000000000000000, 0.8333333333333000637, 0.9166666666667000474, 1.000000000000000000, 1.010365777941000021 ),
 ( -0.3559705546970999834, 1.357612346730000086 ),
 .UNSPECIFIED. ) ;
#45769=CARTESIAN_POINT ( 'NONE',  ( 3.362134302577637790, -2.075432297516660363, -1.039236911360384985 ) ) ;
#45770=CARTESIAN_POINT ( 'NONE',  ( 12.64502302238000020, -19.22870851082999977, 1.799490220168999954 ) ) ;
#45771=CARTESIAN_POINT ( 'NONE',  ( -9.356096982537000173, -78.96139059408000094, 7.928589704419000128 ) ) ;
#45774=EDGE_CURVE ( 'NONE', #32986, #35553, #57415, .T. ) ;
#45776=FACE_OUTER_BOUND ( 'NONE', #50100, .T. ) ;
#45778=AXIS2_PLACEMENT_3D ( 'NONE', #17019, #52177, #30582 ) ;
#45781=B_SPLINE_CURVE_WITH_KNOTS ( 'NONE', 3,
 ( #8124, #26405, #35256, #3980, #51643, #51926 ),
 .UNSPECIFIED., .F., .F.,
 ( 4, 1, 1, 4 ),
 ( 0.000000000000000000, 0.3333333333333000081, 0.6666666666667000474, 1.000000000000000000 ),
 .UNSPECIFIED. ) ;
#45782=TOROIDAL_SURFACE ( 'NONE', #58018, 1.250000000000000000, 0.5000000000000000000 ) ;
#45789=CARTESIAN_POINT ( 'NONE',  ( 2.342546989920156530, -76.05880917198733471, 11.51398673525604011 ) ) ;
#45793=CARTESIAN_POINT ( 'NONE',  ( 7.644092900773786781, -18.47619833611041429, -10.09634159701095690 ) ) ;
#45794=EDGE_CURVE ( 'NONE', #35802, #26558, #1895, .T. ) ;
#45797=CARTESIAN_POINT ( 'NONE',  ( -8.485281374238999419, -55.54999999966999980, -8.485281374238999419 ) ) ;
#45799=CARTESIAN_POINT ( 'NONE',  ( 7.954951288349001004, -18.75000000000000000, -9.722718241315000398 ) ) ;
#45800=CARTESIAN_POINT ( 'NONE',  ( 10.30457855492000085, -18.23665569414000132, -7.636266481018999741 ) ) ;
#45801=CARTESIAN_POINT ( 'NONE',  ( 0.000000000000000000, -59.58578169018999660, -13.15643568216998638 ) ) ;
#45802=ORIENTED_EDGE ( 'NONE', *, *, #14507, .F. ) ;
#45804=CARTESIAN_POINT ( 'NONE',  ( 12.71466563513520676, -54.66210710670185335, 1.778810201848326500 ) ) ;
#45811=CARTESIAN_POINT ( 'NONE',  ( 10.45204383630000144, -19.23743350652000217, 7.651147548127999798 ) ) ;
#45813=DIRECTION ( 'NONE',  ( 0.7071067811865475727, 0.000000000000000000, 0.7071067811865475727 ) ) ;
#45815=AXIS2_PLACEMENT_3D ( 'NONE', #5177, #15491, #32891 ) ;
#45816=CARTESIAN_POINT ( 'NONE',  ( -12.50745077494999968, -61.79994448255000350, -2.661703094427999907E-09 ) ) ;
#45817=ORIENTED_EDGE ( 'NONE', *, *, #51087, .T. ) ;
#45818=ORIENTED_EDGE ( 'NONE', *, *, #39358, .T. ) ;
#45822=LINE ( 'NONE', #23366, #23679 ) ;
#45825=AXIS2_PLACEMENT_3D ( 'NONE', #13314, #35749, #31607 ) ;
#45826=CARTESIAN_POINT ( 'NONE',  ( 7.647093862774999806, -60.16895637605999525, 10.00844027277999970 ) ) ;
#45831=B_SPLINE_CURVE_WITH_KNOTS ( 'NONE', 3,
 ( #47822, #57514, #20927, #16505, #48387, #30345, #7925, #38928, #3500, #16795, #34779, #12643, #7352, #25638, #30055, #48106, #52803 ),
 .UNSPECIFIED., .F., .F.,
 ( 4, 2, 1, 2, 2, 1, 1, 2, 2, 4 ),
 ( 0.000000000000000000, 0.2500000000000005551, 0.3750000000000007772, 0.4375000000000007772, 0.5000000000000007772, 0.6250000000000006661, 0.6875000000000004441, 0.7187500000000002220, 0.7500000000000001110, 1.000000000000000000 ),
 .UNSPECIFIED. ) ;
#45833=CARTESIAN_POINT ( 'NONE',  ( -9.175573575508092716, -25.22695822358256024, 8.792784719773246493 ) ) ;
#45834=ORIENTED_EDGE ( 'NONE', *, *, #23650, .F. ) ;
#45837=FACE_OUTER_BOUND ( 'NONE', #47307, .T. ) ;
#45842=B_SPLINE_CURVE_WITH_KNOTS ( 'NONE', 3,
 ( #56634, #51058, #16192, #15898, #24757, #29739, #5866, #2334, #23875, #1757 ),
 .UNSPECIFIED., .F., .F.,
 ( 4, 2, 2, 2, 4 ),
 ( 0.000000000000000000, 0.2500000000000000000, 0.5000000000000000000, 0.7500000000000000000, 1.000000000000000000 ),
 .UNSPECIFIED. ) ;
#45845=ADVANCED_FACE ( 'NONE', ( #34090 ), #55126, .F. ) ;
#45846=CARTESIAN_POINT ( 'NONE',  ( 1.799501877793999949, -60.08917723397000543, -12.60552511012999943 ) ) ;
#45847=CARTESIAN_POINT ( 'NONE',  ( -7.401770473313917797, -60.25155696365191460, 8.137215171344811537 ) ) ;
#45850=EDGE_CURVE ( 'NONE', #52629, #35908, #4700, .T. ) ;
#45855=CARTESIAN_POINT ( 'NONE',  ( 3.250000000000000000, -3.250000000000000000, 0.000000000000000000 ) ) ;
#45856=CARTESIAN_POINT ( 'NONE',  ( -1.405334851868360602, -61.11492947527288777, -12.50716844841877773 ) ) ;
#45858=CARTESIAN_POINT ( 'NONE',  ( -3.043150799898603154, -3.291925712094595280, -1.769611200578169008 ) ) ;
#45862=DIRECTION ( 'NONE',  ( 0.000000000000000000, 1.000000000000000000, 0.000000000000000000 ) ) ;
#45864=ORIENTED_EDGE ( 'NONE', *, *, #40249, .F. ) ;
#45866=EDGE_CURVE ( 'NONE', #45077, #11731, #48513, .T. ) ;
#45867=CARTESIAN_POINT ( 'NONE',  ( -3.943885540262999534, -3.314075421107999908, -0.4205739404420000271 ) ) ;
#45870=CARTESIAN_POINT ( 'NONE',  ( 8.878335097414000288, -25.06963071744000260, -8.870344075630997693 ) ) ;
#45871=DIRECTION ( 'NONE',  ( 0.000000000000000000, 1.000000000000000000, 8.313952627639000142E-11 ) ) ;
#45873=CARTESIAN_POINT ( 'NONE',  ( -8.532671860894721405, -53.67201063361042657, -9.433519686823784056 ) ) ;
#45876=CARTESIAN_POINT ( 'NONE',  ( -7.651160336708000109, -59.56232686183999903, 10.45205658995999976 ) ) ;
#45877=CIRCLE ( 'NONE', #50592, 1.250000000000000444 ) ;
#45878=CARTESIAN_POINT ( 'NONE',  ( 10.01749678874999994, -55.60819056964000140, -7.660430392551000445 ) ) ;
#45884=CARTESIAN_POINT ( 'NONE',  ( 0.000000000000000000, -32.36102867817999851, 0.000000000000000000 ) ) ;
#45887=ORIENTED_EDGE ( 'NONE', *, *, #15183, .T. ) ;
#45889=CARTESIAN_POINT ( 'NONE',  ( 0.000000000000000000, 0.000000000000000000, 0.000000000000000000 ) ) ;
#45895=EDGE_LOOP ( 'NONE', ( #174, #46403, #6966 ) ) ;
#45897=EDGE_CURVE ( 'NONE', #58122, #28795, #4215, .T. ) ;
#45898=CARTESIAN_POINT ( 'NONE',  ( -1.930628539545000022, -18.77875555914000216, 12.72375828104000028 ) ) ;
#45900=CARTESIAN_POINT ( 'NONE',  ( 1.750000000000000000, -58.54977139303999678, 12.65375411740000011 ) ) ;
#45901=B_SPLINE_CURVE_WITH_KNOTS ( 'NONE', 3,
 ( #36542, #9685, #19419, #9981, #1430, #14389 ),
 .UNSPECIFIED., .F., .F.,
 ( 4, 1, 1, 4 ),
 ( 0.000000000000000000, 0.3333333333333000081, 0.6666666666667000474, 1.000000000000000000 ),
 .UNSPECIFIED. ) ;
#45910=AXIS2_PLACEMENT_3D ( 'NONE', #31183, #57779, #40361 ) ;
#45913=CARTESIAN_POINT ( 'NONE',  ( 10.41144098945170171, -60.32546312028583202, 7.610433527984337587 ) ) ;
#45915=VECTOR ( 'NONE', #42721, 1000.000000000000000 ) ;
#45916=CARTESIAN_POINT ( 'NONE',  ( -12.91020013338000005, -76.92524667502999591, -1.090565897604000023 ) ) ;
#45918=CARTESIAN_POINT ( 'NONE',  ( -12.69616050742999924, -21.75171076523999858, -1.799475304559999822 ) ) ;
#45919=AXIS2_PLACEMENT_3D ( 'NONE', #36099, #57951, #35200 ) ;
#45920=CARTESIAN_POINT ( 'NONE',  ( 0.5805005430889391693, -76.57101688036192400, 11.73679383478257243 ) ) ;
#45921=EDGE_CURVE ( 'NONE', #47903, #29770, #3944, .T. ) ;
#45926=DIRECTION ( 'NONE',  ( 0.000000000000000000, 1.000000000000000000, 0.000000000000000000 ) ) ;
#45930=CARTESIAN_POINT ( 'NONE',  ( 11.80100040161109298, -79.24999999999997158, 2.513071073578707626 ) ) ;
#45931=CARTESIAN_POINT ( 'NONE',  ( 1.911540947291000103, -3.150461020869000262, 3.291214574437999918 ) ) ;
#45933=ORIENTED_EDGE ( 'NONE', *, *, #42200, .T. ) ;
#45934=CARTESIAN_POINT ( 'NONE',  ( 2.460715419384281066, -78.94166666666667709, -11.55514622821795889 ) ) ;
#45935=CARTESIAN_POINT ( 'NONE',  ( -12.04999999926000243, -79.29999999926000953, -5.384918809984000181E-09 ) ) ;
#45936=CARTESIAN_POINT ( 'NONE',  ( 10.27281115125161648, -77.48889879997290109, 5.919856814084291763 ) ) ;
#45939=CARTESIAN_POINT ( 'NONE',  ( -12.97861384075000046, -77.95378978747999099, -0.9459496016724999734 ) ) ;
#45942=CARTESIAN_POINT ( 'NONE',  ( 11.19195407364522943, -78.47360375268350197, 3.576835338053799607 ) ) ;
#45943=LINE ( 'NONE', #1358, #6146 ) ;
#45947=DIRECTION ( 'NONE',  ( 0.000000000000000000, 0.000000000000000000, 1.000000000000000000 ) ) ;
#45950=CARTESIAN_POINT ( 'NONE',  ( -1.488596180559999871, -0.9467806054949000627, -3.730054860412999940 ) ) ;
#45956=DIRECTION ( 'NONE',  ( 0.000000000000000000, -1.000000000000000000, 1.273055734904000118E-13 ) ) ;
#45957=PRODUCT_DEFINITION ( 'UNKNOWN', '', #48051, #17404 ) ;
#45967=AXIS2_PLACEMENT_3D ( 'NONE', #45884, #5416, #36708 ) ;
#45968=ORIENTED_EDGE ( 'NONE', *, *, #4344, .T. ) ;
#45970=EDGE_CURVE ( 'NONE', #40049, #20675, #30581, .T. ) ;
#45971=CARTESIAN_POINT ( 'NONE',  ( 0.02549637870113643373, -2.726424292193095678, -3.249520170519987428 ) ) ;
#45976=VERTEX_POINT ( 'NONE', #50029 ) ;
#45977=CARTESIAN_POINT ( 'NONE',  ( -8.872949061359179268, -53.78989818412208024, -8.813905827841837848 ) ) ;
#45978=EDGE_LOOP ( 'NONE', ( #23592, #37808, #44779, #9711 ) ) ;
#45982=DIRECTION ( 'NONE',  ( 0.000000000000000000, 1.000000000000000000, 0.000000000000000000 ) ) ;
#45983=CARTESIAN_POINT ( 'NONE',  ( -12.99510751537000353, -26.30294702886003222, 6.911973076623003642 ) ) ;
#45988=CARTESIAN_POINT ( 'NONE',  ( 2.311693661511226239, -76.55883260880376895, 11.52009055038358198 ) ) ;
#45992=CARTESIAN_POINT ( 'NONE',  ( 0.5788847457760372128, -78.32421909374012614, 12.05596584941754834 ) ) ;
#45993=VECTOR ( 'NONE', #28087, 1000.000000000000114 ) ;
#45996=CARTESIAN_POINT ( 'NONE',  ( -1.750000000000000000, -58.55064714144999982, 12.65372179280999987 ) ) ;
#45998=DIRECTION ( 'NONE',  ( 0.7592504788685162653, 0.04890177849164110968, -0.6489586476797141179 ) ) ;
#46001=CARTESIAN_POINT ( 'NONE',  ( -1.001315002179000047, -24.68522411714000242, 12.50000000000000000 ) ) ;
#46002=TOROIDAL_SURFACE ( 'NONE', #6410, 1.250000000000000000, 0.5000000000000000000 ) ;
#46003=CARTESIAN_POINT ( 'NONE',  ( 10.35747145890000098, -55.48415267986000288, 7.626500777218999438 ) ) ;
#46009=CARTESIAN_POINT ( 'NONE',  ( 12.79972228482999874, -23.79021513454000214, 2.019125729023000027 ) ) ;
#46011=CARTESIAN_POINT ( 'NONE',  ( -3.599999993293999889, -0.2000000067061999953, -5.600095662875000459E-09 ) ) ;
#46012=CIRCLE ( 'NONE', #3540, 1.750000000000000000 ) ;
#46013=DIRECTION ( 'NONE',  ( -1.000000000000000000, 0.000000000000000000, 0.000000000000000000 ) ) ;
#46014=CARTESIAN_POINT ( 'NONE',  ( -1.718598679968283971, -24.24962933044487912, -12.71111582768035220 ) ) ;
#46015=DIRECTION ( 'NONE',  ( 0.000000000000000000, 0.000000000000000000, -1.000000000000000000 ) ) ;
#46017=ORIENTED_EDGE ( 'NONE', *, *, #40304, .T. ) ;
#46021=CARTESIAN_POINT ( 'NONE',  ( 8.620934061238347823, -53.63470696644542812, 9.346030177867731936 ) ) ;
#46023=CARTESIAN_POINT ( 'NONE',  ( 2.426647618366999603E-14, -6.000000000000000000, -13.00000000000343547 ) ) ;
#46025=CARTESIAN_POINT ( 'NONE',  ( -3.726464253369000001, -0.8073096613111999664, -0.05413188946992000122 ) ) ;
#46028=VERTEX_POINT ( 'NONE', #26974 ) ;
#46032=DIRECTION ( 'NONE',  ( 1.000000000000000000, 0.000000000000000000, 0.000000000000000000 ) ) ;
#46033=VERTEX_POINT ( 'NONE', #56109 ) ;
#46036=ORIENTED_EDGE ( 'NONE', *, *, #54587, .F. ) ;
#46039=CARTESIAN_POINT ( 'NONE',  ( -2.062502994258999856, -20.24351820077000141, 12.92181194099999963 ) ) ;
#46040=VERTEX_POINT ( 'NONE', #33062 ) ;
#46041=FACE_OUTER_BOUND ( 'NONE', #15159, .T. ) ;
#46044=EDGE_LOOP ( 'NONE', ( #39300, #25097, #13001, #33514, #39754, #54226 ) ) ;
#46045=CARTESIAN_POINT ( 'NONE',  ( -7.648026768008000076, -55.55000001556999933, 10.12290050216000026 ) ) ;
#46046=CARTESIAN_POINT ( 'NONE',  ( -9.050966798898000931, -59.94999999040999938, -7.919595949288999570 ) ) ;
#46047=CARTESIAN_POINT ( 'NONE',  ( -12.43422056531000131, -24.43655741434000106, -1.197404442627999943 ) ) ;
#46049=CARTESIAN_POINT ( 'NONE',  ( -17.49999999998999911, -65.72928575305999743, -1.613072092318999730E-05 ) ) ;
#46050=AXIS2_PLACEMENT_3D ( 'NONE', #41119, #45862, #23404 ) ;
#46052=CARTESIAN_POINT ( 'NONE',  ( -7.710095619848000403, -57.04935285743999884, 10.18496935399999970 ) ) ;
#46053=LINE ( 'NONE', #14143, #51385 ) ;
#46055=CARTESIAN_POINT ( 'NONE',  ( -8.838834764832000701, -23.25000000000000000, -8.838834764832000701 ) ) ;
#46060=CARTESIAN_POINT ( 'NONE',  ( 12.21199139566000014, -76.24271386089000657, 1.550091862394999964 ) ) ;
#46062=CARTESIAN_POINT ( 'NONE',  ( 2.863104762478203558, -2.049854368984712405, -2.050083987754392822 ) ) ;
#46063=CARTESIAN_POINT ( 'NONE',  ( 7.645398488040000551, -60.01531609111000165, -10.18948971875999909 ) ) ;
#46064=CARTESIAN_POINT ( 'NONE',  ( 9.889431646000000242, -78.81768700370000147, 7.252463523969000292 ) ) ;
#46068=CARTESIAN_POINT ( 'NONE',  ( 2.355521564011713309, -2.790126448396267111, -2.238901740357879699 ) ) ;
#46069=CARTESIAN_POINT ( 'NONE',  ( 11.93997985869404310, -77.31377101359005621, 2.095138499075543059 ) ) ;
#46072=ORIENTED_EDGE ( 'NONE', *, *, #42868, .T. ) ;
#46077=CARTESIAN_POINT ( 'NONE',  ( 0.7203371404106000409, -1.934275774374000001, -3.802791496513000080 ) ) ;
#46080=AXIS2_PLACEMENT_3D ( 'NONE', #24060, #14614, #32608 ) ;
#46081=CARTESIAN_POINT ( 'NONE',  ( 8.345306581575338001, -76.01155566110702466, 8.271040368256810993 ) ) ;
#46087=CARTESIAN_POINT ( 'NONE',  ( -6.543376917090838241, -76.27791085602611076, -9.759379282097372155 ) ) ;
#46091=DIRECTION ( 'NONE',  ( 0.000000000000000000, 1.000000000000000000, 0.000000000000000000 ) ) ;
#46092=CARTESIAN_POINT ( 'NONE',  ( 7.631889106325000505, -18.77878585407000145, -10.36222439674000029 ) ) ;
#46093=CARTESIAN_POINT ( 'NONE',  ( -5.747123378374999980, -78.21567021303999923, 10.24856442990000005 ) ) ;
#46096=CARTESIAN_POINT ( 'NONE',  ( 0.000000000000000000, 4.040000000000000036, 0.000000000000000000 ) ) ;
#46097=COLOUR_RGB ( '', 0.66274510, 0.83137255, 0.94901961) ;
#46098=CARTESIAN_POINT ( 'NONE',  ( 12.50485632861550833, -53.93407884522628137, 0.6924337384548601149 ) ) ;
#46100=EDGE_CURVE ( 'NONE', #39575, #16917, #5747, .T. ) ;
#46101=CARTESIAN_POINT ( 'NONE',  ( -6.398554566410420641, -77.37244341094226741, 10.23462864614716139 ) ) ;
#46105=DIRECTION ( 'NONE',  ( 0.000000000000000000, -1.000000000000000000, 0.000000000000000000 ) ) ;
#46107=DIRECTION ( 'NONE',  ( 0.000000000000000000, 1.000000000000000000, 0.000000000000000000 ) ) ;
#46111=ORIENTED_EDGE ( 'NONE', *, *, #38049, .F. ) ;
#46118=AXIS2_PLACEMENT_3D ( 'NONE', #9744, #27144, #41328 ) ;
#46122=CARTESIAN_POINT ( 'NONE',  ( 7.956422463042999382, -61.32889896150999931, 9.787948076380001083 ) ) ;
#46128=CARTESIAN_POINT ( 'NONE',  ( 7.648026766753000416, -60.05000000550000294, -10.12290050090999927 ) ) ;
#46129=VERTEX_POINT ( 'NONE', #15488 ) ;
#46136=CARTESIAN_POINT ( 'NONE',  ( -9.722718241315000398, -55.35321828636000419, -7.954951288349001004 ) ) ;
#46138=CARTESIAN_POINT ( 'NONE',  ( 10.07627163191000008, -55.55000000278000272, 7.601397897754999633 ) ) ;
#46140=CARTESIAN_POINT ( 'NONE',  ( -7.658894224177999810, -23.20939395863999977, -10.01676912201999947 ) ) ;
#46141=CARTESIAN_POINT ( 'NONE',  ( 12.53241208775999915, -59.56462890159999546, -1.667936697358999965 ) ) ;
#46149=DIRECTION ( 'NONE',  ( -1.000000000000000000, 0.000000000000000000, 0.000000000000000000 ) ) ;
#46150=DIRECTION ( 'NONE',  ( 0.7071067811865474617, 0.000000000000000000, 0.7071067811865474617 ) ) ;
#46151=CARTESIAN_POINT ( 'NONE',  ( -2.822700266548876069, -3.300972420264427498, -2.107553880886188669 ) ) ;
#46156=CARTESIAN_POINT ( 'NONE',  ( 0.4479210110389621469, -0.8346353966065711560, -3.415364800656486288 ) ) ;
#46164=CARTESIAN_POINT ( 'NONE',  ( 7.646788277333999240, -23.37228598377000210, -10.00831419131999844 ) ) ;
#46166=CARTESIAN_POINT ( 'NONE',  ( 3.248892733988256953, -1.861934577303119953, 0.4260366050094578916 ) ) ;
#46167=CARTESIAN_POINT ( 'NONE',  ( -9.848035040979025823, -53.97131634255971022, -8.114786739965461848 ) ) ;
#46169=VECTOR ( 'NONE', #42655, 1000.000000000000114 ) ;
#46170=CARTESIAN_POINT ( 'NONE',  ( -7.686918321190000292, -21.75560170997999876, -10.48771805380000011 ) ) ;
#46171=CARTESIAN_POINT ( 'NONE',  ( 6.196431984783000502, -79.15908388498999670, -11.36888734437999915 ) ) ;
#46177=VECTOR ( 'NONE', #52678, 999.9999999999998863 ) ;
#46181=CONICAL_SURFACE ( 'NONE', #34796, 0.6999999997694995590, 0.7853981633972997312 ) ;
#46185=ADVANCED_FACE ( 'NONE', ( #14890 ), #24047, .T. ) ;
#46194=ORIENTED_EDGE ( 'NONE', *, *, #738, .F. ) ;
#46201=ADVANCED_FACE ( 'NONE', ( #29625 ), #16071, .F. ) ;
#46202=ORIENTED_EDGE ( 'NONE', *, *, #6554, .F. ) ;
#46206=DIRECTION ( 'NONE',  ( 0.000000000000000000, 1.000000000000000000, 0.000000000000000000 ) ) ;
#46207=CARTESIAN_POINT ( 'NONE',  ( 0.04193593612906149071, -16.98990258663310726, 12.50649570005709599 ) ) ;
#46211=CARTESIAN_POINT ( 'NONE',  ( 7.255994938323000021, -78.09084413521999579, -10.73374472359000009 ) ) ;
#46213=CARTESIAN_POINT ( 'NONE',  ( -8.838834764832000701, -18.75000000000000000, -8.838834764832000701 ) ) ;
#46214=CARTESIAN_POINT ( 'NONE',  ( 0.02731002720095722369, -76.57469656089436683, 11.74987924982600696 ) ) ;
#46220=ADVANCED_FACE ( 'NONE', ( #19337 ), #24349, .T. ) ;
#46225=DIRECTION ( 'NONE',  ( 0.000000000000000000, 1.000000000000000000, 0.000000000000000000 ) ) ;
#46226=CARTESIAN_POINT ( 'NONE',  ( -12.50240681836000078, -61.48234730679999416, 1.005418944265999981 ) ) ;
#46227=CARTESIAN_POINT ( 'NONE',  ( -3.268529449828999844, -2.360140595155999943, -1.950076325099000085 ) ) ;
#46228=DIRECTION ( 'NONE',  ( 1.000000000000000000, 0.000000000000000000, 0.000000000000000000 ) ) ;
#46229=ORIENTED_EDGE ( 'NONE', *, *, #43089, .F. ) ;
#46231=CARTESIAN_POINT ( 'NONE',  ( 0.5200379331660126558, -18.54844303601859679, -10.98772212209857102 ) ) ;
#46232=CARTESIAN_POINT ( 'NONE',  ( -7.217346475716882814, -77.62574498632518782, 9.390375165279603920 ) ) ;
#46233=CARTESIAN_POINT ( 'NONE',  ( 1.667917367065999912, -60.08056535122999975, 12.49306764019000049 ) ) ;
#46234=CARTESIAN_POINT ( 'NONE',  ( -12.54981748959999877, -53.75163512338999539, -0.03767836620429999839 ) ) ;
#46236=ADVANCED_FACE ( 'NONE', ( #20500 ), #42065, .F. ) ;
#46238=DIRECTION ( 'NONE',  ( -0.9999999999999693578, 2.479738204331925575E-07, -1.114546890695966335E-12 ) ) ;
#46241=FACE_OUTER_BOUND ( 'NONE', #35541, .T. ) ;
#46247=LINE ( 'NONE', #33208, #50386 ) ;
#46248=CARTESIAN_POINT ( 'NONE',  ( 7.954951288349001004, -60.24678171298000251, 9.722718241315000398 ) ) ;
#46249=B_SPLINE_CURVE_WITH_KNOTS ( 'NONE', 3,
 ( #12034, #53047, #7308, #16752, #38600, #17034 ),
 .UNSPECIFIED., .F., .F.,
 ( 4, 2, 4 ),
 ( 0.000000000000000000, 0.5000000000000000000, 1.000000000000000000 ),
 .UNSPECIFIED. ) ;
#46255=CARTESIAN_POINT ( 'NONE',  ( -12.50385649911392605, -61.58436722984689027, -0.8579675320882300671 ) ) ;
#46264=CIRCLE ( 'NONE', #55683, 0.5000000000000000000 ) ;
#46267=CARTESIAN_POINT ( 'NONE',  ( -0.5999999999999999778, -18.84999999999000053, -11.79999999999999893 ) ) ;
#46268=ORIENTED_EDGE ( 'NONE', *, *, #41580, .F. ) ;
#46270=EDGE_CURVE ( 'NONE', #53710, #5930, #26878, .T. ) ;
#46271=CARTESIAN_POINT ( 'NONE',  ( -7.705119999435999567, -57.04828923575999511, 10.24996238029999951 ) ) ;
#46272=ORIENTED_EDGE ( 'NONE', *, *, #49041, .F. ) ;
#46273=CARTESIAN_POINT ( 'NONE',  ( 1.001315002179999913, -17.31477588286000113, 12.50000000000000000 ) ) ;
#46276=CARTESIAN_POINT ( 'NONE',  ( -12.50745077490000057, -17.00005551713000074, 2.011909873286000185E-09 ) ) ;
#46278=DIRECTION ( 'NONE',  ( 0.000000000000000000, 1.000000000000000000, 0.000000000000000000 ) ) ;
#46280=CARTESIAN_POINT ( 'NONE',  ( -7.654537085048000122, -60.08056692637000396, -10.01332844639000008 ) ) ;
#46282=AXIS2_PLACEMENT_3D ( 'NONE', #45196, #4744, #56015 ) ;
#46286=CARTESIAN_POINT ( 'NONE',  ( 11.74999999999999289, -76.56041666666666856, 1.538071403320028452 ) ) ;
#46290=CARTESIAN_POINT ( 'NONE',  ( 11.99999999979999821, -18.85000000927000130, 0.7999999997951999786 ) ) ;
#46294=DIRECTION ( 'NONE',  ( -0.9999999924279685537, 0.000000000000000000, -0.0001230612157848962919 ) ) ;
#46296=CARTESIAN_POINT ( 'NONE',  ( -1.807051837523000026, -24.30078415243000123, -12.77977401834999860 ) ) ;
#46297=CIRCLE ( 'NONE', #28346, 12.50000000000000000 ) ;
#46298=DIRECTION ( 'NONE',  ( 0.9999463328794432337, 0.000000000000000000, -0.01036008498777044214 ) ) ;
#46299=CARTESIAN_POINT ( 'NONE',  ( -0.4716531882653000052, -2.930179953964000106, 3.453513650901000265 ) ) ;
#46300=CARTESIAN_POINT ( 'NONE',  ( 12.55486071735000131, -24.15393633008000407, 1.580832792524999864 ) ) ;
#46302=EDGE_CURVE ( 'NONE', #42030, #31323, #24996, .T. ) ;
#46307=CARTESIAN_POINT ( 'NONE',  ( -10.23598640736999954, -76.21444405523999421, -6.660190322323000345 ) ) ;
#46308=VERTEX_POINT ( 'NONE', #24636 ) ;
#46312=CARTESIAN_POINT ( 'NONE',  ( 9.355955347601371486, -53.62516908774130542, 8.610895743687590809 ) ) ;
#46319=ORIENTED_EDGE ( 'NONE', *, *, #19661, .T. ) ;
#46322=CARTESIAN_POINT ( 'NONE',  ( 12.05000000000000071, -79.29999999999999716, 0.000000000000000000 ) ) ;
#46327=CIRCLE ( 'NONE', #16134, 12.05000000000000071 ) ;
#46330=CARTESIAN_POINT ( 'NONE',  ( -12.50000000000000000, -18.75000000000000000, 1.250000000000000000 ) ) ;
#46336=CARTESIAN_POINT ( 'NONE',  ( 12.54705919854999863, -54.26307476595999901, 1.287183453418999868 ) ) ;
#46337=EDGE_CURVE ( 'NONE', #37515, #12596, #53521, .T. ) ;
#46340=VECTOR ( 'NONE', #9804, 999.9999999999998863 ) ;
#46341=CARTESIAN_POINT ( 'NONE',  ( -12.66322140209000047, -25.18161935732999623, -0.1487435796151999889 ) ) ;
#46342=ADVANCED_FACE ( 'NONE', ( #48523 ), #18885, .F. ) ;
#46344=AXIS2_PLACEMENT_3D ( 'NONE', #49726, #155, #36414 ) ;
#46346=CARTESIAN_POINT ( 'NONE',  ( -1.980584515752000119, -18.73514853375999678, -12.76303204602000108 ) ) ;
#46348=CARTESIAN_POINT ( 'NONE',  ( -12.70619604133053926, -17.53855724472153454, -1.571828507134811703 ) ) ;
#46350=CYLINDRICAL_SURFACE ( 'NONE', #11481, 1.750000000000001332 ) ;
#46351=VERTEX_POINT ( 'NONE', #35493 ) ;
#46352=CARTESIAN_POINT ( 'NONE',  ( -11.84062247810999935, -76.49528801428999714, 3.366775603358000080 ) ) ;
#46356=CARTESIAN_POINT ( 'NONE',  ( -12.26143800982999998, -79.01887203022999984, -0.2371146996492999870 ) ) ;
#46358=CARTESIAN_POINT ( 'NONE',  ( -10.12290050255000118, -55.55000002206000431, -7.648026768392999664 ) ) ;
#46359=CARTESIAN_POINT ( 'NONE',  ( 12.50728321917716102, -24.99975184167002595, 0.1774118160392116339 ) ) ;
#46360=CARTESIAN_POINT ( 'NONE',  ( 4.821392521053025959, -78.20771595215950356, -11.06363226005912637 ) ) ;
#46361=CARTESIAN_POINT ( 'NONE',  ( -10.12290050124000018, -18.75000000007999645, 7.648026767085999822 ) ) ;
#46363=VERTEX_POINT ( 'NONE', #16934 ) ;
#46366=CARTESIAN_POINT ( 'NONE',  ( -1.750000000001000089, -60.05000000958000328, -12.56594317859000043 ) ) ;
#46368=CARTESIAN_POINT ( 'NONE',  ( -3.285477502895000068, -2.838700577026000094, -2.045963233116000257 ) ) ;
#46369=EDGE_CURVE ( 'NONE', #51037, #56919, #34915, .T. ) ;
#46372=CARTESIAN_POINT ( 'NONE',  ( -10.83206147397086738, -76.16818589886489121, 4.552669838977208450 ) ) ;
#46376=ADVANCED_FACE ( 'NONE', ( #26064 ), #44089, .T. ) ;
#46377=CARTESIAN_POINT ( 'NONE',  ( -9.662446363795996973, -76.49682594560466953, 7.627099640079997300 ) ) ;
#46380=AXIS2_PLACEMENT_3D ( 'NONE', #41179, #40890, #40601 ) ;
#46385=CARTESIAN_POINT ( 'NONE',  ( 9.929695104603000644, -17.36901065046999904, -7.973993995755001229 ) ) ;
#46386=CARTESIAN_POINT ( 'NONE',  ( 12.99510751537000353, -63.10294702886003648, -6.911973076623003642 ) ) ;
#46388=AXIS2_PLACEMENT_3D ( 'NONE', #4328, #54522, #36493 ) ;
#46389=FACE_OUTER_BOUND ( 'NONE', #45680, .T. ) ;
#46392=CARTESIAN_POINT ( 'NONE',  ( -7.842892531714791282, -77.88391165169997521, 9.250934933446409048 ) ) ;
#46397=CARTESIAN_POINT ( 'NONE',  ( 0.000000000000000000, -15.06282895647999887, 0.000000000000000000 ) ) ;
#46399=CARTESIAN_POINT ( 'NONE',  ( 1.980584515752000119, -18.73514853375999678, 12.76303204602000108 ) ) ;
#46400=CARTESIAN_POINT ( 'NONE',  ( 8.343860018000999190, -59.94999999967000548, -8.343860018000999190 ) ) ;
#46401=CARTESIAN_POINT ( 'NONE',  ( 10.42531125068999920, -23.26485145404000221, -7.624341767093000044 ) ) ;
#46402=ORIENTED_EDGE ( 'NONE', *, *, #10366, .T. ) ;
#46403=ORIENTED_EDGE ( 'NONE', *, *, #8018, .F. ) ;
#46407=EDGE_LOOP ( 'NONE', ( #9793, #24019, #13251, #24540, #57872, #18969 ) ) ;
#46410=CARTESIAN_POINT ( 'NONE',  ( 9.101516360845000264, -61.68066799025999813, 8.485522730770000521 ) ) ;
#46411=CARTESIAN_POINT ( 'NONE',  ( 0.5999999999999999778, -23.15000000000000213, 12.00000000000000000 ) ) ;
#46414=ORIENTED_EDGE ( 'NONE', *, *, #34883, .F. ) ;
#46415=DIRECTION ( 'NONE',  ( 0.000000000000000000, 0.7071067811866525998, -0.7071067811864425456 ) ) ;
#46416=ORIENTED_EDGE ( 'NONE', *, *, #43234, .T. ) ;
#46419=AXIS2_PLACEMENT_3D ( 'NONE', #30177, #37894, #43492 ) ;
#46420=CARTESIAN_POINT ( 'NONE',  ( 0.000000000000000000, -2.660000000000000142, 0.000000000000000000 ) ) ;
#46429=CARTESIAN_POINT ( 'NONE',  ( 12.70299718804698763, -61.82583482779825346, 0.8845454260210772190 ) ) ;
#46441=CARTESIAN_POINT ( 'NONE',  ( -1.630911441802957329, -3.337159252943526777, -3.168633379730300348 ) ) ;
#46444=LINE ( 'NONE', #13953, #49945 ) ;
#46448=EDGE_LOOP ( 'NONE', ( #954, #33734, #39840, #31538 ) ) ;
#46449=EDGE_CURVE ( 'NONE', #48634, #30476, #21509, .T. ) ;
#46450=CARTESIAN_POINT ( 'NONE',  ( -1.807051837523000026, -61.10078415209999747, -12.77977401837999949 ) ) ;
#46454=CARTESIAN_POINT ( 'NONE',  ( 7.762981007049000404, -24.16089459216999913, -9.992000916352999695 ) ) ;
#46456=CARTESIAN_POINT ( 'NONE',  ( 3.167321027750415130, -1.872349564160396884, 0.8521775410308326526 ) ) ;
#46457=CARTESIAN_POINT ( 'NONE',  ( -9.175589924910891426, -53.57304466829480560, -8.792768277102885222 ) ) ;
#46461=FACE_OUTER_BOUND ( 'NONE', #44711, .T. ) ;
#46462=EDGE_CURVE ( 'NONE', #15626, #43717, #55405, .T. ) ;
#46469=CARTESIAN_POINT ( 'NONE',  ( -12.66313299637999989, -61.97803434819999779, -0.06050769725595999543 ) ) ;
#46471=CARTESIAN_POINT ( 'NONE',  ( -1.980464439859999981, -21.75472017459999918, -12.85144117154000121 ) ) ;
#46472=CARTESIAN_POINT ( 'NONE',  ( 8.768124086712999699, -55.64999999965999677, 7.919595949288999570 ) ) ;
#46473=B_SPLINE_CURVE_WITH_KNOTS ( 'NONE', 3,
 ( #41605, #615, #31855, #1185, #49896, #41899, #41024, #55478 ),
 .UNSPECIFIED., .F., .F.,
 ( 4, 2, 2, 4 ),
 ( 0.000000000000000000, 0.5000000000000000000, 0.7500000000000000000, 1.000000000000000000 ),
 .UNSPECIFIED. ) ;
#46476=AXIS2_PLACEMENT_3D ( 'NONE', #1841, #32797, #46725 ) ;
#46480=ORIENTED_EDGE ( 'NONE', *, *, #52416, .T. ) ;
#46481=EDGE_LOOP ( 'NONE', ( #45391, #1665, #47590 ) ) ;
#46483=EDGE_CURVE ( 'NONE', #17174, #34958, #35325, .T. ) ;
#46486=CARTESIAN_POINT ( 'NONE',  ( 1.632307027708999936, -18.33072810443000122, 12.46200249212000166 ) ) ;
#46487=CONICAL_SURFACE ( 'NONE', #3109, 13.94999999997000018, 0.7853981633972997312 ) ;
#46491=CIRCLE ( 'NONE', #55875, 1.250000000000000444 ) ;
#46495=ORIENTED_EDGE ( 'NONE', *, *, #29887, .F. ) ;
#46496=EDGE_LOOP ( 'NONE', ( #8990, #49936, #45756, #29490 ) ) ;
#46502=DIRECTION ( 'NONE',  ( 1.205798306211979422E-11, -1.868136817095964273E-07, 0.9999999999999824585 ) ) ;
#46507=CARTESIAN_POINT ( 'NONE',  ( -8.304142175982839547, -76.63735098509414456, 8.312756051645006750 ) ) ;
#46510=VECTOR ( 'NONE', #48739, 1000.000000000000114 ) ;
#46513=CARTESIAN_POINT ( 'NONE',  ( -7.645398650971000798, -18.78468617155999709, -10.18948982068999953 ) ) ;
#46516=DIRECTION ( 'NONE',  ( 0.000000000000000000, 1.000000000000000000, 0.000000000000000000 ) ) ;
#46517=DIRECTION ( 'NONE',  ( -0.07798810297638607281, 0.04890180917552757606, -0.9957542211075506300 ) ) ;
#46521=CARTESIAN_POINT ( 'NONE',  ( -2.848735472152420733, -3.499999999999999556, -1.711658475673403013 ) ) ;
#46522=EDGE_CURVE ( 'NONE', #43183, #1186, #50464, .T. ) ;
#46523=DIRECTION ( 'NONE',  ( -0.7071067811865474617, 0.000000000000000000, -0.7071067811865474617 ) ) ;
#46525=FACE_OUTER_BOUND ( 'NONE', #50384, .T. ) ;
#46526=CARTESIAN_POINT ( 'NONE',  ( 12.77656765298000074, -62.11198129881000085, -0.1555235816857000186 ) ) ;
#46528=CARTESIAN_POINT ( 'NONE',  ( 5.512103878356000131, -76.78819232728000088, 11.78783395355999986 ) ) ;
#46529=CARTESIAN_POINT ( 'NONE',  ( -12.50000000000000000, -15.06282895647999887, 0.000000000000000000 ) ) ;
#46530=CARTESIAN_POINT ( 'NONE',  ( 3.343750000583999960, -0.9062499994161000716, -3.925818329445000231E-08 ) ) ;
#46532=CIRCLE ( 'NONE', #37987, 12.90000000000000036 ) ;
#46535=EDGE_CURVE ( 'NONE', #18636, #20606, #52584, .T. ) ;
#46537=DIRECTION ( 'NONE',  ( -1.000000000000000000, 0.000000000000000000, 0.000000000000000000 ) ) ;
#46540=CARTESIAN_POINT ( 'NONE',  ( -3.431352783032999731, -1.308516015699999979, 2.086989923523999924 ) ) ;
#46542=FACE_OUTER_BOUND ( 'NONE', #9053, .T. ) ;
#46545=DIRECTION ( 'NONE',  ( -0.7071067811865475727, 0.000000000000000000, -0.7071067811865475727 ) ) ;
#46547=ORIENTED_EDGE ( 'NONE', *, *, #1400, .F. ) ;
#46550=CYLINDRICAL_SURFACE ( 'NONE', #216, 14.00000000000000000 ) ;
#46551=VERTEX_POINT ( 'NONE', #13595 ) ;
#46554=ORIENTED_EDGE ( 'NONE', *, *, #26526, .F. ) ;
#46557=ORIENTED_EDGE ( 'NONE', *, *, #53293, .T. ) ;
#46558=VECTOR ( 'NONE', #21555, 1000.000000000000000 ) ;
#46560=CARTESIAN_POINT ( 'NONE',  ( 10.48771805367000098, -57.04439828530000511, 7.686918321054999836 ) ) ;
#46563=CARTESIAN_POINT ( 'NONE',  ( -7.718368845781999887, -58.54800977479000323, 10.07722254367000048 ) ) ;
#46565=CARTESIAN_POINT ( 'NONE',  ( 1.668607604570606640, -18.20618368758884387, 12.52787843850908445 ) ) ;
#46569=CARTESIAN_POINT ( 'NONE',  ( 11.09903705321281464, -79.23326252747547471, 4.904546639011450715 ) ) ;
#46572=CARTESIAN_POINT ( 'NONE',  ( 0.000000000000000000, 4.040000000000000036, 0.000000000000000000 ) ) ;
#46574=CARTESIAN_POINT ( 'NONE',  ( -7.626500902197000720, -55.48415522678000400, -10.35747158360999975 ) ) ;
#46576=CARTESIAN_POINT ( 'NONE',  ( 4.524948720244553968, -76.54318040950390412, 10.84353445346675748 ) ) ;
#46580=CARTESIAN_POINT ( 'NONE',  ( -3.250000000000000000, -3.100000000000000089, 0.000000000000000000 ) ) ;
#46588=CARTESIAN_POINT ( 'NONE',  ( -10.01749676171999859, -59.99181054660999735, -7.660430254678000317 ) ) ;
#46589=EDGE_CURVE ( 'NONE', #25178, #40639, #44737, .T. ) ;
#46591=DIRECTION ( 'NONE',  ( 0.000000000000000000, 1.000000000000000000, 0.000000000000000000 ) ) ;
#46592=CARTESIAN_POINT ( 'NONE',  ( -1.929975092517999924, -23.20107256264000029, -12.72537404210999945 ) ) ;
#46594=CARTESIAN_POINT ( 'NONE',  ( 13.13047446164998711, -19.21421830981000767, 0.8260994316375004365 ) ) ;
#46596=CARTESIAN_POINT ( 'NONE',  ( -7.921335223404320836, -24.55094696616630401, -10.04563431748756130 ) ) ;
#46599=CARTESIAN_POINT ( 'NONE',  ( 11.51413715134999904, -76.48154810978000739, -3.593459816516999972 ) ) ;
#46600=ORIENTED_EDGE ( 'NONE', *, *, #39847, .T. ) ;
#46603=ADVANCED_FACE ( 'NONE', ( #38362 ), #6785, .T. ) ;
#46611=CARTESIAN_POINT ( 'NONE',  ( 1.750000000001000089, -23.25000000990999993, 12.56594317857000043 ) ) ;
#46612=ORIENTED_EDGE ( 'NONE', *, *, #3384, .T. ) ;
#46613=FACE_OUTER_BOUND ( 'NONE', #2029, .T. ) ;
#46614=LINE ( 'NONE', #1445, #46762 ) ;
#46616=VERTEX_POINT ( 'NONE', #11517 ) ;
#46622=CARTESIAN_POINT ( 'NONE',  ( 9.175573575496967393, -62.02695822328877995, -8.792784719842536845 ) ) ;
#46623=VERTEX_POINT ( 'NONE', #5613 ) ;
#46628=AXIS2_PLACEMENT_3D ( 'NONE', #5657, #24257, #28966 ) ;
#46630=CARTESIAN_POINT ( 'NONE',  ( 12.77306291382000047, -53.74129324268999852, 1.041150512314999999 ) ) ;
#46631=CARTESIAN_POINT ( 'NONE',  ( 10.42531125068999920, -23.26485145404000221, -7.624341767093000044 ) ) ;
#46632=ORIENTED_EDGE ( 'NONE', *, *, #24009, .T. ) ;
#46633=CARTESIAN_POINT ( 'NONE',  ( -12.68703394091000014, -23.75066116476999767, -1.889962945499999991 ) ) ;
#46636=DIRECTION ( 'NONE',  ( 0.000000000000000000, 0.000000000000000000, 1.000000000000000000 ) ) ;
#46638=CARTESIAN_POINT ( 'NONE',  ( -1.501534314733827147, -17.44847048338573359, -12.70455943739971794 ) ) ;
#46644=CARTESIAN_POINT ( 'NONE',  ( -7.685416442687999172, -76.58867693717000691, -9.616126112745998711 ) ) ;
#46646=AXIS2_PLACEMENT_3D ( 'NONE', #55810, #24216, #51389 ) ;
#46647=CARTESIAN_POINT ( 'NONE',  ( -3.392118867033536489, -1.870808869262021501, -0.9407460553073063725 ) ) ;
#46648=CARTESIAN_POINT ( 'NONE',  ( 10.01676948373999920, -60.00938276551000428, -7.658894993385999328 ) ) ;
#46649=CARTESIAN_POINT ( 'NONE',  ( 12.16303714866999997, -79.31220515959000750, 1.568404430622000190 ) ) ;
#46651=CARTESIAN_POINT ( 'NONE',  ( 12.72966282071409161, -18.23110224985535055, -1.931329623869578072 ) ) ;
#46652=CARTESIAN_POINT ( 'NONE',  ( 9.850507816072846978, -61.10508874482292185, -7.836744050180014298 ) ) ;
#46653=CARTESIAN_POINT ( 'NONE',  ( 12.18176164782117965, -78.30556067180121715, 0.8546284421110175167 ) ) ;
#46655=ORIENTED_EDGE ( 'NONE', *, *, #39304, .T. ) ;
#46657=EDGE_CURVE ( 'NONE', #11745, #15123, #16526, .T. ) ;
#46658=CARTESIAN_POINT ( 'NONE',  ( 0.000000000000000000, -18.75000000000000000, -12.50000000000000000 ) ) ;
#46660=CARTESIAN_POINT ( 'NONE',  ( -12.50000000000000000, -55.54999999966999980, 0.000000000000000000 ) ) ;
#46661=CARTESIAN_POINT ( 'NONE',  ( 0.2119930951406999997, -3.510997475527999789, -3.707774086492000354 ) ) ;
#46664=CARTESIAN_POINT ( 'NONE',  ( -1.728878934773139475, -76.08638080640866974, 11.64666186654994284 ) ) ;
#46668=ORIENTED_EDGE ( 'NONE', *, *, #1582, .T. ) ;
#46669=CARTESIAN_POINT ( 'NONE',  ( 12.71536556657276584, -24.12544729045777459, 1.781281568995779940 ) ) ;
#46671=VECTOR ( 'NONE', #26560, 1000.000000000000000 ) ;
#46673=EDGE_CURVE ( 'NONE', #47780, #21405, #57064, .T. ) ;
#46675=CARTESIAN_POINT ( 'NONE',  ( 3.165411199172024848, -2.270833333333332593, 0.8506806241676669877 ) ) ;
#46678=EDGE_CURVE ( 'NONE', #23001, #20606, #8009, .T. ) ;
#46680=DIRECTION ( 'NONE',  ( -0.7071067811865475727, 0.000000000000000000, 0.7071067811865475727 ) ) ;
#46682=CARTESIAN_POINT ( 'NONE',  ( 7.956418361382000981, -17.47110680143000039, -9.787952249849000808 ) ) ;
#46683=CARTESIAN_POINT ( 'NONE',  ( 0.000000000000000000, -56.01421830981000483, -13.15643568216998638 ) ) ;
#46689=CARTESIAN_POINT ( 'NONE',  ( 5.205657071218882770, -77.29238751238693794, 10.83901206616341106 ) ) ;
#46690=AXIS2_PLACEMENT_3D ( 'NONE', #7814, #24951, #39398 ) ;
#46693=DIRECTION ( 'NONE',  ( 0.000000000000000000, -1.433670265775999799E-08, -0.9999999999999998890 ) ) ;
#46694=CARTESIAN_POINT ( 'NONE',  ( -9.546815224142999767, -17.31472046677999899, -8.130854305520999858 ) ) ;
#46695=EDGE_CURVE ( 'NONE', #26753, #12183, #40058, .T. ) ;
#46697=DIRECTION ( 'NONE',  ( -1.000000000000000000, 0.000000000000000000, 0.000000000000000000 ) ) ;
#46700=ORIENTED_EDGE ( 'NONE', *, *, #3177, .T. ) ;
#46701=EDGE_LOOP ( 'NONE', ( #32276, #24904, #54003, #3046 ) ) ;
#46705=CARTESIAN_POINT ( 'NONE',  ( 7.605690612615000568, -18.57434870741999688, 10.52682230157000021 ) ) ;
#46706=EDGE_CURVE ( 'NONE', #27787, #42393, #3834, .T. ) ;
#46707=DIRECTION ( 'NONE',  ( -0.9999548435846228323, 0.000000000000000000, -0.009503199022040218977 ) ) ;
#46708=CARTESIAN_POINT ( 'NONE',  ( 6.964475361433999367, -79.00544258048999779, -9.848025321434999313 ) ) ;
#46710=CARTESIAN_POINT ( 'NONE',  ( 10.36221643470000053, -60.02123873632999818, 7.631895748967999715 ) ) ;
#46714=AXIS2_PLACEMENT_3D ( 'NONE', #51245, #51536, #6350 ) ;
#46715=VERTEX_POINT ( 'NONE', #47550 ) ;
#46724=AXIS2_PLACEMENT_3D ( 'NONE', #18544, #1135, #32098 ) ;
#46725=DIRECTION ( 'NONE',  ( -0.7071067811865474617, 0.000000000000000000, -0.7071067811865474617 ) ) ;
#46729=CARTESIAN_POINT ( 'NONE',  ( -7.647093862755999893, -23.36895637638999901, -10.00844027276999881 ) ) ;
#46730=CARTESIAN_POINT ( 'NONE',  ( 12.58338334669999981, -58.54800977479000323, -1.667961445601999992 ) ) ;
#46732=ORIENTED_EDGE ( 'NONE', *, *, #22033, .F. ) ;
#46733=CARTESIAN_POINT ( 'NONE',  ( 0.000000000000000000, -49.87071424677999687, 0.000000000000000000 ) ) ;
#46737=CARTESIAN_POINT ( 'NONE',  ( -9.389188763474001220, -17.28956227326999695, 8.194870530173000489 ) ) ;
#46739=CARTESIAN_POINT ( 'NONE',  ( -3.362520228900586439, -3.273832295754924182, -1.040226447706077639 ) ) ;
#46746=ORIENTED_EDGE ( 'NONE', *, *, #19243, .F. ) ;
#46748=CARTESIAN_POINT ( 'NONE',  ( -1.669849926066999890, -60.17228600383999293, -12.48404299555999941 ) ) ;
#46749=CARTESIAN_POINT ( 'NONE',  ( -7.553727747516310487, -55.11418618784217927, 7.997114030217357339 ) ) ;
#46753=CARTESIAN_POINT ( 'NONE',  ( 7.624757096123999212, -23.80351363819999833, -10.47516529248999895 ) ) ;
#46754=ADVANCED_FACE ( 'NONE', ( #43101 ), #54917, .F. ) ;
#46758=ORIENTED_EDGE ( 'NONE', *, *, #33418, .T. ) ;
#46761=CARTESIAN_POINT ( 'NONE',  ( 8.188285776285999518, -54.09506253957000155, -9.395726099541001020 ) ) ;
#46762=VECTOR ( 'NONE', #6141, 999.9999999999998863 ) ;
#46766=CARTESIAN_POINT ( 'NONE',  ( -7.764010764696696931, -24.12280919933758128, 9.931043767187555105 ) ) ;
#46771=EDGE_CURVE ( 'NONE', #16168, #56208, #45496, .T. ) ;
#46776=PLANE ( 'NONE',  #55380 ) ;
#46778=ORIENTED_EDGE ( 'NONE', *, *, #41341, .T. ) ;
#46782=CARTESIAN_POINT ( 'NONE',  ( 1.582498447119000229, -17.84913877521999837, 12.55493832972999968 ) ) ;
#46789=ORIENTED_EDGE ( 'NONE', *, *, #25850, .F. ) ;
#46792=CARTESIAN_POINT ( 'NONE',  ( 0.000000000000000000, -39.49523982883999906, 0.000000000000000000 ) ) ;
#46794=CARTESIAN_POINT ( 'NONE',  ( -0.8804656548076286171, -61.82803394674684228, -12.70299681155893268 ) ) ;
#46796=DIRECTION ( 'NONE',  ( 0.000000000000000000, 0.000000000000000000, 1.000000000000000000 ) ) ;
#46801=B_SPLINE_CURVE_WITH_KNOTS ( 'NONE', 3,
 ( #23385, #18381, #36084, #18091, #36667, #13938 ),
 .UNSPECIFIED., .F., .F.,
 ( 4, 1, 1, 4 ),
 ( 0.000000000000000000, 0.3333333333333000081, 0.6666666666667000474, 1.000000000000000000 ),
 .UNSPECIFIED. ) ;
#46802=CARTESIAN_POINT ( 'NONE',  ( 6.277130266346461873, -79.23046873804318579, -10.24763708790730554 ) ) ;
#46803=CARTESIAN_POINT ( 'NONE',  ( -10.00831378476999944, -55.42769332259999260, 7.646786280026000249 ) ) ;
#46805=CARTESIAN_POINT ( 'NONE',  ( 2.062503053667999797, -21.75736537952000305, -12.92177931904999966 ) ) ;
#46806=AXIS2_PLACEMENT_3D ( 'NONE', #7141, #42298, #19558 ) ;
#46808=CARTESIAN_POINT ( 'NONE',  ( 1.929975092517999924, -18.79892743736000327, -12.72537404210999945 ) ) ;
#46810=CARTESIAN_POINT ( 'NONE',  ( 0.000000000000000000, -13.07071424677999971, 0.000000000000000000 ) ) ;
#46813=CARTESIAN_POINT ( 'NONE',  ( 2.862077683958035301, -1.551983691494210005, 2.221749198134896464 ) ) ;
#46814=AXIS2_PLACEMENT_3D ( 'NONE', #21563, #57571, #22434 ) ;
#46815=ORIENTED_EDGE ( 'NONE', *, *, #42973, .T. ) ;
#46816=CARTESIAN_POINT ( 'NONE',  ( -5.911015991356902255, -78.88333333333332575, -10.22919423418180074 ) ) ;
#46817=CARTESIAN_POINT ( 'NONE',  ( 7.342331066867000544, -59.94999999967000548, -8.190859204290999784 ) ) ;
#46818=DIRECTION ( 'NONE',  ( 0.7071067811865474617, 0.000000000000000000, -0.7071067811865474617 ) ) ;
#46821=CARTESIAN_POINT ( 'NONE',  ( 12.55432891853855004, -18.61272687758708599, -1.749897736042411944 ) ) ;
#46830=CARTESIAN_POINT ( 'NONE',  ( -9.722718241315000398, -18.75000000000000000, -7.954951288349001004 ) ) ;
#46837=ORIENTED_EDGE ( 'NONE', *, *, #50654, .F. ) ;
#46838=ORIENTED_EDGE ( 'NONE', *, *, #46522, .F. ) ;
#46841=CARTESIAN_POINT ( 'NONE',  ( -10.12290050253000118, -23.24999997822999731, 7.648026768374000639 ) ) ;
#46842=ORIENTED_EDGE ( 'NONE', *, *, #44473, .F. ) ;
#46846=ORIENTED_EDGE ( 'NONE', *, *, #28163, .T. ) ;
#46847=EDGE_CURVE ( 'NONE', #3549, #41145, #1777, .T. ) ;
#46853=CARTESIAN_POINT ( 'NONE',  ( 3.188330803860000007, -2.833935831311999998, 1.184873324962000041 ) ) ;
#46854=ORIENTED_EDGE ( 'NONE', *, *, #3749, .T. ) ;
#46857=AXIS2_PLACEMENT_3D ( 'NONE', #51125, #28659, #46707 ) ;
#46860=CARTESIAN_POINT ( 'NONE',  ( 11.93290200807439660, -79.18167642368507586, -2.830846369544400609 ) ) ;
#46865=EDGE_CURVE ( 'NONE', #7685, #36041, #26800, .T. ) ;
#46868=CARTESIAN_POINT ( 'NONE',  ( 6.715696511375072397, -76.52634182472844770, 9.641850707901006956 ) ) ;
#46871=CARTESIAN_POINT ( 'NONE',  ( -0.3664097495403158544, -61.77190017435498959, -12.50575740046304674 ) ) ;
#46877=CARTESIAN_POINT ( 'NONE',  ( 10.04115011120000034, -19.23513569609999863, 7.682331425195999763 ) ) ;
#46878=CARTESIAN_POINT ( 'NONE',  ( -10.15323304115999825, -61.03079615981999950, -7.760925857031000241 ) ) ;
#46881=CARTESIAN_POINT ( 'NONE',  ( -0.06244121081497999715, -3.420791625799999736, 3.484461396181999682 ) ) ;
#46883=CARTESIAN_POINT ( 'NONE',  ( 12.43647262253000108, -24.91807034734999959, -0.03492325570150000419 ) ) ;
#46884=ADVANCED_FACE ( 'NONE', ( #5262, #36551 ), #40092, .F. ) ;
#46885=CIRCLE ( 'NONE', #58191, 0.5000000000000006661 ) ;
#46887=CARTESIAN_POINT ( 'NONE',  ( 0.000000000000000000, -18.75000000000000000, -12.00000000000000000 ) ) ;
#46889=CARTESIAN_POINT ( 'NONE',  ( -8.992856345071000845, -76.69757595554999341, 8.038460196811000102 ) ) ;
#46890=ORIENTED_EDGE ( 'NONE', *, *, #56903, .T. ) ;
#46891=CIRCLE ( 'NONE', #6323, 0.5000000000000004441 ) ;
#46894=VECTOR ( 'NONE', #30660, 1000.000000000000227 ) ;
#46896=CARTESIAN_POINT ( 'NONE',  ( 7.635939924770683618, -55.02474192263417763, 10.36595855978725744 ) ) ;
#46898=DIRECTION ( 'NONE',  ( 0.7071067811865475727, 0.000000000000000000, 0.7071067811865475727 ) ) ;
#46900=VECTOR ( 'NONE', #10076, 1000.000000000000000 ) ;
#46902=DIRECTION ( 'NONE',  ( 0.000000000000000000, 0.000000000000000000, 1.000000000000000000 ) ) ;
#46904=VERTEX_POINT ( 'NONE', #9402 ) ;
#46905=CARTESIAN_POINT ( 'NONE',  ( -1.081559480311999888, -0.7500000000000000000, 3.328697807033000000 ) ) ;
#46908=ORIENTED_EDGE ( 'NONE', *, *, #21054, .T. ) ;
#46915=EDGE_LOOP ( 'NONE', ( #28904, #21237, #40416, #36902 ) ) ;
#46916=ORIENTED_EDGE ( 'NONE', *, *, #3651, .T. ) ;
#46918=EDGE_CURVE ( 'NONE', #52919, #51909, #49859, .T. ) ;
#46921=ORIENTED_EDGE ( 'NONE', *, *, #38456, .F. ) ;
#46922=CARTESIAN_POINT ( 'NONE',  ( 12.59651451715000015, -55.40944962329000134, 1.801708894189000043 ) ) ;
#46926=CARTESIAN_POINT ( 'NONE',  ( -12.43647262253000108, -24.91807034734999959, 0.03492325570151000314 ) ) ;
#46928=CIRCLE ( 'NONE', #10163, 12.05000000000000071 ) ;
#46930=CARTESIAN_POINT ( 'NONE',  ( -12.50000000000000000, -13.07071422275999950, 0.000000000000000000 ) ) ;
#46935=VECTOR ( 'NONE', #23433, 999.9999999999998863 ) ;
#46938=CARTESIAN_POINT ( 'NONE',  ( -7.450482419345999752, -76.09060268177999831, -9.799277032148999922 ) ) ;
#46943=CARTESIAN_POINT ( 'NONE',  ( 0.4482635754052999855, -78.57590936191000708, -12.25553529036999834 ) ) ;
#46946=CARTESIAN_POINT ( 'NONE',  ( 1.705242708866661738, -2.770368159655117957, -2.767455873028740854 ) ) ;
#46947=CARTESIAN_POINT ( 'NONE',  ( 8.193144588781670734, -78.23440087569812817, -8.866198533586608477 ) ) ;
#46948=DIRECTION ( 'NONE',  ( 0.000000000000000000, 0.000000000000000000, -1.000000000000000000 ) ) ;
#46954=CARTESIAN_POINT ( 'NONE',  ( -3.558211308106999926, -3.404594557569000202, -1.064603940041000119 ) ) ;
#46957=CARTESIAN_POINT ( 'NONE',  ( -10.85381960069883611, -76.16858560240085296, 4.500525175705931247 ) ) ;
#46958=CARTESIAN_POINT ( 'NONE',  ( 1.750000000000000000, -23.25000000000000000, 12.00000000000000000 ) ) ;
#46960=CARTESIAN_POINT ( 'NONE',  ( 9.505949683906999681, -79.00000000000000000, 6.906476714433999575 ) ) ;
#46961=ORIENTED_EDGE ( 'NONE', *, *, #22891, .T. ) ;
#46964=CARTESIAN_POINT ( 'NONE',  ( -2.598917237794094337, -2.447916666666666519, 1.997276839918461722 ) ) ;
#46968=CARTESIAN_POINT ( 'NONE',  ( 3.250000000000000000, -3.350000000000000089, 0.000000000000000000 ) ) ;
#46969=CARTESIAN_POINT ( 'NONE',  ( 7.714303428875997959, -63.10294702886003648, -12.53545825868000385 ) ) ;
#46973=CARTESIAN_POINT ( 'NONE',  ( 7.958776492191999452, -24.47699850276000078, -9.723157982392999443 ) ) ;
#46974=DIRECTION ( 'NONE',  ( -0.7071067811865475727, 0.000000000000000000, -0.7071067811865475727 ) ) ;
#46976=CARTESIAN_POINT ( 'NONE',  ( 0.2838762717877208464, -77.82609350274218230, 12.06818374436646124 ) ) ;
#46977=B_SPLINE_SURFACE_WITH_KNOTS ( 'NONE', 3, 3, ( 
 ( #21362, #33488, #51528, #20225 ),
 ( #11371, #29348, #47394, #42950 ),
 ( #2507, #20511, #35504, #17221 ),
 ( #27236, #12506, #16944, #53533 ),
 ( #49109, #21934, #44380, #17513 ),
 ( #48533, #44977, #57960, #26645 ),
 ( #31071, #26944, #58257, #48821 ),
 ( #4824, #30505, #36107, #4234 ),
 ( #4532, #22532, #22823, #8659 ),
 ( #40542, #137, #57664, #17817 ),
 ( #49706, #13074, #44100, #26075 ),
 ( #3649, #40243, #12788, #18113 ),
 ( #9252, #22231, #44681, #35804 ),
 ( #13368, #45275, #53833, #31366 ),
 ( #54124, #21652, #13665, #31660 ),
 ( #35210, #49411, #40833, #8959 ),
 ( #34925, #52957, #8078, #53240 ) ),
 .UNSPECIFIED., .F., .F., .F.,
 ( 4, 1, 1, 1, 1, 1, 1, 1, 1, 1, 1, 1, 1, 1, 4 ),
 ( 4, 4 ),
 ( -0.01011408452864000045, 0.000000000000000000, 0.08333333333333001192, 0.1666666666667000196, 0.2500000000000000000, 0.3333333333333000081, 0.4166666666666999919, 0.5000000000000000000, 0.5833333333333000637, 0.6666666666667000474, 0.7500000000000000000, 0.8333333333333000637, 0.9166666666667000474, 1.000000000000000000, 1.010362559107000013 ),
 ( -0.3559705546267999954, 1.357612419580000118 ),
 .UNSPECIFIED. ) ;
#46982=CARTESIAN_POINT ( 'NONE',  ( -7.639893274927808342, -23.38715751204584237, -10.11462445490720974 ) ) ;
#46984=DIRECTION ( 'NONE',  ( 1.000000000000000000, 0.000000000000000000, 0.000000000000000000 ) ) ;
#46987=VERTEX_POINT ( 'NONE', #9109 ) ;
#46993=CARTESIAN_POINT ( 'NONE',  ( 7.646788101826000883, -18.62771363264999991, 10.00831428591000005 ) ) ;
#46995=CARTESIAN_POINT ( 'NONE',  ( -3.361591574393000048, -78.22944319244000155, 11.31358112888999834 ) ) ;
#46997=FACE_BOUND ( 'NONE', #50899, .T. ) ;
#47000=EDGE_CURVE ( 'NONE', #28385, #7685, #31218, .T. ) ;
#47002=CARTESIAN_POINT ( 'NONE',  ( 12.05000000000000071, -74.80000000000001137, 0.000000000000000000 ) ) ;
#47003=VERTEX_POINT ( 'NONE', #54850 ) ;
#47008=CARTESIAN_POINT ( 'NONE',  ( -9.546815224142999767, -17.31472046677999899, -8.130854305520999858 ) ) ;
#47009=CONICAL_SURFACE ( 'NONE', #9274, 0.6999999997695030007, 0.7853981633972997312 ) ;
#47012=CARTESIAN_POINT ( 'NONE',  ( -7.678690995204998870, -21.75648180056000314, 10.59551070212000035 ) ) ;
#47014=CARTESIAN_POINT ( 'NONE',  ( 0.000000000000000000, -0.7781249991808000255, -3.471875000818999801 ) ) ;
#47016=FACE_OUTER_BOUND ( 'NONE', #25322, .T. ) ;
#47021=CARTESIAN_POINT ( 'NONE',  ( 10.10912517728393567, -60.27586858096238132, 7.634643689465026917 ) ) ;
#47023=CARTESIAN_POINT ( 'NONE',  ( -8.813906587716449081, -53.78989792558626704, 8.872948314128050740 ) ) ;
#47026=CARTESIAN_POINT ( 'NONE',  ( 3.500000000000000000, -3.500000000000000000, 1.049058100190999900E-13 ) ) ;
#47031=DIRECTION ( 'NONE',  ( 0.7071067811865474617, -0.7071067811865474617, 3.873929780297256383E-09 ) ) ;
#47034=VERTEX_POINT ( 'NONE', #58106 ) ;
#47036=CARTESIAN_POINT ( 'NONE',  ( -1.382886570147999983, -61.43098219798999793, -12.65982054480000052 ) ) ;
#47037=CYLINDRICAL_SURFACE ( 'NONE', #37088, 1.750000000000001332 ) ;
#47040=CARTESIAN_POINT ( 'NONE',  ( 9.523353692535000192, -24.81947015623000041, -8.220363114681999761 ) ) ;
#47043=CARTESIAN_POINT ( 'NONE',  ( 6.519098162841222788, -78.52704705454330281, 9.775845571359413455 ) ) ;
#47045=VERTEX_POINT ( 'NONE', #40395 ) ;
#47046=EDGE_CURVE ( 'NONE', #4000, #17032, #48966, .T. ) ;
#47049=EDGE_CURVE ( 'NONE', #32490, #21905, #7762, .T. ) ;
#47050=CARTESIAN_POINT ( 'NONE',  ( 7.658894278873999539, -55.59060682883999505, -10.01676917980999981 ) ) ;
#47052=CARTESIAN_POINT ( 'NONE',  ( -12.50000000000000000, -18.55321828668999729, 1.250000000000000000 ) ) ;
#47053=CARTESIAN_POINT ( 'NONE',  ( -7.648026766735999793, -23.25000000582000226, 10.12290050089000104 ) ) ;
#47057=AXIS2_PLACEMENT_3D ( 'NONE', #32963, #9973, #6114 ) ;
#47058=CARTESIAN_POINT ( 'NONE',  ( -9.073547343405500953, -53.57191135162067752, 8.894853367357773877 ) ) ;
#47059=VERTEX_POINT ( 'NONE', #13224 ) ;
#47065=ORIENTED_EDGE ( 'NONE', *, *, #17520, .T. ) ;
#47067=ADVANCED_FACE ( 'NONE', ( #17967 ), #27097, .T. ) ;
#47069=ORIENTED_EDGE ( 'NONE', *, *, #36109, .F. ) ;
#47070=CARTESIAN_POINT ( 'NONE',  ( 1.798954018882000128, -18.78469026612999926, 12.61117007302000026 ) ) ;
#47079=ORIENTED_EDGE ( 'NONE', *, *, #40204, .F. ) ;
#47081=CARTESIAN_POINT ( 'NONE',  ( -12.71106812364130789, -24.25135172969568131, 1.717582538841718520 ) ) ;
#47083=CARTESIAN_POINT ( 'NONE',  ( -12.66322140213000047, -61.98161935699999958, -0.1487435796151000134 ) ) ;
#47085=DIRECTION ( 'NONE',  ( 0.000000000000000000, -0.7071067811866525998, -0.7071067811864425456 ) ) ;
#47087=CARTESIAN_POINT ( 'NONE',  ( 10.51493804038999968, -79.03332460306999963, 5.600620773984999801 ) ) ;
#47095=CARTESIAN_POINT ( 'NONE',  ( 1.933650113856000052, -18.59213746974000259, -12.70909635754000000 ) ) ;
#47097=EDGE_CURVE ( 'NONE', #20752, #29379, #28510, .T. ) ;
#47101=CARTESIAN_POINT ( 'NONE',  ( 12.00000000000000000, -55.54999999966999980, 1.250000000000000000 ) ) ;
#47103=CARTESIAN_POINT ( 'NONE',  ( 3.034718321201248070, -1.045467675721396095, 1.979367435497295435 ) ) ;
#47105=CARTESIAN_POINT ( 'NONE',  ( 0.03170276877622815043, -3.500000000000000444, -3.470587695368843040 ) ) ;
#47107=CARTESIAN_POINT ( 'NONE',  ( -1.980584515756000030, -23.26485150094000076, -12.76303204340999997 ) ) ;
#47111=CARTESIAN_POINT ( 'NONE',  ( -12.96685733093999993, -76.95470625016000099, -1.095351912296000041 ) ) ;
#47112=DIRECTION ( 'NONE',  ( 1.000000000000000000, 0.000000000000000000, 0.000000000000000000 ) ) ;
#47116=DIRECTION ( 'NONE',  ( 0.9957542233912697327, -0.04890176544230847439, -0.07798810124034757929 ) ) ;
#47117=EDGE_CURVE ( 'NONE', #55491, #38967, #32683, .T. ) ;
#47118=DIRECTION ( 'NONE',  ( 0.000000000000000000, -1.000000000000000000, 0.000000000000000000 ) ) ;
#47124=CARTESIAN_POINT ( 'NONE',  ( 1.980584515752000119, -18.73514853375999678, 12.76303204602000108 ) ) ;
#47126=CYLINDRICAL_SURFACE ( 'NONE', #27045, 1.750000000000001332 ) ;
#47130=ORIENTED_EDGE ( 'NONE', *, *, #16434, .F. ) ;
#47131=ORIENTED_EDGE ( 'NONE', *, *, #54939, .F. ) ;
#47133=CARTESIAN_POINT ( 'NONE',  ( -8.838834764832000701, -55.54999999966999980, 8.838834764832000701 ) ) ;
#47134=DIRECTION ( 'NONE',  ( 0.000000000000000000, 1.000000000000000000, 0.000000000000000000 ) ) ;
#47138=ORIENTED_EDGE ( 'NONE', *, *, #39681, .T. ) ;
#47143=CARTESIAN_POINT ( 'NONE',  ( -10.45204383628000144, -56.03743350618999841, -7.651147548114000330 ) ) ;
#47144=ORIENTED_EDGE ( 'NONE', *, *, #56179, .F. ) ;
#47145=CARTESIAN_POINT ( 'NONE',  ( -1.151238488875999888, -3.153144585189999738, -3.200629320682000234 ) ) ;
#47147=EDGE_LOOP ( 'NONE', ( #36138, #50503, #48342 ) ) ;
#47152=CARTESIAN_POINT ( 'NONE',  ( -8.414570695956999913, -60.64999999943950826, 8.414570695956999913 ) ) ;
#47154=CARTESIAN_POINT ( 'NONE',  ( 0.4482767731681003287, -78.57812134408507632, -12.25589611745950869 ) ) ;
#47161=CARTESIAN_POINT ( 'NONE',  ( 5.516207834483522809, -76.53601079641730109, 10.37660978597248018 ) ) ;
#47169=CARTESIAN_POINT ( 'NONE',  ( -12.51072239526000196, -52.49705297114005020, -0.7871079366006996647 ) ) ;
#47172=CARTESIAN_POINT ( 'NONE',  ( -10.13402523426999835, -60.52303809408999768, -7.647751776506999555 ) ) ;
#47176=CARTESIAN_POINT ( 'NONE',  ( 12.52582254643368209, -54.99059700767242731, 1.680974932891769358 ) ) ;
#47177=CARTESIAN_POINT ( 'NONE',  ( 12.66761950490999844, -24.22355206198999866, 1.696827901577000031 ) ) ;
#47181=CARTESIAN_POINT ( 'NONE',  ( 0.7656296041185000067, -76.62556667361999985, 12.03752960824999896 ) ) ;
#47182=EDGE_LOOP ( 'NONE', ( #49952, #2583, #3407, #57620 ) ) ;
#47183=ADVANCED_FACE ( 'NONE', ( #11261 ), #48318, .F. ) ;
#47185=DIRECTION ( 'NONE',  ( -1.000000000000000000, 0.000000000000000000, 0.000000000000000000 ) ) ;
#47187=CARTESIAN_POINT ( 'NONE',  ( 8.274781782443849210, -53.82110650083671288, 9.689260013493322887 ) ) ;
#47189=CARTESIAN_POINT ( 'NONE',  ( 12.78037507859000144, -54.50670131396999807, -1.812742845509000000 ) ) ;
#47194=VERTEX_POINT ( 'NONE', #11551 ) ;
#47195=CARTESIAN_POINT ( 'NONE',  ( -3.250000000000000000, -1.000000000000000000, 1.223542571470000149E-13 ) ) ;
#47197=AXIS2_PLACEMENT_3D ( 'NONE', #29310, #41451, #1036 ) ;
#47200=VERTEX_POINT ( 'NONE', #56986 ) ;
#47208=ORIENTED_EDGE ( 'NONE', *, *, #20760, .T. ) ;
#47209=ORIENTED_EDGE ( 'NONE', *, *, #46695, .T. ) ;
#47214=CARTESIAN_POINT ( 'NONE',  ( -1.634907902065669383, -2.517778331623519605, 2.839622281756045030 ) ) ;
#47217=ORIENTED_EDGE ( 'NONE', *, *, #22608, .F. ) ;
#47220=CARTESIAN_POINT ( 'NONE',  ( 8.485281374238999419, -60.04999999966999980, -8.485281374238999419 ) ) ;
#47222=DIRECTION ( 'NONE',  ( 0.000000000000000000, 1.000000000000000000, 0.000000000000000000 ) ) ;
#47223=B_SPLINE_CURVE_WITH_KNOTS ( 'NONE', 3,
 ( #34137, #11733, #49491, #53615, #22614, #4615, #36190, #30865, #44460, #40024 ),
 .UNSPECIFIED., .F., .F.,
 ( 4, 2, 2, 2, 4 ),
 ( 0.000000000000000000, 0.2500000000000000000, 0.5000000000000000000, 0.7500000000000000000, 1.000000000000000000 ),
 .UNSPECIFIED. ) ;
#47227=CARTESIAN_POINT ( 'NONE',  ( -7.760939450736999312, -24.23085356333000107, 10.15321588359000060 ) ) ;
#47232=DIRECTION ( 'NONE',  ( 0.000000000000000000, -1.000000000000000000, -9.095580416467000435E-12 ) ) ;
#47233=CARTESIAN_POINT ( 'NONE',  ( 7.914613980750001332, -79.30035326240999893, 9.019916049260999102 ) ) ;
#47235=DIRECTION ( 'NONE',  ( 0.000000000000000000, -1.000000000000000000, 0.000000000000000000 ) ) ;
#47236=CARTESIAN_POINT ( 'NONE',  ( 11.19183857952876338, -77.82967953535423078, 4.379999559240030926 ) ) ;
#47240=CARTESIAN_POINT ( 'NONE',  ( 1.666698456700999920, -23.19181739840000134, 12.50018138921000066 ) ) ;
#47242=CARTESIAN_POINT ( 'NONE',  ( 3.533935378582000020, -2.606572672876999786, -1.142694998219000002 ) ) ;
#47245=CARTESIAN_POINT ( 'NONE',  ( -8.399527302420572994, -76.13838338929400607, 8.217467006092146420 ) ) ;
#47250=EDGE_CURVE ( 'NONE', #26247, #49440, #12316, .T. ) ;
#47251=CARTESIAN_POINT ( 'NONE',  ( -3.438348731681998949, -76.65247415041467605, -11.82003900998999946 ) ) ;
#47254=CARTESIAN_POINT ( 'NONE',  ( 0.8506806241676515556, -2.354166666666666963, 3.165411199172028844 ) ) ;
#47255=CARTESIAN_POINT ( 'NONE',  ( -8.541150802335000236, -61.80800189248000009, 9.205830468622998808 ) ) ;
#47258=DIRECTION ( 'NONE',  ( 0.000000000000000000, 0.000000000000000000, -1.000000000000000000 ) ) ;
#47259=DIRECTION ( 'NONE',  ( 0.000000000000000000, 0.000000000000000000, -1.000000000000000000 ) ) ;
#47260=ORIENTED_EDGE ( 'NONE', *, *, #11514, .F. ) ;
#47262=CARTESIAN_POINT ( 'NONE',  ( 7.850076763456510953, -24.31471441247266796, -9.837736658173248827 ) ) ;
#47265=B_SPLINE_CURVE_WITH_KNOTS ( 'NONE', 3,
 ( #38579, #51885, #42148, #16154, #7000, #20581, #2296, #6711, #15861, #11158, #11442, #29132, #55730, #2013, #56595, #29422, #1717, #34131, #25002, #52173, #20292, #20011, #42445, #15568 ),
 .UNSPECIFIED., .F., .F.,
 ( 4, 2, 2, 2, 2, 2, 2, 2, 2, 2, 2, 4 ),
 ( 0.000000000000000000, 0.1250000000000000555, 0.2500000000000001110, 0.3750000000000001665, 0.4375000000000002220, 0.5000000000000002220, 0.6250000000000002220, 0.6875000000000003331, 0.7500000000000003331, 0.8750000000000001110, 0.9375000000000001110, 1.000000000000000000 ),
 .UNSPECIFIED. ) ;
#47267=DIRECTION ( 'NONE',  ( 0.000000000000000000, -1.000000000000000000, 9.283980536439000051E-14 ) ) ;
#47268=EDGE_CURVE ( 'NONE', #51486, #11972, #25396, .T. ) ;
#47270=AXIS2_PLACEMENT_3D ( 'NONE', #53288, #34102, #52143 ) ;
#47271=CARTESIAN_POINT ( 'NONE',  ( -1.001315001699999874, -54.11477588220000001, -12.50000000000000000 ) ) ;
#47272=CARTESIAN_POINT ( 'NONE',  ( -7.678657038172577387, -23.79377623515384954, -10.03844138475501957 ) ) ;
#47275=CARTESIAN_POINT ( 'NONE',  ( 1.980584515756000030, -23.26485150094000076, 12.76303204340999997 ) ) ;
#47278=EDGE_LOOP ( 'NONE', ( #43371, #11184, #51919, #13988 ) ) ;
#47279=EDGE_LOOP ( 'NONE', ( #53345, #1900, #53643, #8911 ) ) ;
#47282=ORIENTED_EDGE ( 'NONE', *, *, #57618, .T. ) ;
#47283=EDGE_CURVE ( 'NONE', #2251, #6738, #56128, .T. ) ;
#47284=CARTESIAN_POINT ( 'NONE',  ( 10.30768118225000052, -18.25239703915999812, 7.634415485503000198 ) ) ;
#47285=CARTESIAN_POINT ( 'NONE',  ( -0.8804656548849725262, -53.77196605263301166, 12.70299681147155191 ) ) ;
#47286=CARTESIAN_POINT ( 'NONE',  ( -1.285688189784000013, -78.94796114434001311, -11.99310356001000066 ) ) ;
#47288=DIRECTION ( 'NONE',  ( 1.000000000000000000, 0.000000000000000000, 0.000000000000000000 ) ) ;
#47293=AXIS2_PLACEMENT_3D ( 'NONE', #7239, #16968, #52982 ) ;
#47294=ORIENTED_EDGE ( 'NONE', *, *, #52763, .T. ) ;
#47296=DIRECTION ( 'NONE',  ( -0.7071067811865473507, -1.433669009702094715E-08, -0.7071067811865473507 ) ) ;
#47302=DIRECTION ( 'NONE',  ( -0.7071067811865475727, 0.000000000000000000, 0.7071067811865475727 ) ) ;
#47304=DIRECTION ( 'NONE',  ( 1.000000000000000000, 0.000000000000000000, 0.000000000000000000 ) ) ;
#47307=EDGE_LOOP ( 'NONE', ( #13219, #55251, #4915, #1466 ) ) ;
#47309=VECTOR ( 'NONE', #7906, 1000.000000000000000 ) ;
#47311=CARTESIAN_POINT ( 'NONE',  ( 9.837756817801476927, -61.11467795335811815, 7.850057933454666959 ) ) ;
#47313=CARTESIAN_POINT ( 'NONE',  ( -9.516265623875000301, -17.17460635740999919, 8.227505979428000771 ) ) ;
#47316=CARTESIAN_POINT ( 'NONE',  ( -2.617062270065174001, -1.808265572247988562, -2.353168472005194634 ) ) ;
#47319=CARTESIAN_POINT ( 'NONE',  ( 1.929975092519000013, -55.59892743702999240, -12.72537404207999856 ) ) ;
#47324=ORIENTED_EDGE ( 'NONE', *, *, #29568, .T. ) ;
#47325=CARTESIAN_POINT ( 'NONE',  ( 10.98384528668755244, -18.77109020608506995, -0.5959859912293845596 ) ) ;
#47326=ADVANCED_FACE ( 'NONE', ( #57276 ), #7110, .F. ) ;
#47327=CARTESIAN_POINT ( 'NONE',  ( -1.629367637654999923, -60.48263643365999798, -12.46114270829000148 ) ) ;
#47328=CARTESIAN_POINT ( 'NONE',  ( -8.180687091746479567, -55.49344856148417904, 7.353725627630893769 ) ) ;
#47334=CARTESIAN_POINT ( 'NONE',  ( -9.998727717549755312, -60.72738947565338208, 7.709134076929469614 ) ) ;
#47335=CARTESIAN_POINT ( 'NONE',  ( 9.758259394072377191, -78.49507498617447254, 6.543158735238040258 ) ) ;
#47336=CARTESIAN_POINT ( 'NONE',  ( -8.803747447685278615, -62.01568152305762283, 9.164340453807367837 ) ) ;
#47340=ADVANCED_FACE ( 'NONE', ( #25481 ), #43505, .F. ) ;
#47345=DIRECTION ( 'NONE',  ( -0.7071067811865475727, 0.000000000000000000, -0.7071067811865475727 ) ) ;
#47348=CARTESIAN_POINT ( 'NONE',  ( -9.689263856727277968, -53.82111184930475645, 8.274777958929785626 ) ) ;
#47349=ORIENTED_EDGE ( 'NONE', *, *, #1215, .F. ) ;
#47350=CARTESIAN_POINT ( 'NONE',  ( 1.667917367065999912, -23.28056535155999995, 12.49306764015999960 ) ) ;
#47352=ORIENTED_EDGE ( 'NONE', *, *, #57496, .F. ) ;
#47353=ORIENTED_EDGE ( 'NONE', *, *, #29073, .T. ) ;
#47354=CARTESIAN_POINT ( 'NONE',  ( -12.54902617714999913, -53.79030198112999273, -0.4617931494615999943 ) ) ;
#47355=AXIS2_PLACEMENT_3D ( 'NONE', #28745, #46796, #41757 ) ;
#47356=VERTEX_POINT ( 'NONE', #43501 ) ;
#47358=ORIENTED_EDGE ( 'NONE', *, *, #41341, .F. ) ;
#47360=CARTESIAN_POINT ( 'NONE',  ( -0.4356486348717999446, -17.11935044189999999, 12.43591427121000237 ) ) ;
#47362=LINE ( 'NONE', #29313, #1381 ) ;
#47366=EDGE_LOOP ( 'NONE', ( #10761, #21260, #6768, #50799 ) ) ;
#47369=LINE ( 'NONE', #33753, #30992 ) ;
#47370=ADVANCED_FACE ( 'NONE', ( #48235 ), #23123, .F. ) ;
#47371=CARTESIAN_POINT ( 'NONE',  ( -12.66761950495000022, -61.02355206165999846, -1.696827901577000031 ) ) ;
#47373=CARTESIAN_POINT ( 'NONE',  ( 7.613962827178999859, -18.69360374348000065, 10.53101998747000145 ) ) ;
#47380=CARTESIAN_POINT ( 'NONE',  ( -10.36289663187000087, -55.59893657650000165, 7.633501051906999457 ) ) ;
#47383=CARTESIAN_POINT ( 'NONE',  ( 1.931043762602999925, -22.77819125662999866, -12.75761570867000039 ) ) ;
#47384=DIRECTION ( 'NONE',  ( 0.000000000000000000, -1.000000000000000000, 0.000000000000000000 ) ) ;
#47385=CARTESIAN_POINT ( 'NONE',  ( 2.065550207748000133, -18.57434920668999823, -12.82162303854000029 ) ) ;
#47386=CARTESIAN_POINT ( 'NONE',  ( -2.000078442263883094, -1.174552220937325364, -2.601275589776585573 ) ) ;
#47388=CARTESIAN_POINT ( 'NONE',  ( 1.001315002179999913, -17.31477588286000113, 12.50000000000000000 ) ) ;
#47390=CARTESIAN_POINT ( 'NONE',  ( 0.7085295082841903680, -1.108782177693018456, 3.546401372608706914 ) ) ;
#47392=LINE ( 'NONE', #42948, #7497 ) ;
#47393=DIRECTION ( 'NONE',  ( 0.000000000000000000, 0.000000000000000000, 1.000000000000000000 ) ) ;
#47394=CARTESIAN_POINT ( 'NONE',  ( -1.798944584246999989, -55.58466771687000119, 12.61116915997000021 ) ) ;
#47399=CARTESIAN_POINT ( 'NONE',  ( -12.46164872704999915, -55.12834420008999814, 1.631615798669999950 ) ) ;
#47401=CARTESIAN_POINT ( 'NONE',  ( 2.015551294784000191, -60.60347704811000824, 12.79857978897999971 ) ) ;
#47402=CARTESIAN_POINT ( 'NONE',  ( 3.250000000000000444, -3.239583333333332593, -0.4254240051736113415 ) ) ;
#47407=EDGE_CURVE ( 'NONE', #31775, #30023, #33435, .T. ) ;
#47408=CARTESIAN_POINT ( 'NONE',  ( -0.02218730529862296408, -76.32463168808217802, -11.74982668617501602 ) ) ;
#47410=CARTESIAN_POINT ( 'NONE',  ( -1.823750004803999641E-14, -80.79999999999999716, 0.000000000000000000 ) ) ;
#47411=EDGE_CURVE ( 'NONE', #53718, #308, #15883, .T. ) ;
#47414=CARTESIAN_POINT ( 'NONE',  ( 1.636761686205427058, -2.666666666666666519, -2.839805762151336399 ) ) ;
#47416=CARTESIAN_POINT ( 'NONE',  ( -12.56594317823000040, -18.74999998606000062, -1.750000000000000000 ) ) ;
#47419=CARTESIAN_POINT ( 'NONE',  ( 1.001315002657000131, -61.48522411647999775, -12.50000000000000000 ) ) ;
#47421=B_SPLINE_CURVE_WITH_KNOTS ( 'NONE', 3,
 ( #45236, #99, #3128, #17779, #4783, #25545, #9211, #26908, #7833, #56850, #13331, #25834, #36068, #22194, #31325, #40793, #8918, #44938 ),
 .UNSPECIFIED., .F., .F.,
 ( 4, 2, 2, 2, 2, 2, 2, 2, 4 ),
 ( 0.000000000000000000, 0.06250000000000004163, 0.1250000000000000833, 0.2499999999999991118, 0.4999999999999977796, 0.7499999999999963363, 0.8124999999999972244, 0.8749999999999980016, 1.000000000000000000 ),
 .UNSPECIFIED. ) ;
#47422=ORIENTED_EDGE ( 'NONE', *, *, #22102, .T. ) ;
#47423=CARTESIAN_POINT ( 'NONE',  ( 0.5135400119441678735, -25.17868533861081914, 12.70453250098436904 ) ) ;
#47425=ORIENTED_EDGE ( 'NONE', *, *, #31348, .F. ) ;
#47427=EDGE_CURVE ( 'NONE', #43451, #53718, #31329, .T. ) ;
#47429=CARTESIAN_POINT ( 'NONE',  ( -11.75000000000000000, -77.29999999999999716, 0.000000000000000000 ) ) ;
#47435=CARTESIAN_POINT ( 'NONE',  ( -1.574774750116000099, -2.142316864579000057, -3.014985959147999939 ) ) ;
#47437=CARTESIAN_POINT ( 'NONE',  ( 9.050966799188000067, -55.64999999964999233, 7.919595949288999570 ) ) ;
#47444=CARTESIAN_POINT ( 'NONE',  ( 11.03923301813926727, -78.66434349831403949, -5.342590761205005201 ) ) ;
#47455=DIRECTION ( 'NONE',  ( -0.7071067811865474617, 3.445410891336226740E-11, -0.7071067811865474617 ) ) ;
#47456=CARTESIAN_POINT ( 'NONE',  ( -3.055408317354031844, -3.073761893863659722, 1.105607771687054264 ) ) ;
#47457=B_SPLINE_CURVE_WITH_KNOTS ( 'NONE', 3,
 ( #40267, #5419, #23428, #19006, #58279, #17843, #13392, #40567 ),
 .UNSPECIFIED., .F., .F.,
 ( 4, 2, 2, 4 ),
 ( 0.000000000000000000, 0.5000000000000000000, 0.7500000000000000000, 1.000000000000000000 ),
 .UNSPECIFIED. ) ;
#47460=CIRCLE ( 'NONE', #24801, 0.5999999999999999778 ) ;
#47463=CARTESIAN_POINT ( 'NONE',  ( -7.714303428875997959, -63.10294702886003648, 12.53545825868000385 ) ) ;
#47465=CARTESIAN_POINT ( 'NONE',  ( -11.75000000000000000, -76.20000000000000284, -1.391479524197000231E-14 ) ) ;
#47467=CIRCLE ( 'NONE', #36132, 12.05000000000000071 ) ;
#47472=CARTESIAN_POINT ( 'NONE',  ( 12.51033564907000084, -78.27980835132001403, -3.582046052171000028 ) ) ;
#47474=CARTESIAN_POINT ( 'NONE',  ( 9.837756816588985487, -24.31467795598597093, 7.850057934554545369 ) ) ;
#47476=CARTESIAN_POINT ( 'NONE',  ( -12.02449095972999871, -76.68250438773999633, -2.131941081079999911 ) ) ;
#47477=ORIENTED_EDGE ( 'NONE', *, *, #47821, .F. ) ;
#47480=CARTESIAN_POINT ( 'NONE',  ( 12.43647262256999930, -61.71807034702999317, -0.03492325570155000586 ) ) ;
#47481=CARTESIAN_POINT ( 'NONE',  ( -9.821634722185001110, -78.80854920034998656, -7.703425204176999941 ) ) ;
#47484=CIRCLE ( 'NONE', #19179, 12.90000000000000036 ) ;
#47486=CARTESIAN_POINT ( 'NONE',  ( 0.6999999999999999556, -21.00000000000000000, 11.90000000000000036 ) ) ;
#47489=CARTESIAN_POINT ( 'NONE',  ( 0.000000000000000000, -3.500000000000000000, 0.000000000000000000 ) ) ;
#47491=EDGE_LOOP ( 'NONE', ( #9985, #19259, #50311 ) ) ;
#47492=AXIS2_PLACEMENT_3D ( 'NONE', #19108, #50411, #14369 ) ;
#47494=DIRECTION ( 'NONE',  ( -0.9957542233912675123, -0.04890176544233841571, 0.07798810124035751579 ) ) ;
#47498=VERTEX_POINT ( 'NONE', #24258 ) ;
#47501=EDGE_CURVE ( 'NONE', #8280, #891, #22848, .T. ) ;
#47503=AXIS2_PLACEMENT_3D ( 'NONE', #39100, #25809, #35223 ) ;
#47504=ADVANCED_FACE ( 'NONE', ( #1545 ), #37002, .F. ) ;
#47507=ORIENTED_EDGE ( 'NONE', *, *, #53293, .F. ) ;
#47508=CARTESIAN_POINT ( 'NONE',  ( -12.76303204522000101, -23.26485147686999966, -1.980584515753000208 ) ) ;
#47511=CARTESIAN_POINT ( 'NONE',  ( 4.750030159171999777, -78.70665068745630322, -11.30647155123999958 ) ) ;
#47513=CARTESIAN_POINT ( 'NONE',  ( 9.650965486062000664, -53.86598967493999623, 8.252456811976999873 ) ) ;
#47514=CARTESIAN_POINT ( 'NONE',  ( -7.247844507162001015, -60.04999999966999980, 9.722718241315000398 ) ) ;
#47516=FACE_OUTER_BOUND ( 'NONE', #32516, .T. ) ;
#47517=EDGE_CURVE ( 'NONE', #31168, #10827, #30367, .T. ) ;
#47521=CARTESIAN_POINT ( 'NONE',  ( -7.450482419345999752, -76.02126934844999084, -9.799277032148999922 ) ) ;
#47524=CARTESIAN_POINT ( 'NONE',  ( 9.966224254750001066, -60.46904904752999954, -7.657729124028000101 ) ) ;
#47525=CARTESIAN_POINT ( 'NONE',  ( -9.042566447131001439, -79.04168679971999723, -8.284387575507999202 ) ) ;
#47528=CARTESIAN_POINT ( 'NONE',  ( 7.383247350150824673, -77.72738732844908327, -9.556516804512405372 ) ) ;
#47533=B_SPLINE_CURVE_WITH_KNOTS ( 'NONE', 3,
 ( #52772, #12327, #2046, #56341, #11759, #6743, #15894, #56056, #33598, #30314, #51637, #11191, #33880, #51920, #25035, #47508 ),
 .UNSPECIFIED., .F., .F.,
 ( 4, 2, 2, 2, 2, 2, 2, 4 ),
 ( 0.000000000000000000, 0.2500000000000004996, 0.3750000000000001110, 0.4999999999999997780, 0.6249999999999993339, 0.6875000000000004441, 0.7500000000000017764, 1.000000000000000000 ),
 .UNSPECIFIED. ) ;
#47534=ORIENTED_EDGE ( 'NONE', *, *, #48945, .T. ) ;
#47536=CARTESIAN_POINT ( 'NONE',  ( 12.61271904362000029, -59.99692351013000291, -1.798332623270000097 ) ) ;
#47539=CARTESIAN_POINT ( 'NONE',  ( 2.686313133137999909, -2.161638932810000302, -2.332641043696000338 ) ) ;
#47543=CARTESIAN_POINT ( 'NONE',  ( -3.271883600065454090, -76.09715442452088041, 11.29549362133648671 ) ) ;
#47547=EDGE_LOOP ( 'NONE', ( #24161, #44889, #30241 ) ) ;
#47550=CARTESIAN_POINT ( 'NONE',  ( -11.99999999979999821, -18.85000000927000130, -0.7999999997951999786 ) ) ;
#47551=CARTESIAN_POINT ( 'NONE',  ( -8.194866293469999619, -61.51043252617999713, 9.389192598819999347 ) ) ;
#47558=CARTESIAN_POINT ( 'NONE',  ( -12.50000000000000000, -26.93717104351999936, 0.000000000000000000 ) ) ;
#47562=AXIS2_PLACEMENT_3D ( 'NONE', #7264, #29968, #39129 ) ;
#47565=CARTESIAN_POINT ( 'NONE',  ( -7.709155920968131070, -23.92747430419197485, -9.998700314110912757 ) ) ;
#47567=EDGE_CURVE ( 'NONE', #54533, #18787, #39275, .T. ) ;
#47578=DIRECTION ( 'NONE',  ( -0.7071067811865474617, 0.7071067811865474617, 1.545233129589103907E-10 ) ) ;
#47580=CARTESIAN_POINT ( 'NONE',  ( -1.208267227064446780, -53.97409317820400787, 12.70228502419021765 ) ) ;
#47581=CARTESIAN_POINT ( 'NONE',  ( 7.139902610388999982, -77.92838321630000564, -10.43201753306000157 ) ) ;
#47582=CARTESIAN_POINT ( 'NONE',  ( 10.98362417419999915, -18.84999999999999787, -0.5999999999999999778 ) ) ;
#47583=FACE_OUTER_BOUND ( 'NONE', #15077, .T. ) ;
#47584=ADVANCED_FACE ( 'NONE', ( #56428 ), #14363, .F. ) ;
#47585=CARTESIAN_POINT ( 'NONE',  ( 10.12290050256999940, -18.75000002239000096, 7.648026768411000376 ) ) ;
#47588=ORIENTED_EDGE ( 'NONE', *, *, #27890, .F. ) ;
#47589=CARTESIAN_POINT ( 'NONE',  ( -1.250000000000000000, -18.75000000000000000, -12.00000000000000000 ) ) ;
#47590=ORIENTED_EDGE ( 'NONE', *, *, #55632, .T. ) ;
#47595=CARTESIAN_POINT ( 'NONE',  ( 14.00000000000000000, -5.900000000000010125, 0.000000000000000000 ) ) ;
#47599=FACE_OUTER_BOUND ( 'NONE', #32242, .T. ) ;
#47602=EDGE_CURVE ( 'NONE', #36570, #33521, #34830, .T. ) ;
#47603=( NAMED_UNIT ( * ) SI_UNIT ( $, .STERADIAN. ) SOLID_ANGLE_UNIT ( ) );
#47605=EDGE_LOOP ( 'NONE', ( #790, #27486, #8113, #27914, #9441 ) ) ;
#47610=CARTESIAN_POINT ( 'NONE',  ( -8.870405106263998363, -16.93036971772000143, 8.878274241758997931 ) ) ;
#47619=VERTEX_POINT ( 'NONE', #52576 ) ;
#47620=CARTESIAN_POINT ( 'NONE',  ( -11.18238235180553630, -78.67127684549025446, 4.147843596343820494 ) ) ;
#47621=CARTESIAN_POINT ( 'NONE',  ( 9.394120223593105834, -76.99930578456108776, 7.218235409050908657 ) ) ;
#47623=CARTESIAN_POINT ( 'NONE',  ( 0.4450739772378000114, -61.67813214767999597, -12.43586747599000120 ) ) ;
#47629=EDGE_CURVE ( 'NONE', #35538, #22602, #43996, .T. ) ;
#47632=CARTESIAN_POINT ( 'NONE',  ( -8.121699804379593601, -61.63626205714820827, 9.841121124294026856 ) ) ;
#47637=DIRECTION ( 'NONE',  ( 0.000000000000000000, 1.000000000000000000, 0.000000000000000000 ) ) ;
#47638=CARTESIAN_POINT ( 'NONE',  ( -7.220923959705292994, -77.72708333333335418, 9.396085398178589898 ) ) ;
#47639=CARTESIAN_POINT ( 'NONE',  ( -7.651160336697000020, -56.03767313780999615, -10.45205658995000064 ) ) ;
#47642=ORIENTED_EDGE ( 'NONE', *, *, #53424, .F. ) ;
#47643=CARTESIAN_POINT ( 'NONE',  ( 1.799501877793999949, -18.71082276572999703, 12.60552511010000032 ) ) ;
#47645=CARTESIAN_POINT ( 'NONE',  ( 11.44417895085270054, -76.07083333333332575, 3.075537641221564922 ) ) ;
#47646=VERTEX_POINT ( 'NONE', #25980 ) ;
#47647=EDGE_LOOP ( 'NONE', ( #14413, #50839, #20886, #47352 ) ) ;
#47648=CARTESIAN_POINT ( 'NONE',  ( -12.66737112512999985, -54.56697834100999955, -1.690666607834999891 ) ) ;
#47651=ORIENTED_EDGE ( 'NONE', *, *, #14682, .T. ) ;
#47652=CARTESIAN_POINT ( 'NONE',  ( 10.00831380745999866, -23.37230364585000331, 7.646786653130999589 ) ) ;
#47654=CARTESIAN_POINT ( 'NONE',  ( -7.655984445742507027, -60.50337239307266657, 10.06694410270485918 ) ) ;
#47662=ORIENTED_EDGE ( 'NONE', *, *, #151, .T. ) ;
#47665=CARTESIAN_POINT ( 'NONE',  ( -12.54981857179000038, -61.84836586168999872, 0.03768635776142000016 ) ) ;
#47667=CARTESIAN_POINT ( 'NONE',  ( 7.678667886032999768, -21.75736537952000305, 10.59548767697000038 ) ) ;
#47668=CARTESIAN_POINT ( 'NONE',  ( 7.921335223427023564, -61.35094696583096407, 10.04563431751979508 ) ) ;
#47671=CARTESIAN_POINT ( 'NONE',  ( -1.276771495430000038E-14, -69.50420297070000686, 0.000000000000000000 ) ) ;
#47674=CARTESIAN_POINT ( 'NONE',  ( -10.43474250408442217, -76.66142246521233972, 5.404247698127043975 ) ) ;
#47675=CARTESIAN_POINT ( 'NONE',  ( -10.01676221090000141, -55.59058563439999290, 7.658899961832999814 ) ) ;
#47678=CARTESIAN_POINT ( 'NONE',  ( 1.799490220168999954, -19.22870851082999977, -12.64502302238000020 ) ) ;
#47681=CARTESIAN_POINT ( 'NONE',  ( -1.750000000000000000, -60.04999999657000131, 12.50000000000000000 ) ) ;
#47684=CARTESIAN_POINT ( 'NONE',  ( -2.588619782347023168, -1.309278100603108008, -2.388616040639797156 ) ) ;
#47686=CARTESIAN_POINT ( 'NONE',  ( -3.271260265871036577, -3.500000000000000000, -0.5209705415795669037 ) ) ;
#47693=CARTESIAN_POINT ( 'NONE',  ( 3.250000000000000000, -3.250000000000000000, 0.000000000000000000 ) ) ;
#47694=DIRECTION ( 'NONE',  ( 0.000000000000000000, -1.000000000000000000, 0.000000000000000000 ) ) ;
#47697=CARTESIAN_POINT ( 'NONE',  ( 9.278274563759739024, -76.39710617612774968, -7.210752084677405804 ) ) ;
#47700=LINE ( 'NONE', #48550, #16094 ) ;
#47703=CARTESIAN_POINT ( 'NONE',  ( 0.8506806241676642122, -2.645833333333333037, -3.165411199172024848 ) ) ;
#47705=ADVANCED_FACE ( 'NONE', ( #33970 ), #13477, .F. ) ;
#47711=VERTEX_POINT ( 'NONE', #47595 ) ;
#47712=DIRECTION ( 'NONE',  ( -2.678926851037000120E-11, -1.000000000000000000, -2.678911359553000079E-11 ) ) ;
#47713=VERTEX_POINT ( 'NONE', #56719 ) ;
#47714=EDGE_LOOP ( 'NONE', ( #45818, #51967, #7246, #28068, #56451 ) ) ;
#47716=ORIENTED_EDGE ( 'NONE', *, *, #13188, .T. ) ;
#47719=ORIENTED_EDGE ( 'NONE', *, *, #11880, .F. ) ;
#47720=LINE ( 'NONE', #38543, #8242 ) ;
#47722=B_SPLINE_CURVE_WITH_KNOTS ( 'NONE', 3,
 ( #13800, #10264, #54560, #566, #55128, #50137 ),
 .UNSPECIFIED., .F., .F.,
 ( 4, 1, 1, 4 ),
 ( 0.000000000000000000, 0.3333333333333000081, 0.6666666666667000474, 1.000000000000000000 ),
 .UNSPECIFIED. ) ;
#47727=AXIS2_PLACEMENT_3D ( 'NONE', #54982, #8949, #19267 ) ;
#47732=AXIS2_PLACEMENT_3D ( 'NONE', #53190, #18058, #4180 ) ;
#47733=CARTESIAN_POINT ( 'NONE',  ( 0.000000000000000000, -80.70000000000000284, 0.000000000000000000 ) ) ;
#47740=CARTESIAN_POINT ( 'NONE',  ( 1.239372798835131739, -2.944998029927256677, 3.003655695478087750 ) ) ;
#47744=CARTESIAN_POINT ( 'NONE',  ( 8.096452064242996016, -59.58578169018998949, 13.15643568217000769 ) ) ;
#47746=CARTESIAN_POINT ( 'NONE',  ( -11.74507272963526638, -76.20387938085427493, -0.6100094135503494330 ) ) ;
#47752=CARTESIAN_POINT ( 'NONE',  ( 12.83677138648000060, -23.22737696056999823, 2.062839765281999860 ) ) ;
#47753=CARTESIAN_POINT ( 'NONE',  ( 10.10912517723447124, -23.47586858184537206, 7.634643689412686562 ) ) ;
#47754=LINE ( 'NONE', #7289, #20696 ) ;
#47755=CARTESIAN_POINT ( 'NONE',  ( 11.43133530979999968, -76.89853223350999656, -2.936322344009000052 ) ) ;
#47756=ORIENTED_EDGE ( 'NONE', *, *, #1100, .T. ) ;
#47759=B_SPLINE_CURVE_WITH_KNOTS ( 'NONE', 3,
 ( #48825, #8367, #31371, #44686, #49415, #26650, #8963, #4536, #50004, #9257, #26366, #27242, #45281, #22538, #53538, #40548, #44384, #18119 ),
 .UNSPECIFIED., .F., .F.,
 ( 4, 2, 2, 2, 2, 2, 2, 2, 4 ),
 ( 0.000000000000000000, 0.1250000000000000000, 0.2500000000000000000, 0.3750000000000000000, 0.5000000000000000000, 0.6250000000000000000, 0.7500000000000000000, 0.8750000000000000000, 1.000000000000000000 ),
 .UNSPECIFIED. ) ;
#47760=CARTESIAN_POINT ( 'NONE',  ( 12.43652404748999984, -61.72065244505999715, 0.1284256373645000227 ) ) ;
#47761=CARTESIAN_POINT ( 'NONE',  ( 4.693157761522999571, -78.73635037319999697, -11.90123672215999839 ) ) ;
#47768=AXIS2_PLACEMENT_3D ( 'NONE', #281, #27673, #54273 ) ;
#47769=EDGE_CURVE ( 'NONE', #16112, #35060, #41913, .T. ) ;
#47774=ORIENTED_EDGE ( 'NONE', *, *, #2056, .F. ) ;
#47775=EDGE_CURVE ( 'NONE', #45976, #8616, #41609, .T. ) ;
#47777=CARTESIAN_POINT ( 'NONE',  ( 12.92181194098999875, -57.04351820043999766, 2.062502994258999856 ) ) ;
#47779=CIRCLE ( 'NONE', #57188, 14.00000000000000000 ) ;
#47780=VERTEX_POINT ( 'NONE', #28303 ) ;
#47784=CARTESIAN_POINT ( 'NONE',  ( -11.28006698294270471, -78.17317328678146282, 3.842900084313429776 ) ) ;
#47786=ORIENTED_EDGE ( 'NONE', *, *, #30318, .T. ) ;
#47787=CARTESIAN_POINT ( 'NONE',  ( 12.66313295592999921, -53.62196533848999991, -0.06049275240488000138 ) ) ;
#47790=CARTESIAN_POINT ( 'NONE',  ( 12.21456857099000004, -78.79287284168630379, -1.096995930408000142 ) ) ;
#47792=CARTESIAN_POINT ( 'NONE',  ( 9.934825859729000896, -54.17633188858999915, 7.968960864672001598 ) ) ;
#47800=CARTESIAN_POINT ( 'NONE',  ( -7.646966600018000548, -23.19642081717000082, 10.19019745247000053 ) ) ;
#47805=CARTESIAN_POINT ( 'NONE',  ( 9.835223439052001027, -60.88138927622999574, -7.760980897183999971 ) ) ;
#47806=CARTESIAN_POINT ( 'NONE',  ( 10.16243366810999937, -79.18539039009999669, -6.864696462387000153 ) ) ;
#47810=DIRECTION ( 'NONE',  ( 1.000000000000000000, 0.000000000000000000, 0.000000000000000000 ) ) ;
#47814=CARTESIAN_POINT ( 'NONE',  ( 12.83675988122999989, -60.02754371127999633, -2.062832873794000044 ) ) ;
#47816=VECTOR ( 'NONE', #53640, 1000.000000000000000 ) ;
#47818=CARTESIAN_POINT ( 'NONE',  ( -3.201679521582999843, -1.948833096892000016, 0.8095118808495000984 ) ) ;
#47821=EDGE_CURVE ( 'NONE', #15231, #57621, #35124, .T. ) ;
#47822=CARTESIAN_POINT ( 'NONE',  ( 3.708203932500000022, -75.80000000000001137, 11.41267819554000162 ) ) ;
#47825=CARTESIAN_POINT ( 'NONE',  ( 8.485281374238999419, -55.64999999967000122, -8.485281374238999419 ) ) ;
#47827=CARTESIAN_POINT ( 'NONE',  ( -10.24996238031000040, -20.24828923609000242, -7.705119999441000012 ) ) ;
#47831=CARTESIAN_POINT ( 'NONE',  ( -7.618394338655000375, -60.02713821237000502, 10.53494418060999926 ) ) ;
#47834=CYLINDRICAL_SURFACE ( 'NONE', #9785, 12.80000000000000071 ) ;
#47837=FACE_OUTER_BOUND ( 'NONE', #40292, .T. ) ;
#47841=CARTESIAN_POINT ( 'NONE',  ( 0.000000000000000000, -23.75000000000000000, -11.79999999999999893 ) ) ;
#47843=ORIENTED_EDGE ( 'NONE', *, *, #29990, .F. ) ;
#47847=CIRCLE ( 'NONE', #5388, 10.20000000000000107 ) ;
#47848=CARTESIAN_POINT ( 'NONE',  ( -12.71658889743999943, -60.11584477251999203, 1.931087888049999979 ) ) ;
#47851=VERTEX_POINT ( 'NONE', #25624 ) ;
#47852=AXIS2_PLACEMENT_3D ( 'NONE', #18140, #40863, #26387 ) ;
#47853=ORIENTED_EDGE ( 'NONE', *, *, #36765, .F. ) ;
#47856=EDGE_LOOP ( 'NONE', ( #44168, #736, #32345 ) ) ;
#47857=CARTESIAN_POINT ( 'NONE',  ( 8.292781013307999771, -16.94469293076999961, 9.770415148734000965 ) ) ;
#47859=AXIS2_PLACEMENT_3D ( 'NONE', #9782, #31312, #17464 ) ;
#47860=CARTESIAN_POINT ( 'NONE',  ( 1.003693376005942550, -53.83776007856020840, 12.70247752660074347 ) ) ;
#47861=CARTESIAN_POINT ( 'NONE',  ( 9.024219425886000678, -76.86072037624001041, -8.086445476350000661 ) ) ;
#47862=DIRECTION ( 'NONE',  ( 0.9999999999999998890, -1.433670265775999799E-08, 0.000000000000000000 ) ) ;
#47863=FACE_BOUND ( 'NONE', #50256, .T. ) ;
#47864=DIRECTION ( 'NONE',  ( 0.000000000000000000, 1.000000000000000000, 0.000000000000000000 ) ) ;
#47867=VERTEX_POINT ( 'NONE', #10914 ) ;
#47868=CARTESIAN_POINT ( 'NONE',  ( -11.75000000000000000, -76.20000000000000284, -1.391479524197000231E-14 ) ) ;
#47881=CARTESIAN_POINT ( 'NONE',  ( -7.626500777237000150, -18.68415268018999953, 10.35747145892000098 ) ) ;
#47883=CARTESIAN_POINT ( 'NONE',  ( -9.837756816580965236, -24.31467795600408266, -7.850057934563161588 ) ) ;
#47885=SURFACE_SIDE_STYLE ('',( #42861 ) ) ;
#47886=DIRECTION ( 'NONE',  ( 0.000000000000000000, -0.7071067811866525998, -0.7071067811864425456 ) ) ;
#47887=ORIENTED_EDGE ( 'NONE', *, *, #40304, .F. ) ;
#47890=DIRECTION ( 'NONE',  ( -1.000000000000000000, 0.000000000000000000, -1.158063445485999906E-14 ) ) ;
#47892=CARTESIAN_POINT ( 'NONE',  ( -12.71162569433759515, -17.76025712765776987, 1.720540999454742481 ) ) ;
#47894=CARTESIAN_POINT ( 'NONE',  ( 2.125686459585773846, -1.925872778455320455, -2.860343808299961488 ) ) ;
#47902=CARTESIAN_POINT ( 'NONE',  ( 7.601397897754999633, -60.04999999966999980, -9.369164850722000892 ) ) ;
#47903=VERTEX_POINT ( 'NONE', #30038 ) ;
#47905=CARTESIAN_POINT ( 'NONE',  ( 5.918638737202504885, -77.03089283734779258, 10.27313499612968251 ) ) ;
#47914=CARTESIAN_POINT ( 'NONE',  ( 11.21770439229572247, -78.47291413386186321, 3.494388818491212856 ) ) ;
#47915=DIRECTION ( 'NONE',  ( 0.000000000000000000, 1.000000000000000000, 0.000000000000000000 ) ) ;
#47922=CARTESIAN_POINT ( 'NONE',  ( -12.49168433582000226, -60.09849137195000424, -1.667916687244999974 ) ) ;
#47923=CARTESIAN_POINT ( 'NONE',  ( 11.74999999999999289, -77.56041666666666856, 1.538071403320028452 ) ) ;
#47924=CARTESIAN_POINT ( 'NONE',  ( 12.50000000000000000, -23.25000000000000000, -1.250000000000000000 ) ) ;
#47929=DIRECTION ( 'NONE',  ( 0.000000000000000000, 1.000000000000000000, 0.000000000000000000 ) ) ;
#47932=CARTESIAN_POINT ( 'NONE',  ( -12.83675988120999989, -23.22754371161000009, 2.062832873794000044 ) ) ;
#47935=CARTESIAN_POINT ( 'NONE',  ( -12.66001647282000064, -54.16746073337000666, -1.381678996660000047 ) ) ;
#47936=VERTEX_POINT ( 'NONE', #22779 ) ;
#47937=VERTEX_POINT ( 'NONE', #38032 ) ;
#47940=CIRCLE ( 'NONE', #46080, 12.57042253521000141 ) ;
#47941=FACE_BOUND ( 'NONE', #56548, .T. ) ;
#47942=VECTOR ( 'NONE', #18157, 999.9999999999998863 ) ;
#47945=ORIENTED_EDGE ( 'NONE', *, *, #18621, .T. ) ;
#47946=ORIENTED_EDGE ( 'NONE', *, *, #1100, .F. ) ;
#47950=CARTESIAN_POINT ( 'NONE',  ( -12.66008999775999833, -61.42705329315000284, -1.387101471715999956 ) ) ;
#47953=AXIS2_PLACEMENT_3D ( 'NONE', #43153, #29258, #20706 ) ;
#47954=LINE ( 'NONE', #7485, #15303 ) ;
#47955=CARTESIAN_POINT ( 'NONE',  ( -10.18491080493000212, -18.69283319134000010, 7.640030264154999529 ) ) ;
#47961=CARTESIAN_POINT ( 'NONE',  ( -10.36292447790000004, -18.79904187578000219, -7.633480004415999609 ) ) ;
#47962=CARTESIAN_POINT ( 'NONE',  ( -2.062323307449999810, -18.77286846807999865, -12.83634826442999888 ) ) ;
#47963=CARTESIAN_POINT ( 'NONE',  ( 12.00000000000000000, -23.25000000000000000, -1.250000000000000000 ) ) ;
#47966=CARTESIAN_POINT ( 'NONE',  ( 12.50000000000000000, -24.68359816828999698, 1.003641515614000168 ) ) ;
#47967=CARTESIAN_POINT ( 'NONE',  ( 12.50000000000000000, -18.75000000240999753, 1.750000000000000000 ) ) ;
#47968=VERTEX_POINT ( 'NONE', #51050 ) ;
#47970=CARTESIAN_POINT ( 'NONE',  ( -12.54238283049878788, -60.32853599783591392, 1.749799162368518513 ) ) ;
#47972=CARTESIAN_POINT ( 'NONE',  ( -2.445119831658000287, -3.656279784236000197, 2.430454651384000186 ) ) ;
#47973=CARTESIAN_POINT ( 'NONE',  ( -12.61277494327999982, -55.60332099621999902, 1.798398135845999946 ) ) ;
#47976=VECTOR ( 'NONE', #17134, 999.9999999999998863 ) ;
#47978=EDGE_CURVE ( 'NONE', #14764, #45494, #15355, .T. ) ;
#47979=CARTESIAN_POINT ( 'NONE',  ( -14.00000000000000000, -5.899999999999999467, 0.000000000000000000 ) ) ;
#47983=CARTESIAN_POINT ( 'NONE',  ( 7.575616321950742638, -76.38051645574682880, -8.984648930537860068 ) ) ;
#47985=B_SPLINE_CURVE_WITH_KNOTS ( 'NONE', 3,
 ( #56521, #16080, #34061, #52099, #11656, #30786, #26074, #4232, #8658, #57958, #17512, #21933, #35503, #26644, #136, #53832, #53239, #13367 ),
 .UNSPECIFIED., .F., .F.,
 ( 4, 2, 2, 2, 2, 2, 2, 2, 4 ),
 ( 0.000000000000000000, 0.1250000000000000000, 0.2500000000000000000, 0.3750000000000000000, 0.5000000000000000000, 0.6250000000000000000, 0.7500000000000000000, 0.8750000000000000000, 1.000000000000000000 ),
 .UNSPECIFIED. ) ;
#47987=DIRECTION ( 'NONE',  ( -0.7071067811705844530, 1.925104039395958879E-07, -0.7071067812024844912 ) ) ;
#47992=DIRECTION ( 'NONE',  ( 0.000000000000000000, 0.000000000000000000, 1.000000000000000000 ) ) ;
#47993=CARTESIAN_POINT ( 'NONE',  ( -8.620934061270462578, -16.83470696675769673, -9.346030177896617275 ) ) ;
#47996=DIRECTION ( 'NONE',  ( 1.000000000000000000, 0.000000000000000000, 0.000000000000000000 ) ) ;
#48001=CARTESIAN_POINT ( 'NONE',  ( 1.980584515756000030, -23.26485150094000076, 12.76303204340999997 ) ) ;
#48002=ORIENTED_EDGE ( 'NONE', *, *, #33347, .F. ) ;
#48005=ORIENTED_EDGE ( 'NONE', *, *, #2953, .F. ) ;
#48012=VERTEX_POINT ( 'NONE', #16471 ) ;
#48014=CARTESIAN_POINT ( 'NONE',  ( 0.000000000000000000, -23.94999999999946994, 12.00000000000000000 ) ) ;
#48016=EDGE_CURVE ( 'NONE', #53695, #21736, #41778, .T. ) ;
#48019=AXIS2_PLACEMENT_3D ( 'NONE', #25419, #26555, #44585 ) ;
#48022=CARTESIAN_POINT ( 'NONE',  ( 11.91901974179999968, -77.28985072955998703, 5.468333046474000980 ) ) ;
#48030=CARTESIAN_POINT ( 'NONE',  ( -0.08333306579402115222, -2.977413547009986949, 3.248820096312940997 ) ) ;
#48034=CIRCLE ( 'NONE', #9329, 11.75000000000000178 ) ;
#48035=CARTESIAN_POINT ( 'NONE',  ( 0.6454797251240073086, -24.88806512139955984, -12.50471521368228167 ) ) ;
#48037=CARTESIAN_POINT ( 'NONE',  ( 3.542727183245000244, -3.002891436244000456, -1.391102635753999950 ) ) ;
#48038=CARTESIAN_POINT ( 'NONE',  ( 10.18491068059999805, -18.69283065396999888, 7.640030139758000161 ) ) ;
#48039=CARTESIAN_POINT ( 'NONE',  ( -9.636781270596999960, -61.24031362749000351, -7.948066289865000300 ) ) ;
#48043=CARTESIAN_POINT ( 'NONE',  ( 7.287838312904000304, -78.22430371036000452, -10.78085041437000058 ) ) ;
#48045=CARTESIAN_POINT ( 'NONE',  ( 0.6484536763440467144, -25.12402982711201105, -12.70397497891696226 ) ) ;
#48046=CARTESIAN_POINT ( 'NONE',  ( -6.449220533167999925, -76.07628699674000927, -10.72226218736000014 ) ) ;
#48048=EDGE_CURVE ( 'NONE', #50691, #38883, #41803, .T. ) ;
#48049=FACE_OUTER_BOUND ( 'NONE', #30171, .T. ) ;
#48051=PRODUCT_DEFINITION_FORMATION_WITH_SPECIFIED_SOURCE ( 'ANY', '', #56856, .NOT_KNOWN. ) ;
#48052=EDGE_CURVE ( 'NONE', #36787, #326, #25581, .T. ) ;
#48053=CARTESIAN_POINT ( 'NONE',  ( 12.57434559700999976, -60.51110719467000365, 1.760800161976000089 ) ) ;
#48054=CARTESIAN_POINT ( 'NONE',  ( -12.65371606323000009, -79.09322042626999405, -1.883862808345000195 ) ) ;
#48055=CARTESIAN_POINT ( 'NONE',  ( 12.77301916222999800, -53.74808379519999590, -1.052060437763999934 ) ) ;
#48065=ORIENTED_EDGE ( 'NONE', *, *, #18574, .F. ) ;
#48067=CARTESIAN_POINT ( 'NONE',  ( 12.75763395696999858, -56.02204592290999585, 1.931043742978000077 ) ) ;
#48070=ORIENTED_EDGE ( 'NONE', *, *, #52887, .F. ) ;
#48073=ORIENTED_EDGE ( 'NONE', *, *, #12623, .T. ) ;
#48074=CIRCLE ( 'NONE', #51823, 10.40000000000000036 ) ;
#48076=CARTESIAN_POINT ( 'NONE',  ( 1.749722766153996911, -60.27588992799950063, 12.54673760685730954 ) ) ;
#48078=ORIENTED_EDGE ( 'NONE', *, *, #27149, .F. ) ;
#48079=ORIENTED_EDGE ( 'NONE', *, *, #19969, .T. ) ;
#48080=CARTESIAN_POINT ( 'NONE',  ( -7.766269599678000013, -78.62042853322630265, -9.491266709826003733 ) ) ;
#48082=CARTESIAN_POINT ( 'NONE',  ( 10.47840693000000023, -55.01310507149000273, 7.622759963108999948 ) ) ;
#48083=FACE_OUTER_BOUND ( 'NONE', #5269, .T. ) ;
#48085=CARTESIAN_POINT ( 'NONE',  ( 9.392127196910033504, -77.39524328896870031, -7.218255399355257396 ) ) ;
#48086=DIRECTION ( 'NONE',  ( -1.000000000000000000, 0.000000000000000000, 0.000000000000000000 ) ) ;
#48089=CARTESIAN_POINT ( 'NONE',  ( -9.844172144369998989, -75.89675078460000179, 7.391061701651999272 ) ) ;
#48093=CARTESIAN_POINT ( 'NONE',  ( -12.54987159816999842, -16.94886760191999997, 0.1385534523823999942 ) ) ;
#48094=CARTESIAN_POINT ( 'NONE',  ( -7.766269599678000013, -78.51842792576000818, -9.491266709826000181 ) ) ;
#48096=CARTESIAN_POINT ( 'NONE',  ( -7.342331066867000544, -59.94999999967000548, -8.190859204290999784 ) ) ;
#48097=DIRECTION ( 'NONE',  ( 0.000000000000000000, -1.000000000000000000, 0.000000000000000000 ) ) ;
#48102=CARTESIAN_POINT ( 'NONE',  ( -3.161480484322999995, -3.525554798046000027, 1.254767625763999916 ) ) ;
#48106=CARTESIAN_POINT ( 'NONE',  ( -11.77140462957510714, -75.79999999999998295, 1.896298482247357198 ) ) ;
#48117=CARTESIAN_POINT ( 'NONE',  ( -3.055517426832999650, -0.5241180847798000420, 0.7952000566461999709 ) ) ;
#48119=DIRECTION ( 'NONE',  ( 0.9957542233430587419, 0.04890176636653797981, 0.07798810127637677281 ) ) ;
#48121=ORIENTED_EDGE ( 'NONE', *, *, #3071, .F. ) ;
#48124=CARTESIAN_POINT ( 'NONE',  ( 9.019414222045478269, -24.99291943955440942, -8.666941068747364696 ) ) ;
#48125=CARTESIAN_POINT ( 'NONE',  ( -10.42272502865000128, -57.04546192861999998, -7.691893942748999180 ) ) ;
#48127=ADVANCED_FACE ( 'NONE', ( #12324 ), #30311, .F. ) ;
#48128=ORIENTED_EDGE ( 'NONE', *, *, #2194, .T. ) ;
#48129=AXIS2_PLACEMENT_3D ( 'NONE', #44714, #8691, #4268 ) ;
#48132=CARTESIAN_POINT ( 'NONE',  ( 1.931043762602999925, -59.57819125629999490, -12.75761570869000039 ) ) ;
#48134=CARTESIAN_POINT ( 'NONE',  ( -12.64500484464000074, -56.02847221959000024, 1.799490225533999732 ) ) ;
#48137=ORIENTED_EDGE ( 'NONE', *, *, #51329, .F. ) ;
#48138=ORIENTED_EDGE ( 'NONE', *, *, #45154, .F. ) ;
#48143=CARTESIAN_POINT ( 'NONE',  ( 10.36222501930000028, -18.77880030165999869, 7.631889976314999657 ) ) ;
#48146=EDGE_CURVE ( 'NONE', #44548, #32213, #53999, .T. ) ;
#48147=CARTESIAN_POINT ( 'NONE',  ( 1.501534314742096310, -54.24847048308878072, 12.70455943736382132 ) ) ;
#48148=CARTESIAN_POINT ( 'NONE',  ( -12.76493461869000079, -78.17433021234000989, -0.9303755367166000045 ) ) ;
#48149=DIRECTION ( 'NONE',  ( 0.000000000000000000, -1.000000000000000000, 0.000000000000000000 ) ) ;
#48155=CARTESIAN_POINT ( 'NONE',  ( 1.129552310421328976, -78.16734973423666588, 11.73990984186074016 ) ) ;
#48160=CARTESIAN_POINT ( 'NONE',  ( 7.342331066867000544, -55.64999999967000122, -8.190859204290999784 ) ) ;
#48163=CARTESIAN_POINT ( 'NONE',  ( -0.5999999998848000171, -18.85000000520999919, 11.79999999988000070 ) ) ;
#48166=DIRECTION ( 'NONE',  ( 0.000000000000000000, -1.000000000000000000, 0.000000000000000000 ) ) ;
#48167=DIRECTION ( 'NONE',  ( 0.000000000000000000, -1.000000000000000000, 0.000000000000000000 ) ) ;
#48168=EDGE_CURVE ( 'NONE', #57192, #12818, #53054, .T. ) ;
#48170=DIRECTION ( 'NONE',  ( -0.4045849535019032661, -0.8201353734596047440, 0.4045849535019032661 ) ) ;
#48171=CARTESIAN_POINT ( 'NONE',  ( 8.485281374238999419, -55.54999999966999980, 8.485281374238999419 ) ) ;
#48181=CARTESIAN_POINT ( 'NONE',  ( -3.256586129738097135, -1.781125447738561851, -1.344250386147469500 ) ) ;
#48185=CARTESIAN_POINT ( 'NONE',  ( 8.485281374238999419, -55.54999999966999980, 8.485281374238999419 ) ) ;
#48186=CARTESIAN_POINT ( 'NONE',  ( 9.850786281789762455, -75.99584267488174305, 6.405190026801080627 ) ) ;
#48188=ORIENTED_EDGE ( 'NONE', *, *, #36608, .F. ) ;
#48189=DIRECTION ( 'NONE',  ( -1.000000000000000000, 0.000000000000000000, 0.000000000000000000 ) ) ;
#48191=CARTESIAN_POINT ( 'NONE',  ( 9.537121434155222843, -78.89952835878608539, -6.926593624396411464 ) ) ;
#48194=VECTOR ( 'NONE', #26884, 1000.000000000000000 ) ;
#48196=CARTESIAN_POINT ( 'NONE',  ( 10.36292431357999888, -23.20096201633999655, -7.633479737313000335 ) ) ;
#48199=CARTESIAN_POINT ( 'NONE',  ( 5.943163592195922718, -78.53230635707669194, 10.13577355096580668 ) ) ;
#48200=CARTESIAN_POINT ( 'NONE',  ( -10.25201842922365358, -60.92180395180005092, 7.730408553586130438 ) ) ;
#48202=VECTOR ( 'NONE', #13187, 1000.000000000000114 ) ;
#48208=CARTESIAN_POINT ( 'NONE',  ( 8.909545442949999838, -57.79999999967000690, 7.919595949288999570 ) ) ;
#48209=DIRECTION ( 'NONE',  ( -0.7071067811865474617, 0.000000000000000000, 0.7071067811865474617 ) ) ;
#48212=B_SPLINE_CURVE_WITH_KNOTS ( 'NONE', 3,
 ( #43574, #8713, #11993, #26704, #34976, #52721, #53006, #57144, #56860, #44735, #8133, #26134, #3137, #7556, #12557, #43870, #7841, #39428 ),
 .UNSPECIFIED., .F., .F.,
 ( 4, 2, 2, 2, 2, 2, 2, 2, 4 ),
 ( 0.000000000000000000, 0.1250000000000000833, 0.2500000000000001110, 0.3750000000000001110, 0.5000000000000001110, 0.6250000000000001110, 0.7500000000000000000, 0.8750000000000000000, 1.000000000000000000 ),
 .UNSPECIFIED. ) ;
#48213=DIRECTION ( 'NONE',  ( 0.6489586447433830507, 0.04890182323489870864, -0.7592504784964801967 ) ) ;
#48214=CARTESIAN_POINT ( 'NONE',  ( 1.667916687244999974, -18.70150862776000267, 12.49168433580000048 ) ) ;
#48216=CARTESIAN_POINT ( 'NONE',  ( -12.46083365854999769, -23.68341615479999973, 1.628972628240999976 ) ) ;
#48217=ORIENTED_EDGE ( 'NONE', *, *, #43394, .T. ) ;
#48219=CIRCLE ( 'NONE', #22735, 12.50000000000000000 ) ;
#48220=CARTESIAN_POINT ( 'NONE',  ( -7.648026766735999793, -23.25000000582000226, 10.12290050089000104 ) ) ;
#48221=ORIENTED_EDGE ( 'NONE', *, *, #27046, .F. ) ;
#48230=ORIENTED_EDGE ( 'NONE', *, *, #36282, .T. ) ;
#48233=CARTESIAN_POINT ( 'NONE',  ( -12.54715528154999937, -61.33180535358000185, -1.292252957172000061 ) ) ;
#48235=FACE_OUTER_BOUND ( 'NONE', #34427, .T. ) ;
#48237=CARTESIAN_POINT ( 'NONE',  ( 7.770365053994759741, -54.56417299442668423, -10.20675369723379156 ) ) ;
#48240=CARTESIAN_POINT ( 'NONE',  ( 12.61277494329999982, -18.80332099654000189, -1.798398135845000079 ) ) ;
#48241=CARTESIAN_POINT ( 'NONE',  ( -1.750000000000000000, -55.54999999966999980, 12.00000000000000000 ) ) ;
#48242=CARTESIAN_POINT ( 'NONE',  ( -10.71456977360709928, -76.66589582642508560, 4.824031268171789399 ) ) ;
#48244=CARTESIAN_POINT ( 'NONE',  ( -7.660411364605000273, -55.60826384781999820, 10.01752038681999935 ) ) ;
#48246=CARTESIAN_POINT ( 'NONE',  ( -9.523369619462000557, -17.18054357685999989, -8.220347091616000412 ) ) ;
#48249=CARTESIAN_POINT ( 'NONE',  ( 2.841157093317593141, -1.309822438106574616, -1.639539360290898307 ) ) ;
#48250=EDGE_CURVE ( 'NONE', #22264, #23504, #54232, .T. ) ;
#48254=EDGE_LOOP ( 'NONE', ( #25025, #34025, #9234 ) ) ;
#48260=CARTESIAN_POINT ( 'NONE',  ( -3.784563998892999770, -3.226994571379000032, -0.4035839726128000460 ) ) ;
#48263=CARTESIAN_POINT ( 'NONE',  ( -12.43647099676999979, -53.88193128055999637, -0.03491583288326999962 ) ) ;
#48265=CARTESIAN_POINT ( 'NONE',  ( -2.598938867667634156, -2.049404340733311347, 1.996446441638521030 ) ) ;
#48270=CARTESIAN_POINT ( 'NONE',  ( 10.83581499240337997, -76.41815442928682955, -4.543561087761390560 ) ) ;
#48273=CARTESIAN_POINT ( 'NONE',  ( -3.251154051729839178, -1.100857096137070279, 2.995606203745920413E-05 ) ) ;
#48283=CARTESIAN_POINT ( 'NONE',  ( -10.99999999999999467, -23.74999999999998934, -0.1603812274926581793 ) ) ;
#48285=CARTESIAN_POINT ( 'NONE',  ( -1.931736162947090385, -23.76670395714575790, 12.72978979890153362 ) ) ;
#48286=ORIENTED_EDGE ( 'NONE', *, *, #31298, .F. ) ;
#48287=EDGE_LOOP ( 'NONE', ( #33864, #34221, #7037, #47144 ) ) ;
#48288=PLANE ( 'NONE',  #39525 ) ;
#48289=EDGE_LOOP ( 'NONE', ( #48230, #55765, #44062, #24737 ) ) ;
#48292=VERTEX_POINT ( 'NONE', #45385 ) ;
#48293=CARTESIAN_POINT ( 'NONE',  ( -12.19527860736999969, -78.51856776420000017, -2.001746843535999965 ) ) ;
#48295=ORIENTED_EDGE ( 'NONE', *, *, #23059, .T. ) ;
#48296=DIRECTION ( 'NONE',  ( -1.000000000000000000, 0.000000000000000000, 0.000000000000000000 ) ) ;
#48297=LINE ( 'NONE', #22791, #39688 ) ;
#48299=LINE ( 'NONE', #43867, #44708 ) ;
#48302=CARTESIAN_POINT ( 'NONE',  ( -1.273906987915999878, -77.62287857533000590, -13.05154622979999957 ) ) ;
#48303=EDGE_CURVE ( 'NONE', #28385, #22487, #40944, .T. ) ;
#48307=CARTESIAN_POINT ( 'NONE',  ( -10.18496935385000057, -21.75064714707999869, 7.710095619702999947 ) ) ;
#48309=AXIS2_PLACEMENT_3D ( 'NONE', #8711, #32006, #50048 ) ;
#48311=CARTESIAN_POINT ( 'NONE',  ( 2.286833087265501163, -2.913422680531678743, 2.308828009290456951 ) ) ;
#48313=CARTESIAN_POINT ( 'NONE',  ( -13.99609303101000002, -32.95862266598000190, -3.303296643088999776E-05 ) ) ;
#48315=CARTESIAN_POINT ( 'NONE',  ( -0.4587696627765999735, -3.398051649099999683, -3.778272981138000031 ) ) ;
#48318=CONICAL_SURFACE ( 'NONE', #253, 10.29999999923999887, 0.7853981633972997312 ) ;
#48322=CARTESIAN_POINT ( 'NONE',  ( -12.65989785480000229, -17.05665906540999899, -0.9744897697751000454 ) ) ;
#48323=CARTESIAN_POINT ( 'NONE',  ( 12.49837680049000177, -23.20957148803000081, 1.667051419334999895 ) ) ;
#48325=CARTESIAN_POINT ( 'NONE',  ( 1.423904377506817864, -24.30512805201019688, -12.50677628656594642 ) ) ;
#48326=CARTESIAN_POINT ( 'NONE',  ( -8.784096368091999452, -76.01934928261999858, 8.698479859056998720 ) ) ;
#48327=ORIENTED_EDGE ( 'NONE', *, *, #24901, .F. ) ;
#48328=AXIS2_PLACEMENT_3D ( 'NONE', #20797, #16376, #3658 ) ;
#48342=ORIENTED_EDGE ( 'NONE', *, *, #39959, .T. ) ;
#48346=VERTEX_POINT ( 'NONE', #30699 ) ;
#48348=CIRCLE ( 'NONE', #3992, 13.86363636363999952 ) ;
#48349=ORIENTED_EDGE ( 'NONE', *, *, #8799, .T. ) ;
#48350=VERTEX_POINT ( 'NONE', #15185 ) ;
#48351=LINE ( 'NONE', #31404, #6627 ) ;
#48353=CARTESIAN_POINT ( 'NONE',  ( -3.862145970064539746, -0.8702854025945180316, -1.118418364751955218 ) ) ;
#48354=ORIENTED_EDGE ( 'NONE', *, *, #1245, .F. ) ;
#48357=CARTESIAN_POINT ( 'NONE',  ( -9.042566447131001439, -79.10902074051685418, -8.284387575507999202 ) ) ;
#48360=CARTESIAN_POINT ( 'NONE',  ( 7.974020021219000220, -54.16898233660000272, 9.929669236765001017 ) ) ;
#48362=DIRECTION ( 'NONE',  ( 0.000000000000000000, 0.000000000000000000, -1.000000000000000000 ) ) ;
#48363=CIRCLE ( 'NONE', #9715, 5.000000000000000000 ) ;
#48364=EDGE_CURVE ( 'NONE', #47937, #54593, #31201, .T. ) ;
#48365=CARTESIAN_POINT ( 'NONE',  ( -1.626826133776999786E-14, -74.80000000000001137, 0.000000000000000000 ) ) ;
#48369=CARTESIAN_POINT ( 'NONE',  ( 12.21199139566000014, -76.20804719422000062, 1.550091862394999964 ) ) ;
#48377=CARTESIAN_POINT ( 'NONE',  ( -12.90000000000000036, 0.000000000000000000, 0.000000000000000000 ) ) ;
#48382=CIRCLE ( 'NONE', #19138, 12.69999999999999929 ) ;
#48383=DIRECTION ( 'NONE',  ( -0.6562721000522208081, -0.7545243075561237633, -7.874467463877248089E-10 ) ) ;
#48384=CARTESIAN_POINT ( 'NONE',  ( -1.204158649194000175, -3.066063735461000306, -3.347755931201000124 ) ) ;
#48386=DIRECTION ( 'NONE',  ( 0.000000000000000000, -1.000000000000000000, 0.000000000000000000 ) ) ;
#48387=CARTESIAN_POINT ( 'NONE',  ( -4.131565180156527184, -75.80000000000001137, 11.24552900431304892 ) ) ;
#48391=ORIENTED_EDGE ( 'NONE', *, *, #5281, .F. ) ;
#48392=CARTESIAN_POINT ( 'NONE',  ( 0.000000000000000000, -39.30476017083000073, 0.000000000000000000 ) ) ;
#48393=CIRCLE ( 'NONE', #54078, 13.86363636363999952 ) ;
#48397=CARTESIAN_POINT ( 'NONE',  ( -12.80088938724999892, -59.56256651724000051, -1.980532758767000301 ) ) ;
#48398=CARTESIAN_POINT ( 'NONE',  ( -3.274849198131999817, -0.5460671121268000361, -0.04757157529786999739 ) ) ;
#48400=CARTESIAN_POINT ( 'NONE',  ( 12.54705830248999909, -24.53699017355999956, -1.287129557046000183 ) ) ;
#48401=CARTESIAN_POINT ( 'NONE',  ( -12.71107039379021586, -54.54871969218453387, -1.717622521768342292 ) ) ;
#48402=EDGE_LOOP ( 'NONE', ( #30466, #51032, #21896, #45089, #53129 ) ) ;
#48406=CARTESIAN_POINT ( 'NONE',  ( -1.750000000000000000, -23.25000000000000000, -12.00000000000000000 ) ) ;
#48410=VERTEX_POINT ( 'NONE', #45479 ) ;
#48412=CARTESIAN_POINT ( 'NONE',  ( 1.535712162480687759, -77.83339044027641762, -11.74751977916936418 ) ) ;
#48413=CARTESIAN_POINT ( 'NONE',  ( -9.050966799188000067, -59.94999999969999749, 7.919595949288999570 ) ) ;
#48415=CARTESIAN_POINT ( 'NONE',  ( -12.71798280857999863, -60.09778595451999905, 1.931086388455000025 ) ) ;
#48416=CARTESIAN_POINT ( 'NONE',  ( -8.596775676211999340, -53.66467110130999885, -9.310147894663000301 ) ) ;
#48419=VERTEX_POINT ( 'NONE', #36309 ) ;
#48423=CARTESIAN_POINT ( 'NONE',  ( 12.50412681322812958, -17.48010473091090589, 1.235016000439091988 ) ) ;
#48426=CARTESIAN_POINT ( 'NONE',  ( -1.169957374810000061, -77.28625595695000072, -12.74520906849999946 ) ) ;
#48428=CARTESIAN_POINT ( 'NONE',  ( -8.096452064242996016, -19.21421830981000056, 13.15643568217000769 ) ) ;
#48432=DIRECTION ( 'NONE',  ( -0.7592504785509017751, -0.04890181650815008524, 0.6489586451866018457 ) ) ;
#48433=ORIENTED_EDGE ( 'NONE', *, *, #23941, .F. ) ;
#48441=CARTESIAN_POINT ( 'NONE',  ( -7.644093100862067836, -60.32380578946135330, -10.09634101415690566 ) ) ;
#48442=CARTESIAN_POINT ( 'NONE',  ( -8.114915067892086498, -17.17115967855345104, 9.847905526149444810 ) ) ;
#48443=DIRECTION ( 'NONE',  ( 0.000000000000000000, -1.000000000000000000, 0.000000000000000000 ) ) ;
#48450=ORIENTED_EDGE ( 'NONE', *, *, #39828, .T. ) ;
#48454=EDGE_CURVE ( 'NONE', #44413, #23208, #25704, .T. ) ;
#48456=DIRECTION ( 'NONE',  ( 0.000000000000000000, 1.000000000000000000, 0.000000000000000000 ) ) ;
#48458=CARTESIAN_POINT ( 'NONE',  ( 3.008183132799063131, -2.043479984662694093, 1.827109633313784620 ) ) ;
#48460=CARTESIAN_POINT ( 'NONE',  ( -1.582498447122000051, -54.64913877488999816, -12.55493832969000145 ) ) ;
#48461=CARTESIAN_POINT ( 'NONE',  ( 11.09363377535068196, -75.97617094292559159, 3.874839546677522506 ) ) ;
#48463=VERTEX_POINT ( 'NONE', #27443 ) ;
#48464=CARTESIAN_POINT ( 'NONE',  ( 0.000000000000000000, -51.86282895648000135, 0.000000000000000000 ) ) ;
#48465=CARTESIAN_POINT ( 'NONE',  ( 0.4259464286568289682, -2.236800215964222627, -3.249988294983786830 ) ) ;
#48470=CARTESIAN_POINT ( 'NONE',  ( 0.9356112518261625599, -17.25892169760723860, -12.50329130247260601 ) ) ;
#48472=CARTESIAN_POINT ( 'NONE',  ( 3.171384185490563112, -78.55103045045009935, 11.31254194630599486 ) ) ;
#48474=ORIENTED_EDGE ( 'NONE', *, *, #26694, .F. ) ;
#48478=CARTESIAN_POINT ( 'NONE',  ( 11.40864393521657227, -75.79999999999999716, -3.704034794931656993 ) ) ;
#48483=DIRECTION ( 'NONE',  ( 0.000000000000000000, -1.000000000000000000, 0.000000000000000000 ) ) ;
#48485=DIRECTION ( 'NONE',  ( 1.000000000000000000, 0.000000000000000000, 2.582621269619999448E-11 ) ) ;
#48486=EDGE_CURVE ( 'NONE', #53713, #39513, #45376, .T. ) ;
#48489=PLANE ( 'NONE',  #3750 ) ;
#48491=CARTESIAN_POINT ( 'NONE',  ( -1.538071403320043551, -76.18541666666665435, 11.74999999999999467 ) ) ;
#48492=VERTEX_POINT ( 'NONE', #33329 ) ;
#48493=ORIENTED_EDGE ( 'NONE', *, *, #3071, .T. ) ;
#48494=CARTESIAN_POINT ( 'NONE',  ( -12.70926961117000076, -55.39159259587000150, -1.933875435151000133 ) ) ;
#48497=ORIENTED_EDGE ( 'NONE', *, *, #21868, .T. ) ;
#48503=ORIENTED_EDGE ( 'NONE', *, *, #40726, .F. ) ;
#48504=EDGE_LOOP ( 'NONE', ( #17917, #11524, #20605, #15076, #53802, #11022 ) ) ;
#48512=CARTESIAN_POINT ( 'NONE',  ( 12.66008925484999992, -17.37289997915000228, -1.387046028394999908 ) ) ;
#48513=CIRCLE ( 'NONE', #56067, 14.00000000000000533 ) ;
#48514=CARTESIAN_POINT ( 'NONE',  ( -9.830801209626999437, -24.09088558010999748, -7.765011064334000679 ) ) ;
#48515=CARTESIAN_POINT ( 'NONE',  ( -11.46828826707757365, -76.68240725586073836, 2.559436963939517362 ) ) ;
#48520=ADVANCED_FACE ( 'NONE', ( #10921 ), #30414, .T. ) ;
#48522=CARTESIAN_POINT ( 'NONE',  ( -9.213130513696000889, -16.99475660687000200, -8.533779407534000327 ) ) ;
#48523=FACE_OUTER_BOUND ( 'NONE', #57649, .T. ) ;
#48524=CARTESIAN_POINT ( 'NONE',  ( -0.4450739772392999782, -17.12186785197999939, -12.43586747594999942 ) ) ;
#48525=CARTESIAN_POINT ( 'NONE',  ( 1.634168180750863897, -1.268200832823612956, -2.838472589007412061 ) ) ;
#48526=CARTESIAN_POINT ( 'NONE',  ( 10.18491068061999982, -60.10716934574000447, -7.640030139773000606 ) ) ;
#48529=CARTESIAN_POINT ( 'NONE',  ( 12.52134121557681468, -23.92745484923118937, 1.618935178668554631 ) ) ;
#48532=CARTESIAN_POINT ( 'NONE',  ( 0.000000000000000000, 0.000000000000000000, -13.80000000000000071 ) ) ;
#48533=CARTESIAN_POINT ( 'NONE',  ( -1.477284502223000118, -54.07368499670000261, 12.77254812464999922 ) ) ;
#48534=CARTESIAN_POINT ( 'NONE',  ( 7.651160336694000641, -22.76232686216999923, -10.45205658994000153 ) ) ;
#48535=CARTESIAN_POINT ( 'NONE',  ( -2.072817167316999942, -2.797709358522999956, -3.192057609956000075 ) ) ;
#48540=CARTESIAN_POINT ( 'NONE',  ( -0.5154756746308999382, -61.93240599730000184, 12.66205448077000106 ) ) ;
#48543=EDGE_CURVE ( 'NONE', #17562, #53718, #5928, .T. ) ;
#48545=CYLINDRICAL_SURFACE ( 'NONE', #18276, 1.750000000000001332 ) ;
#48547=CARTESIAN_POINT ( 'NONE',  ( 9.566106889961746518, -76.40027222109127081, -6.823059203283996510 ) ) ;
#48550=CARTESIAN_POINT ( 'NONE',  ( -12.05000000000000071, -74.80000000000001137, 0.000000000000000000 ) ) ;
#48553=LINE ( 'NONE', #43256, #16152 ) ;
#48556=DIRECTION ( 'NONE',  ( 0.000000000000000000, 1.000000000000000000, 0.000000000000000000 ) ) ;
#48557=CARTESIAN_POINT ( 'NONE',  ( -10.27342224349341926, -17.93842478175206523, -7.712153330322490952 ) ) ;
#48559=ADVANCED_FACE ( 'NONE', ( #41617 ), #55195, .F. ) ;
#48561=VECTOR ( 'NONE', #23755, 1000.000000000000000 ) ;
#48565=ORIENTED_EDGE ( 'NONE', *, *, #12691, .F. ) ;
#48566=EDGE_LOOP ( 'NONE', ( #55976, #53879, #27332, #34167, #30251 ) ) ;
#48567=CARTESIAN_POINT ( 'NONE',  ( -1.811016405462510859, -24.06173555372251371, 12.71771640064107523 ) ) ;
#48568=ORIENTED_EDGE ( 'NONE', *, *, #45634, .T. ) ;
#48569=PLANE ( 'NONE',  #15107 ) ;
#48570=ORIENTED_EDGE ( 'NONE', *, *, #55153, .F. ) ;
#48571=DIRECTION ( 'NONE',  ( 0.000000000000000000, -1.000000000000000000, 0.000000000000000000 ) ) ;
#48572=CIRCLE ( 'NONE', #41949, 0.5000000000000004441 ) ;
#48579=CARTESIAN_POINT ( 'NONE',  ( 4.729275446575999631, -78.57519050484999923, -11.25706921911999991 ) ) ;
#48580=ORIENTED_EDGE ( 'NONE', *, *, #46706, .T. ) ;
#48582=CARTESIAN_POINT ( 'NONE',  ( 12.80000000000000071, -6.000000000000000000, 0.000000000000000000 ) ) ;
#48584=CARTESIAN_POINT ( 'NONE',  ( 0.000000000000000000, -65.72928575305999743, 0.000000000000000000 ) ) ;
#48587=CARTESIAN_POINT ( 'NONE',  ( 11.88773275212999891, -76.79030896091001068, 5.537155082298999886 ) ) ;
#48588=CARTESIAN_POINT ( 'NONE',  ( -3.180509609271000127, -77.13961746229999505, 12.23476839664999893 ) ) ;
#48589=AXIS2_PLACEMENT_3D ( 'NONE', #11240, #37497, #29506 ) ;
#48593=CARTESIAN_POINT ( 'NONE',  ( -10.35747145894000099, -60.11584731951999316, 7.626500777253000685 ) ) ;
#48594=CARTESIAN_POINT ( 'NONE',  ( -2.103158146349364710, -3.031636871358540208, 2.492261966649085281 ) ) ;
#48596=B_SPLINE_CURVE_WITH_KNOTS ( 'NONE', 3,
 ( #16291, #47021, #29553, #56732, #47311, #28979 ),
 .UNSPECIFIED., .F., .F.,
 ( 4, 2, 4 ),
 ( 0.000000000000000000, 0.5000000000000000000, 1.000000000000000000 ),
 .UNSPECIFIED. ) ;
#48600=CARTESIAN_POINT ( 'NONE',  ( -3.796701970596999764, -2.742418933659000135, 0.2667143827384000354 ) ) ;
#48606=CARTESIAN_POINT ( 'NONE',  ( -12.82202470520000048, -18.57373556878999921, -2.066041976111999467 ) ) ;
#48607=DIRECTION ( 'NONE',  ( -0.5721800012450221073, 0.8201280669354309438, 0.000000000000000000 ) ) ;
#48611=CARTESIAN_POINT ( 'NONE',  ( -11.74660045421000021, -76.64649974677999467, 3.339300926223000232 ) ) ;
#48612=ORIENTED_EDGE ( 'NONE', *, *, #34477, .F. ) ;
#48613=CARTESIAN_POINT ( 'NONE',  ( 12.50000000000000000, -18.75000000000000000, 0.000000000000000000 ) ) ;
#48616=CARTESIAN_POINT ( 'NONE',  ( 0.000000000000000000, -3.000000000000000000, 0.000000000000000000 ) ) ;
#48625=VERTEX_POINT ( 'NONE', #38344 ) ;
#48626=EDGE_LOOP ( 'NONE', ( #35901, #26752, #7188 ) ) ;
#48629=CARTESIAN_POINT ( 'NONE',  ( 12.53241208775000004, -56.03537109808000594, 1.667936697358999965 ) ) ;
#48634=VERTEX_POINT ( 'NONE', #52793 ) ;
#48636=VERTEX_POINT ( 'NONE', #48377 ) ;
#48637=ADVANCED_FACE ( 'NONE', ( #7058 ), #12517, .F. ) ;
#48638=CARTESIAN_POINT ( 'NONE',  ( 8.485281374238999419, -59.94999999967000548, 8.485281374238999419 ) ) ;
#48639=CARTESIAN_POINT ( 'NONE',  ( -3.567760415766010773, -1.844193969458715276, 0.1559241275462920073 ) ) ;
#48642=CARTESIAN_POINT ( 'NONE',  ( 10.98364301412005517, -18.76988149294329844, 0.5996551156055476284 ) ) ;
#48646=CARTESIAN_POINT ( 'NONE',  ( 8.878349648264999061, -53.73036913477000098, 8.870329531799001188 ) ) ;
#48647=CARTESIAN_POINT ( 'NONE',  ( -7.613962827178999859, -18.69360374348000065, -10.53101998747000145 ) ) ;
#48648=CARTESIAN_POINT ( 'NONE',  ( 5.208905169669622914, -77.35915899447975619, -10.56041358256653062 ) ) ;
#48653=EDGE_CURVE ( 'NONE', #31908, #42463, #25629, .T. ) ;
#48657=CARTESIAN_POINT ( 'NONE',  ( 12.80088938719999803, -19.23743348210000192, -1.980532758767000301 ) ) ;
#48658=DIRECTION ( 'NONE',  ( 1.000000000000000000, 0.000000000000000000, 0.000000000000000000 ) ) ;
#48660=CARTESIAN_POINT ( 'NONE',  ( 12.52582323433381362, -23.80939730775251917, -1.680974276152543467 ) ) ;
#48661=CARTESIAN_POINT ( 'NONE',  ( 7.624341766656999475, -60.06485146221000093, 10.42531125026000005 ) ) ;
#48665=CARTESIAN_POINT ( 'NONE',  ( 8.096452064242996016, -19.21421830981000056, -13.15643568217000769 ) ) ;
#48666=VECTOR ( 'NONE', #38790, 999.9999999999998863 ) ;
#48670=DIRECTION ( 'NONE',  ( -1.000000000000000000, 0.000000000000000000, 0.000000000000000000 ) ) ;
#48681=CARTESIAN_POINT ( 'NONE',  ( 2.965054089066000209, -1.248435987229999933, -1.931333211479999923 ) ) ;
#48683=CARTESIAN_POINT ( 'NONE',  ( 12.43641409351999982, -24.91801033895000117, 0.03481937293212000045 ) ) ;
#48684=CARTESIAN_POINT ( 'NONE',  ( -1.799501877793999949, -60.08917723397000543, 12.60552511012999943 ) ) ;
#48685=EDGE_LOOP ( 'NONE', ( #1143, #33227, #27621, #51913, #46789, #30768 ) ) ;
#48686=DIRECTION ( 'NONE',  ( 0.000000000000000000, -1.000000000000000000, 0.000000000000000000 ) ) ;
#48689=EDGE_CURVE ( 'NONE', #35908, #53225, #11781, .T. ) ;
#48695=CARTESIAN_POINT ( 'NONE',  ( 9.392095713130165890, -77.89521769223929937, -7.218153635797654566 ) ) ;
#48696=CARTESIAN_POINT ( 'NONE',  ( -1.931087888240000217, -23.31584731985000047, 12.71658872084999992 ) ) ;
#48697=VERTEX_POINT ( 'NONE', #34476 ) ;
#48698=CARTESIAN_POINT ( 'NONE',  ( -12.87022657272000004, -56.01514526721999943, 2.062597299672999540 ) ) ;
#48702=ORIENTED_EDGE ( 'NONE', *, *, #10459, .T. ) ;
#48703=ADVANCED_FACE ( 'NONE', ( #25342 ), #43357, .F. ) ;
#48704=ORIENTED_EDGE ( 'NONE', *, *, #43376, .F. ) ;
#48712=CARTESIAN_POINT ( 'NONE',  ( 11.77596950146999966, -77.36568903011000486, 5.402702954953999992 ) ) ;
#48714=AXIS2_PLACEMENT_3D ( 'NONE', #25055, #47235, #6763 ) ;
#48719=CIRCLE ( 'NONE', #23269, 1.750000000000001998 ) ;
#48720=CARTESIAN_POINT ( 'NONE',  ( 8.803761571639995509, -16.78431590350725244, 9.164326402704537244 ) ) ;
#48725=CARTESIAN_POINT ( 'NONE',  ( -12.60356226362999976, -19.24922971138999728, -1.750000000000000000 ) ) ;
#48727=CARTESIAN_POINT ( 'NONE',  ( 2.281100415086936284, -3.030341629373181078, -2.679643809356492490 ) ) ;
#48729=CARTESIAN_POINT ( 'NONE',  ( 11.75000000000000000, -77.45000000000000284, 1.043320980279999928E-14 ) ) ;
#48730=DIRECTION ( 'NONE',  ( 0.000000000000000000, 1.000000000000000000, 0.000000000000000000 ) ) ;
#48732=CARTESIAN_POINT ( 'NONE',  ( 7.648026766715999791, -55.54999999381000464, 10.12290050087000104 ) ) ;
#48739=DIRECTION ( 'NONE',  ( 0.7071067811865975328, -0.7071067811864976127, 8.872297124978962287E-10 ) ) ;
#48742=EDGE_CURVE ( 'NONE', #21248, #51275, #4078, .T. ) ;
#48744=CARTESIAN_POINT ( 'NONE',  ( 12.90000000000000036, -5.900000000000010125, 0.000000000000000000 ) ) ;
#48746=CARTESIAN_POINT ( 'NONE',  ( -2.019183793707000074, -55.01279722724000010, -12.79944116701999768 ) ) ;
#48747=CARTESIAN_POINT ( 'NONE',  ( 9.783314345684438251, -75.99666901279969977, 6.507558209343685895 ) ) ;
#48749=ORIENTED_EDGE ( 'NONE', *, *, #35628, .F. ) ;
#48753=DIRECTION ( 'NONE',  ( 0.9999999929803531362, 0.000000000000000000, 0.0001184875252606944153 ) ) ;
#48755=CARTESIAN_POINT ( 'NONE',  ( 1.980610890452897399, -18.47926110520256771, 12.74374574607350574 ) ) ;
#48759=ORIENTED_EDGE ( 'NONE', *, *, #6979, .T. ) ;
#48763=CARTESIAN_POINT ( 'NONE',  ( 12.00000000000000000, -75.80000000000001137, -2.990830162875999918E-13 ) ) ;
#48767=EDGE_CURVE ( 'NONE', #47851, #24723, #17649, .T. ) ;
#48768=LINE ( 'NONE', #26590, #55244 ) ;
#48770=CARTESIAN_POINT ( 'NONE',  ( 10.99607952894010054, -23.68503250286068607, -0.3139933498775518417 ) ) ;
#48772=CARTESIAN_POINT ( 'NONE',  ( 13.99999999961999819, -72.70000000038000110, -1.691901775850999968E-09 ) ) ;
#48775=CARTESIAN_POINT ( 'NONE',  ( 8.485281374238999419, 0.000000000000000000, 8.485281374238999419 ) ) ;
#48776=ORIENTED_EDGE ( 'NONE', *, *, #22302, .F. ) ;
#48777=EDGE_CURVE ( 'NONE', #35786, #470, #36873, .T. ) ;
#48778=EDGE_LOOP ( 'NONE', ( #2311, #34447, #36785, #35465, #8392, #53457 ) ) ;
#48782=ORIENTED_EDGE ( 'NONE', *, *, #45387, .T. ) ;
#48783=CARTESIAN_POINT ( 'NONE',  ( 9.101516360816999551, -24.88066799059000189, 8.485522730740999720 ) ) ;
#48785=CARTESIAN_POINT ( 'NONE',  ( -10.42531124905999995, -18.73514851523999880, 7.624341765453999997 ) ) ;
#48789=ORIENTED_EDGE ( 'NONE', *, *, #35413, .F. ) ;
#48792=CIRCLE ( 'NONE', #35581, 1.749999999999998890 ) ;
#48794=CARTESIAN_POINT ( 'NONE',  ( 10.49984016500000017, -76.62494580621000750, -6.347025226577000190 ) ) ;
#48795=CARTESIAN_POINT ( 'NONE',  ( 3.250000000000000000, -2.250000000000000000, 0.000000000000000000 ) ) ;
#48796=DIRECTION ( 'NONE',  ( 0.7071067811865475727, 0.000000000000000000, -0.7071067811865475727 ) ) ;
#48798=FACE_OUTER_BOUND ( 'NONE', #36500, .T. ) ;
#48802=ORIENTED_EDGE ( 'NONE', *, *, #10590, .T. ) ;
#48805=CARTESIAN_POINT ( 'NONE',  ( -8.588893914397997875, -53.66760216274000328, 9.317954957978999531 ) ) ;
#48807=CARTESIAN_POINT ( 'NONE',  ( -12.74331206683534390, -60.32649290773906614, 1.980611467281705229 ) ) ;
#48809=CARTESIAN_POINT ( 'NONE',  ( 7.627487606591000002, -55.50221404479999876, 10.35845616725999996 ) ) ;
#48810=CARTESIAN_POINT ( 'NONE',  ( -1.798954018882000128, -18.78469026612999926, -12.61117007302000026 ) ) ;
#48812=DIRECTION ( 'NONE',  ( 1.000000000000000000, 0.000000000000000000, 1.147001872820999768E-14 ) ) ;
#48814=CARTESIAN_POINT ( 'NONE',  ( 11.19999999861000006, -74.79999999860999083, 9.230036577774000073E-09 ) ) ;
#48816=FACE_OUTER_BOUND ( 'NONE', #55164, .T. ) ;
#48820=CARTESIAN_POINT ( 'NONE',  ( -11.79999999988000070, -23.14999999478999726, 0.5999999998848000171 ) ) ;
#48821=CARTESIAN_POINT ( 'NONE',  ( -0.8445585116460000430, -54.08959556723999640, 12.43380736233000050 ) ) ;
#48822=CARTESIAN_POINT ( 'NONE',  ( -12.75763395695999947, -22.77795407709999864, 1.931043742978000077 ) ) ;
#48823=CARTESIAN_POINT ( 'NONE',  ( 3.208820596785000312, -1.826303692333000050, 1.361140077406000071 ) ) ;
#48825=CARTESIAN_POINT ( 'NONE',  ( 3.250000000000000000, -1.750000000000000000, 0.000000000000000000 ) ) ;
#48827=CARTESIAN_POINT ( 'NONE',  ( 0.4701041210467000186, -61.80796934391000264, 12.54901038419999892 ) ) ;
#48828=CARTESIAN_POINT ( 'NONE',  ( 12.66235371498999918, -16.86260492134000089, 0.4957155363045000485 ) ) ;
#48830=CARTESIAN_POINT ( 'NONE',  ( 12.90000000000000036, 0.000000000000000000, 0.000000000000000000 ) ) ;
#48832=B_SPLINE_SURFACE_WITH_KNOTS ( 'NONE', 3, 3, ( 
 ( #34498, #8511, #57815, #53386, #53104, #57524, #48681, #3512, #3795, #21513, #30066, #52814, #12932, #17674, #35660, #22084, #38939, #48398, #48117 ),
 ( #7649, #43674, #2938, #40098, #44243, #44531, #53691, #12653, #58111, #13229, #39802, #7363, #48970, #57241, #8225, #20937, #21223, #56956, #21797 ),
 ( #25648, #17374, #39228, #26505, #16805, #12369, #34790, #35361, #30357, #7935, #43962, #39519, #9408, #36556, #37133, #36843, #53989, #54855, #18850 ),
 ( #19139, #27398, #5546, #13527, #34769, #8813, #14402, #49568, #27976, #55144, #41572, #54578, #26805, #13824, #18565, #9115, #22982, #46025, #22389 ) ),
 .UNSPECIFIED., .F., .F., .F.,
 ( 4, 4 ),
 ( 4, 1, 1, 1, 1, 1, 1, 1, 1, 1, 1, 1, 1, 1, 1, 1, 4 ),
 ( -0.3708084972812999980, 1.370808497280999960 ),
 ( -0.01016343285802999950, 0.02286772393056000011, 0.05589888071915000145, 0.08893003750774999827, 0.1219611942962999934, 0.1549923510849000041, 0.1880235078735000009, 0.2210546646621000255, 0.2540858214506999668, 0.2871169782393000469, 0.3201481350279000160, 0.3531792918164999850, 0.3862104486051000096, 0.4192416053937000342, 0.4522727621821999722, 0.4853039189707999967, 0.5183350757593999658 ),
 .UNSPECIFIED. ) ;
#48834=ADVANCED_FACE ( 'NONE', ( #30912 ), #19188, .F. ) ;
#48839=CARTESIAN_POINT ( 'NONE',  ( -12.83836863002999884, -60.00626272179999887, 2.062146390631000248 ) ) ;
#48842=CARTESIAN_POINT ( 'NONE',  ( -7.610436392414960061, -18.47459049293312816, -10.41144384038885207 ) ) ;
#48844=CARTESIAN_POINT ( 'NONE',  ( 0.000000000000000000, -2.660000000000000142, 0.000000000000000000 ) ) ;
#48852=EDGE_LOOP ( 'NONE', ( #24380, #52521, #13983, #47138, #23217, #17367 ) ) ;
#48853=CARTESIAN_POINT ( 'NONE',  ( 0.000000000000000000, -32.70420297070000260, 0.000000000000000000 ) ) ;
#48854=ORIENTED_EDGE ( 'NONE', *, *, #34778, .F. ) ;
#48862=ORIENTED_EDGE ( 'NONE', *, *, #51247, .F. ) ;
#48864=CARTESIAN_POINT ( 'NONE',  ( 8.504094770722000263, -78.69101207264999687, -8.967282323152000245 ) ) ;
#48865=ORIENTED_EDGE ( 'NONE', *, *, #56821, .T. ) ;
#48866=VERTEX_POINT ( 'NONE', #9677 ) ;
#48870=DIRECTION ( 'NONE',  ( -0.7071067811865475727, 0.000000000000000000, 0.7071067811865475727 ) ) ;
#48874=CARTESIAN_POINT ( 'NONE',  ( -9.412102823527000339, -78.06691570303000560, -9.131157420175998851 ) ) ;
#48875=CARTESIAN_POINT ( 'NONE',  ( -7.818192365797999699, -78.17570409358999939, 9.061685001942999307 ) ) ;
#48880=CARTESIAN_POINT ( 'NONE',  ( -1.389309474284118329, -3.011527199678093680, 2.937373092524380169 ) ) ;
#48882=EDGE_CURVE ( 'NONE', #29606, #22997, #6823, .T. ) ;
#48887=CARTESIAN_POINT ( 'NONE',  ( 2.534829140202000008, -2.065001425904999799, 2.839140403359000420 ) ) ;
#48891=DIRECTION ( 'NONE',  ( -1.000000000000000000, 0.000000000000000000, 0.000000000000000000 ) ) ;
#48895=CARTESIAN_POINT ( 'NONE',  ( -12.43410192431999839, -17.55868879885999689, -1.192687910177000044 ) ) ;
#48896=CARTESIAN_POINT ( 'NONE',  ( -9.287618194362000423, -77.54441932644999724, -9.114789584104999065 ) ) ;
#48897=VECTOR ( 'NONE', #50259, 1000.000000000000114 ) ;
#48899=CARTESIAN_POINT ( 'NONE',  ( -5.893333102785000222, -76.58035197021000329, -11.03757542588999918 ) ) ;
#48901=CARTESIAN_POINT ( 'NONE',  ( -10.12290050122000018, -55.54999999974999980, 7.648026767069000087 ) ) ;
#48914=ORIENTED_EDGE ( 'NONE', *, *, #45640, .F. ) ;
#48916=CARTESIAN_POINT ( 'NONE',  ( -7.342331066867000544, -55.64999999967000122, -8.190859204290999784 ) ) ;
#48920=ORIENTED_EDGE ( 'NONE', *, *, #23668, .T. ) ;
#48924=LINE ( 'NONE', #39478, #14785 ) ;
#48930=PLANE ( 'NONE',  #57604 ) ;
#48931=EDGE_CURVE ( 'NONE', #32213, #10018, #20410, .T. ) ;
#48932=CARTESIAN_POINT ( 'NONE',  ( 0.5245219981312709834, -18.54839576652498323, 10.98753021428709253 ) ) ;
#48934=EDGE_CURVE ( 'NONE', #21614, #54902, #28609, .T. ) ;
#48935=CARTESIAN_POINT ( 'NONE',  ( -1.749722766161712073, -55.32411007028972705, 12.54673760671600213 ) ) ;
#48936=CARTESIAN_POINT ( 'NONE',  ( 7.627487525399000212, -55.50221245779999890, -10.35845608624000036 ) ) ;
#48943=CARTESIAN_POINT ( 'NONE',  ( -1.295048492660999973, -24.52893519126000044, 12.54716442236999896 ) ) ;
#48945=EDGE_CURVE ( 'NONE', #15410, #56481, #16272, .T. ) ;
#48952=CARTESIAN_POINT ( 'NONE',  ( -13.13047446164998711, -19.21421830981000767, 0.8260994316375004365 ) ) ;
#48955=DIRECTION ( 'NONE',  ( -8.659560562353647261E-17, 0.7071067811866525998, 0.7071067811864425456 ) ) ;
#48956=CONICAL_SURFACE ( 'NONE', #23506, 11.09999999881999955, 0.7853981633972997312 ) ;
#48958=DIRECTION ( 'NONE',  ( 0.000000000000000000, -0.7071067811864425456, -0.7071067811866525998 ) ) ;
#48962=CARTESIAN_POINT ( 'NONE',  ( -10.01234990228999955, -18.70150862776000267, -7.653559502277999194 ) ) ;
#48964=ADVANCED_FACE ( 'NONE', ( #30401 ), #29529, .T. ) ;
#48966=LINE ( 'NONE', #8508, #25659 ) ;
#48968=CARTESIAN_POINT ( 'NONE',  ( -9.641208724103000449, -61.23394297667999808, 7.943747389727000119 ) ) ;
#48970=CARTESIAN_POINT ( 'NONE',  ( 2.730509227798000094, -0.9404343447128000744, 2.498711234688000271 ) ) ;
#48972=CARTESIAN_POINT ( 'NONE',  ( 12.49830695668999958, -23.20970582274999927, -1.666977511086999986 ) ) ;
#48973=DIRECTION ( 'NONE',  ( -1.000000000000000000, 0.000000000000000000, 0.000000000000000000 ) ) ;
#48974=ORIENTED_EDGE ( 'NONE', *, *, #25374, .T. ) ;
#48977=CARTESIAN_POINT ( 'NONE',  ( -12.50409217856559962, -17.47871355536218729, 1.233808107092820183 ) ) ;
#48981=LINE ( 'NONE', #25661, #28495 ) ;
#48984=ADVANCED_FACE ( 'NONE', ( #34540 ), #43422, .F. ) ;
#48985=EDGE_LOOP ( 'NONE', ( #37432, #23760, #21112, #52641, #6302, #17786 ) ) ;
#48986=ORIENTED_EDGE ( 'NONE', *, *, #53195, .F. ) ;
#48987=CARTESIAN_POINT ( 'NONE',  ( -8.194873807802000698, -54.08956116737999764, -9.389185139509999445 ) ) ;
#48989=ORIENTED_EDGE ( 'NONE', *, *, #13188, .F. ) ;
#48990=ORIENTED_EDGE ( 'NONE', *, *, #50786, .T. ) ;
#48994=VERTEX_POINT ( 'NONE', #52004 ) ;
#48998=CARTESIAN_POINT ( 'NONE',  ( 12.62753648294000008, -77.72264530807001393, -3.537092078510000182 ) ) ;
#49000=CARTESIAN_POINT ( 'NONE',  ( -13.63885489310999510, -22.78578169018999944, 7.254376133916000668 ) ) ;
#49005=EDGE_LOOP ( 'NONE', ( #13240, #16038, #25544, #50356, #28371, #51525, #17926 ) ) ;
#49011=CARTESIAN_POINT ( 'NONE',  ( -1.484444257814014012, -3.439588485883066316, -3.191343661318504665 ) ) ;
#49013=CARTESIAN_POINT ( 'NONE',  ( -9.689263856525805352, -17.02111184948868328, 8.274777959192654464 ) ) ;
#49015=DIRECTION ( 'NONE',  ( -1.000000000000000000, -3.446666965303000135E-11, 0.000000000000000000 ) ) ;
#49017=EDGE_CURVE ( 'NONE', #21891, #56481, #52573, .T. ) ;
#49019=CARTESIAN_POINT ( 'NONE',  ( 10.01332844637000008, -23.28056692670000061, -7.654537085030000299 ) ) ;
#49021=CARTESIAN_POINT ( 'NONE',  ( 10.35453599130000057, -76.65783510652001098, -6.064947188958000446 ) ) ;
#49023=DIRECTION ( 'NONE',  ( 0.000000000000000000, -1.000000000000000000, 0.000000000000000000 ) ) ;
#49024=ORIENTED_EDGE ( 'NONE', *, *, #40709, .T. ) ;
#49027=CARTESIAN_POINT ( 'NONE',  ( 7.710095619848000403, -57.04935285743999884, -10.18496935399999970 ) ) ;
#49034=CARTESIAN_POINT ( 'NONE',  ( -1.801614160562000189, -55.41347738061999451, -12.59687422885999908 ) ) ;
#49035=CARTESIAN_POINT ( 'NONE',  ( -9.722718241315000398, -60.04999999966999980, 7.954951288349001004 ) ) ;
#49037=ORIENTED_EDGE ( 'NONE', *, *, #52839, .T. ) ;
#49040=CARTESIAN_POINT ( 'NONE',  ( 6.998236738571699256, -78.87457940415021085, -9.608823350299664057 ) ) ;
#49041=EDGE_CURVE ( 'NONE', #51923, #25833, #35110, .T. ) ;
#49045=CARTESIAN_POINT ( 'NONE',  ( 1.722320550008820339, -17.76336311177879779, 12.71171904436578615 ) ) ;
#49047=CARTESIAN_POINT ( 'NONE',  ( 3.536460498928797769, -78.54893592801708735, 11.20448496730672794 ) ) ;
#49048=CARTESIAN_POINT ( 'NONE',  ( 10.53559655343999957, -18.79430958026000198, -7.620036381602000475 ) ) ;
#49049=ORIENTED_EDGE ( 'NONE', *, *, #31173, .T. ) ;
#49055=CARTESIAN_POINT ( 'NONE',  ( 12.50240681836000078, -61.48234730679999416, -1.005418944265000114 ) ) ;
#49060=CIRCLE ( 'NONE', #51901, 13.86363636363999952 ) ;
#49061=CARTESIAN_POINT ( 'NONE',  ( 8.130813118010999929, -17.31476110167000115, -9.546856411651999608 ) ) ;
#49062=CARTESIAN_POINT ( 'NONE',  ( -12.70610460586324386, -61.25512899760538232, -1.580683094070863604 ) ) ;
#49069=CARTESIAN_POINT ( 'NONE',  ( -10.39285214024000048, -78.50746505344999093, 6.510605926401999533 ) ) ;
#49071=CARTESIAN_POINT ( 'NONE',  ( 9.929702205000999982, -24.63097880280000140, 7.973987073284000360 ) ) ;
#49072=CARTESIAN_POINT ( 'NONE',  ( -10.42531125068999920, -23.26485145404000221, 7.624341767093000044 ) ) ;
#49073=CARTESIAN_POINT ( 'NONE',  ( -12.50728321917715391, -24.99975184166999753, -0.1774118160393889920 ) ) ;
#49082=CARTESIAN_POINT ( 'NONE',  ( 6.758991595627000137, -76.50069210185999680, -10.87838826503999989 ) ) ;
#49088=CARTESIAN_POINT ( 'NONE',  ( 0.000000000000000000, -15.06282895647999887, 0.000000000000000000 ) ) ;
#49091=EDGE_CURVE ( 'NONE', #41589, #48697, #33290, .T. ) ;
#49094=CARTESIAN_POINT ( 'NONE',  ( -7.758650587924000419, -54.64922688096000059, 9.996717134826001327 ) ) ;
#49097=CARTESIAN_POINT ( 'NONE',  ( -12.70255466322978144, -61.54616562041045569, 1.306323829516669255 ) ) ;
#49098=VECTOR ( 'NONE', #49820, 1000.000000000000114 ) ;
#49099=CARTESIAN_POINT ( 'NONE',  ( 7.655555357438999842, -56.02204592290999585, 10.38646360829000059 ) ) ;
#49100=CARTESIAN_POINT ( 'NONE',  ( -1.667269374596999976, -18.79060116514999734, -12.49858097730999873 ) ) ;
#49102=CARTESIAN_POINT ( 'NONE',  ( 10.53101990622000095, -60.10639784916000394, -7.613962745625999062 ) ) ;
#49106=CARTESIAN_POINT ( 'NONE',  ( -2.507084801459968038, -0.8133145018255537595, -2.558030464532227821 ) ) ;
#49107=ORIENTED_EDGE ( 'NONE', *, *, #22266, .T. ) ;
#49108=DIRECTION ( 'NONE',  ( 0.009503199022040095811, 0.000000000000000000, -0.9999548435846228323 ) ) ;
#49109=CARTESIAN_POINT ( 'NONE',  ( -1.807051837523000026, -54.49921584723999501, 12.77977401831000037 ) ) ;
#49110=DIRECTION ( 'NONE',  ( 0.9999999930530776293, 0.000000000000000000, 0.0001178721535674748841 ) ) ;
#49111=ADVANCED_FACE ( 'NONE', ( #9665 ), #39896, .F. ) ;
#49112=CARTESIAN_POINT ( 'NONE',  ( -3.266298089353000034, -1.668078706142999801, -1.618310284079999883 ) ) ;
#49114=PLANE ( 'NONE',  #39437 ) ;
#49115=CARTESIAN_POINT ( 'NONE',  ( -0.9887300587116000239, -61.73410057736000311, 12.65963207093999898 ) ) ;
#49118=CARTESIAN_POINT ( 'NONE',  ( 9.722718241315000398, -23.44678171330999916, -7.954951288349001004 ) ) ;
#49119=CARTESIAN_POINT ( 'NONE',  ( 12.07139231284771164, -77.20343651399288376, 0.05712616762542849919 ) ) ;
#49120=CARTESIAN_POINT ( 'NONE',  ( -6.190658199239000403, -78.41135615475999998, 10.70411142322000053 ) ) ;
#49121=CIRCLE ( 'NONE', #39670, 1.749999999999999556 ) ;
#49134=CARTESIAN_POINT ( 'NONE',  ( 8.190836719257328369, -55.61035107871643390, 7.342356150419330874 ) ) ;
#49140=CARTESIAN_POINT ( 'NONE',  ( -11.75000000000000000, -78.79999999999999716, 1.318041981624000073E-14 ) ) ;
#49144=CARTESIAN_POINT ( 'NONE',  ( 0.000000000000000000, -46.09579702914000165, 0.000000000000000000 ) ) ;
#49150=EDGE_LOOP ( 'NONE', ( #37443, #16474, #23507, #9644, #33804, #35314 ) ) ;
#49152=CARTESIAN_POINT ( 'NONE',  ( -9.315216588649001039, -78.86259768561001238, 7.893946640039000151 ) ) ;
#49153=ORIENTED_EDGE ( 'NONE', *, *, #42765, .T. ) ;
#49154=EDGE_LOOP ( 'NONE', ( #40589, #21790, #3193, #30874, #40790, #10160 ) ) ;
#49155=FACE_OUTER_BOUND ( 'NONE', #8461, .T. ) ;
#49156=DIRECTION ( 'NONE',  ( -0.9999463328794432337, 0.000000000000000000, 0.01036008498777044214 ) ) ;
#49160=DIRECTION ( 'NONE',  ( -2.622163234167000180E-09, -1.000000000000000000, -6.038615341233999930E-09 ) ) ;
#49161=CARTESIAN_POINT ( 'NONE',  ( -10.33814977949000102, -76.69558033460998558, 7.275158806450000348 ) ) ;
#49163=CARTESIAN_POINT ( 'NONE',  ( -10.18499221077999906, -20.25022860214999909, 7.710118476625000383 ) ) ;
#49164=EDGE_CURVE ( 'NONE', #14569, #52925, #48393, .T. ) ;
#49166=B_SPLINE_CURVE_WITH_KNOTS ( 'NONE', 3,
 ( #23022, #10039, #33029, #45476 ),
 .UNSPECIFIED., .F., .F.,
 ( 4, 4 ),
 ( 0.000000000000000000, 1.000000000000000000 ),
 .UNSPECIFIED. ) ;
#49167=CARTESIAN_POINT ( 'NONE',  ( 12.65372179303999900, -21.75064713777999970, 1.750000000000000000 ) ) ;
#49168=DIRECTION ( 'NONE',  ( 0.000000000000000000, -1.000000000000000000, 0.000000000000000000 ) ) ;
#49170=CARTESIAN_POINT ( 'NONE',  ( 0.7999999999999001243, -18.84999999997999964, 12.00000000000000000 ) ) ;
#49172=CARTESIAN_POINT ( 'NONE',  ( -2.809159726167000048, -3.341600190120999958, -2.568020482856000264 ) ) ;
#49175=CARTESIAN_POINT ( 'NONE',  ( 0.5999381870725726262, -23.23019609313229239, 10.98362755083784847 ) ) ;
#49179=VECTOR ( 'NONE', #17876, 1000.000000000000000 ) ;
#49180=CARTESIAN_POINT ( 'NONE',  ( -12.77568125278999922, -16.73490786122999907, -0.5296379231476000538 ) ) ;
#49182=CARTESIAN_POINT ( 'NONE',  ( 12.53073434187000146, -77.71093324932999735, -3.509976885708000260 ) ) ;
#49185=CARTESIAN_POINT ( 'NONE',  ( 12.83044027761000017, -18.69360215052999763, -2.062670899361999766 ) ) ;
#49186=ORIENTED_EDGE ( 'NONE', *, *, #18704, .F. ) ;
#49187=DIRECTION ( 'NONE',  ( 1.000000000000000000, 0.000000000000000000, 0.000000000000000000 ) ) ;
#49188=DIRECTION ( 'NONE',  ( 0.000000000000000000, 1.000000000000000000, 0.000000000000000000 ) ) ;
#49190=CARTESIAN_POINT ( 'NONE',  ( -1.799490225533999732, -19.22847221992000044, -12.64500484465999897 ) ) ;
#49193=CARTESIAN_POINT ( 'NONE',  ( 2.627446458840999810, -1.600918092571000040, 3.037392460054000320 ) ) ;
#49198=CARTESIAN_POINT ( 'NONE',  ( -3.251154051729839178, -1.100857096137070279, 2.995606203745920413E-05 ) ) ;
#49201=ORIENTED_EDGE ( 'NONE', *, *, #481, .T. ) ;
#49202=ORIENTED_EDGE ( 'NONE', *, *, #10820, .F. ) ;
#49205=CARTESIAN_POINT ( 'NONE',  ( 8.838834764832000701, -23.25000000000000000, -8.838834764832000701 ) ) ;
#49206=EDGE_LOOP ( 'NONE', ( #22259, #56698, #9132, #57885 ) ) ;
#49209=ORIENTED_EDGE ( 'NONE', *, *, #39447, .T. ) ;
#49211=EDGE_LOOP ( 'NONE', ( #8957, #46495, #4530, #13566, #970 ) ) ;
#49213=CARTESIAN_POINT ( 'NONE',  ( 7.364280830343314044, -60.14010097497207141, 8.171144579306906408 ) ) ;
#49214=EDGE_CURVE ( 'NONE', #41145, #23631, #44495, .T. ) ;
#49216=CARTESIAN_POINT ( 'NONE',  ( -1.081559480311999888, -0.7500000000000000000, 3.328697807033000000 ) ) ;
#49217=ORIENTED_EDGE ( 'NONE', *, *, #37975, .T. ) ;
#49220=VECTOR ( 'NONE', #8262, 1000.000000000000114 ) ;
#49221=DIRECTION ( 'NONE',  ( -0.9859154929576978699, -0.1672442547472993701, -2.241743217924995723E-11 ) ) ;
#49223=CARTESIAN_POINT ( 'NONE',  ( 10.53495272788000214, -55.57289072595000334, 7.618387390351999855 ) ) ;
#49224=CARTESIAN_POINT ( 'NONE',  ( -7.682344222590000271, -19.23537109840999904, -10.04116292118000153 ) ) ;
#49226=CARTESIAN_POINT ( 'NONE',  ( -9.396085398178650294, -78.74791666666668277, 7.220923959705211281 ) ) ;
#49227=CARTESIAN_POINT ( 'NONE',  ( 7.627487606627999739, -60.09778595451999905, -10.35845616728999907 ) ) ;
#49228=CARTESIAN_POINT ( 'NONE',  ( 8.768124086712999699, -59.94999999969000015, -7.919595949288999570 ) ) ;
#49229=CARTESIAN_POINT ( 'NONE',  ( -9.778543098479998363, -25.04857981702999936, 8.284584910395000890 ) ) ;
#49233=AXIS2_PLACEMENT_3D ( 'NONE', #46248, #42094, #46545 ) ;
#49234=CARTESIAN_POINT ( 'NONE',  ( -12.43645963092999907, -17.08248289540999920, -0.05235777564062000372 ) ) ;
#49236=CARTESIAN_POINT ( 'NONE',  ( 1.194090705999000024, -24.44031658902999737, 12.43436538489999954 ) ) ;
#49237=CARTESIAN_POINT ( 'NONE',  ( -8.090910852015257504, -60.34721902435955343, -7.452378523310254188 ) ) ;
#49239=CARTESIAN_POINT ( 'NONE',  ( 2.702298720593999892, -1.280362276481999961, 2.656632122398999485 ) ) ;
#49240=CARTESIAN_POINT ( 'NONE',  ( 7.686941364987999847, -57.04527982297999955, 10.48774103564000093 ) ) ;
#49244=FACE_BOUND ( 'NONE', #11480, .T. ) ;
#49249=CARTESIAN_POINT ( 'NONE',  ( 0.000000000000000000, -0.2000000000000000111, 0.000000000000000000 ) ) ;
#49252=ORIENTED_EDGE ( 'NONE', *, *, #12591, .F. ) ;
#49256=CARTESIAN_POINT ( 'NONE',  ( 7.919595949288999570, -57.79999999967000690, -8.909545442949999838 ) ) ;
#49261=CONICAL_SURFACE ( 'NONE', #31320, 8.899999998586000771, 0.7853981633972997312 ) ;
#49263=DIRECTION ( 'NONE',  ( -0.9999999999999992228, 4.158392525768991814E-08, -7.902844367246985944E-12 ) ) ;
#49264=CARTESIAN_POINT ( 'NONE',  ( -3.250000000000000000, -3.100000000000000089, 0.000000000000000000 ) ) ;
#49265=CARTESIAN_POINT ( 'NONE',  ( -1.930989144707000005, -57.04634220890999785, 12.80900240956999880 ) ) ;
#49266=ORIENTED_EDGE ( 'NONE', *, *, #54501, .F. ) ;
#49270=B_SPLINE_CURVE_WITH_KNOTS ( 'NONE', 3,
 ( #38094, #37508, #23931, #16247, #24231, #25093 ),
 .UNSPECIFIED., .F., .F.,
 ( 4, 2, 4 ),
 ( 0.000000000000000000, 0.5000000000000000000, 1.000000000000000000 ),
 .UNSPECIFIED. ) ;
#49272=CARTESIAN_POINT ( 'NONE',  ( -10.35845608624000036, -55.50221245779999890, -7.627487525399000212 ) ) ;
#49275=VERTEX_POINT ( 'NONE', #19032 ) ;
#49277=DIRECTION ( 'NONE',  ( -2.678911359553000079E-11, -1.000000000000000000, 2.678929432950999965E-11 ) ) ;
#49278=CARTESIAN_POINT ( 'NONE',  ( 12.50000000000000000, -61.48359816765000119, 1.003641516062000250 ) ) ;
#49280=VECTOR ( 'NONE', #55209, 1000.000000000000000 ) ;
#49281=CARTESIAN_POINT ( 'NONE',  ( -8.958657468006999025, -53.59887336276000269, -8.950049500613999953 ) ) ;
#49282=ADVANCED_FACE ( 'NONE', ( #6024 ), #14452, .F. ) ;
#49283=CIRCLE ( 'NONE', #52122, 0.5999999999999999778 ) ;
#49285=ORIENTED_EDGE ( 'NONE', *, *, #37333, .F. ) ;
#49286=EDGE_LOOP ( 'NONE', ( #4114, #8039, #5145, #53053 ) ) ;
#49290=ORIENTED_EDGE ( 'NONE', *, *, #33717, .T. ) ;
#49294=CARTESIAN_POINT ( 'NONE',  ( -10.50899237707999845, -78.03174472164999997, 7.577845091584000770 ) ) ;
#49296=DIRECTION ( 'NONE',  ( 0.6489586469986090567, 0.04890178910789071826, 0.7592504787669100974 ) ) ;
#49299=EDGE_CURVE ( 'NONE', #26517, #8180, #32573, .T. ) ;
#49301=CARTESIAN_POINT ( 'NONE',  ( 8.121706841783367992, -17.16372996693625197, 9.841114038361700622 ) ) ;
#49307=CARTESIAN_POINT ( 'NONE',  ( -3.296692919738537064, -2.817192224941006629, 1.392370562533553180 ) ) ;
#49308=CARTESIAN_POINT ( 'NONE',  ( -7.921329716887100858, -17.44906234264657741, 10.04564005581343267 ) ) ;
#49313=CARTESIAN_POINT ( 'NONE',  ( 9.098185902166729733, -77.24261121748705250, -8.011918831721102308 ) ) ;
#49316=AXIS2_PLACEMENT_3D ( 'NONE', #52008, #11562, #29540 ) ;
#49318=CARTESIAN_POINT ( 'NONE',  ( -8.343860018000999190, -59.94999999967000548, -8.343860018000999190 ) ) ;
#49319=ORIENTED_EDGE ( 'NONE', *, *, #34513, .T. ) ;
#49322=FACE_OUTER_BOUND ( 'NONE', #17976, .T. ) ;
#49330=CARTESIAN_POINT ( 'NONE',  ( -1.389926494652000022, -54.17618663712000426, -12.65988803918999928 ) ) ;
#49331=CARTESIAN_POINT ( 'NONE',  ( 8.326851758844648899, -76.01173316031734828, 8.289602951553833421 ) ) ;
#49334=DIRECTION ( 'NONE',  ( -0.7071067811865475727, 0.000000000000000000, 0.7071067811865475727 ) ) ;
#49348=CARTESIAN_POINT ( 'NONE',  ( 11.98956178826566799, -75.80000000000001137, -0.9444271482678882057 ) ) ;
#49350=EDGE_CURVE ( 'NONE', #37882, #7601, #43669, .T. ) ;
#49353=CARTESIAN_POINT ( 'NONE',  ( -10.98362417419999915, -23.15000000000000213, 0.5999999999999999778 ) ) ;
#49357=CARTESIAN_POINT ( 'NONE',  ( 9.369164850722000892, -55.54999999966999980, -7.601397897754999633 ) ) ;
#49358=EDGE_CURVE ( 'NONE', #24745, #9508, #762, .T. ) ;
#49359=AXIS2_PLACEMENT_3D ( 'NONE', #54543, #40960, #33248 ) ;
#49360=CARTESIAN_POINT ( 'NONE',  ( -12.65989858207000118, -24.94344101132999825, 0.9743214026256000748 ) ) ;
#49362=ORIENTED_EDGE ( 'NONE', *, *, #39826, .T. ) ;
#49364=ORIENTED_EDGE ( 'NONE', *, *, #25335, .F. ) ;
#49367=CARTESIAN_POINT ( 'NONE',  ( 8.790688707546999936, -24.93813493249999880, 8.797962936834998970 ) ) ;
#49369=EDGE_CURVE ( 'NONE', #37143, #11113, #32349, .T. ) ;
#49370=VECTOR ( 'NONE', #31383, 1000.000000000000000 ) ;
#49371=CARTESIAN_POINT ( 'NONE',  ( -7.612971540294999784, -60.12452273675999947, 10.53003236235000095 ) ) ;
#49375=CARTESIAN_POINT ( 'NONE',  ( 3.250000000000000000, -1.850000000000000089, 0.000000000000000000 ) ) ;
#49376=ADVANCED_FACE ( 'NONE', ( #11915 ), #32541, .F. ) ;
#49378=ORIENTED_EDGE ( 'NONE', *, *, #51033, .F. ) ;
#49383=CARTESIAN_POINT ( 'NONE',  ( 10.37229188467999919, -76.53786495648000709, -6.269923847882999723 ) ) ;
#49385=CARTESIAN_POINT ( 'NONE',  ( 10.21026245498356033, -54.54392421755085962, -7.764236519575772100 ) ) ;
#49388=CARTESIAN_POINT ( 'NONE',  ( 12.59682398758999966, -18.61262488659000169, -1.801644812721000077 ) ) ;
#49389=CARTESIAN_POINT ( 'NONE',  ( -10.13402523425000012, -23.72303809441999789, -7.647751776486000352 ) ) ;
#49390=CARTESIAN_POINT ( 'NONE',  ( -11.37990774082085466, -76.67987294336911930, 2.931073317825884317 ) ) ;
#49397=EDGE_CURVE ( 'NONE', #23446, #16168, #25193, .T. ) ;
#49399=CARTESIAN_POINT ( 'NONE',  ( -3.075537641221531615, -78.40416666666666856, -11.44417895085270942 ) ) ;
#49400=FACE_OUTER_BOUND ( 'NONE', #12464, .T. ) ;
#49401=DIRECTION ( 'NONE',  ( 0.000000000000000000, 1.000000000000000000, 0.000000000000000000 ) ) ;
#49403=CARTESIAN_POINT ( 'NONE',  ( 10.18491080491000034, -55.49283319101999723, -7.640030264136999705 ) ) ;
#49410=AXIS2_PLACEMENT_3D ( 'NONE', #25732, #29575, #20450 ) ;
#49411=CARTESIAN_POINT ( 'NONE',  ( 1.930638663168000146, -55.57877936677999742, 12.72375916870000090 ) ) ;
#49412=CARTESIAN_POINT ( 'NONE',  ( -12.83044027761000017, -18.69360215052999763, 2.062670899361999766 ) ) ;
#49413=CARTESIAN_POINT ( 'NONE',  ( -2.548053818379999669, -3.743360633963999984, 2.532771267353999711 ) ) ;
#49415=CARTESIAN_POINT ( 'NONE',  ( 2.598917237794088564, -1.697916666666666519, -1.997276839918468605 ) ) ;
#49416=DIRECTION ( 'NONE',  ( 0.000000000000000000, 0.000000000000000000, -1.000000000000000000 ) ) ;
#49418=CARTESIAN_POINT ( 'NONE',  ( 12.66001647286000065, -17.36746073369999621, 1.381678996660999914 ) ) ;
#49420=DIRECTION ( 'NONE',  ( 1.000000000000000000, 0.000000000000000000, 0.000000000000000000 ) ) ;
#49422=CARTESIAN_POINT ( 'NONE',  ( 4.636146969708000221, -78.82343122293001159, -11.75666478071000043 ) ) ;
#49426=CARTESIAN_POINT ( 'NONE',  ( -0.6484536763444428420, -61.92402982674907719, 12.70397497896646932 ) ) ;
#49428=CARTESIAN_POINT ( 'NONE',  ( -12.46083365857999858, -60.48341615446999953, 1.628972628240000109 ) ) ;
#49430=CARTESIAN_POINT ( 'NONE',  ( 12.60356226360999798, -22.75077028889999653, -1.750000000000000000 ) ) ;
#49437=VECTOR ( 'NONE', #20687, 1000.000000000000000 ) ;
#49440=VERTEX_POINT ( 'NONE', #43211 ) ;
#49441=EDGE_CURVE ( 'NONE', #41447, #24970, #30459, .T. ) ;
#49442=DIRECTION ( 'NONE',  ( 0.000000000000000000, 1.000000000000000000, 0.000000000000000000 ) ) ;
#49443=ORIENTED_EDGE ( 'NONE', *, *, #16396, .F. ) ;
#49444=FACE_OUTER_BOUND ( 'NONE', #46496, .T. ) ;
#49445=VERTEX_POINT ( 'NONE', #38769 ) ;
#49446=CARTESIAN_POINT ( 'NONE',  ( 9.722718241315000398, -60.04999999966999980, 7.247844507162001015 ) ) ;
#49448=DIRECTION ( 'NONE',  ( 0.000000000000000000, -0.7071067811866525998, -0.7071067811864425456 ) ) ;
#49451=CARTESIAN_POINT ( 'NONE',  ( 1.389926494651000155, -24.62381336254999908, -12.65988803923000106 ) ) ;
#49452=CIRCLE ( 'NONE', #38096, 0.5000000000000006661 ) ;
#49456=CARTESIAN_POINT ( 'NONE',  ( 10.77676250696000082, -79.20748630253001465, 5.740077567832999605 ) ) ;
#49458=ORIENTED_EDGE ( 'NONE', *, *, #19753, .T. ) ;
#49464=DIRECTION ( 'NONE',  ( 0.000000000000000000, 0.000000000000000000, -1.000000000000000000 ) ) ;
#49466=CARTESIAN_POINT ( 'NONE',  ( -1.184344363998000027, -77.03625595695000072, -12.90193715879000003 ) ) ;
#49471=CARTESIAN_POINT ( 'NONE',  ( -7.954951288349001004, -18.55321828668999729, 9.722718241315000398 ) ) ;
#49472=CARTESIAN_POINT ( 'NONE',  ( 2.970834971129885815, -2.884370106164003467, 1.316369104713672966 ) ) ;
#49476=CARTESIAN_POINT ( 'NONE',  ( -0.6934022908089999548, -3.241579146514999898, 3.742362521638999961 ) ) ;
#49478=ORIENTED_EDGE ( 'NONE', *, *, #53613, .F. ) ;
#49479=CARTESIAN_POINT ( 'NONE',  ( 0.5200379331771535218, -23.45155696396579970, 10.98772212209804700 ) ) ;
#49480=DIRECTION ( 'NONE',  ( 0.000000000000000000, 1.000000000000000000, 0.000000000000000000 ) ) ;
#49481=AXIS2_PLACEMENT_3D ( 'NONE', #5669, #5385, #41403 ) ;
#49483=CIRCLE ( 'NONE', #52303, 0.5000000000000004441 ) ;
#49484=CARTESIAN_POINT ( 'NONE',  ( -12.54902617719999824, -16.99030198144999915, -0.4617931494615999943 ) ) ;
#49485=CARTESIAN_POINT ( 'NONE',  ( 11.88928085110999966, -78.26597965894998765, 5.289737169833999886 ) ) ;
#49487=CARTESIAN_POINT ( 'NONE',  ( -9.073558136300860610, -62.02808769461389460, -8.894842552386064582 ) ) ;
#49488=CARTESIAN_POINT ( 'NONE',  ( 12.71798280855999863, -23.29778595484999926, -1.931086388455000025 ) ) ;
#49489=ORIENTED_EDGE ( 'NONE', *, *, #41967, .F. ) ;
#49491=CARTESIAN_POINT ( 'NONE',  ( 9.502921958894958721, -54.05907999833515021, -8.179400290810697527 ) ) ;
#49493=CARTESIAN_POINT ( 'NONE',  ( 7.613962745610000304, -18.69360215052999763, -10.53101990620000095 ) ) ;
#49496=CARTESIAN_POINT ( 'NONE',  ( 2.301364338783000285, -1.525557261822999999, -3.291430154679999998 ) ) ;
#49497=CARTESIAN_POINT ( 'NONE',  ( -1.799501877759999813, -60.08917565288000162, -12.60552522438000089 ) ) ;
#49501=CYLINDRICAL_SURFACE ( 'NONE', #10609, 14.00000000000000000 ) ;
#49506=CARTESIAN_POINT ( 'NONE',  ( 9.050966798898000931, -59.94999999040999938, 7.919595949288999570 ) ) ;
#49508=ORIENTED_EDGE ( 'NONE', *, *, #45300, .F. ) ;
#49509=EDGE_CURVE ( 'NONE', #16536, #30070, #12763, .T. ) ;
#49513=CARTESIAN_POINT ( 'NONE',  ( -1.872510430921729752, -2.676471623700526159, -2.659056711493340774 ) ) ;
#49515=CARTESIAN_POINT ( 'NONE',  ( -3.758731266216853939, -1.376714976881707297, -1.426415079042028689 ) ) ;
#49517=LINE ( 'NONE', #13183, #31787 ) ;
#49521=VECTOR ( 'NONE', #13779, 1000.000000000000000 ) ;
#49523=FACE_OUTER_BOUND ( 'NONE', #47547, .T. ) ;
#49526=DIRECTION ( 'NONE',  ( -1.000000000000000000, 0.000000000000000000, 0.000000000000000000 ) ) ;
#49528=CARTESIAN_POINT ( 'NONE',  ( 10.26699006316251683, -78.59166666666666856, 5.917523019358090330 ) ) ;
#49531=CARTESIAN_POINT ( 'NONE',  ( -8.485538010655998775, -24.88067982437999959, 9.101501073481999882 ) ) ;
#49534=CARTESIAN_POINT ( 'NONE',  ( 9.137847679653942734, -78.14631709695343886, -7.887011953151875865 ) ) ;
#49539=DIRECTION ( 'NONE',  ( 9.217554796542082011E-07, 2.920569602132825499E-20, -0.9999999999995752287 ) ) ;
#49540=CARTESIAN_POINT ( 'NONE',  ( -2.062323307449999810, -23.22713153192000135, 12.83634826442999888 ) ) ;
#49541=DIRECTION ( 'NONE',  ( 1.000000000000000000, 0.000000000000000000, 0.000000000000000000 ) ) ;
#49543=CARTESIAN_POINT ( 'NONE',  ( -1.466295893230999958, -0.9762401806307999808, -3.674175840820999905 ) ) ;
#49545=CARTESIAN_POINT ( 'NONE',  ( 1.750000000001000089, -55.54999998977000075, -12.56594317853999954 ) ) ;
#49549=CARTESIAN_POINT ( 'NONE',  ( 0.000000000000000000, -72.39999999999999147, 0.000000000000000000 ) ) ;
#49551=ADVANCED_FACE ( 'NONE', ( #19412 ), #34008, .T. ) ;
#49558=EDGE_CURVE ( 'NONE', #55909, #50392, #10016, .T. ) ;
#49560=CARTESIAN_POINT ( 'NONE',  ( 17.50000000000000000, -15.06282895647999887, 3.979097884520999899E-10 ) ) ;
#49561=CIRCLE ( 'NONE', #33526, 0.5999999999999999778 ) ;
#49566=CARTESIAN_POINT ( 'NONE',  ( 13.79999999999999893, 0.000000000000000000, 0.000000000000000000 ) ) ;
#49568=CARTESIAN_POINT ( 'NONE',  ( 0.6653596569558999363, -1.443831454374000067, -3.971211220357999672 ) ) ;
#49569=CARTESIAN_POINT ( 'NONE',  ( 1.998841639285485527, -76.43855673768001679, -11.64912468341469776 ) ) ;
#49571=CARTESIAN_POINT ( 'NONE',  ( -2.062503053667999797, -58.55736537918999574, 12.92177931905999877 ) ) ;
#49572=VERTEX_POINT ( 'NONE', #10560 ) ;
#49575=CARTESIAN_POINT ( 'NONE',  ( -7.958763982144999360, -54.32301960774000094, -9.723170657514000226 ) ) ;
#49578=CARTESIAN_POINT ( 'NONE',  ( -12.87022657274000004, -59.58485473249000108, -2.062597299672999540 ) ) ;
#49579=CARTESIAN_POINT ( 'NONE',  ( -3.250000000000000000, -2.600000000000000089, 0.000000000000000000 ) ) ;
#49580=ORIENTED_EDGE ( 'NONE', *, *, #54291, .T. ) ;
#49583=CARTESIAN_POINT ( 'NONE',  ( 2.598917237794088564, -1.197916666666666963, -1.997276839918468605 ) ) ;
#49585=ORIENTED_EDGE ( 'NONE', *, *, #51695, .F. ) ;
#49586=CARTESIAN_POINT ( 'NONE',  ( -7.948094694382998426, -54.35965255578000210, -9.636752590464999102 ) ) ;
#49590=EDGE_CURVE ( 'NONE', #1742, #42116, #11400, .T. ) ;
#49593=EDGE_CURVE ( 'NONE', #57120, #51909, #50721, .T. ) ;
#49596=DIRECTION ( 'NONE',  ( 0.000000000000000000, 0.000000000000000000, -1.000000000000000000 ) ) ;
#49597=CARTESIAN_POINT ( 'NONE',  ( -9.412102823527000339, -78.05567315384000437, -9.131157420175998851 ) ) ;
#49601=CIRCLE ( 'NONE', #11888, 1.750000000000000000 ) ;
#49604=VERTEX_POINT ( 'NONE', #564 ) ;
#49606=CARTESIAN_POINT ( 'NONE',  ( 5.894077591580000330, -76.71673252672998444, -10.80721126921000064 ) ) ;
#49608=VECTOR ( 'NONE', #2220, 1000.000000000000000 ) ;
#49609=CARTESIAN_POINT ( 'NONE',  ( -2.677348439713063133, -3.405484581173921388, -2.283878904445620694 ) ) ;
#49610=ADVANCED_FACE ( 'NONE', ( #5821 ), #22130, .F. ) ;
#49611=CARTESIAN_POINT ( 'NONE',  ( -7.712209501881797102, -17.93822238229371635, 10.27335463211299960 ) ) ;
#49613=AXIS2_PLACEMENT_3D ( 'NONE', #12946, #44546, #30944 ) ;
#49614=CARTESIAN_POINT ( 'NONE',  ( -9.621717088248901817, -61.42064477338403350, -8.060172376582604770 ) ) ;
#49616=CARTESIAN_POINT ( 'NONE',  ( -10.34293954422016348, -77.00689439288741767, 6.233549652297469379 ) ) ;
#49617=CARTESIAN_POINT ( 'NONE',  ( 5.976685521875192642, -76.61603491465773175, -11.25172029877191093 ) ) ;
#49618=DIRECTION ( 'NONE',  ( -0.7071067811865474617, 0.000000000000000000, 0.7071067811865474617 ) ) ;
#49619=EDGE_LOOP ( 'NONE', ( #47588, #43331, #10817 ) ) ;
#49622=DIRECTION ( 'NONE',  ( -1.000000000000000000, 0.000000000000000000, 0.000000000000000000 ) ) ;
#49627=CARTESIAN_POINT ( 'NONE',  ( 4.498217319268383640, -76.04320575685785855, 10.85453619212339227 ) ) ;
#49629=DIRECTION ( 'NONE',  ( -0.7071067811865475727, 0.000000000000000000, -0.7071067811865475727 ) ) ;
#49630=ORIENTED_EDGE ( 'NONE', *, *, #52987, .T. ) ;
#49636=DIRECTION ( 'NONE',  ( 0.7071067811865475727, 0.000000000000000000, 0.7071067811865475727 ) ) ;
#49638=DIRECTION ( 'NONE',  ( -1.000000000000000000, 0.000000000000000000, 0.000000000000000000 ) ) ;
#49641=VERTEX_POINT ( 'NONE', #29703 ) ;
#49648=CARTESIAN_POINT ( 'NONE',  ( 12.49999991316347270, -39.30476017083000073, 0.001473401919610936930 ) ) ;
#49651=VECTOR ( 'NONE', #17292, 1000.000000000000000 ) ;
#49653=AXIS2_PLACEMENT_3D ( 'NONE', #58157, #48730, #40145 ) ;
#49654=DIRECTION ( 'NONE',  ( -0.9999999999995751176, 0.000000000000000000, -9.217554798440770948E-07 ) ) ;
#49655=CARTESIAN_POINT ( 'NONE',  ( -12.54983138327999903, -25.05098386350000084, 0.1356331847737999863 ) ) ;
#49656=VERTEX_POINT ( 'NONE', #56588 ) ;
#49657=CIRCLE ( 'NONE', #45919, 0.8000000000000011546 ) ;
#49658=VERTEX_POINT ( 'NONE', #7283 ) ;
#49661=VECTOR ( 'NONE', #57481, 1000.000000000000114 ) ;
#49665=CARTESIAN_POINT ( 'NONE',  ( 7.619712170649999727, -23.40404510063000032, 10.35409959310000083 ) ) ;
#49668=CARTESIAN_POINT ( 'NONE',  ( -10.48774103546000092, -20.24527981753999839, 7.686941364807000632 ) ) ;
#49674=ORIENTED_EDGE ( 'NONE', *, *, #17635, .T. ) ;
#49677=DIRECTION ( 'NONE',  ( 0.7071067811865475727, 0.000000000000000000, 0.7071067811865475727 ) ) ;
#49679=CARTESIAN_POINT ( 'NONE',  ( 6.925222504723999251, -76.67485380131999761, -11.14593178024999887 ) ) ;
#49683=CARTESIAN_POINT ( 'NONE',  ( 0.000000000000000000, -23.25000000000000000, -12.50000000000000000 ) ) ;
#49685=FACE_OUTER_BOUND ( 'NONE', #39991, .T. ) ;
#49686=CARTESIAN_POINT ( 'NONE',  ( -11.33353239526517520, -76.67864579003945380, 3.106984491474204191 ) ) ;
#49693=CARTESIAN_POINT ( 'NONE',  ( -10.30457855492000085, -18.23665569414000132, 7.636266481018999741 ) ) ;
#49694=VECTOR ( 'NONE', #38849, 1000.000000000000114 ) ;
#49696=DIRECTION ( 'NONE',  ( -1.000000000000000000, 0.000000000000000000, 0.000000000000000000 ) ) ;
#49701=DIRECTION ( 'NONE',  ( -1.000000000000000000, 0.000000000000000000, 0.000000000000000000 ) ) ;
#49706=CARTESIAN_POINT ( 'NONE',  ( 1.056237665594999875, -53.75133986268999564, 12.77256098193999989 ) ) ;
#49709=CARTESIAN_POINT ( 'NONE',  ( 0.3040822296088999677, -3.436728339067000260, -3.954576031983000117 ) ) ;
#49714=DIRECTION ( 'NONE',  ( -1.000000000000000000, 0.000000000000000000, 0.000000000000000000 ) ) ;
#49716=CARTESIAN_POINT ( 'NONE',  ( 12.77568125278999922, -16.73490786122999907, 0.5296379231475000227 ) ) ;
#49719=EDGE_CURVE ( 'NONE', #54081, #28385, #14194, .T. ) ;
#49720=CARTESIAN_POINT ( 'NONE',  ( 9.636775127257999785, -54.35967715709000458, -7.948072248856999700 ) ) ;
#49721=ADVANCED_FACE ( 'NONE', ( #18476 ), #36183, .F. ) ;
#49726=CARTESIAN_POINT ( 'NONE',  ( -17.49999986748943925, -49.87071424677999687, -0.002153571276212541078 ) ) ;
#49727=CARTESIAN_POINT ( 'NONE',  ( -12.78015149461000100, -61.10330660662999946, 1.806228889759999845 ) ) ;
#49731=ORIENTED_EDGE ( 'NONE', *, *, #37001, .F. ) ;
#49732=CARTESIAN_POINT ( 'NONE',  ( 9.431004454403453252, -53.99940410528930101, 8.251853356943772866 ) ) ;
#49735=CARTESIAN_POINT ( 'NONE',  ( 3.250000000000000000, -1.850000000000000089, 0.000000000000000000 ) ) ;
#49736=ORIENTED_EDGE ( 'NONE', *, *, #46462, .T. ) ;
#49737=ORIENTED_EDGE ( 'NONE', *, *, #46673, .F. ) ;
#49741=CARTESIAN_POINT ( 'NONE',  ( 9.837773999883454579, -54.48535604146630362, -7.850041801328902835 ) ) ;
#49742=CIRCLE ( 'NONE', #2620, 10.20000000000000107 ) ;
#49743=ORIENTED_EDGE ( 'NONE', *, *, #14112, .F. ) ;
#49747=CARTESIAN_POINT ( 'NONE',  ( -0.5390150933986999071, -25.26260891652000140, -12.77520261005000002 ) ) ;
#49751=CARTESIAN_POINT ( 'NONE',  ( -11.36395519648000096, -78.80425755395999943, 4.043272157487999507 ) ) ;
#49752=CIRCLE ( 'NONE', #24284, 0.6000000000000008660 ) ;
#49755=CARTESIAN_POINT ( 'NONE',  ( -10.12290050255000118, -55.55000002206000431, -7.648026768392999664 ) ) ;
#49757=AXIS2_PLACEMENT_3D ( 'NONE', #50524, #51113, #948 ) ;
#49760=CIRCLE ( 'NONE', #21458, 1.250000000000000000 ) ;
#49761=CYLINDRICAL_SURFACE ( 'NONE', #55846, 1.750000000000000000 ) ;
#49763=CARTESIAN_POINT ( 'NONE',  ( 7.289493654314999738, -77.00467974817999561, -10.52009694070999934 ) ) ;
#49764=CARTESIAN_POINT ( 'NONE',  ( 5.486311112560000147, -77.58365458999999476, 11.38883617360999878 ) ) ;
#49769=CARTESIAN_POINT ( 'NONE',  ( -10.59548767697000038, -58.55736537918999574, 7.678667886039000301 ) ) ;
#49772=LINE ( 'NONE', #49170, #18513 ) ;
#49778=CARTESIAN_POINT ( 'NONE',  ( 11.75000000000000000, -78.45000000000000284, 0.000000000000000000 ) ) ;
#49781=CARTESIAN_POINT ( 'NONE',  ( -8.048032176077001054, -78.44865870152001719, 9.328081102756000220 ) ) ;
#49784=CARTESIAN_POINT ( 'NONE',  ( 12.60552511010000032, -18.71082276572999703, -1.799501877793999949 ) ) ;
#49786=CARTESIAN_POINT ( 'NONE',  ( 0.000000000000000000, -55.54999999966999980, 12.00000000000000000 ) ) ;
#49789=AXIS2_PLACEMENT_3D ( 'NONE', #15663, #12388, #38672 ) ;
#49794=CARTESIAN_POINT ( 'NONE',  ( -0.4617212151683000032, -1.166835600325000000, 3.989551193614000013 ) ) ;
#49795=CARTESIAN_POINT ( 'NONE',  ( -2.062673488738000049, -55.47547470607999998, -12.82904091336000008 ) ) ;
#49801=ORIENTED_EDGE ( 'NONE', *, *, #20391, .T. ) ;
#49804=CARTESIAN_POINT ( 'NONE',  ( -1.342463812738999916E-14, -80.79999999999999716, -13.90000000000000036 ) ) ;
#49807=EDGE_CURVE ( 'NONE', #47711, #3338, #21584, .T. ) ;
#49809=VERTEX_POINT ( 'NONE', #39589 ) ;
#49810=CARTESIAN_POINT ( 'NONE',  ( 0.8446295986270583311, -2.746170833900309027, -3.145970808612796876 ) ) ;
#49811=DIRECTION ( 'NONE',  ( 0.7071067811864970576, 3.544461081833985722E-08, -0.7071067811865970887 ) ) ;
#49812=CARTESIAN_POINT ( 'NONE',  ( 8.500000000000000000, -3.500000000000000000, 0.000000000000000000 ) ) ;
#49813=B_SPLINE_SURFACE_WITH_KNOTS ( 'NONE', 3, 3, ( 
 ( #44852, #12671, #3529, #54304 ),
 ( #18289, #31240, #40718, #35682 ),
 ( #310, #25954, #4706, #17102 ),
 ( #40116, #4105, #22106, #30662 ),
 ( #8532, #26525, #4404, #21531 ),
 ( #39536, #57542, #44552, #49586 ),
 ( #36281, #17691, #44261, #48987 ),
 ( #30376, #48416, #53711, #13247 ),
 ( #35088, #49281, #35377, #57835 ),
 ( #7952, #17391, #22406, #12950 ),
 ( #30948, #8833, #26822, #3815 ),
 ( #8243, #26245, #53122, #22704 ),
 ( #9133, #21818, #40418, #12 ),
 ( #39819, #17991, #54007, #13548 ),
 ( #31540, #27117, #45157, #28283 ),
 ( #600, #37151, #9714, #19450 ),
 ( #5859, #45450, #18582, #41591 ) ),
 .UNSPECIFIED., .F., .F., .F.,
 ( 4, 1, 1, 1, 1, 1, 1, 1, 1, 1, 1, 1, 1, 1, 4 ),
 ( 4, 4 ),
 ( -0.01011837001259000002, 0.000000000000000000, 0.08333333333333001192, 0.1666666666667000196, 0.2500000000000000000, 0.3333333333333000081, 0.4166666666666999919, 0.5000000000000000000, 0.5833333333333000637, 0.6666666666667000474, 0.7500000000000000000, 0.8333333333333000637, 0.9166666666667000474, 1.000000000000000000, 1.010372850415000023 ),
 ( -0.3559705548695000221, 1.357613361088000126 ),
 .UNSPECIFIED. ) ;
#49814=VERTEX_POINT ( 'NONE', #56452 ) ;
#49819=EDGE_CURVE ( 'NONE', #30968, #39067, #37500, .T. ) ;
#49820=DIRECTION ( 'NONE',  ( -0.7071067811704841999, -1.939413340559955448E-07, 0.7071067812025843002 ) ) ;
#49821=TOROIDAL_SURFACE ( 'NONE', #11185, 1.250000000000000000, 0.5000000000000000000 ) ;
#49822=CARTESIAN_POINT ( 'NONE',  ( -0.5847500590559130407, -18.69344856180045156, 10.98448857562230252 ) ) ;
#49823=CARTESIAN_POINT ( 'NONE',  ( -1.538071403320043551, -77.18541666666666856, 11.74999999999999467 ) ) ;
#49827=CARTESIAN_POINT ( 'NONE',  ( -12.65372179303999900, -21.75064713777999970, -1.750000000000000000 ) ) ;
#49828=CARTESIAN_POINT ( 'NONE',  ( -10.30767511322000018, -23.74763733895999707, 7.634418707049000830 ) ) ;
#49830=CARTESIAN_POINT ( 'NONE',  ( -11.75000000000000000, -76.79999999999999716, -1.435311119447000145E-14 ) ) ;
#49834=AXIS2_PLACEMENT_3D ( 'NONE', #5087, #27792, #50842 ) ;
#49836=CARTESIAN_POINT ( 'NONE',  ( 1.629367637659999923, -23.68263643397999729, 12.46114270826000059 ) ) ;
#49838=CARTESIAN_POINT ( 'NONE',  ( -3.262415774573999894, -2.066798252606000474, -0.4905674017874000481 ) ) ;
#49840=CARTESIAN_POINT ( 'NONE',  ( 7.651147547619999933, -59.56256650291999222, 10.45204383579000051 ) ) ;
#49841=DIRECTION ( 'NONE',  ( 0.000000000000000000, -1.000000000000000000, 0.000000000000000000 ) ) ;
#49843=EDGE_CURVE ( 'NONE', #22190, #6045, #32140, .T. ) ;
#49845=CARTESIAN_POINT ( 'NONE',  ( 0.000000000000000000, -45.91785611817000046, 0.000000000000000000 ) ) ;
#49846=CARTESIAN_POINT ( 'NONE',  ( 9.546815223802999739, -54.11472046612000497, 8.130854305859999798 ) ) ;
#49854=ORIENTED_EDGE ( 'NONE', *, *, #55651, .F. ) ;
#49858=EDGE_CURVE ( 'NONE', #41874, #11038, #39692, .T. ) ;
#49859=LINE ( 'NONE', #44526, #23811 ) ;
#49862=DIRECTION ( 'NONE',  ( 1.205798305761979436E-11, -1.868137355152963707E-07, 0.9999999999999824585 ) ) ;
#49865=CARTESIAN_POINT ( 'NONE',  ( 6.732849078471510929, -76.47319592210000394, -9.714227559369218667 ) ) ;
#49866=CARTESIAN_POINT ( 'NONE',  ( -8.583677311523363329, -61.77185920727036716, 9.102132575252269930 ) ) ;
#49868=ORIENTED_EDGE ( 'NONE', *, *, #54939, .T. ) ;
#49869=CARTESIAN_POINT ( 'NONE',  ( -1.980584515752000119, -55.53514853344000102, -12.76303204600000107 ) ) ;
#49871=AXIS2_PLACEMENT_3D ( 'NONE', #54899, #36599, #54623 ) ;
#49872=CARTESIAN_POINT ( 'NONE',  ( -1.842306058376209643, -75.81200536713309646, -11.64247462211659290 ) ) ;
#49873=CARTESIAN_POINT ( 'NONE',  ( 14.00000000000000000, -9.295797029142999435, 0.000000000000000000 ) ) ;
#49874=CARTESIAN_POINT ( 'NONE',  ( -12.69616050744000013, -58.55171076491000548, -1.799475304559999822 ) ) ;
#49875=CARTESIAN_POINT ( 'NONE',  ( 10.99608688423679403, -23.68532521788496581, 0.3139246511496328607 ) ) ;
#49876=EDGE_LOOP ( 'NONE', ( #36063, #39539, #28720, #12036, #44060 ) ) ;
#49878=CARTESIAN_POINT ( 'NONE',  ( 10.04567131166087179, -61.35088387338642946, -7.921299640537584175 ) ) ;
#49879=ORIENTED_EDGE ( 'NONE', *, *, #48934, .T. ) ;
#49882=CYLINDRICAL_SURFACE ( 'NONE', #21699, 1.750000000000001332 ) ;
#49884=ORIENTED_EDGE ( 'NONE', *, *, #37066, .F. ) ;
#49886=DIRECTION ( 'NONE',  ( -0.9999999924279686647, 0.000000000000000000, -0.0001230612157847738313 ) ) ;
#49892=CARTESIAN_POINT ( 'NONE',  ( -1.273906987915999878, -77.61163602614999490, -13.05154622979999957 ) ) ;
#49896=CARTESIAN_POINT ( 'NONE',  ( -1.668607604570423009, -23.79381631241137995, 12.52787843850897964 ) ) ;
#49897=VERTEX_POINT ( 'NONE', #43173 ) ;
#49898=DIRECTION ( 'NONE',  ( 1.000000000000000000, 0.000000000000000000, 0.000000000000000000 ) ) ;
#49899=CARTESIAN_POINT ( 'NONE',  ( 1.328206530128999807, -76.68560288576000517, -12.23810562210000086 ) ) ;
#49902=CARTESIAN_POINT ( 'NONE',  ( 0.6527094116100424781, -3.209387129096291424, 3.460698173749425344 ) ) ;
#49904=CARTESIAN_POINT ( 'NONE',  ( 13.86363636363000218, -46.43897132165000130, 1.277887489249999988E-05 ) ) ;
#49905=CARTESIAN_POINT ( 'NONE',  ( 7.081057523560999378, -79.22598300536000693, -10.01287680343000019 ) ) ;
#49907=CARTESIAN_POINT ( 'NONE',  ( 12.71758670598766017, -17.93493368773965813, -1.809547514117120448 ) ) ;
#49909=CARTESIAN_POINT ( 'NONE',  ( 6.160028937834207241, -76.88236474970555889, 10.38583856661684379 ) ) ;
#49910=CARTESIAN_POINT ( 'NONE',  ( -3.009867212368674494, -75.84684136573420687, 12.37993388414874119 ) ) ;
#49911=ORIENTED_EDGE ( 'NONE', *, *, #3630, .F. ) ;
#49914=CARTESIAN_POINT ( 'NONE',  ( -10.42531124905999995, -18.73514851523999880, 7.624341765453999997 ) ) ;
#49915=CARTESIAN_POINT ( 'NONE',  ( 9.164385193226218362, -25.21567483134532139, 8.803702036953628962 ) ) ;
#49917=DIRECTION ( 'NONE',  ( -0.07798810159164812350, -0.04890177460086881506, -0.9957542229139761947 ) ) ;
#49923=CARTESIAN_POINT ( 'NONE',  ( 2.392485446417093264, -76.05844639573089694, 11.50375119131274992 ) ) ;
#49927=CARTESIAN_POINT ( 'NONE',  ( -6.282410744257000523, -75.96762204925410344, 10.58616248715999930 ) ) ;
#49929=EDGE_CURVE ( 'NONE', #3043, #16917, #40326, .T. ) ;
#49931=ADVANCED_FACE ( 'NONE', ( #34856 ), #50092, .F. ) ;
#49932=FACE_OUTER_BOUND ( 'NONE', #56560, .T. ) ;
#49935=CARTESIAN_POINT ( 'NONE',  ( -0.5999999998848000171, -23.14999999478999726, -11.79999999988000070 ) ) ;
#49936=ORIENTED_EDGE ( 'NONE', *, *, #356, .T. ) ;
#49944=CARTESIAN_POINT ( 'NONE',  ( -0.8385792221450999451, -2.855321851618000117, -3.712528424878000166 ) ) ;
#49945=VECTOR ( 'NONE', #10126, 999.9999999999998863 ) ;
#49947=CARTESIAN_POINT ( 'NONE',  ( -12.52582254643367499, -54.99059700767246284, -1.680974932891768914 ) ) ;
#49950=CARTESIAN_POINT ( 'NONE',  ( -12.77568181202000019, -25.26511628633999962, 0.5294980821347999855 ) ) ;
#49952=ORIENTED_EDGE ( 'NONE', *, *, #55708, .T. ) ;
#49955=CIRCLE ( 'NONE', #43362, 0.5000000000000006661 ) ;
#49956=ORIENTED_EDGE ( 'NONE', *, *, #18189, .F. ) ;
#49958=CARTESIAN_POINT ( 'NONE',  ( 9.783241737786999792, -24.53564621530999901, 7.961026681561000018 ) ) ;
#49962=CARTESIAN_POINT ( 'NONE',  ( 10.47513974136000137, -60.60361494148999384, 7.624776006180999488 ) ) ;
#49968=CARTESIAN_POINT ( 'NONE',  ( -9.355938762748150950, -25.17483711029779414, 8.610912454445188047 ) ) ;
#49972=FACE_OUTER_BOUND ( 'NONE', #40938, .T. ) ;
#49974=CARTESIAN_POINT ( 'NONE',  ( -9.924175329023000813, -75.86290228657999535, 8.344828977268999637 ) ) ;
#49975=CARTESIAN_POINT ( 'NONE',  ( -2.588288305445375137, -2.052526692832498334, -2.006457613103411752 ) ) ;
#49979=CARTESIAN_POINT ( 'NONE',  ( -7.956422463014998669, -24.52889896183999596, -9.787948076355000637 ) ) ;
#49980=CARTESIAN_POINT ( 'NONE',  ( -8.140250184790149390, -60.25160423311102420, 7.398464061237165268 ) ) ;
#49982=AXIS2_PLACEMENT_3D ( 'NONE', #9671, #4663, #9382 ) ;
#49988=CARTESIAN_POINT ( 'NONE',  ( 3.165411199172024848, -3.270833333333332593, 0.8506806241676669877 ) ) ;
#49989=CARTESIAN_POINT ( 'NONE',  ( -11.75000000000000000, -78.29999999999999716, 0.000000000000000000 ) ) ;
#49990=DIRECTION ( 'NONE',  ( 0.000000000000000000, -1.000000000000000000, 0.000000000000000000 ) ) ;
#49991=DIRECTION ( 'NONE',  ( -0.7071067811865475727, 0.000000000000000000, 0.7071067811865475727 ) ) ;
#49998=ORIENTED_EDGE ( 'NONE', *, *, #44849, .F. ) ;
#49999=CARTESIAN_POINT ( 'NONE',  ( 10.35453599130000057, -76.75783510652000530, -6.064947188958000446 ) ) ;
#50001=CARTESIAN_POINT ( 'NONE',  ( 0.000000000000000000, -46.43897132165000130, 0.000000000000000000 ) ) ;
#50003=DIRECTION ( 'NONE',  ( 0.000000000000000000, 0.000000000000000000, 1.000000000000000000 ) ) ;
#50004=CARTESIAN_POINT ( 'NONE',  ( 0.4254240051736215000, -1.635416666666666519, -3.250000000000000000 ) ) ;
#50007=CARTESIAN_POINT ( 'NONE',  ( 12.65989785480000229, -17.05665906540999899, 0.9744897697750000143 ) ) ;
#50010=CARTESIAN_POINT ( 'NONE',  ( -11.00000000000000000, -23.75000000000000000, 0.000000000000000000 ) ) ;
#50011=CARTESIAN_POINT ( 'NONE',  ( 9.310166272052999403, -53.66468533943000097, -8.596757084861000209 ) ) ;
#50013=CARTESIAN_POINT ( 'NONE',  ( 12.50000000000000000, -18.75000000310999937, -1.750000000000000000 ) ) ;
#50017=CARTESIAN_POINT ( 'NONE',  ( -12.48375848566000101, -60.17270426026000507, 1.669543623995999981 ) ) ;
#50019=CARTESIAN_POINT ( 'NONE',  ( 0.000000000000000000, -32.70420297070000260, 0.000000000000000000 ) ) ;
#50021=ORIENTED_EDGE ( 'NONE', *, *, #35084, .T. ) ;
#50026=CARTESIAN_POINT ( 'NONE',  ( -17.49999999998999911, -28.92928575306000383, -1.613072089525000228E-05 ) ) ;
#50027=ORIENTED_EDGE ( 'NONE', *, *, #49509, .F. ) ;
#50028=ORIENTED_EDGE ( 'NONE', *, *, #35628, .T. ) ;
#50029=CARTESIAN_POINT ( 'NONE',  ( -12.50000000000000000, -23.24999999688999708, -1.750000000000000000 ) ) ;
#50030=ORIENTED_EDGE ( 'NONE', *, *, #20733, .T. ) ;
#50034=DIRECTION ( 'NONE',  ( -1.000000000000000000, 0.000000000000000000, 0.000000000000000000 ) ) ;
#50035=EDGE_CURVE ( 'NONE', #37958, #54663, #946, .T. ) ;
#50036=CARTESIAN_POINT ( 'NONE',  ( 1.200170490671999879, -24.43405701997999913, -12.43444080551000042 ) ) ;
#50039=CARTESIAN_POINT ( 'NONE',  ( -4.723620464148000408, -78.23902343179999264, 10.90888302421999789 ) ) ;
#50040=VERTEX_POINT ( 'NONE', #20618 ) ;
#50041=ORIENTED_EDGE ( 'NONE', *, *, #52437, .T. ) ;
#50046=CIRCLE ( 'NONE', #11359, 1.750000000000000000 ) ;
#50048=DIRECTION ( 'NONE',  ( 0.000000000000000000, 0.000000000000000000, -1.000000000000000000 ) ) ;
#50049=CARTESIAN_POINT ( 'NONE',  ( -10.53003223722999948, -23.32452529362999982, 7.612971414713999962 ) ) ;
#50050=CARTESIAN_POINT ( 'NONE',  ( -1.243328516745999979, -77.44871687587999531, -12.73826093197000020 ) ) ;
#50052=ADVANCED_FACE ( 'NONE', ( #3472 ), #50482, .F. ) ;
#50053=DIRECTION ( 'NONE',  ( 0.000000000000000000, -1.000000000000000000, 0.000000000000000000 ) ) ;
#50054=CARTESIAN_POINT ( 'NONE',  ( 7.919595949288999570, -59.94999999969999749, 9.050966799188000067 ) ) ;
#50058=CARTESIAN_POINT ( 'NONE',  ( -11.75000000000000000, -78.29999999999999716, 0.000000000000000000 ) ) ;
#50064=CARTESIAN_POINT ( 'NONE',  ( 3.521688171515000132, -3.617922206379000194, 0.7298424208991000084 ) ) ;
#50066=CARTESIAN_POINT ( 'NONE',  ( 0.1577469407148825997, -23.75042584457689898, 11.00002392222777203 ) ) ;
#50067=CARTESIAN_POINT ( 'NONE',  ( -0.5962167095188589672, -18.77158755790547318, -10.98383273456533438 ) ) ;
#50068=B_SPLINE_CURVE_WITH_KNOTS ( 'NONE', 3,
 ( #22902, #40020, #32033, #44457, #4008, #54205, #17299, #5190 ),
 .UNSPECIFIED., .F., .F.,
 ( 4, 2, 2, 4 ),
 ( 0.000000000000000000, 0.4999999999999977796, 0.7499999999999988898, 1.000000000000000000 ),
 .UNSPECIFIED. ) ;
#50069=CARTESIAN_POINT ( 'NONE',  ( -11.75000000000000000, -77.70000000000000284, 0.000000000000000000 ) ) ;
#50071=AXIS2_PLACEMENT_3D ( 'NONE', #56259, #55089, #32920 ) ;
#50074=CARTESIAN_POINT ( 'NONE',  ( -3.129814719915999799, -78.41165560753999841, 12.62985940900000159 ) ) ;
#50077=CARTESIAN_POINT ( 'NONE',  ( -4.744667937345999675, -76.40032876540000473, 11.57788746584999906 ) ) ;
#50078=ORIENTED_EDGE ( 'NONE', *, *, #8781, .F. ) ;
#50079=CYLINDRICAL_SURFACE ( 'NONE', #4248, 1.750000000000000000 ) ;
#50082=CARTESIAN_POINT ( 'NONE',  ( 7.691893942754999713, -20.24546192895000019, -10.42272502865000128 ) ) ;
#50083=VECTOR ( 'NONE', #23069, 1000.000000000000000 ) ;
#50086=CARTESIAN_POINT ( 'NONE',  ( -1.488596180559999871, -0.8427806054948999703, -3.730054860412999940 ) ) ;
#50088=DIRECTION ( 'NONE',  ( -0.9999433559010179051, 0.000000000000000000, -0.01064354214585019887 ) ) ;
#50092=CONICAL_SURFACE ( 'NONE', #8542, 11.09999999881999955, 0.7853981633972997312 ) ;
#50094=ORIENTED_EDGE ( 'NONE', *, *, #35376, .F. ) ;
#50096=CARTESIAN_POINT ( 'NONE',  ( 0.000000000000000000, -13.07071424677999971, 0.000000000000000000 ) ) ;
#50098=ORIENTED_EDGE ( 'NONE', *, *, #46865, .T. ) ;
#50100=EDGE_LOOP ( 'NONE', ( #55679, #15893, #19726, #46036 ) ) ;
#50101=ORIENTED_EDGE ( 'NONE', *, *, #43060, .F. ) ;
#50102=CARTESIAN_POINT ( 'NONE',  ( -3.128637044992019334, -2.622704922558018126, -0.9068569082304414053 ) ) ;
#50104=DIRECTION ( 'NONE',  ( 0.000000000000000000, 0.000000000000000000, -1.000000000000000000 ) ) ;
#50106=ORIENTED_EDGE ( 'NONE', *, *, #56872, .F. ) ;
#50109=ORIENTED_EDGE ( 'NONE', *, *, #12669, .T. ) ;
#50115=DIRECTION ( 'NONE',  ( 0.7071067811865975328, -3.445410891335986341E-11, 0.7071067811864976127 ) ) ;
#50123=DIRECTION ( 'NONE',  ( 0.000000000000000000, 1.000000000000000000, 0.000000000000000000 ) ) ;
#50128=CARTESIAN_POINT ( 'NONE',  ( -1.750000000001000089, -59.55100836327999758, 12.60354432391999957 ) ) ;
#50129=FACE_OUTER_BOUND ( 'NONE', #11009, .T. ) ;
#50130=CARTESIAN_POINT ( 'NONE',  ( 0.5390150933987999382, -25.26260891652000140, 12.77520261005000002 ) ) ;
#50131=CARTESIAN_POINT ( 'NONE',  ( 11.02435598943671380, -79.24999999999995737, -4.903336795166640449 ) ) ;
#50133=CARTESIAN_POINT ( 'NONE',  ( -3.542934954918000034, -1.497403522604999981, -1.344521724440000066 ) ) ;
#50135=CARTESIAN_POINT ( 'NONE',  ( 12.70228545255524111, -24.82820680357308518, -1.205254117560517146 ) ) ;
#50137=CARTESIAN_POINT ( 'NONE',  ( 7.624341764943999955, -60.06485149430999826, -10.42531124854999902 ) ) ;
#50138=FACE_OUTER_BOUND ( 'NONE', #50321, .T. ) ;
#50139=ADVANCED_FACE ( 'NONE', ( #49523 ), #22345, .F. ) ;
#50142=DIRECTION ( 'NONE',  ( -0.7071067811865474617, 0.000000000000000000, 0.7071067811865474617 ) ) ;
#50147=ORIENTED_EDGE ( 'NONE', *, *, #4244, .T. ) ;
#50153=CARTESIAN_POINT ( 'NONE',  ( 10.09635298636608880, -23.52373519997163953, -7.644087781972076279 ) ) ;
#50154=DIRECTION ( 'NONE',  ( 0.000000000000000000, 0.000000000000000000, 1.000000000000000000 ) ) ;
#50155=CARTESIAN_POINT ( 'NONE',  ( -10.29607860738999925, -77.70636465244999158, 7.334573225905999472 ) ) ;
#50159=CARTESIAN_POINT ( 'NONE',  ( 10.98362417419999915, -18.84999999999999787, 0.5999999999999999778 ) ) ;
#50164=ORIENTED_EDGE ( 'NONE', *, *, #30455, .F. ) ;
#50166=CARTESIAN_POINT ( 'NONE',  ( -2.062670899148999926, -18.69360374348000065, 12.83044039274999903 ) ) ;
#50168=CIRCLE ( 'NONE', #53914, 14.00000000000000000 ) ;
#50170=DIRECTION ( 'NONE',  ( 0.7071067811865474617, 0.000000000000000000, -0.7071067811865474617 ) ) ;
#50171=ADVANCED_FACE ( 'NONE', ( #26764 ), #26469, .F. ) ;
#50174=DIRECTION ( 'NONE',  ( 1.000000000000000000, 0.000000000000000000, 0.000000000000000000 ) ) ;
#50175=CARTESIAN_POINT ( 'NONE',  ( 10.27340958483875077, -24.06161210422248331, -7.712164009431025313 ) ) ;
#50178=ORIENTED_EDGE ( 'NONE', *, *, #41362, .T. ) ;
#50184=EDGE_CURVE ( 'NONE', #35775, #19870, #44793, .T. ) ;
#50186=ORIENTED_EDGE ( 'NONE', *, *, #30115, .T. ) ;
#50188=CARTESIAN_POINT ( 'NONE',  ( 11.05577208806000122, -76.69928192833000935, -4.921212746988999243 ) ) ;
#50190=CARTESIAN_POINT ( 'NONE',  ( -3.494184512671483667, -2.339737559012720070, 0.4184823038404273388 ) ) ;
#50192=CARTESIAN_POINT ( 'NONE',  ( -3.417863094299999904, -78.38065028396999878, 11.50296535110000029 ) ) ;
#50193=DIRECTION ( 'NONE',  ( 0.9999999999999998890, 1.433670265775999799E-08, 0.000000000000000000 ) ) ;
#50196=CARTESIAN_POINT ( 'NONE',  ( -10.97112726228940360, -77.01578936740024517, 5.028334835961087990 ) ) ;
#50198=ORIENTED_EDGE ( 'NONE', *, *, #9869, .T. ) ;
#50200=DIRECTION ( 'NONE',  ( 0.7071067811865475727, 0.000000000000000000, 0.7071067811865475727 ) ) ;
#50202=VECTOR ( 'NONE', #42930, 1000.000000000000227 ) ;
#50207=CARTESIAN_POINT ( 'NONE',  ( 9.107554314083696312, -76.00402216969793301, 7.423553679711462294 ) ) ;
#50210=ORIENTED_EDGE ( 'NONE', *, *, #6837, .F. ) ;
#50211=CARTESIAN_POINT ( 'NONE',  ( 7.709154088328855181, -18.07253195914803356, -9.998702477107977771 ) ) ;
#50214=CARTESIAN_POINT ( 'NONE',  ( -13.98934701867000108, -46.22186981632000169, -1.420930502821999868E-05 ) ) ;
#50215=CARTESIAN_POINT ( 'NONE',  ( -5.036310450962679042, -76.28943874799483638, -10.61677181351809374 ) ) ;
#50220=CARTESIAN_POINT ( 'NONE',  ( 9.101506735347001609, -17.11932813898000205, -8.485532457246998561 ) ) ;
#50223=EDGE_CURVE ( 'NONE', #11513, #6154, #23641, .T. ) ;
#50228=AXIS2_PLACEMENT_3D ( 'NONE', #47825, #24788, #37780 ) ;
#50233=CARTESIAN_POINT ( 'NONE',  ( -2.809159726167000048, -3.306933523454000046, -2.568020482856000264 ) ) ;
#50235=DIRECTION ( 'NONE',  ( 0.000000000000000000, -1.000000000000000000, 0.000000000000000000 ) ) ;
#50237=CARTESIAN_POINT ( 'NONE',  ( -12.50659871789747513, -61.77347219457126215, 0.3508073943569843256 ) ) ;
#50243=AXIS2_PLACEMENT_3D ( 'NONE', #6540, #38699, #42563 ) ;
#50247=CARTESIAN_POINT ( 'NONE',  ( 7.606021324617000090, -60.22158946241999899, 10.52692925329000140 ) ) ;
#50252=CARTESIAN_POINT ( 'NONE',  ( 7.919595949288999570, -59.94999999969999749, 9.050966799188000067 ) ) ;
#50253=EDGE_CURVE ( 'NONE', #49445, #46028, #9366, .T. ) ;
#50255=CARTESIAN_POINT ( 'NONE',  ( 7.624341764943999955, -60.06485149430999826, -10.42531124854999902 ) ) ;
#50256=EDGE_LOOP ( 'NONE', ( #45366, #58255, #49153, #38536 ) ) ;
#50259=DIRECTION ( 'NONE',  ( -0.7071067811865474617, -0.7071067811865474617, 4.786452749996315941E-09 ) ) ;
#50266=VECTOR ( 'NONE', #32325, 999.9999999999998863 ) ;
#50268=CARTESIAN_POINT ( 'NONE',  ( 12.70451647738967793, -61.35458569080387292, 1.498866843944270943 ) ) ;
#50269=CARTESIAN_POINT ( 'NONE',  ( -8.171144579303600608, -60.14010097497902052, 7.364280830346968010 ) ) ;
#50271=ORIENTED_EDGE ( 'NONE', *, *, #36765, .T. ) ;
#50276=CARTESIAN_POINT ( 'NONE',  ( -10.13402152809999990, -18.27694524397999842, 7.647754144029000223 ) ) ;
#50277=CARTESIAN_POINT ( 'NONE',  ( -5.917523019358058356, -78.38333333333331154, -10.26699006316253282 ) ) ;
#50278=DIRECTION ( 'NONE',  ( 0.000000000000000000, -1.000000000000000000, 4.107825191113000313E-14 ) ) ;
#50279=CARTESIAN_POINT ( 'NONE',  ( -0.7620112687051859846, -2.857683719944371425, -3.439605056318825405 ) ) ;
#50287=CARTESIAN_POINT ( 'NONE',  ( 8.838834764832000701, -23.25000000000000000, 8.838834764832000701 ) ) ;
#50290=AXIS2_PLACEMENT_3D ( 'NONE', #40156, #49622, #22739 ) ;
#50291=CARTESIAN_POINT ( 'NONE',  ( 8.958641849965999882, -25.20112647804999995, -8.950065109822000764 ) ) ;
#50292=CARTESIAN_POINT ( 'NONE',  ( -7.648026766753000416, -60.05000000550000294, 10.12290050090999927 ) ) ;
#50293=LINE ( 'NONE', #9846, #58138 ) ;
#50294=CARTESIAN_POINT ( 'NONE',  ( -7.861037107713870320, -54.33338873116260004, -10.10708465676067114 ) ) ;
#50299=VECTOR ( 'NONE', #27724, 1000.000000000000114 ) ;
#50300=DIRECTION ( 'NONE',  ( 0.000000000000000000, 0.000000000000000000, 1.000000000000000000 ) ) ;
#50301=B_SPLINE_SURFACE_WITH_KNOTS ( 'NONE', 3, 3, ( 
 ( #3804, #21808, #40106, #39810 ),
 ( #38951, #49272, #39529, #30075 ),
 ( #30939, #53701, #13237, #22092 ),
 ( #7944, #48125, #25372, #7658 ),
 ( #2946, #58119, #57825, #4095 ),
 ( #53114, #17681, #31231, #17382 ),
 ( #12941, #16815, #12661, #43387 ),
 ( #20946, #35369, #43970, #12094 ) ),
 .UNSPECIFIED., .F., .F., .F.,
 ( 4, 1, 1, 1, 1, 4 ),
 ( 4, 4 ),
 ( -0.01200407345746999990, 0.000000000000000000, 0.3333333333333000081, 0.6666666666667000474, 1.000000000000000000, 1.011997855551999947 ),
 ( -0.3559705542741999906, 1.355970554273999928 ),
 .UNSPECIFIED. ) ;
#50305=CARTESIAN_POINT ( 'NONE',  ( -7.655984445823650120, -23.70337239445911237, 10.06694410249481031 ) ) ;
#50309=CARTESIAN_POINT ( 'NONE',  ( -1.980532758766000212, -19.23743349341999931, -12.80088938805999987 ) ) ;
#50311=ORIENTED_EDGE ( 'NONE', *, *, #53886, .F. ) ;
#50320=ORIENTED_EDGE ( 'NONE', *, *, #18845, .F. ) ;
#50321=EDGE_LOOP ( 'NONE', ( #54523, #3533, #38735 ) ) ;
#50322=DIRECTION ( 'NONE',  ( 0.000000000000000000, 0.000000000000000000, 1.000000000000000000 ) ) ;
#50327=ADVANCED_FACE ( 'NONE', ( #17631, #22047 ), #48930, .T. ) ;
#50328=EDGE_LOOP ( 'NONE', ( #57475, #20738, #2888, #5367 ) ) ;
#50329=EDGE_LOOP ( 'NONE', ( #56080, #9347, #33873, #2672 ) ) ;
#50330=CARTESIAN_POINT ( 'NONE',  ( -12.54238271617935041, -18.47146427654275413, -1.749799002659384817 ) ) ;
#50331=DIRECTION ( 'NONE',  ( -1.000000000000000000, 0.000000000000000000, 0.000000000000000000 ) ) ;
#50336=DIRECTION ( 'NONE',  ( 0.000000000000000000, 1.000000000000000000, 0.000000000000000000 ) ) ;
#50338=CARTESIAN_POINT ( 'NONE',  ( -9.082935096011000908, -76.89367046626000501, -9.017176053435999705 ) ) ;
#50340=CARTESIAN_POINT ( 'NONE',  ( -12.87022657272000004, -22.78485473281999774, -2.062597299672999540 ) ) ;
#50341=CARTESIAN_POINT ( 'NONE',  ( -9.369164850722000892, -60.04999999966999980, -7.601397897754999633 ) ) ;
#50342=CARTESIAN_POINT ( 'NONE',  ( -8.187117628376695322, -76.63618780861736468, 8.428237639695421279 ) ) ;
#50346=CLOSED_SHELL ( 'NONE', ( #37665, #5883, #42105, #23762, #15256, #14075, #43788, #1914, #13204, #38228, #43812 ) ) ;
#50347=CARTESIAN_POINT ( 'NONE',  ( 3.250000000000000000, -2.850000000000000089, 0.000000000000000000 ) ) ;
#50348=CARTESIAN_POINT ( 'NONE',  ( -1.250000000000000000, -23.25000000000000000, 12.00000000000000000 ) ) ;
#50351=EDGE_CURVE ( 'NONE', #16006, #41301, #13258, .T. ) ;
#50352=DIRECTION ( 'NONE',  ( 1.000000000000000000, 0.000000000000000000, 0.000000000000000000 ) ) ;
#50354=CARTESIAN_POINT ( 'NONE',  ( 3.702420020526000055, -2.585946431073999907, 0.8821385418971999792 ) ) ;
#50356=ORIENTED_EDGE ( 'NONE', *, *, #48364, .F. ) ;
#50359=PLANE ( 'NONE',  #45662 ) ;
#50361=CARTESIAN_POINT ( 'NONE',  ( 12.56884868898000107, -76.67718304534999163, -3.366471670097000324 ) ) ;
#50364=CARTESIAN_POINT ( 'NONE',  ( 9.728739490418719882, -78.49536251359755568, 6.586777397229446329 ) ) ;
#50370=CARTESIAN_POINT ( 'NONE',  ( -4.514525519966182010, -76.29316198124988091, -10.84781437541200155 ) ) ;
#50372=CARTESIAN_POINT ( 'NONE',  ( -1.704789469148189296, -18.29653838474041549, 12.53199752960649072 ) ) ;
#50375=CARTESIAN_POINT ( 'NONE',  ( -0.1204595238885999980, -0.6604060260386999115, 3.497926457646999943 ) ) ;
#50383=VERTEX_POINT ( 'NONE', #54818 ) ;
#50384=EDGE_LOOP ( 'NONE', ( #746, #56332, #45764 ) ) ;
#50386=VECTOR ( 'NONE', #55374, 1000.000000000000114 ) ;
#50391=EDGE_LOOP ( 'NONE', ( #50837, #11794, #19456, #4466, #27759, #54195 ) ) ;
#50392=VERTEX_POINT ( 'NONE', #19980 ) ;
#50393=CARTESIAN_POINT ( 'NONE',  ( -2.089133851730829328, -2.669960546984883276, -2.490096624221278088 ) ) ;
#50396=CARTESIAN_POINT ( 'NONE',  ( 0.000000000000000000, -2.949999999935999817, -12.84999999993999964 ) ) ;
#50397=VERTEX_POINT ( 'NONE', #15539 ) ;
#50399=EDGE_LOOP ( 'NONE', ( #18220, #40703, #11902, #25827, #14995 ) ) ;
#50400=DIRECTION ( 'NONE',  ( -0.9957542233426791567, 0.04890176637352901257, -0.07798810127683841742 ) ) ;
#50405=DIRECTION ( 'NONE',  ( 0.000000000000000000, 0.000000000000000000, -1.000000000000000000 ) ) ;
#50406=CARTESIAN_POINT ( 'NONE',  ( 12.50000000000000000, -23.24999999688999708, 1.750000000000000000 ) ) ;
#50411=DIRECTION ( 'NONE',  ( -0.7071067811865475727, 0.000000000000000000, 0.7071067811865475727 ) ) ;
#50413=CARTESIAN_POINT ( 'NONE',  ( -3.100723057438616426, -78.05736609856147368, -11.66987326451405416 ) ) ;
#50415=CARTESIAN_POINT ( 'NONE',  ( -12.59682398758999966, -18.61262488659000169, 1.801644812721000077 ) ) ;
#50416=EDGE_CURVE ( 'NONE', #54024, #11618, #35900, .T. ) ;
#50422=CARTESIAN_POINT ( 'NONE',  ( -17.50000000000000000, -13.07071424677999971, -2.007265881287999855E-13 ) ) ;
#50423=AXIS2_PLACEMENT_3D ( 'NONE', #43542, #48556, #3107 ) ;
#50425=CARTESIAN_POINT ( 'NONE',  ( -2.099388381696000023E-14, -0.04999999937963000435, 0.000000000000000000 ) ) ;
#50426=CARTESIAN_POINT ( 'NONE',  ( -1.044910384896000188, -25.05526494194999643, -12.77260826199000121 ) ) ;
#50427=DIRECTION ( 'NONE',  ( 0.000000000000000000, -1.000000000000000000, 0.000000000000000000 ) ) ;
#50428=LINE ( 'NONE', #15269, #41821 ) ;
#50429=CARTESIAN_POINT ( 'NONE',  ( 0.9781264271459000348, -53.85968856090000401, -12.65967462873999949 ) ) ;
#50434=CARTESIAN_POINT ( 'NONE',  ( 9.195259559916998171, -76.94960844227999530, -7.805988517003000560 ) ) ;
#50436=EDGE_CURVE ( 'NONE', #49641, #4635, #42325, .T. ) ;
#50442=CARTESIAN_POINT ( 'NONE',  ( 12.54901566175999861, -53.79264670667999582, -0.4731578885121000555 ) ) ;
#50443=DIRECTION ( 'NONE',  ( 1.000000000000000000, 0.000000000000000000, 0.000000000000000000 ) ) ;
#50444=FACE_OUTER_BOUND ( 'NONE', #37592, .T. ) ;
#50445=CARTESIAN_POINT ( 'NONE',  ( -0.5536397579754658294, -76.42123714547000191, -11.80639474213326601 ) ) ;
#50447=ORIENTED_EDGE ( 'NONE', *, *, #56786, .T. ) ;
#50449=PLANE ( 'NONE',  #44504 ) ;
#50451=DIRECTION ( 'NONE',  ( 0.000000000000000000, 0.000000000000000000, -1.000000000000000000 ) ) ;
#50452=EDGE_CURVE ( 'NONE', #393, #28471, #55728, .T. ) ;
#50453=ORIENTED_EDGE ( 'NONE', *, *, #18945, .F. ) ;
#50456=DIRECTION ( 'NONE',  ( 1.000000000000000000, 0.000000000000000000, 0.000000000000000000 ) ) ;
#50457=VERTEX_POINT ( 'NONE', #24401 ) ;
#50461=CARTESIAN_POINT ( 'NONE',  ( 8.803747447747934274, -62.01568152305735993, -9.164340453748428317 ) ) ;
#50463=DIRECTION ( 'NONE',  ( 0.000000000000000000, -1.000000000000000000, 0.000000000000000000 ) ) ;
#50464=CIRCLE ( 'NONE', #1460, 12.50000000000000000 ) ;
#50467=CARTESIAN_POINT ( 'NONE',  ( 12.82202470518000048, -55.37373556845999900, 2.066041976111999467 ) ) ;
#50469=CARTESIAN_POINT ( 'NONE',  ( -12.54901606605999831, -25.00731603500000233, -0.4733145588205000531 ) ) ;
#50473=CARTESIAN_POINT ( 'NONE',  ( -1.003693375988829573, -17.03776007889603861, -12.70247752664623242 ) ) ;
#50479=DIRECTION ( 'NONE',  ( -1.000000000000000000, 0.000000000000000000, 0.000000000000000000 ) ) ;
#50480=CARTESIAN_POINT ( 'NONE',  ( -7.450482419345999752, -76.05593601512001101, -9.799277032148999922 ) ) ;
#50482=B_SPLINE_SURFACE_WITH_KNOTS ( 'NONE', 3, 3, ( 
 ( #57487, #39485, #25325, #25040 ),
 ( #56635, #8190, #21759, #35032 ),
 ( #43062, #16480, #38618, #39765 ),
 ( #44209, #52778, #30612, #25901 ),
 ( #2621, #43343, #25613, #57778 ),
 ( #3759, #48360, #57202, #34750 ),
 ( #43925, #39187, #16770, #16194 ),
 ( #21478, #17051, #29740, #53066 ),
 ( #12332, #56922, #48646, #34171 ),
 ( #17333, #35321, #11485, #29456 ),
 ( #30320, #47513, #2899, #52207 ),
 ( #11763, #47792, #20900, #38903 ),
 ( #34460, #52491, #12048, #30029 ),
 ( #48082, #7613, #43634, #3196 ),
 ( #21186, #13488, #40950, #22939 ),
 ( #49223, #4345, #58368, #45686 ),
 ( #40658, #12897, #31778, #8772 ) ),
 .UNSPECIFIED., .F., .F., .F.,
 ( 4, 1, 1, 1, 1, 1, 1, 1, 1, 1, 1, 1, 1, 1, 4 ),
 ( 4, 4 ),
 ( -0.01011837001259000002, 0.000000000000000000, 0.08333333333333001192, 0.1666666666667000196, 0.2500000000000000000, 0.3333333333333000081, 0.4166666666666999919, 0.5000000000000000000, 0.5833333333333000637, 0.6666666666667000474, 0.7500000000000000000, 0.8333333333333000637, 0.9166666666667000474, 1.000000000000000000, 1.010372850415000023 ),
 ( -0.3559705548695000221, 1.357613361088000126 ),
 .UNSPECIFIED. ) ;
#50483=CARTESIAN_POINT ( 'NONE',  ( -0.2035211792613734194, -2.228899868708034582, 3.513002120467708433 ) ) ;
#50485=CARTESIAN_POINT ( 'NONE',  ( -3.911342194028000208, -78.61650197717000310, -11.62327352135999980 ) ) ;
#50488=CARTESIAN_POINT ( 'NONE',  ( 3.064790515199006471, -2.824239762174677537, -1.081059584728839562 ) ) ;
#50489=CARTESIAN_POINT ( 'NONE',  ( -3.836625960323930773, -77.14921398509360984, -11.44188731050598129 ) ) ;
#50490=CIRCLE ( 'NONE', #46714, 13.86363636363999952 ) ;
#50491=ORIENTED_EDGE ( 'NONE', *, *, #30847, .T. ) ;
#50493=AXIS2_PLACEMENT_3D ( 'NONE', #34622, #8059, #44079 ) ;
#50497=CARTESIAN_POINT ( 'NONE',  ( 3.145445771509000288, -2.093880151312000226, 2.255325989060000147 ) ) ;
#50500=CARTESIAN_POINT ( 'NONE',  ( 4.500613759774078737, -76.04318847295724026, 10.85354368999166574 ) ) ;
#50503=ORIENTED_EDGE ( 'NONE', *, *, #54978, .F. ) ;
#50508=EDGE_CURVE ( 'NONE', #17378, #48346, #23806, .T. ) ;
#50510=DIRECTION ( 'NONE',  ( 0.000000000000000000, -1.000000000000000000, 0.000000000000000000 ) ) ;
#50511=CARTESIAN_POINT ( 'NONE',  ( 12.50657384761460378, -17.02752583206956416, -0.3552644805215970925 ) ) ;
#50512=CARTESIAN_POINT ( 'NONE',  ( -11.99999999979999821, -18.85000000927000130, -0.7999999997951999786 ) ) ;
#50513=CARTESIAN_POINT ( 'NONE',  ( 7.646091287767998956, -18.29149945126999910, -10.13691902392999999 ) ) ;
#50514=CARTESIAN_POINT ( 'NONE',  ( -9.369164850722000892, -55.54999999966999980, 7.601397897754999633 ) ) ;
#50517=CARTESIAN_POINT ( 'NONE',  ( 12.70253230845987957, -53.82944272757063686, 0.9891673677798649145 ) ) ;
#50518=CARTESIAN_POINT ( 'NONE',  ( 12.50745077485999879, -53.80005551680000053, -2.012158279073999839E-09 ) ) ;
#50519=CARTESIAN_POINT ( 'NONE',  ( -7.396362990145566307, -77.02553451721301769, -9.545941378553289169 ) ) ;
#50522=EDGE_CURVE ( 'NONE', #21905, #37950, #29107, .T. ) ;
#50524=CARTESIAN_POINT ( 'NONE',  ( 0.000000000000000000, -72.89999999999999147, 0.000000000000000000 ) ) ;
#50529=CARTESIAN_POINT ( 'NONE',  ( -12.50485692592790166, -61.66593462659078995, 0.6924071803398014202 ) ) ;
#50536=LINE ( 'NONE', #13622, #21767 ) ;
#50539=CARTESIAN_POINT ( 'NONE',  ( 10.01676216528999852, -60.00941514989000325, 7.658899892539000831 ) ) ;
#50541=AXIS2_PLACEMENT_3D ( 'NONE', #44424, #3975, #58002 ) ;
#50546=ORIENTED_EDGE ( 'NONE', *, *, #4068, .T. ) ;
#50550=ADVANCED_FACE ( 'NONE', ( #10536, #9952 ), #10835, .T. ) ;
#50557=CARTESIAN_POINT ( 'NONE',  ( -7.618386461942000309, -23.22712559346000205, -10.53495196323000016 ) ) ;
#50558=CARTESIAN_POINT ( 'NONE',  ( 12.58335110165999993, -57.05111654290000445, -1.667961430005999945 ) ) ;
#50565=CARTESIAN_POINT ( 'NONE',  ( -2.598917237794094337, -3.447916666666665630, 1.997276839918461722 ) ) ;
#50566=CARTESIAN_POINT ( 'NONE',  ( -7.220923959705244144, -78.37291666666665435, -9.396085398178621872 ) ) ;
#50567=CARTESIAN_POINT ( 'NONE',  ( 3.250000000000000000, -1.250000000000000000, 0.000000000000000000 ) ) ;
#50568=CARTESIAN_POINT ( 'NONE',  ( 2.928645267525979090, -2.450581852303367558, -2.077595690244096627 ) ) ;
#50576=EDGE_CURVE ( 'NONE', #36474, #27203, #1113, .T. ) ;
#50578=CARTESIAN_POINT ( 'NONE',  ( -7.995796640818024770, -55.11315380192719005, 7.555116226634187804 ) ) ;
#50579=B_SPLINE_CURVE_WITH_KNOTS ( 'NONE', 3,
 ( #16563, #41034, #4433, #8859, #36884, #54618 ),
 .UNSPECIFIED., .F., .F.,
 ( 4, 1, 1, 4 ),
 ( 0.000000000000000000, 0.3333333333333000081, 0.6666666666667000474, 1.000000000000000000 ),
 .UNSPECIFIED. ) ;
#50584=CARTESIAN_POINT ( 'NONE',  ( -1.250000000000000000, -60.04999999966999980, 12.50000000000000000 ) ) ;
#50586=CARTESIAN_POINT ( 'NONE',  ( -9.355955347527174837, -53.62516908766477997, -8.610895743755770937 ) ) ;
#50587=B_SPLINE_CURVE_WITH_KNOTS ( 'NONE', 3,
 ( #28314, #32163, #37473, #55494, #5319, #46366 ),
 .UNSPECIFIED., .F., .F.,
 ( 4, 1, 1, 4 ),
 ( 0.000000000000000000, 0.3333333333333000081, 0.6666666666667000474, 1.000000000000000000 ),
 .UNSPECIFIED. ) ;
#50588=AXIS2_PLACEMENT_3D ( 'NONE', #16218, #44232, #17363 ) ;
#50590=CARTESIAN_POINT ( 'NONE',  ( -10.42531124905999995, -23.26485148473999942, -7.624341765453999997 ) ) ;
#50591=VECTOR ( 'NONE', #14030, 1000.000000000000000 ) ;
#50592=AXIS2_PLACEMENT_3D ( 'NONE', #45797, #49636, #13304 ) ;
#50593=CARTESIAN_POINT ( 'NONE',  ( 9.676723759786998613, -78.80221383193000406, 8.603871787294998796 ) ) ;
#50595=CIRCLE ( 'NONE', #21450, 30.49999999999998934 ) ;
#50603=DIRECTION ( 'NONE',  ( 0.000000000000000000, -1.000000000000000000, 0.000000000000000000 ) ) ;
#50605=ORIENTED_EDGE ( 'NONE', *, *, #23281, .F. ) ;
#50606=CARTESIAN_POINT ( 'NONE',  ( 14.00000000000000000, -45.89236309322999574, 1.352041732613999901E-05 ) ) ;
#50611=ORIENTED_EDGE ( 'NONE', *, *, #44033, .F. ) ;
#50613=VERTEX_POINT ( 'NONE', #43320 ) ;
#50614=EDGE_LOOP ( 'NONE', ( #23728, #6589, #26112, #53490 ) ) ;
#50615=CARTESIAN_POINT ( 'NONE',  ( 1.933504092460000212, -18.59593152724999854, 12.70940235707999832 ) ) ;
#50616=CARTESIAN_POINT ( 'NONE',  ( 12.00000000000000000, -60.04999999966999980, -1.250000000000000000 ) ) ;
#50621=CARTESIAN_POINT ( 'NONE',  ( 0.000000000000000000, 4.040000000000000036, 0.000000000000000000 ) ) ;
#50622=EDGE_LOOP ( 'NONE', ( #14632, #10963, #15363, #22790 ) ) ;
#50628=CARTESIAN_POINT ( 'NONE',  ( 0.1380878923674745407, -62.02734402291400784, -12.70555840937129943 ) ) ;
#50633=CARTESIAN_POINT ( 'NONE',  ( -3.187445619818999987, -77.81332093041999087, 12.55797944092000051 ) ) ;
#50636=DIRECTION ( 'NONE',  ( 0.7071067811865475727, 0.000000000000000000, 0.7071067811865475727 ) ) ;
#50638=CARTESIAN_POINT ( 'NONE',  ( -6.829991769570769478, -76.62375042572244865, 9.568360097740603365 ) ) ;
#50640=CONICAL_SURFACE ( 'NONE', #1629, 10.29999999923999887, 0.7853981633972997312 ) ;
#50646=CYLINDRICAL_SURFACE ( 'NONE', #5353, 12.50000000000000000 ) ;
#50647=CARTESIAN_POINT ( 'NONE',  ( 0.000000000000000000, -62.90094976977999863, 0.000000000000000000 ) ) ;
#50648=CARTESIAN_POINT ( 'NONE',  ( 1.911540947291000103, -3.185127687536000174, 3.291214574437999918 ) ) ;
#50651=CARTESIAN_POINT ( 'NONE',  ( -0.7664558997027911547, -3.499999999999999556, -3.353144190923705192 ) ) ;
#50653=CARTESIAN_POINT ( 'NONE',  ( 8.485281374238999419, -60.04999999966999980, 8.485281374238999419 ) ) ;
#50654=EDGE_CURVE ( 'NONE', #22997, #9420, #10645, .T. ) ;
#50655=CARTESIAN_POINT ( 'NONE',  ( 1.799501877759999813, -60.08917565288000162, 12.60552522438000089 ) ) ;
#50656=CARTESIAN_POINT ( 'NONE',  ( 12.52133763471539396, -18.07246868479867885, -1.618901767041418083 ) ) ;
#50659=B_SPLINE_CURVE_WITH_KNOTS ( 'NONE', 3,
 ( #6332, #55936, #10777, #29335, #42062, #14599 ),
 .UNSPECIFIED., .F., .F.,
 ( 4, 1, 1, 4 ),
 ( 0.000000000000000000, 0.3333333333333000081, 0.6666666666667000474, 1.000000000000000000 ),
 .UNSPECIFIED. ) ;
#50660=CARTESIAN_POINT ( 'NONE',  ( 13.86363636363000218, -69.16102867818000277, 1.277888278513000037E-05 ) ) ;
#50662=EDGE_CURVE ( 'NONE', #40049, #8187, #13459, .T. ) ;
#50663=CARTESIAN_POINT ( 'NONE',  ( -3.075839145942573793, -76.30340551261170390, -11.34163394545276837 ) ) ;
#50665=CARTESIAN_POINT ( 'NONE',  ( 8.768124086549999419, -55.65000000488999632, -7.919595949288999570 ) ) ;
#50680=DIRECTION ( 'NONE',  ( -1.000000000000000000, 0.000000000000000000, 0.000000000000000000 ) ) ;
#50682=ORIENTED_EDGE ( 'NONE', *, *, #35748, .F. ) ;
#50688=EDGE_LOOP ( 'NONE', ( #26614, #34674, #27632, #3754 ) ) ;
#50690=DIRECTION ( 'NONE',  ( 0.000000000000000000, -0.7071067811866525998, -0.7071067811864425456 ) ) ;
#50691=VERTEX_POINT ( 'NONE', #18780 ) ;
#50697=ADVANCED_FACE ( 'NONE', ( #45659 ), #13176, .F. ) ;
#50698=CARTESIAN_POINT ( 'NONE',  ( -8.485281374238999419, -55.54999999966999980, 8.485281374238999419 ) ) ;
#50699=CARTESIAN_POINT ( 'NONE',  ( 3.202161418990787212, -0.9218749995132479169, 1.046229558418831473 ) ) ;
#50702=CYLINDRICAL_SURFACE ( 'NONE', #53301, 3.600000000000000089 ) ;
#50705=CARTESIAN_POINT ( 'NONE',  ( -7.691916945423999508, -57.04634220890999785, -10.42274798266000069 ) ) ;
#50710=CARTESIAN_POINT ( 'NONE',  ( -11.98418414837124324, -77.95952000033295803, -0.9817159035101585829 ) ) ;
#50719=DIRECTION ( 'NONE',  ( 1.411450211591999950E-10, -6.386278974555000074E-09, -1.000000000000000000 ) ) ;
#50720=AXIS2_PLACEMENT_3D ( 'NONE', #1166, #23861, #28577 ) ;
#50721=LINE ( 'NONE', #51010, #21740 ) ;
#50722=CARTESIAN_POINT ( 'NONE',  ( -2.061613410425999771, -23.20570014476000154, -12.83797036855999885 ) ) ;
#50723=DIRECTION ( 'NONE',  ( -0.7071067811865475727, 0.000000000000000000, -0.7071067811865475727 ) ) ;
#50724=CARTESIAN_POINT ( 'NONE',  ( 1.072256020167000168, -2.194262446210000217, -3.316546452965000391 ) ) ;
#50725=CARTESIAN_POINT ( 'NONE',  ( 12.78037829248000001, -24.29316779390000036, 1.812823010630000065 ) ) ;
#50728=DIRECTION ( 'NONE',  ( 0.000000000000000000, -1.000000000000000000, 0.000000000000000000 ) ) ;
#50730=CARTESIAN_POINT ( 'NONE',  ( 1.669849926066999890, -60.17228600383999293, 12.48404299555999941 ) ) ;
#50731=CARTESIAN_POINT ( 'NONE',  ( -1.779623408260310846, -24.13630869023863568, -12.71471627657074066 ) ) ;
#50732=CARTESIAN_POINT ( 'NONE',  ( -1.684993323399000209, -75.86946921342000394, -11.94349415379999968 ) ) ;
#50737=CARTESIAN_POINT ( 'NONE',  ( 12.54980660771999901, -61.84777352133000505, -0.05651102257804999779 ) ) ;
#50739=DIRECTION ( 'NONE',  ( -0.7071067811865475727, 0.000000000000000000, -0.7071067811865475727 ) ) ;
#50741=CARTESIAN_POINT ( 'NONE',  ( 12.50000000000000000, -55.55000000209000177, 1.750000000000000000 ) ) ;
#50742=CARTESIAN_POINT ( 'NONE',  ( 7.954951288349001004, -60.04999999966999980, -9.722718241315000398 ) ) ;
#50747=LINE ( 'NONE', #7017, #29952 ) ;
#50748=ORIENTED_EDGE ( 'NONE', *, *, #33219, .F. ) ;
#50750=CARTESIAN_POINT ( 'NONE',  ( 8.768124086549999419, -55.65000000488999632, -7.919595949288999570 ) ) ;
#50751=ORIENTED_EDGE ( 'NONE', *, *, #57025, .F. ) ;
#50754=CARTESIAN_POINT ( 'NONE',  ( 7.764217752279196638, -61.05600304927079947, -10.21028588420891126 ) ) ;
#50756=EDGE_LOOP ( 'NONE', ( #40735, #34445, #51776, #54798 ) ) ;
#50758=B_SPLINE_CURVE_WITH_KNOTS ( 'NONE', 3,
 ( #56564, #53001, #29965, #43281, #21122, #4790, #57137, #34397, #16704, #9219 ),
 .UNSPECIFIED., .F., .F.,
 ( 4, 2, 2, 2, 4 ),
 ( 0.000000000000000000, 0.1250000000000028033, 0.2500000000000056066, 0.5000000000000012212, 1.000000000000000000 ),
 .UNSPECIFIED. ) ;
#50762=ORIENTED_EDGE ( 'NONE', *, *, #52987, .F. ) ;
#50763=CARTESIAN_POINT ( 'NONE',  ( 12.66001647282000064, -54.16746073337000666, 1.381678996660000047 ) ) ;
#50764=CARTESIAN_POINT ( 'NONE',  ( -7.601397897754999633, -23.25000000000000000, 9.369164850722000892 ) ) ;
#50766=CARTESIAN_POINT ( 'NONE',  ( -12.77301895549999955, -25.05186686373999905, -1.052127376137000025 ) ) ;
#50775=ORIENTED_EDGE ( 'NONE', *, *, #4415, .F. ) ;
#50776=CARTESIAN_POINT ( 'NONE',  ( -10.77133038182000035, -76.55754729621000365, -5.959359258312999508 ) ) ;
#50777=CARTESIAN_POINT ( 'NONE',  ( 0.5460188671879216971, -2.211847916353453236, 3.477752717589034592 ) ) ;
#50779=CARTESIAN_POINT ( 'NONE',  ( -3.417863094299999904, -78.41531695063000029, 11.50296535110000029 ) ) ;
#50783=CARTESIAN_POINT ( 'NONE',  ( 3.006733838401902670, -2.820045760104889165, -1.232120965224751563 ) ) ;
#50784=CARTESIAN_POINT ( 'NONE',  ( -11.90430176566012577, -78.06094887269661342, -1.649208845716615635 ) ) ;
#50786=EDGE_CURVE ( 'NONE', #50040, #22044, #10512, .T. ) ;
#50787=ORIENTED_EDGE ( 'NONE', *, *, #18085, .T. ) ;
#50789=CARTESIAN_POINT ( 'NONE',  ( 11.44417895085271475, -78.02916666666666856, -3.075537641221520069 ) ) ;
#50790=DIRECTION ( 'NONE',  ( 0.000000000000000000, -1.000000000000000000, 0.000000000000000000 ) ) ;
#50792=CARTESIAN_POINT ( 'NONE',  ( -3.708003915733999900, -3.317513707840999970, -1.109421345883999876 ) ) ;
#50795=CIRCLE ( 'NONE', #31879, 14.00000000000000000 ) ;
#50796=CARTESIAN_POINT ( 'NONE',  ( -10.58828373193520456, -76.16399079984034870, 5.094882559088077301 ) ) ;
#50799=ORIENTED_EDGE ( 'NONE', *, *, #36699, .F. ) ;
#50800=CARTESIAN_POINT ( 'NONE',  ( 10.54796701376999835, -75.84310348540464020, 6.346365727669000201 ) ) ;
#50801=CARTESIAN_POINT ( 'NONE',  ( 9.505949683908001546, -79.00000000000000000, -6.906476714433999575 ) ) ;
#50802=CARTESIAN_POINT ( 'NONE',  ( -1.538071403319991814, -76.91458333333332575, -11.75000000000000355 ) ) ;
#50804=EDGE_CURVE ( 'NONE', #55909, #37146, #48553, .T. ) ;
#50807=CARTESIAN_POINT ( 'NONE',  ( 9.636775127281000053, -17.55967715742000124, -7.948072248884999524 ) ) ;
#50808=CARTESIAN_POINT ( 'NONE',  ( 1.250000000000000000, -18.75000000000000000, 12.50000000000000000 ) ) ;
#50810=LINE ( 'NONE', #23051, #55018 ) ;
#50811=AXIS2_PLACEMENT_3D ( 'NONE', #23084, #689, #45247 ) ;
#50814=CARTESIAN_POINT ( 'NONE',  ( -3.680468777719496654, -77.85277880226108493, 11.44633469405415838 ) ) ;
#50819=CARTESIAN_POINT ( 'NONE',  ( 14.00000000000000000, -9.337822431690000258, 5.544480874192999735E-06 ) ) ;
#50823=ORIENTED_EDGE ( 'NONE', *, *, #27264, .F. ) ;
#50824=ORIENTED_EDGE ( 'NONE', *, *, #11193, .T. ) ;
#50827=VECTOR ( 'NONE', #33161, 1000.000000000000000 ) ;
#50831=CIRCLE ( 'NONE', #49871, 0.5000000000000006661 ) ;
#50833=CARTESIAN_POINT ( 'NONE',  ( 9.414507962652001183, -62.06263135892999827, 8.652357372810001834 ) ) ;
#50837=ORIENTED_EDGE ( 'NONE', *, *, #49719, .T. ) ;
#50839=ORIENTED_EDGE ( 'NONE', *, *, #57256, .T. ) ;
#50842=DIRECTION ( 'NONE',  ( 0.000000000000000000, 0.000000000000000000, -1.000000000000000000 ) ) ;
#50846=DIRECTION ( 'NONE',  ( 0.000000000000000000, 0.000000000000000000, 1.000000000000000000 ) ) ;
#50851=CARTESIAN_POINT ( 'NONE',  ( -7.622785526030999570, -23.78712283485999990, -10.47836401506999948 ) ) ;
#50856=VERTEX_POINT ( 'NONE', #8676 ) ;
#50857=DIRECTION ( 'NONE',  ( 0.9999999999999994449, -3.428909149164998022E-08, -7.232769372636995941E-12 ) ) ;
#50863=CARTESIAN_POINT ( 'NONE',  ( -1.847034434715450368, -2.667702848378502800, 3.076255871586204726 ) ) ;
#50870=ORIENTED_EDGE ( 'NONE', *, *, #25882, .F. ) ;
#50871=CARTESIAN_POINT ( 'NONE',  ( 2.065394024360999836, -60.22161432612999477, -12.82193048530000112 ) ) ;
#50876=CARTESIAN_POINT ( 'NONE',  ( -12.85140862681000051, -20.24439829998999940, 1.980464483675000054 ) ) ;
#50878=B_SPLINE_CURVE_WITH_KNOTS ( 'NONE', 3,
 ( #22402, #17099, #35978, #27114, #49583, #44547, #16821, #39816, #26521, #53119, #30945, #54002, #7950, #4101, #12667, #9, #31237, #25953 ),
 .UNSPECIFIED., .F., .F.,
 ( 4, 2, 2, 2, 2, 2, 2, 2, 4 ),
 ( 0.000000000000000000, 0.1250000000000000000, 0.2500000000000000000, 0.3750000000000000000, 0.5000000000000000000, 0.6250000000000000000, 0.7500000000000000000, 0.8750000000000000000, 1.000000000000000000 ),
 .UNSPECIFIED. ) ;
#50879=EDGE_CURVE ( 'NONE', #1186, #23001, #2052, .T. ) ;
#50881=DIRECTION ( 'NONE',  ( -0.7071067811865474617, 0.000000000000000000, 0.7071067811865474617 ) ) ;
#50884=FACE_OUTER_BOUND ( 'NONE', #30756, .T. ) ;
#50890=VECTOR ( 'NONE', #43893, 1000.000000000000114 ) ;
#50891=LINE ( 'NONE', #24305, #40295 ) ;
#50893=DIRECTION ( 'NONE',  ( 0.7071067811865475727, 0.000000000000000000, -0.7071067811865475727 ) ) ;
#50899=EDGE_LOOP ( 'NONE', ( #25247, #18275, #15668, #22749 ) ) ;
#50903=ORIENTED_EDGE ( 'NONE', *, *, #36496, .F. ) ;
#50908=ADVANCED_FACE ( 'NONE', ( #44397 ), #8380, .F. ) ;
#50911=VERTEX_POINT ( 'NONE', #39964 ) ;
#50917=CARTESIAN_POINT ( 'NONE',  ( -1.103931348463426776, -17.37916251878369778, 12.50298439259127292 ) ) ;
#50919=DIRECTION ( 'NONE',  ( -1.000000000000000000, 0.000000000000000000, 0.000000000000000000 ) ) ;
#50923=CARTESIAN_POINT ( 'NONE',  ( -12.71658872084999992, -23.31584731985000047, -1.931087888240000217 ) ) ;
#50925=CARTESIAN_POINT ( 'NONE',  ( 0.007752153121785848242, -76.57482323936264379, 11.74990054534275963 ) ) ;
#50927=CARTESIAN_POINT ( 'NONE',  ( -10.36221646771999971, -55.57876216348000042, 7.631895822728999690 ) ) ;
#50928=VECTOR ( 'NONE', #24664, 1000.000000000000000 ) ;
#50931=CARTESIAN_POINT ( 'NONE',  ( -7.620037552712999762, -18.79433113555000290, -10.53559761427999852 ) ) ;
#50937=CARTESIAN_POINT ( 'NONE',  ( -3.370587613551000228, -1.830292672027000078, 0.9429417476038000068 ) ) ;
#50941=LINE ( 'NONE', #45935, #45506 ) ;
#50942=CARTESIAN_POINT ( 'NONE',  ( -5.913068375556633782, -77.61521835660632007, 10.26311275136223244 ) ) ;
#50943=CARTESIAN_POINT ( 'NONE',  ( 12.54902678216000034, -61.80971938179000347, -0.4616712539286000339 ) ) ;
#50944=CARTESIAN_POINT ( 'NONE',  ( 1.799475304559999822, -57.04828923575999511, 12.69616050746999925 ) ) ;
#50945=CARTESIAN_POINT ( 'NONE',  ( -1.338697082642999803, -78.06479906940001001, -12.94399764267999942 ) ) ;
#50947=CARTESIAN_POINT ( 'NONE',  ( 1.250000000000000000, -60.04999999966999980, -12.50000000000000000 ) ) ;
#50948=CARTESIAN_POINT ( 'NONE',  ( -1.250000000000000000, -18.75000000000000000, 12.00000000000000000 ) ) ;
#50964=PLANE ( 'NONE',  #35915 ) ;
#50965=CARTESIAN_POINT ( 'NONE',  ( 12.00000000000000000, -75.80000000000001137, -2.990830162875999918E-13 ) ) ;
#50968=EDGE_LOOP ( 'NONE', ( #6781, #61, #23566 ) ) ;
#50970=ORIENTED_EDGE ( 'NONE', *, *, #46657, .T. ) ;
#50974=ORIENTED_EDGE ( 'NONE', *, *, #57349, .T. ) ;
#50976=LINE ( 'NONE', #46267, #24199 ) ;
#50979=CARTESIAN_POINT ( 'NONE',  ( -7.627487525399000212, -55.50221245779999890, 10.35845608624000036 ) ) ;
#50986=CARTESIAN_POINT ( 'NONE',  ( 6.688842324857636079, -78.77930637062392805, 10.27946156281801571 ) ) ;
#50990=B_SPLINE_CURVE_WITH_KNOTS ( 'NONE', 3,
 ( #46968, #6496, #24506, #42522, #2090, #20088, #38080, #53388, #45140, #31521, #12371, #49264 ),
 .UNSPECIFIED., .F., .F.,
 ( 4, 2, 2, 2, 2, 4 ),
 ( 0.000000000000000000, 0.2500000000000000000, 0.5000000000000000000, 0.7500000000000000000, 0.8750000000000000000, 1.000000000000000000 ),
 .UNSPECIFIED. ) ;
#50991=CARTESIAN_POINT ( 'NONE',  ( -7.640030264136999705, -55.49283319101999723, -10.18491080491000034 ) ) ;
#50994=CARTESIAN_POINT ( 'NONE',  ( 5.036904867883157166, -76.53953860386789643, 10.61617713185392908 ) ) ;
#50995=AXIS2_PLACEMENT_3D ( 'NONE', #5410, #32255, #50300 ) ;
#51000=CARTESIAN_POINT ( 'NONE',  ( 0.5999999999999999778, -23.15000000000000213, -10.98362417419999915 ) ) ;
#51005=LINE ( 'NONE', #32089, #42441 ) ;
#51008=CARTESIAN_POINT ( 'NONE',  ( -7.919595949288999570, -55.64999999964999233, 9.050966799188000067 ) ) ;
#51009=CARTESIAN_POINT ( 'NONE',  ( 0.000000000000000000, -0.2000000000000000111, 0.000000000000000000 ) ) ;
#51010=CARTESIAN_POINT ( 'NONE',  ( -10.42531125068999920, -23.26485145404000221, 7.624341767093000044 ) ) ;
#51017=EDGE_CURVE ( 'NONE', #12253, #34855, #53605, .T. ) ;
#51018=CARTESIAN_POINT ( 'NONE',  ( -0.5135400118894599686, -25.17868533858884561, -12.70453250099059872 ) ) ;
#51019=CARTESIAN_POINT ( 'NONE',  ( 4.287309447300000187, -76.40953882784999962, -11.27418668890000042 ) ) ;
#51021=B_SPLINE_SURFACE_WITH_KNOTS ( 'NONE', 3, 3, ( 
 ( #38363, #2371, #33922, #51384 ),
 ( #47831, #56385, #56672, #6493 ),
 ( #21222, #33640, #38938, #11518 ),
 ( #11229, #10941, #7648, #51681 ),
 ( #29496, #29775, #12083, #39227 ),
 ( #25647, #16515, #42808, #38653 ),
 ( #29208, #57240, #7362, #47551 ),
 ( #2937, #52526, #47255, #7076 ),
 ( #33351, #25362, #34207, #25078 ),
 ( #43102, #43378, #42519, #2087 ),
 ( #56098, #15644, #6786, #58109 ),
 ( #27099, #53385, #22387, #48968 ),
 ( #13525, #31221, #35359, #4388 ),
 ( #17970, #12652, #26226, #21796 ),
 ( #53688, #44528, #57814, #17373 ),
 ( #12931, #4084, #4686, #40398 ),
 ( #57425, #44832, #17672, #45136 ) ),
 .UNSPECIFIED., .F., .F., .F.,
 ( 4, 1, 1, 1, 1, 1, 1, 1, 1, 1, 1, 1, 1, 1, 4 ),
 ( 4, 4 ),
 ( -0.01011786823685000003, 0.000000000000000000, 0.08333333333333001192, 0.1666666666667000196, 0.2500000000000000000, 0.3333333333333000081, 0.4166666666666999919, 0.5000000000000000000, 0.5833333333333000637, 0.6666666666667000474, 0.7500000000000000000, 0.8333333333333000637, 0.9166666666667000474, 1.000000000000000000, 1.010371592463000123 ),
 ( -0.3559705548529999986, 1.357613344763000107 ),
 .UNSPECIFIED. ) ;
#51025=DIRECTION ( 'NONE',  ( 0.000000000000000000, -1.000000000000000000, 0.000000000000000000 ) ) ;
#51027=CARTESIAN_POINT ( 'NONE',  ( 9.713032445540614290, -24.52293762691880374, -7.970418356296344875 ) ) ;
#51032=ORIENTED_EDGE ( 'NONE', *, *, #38408, .T. ) ;
#51033=EDGE_CURVE ( 'NONE', #34714, #47194, #21028, .T. ) ;
#51037=VERTEX_POINT ( 'NONE', #29582 ) ;
#51038=EDGE_CURVE ( 'NONE', #18787, #37143, #2954, .T. ) ;
#51042=ORIENTED_EDGE ( 'NONE', *, *, #30527, .T. ) ;
#51043=CIRCLE ( 'NONE', #9510, 13.94827586206999825 ) ;
#51046=CARTESIAN_POINT ( 'NONE',  ( -1.799475304559999822, -21.75171076523999858, 12.69616050742999924 ) ) ;
#51050=CARTESIAN_POINT ( 'NONE',  ( -13.94764600793045517, -33.10361340872000113, -0.1325532415315603119 ) ) ;
#51053=CARTESIAN_POINT ( 'NONE',  ( -7.970415440577942157, -54.27707676769661305, 9.713035532171998554 ) ) ;
#51054=CARTESIAN_POINT ( 'NONE',  ( 10.18248259416120938, -24.29095036201641022, -7.792398156871034764 ) ) ;
#51055=ORIENTED_EDGE ( 'NONE', *, *, #29337, .F. ) ;
#51056=AXIS2_PLACEMENT_3D ( 'NONE', #47486, #5842, #19433 ) ;
#51058=CARTESIAN_POINT ( 'NONE',  ( 9.621717086613145398, -24.62064477552555175, 8.060172378175863628 ) ) ;
#51059=VECTOR ( 'NONE', #55157, 1000.000000000000114 ) ;
#51061=CARTESIAN_POINT ( 'NONE',  ( 1.495357591784101325, -17.44123662637737837, -12.70444646759294116 ) ) ;
#51062=DIRECTION ( 'NONE',  ( 0.000000000000000000, -1.000000000000000000, 0.000000000000000000 ) ) ;
#51068=CARTESIAN_POINT ( 'NONE',  ( -6.024415200221000077, -76.43302873236000039, 10.73507988388000101 ) ) ;
#51072=CARTESIAN_POINT ( 'NONE',  ( 7.633501923173000137, -60.00104675737999571, -10.36289748054999826 ) ) ;
#51073=CARTESIAN_POINT ( 'NONE',  ( 9.000511195990998914, -79.36010635638000110, 8.067084866081000172 ) ) ;
#51077=CARTESIAN_POINT ( 'NONE',  ( 6.044717002249641702, -77.88304938243121001, 10.38669683180858527 ) ) ;
#51082=CARTESIAN_POINT ( 'NONE',  ( 10.42531124905999995, -23.26485148473999942, 7.624341765453999997 ) ) ;
#51083=LINE ( 'NONE', #42216, #38065 ) ;
#51084=CARTESIAN_POINT ( 'NONE',  ( -2.631409671617999990, -2.359887446210000128, -2.838311312396000208 ) ) ;
#51087=EDGE_CURVE ( 'NONE', #18726, #20471, #34996, .T. ) ;
#51088=CARTESIAN_POINT ( 'NONE',  ( -4.168399266842356177, -76.10359643177146438, 10.99644600840660758 ) ) ;
#51093=CARTESIAN_POINT ( 'NONE',  ( 12.71005379439144178, -24.29489531514696665, 1.687596143071744770 ) ) ;
#51096=CARTESIAN_POINT ( 'NONE',  ( -5.917523019358058356, -76.88333333333329733, -10.26699006316253282 ) ) ;
#51102=CARTESIAN_POINT ( 'NONE',  ( 10.18948933931999967, -18.78467389927000042, -7.645397892299000020 ) ) ;
#51108=CARTESIAN_POINT ( 'NONE',  ( 9.422193216980595309, -77.25680711302858583, 7.547672206128430261 ) ) ;
#51109=EDGE_CURVE ( 'NONE', #6729, #56422, #16285, .T. ) ;
#51112=FACE_OUTER_BOUND ( 'NONE', #40577, .T. ) ;
#51113=DIRECTION ( 'NONE',  ( 0.000000000000000000, 1.000000000000000000, 0.000000000000000000 ) ) ;
#51119=EDGE_LOOP ( 'NONE', ( #5858, #37005, #51565, #3244 ) ) ;
#51120=EDGE_LOOP ( 'NONE', ( #40422, #1487, #42690 ) ) ;
#51123=ORIENTED_EDGE ( 'NONE', *, *, #31916, .F. ) ;
#51124=CARTESIAN_POINT ( 'NONE',  ( 9.934825859755001431, -17.37633188891999936, 7.968960864700001423 ) ) ;
#51125=CARTESIAN_POINT ( 'NONE',  ( 0.000000000000000000, -9.295797029142999435, 0.000000000000000000 ) ) ;
#51126=CARTESIAN_POINT ( 'NONE',  ( -7.209704553483001099, -78.17110306078001258, 9.484251963051999468 ) ) ;
#51127=CARTESIAN_POINT ( 'NONE',  ( 9.830801209645999350, -60.89088557979000171, 7.765011064359000237 ) ) ;
#51131=ORIENTED_EDGE ( 'NONE', *, *, #41988, .F. ) ;
#51132=CARTESIAN_POINT ( 'NONE',  ( -8.532660243322236937, -25.12798380540222709, 9.433531203469305737 ) ) ;
#51133=VERTEX_POINT ( 'NONE', #52336 ) ;
#51136=AXIS2_PLACEMENT_3D ( 'NONE', #37027, #10180, #37902 ) ;
#51138=EDGE_CURVE ( 'NONE', #27991, #30862, #34592, .T. ) ;
#51140=CARTESIAN_POINT ( 'NONE',  ( -1.826212728074999792, -76.35785197021000670, -12.51879797594000010 ) ) ;
#51145=CARTESIAN_POINT ( 'NONE',  ( 2.062673488738000049, -60.12452529330000317, -12.82904091341000097 ) ) ;
#51153=CARTESIAN_POINT ( 'NONE',  ( -8.252512830340000605, -17.06594982557999884, 9.650910120430999939 ) ) ;
#51155=CARTESIAN_POINT ( 'NONE',  ( -2.550741782276678027, -2.812450179095209446, -2.527267954782760118 ) ) ;
#51163=ORIENTED_EDGE ( 'NONE', *, *, #54172, .T. ) ;
#51164=CIRCLE ( 'NONE', #268, 0.5000000000000006661 ) ;
#51166=CARTESIAN_POINT ( 'NONE',  ( 1.632307027704000157, -60.46927189524000568, -12.46200249215000078 ) ) ;
#51170=CARTESIAN_POINT ( 'NONE',  ( 7.645398488021999839, -23.21531609142999741, -10.18948971874999998 ) ) ;
#51173=CARTESIAN_POINT ( 'NONE',  ( -10.27342224347103894, -54.73842478142423573, -7.712153330297224052 ) ) ;
#51177=CARTESIAN_POINT ( 'NONE',  ( 7.619712398427999744, -55.39595871828999663, -10.35409979025000027 ) ) ;
#51185=VERTEX_POINT ( 'NONE', #49579 ) ;
#51187=FACE_OUTER_BOUND ( 'NONE', #55672, .T. ) ;
#51191=EDGE_CURVE ( 'NONE', #21517, #20749, #5559, .T. ) ;
#51193=CARTESIAN_POINT ( 'NONE',  ( -7.648026766715999791, -55.54999999381000464, -10.12290050087000104 ) ) ;
#51198=LINE ( 'NONE', #40868, #37745 ) ;
#51199=ORIENTED_EDGE ( 'NONE', *, *, #49843, .T. ) ;
#51200=CARTESIAN_POINT ( 'NONE',  ( 0.9212224518303000487, -17.18045898161000196, 12.54670315981999984 ) ) ;
#51204=AXIS2_PLACEMENT_3D ( 'NONE', #16163, #51318, #2022 ) ;
#51207=DIRECTION ( 'NONE',  ( -1.000000000000000000, 0.000000000000000000, 0.000000000000000000 ) ) ;
#51208=ORIENTED_EDGE ( 'NONE', *, *, #1472, .F. ) ;
#51212=EDGE_CURVE ( 'NONE', #29156, #54663, #9127, .T. ) ;
#51213=CARTESIAN_POINT ( 'NONE',  ( 1.217390015787464197, -61.61893024884950165, -12.70229597944889299 ) ) ;
#51215=FACE_OUTER_BOUND ( 'NONE', #54159, .T. ) ;
#51219=CARTESIAN_POINT ( 'NONE',  ( 8.838834764832000701, -23.25000000000000000, 8.838834764832000701 ) ) ;
#51220=CARTESIAN_POINT ( 'NONE',  ( -1.516401113037979309, -76.58467496875395852, 11.74961971174281672 ) ) ;
#51221=CARTESIAN_POINT ( 'NONE',  ( 9.151068819668228826, -79.24609374760862579, -7.813608010562005823 ) ) ;
#51222=CARTESIAN_POINT ( 'NONE',  ( -10.35398565885000011, -55.39211376237999929, 7.619387877908000206 ) ) ;
#51223=TOROIDAL_SURFACE ( 'NONE', #30450, 13.50000000000000000, 0.5000000000000000000 ) ;
#51226=CARTESIAN_POINT ( 'NONE',  ( -7.647736468634000140, -18.27704514451999884, -10.13404651205999940 ) ) ;
#51227=DIRECTION ( 'NONE',  ( -1.000000000000000000, 0.000000000000000000, 0.000000000000000000 ) ) ;
#51228=CARTESIAN_POINT ( 'NONE',  ( 14.00000000000000000, -32.66217755555999958, 5.544640309757999441E-06 ) ) ;
#51230=LINE ( 'NONE', #10782, #12789 ) ;
#51232=CARTESIAN_POINT ( 'NONE',  ( -3.517875660386507342, -1.245963598631521396, 0.1758881523666950553 ) ) ;
#51234=CARTESIAN_POINT ( 'NONE',  ( 8.813891479838931176, -61.81010130340824560, 8.872963529851991993 ) ) ;
#51236=CARTESIAN_POINT ( 'NONE',  ( 11.75000000000000000, -77.45000000000000284, 1.043320980279999928E-14 ) ) ;
#51239=CARTESIAN_POINT ( 'NONE',  ( 12.52785477537251246, -18.20586572947235382, -1.668513103012997600 ) ) ;
#51242=CARTESIAN_POINT ( 'NONE',  ( 0.000000000000000000, -5.899999999999999467, 0.000000000000000000 ) ) ;
#51243=VECTOR ( 'NONE', #49862, 1000.000000000000114 ) ;
#51245=CARTESIAN_POINT ( 'NONE',  ( 0.000000000000000000, -69.16102867818000277, 0.000000000000000000 ) ) ;
#51247=EDGE_CURVE ( 'NONE', #42116, #48636, #175, .T. ) ;
#51252=LINE ( 'NONE', #47124, #50928 ) ;
#51256=DIRECTION ( 'NONE',  ( 0.7071067811865475727, 0.000000000000000000, -0.7071067811865475727 ) ) ;
#51257=DIRECTION ( 'NONE',  ( 0.000000000000000000, 1.000000000000000000, 0.000000000000000000 ) ) ;
#51258=ORIENTED_EDGE ( 'NONE', *, *, #52320, .F. ) ;
#51259=ORIENTED_EDGE ( 'NONE', *, *, #10230, .F. ) ;
#51262=EDGE_CURVE ( 'NONE', #37664, #33033, #32702, .T. ) ;
#51263=CARTESIAN_POINT ( 'NONE',  ( 7.958763980604000032, -17.52301961031999866, 9.723170659100999202 ) ) ;
#51264=ORIENTED_EDGE ( 'NONE', *, *, #53083, .F. ) ;
#51268=CARTESIAN_POINT ( 'NONE',  ( 0.000000000000000000, 0.000000000000000000, 0.000000000000000000 ) ) ;
#51273=EDGE_LOOP ( 'NONE', ( #23293, #34159, #4737, #21007 ) ) ;
#51275=VERTEX_POINT ( 'NONE', #5276 ) ;
#51277=EDGE_LOOP ( 'NONE', ( #46557, #26306, #54915, #20405 ) ) ;
#51282=CARTESIAN_POINT ( 'NONE',  ( -1.004305231718999991, -1.000000000000000000, 3.090933677959000203 ) ) ;
#51286=CARTESIAN_POINT ( 'NONE',  ( -7.705119999413000187, -58.55171076491000548, -10.24996238027999951 ) ) ;
#51288=CARTESIAN_POINT ( 'NONE',  ( 8.453463329604378629, -76.51059011408864308, 8.160894682271043976 ) ) ;
#51291=DIRECTION ( 'NONE',  ( -1.000000000000000000, 0.000000000000000000, -2.582635147408000164E-11 ) ) ;
#51292=CARTESIAN_POINT ( 'NONE',  ( -2.873112605672330400, -3.061334993885013400, 1.555068913299749278 ) ) ;
#51299=CARTESIAN_POINT ( 'NONE',  ( -6.649705511044121664, -76.27700826535622980, -9.687362245905358549 ) ) ;
#51301=CARTESIAN_POINT ( 'NONE',  ( 0.3664097479246324340, -24.97190017500190606, 12.50575740043579387 ) ) ;
#51308=CARTESIAN_POINT ( 'NONE',  ( 9.723174505952000501, -24.47697504198000118, 7.958760297001999717 ) ) ;
#51310=CARTESIAN_POINT ( 'NONE',  ( 12.15240475282999988, -75.92640692754000042, 1.205235442679999824 ) ) ;
#51316=CARTESIAN_POINT ( 'NONE',  ( 8.803761571624066917, -53.58431590314945225, 9.164326402650994297 ) ) ;
#51318=DIRECTION ( 'NONE',  ( 0.000000000000000000, 1.000000000000000000, 0.000000000000000000 ) ) ;
#51327=ORIENTED_EDGE ( 'NONE', *, *, #10077, .T. ) ;
#51329=EDGE_CURVE ( 'NONE', #12818, #33527, #29370, .T. ) ;
#51331=VERTEX_POINT ( 'NONE', #27986 ) ;
#51335=ORIENTED_EDGE ( 'NONE', *, *, #35209, .T. ) ;
#51341=CARTESIAN_POINT ( 'NONE',  ( 12.68625206992999921, -55.03580249152999926, 1.886949102778999965 ) ) ;
#51343=ORIENTED_EDGE ( 'NONE', *, *, #32267, .F. ) ;
#51344=CARTESIAN_POINT ( 'NONE',  ( -12.72397319114999981, -23.22144180305999939, -1.930910316632999946 ) ) ;
#51348=CARTESIAN_POINT ( 'NONE',  ( 12.25000000000000000, -80.79999999999999716, 0.000000000000000000 ) ) ;
#51350=CIRCLE ( 'NONE', #16445, 1.750000000000002442 ) ;
#51355=CARTESIAN_POINT ( 'NONE',  ( -10.77133038182000035, -76.52288062955000214, -5.959359258312999508 ) ) ;
#51357=EDGE_CURVE ( 'NONE', #10018, #13012, #35278, .T. ) ;
#51358=CARTESIAN_POINT ( 'NONE',  ( 3.168171656089809662, -2.135114130757833184, 1.534604590466864593 ) ) ;
#51359=CARTESIAN_POINT ( 'NONE',  ( 0.000000000000000000, -13.07071424677999971, 0.000000000000000000 ) ) ;
#51360=CARTESIAN_POINT ( 'NONE',  ( 10.16243366810999937, -79.15072372342999074, -6.864696462387000153 ) ) ;
#51364=CARTESIAN_POINT ( 'NONE',  ( 2.330792175847127723, -2.789315473941151424, -2.264371410303323007 ) ) ;
#51365=CARTESIAN_POINT ( 'NONE',  ( -10.34990674316884629, -78.00757902561348089, 6.106564444846865669 ) ) ;
#51367=ORIENTED_EDGE ( 'NONE', *, *, #43887, .T. ) ;
#51368=DIRECTION ( 'NONE',  ( 0.000000000000000000, 0.000000000000000000, 1.000000000000000000 ) ) ;
#51370=FACE_OUTER_BOUND ( 'NONE', #57414, .T. ) ;
#51372=CARTESIAN_POINT ( 'NONE',  ( -3.846372246388999994, -2.785499118045999811, 0.4309855142524999794 ) ) ;
#51375=CARTESIAN_POINT ( 'NONE',  ( -10.43153131021861668, -76.16150389033835211, 5.412220054083467957 ) ) ;
#51376=DIRECTION ( 'NONE',  ( 1.000000000000000000, 0.000000000000000000, 0.000000000000000000 ) ) ;
#51381=FACE_OUTER_BOUND ( 'NONE', #31706, .T. ) ;
#51382=ADVANCED_FACE ( 'NONE', ( #41003 ), #42623, .F. ) ;
#51383=CARTESIAN_POINT ( 'NONE',  ( -3.165411199172029288, -2.479166666666666519, 0.8506806241676482250 ) ) ;
#51384=CARTESIAN_POINT ( 'NONE',  ( -7.660431276897000430, -59.99179487629999841, 10.01749742442000191 ) ) ;
#51385=VECTOR ( 'NONE', #23303, 1000.000000000000000 ) ;
#51388=CARTESIAN_POINT ( 'NONE',  ( 8.220399303327999618, -17.18050618273999675, -9.523318109998999859 ) ) ;
#51389=DIRECTION ( 'NONE',  ( -1.000000000000000000, 0.000000000000000000, 0.000000000000000000 ) ) ;
#51390=ORIENTED_EDGE ( 'NONE', *, *, #30318, .F. ) ;
#51392=DIRECTION ( 'NONE',  ( 0.000000000000000000, 1.000000000000000000, 0.000000000000000000 ) ) ;
#51395=CARTESIAN_POINT ( 'NONE',  ( 9.214665511417440058, -77.75938025394714259, 7.882923799935633191 ) ) ;
#51398=CIRCLE ( 'NONE', #15520, 14.00000000000000000 ) ;
#51402=CARTESIAN_POINT ( 'NONE',  ( 0.000000000000000000, -0.1000000063292999924, 0.000000000000000000 ) ) ;
#51403=CARTESIAN_POINT ( 'NONE',  ( 1.930989179114000143, -58.55453807205000061, -12.80896991324999945 ) ) ;
#51406=DIRECTION ( 'NONE',  ( 0.000000000000000000, -1.000000000000000000, 0.000000000000000000 ) ) ;
#51408=CARTESIAN_POINT ( 'NONE',  ( 12.70556836324529471, -53.57227722633783173, -0.2641978055039549966 ) ) ;
#51410=ORIENTED_EDGE ( 'NONE', *, *, #41542, .T. ) ;
#51413=ORIENTED_EDGE ( 'NONE', *, *, #57070, .F. ) ;
#51414=FACE_OUTER_BOUND ( 'NONE', #30489, .T. ) ;
#51417=CARTESIAN_POINT ( 'NONE',  ( 10.72365324215999927, -78.45851024155000175, -5.189861527858999679 ) ) ;
#51419=DIRECTION ( 'NONE',  ( -0.7071067811865474617, 0.000000000000000000, 0.7071067811865474617 ) ) ;
#51420=CARTESIAN_POINT ( 'NONE',  ( 10.12290050124000018, -23.24999999991999644, 7.648026767085999822 ) ) ;
#51423=ORIENTED_EDGE ( 'NONE', *, *, #28429, .F. ) ;
#51424=CYLINDRICAL_SURFACE ( 'NONE', #57637, 3.250000000000000000 ) ;
#51425=ORIENTED_EDGE ( 'NONE', *, *, #460, .T. ) ;
#51427=DIRECTION ( 'NONE',  ( 0.000000000000000000, 0.000000000000000000, -1.000000000000000000 ) ) ;
#51432=CARTESIAN_POINT ( 'NONE',  ( -12.64701918103000011, -76.24633340635999446, -0.3107468859061999766 ) ) ;
#51438=DIRECTION ( 'NONE',  ( -0.7071067811865475727, 0.000000000000000000, -0.7071067811865475727 ) ) ;
#51439=CARTESIAN_POINT ( 'NONE',  ( -7.648026766715999791, -55.54999999381000464, -10.12290050087000104 ) ) ;
#51441=ORIENTED_EDGE ( 'NONE', *, *, #9040, .T. ) ;
#51446=CARTESIAN_POINT ( 'NONE',  ( -9.243145380820950052, -53.88347263101093176, 8.441178781459031555 ) ) ;
#51448=CARTESIAN_POINT ( 'NONE',  ( -3.478185120108102879, -3.237645463075707220, 0.5448900037327830681 ) ) ;
#51449=DIRECTION ( 'NONE',  ( -1.000000000000000000, 0.000000000000000000, 0.000000000000000000 ) ) ;
#51451=CARTESIAN_POINT ( 'NONE',  ( 1.666698456705999920, -55.60818260126999490, -12.50018138918999888 ) ) ;
#51456=ORIENTED_EDGE ( 'NONE', *, *, #50804, .F. ) ;
#51458=CARTESIAN_POINT ( 'NONE',  ( 1.667269374591999975, -60.00939883451999890, -12.49858097732999873 ) ) ;
#51459=CARTESIAN_POINT ( 'NONE',  ( 5.940599228801999379E-14, -5.950000000028880187, -13.94999999997000018 ) ) ;
#51462=CARTESIAN_POINT ( 'NONE',  ( -1.814565153809999759E-14, -79.00000000000000000, 0.000000000000000000 ) ) ;
#51465=CARTESIAN_POINT ( 'NONE',  ( 7.295133564347398014, -78.51976047057470964, 9.212451541599802951 ) ) ;
#51467=ORIENTED_EDGE ( 'NONE', *, *, #1809, .T. ) ;
#51470=CARTESIAN_POINT ( 'NONE',  ( 7.631889106307999882, -55.57878585374000124, -10.36222439673000117 ) ) ;
#51471=CIRCLE ( 'NONE', #35392, 5.000000000000000888 ) ;
#51474=LINE ( 'NONE', #11031, #14117 ) ;
#51479=CARTESIAN_POINT ( 'NONE',  ( -10.21026245498356033, -54.54392421755085962, 7.764236519575772100 ) ) ;
#51485=EDGE_LOOP ( 'NONE', ( #27609, #21748, #38723 ) ) ;
#51486=VERTEX_POINT ( 'NONE', #6733 ) ;
#51488=ORIENTED_EDGE ( 'NONE', *, *, #33072, .F. ) ;
#51490=ORIENTED_EDGE ( 'NONE', *, *, #40054, .F. ) ;
#51491=CARTESIAN_POINT ( 'NONE',  ( 2.062323307449999810, -18.77286846807999865, 12.83634826442999888 ) ) ;
#51494=EDGE_CURVE ( 'NONE', #20252, #29379, #16193, .T. ) ;
#51495=B_SPLINE_CURVE_WITH_KNOTS ( 'NONE', 3,
 ( #28369, #10385, #36655, #36365, #37524, #27497, #55542, #51132, #5945, #18952, #13928, #45833, #49968, #10686, #394, #15093, #23660, #41965, #37235, #33089, #54391, #32212, #10098, #45538 ),
 .UNSPECIFIED., .F., .F.,
 ( 4, 2, 2, 2, 2, 2, 2, 2, 2, 2, 2, 4 ),
 ( 0.000000000000000000, 0.1250000000000006661, 0.2500000000000013323, 0.3750000000000019984, 0.4375000000000026645, 0.5000000000000033307, 0.6250000000000039968, 0.7500000000000046629, 0.8125000000000049960, 0.8437500000000042188, 0.8750000000000035527, 1.000000000000000000 ),
 .UNSPECIFIED. ) ;
#51496=CARTESIAN_POINT ( 'NONE',  ( -12.51072239526000196, -63.10294702885996543, 0.7871079366006996647 ) ) ;
#51505=DIRECTION ( 'NONE',  ( -1.000000000000000000, 0.000000000000000000, 0.000000000000000000 ) ) ;
#51506=CARTESIAN_POINT ( 'NONE',  ( -10.21381326473999884, -19.22870851082999977, 7.668949790020999302 ) ) ;
#51507=CARTESIAN_POINT ( 'NONE',  ( 11.59177481778000107, -78.97584316692000073, -2.749920651092999879 ) ) ;
#51508=EDGE_CURVE ( 'NONE', #46033, #26247, #10295, .T. ) ;
#51514=CARTESIAN_POINT ( 'NONE',  ( 1.799490225533999732, -22.77152778045000048, -12.64500484462999985 ) ) ;
#51515=AXIS2_PLACEMENT_3D ( 'NONE', #16301, #2150, #11584 ) ;
#51518=CARTESIAN_POINT ( 'NONE',  ( 0.000000000000000000, -4.000000000000000000, 0.000000000000000000 ) ) ;
#51520=DIRECTION ( 'NONE',  ( -0.7071067811865475727, 0.000000000000000000, -0.7071067811865475727 ) ) ;
#51523=CARTESIAN_POINT ( 'NONE',  ( -1.875163999714702712, -1.330382934593637323, -2.984421498244137716 ) ) ;
#51525=ORIENTED_EDGE ( 'NONE', *, *, #45471, .F. ) ;
#51526=CARTESIAN_POINT ( 'NONE',  ( 4.801183948431940074, -78.95833333333332860, -10.79468190471654410 ) ) ;
#51528=CARTESIAN_POINT ( 'NONE',  ( -1.798336774613000122, -55.60355501915000076, 12.61277771564000005 ) ) ;
#51532=CARTESIAN_POINT ( 'NONE',  ( -12.66316398243999863, -53.62133896622000151, -0.04044089952534000304 ) ) ;
#51533=DIRECTION ( 'NONE',  ( 6.735284179502000863E-11, -1.000000000000000000, 0.000000000000000000 ) ) ;
#51536=DIRECTION ( 'NONE',  ( 0.000000000000000000, -1.000000000000000000, 0.000000000000000000 ) ) ;
#51542=CARTESIAN_POINT ( 'NONE',  ( -0.4254240051736286610, -2.885416666666666519, 3.249999999999997780 ) ) ;
#51544=FACE_OUTER_BOUND ( 'NONE', #6452, .T. ) ;
#51547=FACE_OUTER_BOUND ( 'NONE', #30999, .T. ) ;
#51555=VERTEX_POINT ( 'NONE', #39470 ) ;
#51557=ORIENTED_EDGE ( 'NONE', *, *, #9161, .T. ) ;
#51559=CARTESIAN_POINT ( 'NONE',  ( -11.44417895085270942, -77.32083333333335418, -3.075537641221545826 ) ) ;
#51565=ORIENTED_EDGE ( 'NONE', *, *, #45634, .F. ) ;
#51566=CARTESIAN_POINT ( 'NONE',  ( -7.612971414697999428, -55.47547470607999998, 10.53003223722000037 ) ) ;
#51567=ORIENTED_EDGE ( 'NONE', *, *, #45353, .T. ) ;
#51568=DIRECTION ( 'NONE',  ( 0.000000000000000000, 1.000000000000000000, 0.000000000000000000 ) ) ;
#51570=CIRCLE ( 'NONE', #32691, 0.8000000000000000444 ) ;
#51573=CARTESIAN_POINT ( 'NONE',  ( 12.21492819193520774, -78.69308421639392748, -1.097028228127378435 ) ) ;
#51579=DIRECTION ( 'NONE',  ( 0.000000000000000000, 1.000000000000000000, 0.000000000000000000 ) ) ;
#51582=CARTESIAN_POINT ( 'NONE',  ( 2.331141250342373183, -76.55869204935913785, 11.51617495810127600 ) ) ;
#51583=B_SPLINE_CURVE_WITH_KNOTS ( 'NONE', 3,
 ( #19497, #6497, #19796, #18635, #15061, #18919, #5619, #41064, #37492, #54646 ),
 .UNSPECIFIED., .F., .F.,
 ( 4, 2, 2, 2, 4 ),
 ( 0.000000000000000000, 0.2500000000000000000, 0.5000000000000000000, 0.7500000000000000000, 1.000000000000000000 ),
 .UNSPECIFIED. ) ;
#51590=FACE_OUTER_BOUND ( 'NONE', #5931, .T. ) ;
#51591=DIRECTION ( 'NONE',  ( 0.000000000000000000, 1.000000000000000000, 0.000000000000000000 ) ) ;
#51592=CARTESIAN_POINT ( 'NONE',  ( 10.01332852689000141, -23.28056535155999995, 7.654537165468999760 ) ) ;
#51593=CARTESIAN_POINT ( 'NONE',  ( -0.6454797251259661861, -24.88806512139862903, 12.50471521368227990 ) ) ;
#51594=EDGE_CURVE ( 'NONE', #43980, #26528, #13342, .T. ) ;
#51600=FACE_OUTER_BOUND ( 'NONE', #11912, .T. ) ;
#51602=CARTESIAN_POINT ( 'NONE',  ( 1.379264194910999830, -76.12150170015999606, 11.98273499079000004 ) ) ;
#51607=AXIS2_PLACEMENT_3D ( 'NONE', #49088, #22212, #26343 ) ;
#51609=DIRECTION ( 'NONE',  ( -0.7071067811865474617, 0.000000000000000000, -0.7071067811865474617 ) ) ;
#51611=CARTESIAN_POINT ( 'NONE',  ( 12.54673671095000209, -53.97796527404000244, -0.9173654211234000266 ) ) ;
#51618=ORIENTED_EDGE ( 'NONE', *, *, #1428, .T. ) ;
#51619=CARTESIAN_POINT ( 'NONE',  ( -7.919595949288999570, -57.79999999967000690, 8.909545442949999838 ) ) ;
#51624=CARTESIAN_POINT ( 'NONE',  ( 12.71658872087999903, -60.11584731951999316, 1.931087888240000217 ) ) ;
#51626=ORIENTED_EDGE ( 'NONE', *, *, #3432, .F. ) ;
#51630=B_SPLINE_CURVE_WITH_KNOTS ( 'NONE', 3,
 ( #49545, #45711, #18250, #14097, #27078, #10260 ),
 .UNSPECIFIED., .F., .F.,
 ( 4, 2, 4 ),
 ( 0.000000000000000000, 0.5000000000000000000, 1.000000000000000000 ),
 .UNSPECIFIED. ) ;
#51631=EDGE_LOOP ( 'NONE', ( #41094, #31985, #58101 ) ) ;
#51636=ORIENTED_EDGE ( 'NONE', *, *, #11984, .T. ) ;
#51637=CARTESIAN_POINT ( 'NONE',  ( -12.71162862749995526, -24.23964265629794568, -1.720599174824705813 ) ) ;
#51640=CARTESIAN_POINT ( 'NONE',  ( -12.44210192979000063, -24.08432059816999882, -1.464837683472000052 ) ) ;
#51643=CARTESIAN_POINT ( 'NONE',  ( 12.80090744921000123, -59.56232687415000271, -1.980532734072999901 ) ) ;
#51644=CARTESIAN_POINT ( 'NONE',  ( 9.546815223802999739, -54.11472046612000497, 8.130854305859999798 ) ) ;
#51645=CARTESIAN_POINT ( 'NONE',  ( 0.000000000000000000, -0.1000000063292999924, -3.699999993671000187 ) ) ;
#51646=CARTESIAN_POINT ( 'NONE',  ( -12.50000000000000000, -60.04999999657000131, -1.750000000000000000 ) ) ;
#51650=AXIS2_PLACEMENT_3D ( 'NONE', #46330, #10593, #37149 ) ;
#51654=CARTESIAN_POINT ( 'NONE',  ( 10.54796701376999835, -75.74110257978999527, 6.346365727669000201 ) ) ;
#51657=CARTESIAN_POINT ( 'NONE',  ( 9.038948602550000544, -62.13262223832000331, -9.029786144045999663 ) ) ;
#51658=CIRCLE ( 'NONE', #22376, 1.250000000000000000 ) ;
#51659=CARTESIAN_POINT ( 'NONE',  ( -3.417863094299999904, -78.34598361729999283, 11.50296535110000029 ) ) ;
#51662=CARTESIAN_POINT ( 'NONE',  ( -5.205522333151648695, -77.46053809305541904, 10.88972242663192880 ) ) ;
#51668=FACE_OUTER_BOUND ( 'NONE', #44189, .T. ) ;
#51670=CARTESIAN_POINT ( 'NONE',  ( 3.628014619811000152, -2.572693282128000192, 1.348272186933000105 ) ) ;
#51673=CARTESIAN_POINT ( 'NONE',  ( -9.763989801682905423, -76.15250257597224959, 6.535952189803941437 ) ) ;
#51677=EDGE_LOOP ( 'NONE', ( #55467, #47069, #10936, #48865 ) ) ;
#51680=CARTESIAN_POINT ( 'NONE',  ( -3.250000000000001776, -2.489583333333333037, 0.4254240051736045136 ) ) ;
#51681=CARTESIAN_POINT ( 'NONE',  ( -7.659225027833000077, -60.48266641633000518, 9.963489011801000217 ) ) ;
#51684=CARTESIAN_POINT ( 'NONE',  ( -7.624341764923000753, -18.73514850530999709, -10.42531124853000080 ) ) ;
#51685=CARTESIAN_POINT ( 'NONE',  ( -12.70619604129606373, -54.33855724441426815, -1.571828507127614127 ) ) ;
#51689=CARTESIAN_POINT ( 'NONE',  ( 0.000000000000000000, -6.000000000000000000, 0.000000000000000000 ) ) ;
#51691=CARTESIAN_POINT ( 'NONE',  ( -12.50000000000000000, -26.93717104351999936, -1.871243407866999974E-13 ) ) ;
#51694=CARTESIAN_POINT ( 'NONE',  ( 2.062503053667999797, -58.55736537918999574, -12.92177931905999877 ) ) ;
#51695=EDGE_CURVE ( 'NONE', #33149, #40044, #41219, .T. ) ;
#51698=CARTESIAN_POINT ( 'NONE',  ( -1.980584515752000119, -23.26485146623999967, 12.76303204602000108 ) ) ;
#51701=ORIENTED_EDGE ( 'NONE', *, *, #48777, .F. ) ;
#51702=ORIENTED_EDGE ( 'NONE', *, *, #30669, .T. ) ;
#51705=ORIENTED_EDGE ( 'NONE', *, *, #16481, .F. ) ;
#51706=CARTESIAN_POINT ( 'NONE',  ( 7.624757993428000091, -18.19647951307999989, 10.47516388919000008 ) ) ;
#51708=CARTESIAN_POINT ( 'NONE',  ( 3.035209552710000036, -78.97670186241998636, -11.67368974080000044 ) ) ;
#51709=CARTESIAN_POINT ( 'NONE',  ( 8.909545442949999838, -55.64999999967000122, -8.061017305527000687 ) ) ;
#51714=DIRECTION ( 'NONE',  ( 0.000000000000000000, -1.000000000000000000, 0.000000000000000000 ) ) ;
#51721=CARTESIAN_POINT ( 'NONE',  ( 1.250000000000000000, -55.54999999966999980, -12.50000000000000000 ) ) ;
#51723=FACE_OUTER_BOUND ( 'NONE', #24218, .T. ) ;
#51725=CARTESIAN_POINT ( 'NONE',  ( -7.613962745610000304, -18.69360215052999763, 10.53101990620000095 ) ) ;
#51728=FACE_OUTER_BOUND ( 'NONE', #42589, .T. ) ;
#51737=CARTESIAN_POINT ( 'NONE',  ( -7.658894278891000162, -18.79060682915999791, 10.01676917982000070 ) ) ;
#51742=CARTESIAN_POINT ( 'NONE',  ( 1.933650113858000230, -55.39213746940999528, -12.70909635752000177 ) ) ;
#51746=VERTEX_POINT ( 'NONE', #13169 ) ;
#51748=CARTESIAN_POINT ( 'NONE',  ( 2.062323307449999810, -60.02713153159000115, -12.83634826445999977 ) ) ;
#51749=CARTESIAN_POINT ( 'NONE',  ( -7.342356150419299787, -55.61035107872125849, 8.190836719257353238 ) ) ;
#51754=CARTESIAN_POINT ( 'NONE',  ( -10.12290050255000118, -60.04999997790999799, 7.648026768390999486 ) ) ;
#51755=DIRECTION ( 'NONE',  ( -0.7071067811865475727, 0.000000000000000000, -0.7071067811865475727 ) ) ;
#51764=CARTESIAN_POINT ( 'NONE',  ( -7.624341764906000130, -55.53514850498000044, -10.42531124851000079 ) ) ;
#51767=EDGE_CURVE ( 'NONE', #35617, #17140, #35031, .T. ) ;
#51768=VECTOR ( 'NONE', #50193, 1000.000000000000114 ) ;
#51769=CARTESIAN_POINT ( 'NONE',  ( -10.41144070831380120, -55.27453159746022493, 7.610433246081189651 ) ) ;
#51772=EDGE_CURVE ( 'NONE', #52707, #18726, #9058, .T. ) ;
#51773=CARTESIAN_POINT ( 'NONE',  ( 1.667936688463999895, -19.23513569609999863, 12.53239398062000198 ) ) ;
#51775=ORIENTED_EDGE ( 'NONE', *, *, #28319, .F. ) ;
#51776=ORIENTED_EDGE ( 'NONE', *, *, #53892, .F. ) ;
#51777=CARTESIAN_POINT ( 'NONE',  ( -12.79895942951000087, -54.99538174351000208, -2.015930660723999956 ) ) ;
#51779=ORIENTED_EDGE ( 'NONE', *, *, #37648, .F. ) ;
#51780=CARTESIAN_POINT ( 'NONE',  ( 0.5506765233277000071, -16.74045707756000212, 12.77514798311000099 ) ) ;
#51784=ADVANCED_BREP_SHAPE_REPRESENTATION ( '', ( #17297, #43526 ), #53938 ) ;
#51785=CARTESIAN_POINT ( 'NONE',  ( -9.050966799188000067, -59.94999999967000548, 7.919595949288999570 ) ) ;
#51789=ORIENTED_EDGE ( 'NONE', *, *, #18288, .T. ) ;
#51791=CARTESIAN_POINT ( 'NONE',  ( 12.60354432329999952, -59.55100837068999908, 1.750000000001000089 ) ) ;
#51793=CARTESIAN_POINT ( 'NONE',  ( -12.77562710770000187, -62.06233677629000312, -0.5428386295904999992 ) ) ;
#51796=CARTESIAN_POINT ( 'NONE',  ( 9.872209700914000408, -78.94710244883999906, -6.668650957345999331 ) ) ;
#51799=CARTESIAN_POINT ( 'NONE',  ( -10.78576251690998689, -76.66714693325138796, 4.661353383015510943 ) ) ;
#51801=CARTESIAN_POINT ( 'NONE',  ( -9.516265623847999677, -53.97460635707999899, 8.227505979398999969 ) ) ;
#51804=CARTESIAN_POINT ( 'NONE',  ( -7.633088938756000807, -18.60992532424000245, -10.18115029113000070 ) ) ;
#51805=DIRECTION ( 'NONE',  ( -1.000000000000000000, 0.000000000000000000, 0.000000000000000000 ) ) ;
#51807=AXIS2_PLACEMENT_3D ( 'NONE', #8843, #18806, #824 ) ;
#51808=CARTESIAN_POINT ( 'NONE',  ( -0.4250565598266470846, -1.216173826220077414, -3.248535750966747848 ) ) ;
#51810=CARTESIAN_POINT ( 'NONE',  ( 9.722718241315000398, -60.04999999966999980, 7.954951288349001004 ) ) ;
#51812=CARTESIAN_POINT ( 'NONE',  ( 3.351413303022582557, -1.530878857503674695, 1.345052432851818747 ) ) ;
#51813=EDGE_LOOP ( 'NONE', ( #3789, #33141, #57757, #32284 ) ) ;
#51815=DIRECTION ( 'NONE',  ( -1.000000000000000000, 0.000000000000000000, 0.000000000000000000 ) ) ;
#51816=CARTESIAN_POINT ( 'NONE',  ( 0.000000000000000000, -46.09579702914000165, 0.000000000000000000 ) ) ;
#51819=CIRCLE ( 'NONE', #21611, 13.89999999999999858 ) ;
#51823=AXIS2_PLACEMENT_3D ( 'NONE', #51268, #15528, #14931 ) ;
#51824=EDGE_CURVE ( 'NONE', #29475, #47200, #15226, .T. ) ;
#51827=ADVANCED_FACE ( 'NONE', ( #14635 ), #2248, .F. ) ;
#51829=CARTESIAN_POINT ( 'NONE',  ( 9.516658938990653738, -76.39971689995223869, -6.891841626549551236 ) ) ;
#51832=DIRECTION ( 'NONE',  ( 0.000000000000000000, -1.000000000000000000, 0.000000000000000000 ) ) ;
#51836=CARTESIAN_POINT ( 'NONE',  ( 0.000000000000000000, -0.2000000000000000111, 0.000000000000000000 ) ) ;
#51843=CARTESIAN_POINT ( 'NONE',  ( 12.50745077490000057, -17.00005551713000074, -2.011911479242000131E-09 ) ) ;
#51845=ORIENTED_EDGE ( 'NONE', *, *, #54774, .T. ) ;
#51846=CARTESIAN_POINT ( 'NONE',  ( -3.075537641221531615, -77.40416666666668277, -11.44417895085270942 ) ) ;
#51850=VERTEX_POINT ( 'NONE', #50965 ) ;
#51851=CARTESIAN_POINT ( 'NONE',  ( 7.601397897754999633, -60.04999999725999515, -10.07627163191000008 ) ) ;
#51854=ORIENTED_EDGE ( 'NONE', *, *, #45586, .F. ) ;
#51855=LINE ( 'NONE', #11410, #17707 ) ;
#51859=VECTOR ( 'NONE', #24813, 1000.000000000000227 ) ;
#51860=CARTESIAN_POINT ( 'NONE',  ( 10.16273287016798754, -79.15293570561394176, -6.864898572566356272 ) ) ;
#51869=CARTESIAN_POINT ( 'NONE',  ( 0.000000000000000000, -69.16102867818000277, 0.000000000000000000 ) ) ;
#51877=CARTESIAN_POINT ( 'NONE',  ( 10.59551070212000035, -21.75648180056000314, 7.678690995204998870 ) ) ;
#51878=CARTESIAN_POINT ( 'NONE',  ( -7.761030428359000588, -60.88151201342000007, -9.835168816246000034 ) ) ;
#51882=CARTESIAN_POINT ( 'NONE',  ( -12.61271781521000079, -18.80306329050999992, -1.798333084007999849 ) ) ;
#51883=CARTESIAN_POINT ( 'NONE',  ( 12.66322140209000047, -25.18161935732999623, 0.1487435796151999889 ) ) ;
#51885=CARTESIAN_POINT ( 'NONE',  ( -11.75346344166169743, -78.20980192672932674, -1.536536421794175489 ) ) ;
#51886=B_SPLINE_CURVE_WITH_KNOTS ( 'NONE', 3,
 ( #48273, #25810, #29649, #20524, #30520, #16384, #21379, #52402 ),
 .UNSPECIFIED., .F., .F.,
 ( 4, 2, 2, 4 ),
 ( 0.7143499438395097823, 0.8571749719197548911, 0.9285874859598775011, 1.000000000000000000 ),
 .UNSPECIFIED. ) ;
#51887=CARTESIAN_POINT ( 'NONE',  ( -12.49999990534960226, -49.87071424677999687, -0.001538265197294672385 ) ) ;
#51888=CARTESIAN_POINT ( 'NONE',  ( 8.663048543576998384, -75.68023594616001049, -9.028321399273000480 ) ) ;
#51889=EDGE_LOOP ( 'NONE', ( #608, #33879, #14161, #52487 ) ) ;
#51890=LINE ( 'NONE', #21154, #17282 ) ;
#51891=CARTESIAN_POINT ( 'NONE',  ( 12.61117499584999813, -60.01550664522000034, 1.798980867982999943 ) ) ;
#51892=CARTESIAN_POINT ( 'NONE',  ( -8.799409365152000007, -79.31836356187000092, -8.853116023008999136 ) ) ;
#51893=CARTESIAN_POINT ( 'NONE',  ( 12.65987793659000005, -53.86302453462000273, -0.9847129294438998759 ) ) ;
#51896=CARTESIAN_POINT ( 'NONE',  ( -11.79999999988000070, -18.85000000520999919, -0.5999999998848000171 ) ) ;
#51898=DIRECTION ( 'NONE',  ( -0.9999999999995751176, 0.000000000000000000, -9.217549095371770968E-07 ) ) ;
#51899=ORIENTED_EDGE ( 'NONE', *, *, #17131, .F. ) ;
#51901=AXIS2_PLACEMENT_3D ( 'NONE', #28851, #11741, #51898 ) ;
#51909=VERTEX_POINT ( 'NONE', #46841 ) ;
#51912=ORIENTED_EDGE ( 'NONE', *, *, #34287, .F. ) ;
#51913=ORIENTED_EDGE ( 'NONE', *, *, #26314, .F. ) ;
#51918=ADVANCED_FACE ( 'NONE', ( #20248 ), #28501, .T. ) ;
#51919=ORIENTED_EDGE ( 'NONE', *, *, #38292, .T. ) ;
#51920=CARTESIAN_POINT ( 'NONE',  ( -12.72966770606090670, -23.76881200365143698, -1.931346186345864746 ) ) ;
#51923=VERTEX_POINT ( 'NONE', #55090 ) ;
#51926=CARTESIAN_POINT ( 'NONE',  ( 12.76303204298000082, -60.06485150663000638, -1.980584515756000030 ) ) ;
#51927=FACE_OUTER_BOUND ( 'NONE', #20123, .T. ) ;
#51931=DIRECTION ( 'NONE',  ( -2.678911359553000079E-11, 1.000000000000000000, -2.678929432950999965E-11 ) ) ;
#51933=CARTESIAN_POINT ( 'NONE',  ( 3.295079792876999925, -76.30143611710998641, 11.86077433336000020 ) ) ;
#51934=AXIS2_PLACEMENT_3D ( 'NONE', #29574, #19065, #18769 ) ;
#51939=CARTESIAN_POINT ( 'NONE',  ( 9.422842877325999567, -62.05952027250000214, -8.643944052328999206 ) ) ;
#51940=CARTESIAN_POINT ( 'NONE',  ( 9.369164850722000892, -23.25000000000000000, -7.601397897754999633 ) ) ;
#51943=CARTESIAN_POINT ( 'NONE',  ( -11.88755474194624817, -78.03426394915543085, 2.371826327494228615 ) ) ;
#51945=ORIENTED_EDGE ( 'NONE', *, *, #56303, .F. ) ;
#51948=CARTESIAN_POINT ( 'NONE',  ( 0.000000000000000000, 0.000000000000000000, -12.00000000000000000 ) ) ;
#51950=CARTESIAN_POINT ( 'NONE',  ( -1.781396697799999984, -3.385272489337999957, 3.079626043334999785 ) ) ;
#51953=CARTESIAN_POINT ( 'NONE',  ( -4.649632569072141841, -76.10711892059522654, 10.80545511456402608 ) ) ;
#51954=CARTESIAN_POINT ( 'NONE',  ( 10.14950121162999963, -19.24922972541000021, -7.674627477474999182 ) ) ;
#51960=TOROIDAL_SURFACE ( 'NONE', #50071, 17.50000000000000000, 5.000000000000000000 ) ;
#51961=CARTESIAN_POINT ( 'NONE',  ( 1.997276839918466829, -2.322916666666665630, 2.598917237794090784 ) ) ;
#51963=CARTESIAN_POINT ( 'NONE',  ( -1.980584515756000030, -18.73514849905999924, 12.76303204340999997 ) ) ;
#51964=DIRECTION ( 'NONE',  ( 0.000000000000000000, 0.000000000000000000, -1.000000000000000000 ) ) ;
#51965=CYLINDRICAL_SURFACE ( 'NONE', #1336, 0.6000000000000008660 ) ;
#51967=ORIENTED_EDGE ( 'NONE', *, *, #50436, .T. ) ;
#51970=CARTESIAN_POINT ( 'NONE',  ( -3.616527695712999702, -1.759176978014000081, -0.5438149879621999583 ) ) ;
#51975=EDGE_CURVE ( 'NONE', #46551, #25542, #50168, .T. ) ;
#51977=VECTOR ( 'NONE', #1731, 1000.000000000000114 ) ;
#51978=CARTESIAN_POINT ( 'NONE',  ( 10.12290050255000118, -60.04999997790999799, -7.648026768390999486 ) ) ;
#51979=CARTESIAN_POINT ( 'NONE',  ( 12.50728321921977937, -61.79975184134804778, 0.1774118161309094777 ) ) ;
#51983=CARTESIAN_POINT ( 'NONE',  ( 12.70249541833965345, -53.83496187159536817, -0.9988462570306496646 ) ) ;
#51990=CARTESIAN_POINT ( 'NONE',  ( 10.18127254044999930, -18.61355771719999908, 7.633407132383000615 ) ) ;
#51992=CARTESIAN_POINT ( 'NONE',  ( 0.1380878923454642859, -53.57265597645798749, 12.70555840928343017 ) ) ;
#51993=CARTESIAN_POINT ( 'NONE',  ( -3.220107333416999840, -77.56377916175999587, 12.38709272308999942 ) ) ;
#51994=DIRECTION ( 'NONE',  ( 0.7071067811865475727, 0.000000000000000000, 0.7071067811865475727 ) ) ;
#51996=DIRECTION ( 'NONE',  ( 0.000000000000000000, 0.000000000000000000, -1.000000000000000000 ) ) ;
#52001=ORIENTED_EDGE ( 'NONE', *, *, #39474, .F. ) ;
#52004=CARTESIAN_POINT ( 'NONE',  ( -11.87500000004000000, -79.12500000004000356, -1.061343742159000057E-08 ) ) ;
#52008=CARTESIAN_POINT ( 'NONE',  ( -8.414570695956999913, -59.94999999967000548, 8.414570695956999913 ) ) ;
#52011=CARTESIAN_POINT ( 'NONE',  ( -7.627487525417000036, -18.70221245812999911, 10.35845608625999859 ) ) ;
#52013=CARTESIAN_POINT ( 'NONE',  ( -3.206516299415000049, -2.013032031398999777, -0.5298615117031000299 ) ) ;
#52015=ORIENTED_EDGE ( 'NONE', *, *, #14507, .T. ) ;
#52017=AXIS2_PLACEMENT_3D ( 'NONE', #21423, #16999, #39712 ) ;
#52021=CARTESIAN_POINT ( 'NONE',  ( -9.310166272083998606, -16.86468533975999762, 8.596757084891999412 ) ) ;
#52022=ADVANCED_FACE ( 'NONE', ( #33217 ), #46550, .T. ) ;
#52025=CARTESIAN_POINT ( 'NONE',  ( -2.930423846477897776, -2.296787813417054736, -1.954655114040125374 ) ) ;
#52028=CARTESIAN_POINT ( 'NONE',  ( 1.576170184336000091, -54.63913032751000287, -12.55466896101999907 ) ) ;
#52034=CARTESIAN_POINT ( 'NONE',  ( -1.758095523364999968, -60.52291663846999370, -12.57362173518999882 ) ) ;
#52043=ORIENTED_EDGE ( 'NONE', *, *, #15325, .T. ) ;
#52045=CARTESIAN_POINT ( 'NONE',  ( -1.838192502620780822, -75.79999999999998295, -11.63589874194363816 ) ) ;
#52048=EDGE_CURVE ( 'NONE', #3338, #22170, #6368, .T. ) ;
#52054=CARTESIAN_POINT ( 'NONE',  ( -7.635226873531286707, -55.03391307102463514, 10.36745167320620808 ) ) ;
#52056=CARTESIAN_POINT ( 'NONE',  ( 1.930989179114000143, -20.24546192895000019, 12.80896991329000123 ) ) ;
#52058=CARTESIAN_POINT ( 'NONE',  ( 3.075537641221509411, -76.15416666666668277, 11.44417895085272008 ) ) ;
#52059=VERTEX_POINT ( 'NONE', #6076 ) ;
#52060=EDGE_CURVE ( 'NONE', #52807, #4267, #26158, .T. ) ;
#52061=ORIENTED_EDGE ( 'NONE', *, *, #14664, .F. ) ;
#52062=CARTESIAN_POINT ( 'NONE',  ( -12.55458938217999965, -54.63720883353000346, -1.575070636625000242 ) ) ;
#52066=CARTESIAN_POINT ( 'NONE',  ( 10.53494356938999843, -23.22715052988000295, 7.618393677165000710 ) ) ;
#52072=ORIENTED_EDGE ( 'NONE', *, *, #44758, .T. ) ;
#52075=CARTESIAN_POINT ( 'NONE',  ( -12.70255466318980631, -24.74616562079560467, 1.306323829446151885 ) ) ;
#52078=CIRCLE ( 'NONE', #11534, 12.57042253521000141 ) ;
#52079=CARTESIAN_POINT ( 'NONE',  ( 7.641012305222999679, -23.28917723430000208, 10.18589226631999978 ) ) ;
#52084=FACE_OUTER_BOUND ( 'NONE', #36349, .T. ) ;
#52085=CARTESIAN_POINT ( 'NONE',  ( -10.15323015671000029, -54.56919784871999468, 7.760928569184999404 ) ) ;
#52087=DIRECTION ( 'NONE',  ( -1.000000000000000000, 0.000000000000000000, 0.000000000000000000 ) ) ;
#52088=CARTESIAN_POINT ( 'NONE',  ( 1.667916687331000070, -18.70151115557999688, -12.49168451098999988 ) ) ;
#52089=EDGE_CURVE ( 'NONE', #13029, #44413, #10815, .T. ) ;
#52091=CARTESIAN_POINT ( 'NONE',  ( 1.667260628941999778, -18.79057987526000062, -12.49858003894999925 ) ) ;
#52094=CARTESIAN_POINT ( 'NONE',  ( 12.76303204522000101, -23.26485147686999966, 1.980584515753000208 ) ) ;
#52095=CARTESIAN_POINT ( 'NONE',  ( 1.068619641472000170, -1.999647048965999874, -3.652926003266999899 ) ) ;
#52096=CARTESIAN_POINT ( 'NONE',  ( -1.137713819132262438, -1.150991845674092851, 3.439702573946882946 ) ) ;
#52098=ORIENTED_EDGE ( 'NONE', *, *, #38137, .T. ) ;
#52099=CARTESIAN_POINT ( 'NONE',  ( -2.843405644759636086, -1.560134993415584370, 1.636542488881060464 ) ) ;
#52103=AXIS2_PLACEMENT_3D ( 'NONE', #20415, #10987, #28968 ) ;
#52105=FACE_OUTER_BOUND ( 'NONE', #10589, .T. ) ;
#52108=PLANE ( 'NONE',  #42354 ) ;
#52111=CARTESIAN_POINT ( 'NONE',  ( 8.858913794315254719, -76.39276943178882107, -7.721635716659831061 ) ) ;
#52122=AXIS2_PLACEMENT_3D ( 'NONE', #16790, #11505, #25063 ) ;
#52126=ORIENTED_EDGE ( 'NONE', *, *, #26694, .T. ) ;
#52128=CARTESIAN_POINT ( 'NONE',  ( 1.930860503532993544, -23.77417505915895291, 12.72930866331734734 ) ) ;
#52129=ADVANCED_FACE ( 'NONE', ( #56839 ), #120, .T. ) ;
#52133=VERTEX_POINT ( 'NONE', #30530 ) ;
#52136=ORIENTED_EDGE ( 'NONE', *, *, #48250, .F. ) ;
#52138=CARTESIAN_POINT ( 'NONE',  ( -7.641012305206999145, -55.51082276539999327, 10.18589226629999978 ) ) ;
#52139=ORIENTED_EDGE ( 'NONE', *, *, #6029, .F. ) ;
#52142=CIRCLE ( 'NONE', #26649, 0.5000000000000001110 ) ;
#52143=DIRECTION ( 'NONE',  ( -0.7071067811865474617, 0.000000000000000000, -0.7071067811865474617 ) ) ;
#52145=CYLINDRICAL_SURFACE ( 'NONE', #24903, 14.00000000000000000 ) ;
#52151=VECTOR ( 'NONE', #49811, 1000.000000000000114 ) ;
#52156=CARTESIAN_POINT ( 'NONE',  ( -9.722718241315000398, -18.55321828668999729, -7.954951288349001004 ) ) ;
#52157=DIRECTION ( 'NONE',  ( 1.000000000000000000, 0.000000000000000000, 0.000000000000000000 ) ) ;
#52159=AXIS2_PLACEMENT_3D ( 'NONE', #5468, #22894, #46523 ) ;
#52161=DIRECTION ( 'NONE',  ( 0.000000000000000000, -1.000000000000000000, 0.000000000000000000 ) ) ;
#52162=CARTESIAN_POINT ( 'NONE',  ( 0.000000000000000000, -52.49705297114005020, 12.53545825868000207 ) ) ;
#52167=CIRCLE ( 'NONE', #29507, 1.750000000000000000 ) ;
#52169=DIRECTION ( 'NONE',  ( 0.000000000000000000, -1.000000000000000000, 0.000000000000000000 ) ) ;
#52170=CARTESIAN_POINT ( 'NONE',  ( 10.53003236235000095, -60.12452273675999947, 7.612971540294999784 ) ) ;
#52172=CARTESIAN_POINT ( 'NONE',  ( 12.83838776459000108, -23.20596988487999823, 2.062170466181000528 ) ) ;
#52173=CARTESIAN_POINT ( 'NONE',  ( 11.15501740173857037, -78.42093623943294745, -3.786043910604230955 ) ) ;
#52174=CARTESIAN_POINT ( 'NONE',  ( 1.733997378023099056, -23.52383216769529639, -12.54437956612015626 ) ) ;
#52175=CARTESIAN_POINT ( 'NONE',  ( 11.12361694604000029, -76.79944983679999382, -4.717657731420999312 ) ) ;
#52176=ORIENTED_EDGE ( 'NONE', *, *, #34552, .T. ) ;
#52177=DIRECTION ( 'NONE',  ( 0.000000000000000000, 1.000000000000000000, 0.000000000000000000 ) ) ;
#52178=CARTESIAN_POINT ( 'NONE',  ( 0.000000000000000000, 4.040000000000000036, 0.000000000000000000 ) ) ;
#52180=CARTESIAN_POINT ( 'NONE',  ( -12.47891010869000006, -78.75756776420000449, -0.3053857658451999968 ) ) ;
#52181=FACE_OUTER_BOUND ( 'NONE', #1160, .T. ) ;
#52186=EDGE_LOOP ( 'NONE', ( #5148, #39588, #42553, #21535, #33443, #58131 ) ) ;
#52189=EDGE_LOOP ( 'NONE', ( #52344, #43275, #53580, #43481 ) ) ;
#52194=VERTEX_POINT ( 'NONE', #14749 ) ;
#52196=EDGE_LOOP ( 'NONE', ( #8571, #43734, #29576, #34582 ) ) ;
#52197=VERTEX_POINT ( 'NONE', #29488 ) ;
#52200=CARTESIAN_POINT ( 'NONE',  ( 1.405334851866475443, -61.11492947527372621, 12.50716844841787356 ) ) ;
#52202=VERTEX_POINT ( 'NONE', #41925 ) ;
#52203=CARTESIAN_POINT ( 'NONE',  ( 2.597747286150731583, -2.403326232176795862, 1.995542179488032808 ) ) ;
#52204=ORIENTED_EDGE ( 'NONE', *, *, #16396, .T. ) ;
#52205=CARTESIAN_POINT ( 'NONE',  ( -11.38660623898999980, -79.08028002244630272, -4.554589311945999697 ) ) ;
#52207=CARTESIAN_POINT ( 'NONE',  ( 9.395773752806999113, -54.09509747810999869, 8.188237371196001035 ) ) ;
#52209=CARTESIAN_POINT ( 'NONE',  ( 8.792808668242045655, -16.77303577624769559, -9.175550543643495871 ) ) ;
#52213=CYLINDRICAL_SURFACE ( 'NONE', #52636, 1.750000000000001332 ) ;
#52215=CARTESIAN_POINT ( 'NONE',  ( 7.568503529865000523, -76.27030647614999737, 9.708412483427999007 ) ) ;
#52216=FACE_OUTER_BOUND ( 'NONE', #19664, .T. ) ;
#52219=CARTESIAN_POINT ( 'NONE',  ( 10.35410175341000105, -60.20399325318000194, -7.619715687221999545 ) ) ;
#52220=CARTESIAN_POINT ( 'NONE',  ( 7.081057523560999378, -79.15664967202000923, -10.01287680343000019 ) ) ;
#52224=B_SPLINE_CURVE_WITH_KNOTS ( 'NONE', 3,
 ( #14753, #32752, #62, #50800, #44903, #27163, #40470, #49927, #13592, #9179, #45202, #40761, #355, #18333, #31884, #5040, #36326, #54350, #41056, #13890, #9472, #36618, #54639, #42805, #46377, #2084, #10937, #15932, #7072, #47251, #6782, #25075, #24790, #6196, #2367 ),
 .UNSPECIFIED., .F., .F.,
 ( 4, 1, 1, 1, 1, 1, 1, 1, 1, 1, 1, 1, 1, 1, 1, 1, 1, 1, 1, 1, 1, 1, 1, 1, 1, 1, 1, 1, 1, 1, 1, 1, 4 ),
 ( 0.000000000000000000, 0.01250092184359906378, 0.04500086039013131284, 0.07750079893666367292, 0.1100007374831958179, 0.1425006760297282682, 0.1750006145762605103, 0.2075005531227929745, 0.2400004916693252166, 0.2725004302158574587, 0.3050003687623897286, 0.3375003073089221650, 0.3700002458554544349, 0.4025001844019868713, 0.4350001229485191412, 0.4675000614950513556, 0.5000000000415836254, 0.5324999385881158398, 0.5649998771346483872, 0.5974998156811806016, 0.6299997542277130380, 0.6624996927742452524, 0.6949996313207776888, 0.7274995698673097921, 0.7599995084138420065, 0.7924994469603744429, 0.8249993855069067683, 0.8574993240534392047, 0.8899992625999714191, 0.9224992011465038555, 0.9549991396930359588, 0.9874990782395683953, 1.000000000000000000 ),
 .UNSPECIFIED. ) ;
#52228=DIRECTION ( 'NONE',  ( 1.000000000000000000, 0.000000000000000000, 0.000000000000000000 ) ) ;
#52229=CARTESIAN_POINT ( 'NONE',  ( 1.532229594834795705, -24.12298963131433638, 12.51228690880953387 ) ) ;
#52230=CARTESIAN_POINT ( 'NONE',  ( -1.647164036128999864, -2.055236014850999826, -3.153578910874000218 ) ) ;
#52234=CARTESIAN_POINT ( 'NONE',  ( -11.52085783181860812, -76.18387217134889511, 2.307947444626160305 ) ) ;
#52237=DIRECTION ( 'NONE',  ( 0.000000000000000000, -1.000000000000000000, 0.000000000000000000 ) ) ;
#52239=CARTESIAN_POINT ( 'NONE',  ( -10.18589226631999978, -18.71082276572999703, -7.641012305223999768 ) ) ;
#52244=DIRECTION ( 'NONE',  ( 1.000000000000000000, 0.000000000000000000, 0.000000000000000000 ) ) ;
#52249=ORIENTED_EDGE ( 'NONE', *, *, #47602, .T. ) ;
#52255=AXIS2_PLACEMENT_3D ( 'NONE', #57431, #48870, #25265 ) ;
#52259=CARTESIAN_POINT ( 'NONE',  ( 1.667961430005999945, -58.54888345776999614, -12.58335110162999904 ) ) ;
#52260=EDGE_CURVE ( 'NONE', #35193, #37266, #21731, .T. ) ;
#52271=CARTESIAN_POINT ( 'NONE',  ( 7.636247231030999671, -18.23676232879999759, 10.30460520062000107 ) ) ;
#52273=CARTESIAN_POINT ( 'NONE',  ( -9.396085398178614767, -75.85208333333332575, -7.220923959705254802 ) ) ;
#52274=CARTESIAN_POINT ( 'NONE',  ( 5.488019371950999314, -76.92165190241000516, 11.73632836356999931 ) ) ;
#52280=EDGE_LOOP ( 'NONE', ( #2182, #26030, #47130, #48776 ) ) ;
#52281=CARTESIAN_POINT ( 'NONE',  ( -8.190859204290999784, -55.64999999967000122, 7.342331066867000544 ) ) ;
#52282=ORIENTED_EDGE ( 'NONE', *, *, #57070, .T. ) ;
#52291=CARTESIAN_POINT ( 'NONE',  ( -12.71658889741000031, -18.68415522710999710, -1.931087888049999979 ) ) ;
#52292=CARTESIAN_POINT ( 'NONE',  ( -7.705142895586000407, -21.75083378359999742, 10.24998526315000014 ) ) ;
#52294=ADVANCED_FACE ( 'NONE', ( #11161 ), #8967, .F. ) ;
#52295=CARTESIAN_POINT ( 'NONE',  ( -10.06692847398348434, -23.70343452288557984, -7.655995225932134218 ) ) ;
#52297=TOROIDAL_SURFACE ( 'NONE', #1403, 1.250000000000000000, 0.5000000000000000000 ) ;
#52298=CARTESIAN_POINT ( 'NONE',  ( -3.453171399369999950, -1.863032031399000088, -0.5706200895263999762 ) ) ;
#52303=AXIS2_PLACEMENT_3D ( 'NONE', #54410, #18975, #31356 ) ;
#52305=CARTESIAN_POINT ( 'NONE',  ( 0.5999999999999999778, -18.84999999999000053, 11.79999999999999893 ) ) ;
#52309=CARTESIAN_POINT ( 'NONE',  ( 0.7960987979667577541, -2.106806941851198989, 3.429641257530567255 ) ) ;
#52312=CARTESIAN_POINT ( 'NONE',  ( 8.414570695956999913, -59.94999999967000548, -8.414570695956999913 ) ) ;
#52314=CARTESIAN_POINT ( 'NONE',  ( 7.342331066867000544, -59.94999999967000548, 8.190859204290999784 ) ) ;
#52320=EDGE_CURVE ( 'NONE', #17174, #26247, #50068, .T. ) ;
#52325=CARTESIAN_POINT ( 'NONE',  ( -1.930860503549513663, -18.22582494086907090, 12.72930866331778432 ) ) ;
#52328=CARTESIAN_POINT ( 'NONE',  ( -7.635939347819122425, -60.57525282287573276, 10.36595956262699580 ) ) ;
#52329=EDGE_LOOP ( 'NONE', ( #40869, #41805, #54302, #37523 ) ) ;
#52334=CARTESIAN_POINT ( 'NONE',  ( -12.71658872087999903, -60.11584731951999316, -1.931087888240000217 ) ) ;
#52335=PLANE ( 'NONE',  #37719 ) ;
#52336=CARTESIAN_POINT ( 'NONE',  ( -14.00000000000000000, -32.70420297070000260, 0.000000000000000000 ) ) ;
#52338=ADVANCED_FACE ( 'NONE', ( #39733 ), #4728, .F. ) ;
#52340=CARTESIAN_POINT ( 'NONE',  ( 2.062597265787999845, -22.78461666469000235, 12.87024489156999962 ) ) ;
#52342=AXIS2_PLACEMENT_3D ( 'NONE', #52746, #26160, #21443 ) ;
#52343=CARTESIAN_POINT ( 'NONE',  ( -12.44180635029999848, -24.09260544925000147, 1.459447571597000115 ) ) ;
#52344=ORIENTED_EDGE ( 'NONE', *, *, #18774, .T. ) ;
#52345=ORIENTED_EDGE ( 'NONE', *, *, #11660, .T. ) ;
#52346=PLANE ( 'NONE',  #32393 ) ;
#52347=TOROIDAL_SURFACE ( 'NONE', #24984, 13.50000000000000000, 0.5000000000000000000 ) ;
#52354=CARTESIAN_POINT ( 'NONE',  ( 1.750000000001000089, -59.55077028460999600, 12.60356226396000068 ) ) ;
#52359=ORIENTED_EDGE ( 'NONE', *, *, #1601, .F. ) ;
#52360=EDGE_LOOP ( 'NONE', ( #16222, #12536, #11342, #7733, #17289, #33299 ) ) ;
#52365=CARTESIAN_POINT ( 'NONE',  ( 7.641012386038000592, -18.71082434677000350, 10.18589234708000113 ) ) ;
#52368=CYLINDRICAL_SURFACE ( 'NONE', #40096, 1.750000000000000000 ) ;
#52370=CARTESIAN_POINT ( 'NONE',  ( -7.919595949288999570, -59.94999999967000548, -8.768124086712999699 ) ) ;
#52371=CARTESIAN_POINT ( 'NONE',  ( -9.699677589918225706, -76.65189001212350206, 6.631369083228229933 ) ) ;
#52372=ADVANCED_FACE ( 'NONE', ( #7154 ), #24873, .F. ) ;
#52376=CARTESIAN_POINT ( 'NONE',  ( -12.71466317168545679, -60.93795986706020074, 1.778778223980820306 ) ) ;
#52378=FACE_OUTER_BOUND ( 'NONE', #48504, .T. ) ;
#52379=CARTESIAN_POINT ( 'NONE',  ( 3.247140714122291438, -1.341038642068812736, -0.4257306128977228488 ) ) ;
#52383=DIRECTION ( 'NONE',  ( 0.9859154929577472748, 0.1672442547470080754, 0.000000000000000000 ) ) ;
#52384=CARTESIAN_POINT ( 'NONE',  ( 1.750000000000000000, -55.55000000278000272, 12.50000000000000000 ) ) ;
#52385=EDGE_LOOP ( 'NONE', ( #20178, #22403, #5538, #4189 ) ) ;
#52386=DIRECTION ( 'NONE',  ( 0.7071067811865475727, 0.000000000000000000, -0.7071067811865475727 ) ) ;
#52387=CARTESIAN_POINT ( 'NONE',  ( -1.750000000000000000, -60.04999999657000131, 12.50000000000000000 ) ) ;
#52390=EDGE_CURVE ( 'NONE', #58211, #44781, #17996, .T. ) ;
#52391=CARTESIAN_POINT ( 'NONE',  ( -0.06531150999164000992, -3.507872475527999967, 3.644635206812000039 ) ) ;
#52394=FACE_OUTER_BOUND ( 'NONE', #12952, .T. ) ;
#52395=CARTESIAN_POINT ( 'NONE',  ( 1.997276839918477265, -3.177083333333333481, -2.598917237794082791 ) ) ;
#52399=CARTESIAN_POINT ( 'NONE',  ( -0.004069935249280053416, -76.32474826787533573, -11.74984247143509464 ) ) ;
#52402=CARTESIAN_POINT ( 'NONE',  ( -1.004305231718999991, -1.000000000000000000, 3.090933677959000203 ) ) ;
#52403=CARTESIAN_POINT ( 'NONE',  ( 8.838834764832000701, -18.75000000000000000, -8.838834764832000701 ) ) ;
#52405=CARTESIAN_POINT ( 'NONE',  ( -3.395896365324738486, -0.7630208295731387702, -0.9134964888522767446 ) ) ;
#52413=DIRECTION ( 'NONE',  ( -0.8965517241377957136, -0.4429390544366978988, -5.195107294457976971E-07 ) ) ;
#52416=EDGE_CURVE ( 'NONE', #11264, #30968, #26088, .T. ) ;
#52417=CARTESIAN_POINT ( 'NONE',  ( 0.4254240051736071226, -1.364583333333333037, 3.250000000000001776 ) ) ;
#52418=VERTEX_POINT ( 'NONE', #12163 ) ;
#52421=CIRCLE ( 'NONE', #34478, 0.5000000000000006661 ) ;
#52422=ORIENTED_EDGE ( 'NONE', *, *, #20733, .F. ) ;
#52424=FACE_OUTER_BOUND ( 'NONE', #25973, .T. ) ;
#52428=CARTESIAN_POINT ( 'NONE',  ( 17.50000000000000000, -21.00000000000000000, 0.000000000000000000 ) ) ;
#52429=CIRCLE ( 'NONE', #23216, 0.8000000000000000444 ) ;
#52430=CARTESIAN_POINT ( 'NONE',  ( -0.5999999999999999778, -18.84999999999999787, 10.98362417419999915 ) ) ;
#52437=EDGE_CURVE ( 'NONE', #35953, #45142, #16595, .T. ) ;
#52439=CARTESIAN_POINT ( 'NONE',  ( -0.9650089711215688038, -2.999625284671528558, 3.117517381082792305 ) ) ;
#52445=CARTESIAN_POINT ( 'NONE',  ( -11.74981921324623535, -76.20131312293446513, -0.2383779811271709292 ) ) ;
#52446=CARTESIAN_POINT ( 'NONE',  ( 10.42274798264000069, -21.75365779208000205, 7.691916945395000482 ) ) ;
#52447=CARTESIAN_POINT ( 'NONE',  ( -8.950141054477999347, -62.00112627243999697, -8.958565985388998953 ) ) ;
#52448=CARTESIAN_POINT ( 'NONE',  ( -8.485281374238999419, -23.25000000000000000, 8.485281374238999419 ) ) ;
#52453=LINE ( 'NONE', #53027, #54536 ) ;
#52455=CARTESIAN_POINT ( 'NONE',  ( 1.232226823824839501, -24.52290911267632723, -12.50408896749732968 ) ) ;
#52456=CARTESIAN_POINT ( 'NONE',  ( -0.4636611700996999819, -76.79051831062999156, -12.20320586788999861 ) ) ;
#52460=CARTESIAN_POINT ( 'NONE',  ( 12.65987830577000040, -61.73692962272999551, 0.9847759095506000149 ) ) ;
#52461=CARTESIAN_POINT ( 'NONE',  ( -3.269659986048999656, -78.85953063649999706, -12.04652652115999878 ) ) ;
#52462=CARTESIAN_POINT ( 'NONE',  ( 12.49996905247000001, -55.60797343434000339, -1.666511841116000037 ) ) ;
#52467=VERTEX_POINT ( 'NONE', #39024 ) ;
#52470=EDGE_CURVE ( 'NONE', #54661, #52194, #54746, .T. ) ;
#52476=CARTESIAN_POINT ( 'NONE',  ( 12.69616050744000013, -58.55171076491000548, 1.799475304559999822 ) ) ;
#52478=VECTOR ( 'NONE', #57376, 1000.000000000000000 ) ;
#52480=ORIENTED_EDGE ( 'NONE', *, *, #27126, .T. ) ;
#52481=EDGE_LOOP ( 'NONE', ( #43619, #41522, #9497, #10437 ) ) ;
#52484=ADVANCED_FACE ( 'NONE', ( #52612 ), #44038, .F. ) ;
#52485=CARTESIAN_POINT ( 'NONE',  ( -10.19607599377606633, -78.15737564367177015, 5.890537601704129322 ) ) ;
#52487=ORIENTED_EDGE ( 'NONE', *, *, #47567, .F. ) ;
#52489=CARTESIAN_POINT ( 'NONE',  ( 8.438902753042999194, -78.73539140552688309, -8.898539530003999332 ) ) ;
#52491=CARTESIAN_POINT ( 'NONE',  ( 10.15833271780000047, -54.58011549179999378, 7.756208840337999177 ) ) ;
#52492=CARTESIAN_POINT ( 'NONE',  ( 7.921329716887100858, -17.44906234264657741, -10.04564005581343267 ) ) ;
#52496=DIRECTION ( 'NONE',  ( 0.7071067811865474617, 0.000000000000000000, 0.7071067811865474617 ) ) ;
#52498=CARTESIAN_POINT ( 'NONE',  ( -3.438348731682000281, -76.55047324479998849, -11.82003900998999946 ) ) ;
#52503=CARTESIAN_POINT ( 'NONE',  ( 6.688645397968000950, -78.77709438844000545, 10.27915892414000076 ) ) ;
#52507=CARTESIAN_POINT ( 'NONE',  ( 12.50686498856084228, -24.30484291404728481, -1.423095204833430438 ) ) ;
#52508=CARTESIAN_POINT ( 'NONE',  ( -12.50000000000000000, -60.04999999657000131, -1.750000000000000000 ) ) ;
#52509=CONICAL_SURFACE ( 'NONE', #17650, 0.6999999997695030007, 0.7853981633972997312 ) ;
#52511=CYLINDRICAL_SURFACE ( 'NONE', #17425, 1.750000000000001332 ) ;
#52512=DIRECTION ( 'NONE',  ( 0.000000000000000000, -1.000000000000000000, 0.000000000000000000 ) ) ;
#52514=CARTESIAN_POINT ( 'NONE',  ( 1.848759863635999867, -2.800056440563999605, 3.039663599590999965 ) ) ;
#52517=CARTESIAN_POINT ( 'NONE',  ( -12.70556836343000029, -53.57227722738999631, 1.774192865971000122E-09 ) ) ;
#52521=ORIENTED_EDGE ( 'NONE', *, *, #30353, .T. ) ;
#52526=CARTESIAN_POINT ( 'NONE',  ( -8.596763593984000806, -61.93532396089999992, 9.310159863737000663 ) ) ;
#52529=CARTESIAN_POINT ( 'NONE',  ( -10.42531125070999920, -60.06485145371000556, 7.624341767111000756 ) ) ;
#52530=CARTESIAN_POINT ( 'NONE',  ( -12.76303204291999904, -55.53514849259999409, -1.980584515756000030 ) ) ;
#52532=CARTESIAN_POINT ( 'NONE',  ( -12.70556836343000029, -53.57227722738999631, 1.774192865971000122E-09 ) ) ;
#52537=ADVANCED_FACE ( 'NONE', ( #17162 ), #40767, .F. ) ;
#52542=CARTESIAN_POINT ( 'NONE',  ( 1.799475295154000065, -57.04916621739000249, -12.69619287815999975 ) ) ;
#52545=EDGE_CURVE ( 'NONE', #57774, #9471, #29280, .T. ) ;
#52548=VECTOR ( 'NONE', #33446, 1000.000000000000000 ) ;
#52553=AXIS2_PLACEMENT_3D ( 'NONE', #2228, #12512, #34646 ) ;
#52554=ORIENTED_EDGE ( 'NONE', *, *, #22940, .T. ) ;
#52558=CARTESIAN_POINT ( 'NONE',  ( -0.2584144827919511722, -53.57154603038791407, 12.70558781482546706 ) ) ;
#52559=ADVANCED_FACE ( 'NONE', ( #40475 ), #45207, .F. ) ;
#52560=CARTESIAN_POINT ( 'NONE',  ( -3.148725677322000482, -78.06332093041999087, 12.40542962523000092 ) ) ;
#52562=DIRECTION ( 'NONE',  ( 0.000000000000000000, 0.000000000000000000, 1.000000000000000000 ) ) ;
#52565=EDGE_CURVE ( 'NONE', #34959, #33149, #46297, .T. ) ;
#52566=CARTESIAN_POINT ( 'NONE',  ( 1.034214221880000141E-14, 0.2999999999999999334, 0.000000000000000000 ) ) ;
#52573=LINE ( 'NONE', #48160, #46558 ) ;
#52574=CARTESIAN_POINT ( 'NONE',  ( 9.510318522500906369, -76.49977934536502744, 6.915946567881195328 ) ) ;
#52576=CARTESIAN_POINT ( 'NONE',  ( 1.980584515752000119, -55.53514853344000102, 12.76303204600000107 ) ) ;
#52578=DIRECTION ( 'NONE',  ( 0.000000000000000000, 1.000000000000000000, 0.000000000000000000 ) ) ;
#52579=FACE_OUTER_BOUND ( 'NONE', #11543, .T. ) ;
#52580=CARTESIAN_POINT ( 'NONE',  ( -7.641012305223999768, -18.71082276572999703, 10.18589226631999978 ) ) ;
#52584=B_SPLINE_CURVE_WITH_KNOTS ( 'NONE', 3,
 ( #65, #32174, #50214, #31294, #54059, #41349 ),
 .UNSPECIFIED., .F., .F.,
 ( 4, 1, 1, 4 ),
 ( 0.000000000000000000, 0.3333333311524483422, 0.6666666623049967155, 0.9999999934574449467 ),
 .UNSPECIFIED. ) ;
#52585=( NAMED_UNIT ( * ) PLANE_ANGLE_UNIT ( ) SI_UNIT ( $, .RADIAN. ) );
#52587=ORIENTED_EDGE ( 'NONE', *, *, #12618, .T. ) ;
#52594=CARTESIAN_POINT ( 'NONE',  ( -1.419463091678716093, -2.342021354265884536, -3.223257765105098649 ) ) ;
#52598=CARTESIAN_POINT ( 'NONE',  ( -7.710118476707999768, -21.74977139563000250, 10.18499221085999906 ) ) ;
#52599=CARTESIAN_POINT ( 'NONE',  ( 9.977465883888395837, -75.99422917656416132, 6.207251457660701632 ) ) ;
#52601=EDGE_LOOP ( 'NONE', ( #32050, #35092, #28875, #54808, #19379, #24293 ) ) ;
#52605=AXIS2_PLACEMENT_3D ( 'NONE', #55233, #6220, #10083 ) ;
#52609=CARTESIAN_POINT ( 'NONE',  ( 9.641208724080000181, -24.43394297700999829, -7.943747389698999406 ) ) ;
#52610=CARTESIAN_POINT ( 'NONE',  ( -0.2584144826940477091, -16.77154603077345385, 12.70558781487939015 ) ) ;
#52612=FACE_OUTER_BOUND ( 'NONE', #41561, .T. ) ;
#52613=CARTESIAN_POINT ( 'NONE',  ( -8.620921568068807161, -61.96528830388043474, 9.346042573940106735 ) ) ;
#52617=DIRECTION ( 'NONE',  ( -0.7071067811864980568, 0.7071067811865969777, -1.033897857523995979E-10 ) ) ;
#52620=CARTESIAN_POINT ( 'NONE',  ( 11.75000000000000000, -77.54999999999999716, 2.316376715183999699E-14 ) ) ;
#52621=CARTESIAN_POINT ( 'NONE',  ( -1.980584515756000030, -18.73514849905999924, 12.76303204340999997 ) ) ;
#52625=DIRECTION ( 'NONE',  ( 1.586878776513000076E-12, 1.000000000000000000, -3.446046439139999930E-10 ) ) ;
#52627=CARTESIAN_POINT ( 'NONE',  ( -12.49989425040000057, -23.19225390461999936, 1.666425739591000044 ) ) ;
#52628=VERTEX_POINT ( 'NONE', #22757 ) ;
#52629=VERTEX_POINT ( 'NONE', #10065 ) ;
#52630=CARTESIAN_POINT ( 'NONE',  ( -12.72554264789000023, -55.59839278072999491, -1.930240062458999928 ) ) ;
#52631=ORIENTED_EDGE ( 'NONE', *, *, #3718, .T. ) ;
#52632=ORIENTED_EDGE ( 'NONE', *, *, #21021, .F. ) ;
#52633=CARTESIAN_POINT ( 'NONE',  ( 10.53559655517000060, -23.20569178316999981, 7.620036226160999959 ) ) ;
#52636=AXIS2_PLACEMENT_3D ( 'NONE', #39193, #11770, #52496 ) ;
#52640=ORIENTED_EDGE ( 'NONE', *, *, #46100, .T. ) ;
#52641=ORIENTED_EDGE ( 'NONE', *, *, #23368, .T. ) ;
#52644=CARTESIAN_POINT ( 'NONE',  ( -12.54987272481000105, -61.85113590103000547, -0.1385846084898000041 ) ) ;
#52646=CARTESIAN_POINT ( 'NONE',  ( 7.691916945430000041, -20.24634220924000161, 10.42274798266999980 ) ) ;
#52647=AXIS2_PLACEMENT_3D ( 'NONE', #9515, #19246, #14801 ) ;
#52648=DIRECTION ( 'NONE',  ( 0.9999463328794432337, 0.000000000000000000, -0.01036008498777044214 ) ) ;
#52649=CARTESIAN_POINT ( 'NONE',  ( 9.689263856727277968, -53.82111184930475645, -8.274777958929785626 ) ) ;
#52651=CARTESIAN_POINT ( 'NONE',  ( 12.72558083409999874, -18.79866855842000106, -1.930284430576000076 ) ) ;
#52654=CARTESIAN_POINT ( 'NONE',  ( -9.310166272052999403, -53.66468533943000097, 8.596757084861000209 ) ) ;
#52656=EDGE_CURVE ( 'NONE', #44781, #52628, #28045, .T. ) ;
#52657=CARTESIAN_POINT ( 'NONE',  ( -9.108265402975000313, -17.12189187203999907, -8.478706101062000400 ) ) ;
#52660=CARTESIAN_POINT ( 'NONE',  ( -1.669724228656999987, -18.63102323466000243, -12.48434610067999984 ) ) ;
#52661=LINE ( 'NONE', #47681, #40196 ) ;
#52663=DIRECTION ( 'NONE',  ( -1.000000000000000000, 0.000000000000000000, 0.000000000000000000 ) ) ;
#52665=DIRECTION ( 'NONE',  ( 0.9999999923520045408, 0.000000000000000000, 0.0001236769620550006593 ) ) ;
#52667=ORIENTED_EDGE ( 'NONE', *, *, #21785, .T. ) ;
#52669=CARTESIAN_POINT ( 'NONE',  ( -12.52582323437078493, -60.60939730725204555, 1.680974276192793271 ) ) ;
#52670=CARTESIAN_POINT ( 'NONE',  ( -12.69616050747999836, -20.24828923609000242, 1.799475304559999822 ) ) ;
#52671=CARTESIAN_POINT ( 'NONE',  ( -2.434124730054000096, -3.288321030359000474, -2.925889700817000172 ) ) ;
#52672=CARTESIAN_POINT ( 'NONE',  ( -8.130813118348999780, -54.11476110100999648, 9.546856411314999846 ) ) ;
#52674=DIRECTION ( 'NONE',  ( 1.000000000000000000, 0.000000000000000000, 0.000000000000000000 ) ) ;
#52678=DIRECTION ( 'NONE',  ( 0.9999999999999693578, 2.479738204331925575E-07, 1.114546890695966335E-12 ) ) ;
#52681=CARTESIAN_POINT ( 'NONE',  ( 9.641515966524812242, -76.40113284977830688, -6.715584340997621027 ) ) ;
#52687=DIRECTION ( 'NONE',  ( 1.000000000000000000, 0.000000000000000000, 0.000000000000000000 ) ) ;
#52689=CARTESIAN_POINT ( 'NONE',  ( 0.000000000000000000, -51.86282895648000135, 0.000000000000000000 ) ) ;
#52691=AXIS2_PLACEMENT_3D ( 'NONE', #41307, #1758, #19168 ) ;
#52693=EDGE_CURVE ( 'NONE', #21397, #32631, #14761, .T. ) ;
#52698=ADVANCED_FACE ( 'NONE', ( #37202 ), #27464, .F. ) ;
#52701=EDGE_LOOP ( 'NONE', ( #2477, #42986, #45076, #45887, #35909 ) ) ;
#52707=VERTEX_POINT ( 'NONE', #13895 ) ;
#52708=CARTESIAN_POINT ( 'NONE',  ( 11.88041277708999921, -79.15000486637001131, -2.818394331568000233 ) ) ;
#52710=VERTEX_POINT ( 'NONE', #54922 ) ;
#52711=CARTESIAN_POINT ( 'NONE',  ( -7.640030264173999441, -60.10716680829000325, 10.18491080495000034 ) ) ;
#52712=CARTESIAN_POINT ( 'NONE',  ( -12.70556836352000118, -62.02772277195000328, -2.424224025342999716E-09 ) ) ;
#52714=CARTESIAN_POINT ( 'NONE',  ( -3.206516299415000049, -1.613032031399000088, -0.5298615117031000299 ) ) ;
#52721=CARTESIAN_POINT ( 'NONE',  ( -8.848566283551813072, -79.08854166669489416, 7.961923423609528427 ) ) ;
#52724=CYLINDRICAL_SURFACE ( 'NONE', #14277, 1.750000000000001332 ) ;
#52728=CARTESIAN_POINT ( 'NONE',  ( 0.7997484141426716153, -2.956625672363701440, 3.150668280190185300 ) ) ;
#52731=CARTESIAN_POINT ( 'NONE',  ( -9.369164850722000892, -23.25000000000000000, 7.601397897754999633 ) ) ;
#52734=CARTESIAN_POINT ( 'NONE',  ( 1.911540947291000103, -3.115794354202999994, 3.291214574437999918 ) ) ;
#52735=LINE ( 'NONE', #29697, #26115 ) ;
#52736=LINE ( 'NONE', #3433, #57394 ) ;
#52741=ADVANCED_FACE ( 'NONE', ( #45502 ), #32179, .T. ) ;
#52744=CARTESIAN_POINT ( 'NONE',  ( 12.30184311661000152, -75.83932607782000446, 1.220056246972000213 ) ) ;
#52745=ORIENTED_EDGE ( 'NONE', *, *, #51594, .F. ) ;
#52746=CARTESIAN_POINT ( 'NONE',  ( -12.00000000000000000, -18.75000000000000000, -1.750000000000000000 ) ) ;
#52748=CARTESIAN_POINT ( 'NONE',  ( 12.59682790095999927, -60.18734115192999923, 1.801645751184999922 ) ) ;
#52749=FACE_OUTER_BOUND ( 'NONE', #26743, .T. ) ;
#52754=ORIENTED_EDGE ( 'NONE', *, *, #49397, .T. ) ;
#52760=CARTESIAN_POINT ( 'NONE',  ( -7.387512494710283484, -55.38467666605774298, -8.150146600852353984 ) ) ;
#52763=EDGE_CURVE ( 'NONE', #46715, #26175, #14183, .T. ) ;
#52765=B_SPLINE_CURVE_WITH_KNOTS ( 'NONE', 3,
 ( #55256, #37533, #54965, #19538 ),
 .UNSPECIFIED., .F., .F.,
 ( 4, 4 ),
 ( 0.000000000000000000, 1.000000000000000000 ),
 .UNSPECIFIED. ) ;
#52766=ORIENTED_EDGE ( 'NONE', *, *, #57025, .T. ) ;
#52767=AXIS2_PLACEMENT_3D ( 'NONE', #56690, #20671, #16248 ) ;
#52768=DIRECTION ( 'NONE',  ( 0.000000000000000000, -1.000000000000000000, 0.000000000000000000 ) ) ;
#52770=CARTESIAN_POINT ( 'NONE',  ( 7.919595949288999570, -59.94999999967000548, 9.050966799188000067 ) ) ;
#52772=CARTESIAN_POINT ( 'NONE',  ( -12.70556836347999941, -25.22772277227999993, -2.424223956931999920E-09 ) ) ;
#52773=EDGE_CURVE ( 'NONE', #21248, #45320, #9767, .T. ) ;
#52774=ORIENTED_EDGE ( 'NONE', *, *, #12032, .T. ) ;
#52776=EDGE_CURVE ( 'NONE', #39540, #13397, #33999, .T. ) ;
#52778=CARTESIAN_POINT ( 'NONE',  ( 7.636247231009999581, -55.03676232846999739, 10.30460520059999929 ) ) ;
#52780=CARTESIAN_POINT ( 'NONE',  ( 7.169814592847524537, -77.37462369211782232, -9.346328727328229391 ) ) ;
#52782=LINE ( 'NONE', #33891, #44163 ) ;
#52783=LINE ( 'NONE', #49228, #10546 ) ;
#52784=CIRCLE ( 'NONE', #57494, 0.6000000000000008660 ) ;
#52785=CARTESIAN_POINT ( 'NONE',  ( -7.619389973898000434, -23.40786254230999930, 10.35398617733999949 ) ) ;
#52788=CARTESIAN_POINT ( 'NONE',  ( -12.65987793663000005, -17.06302453494999583, 0.9847129294438998759 ) ) ;
#52789=CARTESIAN_POINT ( 'NONE',  ( 13.94827586207000003, -33.10361340872000113, 8.082385094115998871E-06 ) ) ;
#52792=CARTESIAN_POINT ( 'NONE',  ( 7.943839548388014649, -78.36782549339653769, 9.082008725015928263 ) ) ;
#52793=CARTESIAN_POINT ( 'NONE',  ( -11.75000000000000000, -78.29999999999999716, 0.000000000000000000 ) ) ;
#52798=CARTESIAN_POINT ( 'NONE',  ( -1.952863295937999899, -3.631957716005000059, -2.785027970207999637 ) ) ;
#52799=EDGE_CURVE ( 'NONE', #42112, #26696, #41551, .T. ) ;
#52803=CARTESIAN_POINT ( 'NONE',  ( -11.75000000000000000, -75.80000000000001137, -9.948686767780999254E-14 ) ) ;
#52807=VERTEX_POINT ( 'NONE', #37788 ) ;
#52814=CARTESIAN_POINT ( 'NONE',  ( 0.007921339454490000653, -0.9192005770255999852, 3.538571077850000357 ) ) ;
#52816=DIRECTION ( 'NONE',  ( 0.000000000000000000, 0.000000000000000000, 1.000000000000000000 ) ) ;
#52818=ORIENTED_EDGE ( 'NONE', *, *, #33002, .F. ) ;
#52819=CARTESIAN_POINT ( 'NONE',  ( -12.70228859449707493, -53.97803615216450623, 1.213484947725372409 ) ) ;
#52820=CARTESIAN_POINT ( 'NONE',  ( -12.56594317825999951, -60.05000001354000005, 1.750000000000000000 ) ) ;
#52821=CARTESIAN_POINT ( 'NONE',  ( -1.680996261629376765, -1.683444032095494869, -2.810092171514073200 ) ) ;
#52824=ORIENTED_EDGE ( 'NONE', *, *, #13655, .F. ) ;
#52825=CIRCLE ( 'NONE', #44347, 0.5999999999999999778 ) ;
#52827=CARTESIAN_POINT ( 'NONE',  ( 0.5668640707187667660, -53.88340304924094681, -12.50470739225058736 ) ) ;
#52828=CARTESIAN_POINT ( 'NONE',  ( -1.749899258081046627, -55.41283151199903045, -12.55433901288159326 ) ) ;
#52829=B_SPLINE_CURVE_WITH_KNOTS ( 'NONE', 3,
 ( #5292, #23300, #41309, #54881, #11486, #42774, #20901, #56923, #33886, #7614, #24759, #52209, #2336, #20620, #34461, #52492, #38904, #16482, #25327, #20331, #2900, #29458, #16195, #38326 ),
 .UNSPECIFIED., .F., .F.,
 ( 4, 2, 2, 2, 2, 2, 2, 2, 2, 2, 2, 4 ),
 ( 0.000000000000000000, 0.1249999999999984457, 0.2499999999999968914, 0.3749999999999953371, 0.4374999999999954481, 0.4999999999999955591, 0.6249999999999957812, 0.7499999999999960032, 0.8124999999999968914, 0.8437499999999971134, 0.8749999999999974465, 1.000000000000000000 ),
 .UNSPECIFIED. ) ;
#52830=CARTESIAN_POINT ( 'NONE',  ( -12.71798269383000068, -55.50221245779999890, 1.931086388578000079 ) ) ;
#52833=CARTESIAN_POINT ( 'NONE',  ( 12.74365836111949335, -55.27810168850018613, -1.980611005600377617 ) ) ;
#52838=FACE_OUTER_BOUND ( 'NONE', #47147, .T. ) ;
#52839=EDGE_CURVE ( 'NONE', #2738, #2249, #57834, .T. ) ;
#52840=ORIENTED_EDGE ( 'NONE', *, *, #29472, .T. ) ;
#52841=CARTESIAN_POINT ( 'NONE',  ( 12.52582254647517424, -18.19059700816731961, 1.680974932934241606 ) ) ;
#52845=CARTESIAN_POINT ( 'NONE',  ( 0.2678032735624597538, -53.58567224682256835, 12.70526550765059248 ) ) ;
#52846=CARTESIAN_POINT ( 'NONE',  ( 12.36191581903000092, -76.89772347022000076, -3.311046255921999748 ) ) ;
#52848=CARTESIAN_POINT ( 'NONE',  ( -5.869402599192000025, -78.36567021304000491, 10.46661899222999992 ) ) ;
#52853=EDGE_LOOP ( 'NONE', ( #22858, #26904, #24235, #17315 ) ) ;
#52860=CARTESIAN_POINT ( 'NONE',  ( -8.130811096204000776, -61.48523690322999613, -9.546858433459998849 ) ) ;
#52861=EDGE_CURVE ( 'NONE', #33091, #25591, #56644, .T. ) ;
#52864=CARTESIAN_POINT ( 'NONE',  ( -11.00000000000000000, -74.59999999999999432, 0.000000000000000000 ) ) ;
#52865=CARTESIAN_POINT ( 'NONE',  ( -7.642147947538999730, -19.21514526754999963, 10.55910102244999926 ) ) ;
#52867=CARTESIAN_POINT ( 'NONE',  ( 10.07722254369999959, -20.25199022618999933, -7.718368845809999712 ) ) ;
#52870=CIRCLE ( 'NONE', #17985, 14.00000000000000000 ) ;
#52871=VERTEX_POINT ( 'NONE', #35661 ) ;
#52877=CARTESIAN_POINT ( 'NONE',  ( -8.768124086549999419, -55.65000000488999632, 7.919595949288999570 ) ) ;
#52879=CARTESIAN_POINT ( 'NONE',  ( 3.128537261037801720, -1.962059611134583381, -1.619158658661195016 ) ) ;
#52882=CARTESIAN_POINT ( 'NONE',  ( 0.5390150933986999071, -53.53739108314999839, -12.77520260999999913 ) ) ;
#52883=CARTESIAN_POINT ( 'NONE',  ( 9.771310077954293405, -75.99681162634880138, 6.525553964492908143 ) ) ;
#52885=CARTESIAN_POINT ( 'NONE',  ( -12.00000000000000000, -60.04999999966999980, 1.750000000000000000 ) ) ;
#52887=EDGE_CURVE ( 'NONE', #45976, #34794, #17973, .T. ) ;
#52888=DIRECTION ( 'NONE',  ( 0.000000000000000000, -1.000000000000000000, 0.000000000000000000 ) ) ;
#52889=CARTESIAN_POINT ( 'NONE',  ( 3.250000000000000000, -2.350000000000000089, 0.000000000000000000 ) ) ;
#52890=CARTESIAN_POINT ( 'NONE',  ( 9.505949683906999681, -79.00000000000000000, 6.906476714433999575 ) ) ;
#52891=CARTESIAN_POINT ( 'NONE',  ( 5.940599228801999379E-14, -5.950000000028880187, 0.000000000000000000 ) ) ;
#52892=AXIS2_PLACEMENT_3D ( 'NONE', #28563, #32984, #10879 ) ;
#52897=DIRECTION ( 'NONE',  ( -0.7592504785507919740, 0.04890181649404949649, -0.6489586451877930040 ) ) ;
#52902=CARTESIAN_POINT ( 'NONE',  ( 9.799981295308937135, -75.80000000000001137, -6.813203508582525991 ) ) ;
#52904=CARTESIAN_POINT ( 'NONE',  ( 10.19999999921000011, -0.2000000007865999907, -1.811584077144999807E-09 ) ) ;
#52908=EDGE_LOOP ( 'NONE', ( #5651, #38889, #21305, #16627, #20536 ) ) ;
#52910=CARTESIAN_POINT ( 'NONE',  ( -12.70228857842963421, -61.62190589578845845, -1.213561371295317048 ) ) ;
#52913=ORIENTED_EDGE ( 'NONE', *, *, #45640, .T. ) ;
#52918=CARTESIAN_POINT ( 'NONE',  ( 12.21456857099000004, -78.79487223422000852, -1.096995930408000142 ) ) ;
#52919=VERTEX_POINT ( 'NONE', #36264 ) ;
#52925=VERTEX_POINT ( 'NONE', #8814 ) ;
#52930=CARTESIAN_POINT ( 'NONE',  ( -12.44210192982000152, -60.88432059783999506, -1.464837683472000052 ) ) ;
#52933=CARTESIAN_POINT ( 'NONE',  ( 6.110725863692000104, -75.83846457245998351, 10.43515568098000124 ) ) ;
#52936=CARTESIAN_POINT ( 'NONE',  ( 9.346058022005980348, -53.63471832377268100, -8.620905970535309493 ) ) ;
#52938=CARTESIAN_POINT ( 'NONE',  ( 12.77649734584999841, -16.69171487512999974, 0.06478328530403998364 ) ) ;
#52943=CARTESIAN_POINT ( 'NONE',  ( 11.99999999979999821, -23.14999999072999870, -0.7999999997951999786 ) ) ;
#52945=CARTESIAN_POINT ( 'NONE',  ( -10.52693198617999926, -18.57847693927000066, -7.606025555766000146 ) ) ;
#52946=CARTESIAN_POINT ( 'NONE',  ( 7.626500777253000685, -60.11584731951999316, 10.35747145894000099 ) ) ;
#52947=CARTESIAN_POINT ( 'NONE',  ( -2.065394024360999836, -18.57838567354000148, -12.82193048528000112 ) ) ;
#52948=CARTESIAN_POINT ( 'NONE',  ( 1.995724882004761280, -1.278606234144347820, -2.597261706781343715 ) ) ;
#52954=VERTEX_POINT ( 'NONE', #9409 ) ;
#52957=CARTESIAN_POINT ( 'NONE',  ( 1.930009203937000040, -55.59900967650000325, 12.72537718775000037 ) ) ;
#52959=CARTESIAN_POINT ( 'NONE',  ( 0.2917981891545000095, -3.349647489337999939, -3.794822625742999556 ) ) ;
#52962=CARTESIAN_POINT ( 'NONE',  ( -12.54987159811999931, -53.74886760158999977, 0.1385534523824999975 ) ) ;
#52964=CARTESIAN_POINT ( 'NONE',  ( -2.842643194006085672, -2.059819327590527216, 1.637870626526546136 ) ) ;
#52965=CARTESIAN_POINT ( 'NONE',  ( -3.250000000000000000, -3.000000000000000000, 0.000000000000000000 ) ) ;
#52968=EDGE_CURVE ( 'NONE', #42686, #15955, #11525, .T. ) ;
#52969=CARTESIAN_POINT ( 'NONE',  ( 2.149016008433747960, -77.09224776600551365, -11.93500411286337659 ) ) ;
#52970=ADVANCED_FACE ( 'NONE', ( #56032 ), #29146, .F. ) ;
#52971=CARTESIAN_POINT ( 'NONE',  ( 9.679529469260824470, -76.40157007586634563, -6.660771595346317575 ) ) ;
#52973=CARTESIAN_POINT ( 'NONE',  ( 1.750000000001000089, -56.04922971509999741, -12.60356226394999979 ) ) ;
#52974=DIRECTION ( 'NONE',  ( 0.7071067811865475727, 0.000000000000000000, -0.7071067811865475727 ) ) ;
#52978=DIRECTION ( 'NONE',  ( 1.000000000000000000, 0.000000000000000000, 0.000000000000000000 ) ) ;
#52979=CARTESIAN_POINT ( 'NONE',  ( -10.20679554289983493, -17.76427274284850100, -7.770327721668349064 ) ) ;
#52982=DIRECTION ( 'NONE',  ( -0.7071067811865475727, 0.000000000000000000, -0.7071067811865475727 ) ) ;
#52985=VERTEX_POINT ( 'NONE', #37426 ) ;
#52986=CARTESIAN_POINT ( 'NONE',  ( -0.8898229089158170568, -25.02324531182626544, 12.70296869045239951 ) ) ;
#52987=EDGE_CURVE ( 'NONE', #17043, #8334, #13254, .T. ) ;
#52988=VERTEX_POINT ( 'NONE', #2308 ) ;
#52991=CARTESIAN_POINT ( 'NONE',  ( -8.838834764832000701, -60.04999999966999980, 8.838834764832000701 ) ) ;
#52996=ORIENTED_EDGE ( 'NONE', *, *, #40154, .F. ) ;
#52998=CARTESIAN_POINT ( 'NONE',  ( -7.732335774400000972, -78.48896835061999866, -9.449795707298999758 ) ) ;
#52999=EDGE_LOOP ( 'NONE', ( #2654, #17998, #42759, #55802, #28611, #45607, #47079, #39620 ) ) ;
#53000=CARTESIAN_POINT ( 'NONE',  ( 10.07627163191000008, -60.04999999657000131, -7.601397897754999633 ) ) ;
#53001=CARTESIAN_POINT ( 'NONE',  ( -10.98363359191198185, -18.81005173319954693, 0.5998275989261885321 ) ) ;
#53006=CARTESIAN_POINT ( 'NONE',  ( -7.957538301994783403, -79.08333333335991711, 8.845314404961204247 ) ) ;
#53007=CARTESIAN_POINT ( 'NONE',  ( -1.300465888139999970, -77.86117779481000412, -12.57433635189999954 ) ) ;
#53009=CARTESIAN_POINT ( 'NONE',  ( -10.14948852600000073, -22.75100835510000152, 7.674614791843000106 ) ) ;
#53011=TOROIDAL_SURFACE ( 'NONE', #35067, 1.250000000000000000, 0.5000000000000000000 ) ;
#53012=CARTESIAN_POINT ( 'NONE',  ( -10.04116292115999975, -56.03537109808000594, 7.682344222575999915 ) ) ;
#53013=CARTESIAN_POINT ( 'NONE',  ( -1.549588883243708803, -3.015970767069136027, 2.856984001263128015 ) ) ;
#53015=CARTESIAN_POINT ( 'NONE',  ( -1.103931348490902131, -24.62083748119153981, -12.50298439258945926 ) ) ;
#53017=CARTESIAN_POINT ( 'NONE',  ( 2.534829140202000008, -2.099668092570999622, 2.839140403359000420 ) ) ;
#53019=EDGE_LOOP ( 'NONE', ( #36217, #49362, #21321, #40941 ) ) ;
#53020=CARTESIAN_POINT ( 'NONE',  ( -9.205846894779998735, -61.80798911315000055, -8.541134278117000989 ) ) ;
#53021=EDGE_CURVE ( 'NONE', #21614, #34387, #11171, .T. ) ;
#53026=FACE_OUTER_BOUND ( 'NONE', #32416, .T. ) ;
#53027=CARTESIAN_POINT ( 'NONE',  ( 12.24999999909999993, -80.79999999910000952, 7.143947115078999467E-09 ) ) ;
#53028=VECTOR ( 'NONE', #27334, 1000.000000000000114 ) ;
#53030=CARTESIAN_POINT ( 'NONE',  ( -1.165746613897999928E-14, -72.79999999999999716, 0.000000000000000000 ) ) ;
#53031=CARTESIAN_POINT ( 'NONE',  ( 0.7751617840477000865, -76.53848582389998967, 12.18739828824000071 ) ) ;
#53032=ORIENTED_EDGE ( 'NONE', *, *, #1601, .T. ) ;
#53033=CIRCLE ( 'NONE', #48328, 14.00000000000000000 ) ;
#53035=CARTESIAN_POINT ( 'NONE',  ( -7.919595949288999570, -55.64999999965999677, 8.768124086712999699 ) ) ;
#53038=CARTESIAN_POINT ( 'NONE',  ( -10.98768124890674258, -18.54978970308804875, -0.5208900350597093221 ) ) ;
#53044=ORIENTED_EDGE ( 'NONE', *, *, #3159, .F. ) ;
#53046=ORIENTED_EDGE ( 'NONE', *, *, #56315, .F. ) ;
#53047=CARTESIAN_POINT ( 'NONE',  ( -10.10912517728183069, -60.27586858098902667, -7.634643689463517902 ) ) ;
#53049=ORIENTED_EDGE ( 'NONE', *, *, #5216, .F. ) ;
#53052=ORIENTED_EDGE ( 'NONE', *, *, #20245, .F. ) ;
#53053=ORIENTED_EDGE ( 'NONE', *, *, #9705, .F. ) ;
#53054=CIRCLE ( 'NONE', #33242, 0.5000000000000006661 ) ;
#53055=CARTESIAN_POINT ( 'NONE',  ( -8.852984619042215897, -78.14157800056186431, 7.764154262050229960 ) ) ;
#53058=ORIENTED_EDGE ( 'NONE', *, *, #33310, .T. ) ;
#53059=CARTESIAN_POINT ( 'NONE',  ( 10.98768124890679587, -18.54978970308837916, 0.5208900350585692340 ) ) ;
#53061=CARTESIAN_POINT ( 'NONE',  ( 6.954844635478175441, -79.22307562464830255, -10.07151940748270569 ) ) ;
#53063=B_SPLINE_CURVE_WITH_KNOTS ( 'NONE', 3,
 ( #2461, #51769, #42024, #51479, #38459, #24006, #47348, #6588, #11037, #1593, #47058, #19583, #29299, #15148, #42612, #23717, #6876, #56476, #16032, #28131, #57908, #52054, #7167, #24279 ),
 .UNSPECIFIED., .F., .F.,
 ( 4, 2, 2, 2, 2, 2, 2, 2, 2, 2, 2, 4 ),
 ( 0.000000000000000000, 0.1250000000000002776, 0.2500000000000005551, 0.3750000000000008327, 0.4375000000000006106, 0.5000000000000004441, 0.6249999999999993339, 0.7499999999999983347, 0.8124999999999977796, 0.8437499999999975575, 0.8749999999999972244, 1.000000000000000000 ),
 .UNSPECIFIED. ) ;
#53064=ADVANCED_FACE ( 'NONE', ( #29433 ), #41865, .T. ) ;
#53066=CARTESIAN_POINT ( 'NONE',  ( 8.485548443509999927, -53.91931586703000079, 9.101490738433000161 ) ) ;
#53069=CIRCLE ( 'NONE', #25763, 14.00000000000000000 ) ;
#53070=CARTESIAN_POINT ( 'NONE',  ( 12.70305380116828964, -61.83154493736390833, -0.8725910145092488079 ) ) ;
#53076=DIRECTION ( 'NONE',  ( 0.000000000000000000, 1.000000000000000000, 0.000000000000000000 ) ) ;
#53077=FACE_OUTER_BOUND ( 'NONE', #1102, .T. ) ;
#53078=LINE ( 'NONE', #20631, #15926 ) ;
#53079=CARTESIAN_POINT ( 'NONE',  ( 12.50000000000000000, -39.30476012429000576, 0.000000000000000000 ) ) ;
#53080=LINE ( 'NONE', #7341, #4599 ) ;
#53083=EDGE_CURVE ( 'NONE', #26528, #35802, #38767, .T. ) ;
#53086=CARTESIAN_POINT ( 'NONE',  ( -7.714303428875997959, -26.30294702886003222, -12.53545825868000385 ) ) ;
#53087=CARTESIAN_POINT ( 'NONE',  ( -1.719553322141999852, -1.968155165121999950, -3.292171862600000054 ) ) ;
#53089=CARTESIAN_POINT ( 'NONE',  ( -1.980584515752000119, -60.06485146591000301, 12.76303204605000197 ) ) ;
#53091=LINE ( 'NONE', #53373, #31670 ) ;
#53098=VECTOR ( 'NONE', #12065, 1000.000000000000000 ) ;
#53101=ADVANCED_FACE ( 'NONE', ( #6428 ), #34957, .F. ) ;
#53104=CARTESIAN_POINT ( 'NONE',  ( 1.675401668936999933, -1.380130151312000120, 3.116766381725000201 ) ) ;
#53106=CARTESIAN_POINT ( 'NONE',  ( 12.72394223969999949, -23.22159774865999893, -1.930881086224999876 ) ) ;
#53107=CARTESIAN_POINT ( 'NONE',  ( -2.062673488738000049, -60.12452529330000317, 12.82904091341000097 ) ) ;
#53110=CARTESIAN_POINT ( 'NONE',  ( 12.76303204517000012, -18.73514852243999940, -1.980584515753000208 ) ) ;
#53112=CARTESIAN_POINT ( 'NONE',  ( -12.55432891853854471, -18.61272687758821576, 1.749897736042294039 ) ) ;
#53114=CARTESIAN_POINT ( 'NONE',  ( -10.55911395187000146, -59.58461666436000570, -7.642160924878999673 ) ) ;
#53116=ORIENTED_EDGE ( 'NONE', *, *, #3, .T. ) ;
#53117=CARTESIAN_POINT ( 'NONE',  ( 11.00000000000000000, -4.000000000000000000, 0.000000000000000000 ) ) ;
#53119=CARTESIAN_POINT ( 'NONE',  ( -0.4254240051736147277, -1.114583333333333925, -3.250000000000000888 ) ) ;
#53121=CARTESIAN_POINT ( 'NONE',  ( 1.423904377294109791, -54.49487194733401907, 12.50677628652274898 ) ) ;
#53122=CARTESIAN_POINT ( 'NONE',  ( -9.788022091658000079, -54.27120090369999872, -7.956349397036000859 ) ) ;
#53125=EDGE_LOOP ( 'NONE', ( #23651, #45616, #34895, #43854 ) ) ;
#53126=ORIENTED_EDGE ( 'NONE', *, *, #17830, .F. ) ;
#53128=DIRECTION ( 'NONE',  ( 0.000000000000000000, -0.8191989533105277221, -0.5735094374942192319 ) ) ;
#53129=ORIENTED_EDGE ( 'NONE', *, *, #25882, .T. ) ;
#53134=CARTESIAN_POINT ( 'NONE',  ( 12.34410331423999985, -77.39726523887000553, -3.381164140480000135 ) ) ;
#53135=EDGE_CURVE ( 'NONE', #51746, #37664, #20023, .T. ) ;
#53140=B_SPLINE_CURVE_WITH_KNOTS ( 'NONE', 3,
 ( #15013, #51053, #41013, #54876, #32422, #18585, #1463, #46045 ),
 .UNSPECIFIED., .F., .F.,
 ( 4, 2, 2, 4 ),
 ( 0.000000000000000000, 0.5000000000000000000, 0.7500000000000000000, 1.000000000000000000 ),
 .UNSPECIFIED. ) ;
#53141=CARTESIAN_POINT ( 'NONE',  ( 8.894932048708428241, -16.77190732484968194, 9.073469156717420603 ) ) ;
#53142=ORIENTED_EDGE ( 'NONE', *, *, #32419, .T. ) ;
#53148=CARTESIAN_POINT ( 'NONE',  ( 2.597098890255110426, -3.158231272032415937, 2.378515465166538334 ) ) ;
#53149=CARTESIAN_POINT ( 'NONE',  ( 12.53239398059000109, -22.76486430425999785, 1.667936688463999895 ) ) ;
#53150=CARTESIAN_POINT ( 'NONE',  ( 5.917523019358037040, -76.63333333333329733, 10.26699006316254525 ) ) ;
#53154=CYLINDRICAL_SURFACE ( 'NONE', #48019, 1.750000000000000000 ) ;
#53161=LINE ( 'NONE', #30703, #46510 ) ;
#53167=CARTESIAN_POINT ( 'NONE',  ( -1.666727925320000026, -55.60825518191999350, -12.50018462901999960 ) ) ;
#53168=CARTESIAN_POINT ( 'NONE',  ( 11.15287131721528802, -75.97493627132392646, 3.701768527638496398 ) ) ;
#53171=CARTESIAN_POINT ( 'NONE',  ( -1.996743696302876181, -2.174344397066610313, -2.599173734966482741 ) ) ;
#53173=AXIS2_PLACEMENT_3D ( 'NONE', #46572, #15836, #42125 ) ;
#53178=CARTESIAN_POINT ( 'NONE',  ( -0.04193593611748243355, -16.98990258663360109, -12.50649570005621314 ) ) ;
#53180=CARTESIAN_POINT ( 'NONE',  ( 0.2265013221622945161, -78.57011497404765521, 11.74582188880687816 ) ) ;
#53182=ORIENTED_EDGE ( 'NONE', *, *, #18288, .F. ) ;
#53183=AXIS2_PLACEMENT_3D ( 'NONE', #43821, #57384, #16370 ) ;
#53186=LINE ( 'NONE', #31014, #44282 ) ;
#53190=CARTESIAN_POINT ( 'NONE',  ( -8.838834764832000701, -23.25000000000000000, -8.838834764832000701 ) ) ;
#53191=CARTESIAN_POINT ( 'NONE',  ( 10.98363357722939959, -23.18990228819981780, 0.5998278677060745467 ) ) ;
#53192=CARTESIAN_POINT ( 'NONE',  ( -10.98364304930883506, -23.23021036682267138, 0.5996544714383779118 ) ) ;
#53194=EDGE_LOOP ( 'NONE', ( #37160, #13696, #33221, #11631 ) ) ;
#53195=EDGE_CURVE ( 'NONE', #54081, #8704, #1243, .T. ) ;
#53196=CARTESIAN_POINT ( 'NONE',  ( 0.000000000000000000, -45.69638659094999866, 0.000000000000000000 ) ) ;
#53199=VERTEX_POINT ( 'NONE', #675 ) ;
#53200=LINE ( 'NONE', #22778, #22031 ) ;
#53201=ORIENTED_EDGE ( 'NONE', *, *, #2760, .F. ) ;
#53205=EDGE_CURVE ( 'NONE', #45494, #44485, #50536, .T. ) ;
#53210=AXIS2_PLACEMENT_3D ( 'NONE', #33958, #6816, #2117 ) ;
#53215=DIRECTION ( 'NONE',  ( -4.222595588675998455E-09, 0.9999999999999998890, 1.485890747956999830E-08 ) ) ;
#53217=CARTESIAN_POINT ( 'NONE',  ( -2.499318294468000357, -76.30897654196999724, 12.72266421702999928 ) ) ;
#53219=CARTESIAN_POINT ( 'NONE',  ( 10.36597025940859673, -55.02476146821044978, -7.635927901479407254 ) ) ;
#53221=CARTESIAN_POINT ( 'NONE',  ( 12.77657003524999979, -16.68789974453000369, -0.1588669551756000109 ) ) ;
#53222=CIRCLE ( 'NONE', #26823, 10.20000000000000107 ) ;
#53223=CARTESIAN_POINT ( 'NONE',  ( -9.636781270573999691, -24.44031362782000016, -7.948066289838000564 ) ) ;
#53225=VERTEX_POINT ( 'NONE', #5359 ) ;
#53227=CYLINDRICAL_SURFACE ( 'NONE', #25894, 0.5000000000000004441 ) ;
#53229=CARTESIAN_POINT ( 'NONE',  ( -9.641218323609999530, -17.56606991914999938, -7.943737929428000832 ) ) ;
#53233=CARTESIAN_POINT ( 'NONE',  ( 10.35845608626999947, -60.09778754156999980, -7.627487525433000570 ) ) ;
#53234=CARTESIAN_POINT ( 'NONE',  ( -12.05000000000000071, -75.80000000000001137, 0.000000000000000000 ) ) ;
#53236=LINE ( 'NONE', #12784, #53383 ) ;
#53238=ORIENTED_EDGE ( 'NONE', *, *, #36575, .F. ) ;
#53239=CARTESIAN_POINT ( 'NONE',  ( 3.251169438796622124, -1.361878590890881702, 0.4257723127115868866 ) ) ;
#53240=CARTESIAN_POINT ( 'NONE',  ( 1.666727925320000026, -55.60825518191999350, 12.50018462901999960 ) ) ;
#53241=CARTESIAN_POINT ( 'NONE',  ( -12.92177931909999877, -20.24263462181000151, 2.062503053667999797 ) ) ;
#53242=CARTESIAN_POINT ( 'NONE',  ( -1.744125200577000045, -3.548756781514999847, 2.929807332647999640 ) ) ;
#53246=CARTESIAN_POINT ( 'NONE',  ( 0.5390150933989998894, -62.06260891619000120, 12.77520261008999825 ) ) ;
#53247=CARTESIAN_POINT ( 'NONE',  ( 12.77306291386999959, -16.94129324301999873, 1.041150512314999999 ) ) ;
#53250=CARTESIAN_POINT ( 'NONE',  ( 10.66169269867642022, -77.16340856471717302, -5.782336216534432971 ) ) ;
#53253=CARTESIAN_POINT ( 'NONE',  ( -14.00000000000000000, -9.295797029142999435, 0.000000000000000000 ) ) ;
#53261=CARTESIAN_POINT ( 'NONE',  ( -10.42531125074000009, -18.73514854687000053, -7.624341767140999870 ) ) ;
#53263=ORIENTED_EDGE ( 'NONE', *, *, #49590, .F. ) ;
#53264=CARTESIAN_POINT ( 'NONE',  ( 8.441163350041684055, -53.88348045719643409, 9.243160719878805054 ) ) ;
#53266=ADVANCED_FACE ( 'NONE', ( #45529 ), #36646, .F. ) ;
#53267=DIRECTION ( 'NONE',  ( 0.000000000000000000, 1.000000000000000000, 0.000000000000000000 ) ) ;
#53270=ORIENTED_EDGE ( 'NONE', *, *, #51262, .T. ) ;
#53272=ORIENTED_EDGE ( 'NONE', *, *, #43146, .F. ) ;
#53273=DIRECTION ( 'NONE',  ( 4.079823248806000314E-14, 1.535319084990999808E-11, 1.000000000000000000 ) ) ;
#53274=ORIENTED_EDGE ( 'NONE', *, *, #47411, .T. ) ;
#53275=CARTESIAN_POINT ( 'NONE',  ( -10.98362417419999915, -18.84999999999999787, -0.5999999999999999778 ) ) ;
#53277=EDGE_CURVE ( 'NONE', #11044, #22044, #45822, .T. ) ;
#53279=CARTESIAN_POINT ( 'NONE',  ( 0.006333666751365999749, -25.33262644299999877, -12.77652491955999992 ) ) ;
#53282=ORIENTED_EDGE ( 'NONE', *, *, #41779, .F. ) ;
#53283=CARTESIAN_POINT ( 'NONE',  ( 17.50000000000000000, -13.07071424677999971, 2.026616721661999859E-13 ) ) ;
#53284=CARTESIAN_POINT ( 'NONE',  ( 9.965829256158000860, -78.80597494495999911, 7.308490088571999443 ) ) ;
#53285=ORIENTED_EDGE ( 'NONE', *, *, #5550, .T. ) ;
#53286=ORIENTED_EDGE ( 'NONE', *, *, #18886, .T. ) ;
#53288=CARTESIAN_POINT ( 'NONE',  ( -8.343860018000999190, -55.64999999967000122, 8.343860018000999190 ) ) ;
#53293=EDGE_CURVE ( 'NONE', #17043, #8334, #30281, .T. ) ;
#53294=CARTESIAN_POINT ( 'NONE',  ( -1.198731353186000215, -77.12333680668000113, -13.05866524906999970 ) ) ;
#53295=CARTESIAN_POINT ( 'NONE',  ( 11.54974070075000014, -78.02769171769000423, 5.138670156068000594 ) ) ;
#53296=ADVANCED_FACE ( 'NONE', ( #51414 ), #31560, .F. ) ;
#53301=AXIS2_PLACEMENT_3D ( 'NONE', #23521, #1115, #36802 ) ;
#53303=CARTESIAN_POINT ( 'NONE',  ( -0.05688989330080245627, -2.976795852111999263, 3.249363959324195417 ) ) ;
#53305=CARTESIAN_POINT ( 'NONE',  ( -0.5668640726167896160, -24.91659694980447171, -12.50470739226977379 ) ) ;
#53307=CARTESIAN_POINT ( 'NONE',  ( 3.190249742999000215, -1.952098507945999817, -2.075671974272999876 ) ) ;
#53310=DIRECTION ( 'NONE',  ( 0.000000000000000000, 1.000000000000000000, 0.000000000000000000 ) ) ;
#53313=CARTESIAN_POINT ( 'NONE',  ( -12.66737112516999986, -17.76697834132999887, -1.690666607834999891 ) ) ;
#53314=CARTESIAN_POINT ( 'NONE',  ( 11.88928085110999966, -78.30064632562000781, 5.289737169833999886 ) ) ;
#53316=CARTESIAN_POINT ( 'NONE',  ( 12.64500484465999897, -19.22847221992000044, -1.799490225533999732 ) ) ;
#53317=ORIENTED_EDGE ( 'NONE', *, *, #8781, .T. ) ;
#53318=CARTESIAN_POINT ( 'NONE',  ( -3.453171399369999950, -1.863032031399000088, -0.5706200895263999762 ) ) ;
#53330=ORIENTED_EDGE ( 'NONE', *, *, #34578, .F. ) ;
#53331=ORIENTED_EDGE ( 'NONE', *, *, #17231, .T. ) ;
#53333=CARTESIAN_POINT ( 'NONE',  ( -8.140250184780514431, -55.34839576620330348, -7.398464061247827850 ) ) ;
#53336=VERTEX_POINT ( 'NONE', #53720 ) ;
#53337=ORIENTED_EDGE ( 'NONE', *, *, #45921, .F. ) ;
#53341=B_SPLINE_SURFACE_WITH_KNOTS ( 'NONE', 3, 3, ( 
 ( #14973, #55130, #14675, #33265 ),
 ( #6122, #11155, #38284, #46883 ),
 ( #28246, #51883, #56305, #23540 ),
 ( #6414, #24427, #42443, #2010 ),
 ( #24718, #15859, #5825, #29129 ),
 ( #20009, #33845, #20289, #37991 ),
 ( #50725, #47177, #46300, #6708 ),
 ( #46009, #41554, #19124, #5531 ),
 ( #10267, #41848, #37406, #55427 ),
 ( #47752, #34423, #34995, #48323 ),
 ( #52172, #21438, #39448, #57161 ) ),
 .UNSPECIFIED., .F., .F., .F.,
 ( 4, 1, 1, 1, 1, 1, 1, 1, 4 ),
 ( 4, 4 ),
 ( -0.01994534136796000112, 0.000000000000000000, 0.1666666666667000196, 0.3333333333333000081, 0.5000000000000000000, 0.6666666666667000474, 0.8333333333333000637, 1.000000000000000000, 1.020519780480000138 ),
 ( -0.3582002740325999635, 1.358566136073000141 ),
 .UNSPECIFIED. ) ;
#53342=EDGE_CURVE ( 'NONE', #36311, #35802, #29599, .T. ) ;
#53343=CARTESIAN_POINT ( 'NONE',  ( 10.27275293713955584, -77.98886745049749436, 5.919664110522427691 ) ) ;
#53345=ORIENTED_EDGE ( 'NONE', *, *, #53777, .F. ) ;
#53347=ORIENTED_EDGE ( 'NONE', *, *, #14180, .T. ) ;
#53351=CARTESIAN_POINT ( 'NONE',  ( 0.5999663639300889528, -18.81035107904150294, 10.98362601162691377 ) ) ;
#53354=ADVANCED_FACE ( 'NONE', ( #26534 ), #45360, .F. ) ;
#53355=CARTESIAN_POINT ( 'NONE',  ( 7.626500777218999438, -55.48415267986000288, -10.35747145890000098 ) ) ;
#53362=CARTESIAN_POINT ( 'NONE',  ( -1.698401934077000019, -24.22014045903999957, 12.66748707612999958 ) ) ;
#53366=CARTESIAN_POINT ( 'NONE',  ( 12.66314513620999804, -61.97864743329000703, 0.04033065750138999789 ) ) ;
#53367=CARTESIAN_POINT ( 'NONE',  ( -12.00000000000000000, -23.15000000000000213, 0.000000000000000000 ) ) ;
#53373=CARTESIAN_POINT ( 'NONE',  ( 0.000000000000000000, -23.84999999976950136, -11.89999999977000122 ) ) ;
#53374=CARTESIAN_POINT ( 'NONE',  ( -7.678655902612509188, -18.20623020282190296, 10.03844298039528127 ) ) ;
#53379=VECTOR ( 'NONE', #45871, 1000.000000000000000 ) ;
#53380=CARTESIAN_POINT ( 'NONE',  ( -10.38646360829000059, -22.77795407709999864, -7.655555357433999397 ) ) ;
#53383=VECTOR ( 'NONE', #30782, 1000.000000000000000 ) ;
#53384=DIRECTION ( 'NONE',  ( 0.000000000000000000, -1.000000000000000000, 0.000000000000000000 ) ) ;
#53385=CARTESIAN_POINT ( 'NONE',  ( -9.934814764497000183, -61.42368287795999748, 7.968971842771999547 ) ) ;
#53386=CARTESIAN_POINT ( 'NONE',  ( -1.160983053055000047, -1.445977233352999880, 3.343027787781999827 ) ) ;
#53388=CARTESIAN_POINT ( 'NONE',  ( -2.597362135797363525, -3.152356596647883258, -1.996591761881967075 ) ) ;
#53389=CARTESIAN_POINT ( 'NONE',  ( -1.931086388455000025, -55.50221404479999876, 12.71798280852999952 ) ) ;
#53392=CARTESIAN_POINT ( 'NONE',  ( -12.60356226362999976, -59.55077028856999988, 1.750000000000000000 ) ) ;
#53396=ORIENTED_EDGE ( 'NONE', *, *, #34578, .T. ) ;
#53397=CARTESIAN_POINT ( 'NONE',  ( -12.50000000000000000, -18.75000000000000000, 0.000000000000000000 ) ) ;
#53398=CARTESIAN_POINT ( 'NONE',  ( 11.37980319050488198, -77.92613131821927652, -3.047449828435636388 ) ) ;
#53400=ORIENTED_EDGE ( 'NONE', *, *, #50576, .T. ) ;
#53405=ORIENTED_EDGE ( 'NONE', *, *, #12045, .T. ) ;
#53410=ORIENTED_EDGE ( 'NONE', *, *, #1537, .T. ) ;
#53412=AXIS2_PLACEMENT_3D ( 'NONE', #33353, #46680, #20655 ) ;
#53413=CYLINDRICAL_SURFACE ( 'NONE', #881, 1.750000000000001332 ) ;
#53414=PLANE ( 'NONE',  #51807 ) ;
#53416=CARTESIAN_POINT ( 'NONE',  ( 9.246161438659999732, -76.68655867677999538, -8.285323839175999794 ) ) ;
#53418=CIRCLE ( 'NONE', #54421, 12.50000000000000000 ) ;
#53420=CARTESIAN_POINT ( 'NONE',  ( 0.000000000000000000, -26.30294702885999669, 12.53545825868000207 ) ) ;
#53424=EDGE_CURVE ( 'NONE', #39336, #5887, #45842, .T. ) ;
#53426=CARTESIAN_POINT ( 'NONE',  ( 10.10448976475663407, -17.54884052604848677, 7.864761218169358692 ) ) ;
#53431=AXIS2_PLACEMENT_3D ( 'NONE', #47220, #11197, #38619 ) ;
#53433=CARTESIAN_POINT ( 'NONE',  ( -3.101110553533934944, -3.388432628819295633, -1.664369434271149473 ) ) ;
#53434=CARTESIAN_POINT ( 'NONE',  ( -9.841113773978118928, -17.16371975942079686, 8.121706172286355496 ) ) ;
#53435=B_SPLINE_CURVE_WITH_KNOTS ( 'NONE', 3,
 ( #21484, #17339, #53654, #21765, #3478, #4350 ),
 .UNSPECIFIED., .F., .F.,
 ( 4, 1, 1, 4 ),
 ( 0.000000000000000000, 0.3333333333333000081, 0.6666666666667000474, 1.000000000000000000 ),
 .UNSPECIFIED. ) ;
#53436=DIRECTION ( 'NONE',  ( 0.000000000000000000, -1.000000000000000000, 0.000000000000000000 ) ) ;
#53440=LINE ( 'NONE', #30411, #5554 ) ;
#53454=CARTESIAN_POINT ( 'NONE',  ( -1.200170490674999924, -54.36594297968999712, -12.43444080546999864 ) ) ;
#53455=CARTESIAN_POINT ( 'NONE',  ( 10.86825241270809173, -75.98052679898808037, 4.465012754454932953 ) ) ;
#53457=ORIENTED_EDGE ( 'NONE', *, *, #27467, .T. ) ;
#53460=CARTESIAN_POINT ( 'NONE',  ( -5.346699159600342810, -78.78725806292474942, -10.49909549695743749 ) ) ;
#53467=CARTESIAN_POINT ( 'NONE',  ( 3.768652233081607683, -78.54757323232175281, 11.12973672322252305 ) ) ;
#53468=CARTESIAN_POINT ( 'NONE',  ( -8.485281374238999419, -60.04999999966999980, -8.485281374238999419 ) ) ;
#53470=AXIS2_PLACEMENT_3D ( 'NONE', #37391, #28234, #51291 ) ;
#53476=TOROIDAL_SURFACE ( 'NONE', #51607, 17.50000000000000000, 5.000000000000000000 ) ;
#53479=VECTOR ( 'NONE', #10484, 1000.000000000000000 ) ;
#53482=LINE ( 'NONE', #13023, #32730 ) ;
#53483=CARTESIAN_POINT ( 'NONE',  ( 8.251806177693529420, -17.19944067082483841, -9.431051272833316901 ) ) ;
#53485=CARTESIAN_POINT ( 'NONE',  ( -12.43356840162999966, -24.71269674488000234, 0.8410229959428999758 ) ) ;
#53487=ORIENTED_EDGE ( 'NONE', *, *, #5166, .F. ) ;
#53490=ORIENTED_EDGE ( 'NONE', *, *, #45774, .F. ) ;
#53491=CARTESIAN_POINT ( 'NONE',  ( -1.777672186646999997, -78.93857582459999378, 12.13420648597999829 ) ) ;
#53493=CARTESIAN_POINT ( 'NONE',  ( 8.950141054446001831, -25.20112627276999717, 8.958565985356999661 ) ) ;
#53496=CARTESIAN_POINT ( 'NONE',  ( -12.50745077490000057, -24.99994448286999926, -2.662114616045000020E-09 ) ) ;
#53499=ADVANCED_FACE ( 'NONE', ( #18808 ), #31191, .F. ) ;
#53500=ORIENTED_EDGE ( 'NONE', *, *, #53021, .F. ) ;
#53508=CARTESIAN_POINT ( 'NONE',  ( -12.80447607892999962, -76.33341425608999486, -0.3146157217153000007 ) ) ;
#53515=EDGE_LOOP ( 'NONE', ( #32779, #4320, #11125, #18229 ) ) ;
#53517=CARTESIAN_POINT ( 'NONE',  ( -7.753900686106000251, -54.51068035512000165, 10.31980286347000053 ) ) ;
#53520=CARTESIAN_POINT ( 'NONE',  ( -12.76303204298000082, -60.06485150663000638, 1.980584515756000030 ) ) ;
#53521=LINE ( 'NONE', #20782, #24064 ) ;
#53523=EDGE_CURVE ( 'NONE', #46987, #6045, #54786, .T. ) ;
#53524=VECTOR ( 'NONE', #8232, 1000.000000000000000 ) ;
#53525=CARTESIAN_POINT ( 'NONE',  ( 0.6454797251636636979, -53.91193487831556297, 12.50471521364905136 ) ) ;
#53526=CARTESIAN_POINT ( 'NONE',  ( 10.38646360829000059, -56.02204592290999585, -7.655555357438999842 ) ) ;
#53527=CARTESIAN_POINT ( 'NONE',  ( 8.485281374238999419, 0.000000000000000000, -8.485281374238999419 ) ) ;
#53529=DIRECTION ( 'NONE',  ( 0.000000000000000000, -0.1122098755727947705, -0.9936845293270585300 ) ) ;
#53532=LINE ( 'NONE', #48820, #19729 ) ;
#53533=CARTESIAN_POINT ( 'NONE',  ( -1.629367637664000057, -55.11736356569000606, 12.46114270824000059 ) ) ;
#53534=CARTESIAN_POINT ( 'NONE',  ( 7.624341764926000131, -23.26485149464000202, -10.42531124853000080 ) ) ;
#53535=CARTESIAN_POINT ( 'NONE',  ( -1.162378416399999947, -1.642324315393999923, -3.286269575089999950 ) ) ;
#53536=B_SPLINE_CURVE_WITH_KNOTS ( 'NONE', 3,
 ( #9849, #23416, #41428, #1013, #14551, #50590 ),
 .UNSPECIFIED., .F., .F.,
 ( 4, 1, 1, 4 ),
 ( 0.000000000000000000, 0.3333333333333000081, 0.6666666666667000474, 1.000000000000000000 ),
 .UNSPECIFIED. ) ;
#53538=CARTESIAN_POINT ( 'NONE',  ( -2.839805762151337731, -1.541666666666666519, -1.636761686205423949 ) ) ;
#53539=DIRECTION ( 'NONE',  ( 0.000000000000000000, 0.000000000000000000, -1.000000000000000000 ) ) ;
#53540=CARTESIAN_POINT ( 'NONE',  ( -1.798954018877999994, -60.01530973353999343, 12.61117007304000026 ) ) ;
#53541=CARTESIAN_POINT ( 'NONE',  ( 12.68625206996000010, -18.23580249185999946, 1.886949102778999965 ) ) ;
#53546=CARTESIAN_POINT ( 'NONE',  ( -11.81296717809978780, -76.93658351881686031, 2.479319390824800795 ) ) ;
#53547=CARTESIAN_POINT ( 'NONE',  ( -3.734482694269000369, -78.39436234271001069, 11.50161222062999933 ) ) ;
#53552=DIRECTION ( 'NONE',  ( 0.000000000000000000, 1.000000000000000000, 0.000000000000000000 ) ) ;
#53554=CARTESIAN_POINT ( 'NONE',  ( -7.601397897754999633, -23.25000000000000000, -9.369164850722000892 ) ) ;
#53564=ORIENTED_EDGE ( 'NONE', *, *, #38169, .F. ) ;
#53566=B_SPLINE_CURVE_WITH_KNOTS ( 'NONE', 3,
 ( #23797, #28509, #46560, #14935, #32351, #10232 ),
 .UNSPECIFIED., .F., .F.,
 ( 4, 1, 1, 4 ),
 ( 0.000000000000000000, 0.3333333333333000081, 0.6666666666667000474, 1.000000000000000000 ),
 .UNSPECIFIED. ) ;
#53567=ORIENTED_EDGE ( 'NONE', *, *, #13539, .F. ) ;
#53570=CARTESIAN_POINT ( 'NONE',  ( 7.919595949288999570, -59.94999999040999938, -9.050966798898000931 ) ) ;
#53575=CARTESIAN_POINT ( 'NONE',  ( 1.582498447119000229, -24.15086122477999808, -12.55493832972999968 ) ) ;
#53579=CARTESIAN_POINT ( 'NONE',  ( 9.846220907398999245, -78.71889409522999870, 7.220774715475999805 ) ) ;
#53580=ORIENTED_EDGE ( 'NONE', *, *, #45970, .F. ) ;
#53582=CARTESIAN_POINT ( 'NONE',  ( -0.7999999997951999786, -18.85000000927000130, 11.99999999979999821 ) ) ;
#53586=FACE_BOUND ( 'NONE', #51631, .T. ) ;
#53588=CARTESIAN_POINT ( 'NONE',  ( -9.306321164319999895, -77.06783216571999162, -9.238944841226000904 ) ) ;
#53589=CARTESIAN_POINT ( 'NONE',  ( 5.420640129221999892, -77.08411282133998554, 11.42023903890000014 ) ) ;
#53593=CARTESIAN_POINT ( 'NONE',  ( -10.07722254368999870, -57.05199022587000002, 7.718368845804999268 ) ) ;
#53594=CARTESIAN_POINT ( 'NONE',  ( 1.100350654334843359, -2.948830382931522109, 3.057717532207668398 ) ) ;
#53596=CIRCLE ( 'NONE', #28130, 11.75000000000000178 ) ;
#53598=CARTESIAN_POINT ( 'NONE',  ( 0.000000000000000000, -26.93717104351999936, 0.000000000000000000 ) ) ;
#53600=CARTESIAN_POINT ( 'NONE',  ( -2.707053224964000027, -2.685967474678999878, 2.675433656965999774 ) ) ;
#53602=ORIENTED_EDGE ( 'NONE', *, *, #9568, .T. ) ;
#53605=B_SPLINE_CURVE_WITH_KNOTS ( 'NONE', 3,
 ( #12454, #7742, #20744, #33729, #47639, #51764 ),
 .UNSPECIFIED., .F., .F.,
 ( 4, 1, 1, 4 ),
 ( 0.000000000000000000, 0.3333333333333000081, 0.6666666666667000474, 1.000000000000000000 ),
 .UNSPECIFIED. ) ;
#53606=LINE ( 'NONE', #57733, #49651 ) ;
#53608=CARTESIAN_POINT ( 'NONE',  ( -12.48375942317000131, -18.62730665102000316, -1.669542353227000175 ) ) ;
#53609=CARTESIAN_POINT ( 'NONE',  ( -12.97861384075000046, -77.98845645414000671, -0.9459496016724999734 ) ) ;
#53611=CARTESIAN_POINT ( 'NONE',  ( 12.49306752634999995, -18.71943307332999851, -1.667917367010000040 ) ) ;
#53612=VERTEX_POINT ( 'NONE', #11988 ) ;
#53613=EDGE_CURVE ( 'NONE', #456, #36279, #33106, .T. ) ;
#53614=CARTESIAN_POINT ( 'NONE',  ( -0.7999999997951999786, -23.14999999072999870, -11.99999999979999821 ) ) ;
#53615=CARTESIAN_POINT ( 'NONE',  ( 9.243145380909270514, -53.88347263105222851, -8.441178781369352180 ) ) ;
#53617=CARTESIAN_POINT ( 'NONE',  ( -1.667916687331000070, -23.29848884437999956, -12.49168451098999988 ) ) ;
#53620=CARTESIAN_POINT ( 'NONE',  ( 3.981113306789000106, -0.9874747695768000266, -0.5296481109823999445 ) ) ;
#53623=ORIENTED_EDGE ( 'NONE', *, *, #1322, .F. ) ;
#53627=EDGE_LOOP ( 'NONE', ( #880, #57354, #49319, #31170 ) ) ;
#53630=EDGE_CURVE ( 'NONE', #25746, #46308, #50758, .T. ) ;
#53633=ORIENTED_EDGE ( 'NONE', *, *, #35296, .F. ) ;
#53636=VERTEX_POINT ( 'NONE', #34685 ) ;
#53637=CARTESIAN_POINT ( 'NONE',  ( 0.000000000000000000, -0.8249999994726999741, 0.000000000000000000 ) ) ;
#53638=AXIS2_PLACEMENT_3D ( 'NONE', #25056, #56936, #34475 ) ;
#53640=DIRECTION ( 'NONE',  ( 0.000000000000000000, 1.000000000000000000, 3.788597347406000047E-11 ) ) ;
#53643=ORIENTED_EDGE ( 'NONE', *, *, #1322, .T. ) ;
#53645=EDGE_CURVE ( 'NONE', #2471, #7601, #30550, .T. ) ;
#53648=CIRCLE ( 'NONE', #18767, 13.00000000000000000 ) ;
#53649=CARTESIAN_POINT ( 'NONE',  ( -7.640030264154999529, -18.69283319134000010, -10.18491080493000212 ) ) ;
#53650=CARTESIAN_POINT ( 'NONE',  ( 10.26578641119535007, -77.40555308739415352, -5.914033253227731990 ) ) ;
#53651=CARTESIAN_POINT ( 'NONE',  ( -11.44417895085272008, -78.77916666666666856, 3.075537641221497420 ) ) ;
#53653=B_SPLINE_CURVE_WITH_KNOTS ( 'NONE', 3,
 ( #20707, #38707, #40676, #29834, #38998, #31198, #57006, #18247 ),
 .UNSPECIFIED., .F., .F.,
 ( 4, 2, 2, 4 ),
 ( 0.000000000000000000, 0.5000000000000000000, 0.7500000000000000000, 1.000000000000000000 ),
 .UNSPECIFIED. ) ;
#53654=CARTESIAN_POINT ( 'NONE',  ( -10.18496935386999880, -20.24935285395000051, -7.710095619721000659 ) ) ;
#53655=CARTESIAN_POINT ( 'NONE',  ( 0.5999663639301143769, -23.18964892095651464, -10.98362601162690844 ) ) ;
#53659=CARTESIAN_POINT ( 'NONE',  ( -12.56594317823000040, -23.25000001387000026, 1.750000000000000000 ) ) ;
#53662=CARTESIAN_POINT ( 'NONE',  ( -1.930638663166000191, -23.22122063288999883, 12.72375916873000001 ) ) ;
#53665=CARTESIAN_POINT ( 'NONE',  ( 2.266888174815000045, -1.555016836958999837, -3.242122062176999719 ) ) ;
#53668=CARTESIAN_POINT ( 'NONE',  ( 12.54976804513999866, -61.84775476195000010, 0.05637402076003000112 ) ) ;
#53674=VECTOR ( 'NONE', #11370, 1000.000000000000000 ) ;
#53679=ORIENTED_EDGE ( 'NONE', *, *, #24009, .F. ) ;
#53685=DIRECTION ( 'NONE',  ( 0.7071067811865475727, 0.000000000000000000, -0.7071067811865475727 ) ) ;
#53688=CARTESIAN_POINT ( 'NONE',  ( -10.52693147742000157, -60.22153431716999705, 7.606024891127000309 ) ) ;
#53690=AXIS2_PLACEMENT_3D ( 'NONE', #15205, #37051, #24063 ) ;
#53691=CARTESIAN_POINT ( 'NONE',  ( 3.101351771310999705, -1.335516836959000031, -2.020112785969000235 ) ) ;
#53693=CARTESIAN_POINT ( 'NONE',  ( 12.77297283014999962, -24.72822696531000020, -1.476112654659999857 ) ) ;
#53694=CYLINDRICAL_SURFACE ( 'NONE', #30202, 1.750000000000000000 ) ;
#53695=VERTEX_POINT ( 'NONE', #21696 ) ;
#53696=CARTESIAN_POINT ( 'NONE',  ( -12.70451544420788537, -54.24534321881070298, 1.498804046722062022 ) ) ;
#53701=CARTESIAN_POINT ( 'NONE',  ( -10.38645071868999992, -56.02180874340999850, -7.655542440077000244 ) ) ;
#53703=EDGE_CURVE ( 'NONE', #57279, #33091, #48297, .T. ) ;
#53707=CARTESIAN_POINT ( 'NONE',  ( 9.019414221601653736, -61.79291943934637032, -8.666941069242449558 ) ) ;
#53708=CARTESIAN_POINT ( 'NONE',  ( -1.001315001699999874, -54.11477588220000001, -12.50000000000000000 ) ) ;
#53710=VERTEX_POINT ( 'NONE', #3412 ) ;
#53711=CARTESIAN_POINT ( 'NONE',  ( -8.541162059860999634, -53.79199348416999982, -9.205819316548000231 ) ) ;
#53713=VERTEX_POINT ( 'NONE', #21412 ) ;
#53714=ORIENTED_EDGE ( 'NONE', *, *, #18963, .T. ) ;
#53718=VERTEX_POINT ( 'NONE', #39704 ) ;
#53719=EDGE_CURVE ( 'NONE', #5420, #50457, #17058, .T. ) ;
#53720=CARTESIAN_POINT ( 'NONE',  ( -10.42531124905999995, -23.26485148473999942, -7.624341765453999997 ) ) ;
#53723=CARTESIAN_POINT ( 'NONE',  ( 5.690325051763000630, -78.42027720837999993, 11.64023780191999968 ) ) ;
#53725=CARTESIAN_POINT ( 'NONE',  ( 0.000000000000000000, -22.78578169018998878, 13.15643568216998638 ) ) ;
#53729=CARTESIAN_POINT ( 'NONE',  ( 9.175589925000075198, -16.77304466865986399, 8.792768277085899697 ) ) ;
#53731=DIRECTION ( 'NONE',  ( 0.000000000000000000, 1.000000000000000000, 0.000000000000000000 ) ) ;
#53732=CARTESIAN_POINT ( 'NONE',  ( 1.623944433304999935, -76.18752863036999656, -12.20239005717999881 ) ) ;
#53736=CARTESIAN_POINT ( 'NONE',  ( 1.949429650119547164, -2.680776606104624094, 3.205215495301868334 ) ) ;
#53737=AXIS2_PLACEMENT_3D ( 'NONE', #27854, #37303, #37889 ) ;
#53738=CARTESIAN_POINT ( 'NONE',  ( 12.50000000000000000, -54.11640971901999819, -1.003652782195000093 ) ) ;
#53743=CARTESIAN_POINT ( 'NONE',  ( -7.710763962805349259, -76.98020946934893516, 9.280496569891228731 ) ) ;
#53746=PLANE ( 'NONE',  #45110 ) ;
#53747=ORIENTED_EDGE ( 'NONE', *, *, #55685, .T. ) ;
#53749=LINE ( 'NONE', #32162, #46671 ) ;
#53752=CARTESIAN_POINT ( 'NONE',  ( 7.648026768019999366, -23.24999998419999869, 10.12290050217000115 ) ) ;
#53756=CARTESIAN_POINT ( 'NONE',  ( -1.484804496640999893, -54.08130846584000295, -12.77261165604999960 ) ) ;
#53759=FACE_OUTER_BOUND ( 'NONE', #42034, .T. ) ;
#53760=ORIENTED_EDGE ( 'NONE', *, *, #39447, .F. ) ;
#53761=CARTESIAN_POINT ( 'NONE',  ( 12.56594317982999875, -55.55000000504000468, -1.750000000000000000 ) ) ;
#53765=EDGE_CURVE ( 'NONE', #54609, #57120, #51495, .T. ) ;
#53770=CARTESIAN_POINT ( 'NONE',  ( -4.820688262674111435, -78.60634528047508240, 10.76661437165540747 ) ) ;
#53775=CARTESIAN_POINT ( 'NONE',  ( 10.41874210216987073, -75.80000000000002558, -5.821609190279006363 ) ) ;
#53777=EDGE_CURVE ( 'NONE', #17469, #42116, #28078, .T. ) ;
#53778=B_SPLINE_CURVE_WITH_KNOTS ( 'NONE', 3,
 ( #52, #921, #18903, #22446, #54908, #14460, #22741, #53752 ),
 .UNSPECIFIED., .F., .F.,
 ( 4, 2, 2, 4 ),
 ( 0.000000000000000000, 0.5000000000000007772, 0.7500000000000003331, 1.000000000000000000 ),
 .UNSPECIFIED. ) ;
#53780=DIRECTION ( 'NONE',  ( 0.000000000000000000, -1.000000000000000000, 0.000000000000000000 ) ) ;
#53781=CARTESIAN_POINT ( 'NONE',  ( 7.601397897754999633, -55.55000000278000272, -10.07627163191000008 ) ) ;
#53785=CARTESIAN_POINT ( 'NONE',  ( -1.750000000001000089, -60.04999998641999781, 12.56594318054000148 ) ) ;
#53786=CARTESIAN_POINT ( 'NONE',  ( -12.70259419122151989, -61.53882758497012873, -1.314635108434076383 ) ) ;
#53793=CARTESIAN_POINT ( 'NONE',  ( -4.802691730569000228, -78.45956385665999733, 11.09149278351999968 ) ) ;
#53794=ORIENTED_EDGE ( 'NONE', *, *, #57533, .F. ) ;
#53795=CARTESIAN_POINT ( 'NONE',  ( 8.478749451758998745, -24.87812788920000173, 9.108222796172999125 ) ) ;
#53802=ORIENTED_EDGE ( 'NONE', *, *, #40509, .F. ) ;
#53808=CARTESIAN_POINT ( 'NONE',  ( -2.113979906412999821, -75.85601843290000090, -12.47295230648999897 ) ) ;
#53811=DIRECTION ( 'NONE',  ( 0.7071067811865475727, 0.000000000000000000, -0.7071067811865475727 ) ) ;
#53812=CARTESIAN_POINT ( 'NONE',  ( 12.43359548536000148, -17.29290601378000147, -0.8500179128024000219 ) ) ;
#53813=CARTESIAN_POINT ( 'NONE',  ( -10.18948929998999908, -23.21532694344000092, -7.645397820736000050 ) ) ;
#53822=CARTESIAN_POINT ( 'NONE',  ( -10.36289663187999999, -18.79893657682999830, 7.633501051924000080 ) ) ;
#53826=CARTESIAN_POINT ( 'NONE',  ( 10.01332852686999964, -55.51943464808999806, -7.654537165450999936 ) ) ;
#53827=CARTESIAN_POINT ( 'NONE',  ( 1.568318300085000120E-14, -0.05000000003700048185, 0.000000000000000000 ) ) ;
#53829=FACE_OUTER_BOUND ( 'NONE', #6313, .T. ) ;
#53831=ORIENTED_EDGE ( 'NONE', *, *, #36575, .T. ) ;
#53832=CARTESIAN_POINT ( 'NONE',  ( 3.168764867850674793, -1.372313138392203369, 0.8503644209021197220 ) ) ;
#53833=CARTESIAN_POINT ( 'NONE',  ( 1.761265949711000145, -55.09141781180999686, 12.57448205041000122 ) ) ;
#53835=DIRECTION ( 'NONE',  ( -0.7071067811865475727, 0.000000000000000000, -0.7071067811865475727 ) ) ;
#53836=CARTESIAN_POINT ( 'NONE',  ( -3.736288849819999758, -2.332852077435000115, -1.330886568031999895 ) ) ;
#53840=DIRECTION ( 'NONE',  ( 0.000000000000000000, -1.000000000000000000, 0.000000000000000000 ) ) ;
#53841=CARTESIAN_POINT ( 'NONE',  ( -1.698401934075999931, -61.02014045872000025, 12.66748707616000047 ) ) ;
#53842=CARTESIAN_POINT ( 'NONE',  ( 0.000000000000000000, -60.04999999966999980, 12.50000000000000000 ) ) ;
#53844=DIRECTION ( 'NONE',  ( 0.000000000000000000, 1.000000000000000000, 0.000000000000000000 ) ) ;
#53845=B_SPLINE_CURVE_WITH_KNOTS ( 'NONE', 3,
 ( #41532, #37092, #22942, #54245, #23810, #27648, #55109, #5229, #14654, #32649 ),
 .UNSPECIFIED., .F., .F.,
 ( 4, 2, 2, 2, 4 ),
 ( 0.000000000000000000, 0.2500000000000000000, 0.5000000000000000000, 0.7500000000000000000, 1.000000000000000000 ),
 .UNSPECIFIED. ) ;
#53846=CARTESIAN_POINT ( 'NONE',  ( 6.162632954033368193, -76.78536682155184678, 10.39017533730111964 ) ) ;
#53847=CARTESIAN_POINT ( 'NONE',  ( 12.43608888892000053, -79.01247494496000456, 1.073723900664999897 ) ) ;
#53849=AXIS2_PLACEMENT_3D ( 'NONE', #15810, #42098, #32626 ) ;
#53853=CARTESIAN_POINT ( 'NONE',  ( -0.2678032732400780769, -62.01432775263499764, 12.70526550773306340 ) ) ;
#53855=CARTESIAN_POINT ( 'NONE',  ( -12.61112459821999998, -60.01565178538000112, 1.798929298655999931 ) ) ;
#53860=CARTESIAN_POINT ( 'NONE',  ( 8.872949061366725232, -53.78989818412265578, 8.813905827834215501 ) ) ;
#53863=DIRECTION ( 'NONE',  ( 0.7071067811865475727, 0.000000000000000000, -0.7071067811865475727 ) ) ;
#53865=ORIENTED_EDGE ( 'NONE', *, *, #15642, .F. ) ;
#53867=AXIS2_PLACEMENT_3D ( 'NONE', #5652, #1254, #19241 ) ;
#53868=ORIENTED_EDGE ( 'NONE', *, *, #55651, .T. ) ;
#53869=DIRECTION ( 'NONE',  ( 0.000000000000000000, -1.000000000000000000, 0.000000000000000000 ) ) ;
#53871=VECTOR ( 'NONE', #18282, 1000.000000000000114 ) ;
#53872=CARTESIAN_POINT ( 'NONE',  ( -1.691611010928000036, -17.76917308770000048, 12.66722148969999928 ) ) ;
#53873=FACE_BOUND ( 'NONE', #45978, .T. ) ;
#53876=CARTESIAN_POINT ( 'NONE',  ( 1.761265949708000100, -23.70858218785999938, -12.57448205042999945 ) ) ;
#53879=ORIENTED_EDGE ( 'NONE', *, *, #23221, .F. ) ;
#53881=CARTESIAN_POINT ( 'NONE',  ( 12.10989215130000041, -79.17874558444999877, 1.561551467148000194 ) ) ;
#53882=ORIENTED_EDGE ( 'NONE', *, *, #1068, .F. ) ;
#53883=EDGE_LOOP ( 'NONE', ( #50320, #35974, #17684, #27965 ) ) ;
#53884=DIRECTION ( 'NONE',  ( 0.000000000000000000, 0.000000000000000000, 1.000000000000000000 ) ) ;
#53885=CARTESIAN_POINT ( 'NONE',  ( 1.250000000000000000, -60.04999999966999980, 12.00000000000000000 ) ) ;
#53886=EDGE_CURVE ( 'NONE', #43107, #52954, #8473, .T. ) ;
#53891=CARTESIAN_POINT ( 'NONE',  ( -12.92190527446000026, -77.92433021234000989, -0.9418163832602000074 ) ) ;
#53892=EDGE_CURVE ( 'NONE', #17898, #43107, #18667, .T. ) ;
#53898=CARTESIAN_POINT ( 'NONE',  ( -10.24998526317999925, -57.04916621739000249, 7.705142895613999343 ) ) ;
#53899=CARTESIAN_POINT ( 'NONE',  ( 5.629678282322556626, -76.86401920440739843, -10.39394257255064780 ) ) ;
#53904=CARTESIAN_POINT ( 'NONE',  ( 1.068619641472000170, -1.930313715633000138, -3.652926003266999899 ) ) ;
#53906=ORIENTED_EDGE ( 'NONE', *, *, #56872, .T. ) ;
#53907=CARTESIAN_POINT ( 'NONE',  ( -0.5812841321855987120, -23.30416868476589798, 10.98463311464191605 ) ) ;
#53908=CARTESIAN_POINT ( 'NONE',  ( 0.000000000000000000, 0.000000000000000000, 0.000000000000000000 ) ) ;
#53912=CARTESIAN_POINT ( 'NONE',  ( -12.54976795933000133, -16.95224500006000312, 0.05636009750358000198 ) ) ;
#53913=CARTESIAN_POINT ( 'NONE',  ( 6.891227191158999510, -76.65634507106000228, -9.824000600561999974 ) ) ;
#53914=AXIS2_PLACEMENT_3D ( 'NONE', #15811, #24082, #19961 ) ;
#53915=CARTESIAN_POINT ( 'NONE',  ( -9.164385193292622134, -62.01567483102901690, -8.803702036947488097 ) ) ;
#53916=CARTESIAN_POINT ( 'NONE',  ( 12.64502302235000109, -22.77129148951999937, -1.799490220168999954 ) ) ;
#53917=ORIENTED_EDGE ( 'NONE', *, *, #25191, .T. ) ;
#53918=CARTESIAN_POINT ( 'NONE',  ( 10.07627163191000008, -18.75000000310999937, 7.601397897754999633 ) ) ;
#53920=ADVANCED_FACE ( 'NONE', ( #32500 ), #20858, .F. ) ;
#53922=CARTESIAN_POINT ( 'NONE',  ( -2.062503053667999797, -20.24263462181000151, -12.92177931909999877 ) ) ;
#53926=CARTESIAN_POINT ( 'NONE',  ( 2.863963203921999767, -1.059821851618000021, 2.815564610575000071 ) ) ;
#53927=CARTESIAN_POINT ( 'NONE',  ( -1.667961430005999945, -57.05111654290000445, -12.58335110165999993 ) ) ;
#53929=ORIENTED_EDGE ( 'NONE', *, *, #30091, .T. ) ;
#53932=ORIENTED_EDGE ( 'NONE', *, *, #25893, .F. ) ;
#53933=VERTEX_POINT ( 'NONE', #30104 ) ;
#53936=DIRECTION ( 'NONE',  ( -0.7071067811865475727, 0.000000000000000000, 0.7071067811865475727 ) ) ;
#53938=( GEOMETRIC_REPRESENTATION_CONTEXT ( 3 ) GLOBAL_UNCERTAINTY_ASSIGNED_CONTEXT ( ( #24836 ) ) GLOBAL_UNIT_ASSIGNED_CONTEXT ( ( #24962, #56267, #23291 ) ) REPRESENTATION_CONTEXT ( 'NONE', 'WORKASPACE' ) );
#53940=ORIENTED_EDGE ( 'NONE', *, *, #11253, .T. ) ;
#53942=CARTESIAN_POINT ( 'NONE',  ( -1.218029035538723992, -2.695274461392550780, -3.012586580984925710 ) ) ;
#53946=ORIENTED_EDGE ( 'NONE', *, *, #43394, .F. ) ;
#53951=DIRECTION ( 'NONE',  ( 0.000000000000000000, 0.000000000000000000, -1.000000000000000000 ) ) ;
#53952=CARTESIAN_POINT ( 'NONE',  ( 0.1610657711504699108, -18.25053022707183459, 10.99997582743960400 ) ) ;
#53953=EDGE_CURVE ( 'NONE', #54307, #33230, #43013, .T. ) ;
#53955=CARTESIAN_POINT ( 'NONE',  ( 11.06835501100703034, -76.52189007101335960, -4.078077733570841801 ) ) ;
#53956=CARTESIAN_POINT ( 'NONE',  ( 7.655555357447999754, -59.57795407677000554, -10.38646360829999971 ) ) ;
#53958=CARTESIAN_POINT ( 'NONE',  ( -8.878335097414000288, -25.06963071744000260, 8.870344075630997693 ) ) ;
#53962=CARTESIAN_POINT ( 'NONE',  ( -12.57433760367000097, -18.28878254117000068, 1.760777649351999985 ) ) ;
#53963=DIRECTION ( 'NONE',  ( 0.000000000000000000, -1.000000000000000000, 0.000000000000000000 ) ) ;
#53964=CARTESIAN_POINT ( 'NONE',  ( 1.801750019963999971, -23.39007426722000105, 12.59656967653999970 ) ) ;
#53967=CARTESIAN_POINT ( 'NONE',  ( -0.4739505115940000346, -1.178547659067000097, 4.095219728108999924 ) ) ;
#53970=CARTESIAN_POINT ( 'NONE',  ( 12.54977961489000116, -61.84832888596000089, 0.03757501521674000422 ) ) ;
#53972=CARTESIAN_POINT ( 'NONE',  ( 12.99510751537000353, -15.69705297113999443, -6.911973076623003642 ) ) ;
#53979=ORIENTED_EDGE ( 'NONE', *, *, #22557, .T. ) ;
#53981=DIRECTION ( 'NONE',  ( 2.273770411328430080E-11, 5.530779797664840897E-21, -1.000000000000000000 ) ) ;
#53984=LINE ( 'NONE', #31819, #32060 ) ;
#53988=CIRCLE ( 'NONE', #3088, 13.94827586206999825 ) ;
#53989=CARTESIAN_POINT ( 'NONE',  ( -3.246742581843999886, -0.7641268662769999942, -2.093162713580000389 ) ) ;
#53991=CARTESIAN_POINT ( 'NONE',  ( 12.79895559715999909, -23.80469146265000191, -2.015913954444999767 ) ) ;
#53992=CARTESIAN_POINT ( 'NONE',  ( -7.634645345446921638, -55.32415927443500436, -10.10912681045557449 ) ) ;
#53993=ORIENTED_EDGE ( 'NONE', *, *, #26299, .T. ) ;
#53994=CARTESIAN_POINT ( 'NONE',  ( -0.6484536763416249849, -53.67597017256773739, -12.70397497887333671 ) ) ;
#53996=DIRECTION ( 'NONE',  ( 0.000000000000000000, 1.000000000000000000, 0.000000000000000000 ) ) ;
#53999=CIRCLE ( 'NONE', #14410, 0.5999999999999999778 ) ;
#54000=ORIENTED_EDGE ( 'NONE', *, *, #31610, .F. ) ;
#54001=CARTESIAN_POINT ( 'NONE',  ( 7.958776490642000212, -61.27699850017000216, -9.723157983989999309 ) ) ;
#54002=CARTESIAN_POINT ( 'NONE',  ( -1.636761686205420396, -1.083333333333333703, -2.839805762151339508 ) ) ;
#54003=ORIENTED_EDGE ( 'NONE', *, *, #27261, .F. ) ;
#54007=CARTESIAN_POINT ( 'NONE',  ( -10.13695543446000080, -55.09168900617999753, -7.646071007854999380 ) ) ;
#54014=ORIENTED_EDGE ( 'NONE', *, *, #19352, .F. ) ;
#54017=CARTESIAN_POINT ( 'NONE',  ( 12.45567317068999991, -78.30926792646000933, -3.566394712320999805 ) ) ;
#54019=EDGE_CURVE ( 'NONE', #4032, #24723, #20417, .T. ) ;
#54024=VERTEX_POINT ( 'NONE', #15393 ) ;
#54025=DIRECTION ( 'NONE',  ( -0.7071067811865475727, 0.000000000000000000, 0.7071067811865475727 ) ) ;
#54026=CARTESIAN_POINT ( 'NONE',  ( -7.685416442687999172, -76.62334360383999865, -9.616126112745998711 ) ) ;
#54028=CIRCLE ( 'NONE', #40839, 0.5000000000000006661 ) ;
#54030=CARTESIAN_POINT ( 'NONE',  ( 3.212974253443096728, -3.132653343500664711, 1.435077393723246386 ) ) ;
#54031=CARTESIAN_POINT ( 'NONE',  ( 12.49168433579000137, -23.29849137228000444, 1.667916687244999974 ) ) ;
#54032=EDGE_CURVE ( 'NONE', #3236, #17043, #2405, .T. ) ;
#54034=FACE_OUTER_BOUND ( 'NONE', #47279, .T. ) ;
#54037=CARTESIAN_POINT ( 'NONE',  ( 1.083270717429015040, -76.91794464775904316, 12.16356161538060832 ) ) ;
#54039=ADVANCED_FACE ( 'NONE', ( #15681 ), #51424, .F. ) ;
#54042=ORIENTED_EDGE ( 'NONE', *, *, #19264, .F. ) ;
#54045=LINE ( 'NONE', #13582, #42744 ) ;
#54046=DIRECTION ( 'NONE',  ( 0.000000000000000000, 1.000000000000000000, 0.000000000000000000 ) ) ;
#54047=CARTESIAN_POINT ( 'NONE',  ( -10.07627163191000008, -60.04999999657000131, 7.601397897754999633 ) ) ;
#54048=VECTOR ( 'NONE', #38439, 1000.000000000000000 ) ;
#54051=CARTESIAN_POINT ( 'NONE',  ( -0.4450739772406999695, -53.92186785164999918, -12.43586747591000119 ) ) ;
#54052=CARTESIAN_POINT ( 'NONE',  ( 3.350051352536504545, -76.05149132198432937, 11.26355013934140104 ) ) ;
#54057=CARTESIAN_POINT ( 'NONE',  ( 8.838834764832000701, -60.04999999966999980, 8.838834764832000701 ) ) ;
#54059=CARTESIAN_POINT ( 'NONE',  ( -13.89248035986000041, -46.40840747658999277, -2.632528379792999703E-05 ) ) ;
#54064=DIRECTION ( 'NONE',  ( -0.7071067811865475727, 0.000000000000000000, 0.7071067811865475727 ) ) ;
#54066=ORIENTED_EDGE ( 'NONE', *, *, #33501, .F. ) ;
#54071=CARTESIAN_POINT ( 'NONE',  ( 11.74960618672723101, -76.44458049160198243, -0.7033066962385277066 ) ) ;
#54073=CARTESIAN_POINT ( 'NONE',  ( 8.190859204290999784, -55.64999999967000122, 7.342331066867000544 ) ) ;
#54076=CARTESIAN_POINT ( 'NONE',  ( -12.50686284812396742, -54.49510763085821452, -1.423064270604161630 ) ) ;
#54078=AXIS2_PLACEMENT_3D ( 'NONE', #37690, #23815, #32657 ) ;
#54079=CARTESIAN_POINT ( 'NONE',  ( -12.66235429707000115, -25.13741783422999987, 0.4955846680317000374 ) ) ;
#54081=VERTEX_POINT ( 'NONE', #47589 ) ;
#54082=CARTESIAN_POINT ( 'NONE',  ( 0.000000000000000000, -0.5000000000000000000, 0.000000000000000000 ) ) ;
#54083=ORIENTED_EDGE ( 'NONE', *, *, #52773, .F. ) ;
#54084=CARTESIAN_POINT ( 'NONE',  ( -7.766269599678000013, -78.62242792576000738, -9.491266709826000181 ) ) ;
#54086=CARTESIAN_POINT ( 'NONE',  ( 7.761030428335000231, -24.08151201375000028, 9.835168816226000033 ) ) ;
#54088=AXIS2_PLACEMENT_3D ( 'NONE', #39807, #34503, #38946 ) ;
#54089=CARTESIAN_POINT ( 'NONE',  ( -12.50000000000000000, -13.07071424677999971, 0.000000000000000000 ) ) ;
#54091=EDGE_CURVE ( 'NONE', #5785, #33530, #20692, .T. ) ;
#54094=CARTESIAN_POINT ( 'NONE',  ( 3.176273880393910787, -1.831745995345729128, -0.8078237210779479760 ) ) ;
#54100=CARTESIAN_POINT ( 'NONE',  ( 6.665976575492000400, -76.17302026400000159, -11.30427740477999876 ) ) ;
#54109=EDGE_LOOP ( 'NONE', ( #47651, #55986, #57251, #16345 ) ) ;
#54114=CARTESIAN_POINT ( 'NONE',  ( -12.70556836326691474, -62.02772277412548618, 0.2597962962374435469 ) ) ;
#54115=DIRECTION ( 'NONE',  ( -1.000000000000000000, 0.000000000000000000, 0.000000000000000000 ) ) ;
#54116=LINE ( 'NONE', #8950, #21364 ) ;
#54121=CARTESIAN_POINT ( 'NONE',  ( 1.636761686205415067, -1.833333333333333481, 2.839805762151342616 ) ) ;
#54124=CARTESIAN_POINT ( 'NONE',  ( 2.065394024360999836, -55.37838567321000482, 12.82193048525000023 ) ) ;
#54126=CARTESIAN_POINT ( 'NONE',  ( 3.651330038711999570, -2.087546241516999856, 1.548846843139000118 ) ) ;
#54130=CARTESIAN_POINT ( 'NONE',  ( 10.20000000000000107, -0.2000000000000000111, 0.000000000000000000 ) ) ;
#54133=CARTESIAN_POINT ( 'NONE',  ( -2.062323307449999810, -60.02713153159000115, 12.83634826445999977 ) ) ;
#54134=CARTESIAN_POINT ( 'NONE',  ( 12.66737112516999986, -17.76697834132999887, 1.690666607834999891 ) ) ;
#54137=CARTESIAN_POINT ( 'NONE',  ( 9.830798712606000578, -54.70910918491000530, -7.765013391389000041 ) ) ;
#54141=CARTESIAN_POINT ( 'NONE',  ( 0.8804656547168402403, -61.82803394679353204, 12.70299681155804983 ) ) ;
#54143=CARTESIAN_POINT ( 'NONE',  ( -12.66001556635999847, -61.43260856911000189, 1.381621105853999998 ) ) ;
#54152=CIRCLE ( 'NONE', #15506, 1.250000000000000444 ) ;
#54153=CARTESIAN_POINT ( 'NONE',  ( -1.980584515752000119, -55.53514853344000102, -12.76303204600000107 ) ) ;
#54154=VERTEX_POINT ( 'NONE', #47868 ) ;
#54155=ORIENTED_EDGE ( 'NONE', *, *, #39325, .T. ) ;
#54157=ORIENTED_EDGE ( 'NONE', *, *, #54826, .T. ) ;
#54159=EDGE_LOOP ( 'NONE', ( #48702, #2680, #32790, #40645, #54422 ) ) ;
#54163=CARTESIAN_POINT ( 'NONE',  ( 0.005928781627658000382, -25.20113050262999721, -12.66336824419000173 ) ) ;
#54165=AXIS2_PLACEMENT_3D ( 'NONE', #6140, #29149, #24147 ) ;
#54169=CARTESIAN_POINT ( 'NONE',  ( 11.47679389412999917, -78.51599167770000065, 3.196029325000000032 ) ) ;
#54171=EDGE_LOOP ( 'NONE', ( #53917, #234, #54083, #5191, #35126 ) ) ;
#54172=EDGE_CURVE ( 'NONE', #8616, #45142, #35394, .T. ) ;
#54173=EDGE_LOOP ( 'NONE', ( #11553, #29995, #8333, #10717 ) ) ;
#54174=LINE ( 'NONE', #40879, #30114 ) ;
#54181=CARTESIAN_POINT ( 'NONE',  ( 11.63291926114999875, -77.11568903011000486, 5.337072863433999892 ) ) ;
#54182=CARTESIAN_POINT ( 'NONE',  ( -10.29607860738999925, -77.19512210326000456, 7.334573225905999472 ) ) ;
#54184=EDGE_CURVE ( 'NONE', #4989, #27639, #24660, .T. ) ;
#54189=CARTESIAN_POINT ( 'NONE',  ( -5.747123378374999980, -78.21567021303999923, 10.24856442990000005 ) ) ;
#54195=ORIENTED_EDGE ( 'NONE', *, *, #12093, .T. ) ;
#54196=FACE_OUTER_BOUND ( 'NONE', #26603, .T. ) ;
#54198=AXIS2_PLACEMENT_3D ( 'NONE', #49560, #53981, #26798 ) ;
#54200=AXIS2_PLACEMENT_3D ( 'NONE', #36385, #45558, #46149 ) ;
#54203=CARTESIAN_POINT ( 'NONE',  ( -12.97861384075000046, -78.02312312080999845, -0.9459496016724999734 ) ) ;
#54205=CARTESIAN_POINT ( 'NONE',  ( 10.09635500655283735, -18.47627834136018166, 7.644087038114626864 ) ) ;
#54206=ORIENTED_EDGE ( 'NONE', *, *, #13019, .F. ) ;
#54207=CIRCLE ( 'NONE', #50423, 0.5000000000000004441 ) ;
#54208=CARTESIAN_POINT ( 'NONE',  ( -8.130811096542000627, -24.68523690389000080, -9.546858433121998999 ) ) ;
#54209=CARTESIAN_POINT ( 'NONE',  ( 11.75000000000000000, -77.54999999999999716, 2.316376715183999699E-14 ) ) ;
#54211=DIRECTION ( 'NONE',  ( 1.000000000000000000, 0.000000000000000000, 0.000000000000000000 ) ) ;
#54214=CARTESIAN_POINT ( 'NONE',  ( -1.180494763713999973, -0.6498550533857000433, 3.461421590595000097 ) ) ;
#54220=CARTESIAN_POINT ( 'NONE',  ( -10.98362417419999915, -23.15000000000000213, -0.5999999999999999778 ) ) ;
#54222=VERTEX_POINT ( 'NONE', #21833 ) ;
#54224=CARTESIAN_POINT ( 'NONE',  ( -1.624989163556999141E-14, -74.59999999999999432, -11.00000000000000000 ) ) ;
#54226=ORIENTED_EDGE ( 'NONE', *, *, #45602, .T. ) ;
#54229=B_SPLINE_SURFACE_WITH_KNOTS ( 'NONE', 3, 3, ( 
 ( #33369, #15661, #10959, #28940 ),
 ( #2955, #52830, #44551, #8531 ),
 ( #48698, #25667, #48134, #57257 ),
 ( #12386, #43694, #30375, #22105 ),
 ( #26524, #40115, #3814, #4104 ),
 ( #3249, #17390, #58128, #16823 ),
 ( #17690, #48415, #35681, #3528 ),
 ( #29792, #47848, #34806, #7951 ) ),
 .UNSPECIFIED., .F., .F., .F.,
 ( 4, 1, 1, 1, 1, 4 ),
 ( 4, 4 ),
 ( -0.01200407345747999885, 0.000000000000000000, 0.3333333333333000081, 0.6666666666667000474, 1.000000000000000000, 1.011997855551999947 ),
 ( -0.3559705542741999906, 1.355970554273999928 ),
 .UNSPECIFIED. ) ;
#54231=CARTESIAN_POINT ( 'NONE',  ( -7.919595949288999570, -55.65000000893999754, -9.050966798898000931 ) ) ;
#54232=LINE ( 'NONE', #13769, #52151 ) ;
#54240=CIRCLE ( 'NONE', #41970, 3.600000000000000089 ) ;
#54242=CARTESIAN_POINT ( 'NONE',  ( 12.00000000000000000, -18.75000000000000000, 0.000000000000000000 ) ) ;
#54243=TOROIDAL_SURFACE ( 'NONE', #36318, 13.50000000000000000, 0.5000000000000000000 ) ;
#54244=CARTESIAN_POINT ( 'NONE',  ( -7.691916945430000041, -20.24634220924000161, -10.42274798266999980 ) ) ;
#54245=CARTESIAN_POINT ( 'NONE',  ( -8.441176281571586060, -24.91652561798867183, 9.243148034848644556 ) ) ;
#54246=CARTESIAN_POINT ( 'NONE',  ( 11.61175053437844795, -76.53594503550665706, -2.075198828568620701 ) ) ;
#54248=EDGE_CURVE ( 'NONE', #24315, #8754, #35700, .T. ) ;
#54255=CARTESIAN_POINT ( 'NONE',  ( -4.699224227394298126, -78.35979949309869141, 11.12336296093753596 ) ) ;
#54258=CARTESIAN_POINT ( 'NONE',  ( 12.51072239526000196, -52.49705297114005020, -0.7871079366006996647 ) ) ;
#54259=CARTESIAN_POINT ( 'NONE',  ( -1.814305421036000121, -24.28941969330999839, 12.78003582253000125 ) ) ;
#54262=CARTESIAN_POINT ( 'NONE',  ( 2.588085340131999867, -1.699711001040999925, 2.991890042761000235 ) ) ;
#54264=CARTESIAN_POINT ( 'NONE',  ( 12.76303204294999993, -23.26485150694999859, -1.980584515756000030 ) ) ;
#54272=EDGE_CURVE ( 'NONE', #19448, #46033, #30222, .T. ) ;
#54273=DIRECTION ( 'NONE',  ( -1.000000000000000000, 0.000000000000000000, 0.000000000000000000 ) ) ;
#54276=EDGE_LOOP ( 'NONE', ( #29594, #47358, #5861, #23144 ) ) ;
#54282=CARTESIAN_POINT ( 'NONE',  ( -1.750000000000000000, -23.24999999758999536, -12.50000000000000000 ) ) ;
#54284=CARTESIAN_POINT ( 'NONE',  ( 10.03846658012972703, -23.79367507167476248, -7.678639819101482189 ) ) ;
#54286=CARTESIAN_POINT ( 'NONE',  ( 12.19230762942000013, -77.48434608859999173, -3.339585897562999950 ) ) ;
#54288=CARTESIAN_POINT ( 'NONE',  ( -9.298485322486630622, -61.68812323674685416, 8.385852789354533598 ) ) ;
#54290=ORIENTED_EDGE ( 'NONE', *, *, #6837, .T. ) ;
#54291=EDGE_CURVE ( 'NONE', #15053, #53225, #46473, .T. ) ;
#54294=CARTESIAN_POINT ( 'NONE',  ( 7.601397897754999633, -60.04999999725999515, -10.07627163191000008 ) ) ;
#54295=ADVANCED_FACE ( 'NONE', ( #27134 ), #46350, .F. ) ;
#54296=CARTESIAN_POINT ( 'NONE',  ( -12.71798280852999952, -55.50221404479999876, -1.931086388455000025 ) ) ;
#54297=B_SPLINE_CURVE_WITH_KNOTS ( 'NONE', 3,
 ( #1874, #33427, #24872, #47334, #6863, #15433, #56462, #51754 ),
 .UNSPECIFIED., .F., .F.,
 ( 4, 2, 2, 4 ),
 ( 0.000000000000000000, 0.5000000000000046629, 0.7500000000000023315, 1.000000000000000000 ),
 .UNSPECIFIED. ) ;
#54299=ORIENTED_EDGE ( 'NONE', *, *, #2316, .F. ) ;
#54301=CARTESIAN_POINT ( 'NONE',  ( 10.25201842922365536, -60.92180395180004382, -7.730408553586130438 ) ) ;
#54302=ORIENTED_EDGE ( 'NONE', *, *, #45602, .F. ) ;
#54303=EDGE_LOOP ( 'NONE', ( #33883, #47065, #46916, #28136, #27624, #19089 ) ) ;
#54304=CARTESIAN_POINT ( 'NONE',  ( -7.660431561264000599, -55.60820826791000115, -10.01749754193999919 ) ) ;
#54307=VERTEX_POINT ( 'NONE', #9440 ) ;
#54314=CARTESIAN_POINT ( 'NONE',  ( -10.55245342185999924, -77.53220295299000497, 7.517205849611000801 ) ) ;
#54319=CARTESIAN_POINT ( 'NONE',  ( 10.41172548051542535, -18.47988211125808178, 7.610718780881719603 ) ) ;
#54321=DIRECTION ( 'NONE',  ( 1.000000000000000000, 0.000000000000000000, 0.000000000000000000 ) ) ;
#54322=CARTESIAN_POINT ( 'NONE',  ( 11.65396969189999865, -75.78284329787000217, -2.860942225950000140 ) ) ;
#54326=CARTESIAN_POINT ( 'NONE',  ( 0.3501405267838854085, -3.482218366769342932, -3.504278122193990708 ) ) ;
#54328=CARTESIAN_POINT ( 'NONE',  ( 10.82405698390000026, -79.30627921100000322, 5.765268246940999930 ) ) ;
#54331=AXIS2_PLACEMENT_3D ( 'NONE', #31962, #31667, #49714 ) ;
#54333=CARTESIAN_POINT ( 'NONE',  ( 10.35453599130000057, -76.75783510652000530, -6.064947188958000446 ) ) ;
#54336=ORIENTED_EDGE ( 'NONE', *, *, #39527, .T. ) ;
#54338=DIRECTION ( 'NONE',  ( -1.000000000000000000, 0.000000000000000000, 0.000000000000000000 ) ) ;
#54339=CARTESIAN_POINT ( 'NONE',  ( 9.073558136264555429, -25.22808769493118319, 8.894842552359547128 ) ) ;
#54346=CARTESIAN_POINT ( 'NONE',  ( 4.497237866730260158, -76.04321279041880643, 10.85494175940528372 ) ) ;
#54350=CARTESIAN_POINT ( 'NONE',  ( 11.88049207238000093, -76.27891845887410227, -3.223263369271999856 ) ) ;
#54354=LINE ( 'NONE', #36909, #29809 ) ;
#54356=DIRECTION ( 'NONE',  ( 0.000000000000000000, -1.000000000000000000, 0.000000000000000000 ) ) ;
#54358=EDGE_LOOP ( 'NONE', ( #12817, #49736, #24959, #4103, #46554, #18142 ) ) ;
#54360=CARTESIAN_POINT ( 'NONE',  ( 12.70556836343000029, -53.57227722738999631, -1.774194422348999890E-09 ) ) ;
#54363=B_SPLINE_CURVE_WITH_KNOTS ( 'NONE', 3,
 ( #14040, #5193, #27612, #40624, #40325, #22310, #45652, #18197, #8739, #54208 ),
 .UNSPECIFIED., .F., .F.,
 ( 4, 2, 2, 2, 4 ),
 ( 0.000000000000000000, 0.2500000000000000000, 0.5000000000000000000, 0.7500000000000000000, 1.000000000000000000 ),
 .UNSPECIFIED. ) ;
#54365=CARTESIAN_POINT ( 'NONE',  ( 11.68671316441037789, -76.43942763544110619, -1.473703813607833091 ) ) ;
#54369=AXIS2_PLACEMENT_3D ( 'NONE', #58262, #30511, #3376 ) ;
#54374=EDGE_CURVE ( 'NONE', #54392, #14174, #7619, .T. ) ;
#54375=CARTESIAN_POINT ( 'NONE',  ( -12.54902678210999944, -25.00971938212000012, 0.4616712539286000339 ) ) ;
#54376=VERTEX_POINT ( 'NONE', #44216 ) ;
#54384=CARTESIAN_POINT ( 'NONE',  ( 8.284635637485001425, -25.04861451557999885, 9.778492910169999774 ) ) ;
#54385=CARTESIAN_POINT ( 'NONE',  ( 9.205846894779998735, -61.80798911315000055, 8.541134278117000989 ) ) ;
#54391=CARTESIAN_POINT ( 'NONE',  ( -10.27340958483875077, -24.06161210422248331, 7.712164009431025313 ) ) ;
#54392=VERTEX_POINT ( 'NONE', #57208 ) ;
#54397=CARTESIAN_POINT ( 'NONE',  ( -10.04473064004999827, -75.94998313630999576, 8.446198957084000369 ) ) ;
#54402=CARTESIAN_POINT ( 'NONE',  ( -10.15323304112999914, -24.23079616014999971, -7.760925857005999795 ) ) ;
#54403=CARTESIAN_POINT ( 'NONE',  ( 12.71798280857999863, -60.09778595451999905, -1.931086388455000025 ) ) ;
#54410=CARTESIAN_POINT ( 'NONE',  ( -1.250000000000000000, -23.25000000000000000, -12.50000000000000000 ) ) ;
#54414=DIRECTION ( 'NONE',  ( 0.7071067811865475727, 0.000000000000000000, 0.7071067811865475727 ) ) ;
#54421=AXIS2_PLACEMENT_3D ( 'NONE', #30333, #58086, #35635 ) ;
#54422=ORIENTED_EDGE ( 'NONE', *, *, #28885, .F. ) ;
#54425=TOROIDAL_SURFACE ( 'NONE', #14781, 1.250000000000000000, 0.5000000000000000000 ) ;
#54426=CARTESIAN_POINT ( 'NONE',  ( -10.12290050253000118, -23.24999997822999731, 7.648026768374000639 ) ) ;
#54429=LINE ( 'NONE', #39949, #13037 ) ;
#54432=CARTESIAN_POINT ( 'NONE',  ( 12.43356773666999970, -17.28739071017999862, 0.8411682846947000636 ) ) ;
#54434=DIRECTION ( 'NONE',  ( 0.000000000000000000, 1.000000000000000000, 0.000000000000000000 ) ) ;
#54436=B_SPLINE_CURVE_WITH_KNOTS ( 'NONE', 3,
 ( #10002, #1157, #41285, #868, #19145, #18854, #298, #54860, #31525, #18571, #10287, #5271, #14695, #9702, #13829, #36268, #53994, #23279, #9120, #40704, #32118, #18277, #27692, #17977, #31827, #5552, #14406, #37140, #35969, #49869 ),
 .UNSPECIFIED., .F., .F.,
 ( 4, 2, 2, 2, 2, 2, 2, 2, 2, 2, 2, 2, 2, 2, 4 ),
 ( 0.000000000000000000, 0.1250000000000045242, 0.1875000000000052458, 0.2500000000000059952, 0.3125000000000067724, 0.3750000000000074940, 0.5000000000000089928, 0.5625000000000097700, 0.6250000000000106581, 0.6875000000000113243, 0.7500000000000119904, 0.8125000000000127676, 0.8437500000000116573, 0.8750000000000105471, 1.000000000000000000 ),
 .UNSPECIFIED. ) ;
#54437=CARTESIAN_POINT ( 'NONE',  ( 9.770419344647999438, -53.74469452534000169, -8.292776877908002220 ) ) ;
#54443=CARTESIAN_POINT ( 'NONE',  ( -12.43356840166999788, -61.51269674456000303, 0.8410229959425999935 ) ) ;
#54449=EDGE_CURVE ( 'NONE', #20659, #37664, #52783, .T. ) ;
#54451=CARTESIAN_POINT ( 'NONE',  ( 7.997114030194825141, -55.11418618782499124, 7.553727747540665227 ) ) ;
#54453=EDGE_LOOP ( 'NONE', ( #42407, #10752, #46202, #4918, #28505, #4341, #3807, #25608, #33851, #27480, #17921, #8104 ) ) ;
#54456=VECTOR ( 'NONE', #45548, 1000.000000000000000 ) ;
#54458=CARTESIAN_POINT ( 'NONE',  ( -2.065550207748000133, -18.57434920668999823, 12.82162303854000029 ) ) ;
#54461=CARTESIAN_POINT ( 'NONE',  ( 0.5154756746315999338, -25.13240599763000205, -12.66205448072999928 ) ) ;
#54464=CARTESIAN_POINT ( 'NONE',  ( -11.06142172674999991, -78.77465814038001213, -4.424517025895999822 ) ) ;
#54467=CARTESIAN_POINT ( 'NONE',  ( 12.50000000000000000, -39.49523982883999906, 0.000000000000000000 ) ) ;
#54470=ADVANCED_FACE ( 'NONE', ( #8779 ), #17637, .F. ) ;
#54476=CARTESIAN_POINT ( 'NONE',  ( -1.258617752331000039, -77.53579772561000993, -12.89490358089000033 ) ) ;
#54478=CARTESIAN_POINT ( 'NONE',  ( -12.60413652831999975, -23.30716934606000024, -1.799502287743000029 ) ) ;
#54479=FACE_OUTER_BOUND ( 'NONE', #1528, .T. ) ;
#54483=CARTESIAN_POINT ( 'NONE',  ( -11.61175053437844262, -78.28594503550665706, 2.075198828568656673 ) ) ;
#54488=CARTESIAN_POINT ( 'NONE',  ( -3.448863046786000197, -1.852077464339999979, -1.608907009436000068 ) ) ;
#54491=CARTESIAN_POINT ( 'NONE',  ( -0.5245219981451909597, -23.45160423345543421, 10.98753021428638554 ) ) ;
#54492=CARTESIAN_POINT ( 'NONE',  ( 8.178338515874511216, -60.10416868444934835, -7.356278612544663531 ) ) ;
#54495=CARTESIAN_POINT ( 'NONE',  ( 2.062597299672999540, -56.01514526721999943, 12.87022657272000004 ) ) ;
#54496=CARTESIAN_POINT ( 'NONE',  ( 5.579996517577999526, -77.32240076259999739, 11.75597208960999929 ) ) ;
#54498=CARTESIAN_POINT ( 'NONE',  ( -9.841120606655673342, -61.63627250027259663, -8.121699444612119123 ) ) ;
#54499=CARTESIAN_POINT ( 'NONE',  ( 0.7942261439060999129, -76.36432412444001727, 12.48713564821000155 ) ) ;
#54501=EDGE_CURVE ( 'NONE', #30023, #44757, #53435, .T. ) ;
#54503=AXIS2_PLACEMENT_3D ( 'NONE', #14492, #19227, #953 ) ;
#54504=EDGE_CURVE ( 'NONE', #28795, #10827, #22351, .T. ) ;
#54507=CARTESIAN_POINT ( 'NONE',  ( 7.691916945395000482, -21.75365779208000205, -10.42274798264000069 ) ) ;
#54510=CARTESIAN_POINT ( 'NONE',  ( 2.028166799595999770, -0.9497943542025000241, -3.466423845304999585 ) ) ;
#54511=CARTESIAN_POINT ( 'NONE',  ( -12.56594317823000040, -23.25000001387000026, 1.750000000000000000 ) ) ;
#54512=DIRECTION ( 'NONE',  ( 0.000000000000000000, -1.000000000000000000, 0.000000000000000000 ) ) ;
#54518=ORIENTED_EDGE ( 'NONE', *, *, #7335, .F. ) ;
#54519=DIRECTION ( 'NONE',  ( 0.000000000000000000, 0.000000000000000000, -1.000000000000000000 ) ) ;
#54522=DIRECTION ( 'NONE',  ( 0.000000000000000000, 1.000000000000000000, 0.000000000000000000 ) ) ;
#54523=ORIENTED_EDGE ( 'NONE', *, *, #26958, .T. ) ;
#54525=ORIENTED_EDGE ( 'NONE', *, *, #33780, .F. ) ;
#54527=CARTESIAN_POINT ( 'NONE',  ( -2.805383591734468052, -2.643477393492342120, -1.642515783888874870 ) ) ;
#54529=LINE ( 'NONE', #37080, #28908 ) ;
#54530=B_SPLINE_SURFACE_WITH_KNOTS ( 'NONE', 3, 3, ( 
 ( #4519, #53822, #27517, #31650 ),
 ( #18101, #13358, #22521, #23103 ),
 ( #40530, #36097, #54693, #14236 ),
 ( #32234, #49693, #50276, #9824 ),
 ( #41407, #36966, #14528, #11575 ),
 ( #29265, #6257, #19266, #2142 ),
 ( #15997, #11286, #47313, #46737 ),
 ( #33984, #52021, #37844, #29555 ),
 ( #33111, #28982, #47610, #37547 ),
 ( #56154, #1855, #28391, #6553 ),
 ( #6842, #51153, #24271, #7134 ),
 ( #10407, #24853, #42288, #55565 ),
 ( #33697, #20429, #19850, #1558 ),
 ( #42869, #10708, #23971, #41696 ),
 ( #2426, #15415, #38423, #56442 ),
 ( #1273, #38131, #19549, #51737 ),
 ( #37257, #15113, #55864, #55269 ) ),
 .UNSPECIFIED., .F., .F., .F.,
 ( 4, 1, 1, 1, 1, 1, 1, 1, 1, 1, 1, 1, 1, 1, 4 ),
 ( 4, 4 ),
 ( -0.01011398171662000051, 0.000000000000000000, 0.08333333333333001192, 0.1666666666667000196, 0.2500000000000000000, 0.3333333333333000081, 0.4166666666666999919, 0.5000000000000000000, 0.5833333333333000637, 0.6666666666667000474, 0.7500000000000000000, 0.8333333333333000637, 0.9166666666667000474, 1.000000000000000000, 1.010365777941000021 ),
 ( -0.3559705546970999834, 1.357612346730000086 ),
 .UNSPECIFIED. ) ;
#54533=VERTEX_POINT ( 'NONE', #44499 ) ;
#54536=VECTOR ( 'NONE', #29706, 1000.000000000000000 ) ;
#54538=CARTESIAN_POINT ( 'NONE',  ( 0.5999999999999999778, -23.15000000000000213, 10.98362417419999915 ) ) ;
#54539=DIRECTION ( 'NONE',  ( 0.000000000000000000, 0.000000000000000000, -1.000000000000000000 ) ) ;
#54540=CARTESIAN_POINT ( 'NONE',  ( 7.640030139739999449, -55.49283065365000311, -10.18491068058999893 ) ) ;
#54542=CARTESIAN_POINT ( 'NONE',  ( 1.980584515756000030, -18.73514849905999924, -12.76303204340999997 ) ) ;
#54543=CARTESIAN_POINT ( 'NONE',  ( 0.000000000000000000, -39.49523982883999906, 0.000000000000000000 ) ) ;
#54544=CARTESIAN_POINT ( 'NONE',  ( 0.000000000000000000, 0.000000000000000000, 0.000000000000000000 ) ) ;
#54545=CARTESIAN_POINT ( 'NONE',  ( -9.683190293175545804, -78.00399549952769007, -7.215732957028438754 ) ) ;
#54548=CARTESIAN_POINT ( 'NONE',  ( -12.61117324689999997, -18.78448536116999890, 1.798979683802999885 ) ) ;
#54549=CIRCLE ( 'NONE', #42291, 14.00000000000000000 ) ;
#54550=DIRECTION ( 'NONE',  ( -0.7071067811864980568, -0.7071067811865969777, 1.752039988203994887E-09 ) ) ;
#54551=CARTESIAN_POINT ( 'NONE',  ( -1.200170490671999879, -24.43405701997999913, 12.43444080551000042 ) ) ;
#54554=CARTESIAN_POINT ( 'NONE',  ( -3.412382586387999961, -1.979717402877999799, -0.5131178166667998974 ) ) ;
#54556=DIRECTION ( 'NONE',  ( 0.000000000000000000, 0.000000000000000000, 1.000000000000000000 ) ) ;
#54557=CARTESIAN_POINT ( 'NONE',  ( 12.70255466319078685, -24.74616562078519522, -1.306323829448696516 ) ) ;
#54558=CARTESIAN_POINT ( 'NONE',  ( -1.758095523367999791, -23.72291663880000101, -12.57362173515999970 ) ) ;
#54560=CARTESIAN_POINT ( 'NONE',  ( 7.686918321215999939, -57.04439829094999936, -10.48771805383000100 ) ) ;
#54561=CARTESIAN_POINT ( 'NONE',  ( -2.744117082525000306, -2.991506412944000104, 2.149193971933000213 ) ) ;
#54565=FACE_OUTER_BOUND ( 'NONE', #598, .T. ) ;
#54566=LINE ( 'NONE', #36831, #1530 ) ;
#54569=EDGE_LOOP ( 'NONE', ( #31447, #52126, #34034 ) ) ;
#54572=ADVANCED_FACE ( 'NONE', ( #39137 ), #52724, .F. ) ;
#54573=CARTESIAN_POINT ( 'NONE',  ( 1.028703311283999754E-14, 0.000000000000000000, 0.000000000000000000 ) ) ;
#54576=CARTESIAN_POINT ( 'NONE',  ( 10.20942848027640792, -76.56032164449479183, -5.979968601052592092 ) ) ;
#54577=DIRECTION ( 'NONE',  ( 0.000000000000000000, -1.000000000000000000, 1.998401444324999992E-14 ) ) ;
#54578=CARTESIAN_POINT ( 'NONE',  ( 0.009013724458761000410, -1.180443126209999916, 4.026554455433999813 ) ) ;
#54586=CARTESIAN_POINT ( 'NONE',  ( -12.80900240956999880, -57.04634220890999785, -1.930989144707000005 ) ) ;
#54587=EDGE_CURVE ( 'NONE', #51909, #17562, #22492, .T. ) ;
#54588=CARTESIAN_POINT ( 'NONE',  ( 10.99999999999999645, -23.74999999999999289, 0.1603812274922369330 ) ) ;
#54590=CARTESIAN_POINT ( 'NONE',  ( -2.062503053667999797, -21.75736537952000305, 12.92177931904999966 ) ) ;
#54593=VERTEX_POINT ( 'NONE', #26137 ) ;
#54594=DIRECTION ( 'NONE',  ( 0.7071067811865475727, 0.000000000000000000, 0.7071067811865475727 ) ) ;
#54595=( NAMED_UNIT ( * ) SI_UNIT ( $, .STERADIAN. ) SOLID_ANGLE_UNIT ( ) );
#54598=CARTESIAN_POINT ( 'NONE',  ( 12.72554264789000023, -55.59839278072999491, 1.930240062458999928 ) ) ;
#54599=CARTESIAN_POINT ( 'NONE',  ( 9.848022987176388909, -24.82869493595770649, -8.114799025119214804 ) ) ;
#54605=CARTESIAN_POINT ( 'NONE',  ( 7.255994938323000021, -78.25376328549999982, -10.73374472359000009 ) ) ;
#54609=VERTEX_POINT ( 'NONE', #44158 ) ;
#54611=CARTESIAN_POINT ( 'NONE',  ( 3.295079792876999925, -76.37076945043999388, 11.86077433336000020 ) ) ;
#54613=ADVANCED_FACE ( 'NONE', ( #57148 ), #3904, .T. ) ;
#54614=CARTESIAN_POINT ( 'NONE',  ( -3.428559295506383275, -2.331211582835436946, 0.7930039989315531557 ) ) ;
#54616=CARTESIAN_POINT ( 'NONE',  ( 8.194866293469999619, -61.51043252617999713, -9.389192598819999347 ) ) ;
#54617=CARTESIAN_POINT ( 'NONE',  ( 7.914613980750001332, -79.33501992907000044, 9.019916049260999102 ) ) ;
#54618=CARTESIAN_POINT ( 'NONE',  ( -1.750000000001000089, -18.74999999009000007, 12.56594317857000043 ) ) ;
#54619=CARTESIAN_POINT ( 'NONE',  ( 12.70610308058891569, -17.54479009143859969, -1.580620443400405861 ) ) ;
#54620=ADVANCED_FACE ( 'NONE', ( #25846 ), #35267, .F. ) ;
#54623=DIRECTION ( 'NONE',  ( -0.7071067811865475727, 0.000000000000000000, -0.7071067811865475727 ) ) ;
#54625=ORIENTED_EDGE ( 'NONE', *, *, #3254, .T. ) ;
#54628=CARTESIAN_POINT ( 'NONE',  ( 9.689272046653734094, -24.97888144173617775, 8.274769670417640555 ) ) ;
#54635=CARTESIAN_POINT ( 'NONE',  ( 2.306676788976210979, -76.05906975059716046, 11.52121794999999871 ) ) ;
#54638=ORIENTED_EDGE ( 'NONE', *, *, #2858, .T. ) ;
#54639=CARTESIAN_POINT ( 'NONE',  ( -1.476182556143999403, -76.43456666368409458, 12.22114576030999800 ) ) ;
#54644=CARTESIAN_POINT ( 'NONE',  ( -12.00000000000000000, -55.54999999966999980, 1.250000000000000000 ) ) ;
#54645=CARTESIAN_POINT ( 'NONE',  ( 10.36221646773000060, -18.77876216379999974, -7.631895822745999425 ) ) ;
#54646=CARTESIAN_POINT ( 'NONE',  ( 9.546815224142999767, -17.31472046677999899, 8.130854305520999858 ) ) ;
#54647=ORIENTED_EDGE ( 'NONE', *, *, #21295, .T. ) ;
#54649=CARTESIAN_POINT ( 'NONE',  ( 12.71107039382469850, -17.74871969254651205, 1.717622521802969704 ) ) ;
#54654=CARTESIAN_POINT ( 'NONE',  ( -1.750000000000000000, -18.75000000000000000, 12.00000000000000000 ) ) ;
#54655=EDGE_CURVE ( 'NONE', #21736, #37515, #4882, .T. ) ;
#54656=FACE_OUTER_BOUND ( 'NONE', #40717, .T. ) ;
#54657=CARTESIAN_POINT ( 'NONE',  ( 0.000000000000000000, -26.10094976978000147, 0.000000000000000000 ) ) ;
#54661=VERTEX_POINT ( 'NONE', #14301 ) ;
#54663=VERTEX_POINT ( 'NONE', #480 ) ;
#54665=CARTESIAN_POINT ( 'NONE',  ( 9.310177428684999867, -25.13531023636999961, 8.596745825432000387 ) ) ;
#54667=ADVANCED_FACE ( 'NONE', ( #5169 ), #18747, .F. ) ;
#54668=CARTESIAN_POINT ( 'NONE',  ( 9.516272955320999927, -61.62538765589000178, 8.227498559456998706 ) ) ;
#54669=CARTESIAN_POINT ( 'NONE',  ( 7.624341764923000753, -18.73514850530999709, 10.42531124853000080 ) ) ;
#54673=ORIENTED_EDGE ( 'NONE', *, *, #23149, .F. ) ;
#54680=CARTESIAN_POINT ( 'NONE',  ( -9.867655926066998262, -76.19057412444000477, 7.916616500084998620 ) ) ;
#54686=CARTESIAN_POINT ( 'NONE',  ( 12.71759155194729374, -60.86493881539610840, 1.809604648260254134 ) ) ;
#54687=CARTESIAN_POINT ( 'NONE',  ( 12.83044027758000105, -55.49360215019999742, -2.062670899361999766 ) ) ;
#54689=EDGE_LOOP ( 'NONE', ( #1389, #9633, #24928, #22320, #26180, #58005, #51131 ) ) ;
#54693=CARTESIAN_POINT ( 'NONE',  ( -10.18114972182000066, -18.60990354280999881, 7.633087078986000584 ) ) ;
#54694=CARTESIAN_POINT ( 'NONE',  ( 8.838834764832000701, -18.75000000000000000, 8.838834764832000701 ) ) ;
#54695=DIRECTION ( 'NONE',  ( 1.000000000000000000, 0.000000000000000000, 0.000000000000000000 ) ) ;
#54696=CARTESIAN_POINT ( 'NONE',  ( -3.461458192032003556, -3.264785587585083970, -0.6488018207460357623 ) ) ;
#54702=VERTEX_POINT ( 'NONE', #50341 ) ;
#54704=CARTESIAN_POINT ( 'NONE',  ( -3.282727429393999863, -1.693833096892000123, 1.053290761329999770 ) ) ;
#54707=DIRECTION ( 'NONE',  ( 0.000000000000000000, 0.000000000000000000, 1.000000000000000000 ) ) ;
#54708=DIRECTION ( 'NONE',  ( 0.000000000000000000, 1.000000000000000000, 0.000000000000000000 ) ) ;
#54710=DIRECTION ( 'NONE',  ( 1.000000000000000000, 0.000000000000000000, 0.000000000000000000 ) ) ;
#54711=VECTOR ( 'NONE', #28061, 1000.000000000000114 ) ;
#54712=CIRCLE ( 'NONE', #9450, 0.5000000000000004441 ) ;
#54714=AXIS2_PLACEMENT_3D ( 'NONE', #11233, #6791, #30360 ) ;
#54716=CARTESIAN_POINT ( 'NONE',  ( 8.790679651930998872, -53.86186536156999694, -8.797972003268000663 ) ) ;
#54729=CARTESIAN_POINT ( 'NONE',  ( -7.648026766733999615, -18.74999999413999774, -10.12290050089000104 ) ) ;
#54730=EDGE_LOOP ( 'NONE', ( #37252, #19815, #32922, #48137, #3461, #39118 ) ) ;
#54732=AXIS2_PLACEMENT_3D ( 'NONE', #5265, #44833, #32113 ) ;
#54735=ORIENTED_EDGE ( 'NONE', *, *, #39358, .F. ) ;
#54736=CARTESIAN_POINT ( 'NONE',  ( -2.015551294784000191, -18.19652295155999866, 12.79857978895000059 ) ) ;
#54738=ADVANCED_FACE ( 'NONE', ( #9307 ), #18461, .F. ) ;
#54741=LINE ( 'NONE', #31997, #25344 ) ;
#54742=CARTESIAN_POINT ( 'NONE',  ( -10.31585246991000027, -78.28606593309000061, -5.959411202814999697 ) ) ;
#54743=ORIENTED_EDGE ( 'NONE', *, *, #29021, .T. ) ;
#54746=CIRCLE ( 'NONE', #31283, 3.249999999999999556 ) ;
#54751=DIRECTION ( 'NONE',  ( 0.000000000000000000, 1.000000000000000000, 0.000000000000000000 ) ) ;
#54753=CARTESIAN_POINT ( 'NONE',  ( -9.650487694675000228, -78.36836734003000515, 7.043610823269999877 ) ) ;
#54759=CARTESIAN_POINT ( 'NONE',  ( 0.7554157024156027411, -76.56982309619165505, 11.72738829954458595 ) ) ;
#54763=CARTESIAN_POINT ( 'NONE',  ( 3.162225869758173324, -2.869653500654393063, 0.7815842452000089091 ) ) ;
#54767=CARTESIAN_POINT ( 'NONE',  ( 12.50240633875000107, -54.11762602111000575, 1.005381409374000112 ) ) ;
#54769=CARTESIAN_POINT ( 'NONE',  ( 3.542727183245000244, -3.037558102910000279, -1.391102635753999950 ) ) ;
#54771=ORIENTED_EDGE ( 'NONE', *, *, #8142, .T. ) ;
#54773=CARTESIAN_POINT ( 'NONE',  ( 7.666647577129663382, -60.55042584425824259, -7.889735440113329723 ) ) ;
#54774=EDGE_CURVE ( 'NONE', #34958, #52197, #31719, .T. ) ;
#54775=CARTESIAN_POINT ( 'NONE',  ( 9.722718241315000398, -23.25000000000000000, 7.954951288349001004 ) ) ;
#54777=CARTESIAN_POINT ( 'NONE',  ( 5.715297388934000189, -78.28681763324999565, 11.69132169264999987 ) ) ;
#54780=CARTESIAN_POINT ( 'NONE',  ( 11.23304052927915642, -78.47249383617504748, 3.444503982574532497 ) ) ;
#54781=EDGE_LOOP ( 'NONE', ( #33346, #38241, #47662, #51779 ) ) ;
#54785=CARTESIAN_POINT ( 'NONE',  ( 7.612971540276999960, -23.32452273707999879, -10.53003236233000095 ) ) ;
#54786=CIRCLE ( 'NONE', #16149, 5.000000000000000000 ) ;
#54789=CARTESIAN_POINT ( 'NONE',  ( -3.858199361241999803, -0.8051001901206000788, -1.117275487237999965 ) ) ;
#54790=CARTESIAN_POINT ( 'NONE',  ( -1.931087888240000217, -55.48415267986000288, -12.71658872082999814 ) ) ;
#54793=ORIENTED_EDGE ( 'NONE', *, *, #12169, .F. ) ;
#54798=ORIENTED_EDGE ( 'NONE', *, *, #5058, .F. ) ;
#54799=ORIENTED_EDGE ( 'NONE', *, *, #36578, .T. ) ;
#54801=DIRECTION ( 'NONE',  ( -1.000000000000000000, 0.000000000000000000, 0.000000000000000000 ) ) ;
#54805=ORIENTED_EDGE ( 'NONE', *, *, #48250, .T. ) ;
#54807=CARTESIAN_POINT ( 'NONE',  ( -2.225834838116822034, -2.665714381188136972, -2.367851236585388541 ) ) ;
#54808=ORIENTED_EDGE ( 'NONE', *, *, #54978, .T. ) ;
#54810=DIRECTION ( 'NONE',  ( 3.788556036780999566E-11, -1.000000000000000000, 0.000000000000000000 ) ) ;
#54811=ORIENTED_EDGE ( 'NONE', *, *, #22017, .T. ) ;
#54812=CARTESIAN_POINT ( 'NONE',  ( -9.546815223803999828, -54.11472046612000497, -8.130854305859001485 ) ) ;
#54814=ORIENTED_EDGE ( 'NONE', *, *, #23876, .T. ) ;
#54818=CARTESIAN_POINT ( 'NONE',  ( 1.247385798810000113, -54.32277743478999810, -12.50301438874000048 ) ) ;
#54821=EDGE_CURVE ( 'NONE', #53612, #35878, #50046, .T. ) ;
#54822=CARTESIAN_POINT ( 'NONE',  ( -5.917523019358107206, -78.71666666666666856, 10.26699006316250795 ) ) ;
#54823=CARTESIAN_POINT ( 'NONE',  ( -7.682344222575999915, -56.03537109808000594, -10.04116292115999975 ) ) ;
#54825=CARTESIAN_POINT ( 'NONE',  ( 4.693089899494290229, -76.54199774624609631, 10.77217413037992699 ) ) ;
#54826=EDGE_CURVE ( 'NONE', #42686, #54392, #1010, .T. ) ;
#54830=CARTESIAN_POINT ( 'NONE',  ( 9.760317337979069308, -78.25305829502794097, 7.105173469063493563 ) ) ;
#54835=CARTESIAN_POINT ( 'NONE',  ( 13.63885489310999510, -59.58578169018998949, 7.254376133916000668 ) ) ;
#54837=CARTESIAN_POINT ( 'NONE',  ( -3.385193567608999476, -1.931486014851000022, 1.699696520826999846 ) ) ;
#54838=CARTESIAN_POINT ( 'NONE',  ( 10.55911395187000146, -59.58461666436000570, 7.642160924878999673 ) ) ;
#54839=CARTESIAN_POINT ( 'NONE',  ( -1.691611010928000036, -24.23082691229999952, -12.66722148969999928 ) ) ;
#54840=DIRECTION ( 'NONE',  ( -0.07798810297990073359, -0.04890180925223042846, 0.9957542211035085300 ) ) ;
#54841=CARTESIAN_POINT ( 'NONE',  ( 2.612650524949999831, -3.236812248861999919, -2.307222756693999788 ) ) ;
#54843=LINE ( 'NONE', #18257, #6219 ) ;
#54850=CARTESIAN_POINT ( 'NONE',  ( -12.76303204522000101, -23.26485147686999966, -1.980584515753000208 ) ) ;
#54855=CARTESIAN_POINT ( 'NONE',  ( -3.575925901623000058, -0.7202288115830999260, -0.05194511807925000085 ) ) ;
#54860=CARTESIAN_POINT ( 'NONE',  ( 1.308715794772571828, -54.05595500774170858, -12.70256747352388338 ) ) ;
#54861=CARTESIAN_POINT ( 'NONE',  ( 7.624341766656999475, -60.06485146221000093, 10.42531125026000005 ) ) ;
#54862=FACE_OUTER_BOUND ( 'NONE', #30417, .T. ) ;
#54864=FACE_OUTER_BOUND ( 'NONE', #18770, .T. ) ;
#54865=DIRECTION ( 'NONE',  ( -0.7071067811865475727, 0.000000000000000000, 0.7071067811865475727 ) ) ;
#54866=ORIENTED_EDGE ( 'NONE', *, *, #4869, .T. ) ;
#54869=DIRECTION ( 'NONE',  ( 1.000000000000000000, 0.000000000000000000, 0.000000000000000000 ) ) ;
#54872=ORIENTED_EDGE ( 'NONE', *, *, #13474, .T. ) ;
#54873=CARTESIAN_POINT ( 'NONE',  ( 12.50240681834000078, -24.68234730741999883, -1.005418943851999813 ) ) ;
#54876=CARTESIAN_POINT ( 'NONE',  ( -7.709154088362966561, -54.87253195859281618, 9.998702477015426027 ) ) ;
#54877=CARTESIAN_POINT ( 'NONE',  ( 9.355938762748150950, -25.17483711029779414, -8.610912454445188047 ) ) ;
#54878=CARTESIAN_POINT ( 'NONE',  ( -12.54980660768000078, -25.04777352165000082, 0.05651102257796999928 ) ) ;
#54879=VERTEX_POINT ( 'NONE', #27296 ) ;
#54881=CARTESIAN_POINT ( 'NONE',  ( 10.21026245503029450, -17.74392421793578833, -7.764236519581510620 ) ) ;
#54882=CARTESIAN_POINT ( 'NONE',  ( -1.722320549991694039, -17.76336311174892657, -12.71171904436490685 ) ) ;
#54884=ADVANCED_FACE ( 'NONE', ( #54479 ), #14014, .T. ) ;
#54888=EDGE_LOOP ( 'NONE', ( #16799, #19087, #25895, #8109 ) ) ;
#54889=FACE_OUTER_BOUND ( 'NONE', #3082, .T. ) ;
#54891=CARTESIAN_POINT ( 'NONE',  ( -1.771468677314999907, -75.86915816935000123, 12.18184739844999953 ) ) ;
#54893=CARTESIAN_POINT ( 'NONE',  ( 1.576369461341504019, -2.510257082558531749, -3.216291020494079334 ) ) ;
#54895=CARTESIAN_POINT ( 'NONE',  ( 3.086017585447000222, -79.19724228728000526, -11.86910201801999953 ) ) ;
#54896=CARTESIAN_POINT ( 'NONE',  ( -13.94827586207000003, -45.69638659094999866, -8.082388077679998639E-06 ) ) ;
#54897=CARTESIAN_POINT ( 'NONE',  ( 12.70556836329126149, -16.77227722666621190, -0.2641978056567622635 ) ) ;
#54898=CARTESIAN_POINT ( 'NONE',  ( 10.09635298639789625, -60.32373519955886820, -7.644087781989472141 ) ) ;
#54899=CARTESIAN_POINT ( 'NONE',  ( 7.954951288349001004, -55.54999999966999980, 9.722718241315000398 ) ) ;
#54902=VERTEX_POINT ( 'NONE', #25747 ) ;
#54905=CARTESIAN_POINT ( 'NONE',  ( 7.864802647417423742, -24.45123893519480163, 10.10444599041134417 ) ) ;
#54906=AXIS2_PLACEMENT_3D ( 'NONE', #51359, #56074, #42783 ) ;
#54907=CARTESIAN_POINT ( 'NONE',  ( -12.00000000000000000, -18.84999999997999964, 0.7999999999999001243 ) ) ;
#54908=CARTESIAN_POINT ( 'NONE',  ( 7.678657038172564064, -23.79377623515379270, 10.03844138475566261 ) ) ;
#54912=CARTESIAN_POINT ( 'NONE',  ( 4.496864984682853894, -76.04321546014720923, 10.85509615260737348 ) ) ;
#54915=ORIENTED_EDGE ( 'NONE', *, *, #53, .F. ) ;
#54916=CARTESIAN_POINT ( 'NONE',  ( 1.750000000000000000, -18.75000000310999937, 12.50000000000000000 ) ) ;
#54917=CONICAL_SURFACE ( 'NONE', #44543, 0.6999999997695030007, 0.7853981633972997312 ) ;
#54920=CARTESIAN_POINT ( 'NONE',  ( 12.00000000000000000, -55.54999999966999980, -1.250000000000000000 ) ) ;
#54922=CARTESIAN_POINT ( 'NONE',  ( 0.000000000000000000, -2.900000000000000355, -12.80000000000000071 ) ) ;
#54923=CARTESIAN_POINT ( 'NONE',  ( 7.969034948596000589, -17.37623147815000024, -9.934750886910000744 ) ) ;
#54924=CARTESIAN_POINT ( 'NONE',  ( -5.869402599192000025, -78.36567021304000491, 10.46661899222999992 ) ) ;
#54931=CARTESIAN_POINT ( 'NONE',  ( 10.35453599130000057, -76.65783510652001098, -6.064947188958000446 ) ) ;
#54932=CONICAL_SURFACE ( 'NONE', #37016, 3.471875000818999801, 0.7853981633972997312 ) ;
#54935=CARTESIAN_POINT ( 'NONE',  ( -8.441163348734360028, -17.08348045813886529, -9.243160721213708797 ) ) ;
#54936=EDGE_CURVE ( 'NONE', #9760, #45077, #25492, .T. ) ;
#54937=DIRECTION ( 'NONE',  ( 0.000000000000000000, -1.000000000000000000, 0.000000000000000000 ) ) ;
#54938=CARTESIAN_POINT ( 'NONE',  ( -1.165746613897999928E-14, -72.79999999999999716, 0.000000000000000000 ) ) ;
#54939=EDGE_CURVE ( 'NONE', #14936, #12183, #39327, .T. ) ;
#54941=CYLINDRICAL_SURFACE ( 'NONE', #52605, 0.6000000000000008660 ) ;
#54942=EDGE_LOOP ( 'NONE', ( #37442, #35906, #42282, #41108 ) ) ;
#54946=VECTOR ( 'NONE', #11573, 1000.000000000000114 ) ;
#54950=CARTESIAN_POINT ( 'NONE',  ( 10.07616267223999884, -61.52631138996999738, 7.986947465035998839 ) ) ;
#54954=CARTESIAN_POINT ( 'NONE',  ( 2.443158415888972090, -1.792198805145689633, -2.251047301635219267 ) ) ;
#54957=ORIENTED_EDGE ( 'NONE', *, *, #15251, .T. ) ;
#54959=EDGE_CURVE ( 'NONE', #33527, #28360, #42902, .T. ) ;
#54962=FACE_OUTER_BOUND ( 'NONE', #39858, .T. ) ;
#54964=CARTESIAN_POINT ( 'NONE',  ( -2.438596655773999977, -76.13481484252000087, 12.41356352284000053 ) ) ;
#54965=CARTESIAN_POINT ( 'NONE',  ( 10.35396498619769190, -76.69116843985601406, -6.064612950829414650 ) ) ;
#54967=CARTESIAN_POINT ( 'NONE',  ( -1.456717367586000012E-14, -79.29999999999999716, 0.000000000000000000 ) ) ;
#54968=AXIS2_PLACEMENT_3D ( 'NONE', #45359, #45065, #41790 ) ;
#54970=CARTESIAN_POINT ( 'NONE',  ( -8.588902834690999910, -25.13240111580999780, -9.317946123639000433 ) ) ;
#54971=CARTESIAN_POINT ( 'NONE',  ( -7.555116226634104315, -60.48684619743404056, 7.995796640818095824 ) ) ;
#54978=EDGE_CURVE ( 'NONE', #17731, #9942, #16852, .T. ) ;
#54980=CARTESIAN_POINT ( 'NONE',  ( -3.250000000000000000, -2.000000000000000000, 0.000000000000000000 ) ) ;
#54981=CARTESIAN_POINT ( 'NONE',  ( -1.704789469357325560, -60.50346161385032673, -12.53199752970037473 ) ) ;
#54982=CARTESIAN_POINT ( 'NONE',  ( 0.000000000000000000, -18.84999999999999787, -11.79999999999999893 ) ) ;
#54983=CARTESIAN_POINT ( 'NONE',  ( -2.641758692652436125, -3.192411922226876531, 2.330954230004774086 ) ) ;
#54992=CARTESIAN_POINT ( 'NONE',  ( -3.122542015344999644, -3.252748962127999910, 2.445576582436999935 ) ) ;
#54995=AXIS2_PLACEMENT_3D ( 'NONE', #8653, #45270, #26068 ) ;
#54996=CARTESIAN_POINT ( 'NONE',  ( 9.108250977391000092, -24.87811334491999915, -8.478720681740998799 ) ) ;
#54997=CARTESIAN_POINT ( 'NONE',  ( -1.513914364619621393E-14, -80.70000000000000284, 13.99999999999935874 ) ) ;
#54999=CARTESIAN_POINT ( 'NONE',  ( -8.620934061362914846, -53.63470696640088420, -9.346030177741987188 ) ) ;
#55001=EDGE_CURVE ( 'NONE', #56632, #36279, #8497, .T. ) ;
#55003=VECTOR ( 'NONE', #56499, 1000.000000000000000 ) ;
#55004=CARTESIAN_POINT ( 'NONE',  ( -9.128070454880999662, -79.05712101268998993, -9.183783075634998738 ) ) ;
#55005=B_SPLINE_SURFACE_WITH_KNOTS ( 'NONE', 3, 3, ( 
 ( #40604, #48593, #35567, #27302 ),
 ( #9021, #8422, #22883, #45335 ),
 ( #58019, #40003, #18176, #35869 ),
 ( #49769, #26139, #22292, #26419 ),
 ( #13133, #8139, #53898, #53593 ),
 ( #44441, #45041, #36169, #53012 ),
 ( #3993, #44160, #27007, #17580 ),
 ( #21995, #3707, #9310, #39716 ) ),
 .UNSPECIFIED., .F., .F., .F.,
 ( 4, 1, 1, 1, 1, 4 ),
 ( 4, 4 ),
 ( -0.01200407347463999970, 0.000000000000000000, 0.3333333333333000081, 0.6666666666667000474, 1.000000000000000000, 1.011997855551999947 ),
 ( -0.3559705542741999906, 1.355970554273999928 ),
 .UNSPECIFIED. ) ;
#55011=DIRECTION ( 'NONE',  ( -0.6489586447330936148, -0.04890182338522946343, -0.7592504784955924624 ) ) ;
#55013=CYLINDRICAL_SURFACE ( 'NONE', #14578, 0.5000000000000004441 ) ;
#55014=EDGE_CURVE ( 'NONE', #30887, #9420, #26896, .T. ) ;
#55015=CIRCLE ( 'NONE', #16377, 1.750000000000001332 ) ;
#55016=ORIENTED_EDGE ( 'NONE', *, *, #29887, .T. ) ;
#55018=VECTOR ( 'NONE', #41067, 1000.000000000000000 ) ;
#55019=CARTESIAN_POINT ( 'NONE',  ( 14.00000000000000000, -45.91785611817000046, 0.000000000000000000 ) ) ;
#55021=DIRECTION ( 'NONE',  ( 0.7071067811865475727, 0.000000000000000000, -0.7071067811865475727 ) ) ;
#55025=ORIENTED_EDGE ( 'NONE', *, *, #13441, .T. ) ;
#55026=ORIENTED_EDGE ( 'NONE', *, *, #22404, .F. ) ;
#55027=CARTESIAN_POINT ( 'NONE',  ( 1.200170490671999879, -17.56594298002000087, 12.43444080551000042 ) ) ;
#55033=DIRECTION ( 'NONE',  ( -0.7071067811865475727, 0.000000000000000000, 0.7071067811865475727 ) ) ;
#55035=ORIENTED_EDGE ( 'NONE', *, *, #21547, .T. ) ;
#55038=CARTESIAN_POINT ( 'NONE',  ( 0.000000000000000000, -46.09579702914000165, 0.000000000000000000 ) ) ;
#55039=CARTESIAN_POINT ( 'NONE',  ( -0.2584144828367441193, -62.02845396889886587, -12.70558781492531431 ) ) ;
#55041=CARTESIAN_POINT ( 'NONE',  ( 0.000000000000000000, -2.949999999935999817, 0.000000000000000000 ) ) ;
#55043=CARTESIAN_POINT ( 'NONE',  ( -3.116139353062999717, -78.31286269907000985, 12.57467468523999976 ) ) ;
#55045=AXIS2_PLACEMENT_3D ( 'NONE', #22086, #35662, #26807 ) ;
#55046=CARTESIAN_POINT ( 'NONE',  ( -12.80900240957999969, -20.24634220924000161, -1.930989144707000005 ) ) ;
#55047=CARTESIAN_POINT ( 'NONE',  ( -8.299831609958628675, -76.63730787009656353, 8.317058589932315726 ) ) ;
#55051=AXIS2_PLACEMENT_3D ( 'NONE', #44417, #22570, #58294 ) ;
#55052=CARTESIAN_POINT ( 'NONE',  ( -10.71846391861806858, -76.73410648036755788, -4.978960265409741126 ) ) ;
#55058=CARTESIAN_POINT ( 'NONE',  ( 3.171758640500000226, -3.636739359372000102, 1.479846994257000059 ) ) ;
#55059=CARTESIAN_POINT ( 'NONE',  ( -5.869402599192000025, -78.46567021303999923, 10.46661899222999992 ) ) ;
#55060=ORIENTED_EDGE ( 'NONE', *, *, #32602, .T. ) ;
#55061=CARTESIAN_POINT ( 'NONE',  ( 8.666912951930401121, -61.79291380851744719, 9.019442092634875507 ) ) ;
#55062=CARTESIAN_POINT ( 'NONE',  ( 0.5392637480172763897, -18.58467666638075855, -10.98678411023717416 ) ) ;
#55063=CARTESIAN_POINT ( 'NONE',  ( -11.74610588145644208, -77.68890476463809591, 1.536422268980871308 ) ) ;
#55064=CARTESIAN_POINT ( 'NONE',  ( 1.799501877793999949, -55.51082276539999327, 12.60552511008000032 ) ) ;
#55065=CARTESIAN_POINT ( 'NONE',  ( -9.692839446179998930, -78.39782691517000046, 7.074522137259999788 ) ) ;
#55067=EDGE_CURVE ( 'NONE', #29230, #31908, #57551, .T. ) ;
#55068=DIRECTION ( 'NONE',  ( 0.000000000000000000, 1.000000000000000000, 0.000000000000000000 ) ) ;
#55073=CARTESIAN_POINT ( 'NONE',  ( -3.264115890327925484, -76.30205353464953077, -11.28874797633254090 ) ) ;
#55075=CARTESIAN_POINT ( 'NONE',  ( -1.480597980168999888E-14, -80.60000000000000853, 0.000000000000000000 ) ) ;
#55078=CARTESIAN_POINT ( 'NONE',  ( -3.370206795150183510, -1.714299274284970309, -0.5568820970875701937 ) ) ;
#55082=DIRECTION ( 'NONE',  ( 9.148990415650000800E-11, 1.000000000000000000, -8.583837524864000176E-10 ) ) ;
#55085=EDGE_LOOP ( 'NONE', ( #44428, #31543, #11836, #50903 ) ) ;
#55088=AXIS2_PLACEMENT_3D ( 'NONE', #42186, #1754, #49886 ) ;
#55089=DIRECTION ( 'NONE',  ( 0.000000000000000000, -1.000000000000000000, 0.000000000000000000 ) ) ;
#55090=CARTESIAN_POINT ( 'NONE',  ( 7.601397897754999633, -23.24999999688999708, 10.07627163191000008 ) ) ;
#55092=CARTESIAN_POINT ( 'NONE',  ( 7.970414252720421366, -61.32292089011284730, 9.713036876910342343 ) ) ;
#55094=ORIENTED_EDGE ( 'NONE', *, *, #5550, .F. ) ;
#55095=EDGE_CURVE ( 'NONE', #9508, #27850, #29484, .T. ) ;
#55101=CARTESIAN_POINT ( 'NONE',  ( -8.441163350029313506, -53.88348045720209001, -9.243160719890433086 ) ) ;
#55102=ORIENTED_EDGE ( 'NONE', *, *, #52693, .F. ) ;
#55107=CARTESIAN_POINT ( 'NONE',  ( -9.042832678091775378, -79.00923211523392808, -8.284631484192345852 ) ) ;
#55109=CARTESIAN_POINT ( 'NONE',  ( -9.019414222042072993, -24.99291943955542550, 8.666941068750990240 ) ) ;
#55111=CARTESIAN_POINT ( 'NONE',  ( -7.627487606591000002, -55.50221404479999876, -10.35845616725999996 ) ) ;
#55113=CARTESIAN_POINT ( 'NONE',  ( 8.713488674121839139, -76.50807972678794044, 7.883309514286040987 ) ) ;
#55118=CARTESIAN_POINT ( 'NONE',  ( 8.196558852201880185, -78.13742199711396097, -8.869913710989646205 ) ) ;
#55120=FACE_OUTER_BOUND ( 'NONE', #18881, .T. ) ;
#55123=CARTESIAN_POINT ( 'NONE',  ( 1.750000000000000000, -55.55000000278000272, 12.50000000000000000 ) ) ;
#55125=CARTESIAN_POINT ( 'NONE',  ( -0.1086647425368000019, -0.9333606339641999927, 3.155427364003000168 ) ) ;
#55126=CONICAL_SURFACE ( 'NONE', #29657, 0.6999999997694995590, 0.7853981633972997312 ) ;
#55128=CARTESIAN_POINT ( 'NONE',  ( 7.651160336708000109, -59.56232686183999903, -10.45205658995999976 ) ) ;
#55129=CARTESIAN_POINT ( 'NONE',  ( -2.229182494176999985, -3.114159330903000011, -2.679543090139000050 ) ) ;
#55130=CARTESIAN_POINT ( 'NONE',  ( 12.66315196848000113, -25.17802884708999756, -0.06065366946593000325 ) ) ;
#55135=CARTESIAN_POINT ( 'NONE',  ( -6.217012876707000757, -76.33752954592999629, -10.33620136625999919 ) ) ;
#55140=LINE ( 'NONE', #9992, #29910 ) ;
#55144=CARTESIAN_POINT ( 'NONE',  ( -4.013075295723000480, -1.312137290291999880, -0.3293376867898999971 ) ) ;
#55149=FACE_OUTER_BOUND ( 'NONE', #50329, .T. ) ;
#55152=ORIENTED_EDGE ( 'NONE', *, *, #8253, .T. ) ;
#55153=EDGE_CURVE ( 'NONE', #470, #49572, #41656, .T. ) ;
#55156=CIRCLE ( 'NONE', #31569, 12.50000000000000000 ) ;
#55157=DIRECTION ( 'NONE',  ( 0.9999999999999694689, -2.469235736007923508E-07, -1.232399279922961038E-12 ) ) ;
#55158=VERTEX_POINT ( 'NONE', #86 ) ;
#55161=AXIS2_PLACEMENT_3D ( 'NONE', #29743, #47222, #20056 ) ;
#55162=CARTESIAN_POINT ( 'NONE',  ( 8.620921568006147950, -61.96528830388066922, -9.346042573999042702 ) ) ;
#55164=EDGE_LOOP ( 'NONE', ( #39266, #15918, #50762, #25188 ) ) ;
#55165=ORIENTED_EDGE ( 'NONE', *, *, #28980, .F. ) ;
#55167=AXIS2_PLACEMENT_3D ( 'NONE', #19207, #28628, #19791 ) ;
#55170=EDGE_CURVE ( 'NONE', #36279, #56632, #35858, .T. ) ;
#55171=ORIENTED_EDGE ( 'NONE', *, *, #47117, .T. ) ;
#55172=CARTESIAN_POINT ( 'NONE',  ( 12.77297374709000088, -54.07184670079000455, 1.476174539902000094 ) ) ;
#55173=CARTESIAN_POINT ( 'NONE',  ( 8.274772993773998664, -24.97888614414509334, -9.689268730326240586 ) ) ;
#55174=ORIENTED_EDGE ( 'NONE', *, *, #28890, .F. ) ;
#55179=FACE_OUTER_BOUND ( 'NONE', #57772, .T. ) ;
#55184=ORIENTED_EDGE ( 'NONE', *, *, #23986, .F. ) ;
#55185=CARTESIAN_POINT ( 'NONE',  ( -9.844172144369998989, -75.96608411793999949, 7.391061701651999272 ) ) ;
#55187=EDGE_CURVE ( 'NONE', #47200, #21690, #20781, .T. ) ;
#55188=CARTESIAN_POINT ( 'NONE',  ( -3.449594485955520984, -2.365315487544573436, -0.7067013086087599039 ) ) ;
#55189=CARTESIAN_POINT ( 'NONE',  ( 12.49168451098999988, -18.70151115557999688, 1.667916687331000070 ) ) ;
#55190=CARTESIAN_POINT ( 'NONE',  ( -7.766269599678000013, -78.55309459242000969, -9.491266709826000181 ) ) ;
#55193=CARTESIAN_POINT ( 'NONE',  ( 1.476721224666196930, -2.763797600519179110, -2.894638992734555938 ) ) ;
#55194=CARTESIAN_POINT ( 'NONE',  ( -2.382985193727138462, -77.94086671676463141, 11.78025155718290229 ) ) ;
#55195=CYLINDRICAL_SURFACE ( 'NONE', #37973, 11.75000000000000000 ) ;
#55199=DIRECTION ( 'NONE',  ( 0.9936845293270585300, -0.1122098755727947705, 0.000000000000000000 ) ) ;
#55200=CARTESIAN_POINT ( 'NONE',  ( 8.611000705966242563, -25.17488119224633536, 9.355851007297125932 ) ) ;
#55201=CARTESIAN_POINT ( 'NONE',  ( -12.50000000000000000, -55.55000000209000177, -1.750000000000000000 ) ) ;
#55202=CARTESIAN_POINT ( 'NONE',  ( 2.383991792491000350, -3.477118084780000284, -2.687767044859000087 ) ) ;
#55205=CARTESIAN_POINT ( 'NONE',  ( -9.750154851953961810, -76.15233773468979450, 6.556588445750800354 ) ) ;
#55208=ORIENTED_EDGE ( 'NONE', *, *, #53195, .T. ) ;
#55209=DIRECTION ( 'NONE',  ( 0.000000000000000000, -1.000000000000000000, 0.000000000000000000 ) ) ;
#55211=CARTESIAN_POINT ( 'NONE',  ( -11.44417895085270942, -76.82083333333335418, -3.075537641221545826 ) ) ;
#55215=CARTESIAN_POINT ( 'NONE',  ( 9.414496040451998837, -16.73736394015000073, -8.652369398714998994 ) ) ;
#55216=DIRECTION ( 'NONE',  ( 2.678937178693000147E-11, -1.000000000000000000, 2.678911359553000079E-11 ) ) ;
#55217=ORIENTED_EDGE ( 'NONE', *, *, #35119, .T. ) ;
#55219=CYLINDRICAL_SURFACE ( 'NONE', #19204, 11.00000000000000000 ) ;
#55222=CARTESIAN_POINT ( 'NONE',  ( 11.72872471648087966, -77.68377190531555243, -2.898477863863423654 ) ) ;
#55223=ADVANCED_FACE ( 'NONE', ( #41074 ), #55681, .F. ) ;
#55224=CARTESIAN_POINT ( 'NONE',  ( 11.75000000000000000, -76.45000000000000284, 0.000000000000000000 ) ) ;
#55227=CARTESIAN_POINT ( 'NONE',  ( -3.804208684430999909, -3.250482064474000232, -0.1186911049137999996 ) ) ;
#55230=B_SPLINE_SURFACE_WITH_KNOTS ( 'NONE', 3, 3, ( 
 ( #19136, #45430, #18562, #1151 ),
 ( #27396, #36841, #863, #5264 ),
 ( #23845, #4971, #18848, #32398 ),
 ( #22980, #36554, #50442, #41862 ),
 ( #48055, #51893, #51611, #38003 ),
 ( #11451, #29430, #6425, #10876 ),
 ( #47189, #11168, #42742, #1728 ),
 ( #56603, #29143, #7008, #15283 ),
 ( #12020, #42454, #29714, #6721 ),
 ( #2592, #43031, #16451, #11736 ),
 ( #24729, #2305, #34432, #52462 ) ),
 .UNSPECIFIED., .F., .F., .F.,
 ( 4, 1, 1, 1, 1, 1, 1, 1, 4 ),
 ( 4, 4 ),
 ( -0.01994574723506000249, 0.000000000000000000, 0.1666666666667000196, 0.3333333333333000081, 0.5000000000000000000, 0.6666666666667000474, 0.8333333333333000637, 1.000000000000000000, 1.020511277925000071 ),
 ( -0.3582002740308999900, 1.358574366093000085 ),
 .UNSPECIFIED. ) ;
#55232=AXIS2_PLACEMENT_3D ( 'NONE', #46887, #6124, #33848 ) ;
#55233=CARTESIAN_POINT ( 'NONE',  ( 8.485281374238999419, -59.94999999967000548, 8.485281374238999419 ) ) ;
#55239=ORIENTED_EDGE ( 'NONE', *, *, #33110, .T. ) ;
#55244=VECTOR ( 'NONE', #27180, 1000.000000000000000 ) ;
#55245=CARTESIAN_POINT ( 'NONE',  ( 7.645391636782999711, -60.01530450324999322, 10.18949673577000148 ) ) ;
#55246=DIRECTION ( 'NONE',  ( 0.000000000000000000, 0.000000000000000000, -1.000000000000000000 ) ) ;
#55249=ORIENTED_EDGE ( 'NONE', *, *, #4266, .F. ) ;
#55251=ORIENTED_EDGE ( 'NONE', *, *, #20760, .F. ) ;
#55253=DIRECTION ( 'NONE',  ( -0.7071067811865474617, 0.000000000000000000, -0.7071067811865474617 ) ) ;
#55255=CARTESIAN_POINT ( 'NONE',  ( -10.09635500655283735, -18.47627834136018166, -7.644087038114626864 ) ) ;
#55256=CARTESIAN_POINT ( 'NONE',  ( 10.35453599130000057, -76.75783510652000530, -6.064947188958000446 ) ) ;
#55261=CARTESIAN_POINT ( 'NONE',  ( -9.029867227896000159, -25.33262194290999858, -9.038867509618000895 ) ) ;
#55262=CARTESIAN_POINT ( 'NONE',  ( 12.49306752631999906, -55.51943307300000185, -1.667917367010000040 ) ) ;
#55269=CARTESIAN_POINT ( 'NONE',  ( -7.660411364622000008, -18.80826384815000196, 10.01752038683000023 ) ) ;
#55270=B_SPLINE_CURVE_WITH_KNOTS ( 'NONE', 3,
 ( #20589, #17021, #7584, #7295, #3729, #53038, #30584, #16449, #25297, #12585 ),
 .UNSPECIFIED., .F., .F.,
 ( 4, 2, 2, 2, 4 ),
 ( 0.000000000000000000, 0.5000000000000012212, 0.6250000000000035527, 0.7500000000000057732, 1.000000000000000000 ),
 .UNSPECIFIED. ) ;
#55271=EDGE_CURVE ( 'NONE', #31290, #47045, #12310, .T. ) ;
#55273=CARTESIAN_POINT ( 'NONE',  ( -0.07478521273582763862, -3.373346085622628276, -3.521909467481564082 ) ) ;
#55282=CARTESIAN_POINT ( 'NONE',  ( -8.090910852015777976, -55.25278097498932084, 7.452378523309688418 ) ) ;
#55287=CARTESIAN_POINT ( 'NONE',  ( -14.00000000000000000, -32.88214388149999934, 1.168298652233000123E-11 ) ) ;
#55289=DIRECTION ( 'NONE',  ( 0.000000000000000000, -1.000000000000000000, 0.000000000000000000 ) ) ;
#55295=CARTESIAN_POINT ( 'NONE',  ( 10.13402152808999901, -55.07694524364999467, -7.647754144006999155 ) ) ;
#55296=CIRCLE ( 'NONE', #10085, 1.250000000000000444 ) ;
#55298=EDGE_CURVE ( 'NONE', #56133, #1101, #49270, .T. ) ;
#55301=CARTESIAN_POINT ( 'NONE',  ( -1.980610890454873374, -60.32073889447752890, 12.74374574610012800 ) ) ;
#55311=ORIENTED_EDGE ( 'NONE', *, *, #35956, .F. ) ;
#55317=EDGE_LOOP ( 'NONE', ( #45343, #2545, #37945, #6419 ) ) ;
#55318=CARTESIAN_POINT ( 'NONE',  ( -1.477284502223000118, -17.27368499703000282, 12.77254812468999923 ) ) ;
#55319=CARTESIAN_POINT ( 'NONE',  ( -9.998734510692901978, -54.87263061026161637, -7.709128441167184320 ) ) ;
#55324=CARTESIAN_POINT ( 'NONE',  ( -9.369164850722000892, -18.75000000000000000, -7.601397897754999633 ) ) ;
#55325=ORIENTED_EDGE ( 'NONE', *, *, #21861, .T. ) ;
#55326=VERTEX_POINT ( 'NONE', #56401 ) ;
#55330=AXIS2_PLACEMENT_3D ( 'NONE', #57391, #21941, #34931 ) ;
#55331=CARTESIAN_POINT ( 'NONE',  ( -0.3664097479087854992, -17.02809982499438135, 12.50575740043635697 ) ) ;
#55334=CARTESIAN_POINT ( 'NONE',  ( -8.190859204290999784, -55.64999999967000122, 7.342331066867000544 ) ) ;
#55336=AXIS2_PLACEMENT_3D ( 'NONE', #7785, #7496, #21925 ) ;
#55342=VECTOR ( 'NONE', #40047, 1000.000000000000114 ) ;
#55348=CARTESIAN_POINT ( 'NONE',  ( -1.250000000000000000, -55.54999999966999980, 12.50000000000000000 ) ) ;
#55352=CARTESIAN_POINT ( 'NONE',  ( 0.000000000000000000, -13.07071424677999971, 0.000000000000000000 ) ) ;
#55353=ADVANCED_FACE ( 'NONE', ( #33657, #42250 ), #6804, .T. ) ;
#55355=CARTESIAN_POINT ( 'NONE',  ( -1.148784730228095574, -3.499999999999998668, -3.235125723717343860 ) ) ;
#55357=CARTESIAN_POINT ( 'NONE',  ( -3.047192285975917070, -77.59416509716808719, 11.37765756762788349 ) ) ;
#55359=CARTESIAN_POINT ( 'NONE',  ( 1.799490220168999954, -59.57129148919000272, 12.64502302236999931 ) ) ;
#55360=CARTESIAN_POINT ( 'NONE',  ( -3.129814719915999799, -78.34232227420999095, 12.62985940900000159 ) ) ;
#55362=DIRECTION ( 'NONE',  ( -1.000000000000000000, 0.000000000000000000, 0.000000000000000000 ) ) ;
#55365=CARTESIAN_POINT ( 'NONE',  ( -4.499009195832593733, -76.29327141761633868, -10.85425454283228319 ) ) ;
#55370=CARTESIAN_POINT ( 'NONE',  ( -3.249661007175000282, -0.8020864414130000064, 2.357191814219000037 ) ) ;
#55374=DIRECTION ( 'NONE',  ( -1.205798306660979359E-11, 1.868137356545963916E-07, 0.9999999999999824585 ) ) ;
#55378=DIRECTION ( 'NONE',  ( 1.000000000000000000, 0.000000000000000000, 0.000000000000000000 ) ) ;
#55380=AXIS2_PLACEMENT_3D ( 'NONE', #1597, #55021, #55606 ) ;
#55381=ORIENTED_EDGE ( 'NONE', *, *, #47049, .T. ) ;
#55384=EDGE_CURVE ( 'NONE', #13401, #52629, #16022, .T. ) ;
#55387=ORIENTED_EDGE ( 'NONE', *, *, #25293, .T. ) ;
#55389=CARTESIAN_POINT ( 'NONE',  ( -12.76303204294000082, -18.73514849292999784, -1.980584515756000030 ) ) ;
#55392=CARTESIAN_POINT ( 'NONE',  ( 0.9406238316005999245, -2.408324159475999870, 3.268731539939000008 ) ) ;
#55393=ORIENTED_EDGE ( 'NONE', *, *, #20325, .F. ) ;
#55398=CARTESIAN_POINT ( 'NONE',  ( -7.766498253946735097, -78.52063990793401160, -9.491546151406783594 ) ) ;
#55399=EDGE_CURVE ( 'NONE', #35908, #27991, #37120, .T. ) ;
#55403=ADVANCED_FACE ( 'NONE', ( #55526 ), #42537, .T. ) ;
#55405=B_SPLINE_CURVE_WITH_KNOTS ( 'NONE', 3,
 ( #45560, #36678, #54981, #44669, #45856, #22220 ),
 .UNSPECIFIED., .F., .F.,
 ( 4, 2, 4 ),
 ( 0.000000000000000000, 0.5000000000000000000, 1.000000000000000000 ),
 .UNSPECIFIED. ) ;
#55406=CARTESIAN_POINT ( 'NONE',  ( -7.668949790007999923, -56.02870851050000311, -10.21381326472999795 ) ) ;
#55411=CARTESIAN_POINT ( 'NONE',  ( -12.65375411750999923, -57.05022861049000227, -1.750000000000000000 ) ) ;
#55415=CARTESIAN_POINT ( 'NONE',  ( -1.980584515752000119, -60.06485146591000301, 12.76303204605000197 ) ) ;
#55416=CARTESIAN_POINT ( 'NONE',  ( -12.79999999996999982, -0.1000000000339999751, 4.310442092940000344E-10 ) ) ;
#55420=FACE_OUTER_BOUND ( 'NONE', #42025, .T. ) ;
#55421=CARTESIAN_POINT ( 'NONE',  ( 12.55433072264032823, -23.38725213725910024, 1.749897784985354532 ) ) ;
#55423=CARTESIAN_POINT ( 'NONE',  ( 12.71466317164898285, -24.13795986741620325, -1.778778223976646755 ) ) ;
#55424=CARTESIAN_POINT ( 'NONE',  ( -1.288488638074000159, -24.53564939367999997, -12.54709296483000003 ) ) ;
#55427=CARTESIAN_POINT ( 'NONE',  ( 12.48409101788000086, -23.36970703835000052, 1.669510252625999946 ) ) ;
#55431=B_SPLINE_CURVE_WITH_KNOTS ( 'NONE', 3,
 ( #28793, #55674, #19371, #24383, #46255, #14634 ),
 .UNSPECIFIED., .F., .F.,
 ( 4, 2, 4 ),
 ( 0.000000000000000000, 0.5000000000000000000, 1.000000000000000000 ),
 .UNSPECIFIED. ) ;
#55433=CARTESIAN_POINT ( 'NONE',  ( -1.086153235740000111, -76.28645333715999755, -12.16362709103000128 ) ) ;
#55434=ORIENTED_EDGE ( 'NONE', *, *, #42254, .T. ) ;
#55436=ADVANCED_FACE ( 'NONE', ( #15376 ), #54229, .F. ) ;
#55442=DIRECTION ( 'NONE',  ( 0.7071067811865475727, 0.000000000000000000, -0.7071067811865475727 ) ) ;
#55445=DIRECTION ( 'NONE',  ( -1.000000000000000000, 0.000000000000000000, 0.000000000000000000 ) ) ;
#55446=CARTESIAN_POINT ( 'NONE',  ( -1.799502287691000069, -55.49283319101999723, 12.60413670417000098 ) ) ;
#55447=ORIENTED_EDGE ( 'NONE', *, *, #6663, .F. ) ;
#55448=DIRECTION ( 'NONE',  ( 0.000000000000000000, -1.000000000000000000, 0.000000000000000000 ) ) ;
#55450=CARTESIAN_POINT ( 'NONE',  ( 14.00000000000000000, -45.91785611817000046, 0.000000000000000000 ) ) ;
#55451=ORIENTED_EDGE ( 'NONE', *, *, #40173, .T. ) ;
#55457=CARTESIAN_POINT ( 'NONE',  ( 12.50000000000000000, -28.92928575306000383, 0.000000000000000000 ) ) ;
#55458=VERTEX_POINT ( 'NONE', #21530 ) ;
#55461=AXIS2_PLACEMENT_3D ( 'NONE', #9680, #4672, #5823 ) ;
#55465=CARTESIAN_POINT ( 'NONE',  ( 12.83836748059999877, -55.59372227128000077, 2.062147040909000140 ) ) ;
#55467=ORIENTED_EDGE ( 'NONE', *, *, #36242, .T. ) ;
#55471=AXIS2_PLACEMENT_3D ( 'NONE', #14220, #398, #18376 ) ;
#55472=EDGE_CURVE ( 'NONE', #42112, #1538, #28017, .T. ) ;
#55474=CARTESIAN_POINT ( 'NONE',  ( 1.208267226925118898, -17.17409317848484918, -12.70228502423913497 ) ) ;
#55476=CARTESIAN_POINT ( 'NONE',  ( -12.71107039382202508, -17.74871969248833636, -1.717622521776180466 ) ) ;
#55478=CARTESIAN_POINT ( 'NONE',  ( -1.750000000001000089, -23.24999998674999802, 12.56594318051000059 ) ) ;
#55479=CARTESIAN_POINT ( 'NONE',  ( 11.05577208806000122, -76.73394859499998688, -4.921212746988999243 ) ) ;
#55481=B_SPLINE_CURVE_WITH_KNOTS ( 'NONE', 3,
 ( #6212, #41072, #37503, #41365, #28057, #28643 ),
 .UNSPECIFIED., .F., .F.,
 ( 4, 2, 4 ),
 ( 0.000000000000000000, 0.5000000000000000000, 1.000000000000000000 ),
 .UNSPECIFIED. ) ;
#55483=CARTESIAN_POINT ( 'NONE',  ( 0.000000000000000000, -65.72928575305999743, 0.000000000000000000 ) ) ;
#55484=CARTESIAN_POINT ( 'NONE',  ( 7.081057523560999378, -79.19131633868998676, -10.01287680343000019 ) ) ;
#55487=ADVANCED_FACE ( 'NONE', ( #49444 ), #27273, .T. ) ;
#55489=CARTESIAN_POINT ( 'NONE',  ( 2.256045313337027292, -78.18992600313380592, -11.85249000648438411 ) ) ;
#55491=VERTEX_POINT ( 'NONE', #8396 ) ;
#55494=CARTESIAN_POINT ( 'NONE',  ( -1.750000000000000000, -58.54977139303999678, -12.65375411740000011 ) ) ;
#55496=CARTESIAN_POINT ( 'NONE',  ( 3.854927634485999732, -3.051506412944000157, 0.3462089483260999967 ) ) ;
#55500=EDGE_CURVE ( 'NONE', #28651, #41885, #31402, .T. ) ;
#55501=CARTESIAN_POINT ( 'NONE',  ( -10.72149750877111707, -76.16622351037557337, 4.807460443398728245 ) ) ;
#55506=CARTESIAN_POINT ( 'NONE',  ( 12.70228857838913505, -24.82190589608148201, 1.213561371330137861 ) ) ;
#55509=CARTESIAN_POINT ( 'NONE',  ( -7.220923959705244144, -76.87291666666665435, -9.396085398178621872 ) ) ;
#55513=CARTESIAN_POINT ( 'NONE',  ( 9.963464501286001251, -18.31723479381000175, -7.659241807038999816 ) ) ;
#55515=EDGE_LOOP ( 'NONE', ( #15222, #50186, #53929, #4681 ) ) ;
#55519=CARTESIAN_POINT ( 'NONE',  ( 10.11262422264428196, -77.65708660579868194, -6.589681015037502476 ) ) ;
#55522=CARTESIAN_POINT ( 'NONE',  ( -11.75000000000000000, -77.70000000000000284, 0.000000000000000000 ) ) ;
#55523=CARTESIAN_POINT ( 'NONE',  ( -8.583665412789912352, -17.02814425026586420, -9.102144266520932447 ) ) ;
#55524=ADVANCED_FACE ( 'NONE', ( #26683 ), #41517, .T. ) ;
#55526=FACE_OUTER_BOUND ( 'NONE', #4203, .T. ) ;
#55530=ORIENTED_EDGE ( 'NONE', *, *, #31916, .T. ) ;
#55533=ORIENTED_EDGE ( 'NONE', *, *, #32602, .F. ) ;
#55534=DIRECTION ( 'NONE',  ( 1.000000000000000000, 0.000000000000000000, 0.000000000000000000 ) ) ;
#55535=AXIS2_PLACEMENT_3D ( 'NONE', #39283, #30980, #48170 ) ;
#55537=CARTESIAN_POINT ( 'NONE',  ( 7.758655887927999650, -60.95078616210999911, 9.996711281005000060 ) ) ;
#55542=CARTESIAN_POINT ( 'NONE',  ( -8.274772993773998664, -24.97888614414509334, 9.689268730326240586 ) ) ;
#55546=LINE ( 'NONE', #23952, #48897 ) ;
#55548=CARTESIAN_POINT ( 'NONE',  ( -9.243145382174642322, -17.08347263195844334, 8.441178780136395332 ) ) ;
#55549=AXIS2_PLACEMENT_3D ( 'NONE', #28591, #23299, #46636 ) ;
#55553=EDGE_CURVE ( 'NONE', #23504, #50397, #11116, .T. ) ;
#55555=CARTESIAN_POINT ( 'NONE',  ( -8.533826143225001104, -25.00526450249999755, -9.213084459905999779 ) ) ;
#55558=ORIENTED_EDGE ( 'NONE', *, *, #7318, .F. ) ;
#55559=EDGE_CURVE ( 'NONE', #47356, #51133, #26408, .T. ) ;
#55565=CARTESIAN_POINT ( 'NONE',  ( -7.943801774166999508, -17.56598212471000053, 9.641153612788999183 ) ) ;
#55566=CARTESIAN_POINT ( 'NONE',  ( 1.750000000000000000, -23.24999999688999708, -12.50000000000000000 ) ) ;
#55567=CARTESIAN_POINT ( 'NONE',  ( 1.925972852894063836, -2.921010677132802602, -2.948710677374434486 ) ) ;
#55572=CARTESIAN_POINT ( 'NONE',  ( 0.000000000000000000, -2.660000000000000142, 0.000000000000000000 ) ) ;
#55574=EDGE_LOOP ( 'NONE', ( #6439, #14681, #15314, #39743, #35701 ) ) ;
#55576=CARTESIAN_POINT ( 'NONE',  ( -0.7707251311569810470, -77.07827341652770770, 11.74748571488081517 ) ) ;
#55577=CARTESIAN_POINT ( 'NONE',  ( 0.005119011380000999985, -61.73813862155999743, -12.43705489347999915 ) ) ;
#55578=ADVANCED_FACE ( 'NONE', ( #30536 ), #48569, .F. ) ;
#55579=LINE ( 'NONE', #15716, #54048 ) ;
#55584=CARTESIAN_POINT ( 'NONE',  ( -1.750000000001000089, -23.25000000990999993, -12.56594317857000043 ) ) ;
#55585=CARTESIAN_POINT ( 'NONE',  ( -10.18249594442533024, -54.50907903246198316, -7.792385963363297030 ) ) ;
#55587=AXIS2_PLACEMENT_3D ( 'NONE', #3931, #49108, #21651 ) ;
#55588=CARTESIAN_POINT ( 'NONE',  ( -7.624341764943999955, -60.06485149430999826, 10.42531124854999902 ) ) ;
#55589=CARTESIAN_POINT ( 'NONE',  ( 7.756275637014999447, -54.57995361804000112, -10.15825999914999933 ) ) ;
#55591=B_SPLINE_CURVE_WITH_KNOTS ( 'NONE', 3,
 ( #39108, #34664, #35233, #53264, #8388, #53860, #45597, #31981, #49732, #8683 ),
 .UNSPECIFIED., .F., .F.,
 ( 4, 2, 2, 2, 4 ),
 ( 0.000000000000000000, 0.2500000000000000000, 0.5000000000000000000, 0.7500000000000000000, 1.000000000000000000 ),
 .UNSPECIFIED. ) ;
#55596=TOROIDAL_SURFACE ( 'NONE', #40547, 1.250000000000000000, 0.5000000000000000000 ) ;
#55597=DIRECTION ( 'NONE',  ( 0.000000000000000000, -1.000000000000000000, 0.000000000000000000 ) ) ;
#55602=ORIENTED_EDGE ( 'NONE', *, *, #15874, .F. ) ;
#55606=DIRECTION ( 'NONE',  ( 0.000000000000000000, -1.000000000000000000, 0.000000000000000000 ) ) ;
#55612=EDGE_CURVE ( 'NONE', #53199, #21248, #17937, .T. ) ;
#55613=CARTESIAN_POINT ( 'NONE',  ( 0.9887300587123999396, -17.06589942230999668, 12.65963207090000076 ) ) ;
#55618=CYLINDRICAL_SURFACE ( 'NONE', #7454, 1.750000000000000000 ) ;
#55619=VERTEX_POINT ( 'NONE', #49140 ) ;
#55623=CARTESIAN_POINT ( 'NONE',  ( 0.000000000000000000, -23.25000000000000000, -12.50000000000000000 ) ) ;
#55630=CARTESIAN_POINT ( 'NONE',  ( 1.780723875404367718, -76.56267306090380487, 11.62581106263551156 ) ) ;
#55631=B_SPLINE_CURVE_WITH_KNOTS ( 'NONE', 3,
 ( #33133, #36988, #46170, #41132, #27539, #726 ),
 .UNSPECIFIED., .F., .F.,
 ( 4, 1, 1, 4 ),
 ( 0.000000000000000000, 0.3333333333333000081, 0.6666666666667000474, 1.000000000000000000 ),
 .UNSPECIFIED. ) ;
#55632=EDGE_CURVE ( 'NONE', #29156, #25767, #4751, .T. ) ;
#55637=DIRECTION ( 'NONE',  ( 2.011932846957000032E-11, -1.000000000000000000, -1.337053924462999991E-10 ) ) ;
#55640=CARTESIAN_POINT ( 'NONE',  ( 0.000000000000000000, -2.660000000000000142, 0.000000000000000000 ) ) ;
#55641=CARTESIAN_POINT ( 'NONE',  ( 0.4356486348716999690, -17.11935044189999999, -12.43591427121000237 ) ) ;
#55644=CARTESIAN_POINT ( 'NONE',  ( -7.919595949288999570, -59.94999999969999749, -9.050966799188000067 ) ) ;
#55645=CARTESIAN_POINT ( 'NONE',  ( -3.320509146851418958, -1.277620849617314702, -1.203439844071006126 ) ) ;
#55648=CARTESIAN_POINT ( 'NONE',  ( 0.4764073897346013386, -18.48308356130117502, -10.98970030907996431 ) ) ;
#55649=DIRECTION ( 'NONE',  ( 0.7071067811865475727, 0.000000000000000000, 0.7071067811865475727 ) ) ;
#55651=EDGE_CURVE ( 'NONE', #20090, #20675, #16050, .T. ) ;
#55653=CARTESIAN_POINT ( 'NONE',  ( 1.750000000001000089, -23.24999998674999802, -12.56594318051000059 ) ) ;
#55657=FACE_OUTER_BOUND ( 'NONE', #57545, .T. ) ;
#55662=DIRECTION ( 'NONE',  ( 1.000000000000000000, 0.000000000000000000, 0.000000000000000000 ) ) ;
#55664=CARTESIAN_POINT ( 'NONE',  ( 3.250000000000000000, -2.750000000000000000, 0.000000000000000000 ) ) ;
#55668=LINE ( 'NONE', #10215, #32430 ) ;
#55672=EDGE_LOOP ( 'NONE', ( #33868, #36353, #18503, #16686 ) ) ;
#55674=CARTESIAN_POINT ( 'NONE',  ( -12.50728321921983799, -61.79975184134815436, -0.1774118161306304509 ) ) ;
#55675=CARTESIAN_POINT ( 'NONE',  ( 7.850068285611341956, -17.68530314558086047, 9.837745660714951157 ) ) ;
#55676=VERTEX_POINT ( 'NONE', #28436 ) ;
#55679=ORIENTED_EDGE ( 'NONE', *, *, #46918, .F. ) ;
#55681=CONICAL_SURFACE ( 'NONE', #29235, 8.749999999256001360, 0.7853981633972997312 ) ;
#55683=AXIS2_PLACEMENT_3D ( 'NONE', #18568, #586, #14988 ) ;
#55685=EDGE_CURVE ( 'NONE', #47619, #1538, #51198, .T. ) ;
#55690=CARTESIAN_POINT ( 'NONE',  ( -7.613962827198000660, -60.10639625617000092, 10.53101998748999968 ) ) ;
#55691=ORIENTED_EDGE ( 'NONE', *, *, #44884, .T. ) ;
#55695=CARTESIAN_POINT ( 'NONE',  ( -12.50657384684486573, -17.02752586736362872, 0.3552647087867685238 ) ) ;
#55696=CARTESIAN_POINT ( 'NONE',  ( -0.5211966972079136173, -0.9921874999512605431, 3.256119704917901370 ) ) ;
#55699=CARTESIAN_POINT ( 'NONE',  ( -11.75000000000000711, -77.28958333333332575, 1.538071403319954955 ) ) ;
#55704=CARTESIAN_POINT ( 'NONE',  ( 7.037839055072352856, -76.52353836542157239, 9.409452059956553427 ) ) ;
#55708=EDGE_CURVE ( 'NONE', #15167, #57774, #44313, .T. ) ;
#55711=CARTESIAN_POINT ( 'NONE',  ( -3.002885140990844359, -3.070088000970283115, 1.241022100456280919 ) ) ;
#55717=CARTESIAN_POINT ( 'NONE',  ( -8.246370918359055224, -76.26250308826989510, -8.370124202908149513 ) ) ;
#55719=CARTESIAN_POINT ( 'NONE',  ( -0.2494208068355079355, -24.99288960762974909, 12.50614183112980626 ) ) ;
#55720=CARTESIAN_POINT ( 'NONE',  ( 0.2561524587948984522, -3.499999999999999112, 3.291991744369633377 ) ) ;
#55728=CIRCLE ( 'NONE', #4813, 1.250000000000000444 ) ;
#55730=CARTESIAN_POINT ( 'NONE',  ( 3.074539145570156951, -78.34369197868522861, -11.43814598833678708 ) ) ;
#55732=CARTESIAN_POINT ( 'NONE',  ( 4.340686961497000063, -76.32245797811999921, -11.41455165844999975 ) ) ;
#55739=CARTESIAN_POINT ( 'NONE',  ( -12.76303204522000101, -23.26485147686999966, -1.980584515753000208 ) ) ;
#55747=ADVANCED_FACE ( 'NONE', ( #8325 ), #22655, .F. ) ;
#55754=ORIENTED_EDGE ( 'NONE', *, *, #14682, .F. ) ;
#55765=ORIENTED_EDGE ( 'NONE', *, *, #21561, .F. ) ;
#55766=DIRECTION ( 'NONE',  ( 0.000000000000000000, 0.000000000000000000, 1.000000000000000000 ) ) ;
#55773=DIRECTION ( 'NONE',  ( 0.0001230612157847738313, 0.000000000000000000, -0.9999999924279686647 ) ) ;
#55775=DIRECTION ( 'NONE',  ( 1.000000000000000000, 0.000000000000000000, 0.000000000000000000 ) ) ;
#55778=CARTESIAN_POINT ( 'NONE',  ( -12.22985280536000019, -76.49175098858000865, -1.402219185755000153 ) ) ;
#55779=CARTESIAN_POINT ( 'NONE',  ( -7.624341766656999475, -60.06485146221000093, -10.42531125026000005 ) ) ;
#55780=B_SPLINE_CURVE_WITH_KNOTS ( 'NONE', 3,
 ( #39329, #16330, #47645, #3603, #16900, #30460, #38751, #52058, #34884, #48491, #43196, #8031, #16037, #34598, #34020, #7463, #26029, #21607 ),
 .UNSPECIFIED., .F., .F.,
 ( 4, 2, 2, 2, 2, 2, 2, 2, 4 ),
 ( 0.000000000000000000, 0.1250000000000000833, 0.2500000000000001665, 0.3750000000000001110, 0.5000000000000001110, 0.6250000000000001110, 0.7500000000000000000, 0.8750000000000000000, 1.000000000000000000 ),
 .UNSPECIFIED. ) ;
#55781=CARTESIAN_POINT ( 'NONE',  ( -12.50000000000000000, -23.24999999688999708, -1.750000000000000000 ) ) ;
#55782=LINE ( 'NONE', #29184, #25693 ) ;
#55783=CARTESIAN_POINT ( 'NONE',  ( -1.307210027570999911, -79.06450156920999461, -12.19386267984000050 ) ) ;
#55785=CYLINDRICAL_SURFACE ( 'NONE', #48714, 11.75000000000000000 ) ;
#55786=CARTESIAN_POINT ( 'NONE',  ( 3.224895395523625474, -2.840360689075250189, -0.4480854406879138940 ) ) ;
#55787=CARTESIAN_POINT ( 'NONE',  ( 11.81350916550069563, -77.81633707358489005, 2.468257657043821496 ) ) ;
#55791=CYLINDRICAL_SURFACE ( 'NONE', #16473, 1.750000000000000000 ) ;
#55795=CARTESIAN_POINT ( 'NONE',  ( 2.287685435952000024, -3.564198934507999628, -2.579189048856000088 ) ) ;
#55798=CARTESIAN_POINT ( 'NONE',  ( -8.194277599536388124, -76.13640838913404707, 8.421365530498844620 ) ) ;
#55799=CARTESIAN_POINT ( 'NONE',  ( 10.12290050124000018, -18.75000000007999645, -7.648026767085999822 ) ) ;
#55802=ORIENTED_EDGE ( 'NONE', *, *, #17079, .T. ) ;
#55805=CARTESIAN_POINT ( 'NONE',  ( -2.839805762151343949, -2.458333333333332593, 1.636761686205412181 ) ) ;
#55807=CARTESIAN_POINT ( 'NONE',  ( 7.954951288349001004, -18.55321828668999729, -9.722718241315000398 ) ) ;
#55809=CARTESIAN_POINT ( 'NONE',  ( 9.783235115942000348, -17.46434390394999880, -7.961033122320000821 ) ) ;
#55810=CARTESIAN_POINT ( 'NONE',  ( 0.000000000000000000, -28.92928575306000383, 0.000000000000000000 ) ) ;
#55811=EDGE_LOOP ( 'NONE', ( #24266, #39752, #18666, #42253, #11698 ) ) ;
#55816=ADVANCED_FACE ( 'NONE', ( #34889 ), #30747, .T. ) ;
#55817=CARTESIAN_POINT ( 'NONE',  ( 7.386320950128953733, -77.63040130628132829, -9.560526057520540633 ) ) ;
#55822=CARTESIAN_POINT ( 'NONE',  ( 1.781953555039999859, -2.911773310596999842, -3.363141973650999983 ) ) ;
#55826=ADVANCED_FACE ( 'NONE', ( #22189 ), #2647, .F. ) ;
#55827=CARTESIAN_POINT ( 'NONE',  ( -9.000000000000000000, -4.000000000000000000, 0.000000000000000000 ) ) ;
#55832=EDGE_LOOP ( 'NONE', ( #5000, #23437, #19489, #50164, #19012, #33293 ) ) ;
#55833=CARTESIAN_POINT ( 'NONE',  ( 10.15833271782000047, -17.78011549213000109, 7.756208840363000512 ) ) ;
#55835=EDGE_CURVE ( 'NONE', #2377, #18636, #32036, .T. ) ;
#55836=CARTESIAN_POINT ( 'NONE',  ( 0.4354618354436000649, -78.37228808732000118, -11.90553545880999842 ) ) ;
#55838=DIRECTION ( 'NONE',  ( 1.000000000000000000, 0.000000000000000000, 0.000000000000000000 ) ) ;
#55842=VERTEX_POINT ( 'NONE', #51940 ) ;
#55846=AXIS2_PLACEMENT_3D ( 'NONE', #8413, #18454, #49464 ) ;
#55853=CARTESIAN_POINT ( 'NONE',  ( 1.931087888240000217, -60.11584731951999316, -12.71658872087999903 ) ) ;
#55854=AXIS2_PLACEMENT_3D ( 'NONE', #42273, #19834, #23954 ) ;
#55855=DIRECTION ( 'NONE',  ( 1.000000000000000000, 0.000000000000000000, 0.000000000000000000 ) ) ;
#55858=B_SPLINE_CURVE_WITH_KNOTS ( 'NONE', 3,
 ( #44676, #40238, #11567, #25702, #2710, #24554 ),
 .UNSPECIFIED., .F., .F.,
 ( 4, 1, 1, 4 ),
 ( 0.000000000000000000, 0.3333333333333000081, 0.6666666666667000474, 1.000000000000000000 ),
 .UNSPECIFIED. ) ;
#55863=EDGE_CURVE ( 'NONE', #21570, #2251, #35013, .T. ) ;
#55864=CARTESIAN_POINT ( 'NONE',  ( -7.646944981223999349, -18.80364172516999943, 10.19022195330999914 ) ) ;
#55865=VECTOR ( 'NONE', #35899, 1000.000000000000000 ) ;
#55867=CARTESIAN_POINT ( 'NONE',  ( -2.995811057868809524, -2.703889681057667360, 1.977980227838953775 ) ) ;
#55875=AXIS2_PLACEMENT_3D ( 'NONE', #30512, #11949, #42959 ) ;
#55877=CARTESIAN_POINT ( 'NONE',  ( 1.930638663164000235, -60.02122063256000217, -12.72375916875000179 ) ) ;
#55878=CARTESIAN_POINT ( 'NONE',  ( -7.710118476742000126, -20.25022860572000027, -10.18499221090000084 ) ) ;
#55881=CARTESIAN_POINT ( 'NONE',  ( 8.541150802303999257, -25.00800189280999675, -9.205830468593999782 ) ) ;
#55884=CARTESIAN_POINT ( 'NONE',  ( 7.974576219238914021, -78.51319164874669809, 8.644719456487203857 ) ) ;
#55886=ORIENTED_EDGE ( 'NONE', *, *, #15164, .T. ) ;
#55889=CARTESIAN_POINT ( 'NONE',  ( 7.633403241802001027, -55.41350283619000550, -10.18127013546999926 ) ) ;
#55895=DIRECTION ( 'NONE',  ( 0.7071067811864981678, 0.000000000000000000, -0.7071067811865970887 ) ) ;
#55904=ORIENTED_EDGE ( 'NONE', *, *, #27610, .T. ) ;
#55907=VERTEX_POINT ( 'NONE', #52789 ) ;
#55909=VERTEX_POINT ( 'NONE', #57500 ) ;
#55910=CARTESIAN_POINT ( 'NONE',  ( 1.389926494651000155, -17.37618663744999736, 12.65988803923000106 ) ) ;
#55914=CARTESIAN_POINT ( 'NONE',  ( -13.13047446164998711, -56.01421830981000483, 0.8260994316375004365 ) ) ;
#55919=ADVANCED_FACE ( 'NONE', ( #8487 ), #30179, .T. ) ;
#55920=ORIENTED_EDGE ( 'NONE', *, *, #22628, .T. ) ;
#55921=VERTEX_POINT ( 'NONE', #17944 ) ;
#55922=CARTESIAN_POINT ( 'NONE',  ( 12.65375411750999923, -57.05022861049000227, 1.750000000000000000 ) ) ;
#55923=CARTESIAN_POINT ( 'NONE',  ( -12.80000000000000071, -0.1000000000000002554, 0.000000000000000000 ) ) ;
#55924=CARTESIAN_POINT ( 'NONE',  ( 1.980584515752000119, -60.06485146591000301, -12.76303204605000197 ) ) ;
#55926=FACE_OUTER_BOUND ( 'NONE', #54781, .T. ) ;
#55927=DIRECTION ( 'NONE',  ( 1.000000000000000000, 0.000000000000000000, 0.000000000000000000 ) ) ;
#55928=CARTESIAN_POINT ( 'NONE',  ( 11.81567892624999949, -79.00458388498999796, 1.523613136442999894 ) ) ;
#55931=CARTESIAN_POINT ( 'NONE',  ( -8.247965593175072385, -76.63679069186150628, 8.368539974147305216 ) ) ;
#55936=CARTESIAN_POINT ( 'NONE',  ( -1.750000000001000089, -19.24899163674999869, -12.60354432393000046 ) ) ;
#55937=CARTESIAN_POINT ( 'NONE',  ( 0.000000000000000000, -0.2000000000000000111, -9.000000000000271783 ) ) ;
#55938=DIRECTION ( 'NONE',  ( 0.000000000000000000, 1.000000000000000000, 0.000000000000000000 ) ) ;
#55939=CARTESIAN_POINT ( 'NONE',  ( 1.629367637659999923, -18.31736356602000271, -12.46114270826000059 ) ) ;
#55943=CARTESIAN_POINT ( 'NONE',  ( 3.530886011689700510, -1.499221606517874061, -0.03292542109241022863 ) ) ;
#55945=CARTESIAN_POINT ( 'NONE',  ( 1.750000000000000000, -55.55000000209000177, -12.50000000000000000 ) ) ;
#55946=CARTESIAN_POINT ( 'NONE',  ( 7.342377162853137129, -60.03019609282338109, -8.190817883596540838 ) ) ;
#55947=CARTESIAN_POINT ( 'NONE',  ( -8.852886909552351469, -77.64153493090338998, 7.764045341703079472 ) ) ;
#55950=CARTESIAN_POINT ( 'NONE',  ( 7.287838312904000304, -78.12030371036000531, -10.78085041437000058 ) ) ;
#55951=LINE ( 'NONE', #33495, #14834 ) ;
#55953=AXIS2_PLACEMENT_3D ( 'NONE', #3728, #13744, #45062 ) ;
#55955=DIRECTION ( 'NONE',  ( 0.9999548435846228323, 0.000000000000000000, 0.009503199022040118363 ) ) ;
#55958=DIRECTION ( 'NONE',  ( 1.000000000000000000, 0.000000000000000000, 0.000000000000000000 ) ) ;
#55960=CARTESIAN_POINT ( 'NONE',  ( 2.028166799595999770, -1.019127687536000026, -3.466423845304999585 ) ) ;
#55962=CARTESIAN_POINT ( 'NONE',  ( -8.485281374238999419, -60.04999999966999980, 8.485281374238999419 ) ) ;
#55966=ORIENTED_EDGE ( 'NONE', *, *, #48048, .T. ) ;
#55969=EDGE_CURVE ( 'NONE', #38447, #55909, #5448, .T. ) ;
#55975=ORIENTED_EDGE ( 'NONE', *, *, #36496, .T. ) ;
#55976=ORIENTED_EDGE ( 'NONE', *, *, #44919, .T. ) ;
#55979=AXIS2_PLACEMENT_3D ( 'NONE', #40177, #36332, #26305 ) ;
#55984=EDGE_CURVE ( 'NONE', #35168, #40044, #41493, .T. ) ;
#55985=B_SPLINE_CURVE_WITH_KNOTS ( 'NONE', 3,
 ( #38774, #25483, #15478, #33758, #11064, #3063 ),
 .UNSPECIFIED., .F., .F.,
 ( 4, 1, 1, 4 ),
 ( 0.000000000000000000, 0.3333333333333000081, 0.6666666666667000474, 1.000000000000000000 ),
 .UNSPECIFIED. ) ;
#55986=ORIENTED_EDGE ( 'NONE', *, *, #33671, .T. ) ;
#55987=CARTESIAN_POINT ( 'NONE',  ( -7.641012386057000505, -60.08917565288000162, 10.18589234709999936 ) ) ;
#56000=CARTESIAN_POINT ( 'NONE',  ( 8.381245741137949068, -76.51127116153249119, 8.234743652916119316 ) ) ;
#56008=CARTESIAN_POINT ( 'NONE',  ( 0.000000000000000000, -59.58578169018999660, 13.15643568216998638 ) ) ;
#56010=CARTESIAN_POINT ( 'NONE',  ( -6.589344923537027832, -76.27752133694943382, -9.728425524022272342 ) ) ;
#56011=CARTESIAN_POINT ( 'NONE',  ( 10.01234990228999955, -18.70150862776000267, 7.653559502277999194 ) ) ;
#56012=DIRECTION ( 'NONE',  ( 0.000000000000000000, -1.000000000000000000, -6.735284179502000863E-11 ) ) ;
#56015=DIRECTION ( 'NONE',  ( 0.000000000000000000, 0.000000000000000000, -1.000000000000000000 ) ) ;
#56016=CARTESIAN_POINT ( 'NONE',  ( -7.624341766639000539, -23.26485146254000114, -10.42531125024000005 ) ) ;
#56017=EDGE_CURVE ( 'NONE', #17378, #47194, #52784, .T. ) ;
#56021=CARTESIAN_POINT ( 'NONE',  ( 12.00296638904000091, -76.01348777726998662, 1.190414638386999790 ) ) ;
#56024=CIRCLE ( 'NONE', #34335, 9.000000000000000000 ) ;
#56027=CARTESIAN_POINT ( 'NONE',  ( 9.697390092161668917, -53.82767731314377357, 8.266602378548485675 ) ) ;
#56029=LINE ( 'NONE', #25010, #42723 ) ;
#56032=FACE_OUTER_BOUND ( 'NONE', #33811, .T. ) ;
#56036=CARTESIAN_POINT ( 'NONE',  ( -2.921318291229240138, -0.8958333333332216819, 1.685599492705018632 ) ) ;
#56038=ORIENTED_EDGE ( 'NONE', *, *, #10862, .F. ) ;
#56043=EDGE_LOOP ( 'NONE', ( #41012, #23447, #53993, #37137, #8989 ) ) ;
#56047=DIRECTION ( 'NONE',  ( 0.000000000000000000, -1.000000000000000000, 0.000000000000000000 ) ) ;
#56048=EDGE_LOOP ( 'NONE', ( #20482, #33005, #57126, #11176 ) ) ;
#56055=ORIENTED_EDGE ( 'NONE', *, *, #54248, .F. ) ;
#56056=CARTESIAN_POINT ( 'NONE',  ( -12.70451647735341005, -24.55458569106719224, -1.498866843992721076 ) ) ;
#56059=EDGE_LOOP ( 'NONE', ( #29309, #16114, #24957, #23147 ) ) ;
#56060=CARTESIAN_POINT ( 'NONE',  ( -12.66008999772000010, -24.62705329347999950, -1.387101471715999956 ) ) ;
#56061=ADVANCED_FACE ( 'NONE', ( #53077 ), #8201, .F. ) ;
#56066=CARTESIAN_POINT ( 'NONE',  ( -1.392423410630999929E-14, -75.80000000000001137, 0.000000000000000000 ) ) ;
#56067=AXIS2_PLACEMENT_3D ( 'NONE', #42978, #34382, #52413 ) ;
#56068=CARTESIAN_POINT ( 'NONE',  ( -12.74331394910258197, -18.47353206582842589, -1.980611464662582089 ) ) ;
#56071=CARTESIAN_POINT ( 'NONE',  ( 6.153863461931999623, -76.11465827134000506, -10.66140155521000032 ) ) ;
#56072=DIRECTION ( 'NONE',  ( 0.000000000000000000, 1.000000000000000000, 0.000000000000000000 ) ) ;
#56074=DIRECTION ( 'NONE',  ( 0.000000000000000000, -1.000000000000000000, 0.000000000000000000 ) ) ;
#56075=CARTESIAN_POINT ( 'NONE',  ( 11.81418954875000082, -78.71961295229000655, 3.289986436736999753 ) ) ;
#56077=CARTESIAN_POINT ( 'NONE',  ( -1.359416874709192810E-05, -0.8285695117701413759, -3.421591653122290300 ) ) ;
#56078=CARTESIAN_POINT ( 'NONE',  ( 4.229028970798999865, -77.89639184420045126, 11.24885535038115592 ) ) ;
#56080=ORIENTED_EDGE ( 'NONE', *, *, #16294, .T. ) ;
#56085=CARTESIAN_POINT ( 'NONE',  ( 1.229508168781000110, -2.945103494984999681, -3.669964256485999776 ) ) ;
#56086=EDGE_CURVE ( 'NONE', #54376, #26901, #17643, .T. ) ;
#56088=DIRECTION ( 'NONE',  ( 1.000000000000000000, 0.000000000000000000, 2.582622310454000054E-11 ) ) ;
#56089=CARTESIAN_POINT ( 'NONE',  ( -10.85214655116546645, -76.16855472728988730, 4.504555557915027819 ) ) ;
#56093=VERTEX_POINT ( 'NONE', #46290 ) ;
#56095=DIRECTION ( 'NONE',  ( 0.9999548435846228323, 0.000000000000000000, 0.009503199022040218977 ) ) ;
#56097=CARTESIAN_POINT ( 'NONE',  ( -3.250000000000000000, -2.500000000000000000, 0.000000000000000000 ) ) ;
#56098=CARTESIAN_POINT ( 'NONE',  ( -9.778543098509999254, -61.84857981670000271, 8.284584910426000093 ) ) ;
#56099=VECTOR ( 'NONE', #35769, 1000.000000000000000 ) ;
#56103=DIRECTION ( 'NONE',  ( 0.000000000000000000, -1.000000000000000000, 0.000000000000000000 ) ) ;
#56108=CARTESIAN_POINT ( 'NONE',  ( 11.97397552426821576, -77.69266700515451873, -1.561850544189498313 ) ) ;
#56109=CARTESIAN_POINT ( 'NONE',  ( 10.42531125074000009, -18.73514854687000053, 7.624341767140999870 ) ) ;
#56115=CARTESIAN_POINT ( 'NONE',  ( -1.980464483675000054, -21.75560170741999855, 12.85140862641999959 ) ) ;
#56117=CARTESIAN_POINT ( 'NONE',  ( 12.71162569430416944, -54.56025712733443811, -1.720540999444200914 ) ) ;
#56122=ORIENTED_EDGE ( 'NONE', *, *, #45586, .T. ) ;
#56123=CARTESIAN_POINT ( 'NONE',  ( 9.317995624416001377, -16.86762134170999872, 8.588852714006002032 ) ) ;
#56125=CARTESIAN_POINT ( 'NONE',  ( -5.852825220451999932, -78.74677611781000053, 10.54665655014000158 ) ) ;
#56127=DIRECTION ( 'NONE',  ( 1.000000000000000000, 0.000000000000000000, 0.000000000000000000 ) ) ;
#56128=LINE ( 'NONE', #56418, #33198 ) ;
#56131=ORIENTED_EDGE ( 'NONE', *, *, #15009, .F. ) ;
#56132=DIRECTION ( 'NONE',  ( 0.000000000000000000, -1.000000000000000000, 0.000000000000000000 ) ) ;
#56133=VERTEX_POINT ( 'NONE', #5241 ) ;
#56135=CARTESIAN_POINT ( 'NONE',  ( 12.50686498859614026, -61.10484291343465202, -1.423095205017603782 ) ) ;
#56141=EDGE_CURVE ( 'NONE', #6364, #9942, #557, .T. ) ;
#56154=CARTESIAN_POINT ( 'NONE',  ( -8.643969996075000495, -16.74046576158000121, 9.422817222712001950 ) ) ;
#56156=CARTESIAN_POINT ( 'NONE',  ( -3.192737306412670506, -2.215367439888774381, 1.482404185118484818 ) ) ;
#56167=CARTESIAN_POINT ( 'NONE',  ( 2.019183793707000074, -60.58720277209999949, -12.79944116707999946 ) ) ;
#56168=CARTESIAN_POINT ( 'NONE',  ( -8.107762507646583572, -55.28308356097522847, 7.434020715870143903 ) ) ;
#56174=CARTESIAN_POINT ( 'NONE',  ( 10.73992744223909845, -78.48307862101303556, 4.792036156107691625 ) ) ;
#56179=EDGE_CURVE ( 'NONE', #27205, #46904, #51005, .T. ) ;
#56190=LINE ( 'NONE', #34308, #16952 ) ;
#56192=LINE ( 'NONE', #15739, #46935 ) ;
#56194=ORIENTED_EDGE ( 'NONE', *, *, #28319, .T. ) ;
#56195=CARTESIAN_POINT ( 'NONE',  ( -12.43640296263000167, -53.88252466098000326, 0.05222744260232999730 ) ) ;
#56197=ORIENTED_EDGE ( 'NONE', *, *, #52861, .T. ) ;
#56199=ORIENTED_EDGE ( 'NONE', *, *, #11105, .F. ) ;
#56200=CARTESIAN_POINT ( 'NONE',  ( 0.4802748259353999960, -16.99473092717999734, 12.54896097834000024 ) ) ;
#56207=ORIENTED_EDGE ( 'NONE', *, *, #30881, .F. ) ;
#56208=VERTEX_POINT ( 'NONE', #18535 ) ;
#56210=DIRECTION ( 'NONE',  ( 0.000000000000000000, 1.000000000000000000, 0.000000000000000000 ) ) ;
#56211=CARTESIAN_POINT ( 'NONE',  ( -12.43359700621999941, -61.50705514136999597, -0.8500729763766999847 ) ) ;
#56214=CARTESIAN_POINT ( 'NONE',  ( -10.18589234708000113, -18.71082434677000350, 7.641012386038000592 ) ) ;
#56215=CARTESIAN_POINT ( 'NONE',  ( 6.878833068915999327, -78.91836173076998762, -9.726923957509001184 ) ) ;
#56216=B_SPLINE_SURFACE_WITH_KNOTS ( 'NONE', 3, 3, ( 
 ( #8742, #4313, #22313, #21730 ),
 ( #49493, #17305, #35291, #16738 ),
 ( #12303, #43900, #39163, #30293 ),
 ( #45655, #50082, #509, #5197 ),
 ( #223, #54507, #18485, #36768 ),
 ( #37351, #23199, #14329, #36478 ),
 ( #18776, #14044, #4909, #41497 ),
 ( #54785, #31746, #36193, #41204 ) ),
 .UNSPECIFIED., .F., .F., .F.,
 ( 4, 1, 1, 1, 1, 4 ),
 ( 4, 4 ),
 ( -0.01200407345748999953, 0.000000000000000000, 0.3333333333333000081, 0.6666666666667000474, 1.000000000000000000, 1.011997855551999947 ),
 ( -0.3559705542741000150, 1.355970554273999928 ),
 .UNSPECIFIED. ) ;
#56218=CARTESIAN_POINT ( 'NONE',  ( 1.750000000000000000, -60.04999999966999980, 12.00000000000000000 ) ) ;
#56219=CARTESIAN_POINT ( 'NONE',  ( -10.16113132621832094, -76.65749405865184940, 5.912008408672408066 ) ) ;
#56221=CARTESIAN_POINT ( 'NONE',  ( -9.783235115917999991, -54.26434390361999505, 7.961033122292000108 ) ) ;
#56224=CARTESIAN_POINT ( 'NONE',  ( -7.660431561281999535, -18.80820826823000047, -10.01749754194999831 ) ) ;
#56226=AXIS2_PLACEMENT_3D ( 'NONE', #29639, #32676, #11375 ) ;
#56228=CARTESIAN_POINT ( 'NONE',  ( 14.00000000000000000, -32.70420297070000260, 0.000000000000000000 ) ) ;
#56229=CARTESIAN_POINT ( 'NONE',  ( -7.919595949288999570, -59.94999999969999749, -9.050966799188000067 ) ) ;
#56230=LINE ( 'NONE', #15779, #21982 ) ;
#56231=CARTESIAN_POINT ( 'NONE',  ( 1.432628882339999965, -2.507710179781999837, -3.526139092948999743 ) ) ;
#56232=CARTESIAN_POINT ( 'NONE',  ( 3.516297666798653854, -0.9927055907450104133, -0.3226314711147756920 ) ) ;
#56233=TOROIDAL_SURFACE ( 'NONE', #38308, 13.50000000000000000, 0.5000000000000000000 ) ;
#56234=ORIENTED_EDGE ( 'NONE', *, *, #13539, .T. ) ;
#56235=PLANE ( 'NONE',  #38597 ) ;
#56236=ADVANCED_FACE ( 'NONE', ( #50129 ), #27071, .F. ) ;
#56237=LINE ( 'NONE', #25215, #18192 ) ;
#56238=CARTESIAN_POINT ( 'NONE',  ( -12.50240681834000078, -24.68234730741999883, 1.005418943852999902 ) ) ;
#56240=CIRCLE ( 'NONE', #5315, 3.600000000000000089 ) ;
#56243=CARTESIAN_POINT ( 'NONE',  ( 1.576170184330999868, -60.96086967183000382, 12.55466896108000086 ) ) ;
#56248=EDGE_CURVE ( 'NONE', #8867, #35775, #2861, .T. ) ;
#56252=DIRECTION ( 'NONE',  ( 0.000000000000000000, 0.000000000000000000, -1.000000000000000000 ) ) ;
#56259=CARTESIAN_POINT ( 'NONE',  ( 0.000000000000000000, -28.92928575306000383, 0.000000000000000000 ) ) ;
#56260=DIRECTION ( 'NONE',  ( -1.000000000000000000, 0.000000000000000000, 0.000000000000000000 ) ) ;
#56261=ORIENTED_EDGE ( 'NONE', *, *, #21021, .T. ) ;
#56263=EDGE_CURVE ( 'NONE', #245, #42686, #842, .T. ) ;
#56265=CIRCLE ( 'NONE', #30774, 5.000000000000000000 ) ;
#56266=ORIENTED_EDGE ( 'NONE', *, *, #25296, .T. ) ;
#56267=( NAMED_UNIT ( * ) PLANE_ANGLE_UNIT ( ) SI_UNIT ( $, .RADIAN. ) );
#56269=AXIS2_PLACEMENT_3D ( 'NONE', #40069, #49541, #44508 ) ;
#56274=AXIS2_PLACEMENT_3D ( 'NONE', #14309, #9608, #44744 ) ;
#56276=CARTESIAN_POINT ( 'NONE',  ( -2.417766456716999635, -2.993540208250999868, 2.392442992385000355 ) ) ;
#56277=ORIENTED_EDGE ( 'NONE', *, *, #18056, .F. ) ;
#56283=CARTESIAN_POINT ( 'NONE',  ( 3.086108443883076813, -79.09545426945904012, -11.86945146775599724 ) ) ;
#56284=DIRECTION ( 'NONE',  ( -0.9999999924279685537, 0.000000000000000000, -0.0001230612157848962919 ) ) ;
#56296=CARTESIAN_POINT ( 'NONE',  ( 0.000000000000000000, -39.30476017083000073, 0.000000000000000000 ) ) ;
#56298=LINE ( 'NONE', #33840, #28941 ) ;
#56299=CARTESIAN_POINT ( 'NONE',  ( 0.5668640726090544701, -24.91659694980802797, 12.50470739227063177 ) ) ;
#56300=ADVANCED_FACE ( 'NONE', ( #27661, #40674, #264, #4951 ), #27868, .T. ) ;
#56301=DIRECTION ( 'NONE',  ( 0.000000000000000000, 0.000000000000000000, -1.000000000000000000 ) ) ;
#56303=EDGE_CURVE ( 'NONE', #3192, #1897, #10400, .T. ) ;
#56304=FACE_OUTER_BOUND ( 'NONE', #14939, .T. ) ;
#56305=CARTESIAN_POINT ( 'NONE',  ( 12.54987272477000104, -25.05113590135999857, 0.1385846084899000075 ) ) ;
#56306=AXIS2_PLACEMENT_3D ( 'NONE', #43800, #48796, #34905 ) ;
#56310=CARTESIAN_POINT ( 'NONE',  ( -1.747928427208000013, -75.60822666423999294, -12.38958793587999985 ) ) ;
#56315=EDGE_CURVE ( 'NONE', #15875, #26901, #2003, .T. ) ;
#56316=AXIS2_PLACEMENT_3D ( 'NONE', #44796, #17634, #54539 ) ;
#56318=CARTESIAN_POINT ( 'NONE',  ( 9.668695434387000631, -79.36723320854999031, -7.222620064924999639 ) ) ;
#56321=AXIS2_PLACEMENT_3D ( 'NONE', #46397, #46105, #32190 ) ;
#56325=ORIENTED_EDGE ( 'NONE', *, *, #35686, .T. ) ;
#56330=DIRECTION ( 'NONE',  ( 0.000000000000000000, 1.000000000000000000, 0.000000000000000000 ) ) ;
#56332=ORIENTED_EDGE ( 'NONE', *, *, #45725, .F. ) ;
#56333=B_SPLINE_CURVE_WITH_KNOTS ( 'NONE', 3,
 ( #41615, #46359, #28606, #23319, #5884, #10042 ),
 .UNSPECIFIED., .F., .F.,
 ( 4, 2, 4 ),
 ( 0.000000000000000000, 0.5000000000000000000, 1.000000000000000000 ),
 .UNSPECIFIED. ) ;
#56340=ORIENTED_EDGE ( 'NONE', *, *, #27264, .T. ) ;
#56341=CARTESIAN_POINT ( 'NONE',  ( -12.70299718800736777, -25.02583482805824389, -0.8845454261047099864 ) ) ;
#56343=ORIENTED_EDGE ( 'NONE', *, *, #8375, .F. ) ;
#56347=AXIS2_PLACEMENT_3D ( 'NONE', #36863, #605, #55766 ) ;
#56349=CARTESIAN_POINT ( 'NONE',  ( 10.11462645678659200, -55.41287635801727163, 7.639895286212098569 ) ) ;
#56350=CARTESIAN_POINT ( 'NONE',  ( -7.601397897754999633, -55.54999999966999980, 9.369164850722000892 ) ) ;
#56351=CARTESIAN_POINT ( 'NONE',  ( -11.14527737854716527, -77.22513161494639178, -3.781945882020559591 ) ) ;
#56353=AXIS2_PLACEMENT_3D ( 'NONE', #34953, #24160, #56047 ) ;
#56356=CARTESIAN_POINT ( 'NONE',  ( -12.19234209666000091, -75.95901006652999854, -1.697737568323999913 ) ) ;
#56357=CIRCLE ( 'NONE', #29000, 1.250000000000000444 ) ;
#56360=CARTESIAN_POINT ( 'NONE',  ( 9.650948395536001811, -61.73402498629999968, -8.252474012569001260 ) ) ;
#56361=AXIS2_PLACEMENT_3D ( 'NONE', #35452, #40488, #36637 ) ;
#56362=DIRECTION ( 'NONE',  ( 1.000000000000000000, 0.000000000000000000, 0.000000000000000000 ) ) ;
#56364=CARTESIAN_POINT ( 'NONE',  ( -12.50000000000000000, -23.25000000000000000, 1.250000000000000000 ) ) ;
#56365=CARTESIAN_POINT ( 'NONE',  ( 7.720090653410608184, -77.86970692066191191, 9.274876966509804532 ) ) ;
#56372=CARTESIAN_POINT ( 'NONE',  ( -1.406402020388000107, -2.287363919000000134, 3.437511342334000020 ) ) ;
#56373=B_SPLINE_SURFACE_WITH_KNOTS ( 'NONE', 3, 3, ( 
 ( #34303, #52334, #11890, #47922 ),
 ( #7455, #25453, #22991, #27110 ),
 ( #49578, #22398, #41001, #594 ),
 ( #35973, #26814, #49874, #18576 ),
 ( #10007, #54586, #36851, #22697 ),
 ( #18281, #40710, #32122, #4398 ),
 ( #32410, #54296, #27985, #9125 ),
 ( #303, #36564, #13833, #44843 ) ),
 .UNSPECIFIED., .F., .F., .F.,
 ( 4, 1, 1, 1, 1, 4 ),
 ( 4, 4 ),
 ( -0.01200407347462000007, 0.000000000000000000, 0.3333333333333000081, 0.6666666666667000474, 1.000000000000000000, 1.011997855551999947 ),
 ( -0.3559705542741999906, 1.355970554273999928 ),
 .UNSPECIFIED. ) ;
#56376=CARTESIAN_POINT ( 'NONE',  ( -9.042463335936661295, -76.14465617035568812, 7.502879964933097945 ) ) ;
#56379=DIRECTION ( 'NONE',  ( 0.000000000000000000, 1.000000000000000000, 0.000000000000000000 ) ) ;
#56383=ADVANCED_FACE ( 'NONE', ( #51590 ), #29123, .F. ) ;
#56385=CARTESIAN_POINT ( 'NONE',  ( -7.631896413346999530, -60.02122715173999978, 10.36221694968000051 ) ) ;
#56394=CARTESIAN_POINT ( 'NONE',  ( -13.97864847851000114, -45.76668425569999954, -0.0001086640162462999885 ) ) ;
#56398=CARTESIAN_POINT ( 'NONE',  ( 12.50745077494999968, -61.79994448255000350, 2.662030659623000237E-09 ) ) ;
#56401=CARTESIAN_POINT ( 'NONE',  ( -9.546815223803999828, -54.11472046612000497, -8.130854305859001485 ) ) ;
#56402=FACE_OUTER_BOUND ( 'NONE', #1752, .T. ) ;
#56405=VERTEX_POINT ( 'NONE', #34119 ) ;
#56406=ORIENTED_EDGE ( 'NONE', *, *, #24691, .F. ) ;
#56410=CARTESIAN_POINT ( 'NONE',  ( 9.641218323609999530, -17.56606991914999938, 7.943737929428000832 ) ) ;
#56414=CARTESIAN_POINT ( 'NONE',  ( 11.63291926114999875, -77.45276987983000083, 5.337072863433999892 ) ) ;
#56417=CARTESIAN_POINT ( 'NONE',  ( -12.00000000000000000, -23.15000000000000213, -0.8000000000000000444 ) ) ;
#56418=CARTESIAN_POINT ( 'NONE',  ( 10.42531124905999995, -18.73514851523999880, -7.624341765453999997 ) ) ;
#56422=VERTEX_POINT ( 'NONE', #15117 ) ;
#56424=CARTESIAN_POINT ( 'NONE',  ( 12.56594317825999951, -60.05000001354000005, -1.750000000000000000 ) ) ;
#56425=DIRECTION ( 'NONE',  ( -0.7071067811865475727, 0.000000000000000000, -0.7071067811865475727 ) ) ;
#56426=DIRECTION ( 'NONE',  ( -0.7071067811865475727, 0.000000000000000000, 0.7071067811865475727 ) ) ;
#56428=FACE_OUTER_BOUND ( 'NONE', #41376, .T. ) ;
#56432=CARTESIAN_POINT ( 'NONE',  ( -7.640030264156999706, -23.30716680861999990, 10.18491080493000212 ) ) ;
#56435=CARTESIAN_POINT ( 'NONE',  ( -7.342331066867000544, -59.94999999967000548, 8.190859204290999784 ) ) ;
#56439=CARTESIAN_POINT ( 'NONE',  ( -8.485281374238999419, -59.94999999967000548, 8.485281374238999419 ) ) ;
#56442=CARTESIAN_POINT ( 'NONE',  ( -7.647094085193999469, -18.63104695440999947, 10.00844048070000092 ) ) ;
#56444=CARTESIAN_POINT ( 'NONE',  ( -2.215970870699417006, -2.179180607209704856, 2.738679624322115203 ) ) ;
#56447=CARTESIAN_POINT ( 'NONE',  ( 2.065550207748000133, -55.37434920636000157, -12.82162303852000029 ) ) ;
#56451=ORIENTED_EDGE ( 'NONE', *, *, #31045, .F. ) ;
#56452=CARTESIAN_POINT ( 'NONE',  ( -0.8000000000000000444, -23.15000000000000213, 12.00000000000000000 ) ) ;
#56453=CARTESIAN_POINT ( 'NONE',  ( 11.44512976686996808, -76.96771873177330292, 3.079394274004417564 ) ) ;
#56454=CARTESIAN_POINT ( 'NONE',  ( 0.5506765233276000870, -62.05954292211000478, -12.77514798316000011 ) ) ;
#56455=CARTESIAN_POINT ( 'NONE',  ( -7.674614791488999721, -22.75100836106000202, -10.14948852564000070 ) ) ;
#56456=EDGE_CURVE ( 'NONE', #26037, #10086, #43435, .T. ) ;
#56459=CARTESIAN_POINT ( 'NONE',  ( 9.996770077869998161, -24.15065455350000079, -7.758602204116000323 ) ) ;
#56462=CARTESIAN_POINT ( 'NONE',  ( -10.11462613664629195, -60.18712935448252210, 7.639894945646047653 ) ) ;
#56463=CARTESIAN_POINT ( 'NONE',  ( 9.781558643814788567, -78.49484497342521649, 6.508323693118907904 ) ) ;
#56465=EDGE_LOOP ( 'NONE', ( #55381, #26730, #23365, #34682 ) ) ;
#56467=CARTESIAN_POINT ( 'NONE',  ( -3.190103214945636534, -75.80000000000002558, -11.32367545015943122 ) ) ;
#56470=PLANE ( 'NONE',  #7169 ) ;
#56474=VECTOR ( 'NONE', #15694, 1000.000000000000000 ) ;
#56475=ADVANCED_FACE ( 'NONE', ( #13586 ), #15156, .F. ) ;
#56476=CARTESIAN_POINT ( 'NONE',  ( -7.792421629638690561, -54.50899070338012820, 10.18245656324170412 ) ) ;
#56477=ORIENTED_EDGE ( 'NONE', *, *, #45866, .T. ) ;
#56478=CARTESIAN_POINT ( 'NONE',  ( 1.799502287691000069, -23.30716680861999990, 12.60413670420000010 ) ) ;
#56479=CARTESIAN_POINT ( 'NONE',  ( -12.79895559715999909, -23.80469146265000191, 2.015913954444999767 ) ) ;
#56480=EDGE_LOOP ( 'NONE', ( #17181, #31462, #29443 ) ) ;
#56481=VERTEX_POINT ( 'NONE', #43593 ) ;
#56483=CARTESIAN_POINT ( 'NONE',  ( -12.83675912438999944, -55.57244613998999938, -2.062833085520999976 ) ) ;
#56485=EDGE_LOOP ( 'NONE', ( #52766, #1314, #55904 ) ) ;
#56488=AXIS2_PLACEMENT_3D ( 'NONE', #18591, #893, #14719 ) ;
#56495=EDGE_LOOP ( 'NONE', ( #18450, #49037, #46319, #16809, #43494 ) ) ;
#56498=CARTESIAN_POINT ( 'NONE',  ( -12.70455691843901391, -24.56014620597534659, 1.489817752277837970 ) ) ;
#56499=DIRECTION ( 'NONE',  ( 0.000000000000000000, -1.000000000000000000, 0.000000000000000000 ) ) ;
#56502=CARTESIAN_POINT ( 'NONE',  ( 7.712213536753880661, -60.86179137582710297, 10.27334987167996694 ) ) ;
#56506=DIRECTION ( 'NONE',  ( 0.000000000000000000, 1.433670265775999799E-08, 0.9999999999999998890 ) ) ;
#56507=CARTESIAN_POINT ( 'NONE',  ( -10.65162040723731174, -76.66484428198535284, 4.960591388563448056 ) ) ;
#56508=CARTESIAN_POINT ( 'NONE',  ( -9.389188763448000685, -54.08956227294000740, 8.194870530143999687 ) ) ;
#56510=B_SPLINE_CURVE_WITH_KNOTS ( 'NONE', 3,
 ( #5929, #5635, #50529, #50237, #33073, #45816 ),
 .UNSPECIFIED., .F., .F.,
 ( 4, 2, 4 ),
 ( 0.000000000000000000, 0.4999999999999998890, 1.000000000000000000 ),
 .UNSPECIFIED. ) ;
#56512=CARTESIAN_POINT ( 'NONE',  ( 1.799475295154000065, -20.24916621771999914, -12.69619287815999975 ) ) ;
#56513=DIRECTION ( 'NONE',  ( 0.000000000000000000, -1.000000000000000000, 0.000000000000000000 ) ) ;
#56515=CIRCLE ( 'NONE', #31021, 0.8000000000000000444 ) ;
#56518=CARTESIAN_POINT ( 'NONE',  ( 3.772660615778999915, -2.112549966925000078, 0.5031134774969999723 ) ) ;
#56521=CARTESIAN_POINT ( 'NONE',  ( -3.250000000000000000, -1.600000000000000089, 0.000000000000000000 ) ) ;
#56523=DIRECTION ( 'NONE',  ( 0.000000000000000000, 0.000000000000000000, -1.000000000000000000 ) ) ;
#56529=CARTESIAN_POINT ( 'NONE',  ( -1.997276839918471714, -3.072916666666665186, -2.598917237794086788 ) ) ;
#56530=VECTOR ( 'NONE', #4927, 1000.000000000000114 ) ;
#56534=CARTESIAN_POINT ( 'NONE',  ( 7.388277095310935572, -76.37882974025046678, -9.138970832679994771 ) ) ;
#56538=CARTESIAN_POINT ( 'NONE',  ( -0.7999999999999001243, -23.15000000002000036, 12.00000000000000000 ) ) ;
#56540=CARTESIAN_POINT ( 'NONE',  ( 2.324423181964641483, -3.413061686833799513, 2.330852653237942995 ) ) ;
#56543=CARTESIAN_POINT ( 'NONE',  ( 12.00000000000000000, -75.80000000000001137, -2.990830162875999918E-13 ) ) ;
#56548=EDGE_LOOP ( 'NONE', ( #51557, #54743, #44083, #42908 ) ) ;
#56549=CARTESIAN_POINT ( 'NONE',  ( 7.639893274949067781, -60.18715751166909911, 10.11462445492872320 ) ) ;
#56552=CARTESIAN_POINT ( 'NONE',  ( -3.206516299415000049, -1.613032031399000088, -0.5298615117031000299 ) ) ;
#56553=EDGE_LOOP ( 'NONE', ( #15094, #38953, #56055, #39473 ) ) ;
#56554=EDGE_CURVE ( 'NONE', #2183, #36137, #23126, .T. ) ;
#56557=VERTEX_POINT ( 'NONE', #3156 ) ;
#56558=FACE_OUTER_BOUND ( 'NONE', #54689, .T. ) ;
#56559=CARTESIAN_POINT ( 'NONE',  ( -2.312505707054999693, -2.621129995393999934, -2.494332668574000156 ) ) ;
#56560=EDGE_LOOP ( 'NONE', ( #4634, #39872, #28502, #23148 ) ) ;
#56564=CARTESIAN_POINT ( 'NONE',  ( -10.98362417419999915, -18.84999999999999787, 0.5999999999999999778 ) ) ;
#56566=CIRCLE ( 'NONE', #43365, 1.750000000000001332 ) ;
#56582=CARTESIAN_POINT ( 'NONE',  ( 8.096452064242996016, -56.01421830980998351, 13.15643568217000769 ) ) ;
#56584=CARTESIAN_POINT ( 'NONE',  ( -8.320799520507147662, -76.26179927676547265, -8.295681968662517392 ) ) ;
#56585=FACE_OUTER_BOUND ( 'NONE', #6674, .T. ) ;
#56586=CARTESIAN_POINT ( 'NONE',  ( -8.478749451788999636, -61.67812788887000153, -9.108222796200999838 ) ) ;
#56588=CARTESIAN_POINT ( 'NONE',  ( 9.369164850722000892, -18.75000000000000000, 7.601397897754999633 ) ) ;
#56589=VECTOR ( 'NONE', #37398, 1000.000000000000000 ) ;
#56591=CARTESIAN_POINT ( 'NONE',  ( -12.49989298250000047, -18.80773379996000116, -1.666426105558000081 ) ) ;
#56592=CARTESIAN_POINT ( 'NONE',  ( -3.201433918554999813, -77.94678050555000937, 12.61309089657999927 ) ) ;
#56595=CARTESIAN_POINT ( 'NONE',  ( 5.891627775763704555, -78.36429044821750267, -10.19952481748152984 ) ) ;
#56597=CARTESIAN_POINT ( 'NONE',  ( -5.822602226006999615, -76.66743281994000370, -10.90510414457000010 ) ) ;
#56600=DIRECTION ( 'NONE',  ( 8.659560562353647261E-17, -0.7071067811866525998, 0.7071067811864425456 ) ) ;
#56601=CARTESIAN_POINT ( 'NONE',  ( 12.43571054531000186, -61.67980566386000163, 0.4385525234352000146 ) ) ;
#56602=CARTESIAN_POINT ( 'NONE',  ( -10.06619577067999849, -78.63438750088999996, -7.895242330167000055 ) ) ;
#56603=CARTESIAN_POINT ( 'NONE',  ( 12.79971535682999928, -55.00965922235999983, -2.019101350716999921 ) ) ;
#56610=AXIS2_PLACEMENT_3D ( 'NONE', #26392, #21684, #13700 ) ;
#56611=AXIS2_PLACEMENT_3D ( 'NONE', #3160, #11729, #17298 ) ;
#56615=CARTESIAN_POINT ( 'NONE',  ( -1.456717367586000012E-14, -79.29999999999999716, 0.000000000000000000 ) ) ;
#56627=ORIENTED_EDGE ( 'NONE', *, *, #31742, .F. ) ;
#56628=CARTESIAN_POINT ( 'NONE',  ( 12.77649795258999887, -53.49168567723999956, -0.06462540730615000395 ) ) ;
#56630=AXIS2_PLACEMENT_3D ( 'NONE', #47052, #6581, #56761 ) ;
#56631=ADVANCED_FACE ( 'NONE', ( #56304 ), #16325, .F. ) ;
#56632=VERTEX_POINT ( 'NONE', #39154 ) ;
#56634=CARTESIAN_POINT ( 'NONE',  ( 9.723174505952000501, -24.47697504198000118, 7.958760297001999717 ) ) ;
#56635=CARTESIAN_POINT ( 'NONE',  ( 7.618394506877000261, -55.57286435768999411, 10.53494428257999971 ) ) ;
#56643=CARTESIAN_POINT ( 'NONE',  ( -1.476182556144000069, -76.33256575806998967, 12.22114576030999977 ) ) ;
#56644=CIRCLE ( 'NONE', #4808, 1.250000000000000444 ) ;
#56646=AXIS2_PLACEMENT_3D ( 'NONE', #35920, #826, #53951 ) ;
#56648=CARTESIAN_POINT ( 'NONE',  ( 9.395758989587999821, -61.50491532550999096, -8.188252216855000043 ) ) ;
#56649=CARTESIAN_POINT ( 'NONE',  ( -5.531768889155999958, -79.03576085112999294, -10.94525552207000096 ) ) ;
#56654=ORIENTED_EDGE ( 'NONE', *, *, #53, .T. ) ;
#56657=CARTESIAN_POINT ( 'NONE',  ( 1.933650113856000052, -23.40786253026000097, 12.70909635754000000 ) ) ;
#56658=DIRECTION ( 'NONE',  ( -0.9999999999999694689, -2.469236813514923644E-07, 1.229032068775961321E-12 ) ) ;
#56659=ADVANCED_FACE ( 'NONE', ( #53026 ), #30857, .F. ) ;
#56660=CARTESIAN_POINT ( 'NONE',  ( 1.130171038138000128, -3.119265194441000144, -3.373452425123000253 ) ) ;
#56666=ORIENTED_EDGE ( 'NONE', *, *, #36905, .T. ) ;
#56671=CARTESIAN_POINT ( 'NONE',  ( 1.250000000000000000, -23.25000000000000000, 12.50000000000000000 ) ) ;
#56672=CARTESIAN_POINT ( 'NONE',  ( -7.645398488040000551, -60.01531609111000165, 10.18948971875999909 ) ) ;
#56673=DIRECTION ( 'NONE',  ( -0.7071067811865475727, 0.000000000000000000, 0.7071067811865475727 ) ) ;
#56675=DIRECTION ( 'NONE',  ( -0.7071067811865474617, 0.000000000000000000, -0.7071067811865474617 ) ) ;
#56677=ORIENTED_EDGE ( 'NONE', *, *, #22628, .F. ) ;
#56678=ADVANCED_FACE ( 'NONE', ( #16726 ), #3599, .F. ) ;
#56679=CARTESIAN_POINT ( 'NONE',  ( 0.000000000000000000, 4.040000000000000036, 0.000000000000000000 ) ) ;
#56689=VECTOR ( 'NONE', #29870, 1000.000000000000000 ) ;
#56690=CARTESIAN_POINT ( 'NONE',  ( 0.000000000000000000, 0.000000000000000000, -12.00000000000000000 ) ) ;
#56698=ORIENTED_EDGE ( 'NONE', *, *, #33195, .T. ) ;
#56699=CARTESIAN_POINT ( 'NONE',  ( 7.633502222236000279, -18.79895684643999942, 10.36289759016999845 ) ) ;
#56701=FACE_OUTER_BOUND ( 'NONE', #5944, .T. ) ;
#56702=CARTESIAN_POINT ( 'NONE',  ( 5.917523019358082337, -75.96666666666665435, -10.26699006316252394 ) ) ;
#56703=CARTESIAN_POINT ( 'NONE',  ( 6.861116763436999832, -76.75513797953000505, -9.781075755418999762 ) ) ;
#56705=LINE ( 'NONE', #43708, #35281 ) ;
#56709=EDGE_CURVE ( 'NONE', #46904, #11745, #52870, .T. ) ;
#56710=ORIENTED_EDGE ( 'NONE', *, *, #19989, .T. ) ;
#56711=CARTESIAN_POINT ( 'NONE',  ( 8.130813118348999780, -54.11476110100999648, -9.546856411313999757 ) ) ;
#56715=CARTESIAN_POINT ( 'NONE',  ( -12.76303204517000012, -18.73514852243999940, 1.980584515753000208 ) ) ;
#56719=CARTESIAN_POINT ( 'NONE',  ( 13.86301033151699791, -46.43897132165000130, 0.1317488955328562639 ) ) ;
#56722=LINE ( 'NONE', #35117, #29980 ) ;
#56725=CARTESIAN_POINT ( 'NONE',  ( 0.000000000000000000, -0.6500000000000000222, 0.000000000000000000 ) ) ;
#56727=CARTESIAN_POINT ( 'NONE',  ( -8.838834764832000701, -60.04999999966999980, -8.838834764832000701 ) ) ;
#56730=AXIS2_PLACEMENT_3D ( 'NONE', #45628, #23170, #27004 ) ;
#56732=CARTESIAN_POINT ( 'NONE',  ( 9.931052046391080523, -60.92278631056069571, 7.764003813279091837 ) ) ;
#56737=CARTESIAN_POINT ( 'NONE',  ( -2.021854267373811354, -1.826358988587633680, -2.882029951968737791 ) ) ;
#56744=ORIENTED_EDGE ( 'NONE', *, *, #23668, .F. ) ;
#56746=CARTESIAN_POINT ( 'NONE',  ( 0.4802748259344000181, -61.80526907249000601, -12.54896097838000024 ) ) ;
#56747=FACE_OUTER_BOUND ( 'NONE', #32391, .T. ) ;
#56749=CARTESIAN_POINT ( 'NONE',  ( 9.966224254735001509, -23.66904904784999886, -7.657729124005999921 ) ) ;
#56753=CARTESIAN_POINT ( 'NONE',  ( -10.18248259422395385, -61.09095036164143266, 7.792398156856014779 ) ) ;
#56755=EDGE_CURVE ( 'NONE', #16171, #16697, #7007, .T. ) ;
#56761=DIRECTION ( 'NONE',  ( 1.000000000000000000, 0.000000000000000000, 0.000000000000000000 ) ) ;
#56762=DIRECTION ( 'NONE',  ( 2.622169155355999834E-09, -1.000000000000000000, 6.038616382182999929E-09 ) ) ;
#56767=B_SPLINE_CURVE_WITH_KNOTS ( 'NONE', 3,
 ( #17242, #8383, #26381, #21955, #13390, #44401, #8681, #39967 ),
 .UNSPECIFIED., .F., .F.,
 ( 4, 2, 2, 4 ),
 ( 0.000000000000000000, 0.5000000000000026645, 0.7500000000000013323, 1.000000000000000000 ),
 .UNSPECIFIED. ) ;
#56768=CARTESIAN_POINT ( 'NONE',  ( -12.66736977981000045, -24.23307288772000234, 1.690635117038000068 ) ) ;
#56771=DIRECTION ( 'NONE',  ( 0.000000000000000000, -1.000000000000000000, 0.000000000000000000 ) ) ;
#56772=ADVANCED_FACE ( 'NONE', ( #44988 ), #35644, .F. ) ;
#56773=CIRCLE ( 'NONE', #51136, 1.250000000000000000 ) ;
#56775=EDGE_LOOP ( 'NONE', ( #2092, #10229, #24237, #1967, #28286, #2449 ) ) ;
#56776=CARTESIAN_POINT ( 'NONE',  ( 10.18114973714000016, -23.39009320411999937, 7.633087466104000463 ) ) ;
#56781=ADVANCED_FACE ( 'NONE', ( #50884 ), #14258, .F. ) ;
#56782=ORIENTED_EDGE ( 'NONE', *, *, #36617, .F. ) ;
#56783=ORIENTED_EDGE ( 'NONE', *, *, #43376, .T. ) ;
#56785=CARTESIAN_POINT ( 'NONE',  ( 2.425729133266999670E-14, -6.000000000000000000, 0.000000000000000000 ) ) ;
#56786=EDGE_CURVE ( 'NONE', #425, #1025, #32079, .T. ) ;
#56789=CIRCLE ( 'NONE', #31304, 0.5000000000000006661 ) ;
#56795=DIRECTION ( 'NONE',  ( 1.000000000000000000, 0.000000000000000000, 0.000000000000000000 ) ) ;
#56796=B_SPLINE_CURVE_WITH_KNOTS ( 'NONE', 3,
 ( #27866, #45913, #5449, #23452, #19034, #16057, #16635, #29896, #34619, #33757, #3062, #21058, #38773, #43216, #34331, #47668, #7772, #2203, #11638, #24625, #56502, #2772, #7194, #39059 ),
 .UNSPECIFIED., .F., .F.,
 ( 4, 2, 2, 2, 2, 2, 2, 2, 2, 2, 2, 4 ),
 ( 0.000000000000000000, 0.1250000000000037748, 0.2500000000000075495, 0.3750000000000113243, 0.4375000000000126010, 0.5000000000000138778, 0.6250000000000164313, 0.7500000000000189848, 0.8125000000000188738, 0.8437500000000172085, 0.8750000000000156541, 1.000000000000000000 ),
 .UNSPECIFIED. ) ;
#56797=CARTESIAN_POINT ( 'NONE',  ( -7.646944981205999525, -55.60364172484999301, 10.19022195329000091 ) ) ;
#56801=CARTESIAN_POINT ( 'NONE',  ( 7.642160924870000649, -56.01538333533000014, 10.55911395186000057 ) ) ;
#56802=CARTESIAN_POINT ( 'NONE',  ( 0.9781264271452999592, -17.05968856123000066, -12.65967462879000038 ) ) ;
#56803=ADVANCED_FACE ( 'NONE', ( #46461 ), #34686, .F. ) ;
#56804=DIRECTION ( 'NONE',  ( 0.000000000000000000, -1.000000000000000000, -7.916704280318000023E-14 ) ) ;
#56808=CARTESIAN_POINT ( 'NONE',  ( -17.50000000000000000, -21.00000000000000000, 0.000000000000000000 ) ) ;
#56809=CARTESIAN_POINT ( 'NONE',  ( 0.4149022863988324206, -1.615298193465790844, 3.592925692889842537 ) ) ;
#56811=CARTESIAN_POINT ( 'NONE',  ( 11.75000000000000000, -76.55000000000001137, 0.000000000000000000 ) ) ;
#56813=CARTESIAN_POINT ( 'NONE',  ( 9.723199429438999175, -17.52306056078000296, -7.958735708418001487 ) ) ;
#56815=CARTESIAN_POINT ( 'NONE',  ( -3.403714747353000281, -1.627194400157000009, 0.2011706747331999945 ) ) ;
#56817=TOROIDAL_SURFACE ( 'NONE', #54906, 17.50000000000000000, 5.000000000000000000 ) ;
#56819=CARTESIAN_POINT ( 'NONE',  ( 1.798336774605999944, -59.99644498018999883, 12.61277771568000006 ) ) ;
#56821=EDGE_CURVE ( 'NONE', #33149, #34959, #11383, .T. ) ;
#56826=CARTESIAN_POINT ( 'NONE',  ( 8.472913207660081270, -76.38898086387824549, -8.150121671469577223 ) ) ;
#56834=CARTESIAN_POINT ( 'NONE',  ( -8.121706841748752126, -17.16372996695940500, -9.841114038392955621 ) ) ;
#56835=CIRCLE ( 'NONE', #52159, 1.750000000000001332 ) ;
#56836=TOROIDAL_SURFACE ( 'NONE', #20057, 13.50000000000000000, 0.5000000000000000000 ) ;
#56838=CARTESIAN_POINT ( 'NONE',  ( -12.50000000000000000, -23.25000000000000000, -1.250000000000000000 ) ) ;
#56839=FACE_OUTER_BOUND ( 'NONE', #46915, .T. ) ;
#56840=ORIENTED_EDGE ( 'NONE', *, *, #6751, .F. ) ;
#56841=CARTESIAN_POINT ( 'NONE',  ( 12.50240633877000107, -17.31762602171999887, 1.005381409788000058 ) ) ;
#56842=ORIENTED_EDGE ( 'NONE', *, *, #41347, .F. ) ;
#56844=CARTESIAN_POINT ( 'NONE',  ( 0.000000000000000000, -6.000000000000000000, 0.000000000000000000 ) ) ;
#56845=ORIENTED_EDGE ( 'NONE', *, *, #23986, .T. ) ;
#56848=VERTEX_POINT ( 'NONE', #4085 ) ;
#56849=CARTESIAN_POINT ( 'NONE',  ( -4.839793374392999503, -78.41318513125000322, 11.17717652876000045 ) ) ;
#56850=CARTESIAN_POINT ( 'NONE',  ( 7.889735440105552833, -55.04957415510977370, -7.666647577137438496 ) ) ;
#56854=AXIS2_PLACEMENT_3D ( 'NONE', #29342, #34635, #52663 ) ;
#56856=PRODUCT ( 'Body', 'Body', '', ( #5722 ) ) ;
#56858=FACE_OUTER_BOUND ( 'NONE', #26989, .T. ) ;
#56860=CARTESIAN_POINT ( 'NONE',  ( -4.828331629711049899, -79.06770833335490067, 10.85705384256994677 ) ) ;
#56864=CARTESIAN_POINT ( 'NONE',  ( -10.12290050253000118, -23.24999997822999731, 7.648026768374000639 ) ) ;
#56868=CARTESIAN_POINT ( 'NONE',  ( -1.428377931972672377, -3.012610289119709517, 2.918575344840368402 ) ) ;
#56872=EDGE_CURVE ( 'NONE', #14936, #37124, #28328, .T. ) ;
#56874=CARTESIAN_POINT ( 'NONE',  ( 0.000000000000000000, -63.10294702885996543, 12.53545825868000207 ) ) ;
#56876=CARTESIAN_POINT ( 'NONE',  ( -8.407949263131950346, -76.26097042042334806, -8.207523428525416165 ) ) ;
#56879=CARTESIAN_POINT ( 'NONE',  ( -7.969039355710000549, -61.42377467811000002, -9.934746417661001416 ) ) ;
#56880=ADVANCED_FACE ( 'NONE', ( #32399 ), #23273, .F. ) ;
#56885=LINE ( 'NONE', #16441, #34217 ) ;
#56887=CARTESIAN_POINT ( 'NONE',  ( -8.890802410117000676, -75.93226843290000261, 8.804145862534999978 ) ) ;
#56888=VERTEX_POINT ( 'NONE', #18563 ) ;
#56889=EDGE_CURVE ( 'NONE', #17310, #56405, #44529, .T. ) ;
#56892=CARTESIAN_POINT ( 'NONE',  ( 12.77562710770000187, -62.06233677629000312, 0.5428386295906000303 ) ) ;
#56893=CARTESIAN_POINT ( 'NONE',  ( 9.560585210696000757, -78.88929468166000447, 8.500609442439998276 ) ) ;
#56894=CARTESIAN_POINT ( 'NONE',  ( -1.667917367010000040, -18.71943307332999851, -12.49306752634999995 ) ) ;
#56899=ORIENTED_EDGE ( 'NONE', *, *, #27046, .T. ) ;
#56903=EDGE_CURVE ( 'NONE', #26175, #3300, #52825, .T. ) ;
#56904=EDGE_LOOP ( 'NONE', ( #18760, #41283, #11212, #20186 ) ) ;
#56907=CARTESIAN_POINT ( 'NONE',  ( -7.601397897754999633, -60.04999999657000131, -10.07627163191000008 ) ) ;
#56909=VERTEX_POINT ( 'NONE', #52712 ) ;
#56911=VERTEX_POINT ( 'NONE', #4972 ) ;
#56912=ORIENTED_EDGE ( 'NONE', *, *, #15348, .F. ) ;
#56915=DIRECTION ( 'NONE',  ( -0.7071067811865475727, 0.000000000000000000, -0.7071067811865475727 ) ) ;
#56918=CARTESIAN_POINT ( 'NONE',  ( 12.54977952612999914, -53.75167110003000204, -0.03756586072996999370 ) ) ;
#56919=VERTEX_POINT ( 'NONE', #9995 ) ;
#56920=CARTESIAN_POINT ( 'NONE',  ( -6.353892679860843273, -78.46935512297507387, 10.19451981771113402 ) ) ;
#56922=CARTESIAN_POINT ( 'NONE',  ( 8.958657468006999025, -53.59887336276000269, 8.950049500612998088 ) ) ;
#56923=CARTESIAN_POINT ( 'NONE',  ( 9.433537730491899254, -16.87202052679777253, -8.532653828096353976 ) ) ;
#56926=CARTESIAN_POINT ( 'NONE',  ( 0.000000000000000000, -72.89999999999999147, 0.000000000000000000 ) ) ;
#56929=CARTESIAN_POINT ( 'NONE',  ( -7.685416442687999172, -76.51934360383999945, -9.616126112745998711 ) ) ;
#56932=CARTESIAN_POINT ( 'NONE',  ( 9.108250977419000805, -61.67811334458999539, -8.478720681770999690 ) ) ;
#56933=CARTESIAN_POINT ( 'NONE',  ( -5.950798862880000151, -78.86331654267000602, 10.72320280238000123 ) ) ;
#56935=CARTESIAN_POINT ( 'NONE',  ( -7.398464061242883361, -60.25160423312483715, -8.140250184784974863 ) ) ;
#56936=DIRECTION ( 'NONE',  ( 0.000000000000000000, 0.000000000000000000, -1.000000000000000000 ) ) ;
#56940=DIRECTION ( 'NONE',  ( 0.000000000000000000, -1.000000000000000000, 0.000000000000000000 ) ) ;
#56941=LINE ( 'NONE', #2645, #24764 ) ;
#56942=CARTESIAN_POINT ( 'NONE',  ( -1.347195692331000005, -2.374444768727999922, 3.292799928894000416 ) ) ;
#56956=CARTESIAN_POINT ( 'NONE',  ( -3.425387549877999760, -0.6331479618548999655, -0.04975834668854000470 ) ) ;
#56959=DIRECTION ( 'NONE',  ( -0.9999548435846228323, 0.000000000000000000, -0.009503199022040218977 ) ) ;
#56966=ADVANCED_FACE ( 'NONE', ( #19359 ), #37647, .F. ) ;
#56967=AXIS2_PLACEMENT_3D ( 'NONE', #15676, #20117, #51419 ) ;
#56975=ORIENTED_EDGE ( 'NONE', *, *, #28938, .F. ) ;
#56979=EDGE_CURVE ( 'NONE', #18217, #57339, #14178, .T. ) ;
#56982=CARTESIAN_POINT ( 'NONE',  ( 1.538071403320016461, -75.93541666666665435, -11.74999999999999822 ) ) ;
#56983=CARTESIAN_POINT ( 'NONE',  ( 12.51393054458000087, -76.81064262049000035, -3.351762257813000190 ) ) ;
#56986=CARTESIAN_POINT ( 'NONE',  ( -8.485281374238999419, -60.74999999967048581, -8.485281374238999419 ) ) ;
#56990=CARTESIAN_POINT ( 'NONE',  ( 9.687280504270265880, -78.09832047880331629, 6.727404250420961240 ) ) ;
#56998=DIRECTION ( 'NONE',  ( -0.7071067811865475727, 0.000000000000000000, -0.7071067811865475727 ) ) ;
#57001=CARTESIAN_POINT ( 'NONE',  ( -1.980584515756000030, -55.53514849873000259, 12.76303204337999908 ) ) ;
#57006=CARTESIAN_POINT ( 'NONE',  ( -12.55433072267391914, -60.18725213688281173, -1.749897784984652427 ) ) ;
#57007=EDGE_LOOP ( 'NONE', ( #18717, #9284, #7764, #30608 ) ) ;
#57009=VECTOR ( 'NONE', #45265, 1000.000000000000000 ) ;
#57019=FACE_OUTER_BOUND ( 'NONE', #4485, .T. ) ;
#57020=CARTESIAN_POINT ( 'NONE',  ( 10.90723107005969084, -75.97980330752400846, 4.369188860919290818 ) ) ;
#57023=CARTESIAN_POINT ( 'NONE',  ( -11.74860111630057524, -78.68560678359739313, 2.073359527469779806 ) ) ;
#57025=EDGE_CURVE ( 'NONE', #5930, #22602, #2522, .T. ) ;
#57026=CARTESIAN_POINT ( 'NONE',  ( 0.000000000000000000, -23.25000000000000000, -12.00000000000000000 ) ) ;
#57027=AXIS2_PLACEMENT_3D ( 'NONE', #16964, #25526, #52978 ) ;
#57030=EDGE_CURVE ( 'NONE', #52919, #43451, #21096, .T. ) ;
#57033=CARTESIAN_POINT ( 'NONE',  ( 10.52693147740000157, -23.42153431750000436, -7.606024891108000396 ) ) ;
#57034=CARTESIAN_POINT ( 'NONE',  ( 0.8898229089127220881, -16.97675468816218114, 12.70296869045103527 ) ) ;
#57036=CARTESIAN_POINT ( 'NONE',  ( 0.000000000000000000, -3.500000000000000000, 0.000000000000000000 ) ) ;
#57037=LINE ( 'NONE', #3022, #39030 ) ;
#57041=CARTESIAN_POINT ( 'NONE',  ( 12.89999999994999769, -2.999999999951000085, 1.886268220167000189E-09 ) ) ;
#57042=EDGE_CURVE ( 'NONE', #15888, #8754, #37749, .T. ) ;
#57045=FACE_OUTER_BOUND ( 'NONE', #4276, .T. ) ;
#57050=DIRECTION ( 'NONE',  ( -1.000000000000000000, 0.000000000000000000, 0.000000000000000000 ) ) ;
#57051=CONICAL_SURFACE ( 'NONE', #44786, 13.94999999994999840, 0.7853981633972997312 ) ;
#57054=ORIENTED_EDGE ( 'NONE', *, *, #6153, .T. ) ;
#57055=CARTESIAN_POINT ( 'NONE',  ( -12.43569863936000175, -53.91799904124000165, -0.4278707626187999713 ) ) ;
#57056=AXIS2_PLACEMENT_3D ( 'NONE', #46411, #19237, #23656 ) ;
#57057=ORIENTED_EDGE ( 'NONE', *, *, #51038, .T. ) ;
#57058=B_SPLINE_CURVE_WITH_KNOTS ( 'NONE', 3,
 ( #42854, #15981, #33971, #18014, #30975, #53434, #49013, #35709, #40143, #36006, #3843, #8559, #31562, #31265, #48442, #49308, #13273, #26550, #3557, #44579, #49611, #16850, #3277, #58155 ),
 .UNSPECIFIED., .F., .F.,
 ( 4, 2, 2, 2, 2, 2, 2, 2, 2, 2, 2, 4 ),
 ( 0.000000000000000000, 0.1249999999999984457, 0.2499999999999968914, 0.3749999999999953371, 0.4374999999999954481, 0.4999999999999955591, 0.6249999999999957812, 0.7499999999999960032, 0.8124999999999968914, 0.8437499999999971134, 0.8749999999999974465, 1.000000000000000000 ),
 .UNSPECIFIED. ) ;
#57059=ORIENTED_EDGE ( 'NONE', *, *, #46369, .T. ) ;
#57062=AXIS2_PLACEMENT_3D ( 'NONE', #53367, #8494, #7919 ) ;
#57064=CIRCLE ( 'NONE', #32512, 12.69999999999999929 ) ;
#57070=EDGE_CURVE ( 'NONE', #38980, #33666, #51886, .T. ) ;
#57071=CARTESIAN_POINT ( 'NONE',  ( -12.54673765600000124, -61.62199238204999574, -0.9174244429635999287 ) ) ;
#57081=CARTESIAN_POINT ( 'NONE',  ( -7.762982794245000484, -17.83910040287999621, -9.991998894192999359 ) ) ;
#57082=CARTESIAN_POINT ( 'NONE',  ( 7.668949790007999923, -56.02870851050000311, 10.21381326472999795 ) ) ;
#57092=CARTESIAN_POINT ( 'NONE',  ( -12.71798269385000069, -18.70221245812999911, 1.931086388578000079 ) ) ;
#57093=CARTESIAN_POINT ( 'NONE',  ( -3.554538774556999847, -2.649302049814999727, -0.8106109833587000768 ) ) ;
#57095=EDGE_CURVE ( 'NONE', #26282, #8334, #47700, .T. ) ;
#57097=CARTESIAN_POINT ( 'NONE',  ( -12.78037507859000144, -54.50670131396999807, 1.812742845509000000 ) ) ;
#57098=CARTESIAN_POINT ( 'NONE',  ( -7.342331066867000544, -55.64999999967000122, 8.190859204290999784 ) ) ;
#57099=CARTESIAN_POINT ( 'NONE',  ( 1.801750019961000149, -60.19007426689000084, 12.59656967656000148 ) ) ;
#57100=CARTESIAN_POINT ( 'NONE',  ( -7.954951288349001004, -55.54999999966999980, -9.722718241315000398 ) ) ;
#57105=EDGE_CURVE ( 'NONE', #4102, #52807, #58250, .T. ) ;
#57106=CARTESIAN_POINT ( 'NONE',  ( 10.39516313037050743, -76.41088147063496194, -5.479998801784073947 ) ) ;
#57112=CARTESIAN_POINT ( 'NONE',  ( -1.636761686205420396, -2.583333333333333037, -2.839805762151339508 ) ) ;
#57115=CARTESIAN_POINT ( 'NONE',  ( 11.02509224276342259, -75.79999999999999716, 4.905407213634159547 ) ) ;
#57117=CARTESIAN_POINT ( 'NONE',  ( 0.000000000000000000, -0.2000000000000000111, -10.20000000000000107 ) ) ;
#57120=VERTEX_POINT ( 'NONE', #41721 ) ;
#57121=CARTESIAN_POINT ( 'NONE',  ( -1.430139897903401236, -0.7500000000000001110, 3.215437163636295725 ) ) ;
#57122=ORIENTED_EDGE ( 'NONE', *, *, #52048, .F. ) ;
#57126=ORIENTED_EDGE ( 'NONE', *, *, #9956, .F. ) ;
#57127=B_SPLINE_CURVE_WITH_KNOTS ( 'NONE', 3,
 ( #52889, #57313, #44607, #12721, #30714, #25726, #30141, #17155, #48465, #30433, #39590, #4161, #53171, #16877, #34857, #22160, #57595, #40167 ),
 .UNSPECIFIED., .F., .F.,
 ( 4, 2, 2, 2, 2, 2, 2, 2, 4 ),
 ( 0.000000000000000000, 0.1249999999999999722, 0.2500000000000000000, 0.3750000000000000000, 0.5000000000000001110, 0.6250000000000001110, 0.7500000000000000000, 0.8750000000000000000, 1.000000000000000000 ),
 .UNSPECIFIED. ) ;
#57130=VECTOR ( 'NONE', #14105, 1000.000000000000000 ) ;
#57132=CARTESIAN_POINT ( 'NONE',  ( -9.003055988996001346, -78.97756055792000041, -8.248189893095000613 ) ) ;
#57133=ORIENTED_EDGE ( 'NONE', *, *, #21768, .F. ) ;
#57135=ORIENTED_EDGE ( 'NONE', *, *, #26142, .T. ) ;
#57136=CARTESIAN_POINT ( 'NONE',  ( 0.000000000000000000, -23.15000000000000213, 12.00000000000000000 ) ) ;
#57137=CARTESIAN_POINT ( 'NONE',  ( -10.98961866300655466, -18.48267221963240914, 0.4810437121599021593 ) ) ;
#57138=AXIS2_PLACEMENT_3D ( 'NONE', #39217, #2926, #4071 ) ;
#57141=CARTESIAN_POINT ( 'NONE',  ( -8.838834764832000701, -23.25000000000000000, 8.838834764832000701 ) ) ;
#57144=CARTESIAN_POINT ( 'NONE',  ( -5.947256583267294339, -79.07291666668990615, 10.29299386049553711 ) ) ;
#57148=FACE_OUTER_BOUND ( 'NONE', #15816, .T. ) ;
#57150=CARTESIAN_POINT ( 'NONE',  ( 8.190859204290999784, -59.94999999967000548, 7.342331066867000544 ) ) ;
#57151=CARTESIAN_POINT ( 'NONE',  ( 2.275600661772546829, -2.913783080248345314, 2.319952847705075705 ) ) ;
#57155=CARTESIAN_POINT ( 'NONE',  ( 3.665025684363000025, -3.510954567059000109, -1.025097465345000236 ) ) ;
#57156=CARTESIAN_POINT ( 'NONE',  ( 10.35747158362999976, -23.31584477285000290, 7.626500902217000721 ) ) ;
#57157=CARTESIAN_POINT ( 'NONE',  ( -7.631889049370999878, -60.02121504819000108, -10.36222434951000082 ) ) ;
#57161=CARTESIAN_POINT ( 'NONE',  ( 12.49997170191999984, -23.19201514549000009, 1.666513530428999967 ) ) ;
#57164=CARTESIAN_POINT ( 'NONE',  ( 11.59740219448999987, -75.80332143684999835, -4.280683990382000204 ) ) ;
#57170=CARTESIAN_POINT ( 'NONE',  ( 12.79972228485999963, -60.59021513420999838, 2.019125729023000027 ) ) ;
#57171=CARTESIAN_POINT ( 'NONE',  ( 9.787591575112999820, -79.28015235882000411, -7.311436768013999554 ) ) ;
#57176=CARTESIAN_POINT ( 'NONE',  ( -12.60354432325999952, -19.24899162885999715, 1.750000000000000000 ) ) ;
#57177=DIRECTION ( 'NONE',  ( 0.7071067811865474617, 0.000000000000000000, -0.7071067811865474617 ) ) ;
#57180=DIRECTION ( 'NONE',  ( 0.9999999999998321343, 0.000000000000000000, 5.794542749929189768E-07 ) ) ;
#57183=CIRCLE ( 'NONE', #31713, 13.79999999999999893 ) ;
#57185=VECTOR ( 'NONE', #49015, 1000.000000000000000 ) ;
#57186=CARTESIAN_POINT ( 'NONE',  ( -8.171144579308439404, -55.45989902438520858, -7.364280830341621176 ) ) ;
#57188=AXIS2_PLACEMENT_3D ( 'NONE', #32598, #1637, #50352 ) ;
#57192=VERTEX_POINT ( 'NONE', #40108 ) ;
#57194=CARTESIAN_POINT ( 'NONE',  ( -1.886823409076000102, -18.23680315638000238, 12.68610076205999881 ) ) ;
#57195=CARTESIAN_POINT ( 'NONE',  ( 1.532229595823858759, -60.92298962908745352, 12.51228690890383177 ) ) ;
#57198=CARTESIAN_POINT ( 'NONE',  ( -3.247771509845949200, -2.590611485816939119, 0.4256070685482727933 ) ) ;
#57200=CARTESIAN_POINT ( 'NONE',  ( -1.307210027570999911, -79.16650217667631750, -12.19386267984000050 ) ) ;
#57202=CARTESIAN_POINT ( 'NONE',  ( 7.961057357800999768, -54.26431744618999886, 9.783210913615000948 ) ) ;
#57205=ADVANCED_FACE ( 'NONE', ( #3030 ), #43473, .F. ) ;
#57206=CARTESIAN_POINT ( 'NONE',  ( 12.76303204298000082, -60.06485150663000638, -1.980584515756000030 ) ) ;
#57208=CARTESIAN_POINT ( 'NONE',  ( 9.369164850722000892, -60.04999999966999980, -7.601397897754999633 ) ) ;
#57209=CARTESIAN_POINT ( 'NONE',  ( -7.758897894424999997, -24.30081253449000300, 10.31443085083000000 ) ) ;
#57210=AXIS2_PLACEMENT_3D ( 'NONE', #41886, #9720, #41302 ) ;
#57213=CARTESIAN_POINT ( 'NONE',  ( -12.66232176275999954, -16.86513311418999805, 0.5079086068997000769 ) ) ;
#57214=DIRECTION ( 'NONE',  ( 0.000000000000000000, 1.000000000000000000, 0.000000000000000000 ) ) ;
#57217=VECTOR ( 'NONE', #13793, 1000.000000000000000 ) ;
#57218=CARTESIAN_POINT ( 'NONE',  ( -3.712316210013999918, -1.805555703421999780, -0.5582186464255000091 ) ) ;
#57220=ADVANCED_FACE ( 'NONE', ( #12171 ), #29013, .F. ) ;
#57221=AXIS2_PLACEMENT_3D ( 'NONE', #56926, #35326, #48086 ) ;
#57227=CARTESIAN_POINT ( 'NONE',  ( 3.385164732404000176, -2.693653522605000017, -1.094590136342000086 ) ) ;
#57229=CARTESIAN_POINT ( 'NONE',  ( 12.90000000000000036, -3.000000000000000000, 0.000000000000000000 ) ) ;
#57230=CARTESIAN_POINT ( 'NONE',  ( -11.79999999999999893, -23.15000000000999947, -0.5999999999999999778 ) ) ;
#57231=CARTESIAN_POINT ( 'NONE',  ( -7.639893379697016762, -18.61284423925064146, 10.11462454831194435 ) ) ;
#57234=ORIENTED_EDGE ( 'NONE', *, *, #31045, .T. ) ;
#57236=B_SPLINE_CURVE_WITH_KNOTS ( 'NONE', 3,
 ( #33648, #42814, #6500, #43384, #47262, #46973 ),
 .UNSPECIFIED., .F., .F.,
 ( 4, 2, 4 ),
 ( 0.000000000000000000, 0.5000000000000000000, 1.000000000000000000 ),
 .UNSPECIFIED. ) ;
#57240=CARTESIAN_POINT ( 'NONE',  ( -8.260136572142998901, -61.74034376533999335, 9.643347111204001010 ) ) ;
#57241=CARTESIAN_POINT ( 'NONE',  ( 3.687443820737999811, -0.8745872626717998699, -0.3192645131365000055 ) ) ;
#57251=ORIENTED_EDGE ( 'NONE', *, *, #27168, .T. ) ;
#57253=CARTESIAN_POINT ( 'NONE',  ( -0.04193593714361701363, -53.78990258635174371, -12.50649570002511979 ) ) ;
#57254=CARTESIAN_POINT ( 'NONE',  ( -1.667936688463999895, -22.76486430425999785, 12.53239398059000109 ) ) ;
#57256=EDGE_CURVE ( 'NONE', #54593, #48994, #32820, .T. ) ;
#57257=CARTESIAN_POINT ( 'NONE',  ( -12.53239398060000021, -56.03513569577999931, 1.667936688463999895 ) ) ;
#57259=CARTESIAN_POINT ( 'NONE',  ( 12.72966282068020227, -55.03110224949036677, -1.931329623869370238 ) ) ;
#57261=AXIS2_PLACEMENT_3D ( 'NONE', #48775, #44926, #39897 ) ;
#57262=ORIENTED_EDGE ( 'NONE', *, *, #10109, .T. ) ;
#57269=CARTESIAN_POINT ( 'NONE',  ( -12.56594317982999875, -55.55000000504000468, 1.750000000000000000 ) ) ;
#57270=AXIS2_PLACEMENT_3D ( 'NONE', #30654, #35368, #25945 ) ;
#57271=CARTESIAN_POINT ( 'NONE',  ( 9.396085398178630754, -75.99791666666666856, -7.220923959705230821 ) ) ;
#57272=CARTESIAN_POINT ( 'NONE',  ( -12.60796396291999955, -78.26141106207001030, -0.9189346901731000328 ) ) ;
#57274=CYLINDRICAL_SURFACE ( 'NONE', #53210, 1.750000000000001332 ) ;
#57275=ADVANCED_FACE ( 'NONE', ( #2455 ), #31139, .F. ) ;
#57276=FACE_OUTER_BOUND ( 'NONE', #52908, .T. ) ;
#57277=DIRECTION ( 'NONE',  ( 0.000000000000000000, -1.000000000000000000, 0.000000000000000000 ) ) ;
#57279=VERTEX_POINT ( 'NONE', #25165 ) ;
#57285=CARTESIAN_POINT ( 'NONE',  ( -7.678657038162065795, -60.59377623463994667, -10.03844138482057247 ) ) ;
#57286=CARTESIAN_POINT ( 'NONE',  ( 12.60552511010000032, -23.28917723430000208, 1.799501877793999949 ) ) ;
#57288=EDGE_CURVE ( 'NONE', #12596, #15875, #43189, .T. ) ;
#57296=ADVANCED_FACE ( 'NONE', ( #16320 ), #56373, .F. ) ;
#57303=CARTESIAN_POINT ( 'NONE',  ( -12.70299804978423097, -16.97411689985228378, 0.8844418155559133909 ) ) ;
#57307=DIRECTION ( 'NONE',  ( 0.000000000000000000, 1.000000000000000000, 0.000000000000000000 ) ) ;
#57308=LINE ( 'NONE', #6850, #20582 ) ;
#57309=CARTESIAN_POINT ( 'NONE',  ( 10.60049343523006016, -75.98544560680211646, 5.111788561552529586 ) ) ;
#57311=EDGE_LOOP ( 'NONE', ( #7653, #29161, #50682, #22037, #50748 ) ) ;
#57312=CARTESIAN_POINT ( 'NONE',  ( -1.624989163556999772E-14, -74.69999999881999031, 0.000000000000000000 ) ) ;
#57313=CARTESIAN_POINT ( 'NONE',  ( 3.248050210770150326, -2.340893247460261062, -0.4258979702238827048 ) ) ;
#57319=CARTESIAN_POINT ( 'NONE',  ( -0.8804656547847903303, -16.97196605292977623, 12.70299681151712612 ) ) ;
#57322=CARTESIAN_POINT ( 'NONE',  ( -10.42531125072000009, -55.53514854654000032, -7.624341767124000135 ) ) ;
#57329=DIRECTION ( 'NONE',  ( -0.9999999999999998890, -1.433670265775999799E-08, 0.000000000000000000 ) ) ;
#57334=ORIENTED_EDGE ( 'NONE', *, *, #29794, .F. ) ;
#57336=CARTESIAN_POINT ( 'NONE',  ( 1.799475295154000065, -21.75083378359999742, 12.69619287811000063 ) ) ;
#57338=ORIENTED_EDGE ( 'NONE', *, *, #20365, .F. ) ;
#57339=VERTEX_POINT ( 'NONE', #5275 ) ;
#57341=ORIENTED_EDGE ( 'NONE', *, *, #28961, .F. ) ;
#57349=EDGE_CURVE ( 'NONE', #20811, #49641, #16634, .T. ) ;
#57353=EDGE_CURVE ( 'NONE', #13623, #29156, #34980, .T. ) ;
#57354=ORIENTED_EDGE ( 'NONE', *, *, #22297, .T. ) ;
#57356=CARTESIAN_POINT ( 'NONE',  ( 0.000000000000000000, -18.75000000000000000, -12.00000000000000000 ) ) ;
#57358=CARTESIAN_POINT ( 'NONE',  ( -12.66316452100000056, -61.97866137636000161, 0.04044945982128999445 ) ) ;
#57360=CARTESIAN_POINT ( 'NONE',  ( 7.654537165467999671, -18.71943464842000182, 10.01332852689000141 ) ) ;
#57363=CARTESIAN_POINT ( 'NONE',  ( 9.841113773926924324, -53.96371975908724750, -8.121706172282767255 ) ) ;
#57367=ADVANCED_FACE ( 'NONE', ( #54864 ), #14411, .F. ) ;
#57368=CARTESIAN_POINT ( 'NONE',  ( -9.571781413763634561, -76.65043581209883428, 6.814946930798515545 ) ) ;
#57371=CARTESIAN_POINT ( 'NONE',  ( -7.606021555054999439, -55.37841460039999930, 10.52692944503000128 ) ) ;
#57373=CARTESIAN_POINT ( 'NONE',  ( -10.30768118225000052, -18.25239703915999812, -7.634415485503000198 ) ) ;
#57375=CARTESIAN_POINT ( 'NONE',  ( -0.005928781627584999749, -16.79886949736999924, -12.66336824419000173 ) ) ;
#57376=DIRECTION ( 'NONE',  ( 0.000000000000000000, 1.000000000000000000, 0.000000000000000000 ) ) ;
#57378=DIRECTION ( 'NONE',  ( 1.000000000000000000, 0.000000000000000000, 0.000000000000000000 ) ) ;
#57380=CARTESIAN_POINT ( 'NONE',  ( 1.588866964187630071, -3.499999999999999556, 2.959281665799033512 ) ) ;
#57382=ORIENTED_EDGE ( 'NONE', *, *, #53892, .T. ) ;
#57383=LINE ( 'NONE', #16943, #46169 ) ;
#57384=DIRECTION ( 'NONE',  ( 0.000000000000000000, 1.000000000000000000, 0.000000000000000000 ) ) ;
#57386=CARTESIAN_POINT ( 'NONE',  ( 7.624341766647000362, -18.73514853758999976, -10.42531125024999916 ) ) ;
#57387=CARTESIAN_POINT ( 'NONE',  ( 2.162366405920999490, -2.955934344712999984, 2.935303670011000232 ) ) ;
#57389=CARTESIAN_POINT ( 'NONE',  ( -12.72397198031000087, -55.57854962903999763, 1.930909771329999858 ) ) ;
#57391=CARTESIAN_POINT ( 'NONE',  ( 0.000000000000000000, -55.54999999966999980, -12.00000000000000000 ) ) ;
#57394=VECTOR ( 'NONE', #12287, 1000.000000000000114 ) ;
#57396=B_SPLINE_CURVE_WITH_KNOTS ( 'NONE', 3,
 ( #27936, #23234, #18234, #14079, #37386, #31480, #45097, #251, #31780, #49823, #19683, #20838, #37683, #33241, #32947, #29682, #55699, #29397 ),
 .UNSPECIFIED., .F., .F.,
 ( 4, 2, 2, 2, 2, 2, 2, 2, 4 ),
 ( 0.000000000000000000, 0.1250000000000000833, 0.2500000000000001665, 0.3750000000000001110, 0.5000000000000001110, 0.6250000000000001110, 0.7500000000000000000, 0.8750000000000000000, 1.000000000000000000 ),
 .UNSPECIFIED. ) ;
#57398=CARTESIAN_POINT ( 'NONE',  ( 10.99484708662753185, -76.42110442038233487, -4.160114065378057724 ) ) ;
#57404=CARTESIAN_POINT ( 'NONE',  ( -2.772200916640183976, -0.7825520741520030077, -2.131510823956923151 ) ) ;
#57406=EDGE_CURVE ( 'NONE', #37071, #4000, #40654, .T. ) ;
#57407=DIRECTION ( 'NONE',  ( 1.000000000000000000, 0.000000000000000000, 0.000000000000000000 ) ) ;
#57409=AXIS2_PLACEMENT_3D ( 'NONE', #57356, #39055, #4206 ) ;
#57414=EDGE_LOOP ( 'NONE', ( #43268, #7606, #22201, #48391 ) ) ;
#57415=LINE ( 'NONE', #29949, #506 ) ;
#57416=ORIENTED_EDGE ( 'NONE', *, *, #34032, .F. ) ;
#57417=ORIENTED_EDGE ( 'NONE', *, *, #4006, .F. ) ;
#57418=CARTESIAN_POINT ( 'NONE',  ( 1.997276839918466829, -1.322916666666666963, 2.598917237794090784 ) ) ;
#57419=CARTESIAN_POINT ( 'NONE',  ( 11.75000000000000178, -77.53958333333331154, -1.538071403319980268 ) ) ;
#57423=CARTESIAN_POINT ( 'NONE',  ( 11.12418552951999828, -78.71975279073001275, -5.383704713749000170 ) ) ;
#57424=ORIENTED_EDGE ( 'NONE', *, *, #43089, .T. ) ;
#57425=CARTESIAN_POINT ( 'NONE',  ( -10.53562597590999950, -60.00558297591999946, 7.620013358898000355 ) ) ;
#57428=LINE ( 'NONE', #53000, #41427 ) ;
#57431=CARTESIAN_POINT ( 'NONE',  ( 8.838834764832000701, -23.25000000000000000, -8.838834764832000701 ) ) ;
#57432=CIRCLE ( 'NONE', #32929, 12.50000000000000000 ) ;
#57433=DIRECTION ( 'NONE',  ( 0.000000000000000000, -1.000000000000000000, 0.000000000000000000 ) ) ;
#57436=CARTESIAN_POINT ( 'NONE',  ( -12.60246356036999948, -77.25062674423000431, -0.9915196953554998860 ) ) ;
#57442=CARTESIAN_POINT ( 'NONE',  ( -1.245586717227264106, -3.007515495460388433, 3.001037710528552616 ) ) ;
#57445=FACE_OUTER_BOUND ( 'NONE', #18578, .T. ) ;
#57447=CARTESIAN_POINT ( 'NONE',  ( 1.068619641472000170, -1.895647048966000003, -3.652926003266999899 ) ) ;
#57449=CARTESIAN_POINT ( 'NONE',  ( -7.658894224196000522, -60.00939395830999956, -10.01676912202999858 ) ) ;
#57455=LINE ( 'NONE', #16156, #41518 ) ;
#57456=CARTESIAN_POINT ( 'NONE',  ( -4.097539515550000289, -75.98334464165999691, 11.66336447688000000 ) ) ;
#57457=ORIENTED_EDGE ( 'NONE', *, *, #7484, .T. ) ;
#57459=DIRECTION ( 'NONE',  ( 0.000000000000000000, -1.000000000000000000, 0.000000000000000000 ) ) ;
#57460=CARTESIAN_POINT ( 'NONE',  ( 12.43422056534000042, -61.23655741401000085, 1.197404442626999854 ) ) ;
#57461=CARTESIAN_POINT ( 'NONE',  ( -1.799502287691000069, -23.30716680861999990, -12.60413670420000010 ) ) ;
#57471=ADVANCED_FACE ( 'NONE', ( #7020 ), #26699, .F. ) ;
#57473=CARTESIAN_POINT ( 'NONE',  ( 12.58335110162999904, -58.54888345776999614, 1.667961430005999945 ) ) ;
#57475=ORIENTED_EDGE ( 'NONE', *, *, #34364, .T. ) ;
#57477=EDGE_LOOP ( 'NONE', ( #6079, #42912, #58004, #699 ) ) ;
#57478=ORIENTED_EDGE ( 'NONE', *, *, #9886, .T. ) ;
#57479=AXIS2_PLACEMENT_3D ( 'NONE', #35161, #12742, #8907 ) ;
#57480=CARTESIAN_POINT ( 'NONE',  ( -3.047098712557896771, -78.09418507123076836, 11.37766269708934708 ) ) ;
#57481=DIRECTION ( 'NONE',  ( 0.7071067812094172789, -2.924115120139070516E-07, 0.7071067811636172484 ) ) ;
#57484=EDGE_CURVE ( 'NONE', #30606, #1677, #42517, .T. ) ;
#57487=CARTESIAN_POINT ( 'NONE',  ( 7.620037552694999938, -55.59433113521999559, 10.53559761426999764 ) ) ;
#57490=CARTESIAN_POINT ( 'NONE',  ( 12.70253258978874733, -61.77063167637336960, -0.9890392130593611553 ) ) ;
#57492=EDGE_CURVE ( 'NONE', #19229, #44346, #46249, .T. ) ;
#57494=AXIS2_PLACEMENT_3D ( 'NONE', #9085, #39496, #17062 ) ;
#57495=CARTESIAN_POINT ( 'NONE',  ( -10.36292431357999888, -23.20096201633999655, 7.633479737313000335 ) ) ;
#57496=EDGE_CURVE ( 'NONE', #16250, #19958, #46327, .T. ) ;
#57500=CARTESIAN_POINT ( 'NONE',  ( 12.76303204294999993, -23.26485150694999859, -1.980584515756000030 ) ) ;
#57503=CARTESIAN_POINT ( 'NONE',  ( 12.50412785605847432, -24.51985834634450256, -1.235051469881349506 ) ) ;
#57508=CARTESIAN_POINT ( 'NONE',  ( -13.63885489310999510, -19.21421830981000056, -7.254376133916000668 ) ) ;
#57509=CARTESIAN_POINT ( 'NONE',  ( 0.2030686677330999779, -3.598078325257000110, -3.551685225877000196 ) ) ;
#57513=EDGE_CURVE ( 'NONE', #5930, #10595, #17318, .T. ) ;
#57514=CARTESIAN_POINT ( 'NONE',  ( 1.883721702039359291, -75.80000000000002558, 11.98327435467166602 ) ) ;
#57518=ORIENTED_EDGE ( 'NONE', *, *, #39730, .F. ) ;
#57524=CARTESIAN_POINT ( 'NONE',  ( 3.428456835174999995, -1.314283069271000137, 0.8759089407426000617 ) ) ;
#57526=CARTESIAN_POINT ( 'NONE',  ( 12.77651065749000026, -25.30896598096000005, 0.04308629978603999849 ) ) ;
#57527=CARTESIAN_POINT ( 'NONE',  ( -1.799502287743000029, -60.10716934574000447, 12.60413652834999887 ) ) ;
#57529=EDGE_CURVE ( 'NONE', #22028, #38753, #36390, .T. ) ;
#57532=CARTESIAN_POINT ( 'NONE',  ( 7.342331066867000544, -55.64999999967000122, 8.190859204290999784 ) ) ;
#57533=EDGE_CURVE ( 'NONE', #28878, #48346, #18107, .T. ) ;
#57536=ORIENTED_EDGE ( 'NONE', *, *, #46270, .F. ) ;
#57537=VECTOR ( 'NONE', #47987, 999.9999999999998863 ) ;
#57538=DIRECTION ( 'NONE',  ( -1.000000000000000000, 0.000000000000000000, 0.000000000000000000 ) ) ;
#57539=CARTESIAN_POINT ( 'NONE',  ( 9.546819346760999636, -61.48527546573999558, -8.130850182902999990 ) ) ;
#57540=CARTESIAN_POINT ( 'NONE',  ( -1.750000000001000089, -55.55000001292999912, -12.56594318049000059 ) ) ;
#57542=CARTESIAN_POINT ( 'NONE',  ( -7.974020021219000220, -54.16898233660000272, -9.929669236765001017 ) ) ;
#57545=EDGE_LOOP ( 'NONE', ( #56842, #6009, #40948, #7894, #31533, #35023 ) ) ;
#57546=ORIENTED_EDGE ( 'NONE', *, *, #37431, .F. ) ;
#57549=ORIENTED_EDGE ( 'NONE', *, *, #25689, .T. ) ;
#57551=CIRCLE ( 'NONE', #17030, 1.750000000000000000 ) ;
#57554=CARTESIAN_POINT ( 'NONE',  ( -3.291354266399999950, -77.06423739310000087, 12.36836470155000001 ) ) ;
#57556=CARTESIAN_POINT ( 'NONE',  ( -10.39315812627616431, -78.40567703563392854, 6.510797611460747092 ) ) ;
#57565=DIRECTION ( 'NONE',  ( -1.000000000000000000, 1.534883903844000000E-11, 4.134220892123999815E-14 ) ) ;
#57566=CARTESIAN_POINT ( 'NONE',  ( 1.668607604626967778, -60.59381631189521755, -12.52787843855117345 ) ) ;
#57567=CARTESIAN_POINT ( 'NONE',  ( 3.328509078748080441, -3.072971510259623784, -1.143234280529020763 ) ) ;
#57568=CARTESIAN_POINT ( 'NONE',  ( 12.87022657272000004, -22.78485473281999774, 2.062597299672999540 ) ) ;
#57569=CARTESIAN_POINT ( 'NONE',  ( 7.947168433127743015, -78.27084849470611516, 9.085795500190322116 ) ) ;
#57570=CARTESIAN_POINT ( 'NONE',  ( -12.60552522436000089, -18.71082434677000350, -1.799501877760999902 ) ) ;
#57571=DIRECTION ( 'NONE',  ( 0.7071067811865475727, 0.000000000000000000, 0.7071067811865475727 ) ) ;
#57573=CARTESIAN_POINT ( 'NONE',  ( 10.18589234708000113, -18.71082434677000350, -7.641012386038000592 ) ) ;
#57577=AXIS2_PLACEMENT_3D ( 'NONE', #28862, #56330, #15882 ) ;
#57584=CARTESIAN_POINT ( 'NONE',  ( -12.71005124797314778, -17.70500926713873469, 1.687536500553408647 ) ) ;
#57589=CARTESIAN_POINT ( 'NONE',  ( -1.798368564629000188, -55.60363242921000193, -12.61278090839000043 ) ) ;
#57591=CARTESIAN_POINT ( 'NONE',  ( 11.55626480159407876, -75.96425890079613907, 2.125201638845596097 ) ) ;
#57593=ORIENTED_EDGE ( 'NONE', *, *, #54501, .T. ) ;
#57595=CARTESIAN_POINT ( 'NONE',  ( -3.249633467300476308, -2.111888578168985120, -0.4260072675962560673 ) ) ;
#57599=CARTESIAN_POINT ( 'NONE',  ( 0.5668640726082777581, -17.08340305019257244, -12.50470739226994965 ) ) ;
#57601=DIRECTION ( 'NONE',  ( -0.3090169943750105674, 0.000000000000000000, 0.9510565162951329921 ) ) ;
#57602=CARTESIAN_POINT ( 'NONE',  ( 0.000000000000000000, -72.39999999999999147, 0.000000000000000000 ) ) ;
#57604=AXIS2_PLACEMENT_3D ( 'NONE', #8472, #9657, #5227 ) ;
#57607=CARTESIAN_POINT ( 'NONE',  ( 7.376264119752973691, -75.80000000000003979, -9.324595548898168218 ) ) ;
#57611=CARTESIAN_POINT ( 'NONE',  ( 8.838834764832000701, -18.75000000000000000, -8.838834764832000701 ) ) ;
#57614=ADVANCED_FACE ( 'NONE', ( #22921 ), #17615, .F. ) ;
#57616=DIRECTION ( 'NONE',  ( 0.000000000000000000, -1.000000000000000000, 0.000000000000000000 ) ) ;
#57618=EDGE_CURVE ( 'NONE', #55907, #47968, #51043, .T. ) ;
#57619=DIRECTION ( 'NONE',  ( -1.000000000000000000, 0.000000000000000000, 0.000000000000000000 ) ) ;
#57620=ORIENTED_EDGE ( 'NONE', *, *, #8442, .T. ) ;
#57621=VERTEX_POINT ( 'NONE', #49804 ) ;
#57628=ORIENTED_EDGE ( 'NONE', *, *, #11911, .T. ) ;
#57635=VERTEX_POINT ( 'NONE', #27338 ) ;
#57637=AXIS2_PLACEMENT_3D ( 'NONE', #34246, #51714, #6529 ) ;
#57640=AXIS2_PLACEMENT_3D ( 'NONE', #44698, #21952, #13386 ) ;
#57642=CARTESIAN_POINT ( 'NONE',  ( 7.718368845809999712, -20.25199022618999933, 10.07722254369999959 ) ) ;
#57646=CARTESIAN_POINT ( 'NONE',  ( 12.54980553589999914, -16.95222688865000293, 0.05649961219511000221 ) ) ;
#57648=DIRECTION ( 'NONE',  ( -1.000000000000000000, 6.386283326366000088E-09, 1.411454291414999872E-10 ) ) ;
#57649=EDGE_LOOP ( 'NONE', ( #5099, #57262, #48570, #51701 ) ) ;
#57651=CARTESIAN_POINT ( 'NONE',  ( -7.631889106307999882, -55.57878585374000124, 10.36222439673000117 ) ) ;
#57653=CARTESIAN_POINT ( 'NONE',  ( -8.596775676242998543, -16.86467110163999905, -9.310147894694001280 ) ) ;
#57654=CARTESIAN_POINT ( 'NONE',  ( 7.718346056099999686, -58.54888345776999614, 10.07719973192999952 ) ) ;
#57655=CARTESIAN_POINT ( 'NONE',  ( -1.295048492660999973, -17.47106480873999956, -12.54716442236999896 ) ) ;
#57656=CARTESIAN_POINT ( 'NONE',  ( 12.50000000000000000, -55.54999999966999980, 1.250000000000000000 ) ) ;
#57660=CARTESIAN_POINT ( 'NONE',  ( 3.250000000000000444, -1.760416666666666963, 0.4254240051736247197 ) ) ;
#57662=ORIENTED_EDGE ( 'NONE', *, *, #54019, .F. ) ;
#57663=DIRECTION ( 'NONE',  ( -0.6489586447440029993, 0.04890182322787019892, 0.7592504784964030362 ) ) ;
#57664=CARTESIAN_POINT ( 'NONE',  ( 0.4802748259362999983, -53.79473092685000069, 12.54896097830000024 ) ) ;
#57665=CARTESIAN_POINT ( 'NONE',  ( -12.49168433580000048, -18.70150862776000267, 1.667916687244999974 ) ) ;
#57666=CARTESIAN_POINT ( 'NONE',  ( 3.641686272398999780, -3.385219557569000060, 0.1721552302819999991 ) ) ;
#57667=STYLED_ITEM ( 'NONE', ( #14423 ), #51784 ) ;
#57670=LINE ( 'NONE', #25799, #20399 ) ;
#57671=CARTESIAN_POINT ( 'NONE',  ( -1.669724228651999987, -60.16897676502000536, 12.48434610070000161 ) ) ;
#57676=CARTESIAN_POINT ( 'NONE',  ( 5.913553462076830414, -77.11893306552236993, -10.46716446491110553 ) ) ;
#57680=DIRECTION ( 'NONE',  ( 0.7071067811865474617, 3.445410891336226740E-11, -0.7071067811865474617 ) ) ;
#57682=TOROIDAL_SURFACE ( 'NONE', #9655, 1.250000000000000000, 0.5000000000000000000 ) ;
#57683=CARTESIAN_POINT ( 'NONE',  ( 8.838834764832000701, -18.75000000000000000, -8.838834764832000701 ) ) ;
#57686=CARTESIAN_POINT ( 'NONE',  ( -9.848035041027015879, -17.17131634292993070, -8.114786739979949814 ) ) ;
#57687=VECTOR ( 'NONE', #18791, 1000.000000000000000 ) ;
#57693=LINE ( 'NONE', #15597, #6369 ) ;
#57695=CARTESIAN_POINT ( 'NONE',  ( 0.2584144827583641502, -25.22845396923335670, 12.70558781487846645 ) ) ;
#57697=CARTESIAN_POINT ( 'NONE',  ( 1.750000000001000089, -55.55000001292999912, 12.56594318049000059 ) ) ;
#57699=CARTESIAN_POINT ( 'NONE',  ( 2.879448115664242636, -3.500000000000000000, -1.991622112753421714 ) ) ;
#57703=CARTESIAN_POINT ( 'NONE',  ( -0.4701041210472999832, -25.00796934423999929, -12.54901038416000070 ) ) ;
#57706=ORIENTED_EDGE ( 'NONE', *, *, #47501, .F. ) ;
#57707=DIRECTION ( 'NONE',  ( -1.000000000000000000, 0.000000000000000000, -1.158066155992000204E-14 ) ) ;
#57708=CARTESIAN_POINT ( 'NONE',  ( -4.781706919269999467, -78.32610428151998860, 11.04302977649000006 ) ) ;
#57709=ORIENTED_EDGE ( 'NONE', *, *, #35949, .T. ) ;
#57711=EDGE_CURVE ( 'NONE', #53636, #47936, #48219, .T. ) ;
#57716=CARTESIAN_POINT ( 'NONE',  ( 11.95031029473000039, -77.78939249822001045, 5.399609419473999417 ) ) ;
#57723=CARTESIAN_POINT ( 'NONE',  ( 12.56594317823000040, -18.74999998606000062, 1.750000000000000000 ) ) ;
#57724=CARTESIAN_POINT ( 'NONE',  ( -1.245573248748376605, -3.007515109725281910, 3.001042606595181628 ) ) ;
#57726=CARTESIAN_POINT ( 'NONE',  ( -14.00000000000000000, -32.88214388149999934, 0.000000000000000000 ) ) ;
#57729=CARTESIAN_POINT ( 'NONE',  ( -2.422546195149999804, -2.177904343863999781, 2.935532677474999907 ) ) ;
#57733=CARTESIAN_POINT ( 'NONE',  ( -11.79999999988000070, -18.85000000520999919, -0.5999999998848000171 ) ) ;
#57736=B_SPLINE_CURVE_WITH_KNOTS ( 'NONE', 3,
 ( #35025, #48639, #12325, #27051, #31175, #31472, #4640, #4035, #49515, #40652, #8765, #243, #30312, #26184, #22041, #48353, #12889, #7893, #49216 ),
 .UNSPECIFIED., .F., .F.,
 ( 4, 1, 1, 1, 1, 1, 1, 1, 1, 1, 1, 1, 1, 1, 1, 1, 4 ),
 ( 0.000000000000000000, 0.04500688274078824824, 0.1100060414497904537, 0.1750052001587747708, 0.2400043588678306694, 0.3050035175767074613, 0.3700026762857634433, 0.4350018349948194252, 0.5000009937036962171, 0.5650001524127522545, 0.6299993111216289909, 0.6949984698306849173, 0.7599976285397409548, 0.8249967872486176912, 0.8899959459576736176, 0.9549951046667297661, 1.000000000000000000 ),
 .UNSPECIFIED. ) ;
#57737=CARTESIAN_POINT ( 'NONE',  ( 7.411516475408999050, -77.22522017305000475, -10.69619859711000132 ) ) ;
#57738=CONICAL_SURFACE ( 'NONE', #44550, 13.89999999994999946, 0.7853981633972997312 ) ;
#57740=CARTESIAN_POINT ( 'NONE',  ( 5.038785450664000187, -76.65236125213000662, -11.45299339640000014 ) ) ;
#57741=ORIENTED_EDGE ( 'NONE', *, *, #22266, .F. ) ;
#57742=TOROIDAL_SURFACE ( 'NONE', #29461, 1.250000000000000000, 0.5000000000000000000 ) ;
#57744=EDGE_CURVE ( 'NONE', #11731, #45320, #2935, .T. ) ;
#57745=CARTESIAN_POINT ( 'NONE',  ( 0.000000000000000000, -18.84999999999999787, 12.00000000000000000 ) ) ;
#57747=CARTESIAN_POINT ( 'NONE',  ( 12.44210192982000152, -60.88432059783999506, 1.464837683472000052 ) ) ;
#57748=CARTESIAN_POINT ( 'NONE',  ( -1.799501877760999902, -23.28917565320000094, -12.60552522436000089 ) ) ;
#57753=EDGE_LOOP ( 'NONE', ( #3268, #44648, #53286, #8706, #809 ) ) ;
#57757=ORIENTED_EDGE ( 'NONE', *, *, #11136, .F. ) ;
#57758=EDGE_LOOP ( 'NONE', ( #32700, #30815, #39829, #41880 ) ) ;
#57760=DIRECTION ( 'NONE',  ( 0.000000000000000000, 1.000000000000000000, 0.000000000000000000 ) ) ;
#57765=CIRCLE ( 'NONE', #43621, 12.50000000000000000 ) ;
#57766=VERTEX_POINT ( 'NONE', #49506 ) ;
#57767=ORIENTED_EDGE ( 'NONE', *, *, #6153, .F. ) ;
#57768=AXIS2_PLACEMENT_3D ( 'NONE', #25917, #48097, #39204 ) ;
#57770=FACE_OUTER_BOUND ( 'NONE', #58299, .T. ) ;
#57771=B_SPLINE_SURFACE_WITH_KNOTS ( 'NONE', 3, 3, ( 
 ( #24890, #3041, #33737, #52627 ),
 ( #47932, #20469, #11324, #2749 ),
 ( #29302, #12182, #38463, #6881 ),
 ( #56479, #39040, #30167, #48216 ),
 ( #7748, #56768, #34310, #52343 ),
 ( #11897, #45521, #13914, #31316 ),
 ( #35163, #49360, #57911, #53485 ),
 ( #49950, #54079, #54375, #27479 ),
 ( #31907, #5067, #49655, #9495 ),
 ( #8611, #4484, #23063, #13026 ),
 ( #31615, #35756, #3887, #40491 ) ),
 .UNSPECIFIED., .F., .F., .F.,
 ( 4, 1, 1, 1, 1, 1, 1, 1, 4 ),
 ( 4, 4 ),
 ( -0.02001474922154999891, 0.000000000000000000, 0.1666666666667000196, 0.3333333333333000081, 0.5000000000000000000, 0.6666666666667000474, 0.8333333333333000637, 1.000000000000000000, 1.020283381528000133 ),
 ( -0.3582002740325999635, 1.358862457854000061 ),
 .UNSPECIFIED. ) ;
#57772=EDGE_LOOP ( 'NONE', ( #32458, #4780, #18853, #31924 ) ) ;
#57774=VERTEX_POINT ( 'NONE', #54224 ) ;
#57777=CIRCLE ( 'NONE', #37050, 1.749999999999997558 ) ;
#57778=CARTESIAN_POINT ( 'NONE',  ( 7.765024210398999926, -54.70905971351000119, 9.830784063398999351 ) ) ;
#57779=DIRECTION ( 'NONE',  ( -0.7071067811865475727, 0.000000000000000000, 0.7071067811865475727 ) ) ;
#57783=CARTESIAN_POINT ( 'NONE',  ( 7.682331425181999407, -56.03513569577999931, -10.04115011118999945 ) ) ;
#57785=CARTESIAN_POINT ( 'NONE',  ( -9.038948602518001252, -25.33262223864999640, 9.029786144013998594 ) ) ;
#57788=EDGE_CURVE ( 'NONE', #3286, #29384, #45669, .T. ) ;
#57794=CARTESIAN_POINT ( 'NONE',  ( -3.682737394452999968, -1.757324315393999914, 1.849092470328999926 ) ) ;
#57797=CARTESIAN_POINT ( 'NONE',  ( 12.77649794763000024, -62.10831393445000259, 0.06464137375187999079 ) ) ;
#57803=DIRECTION ( 'NONE',  ( -0.9999999923520045408, 0.000000000000000000, -0.0001236769620547006605 ) ) ;
#57808=CARTESIAN_POINT ( 'NONE',  ( -10.53003223724000037, -18.67547470641000018, -7.612971414716000140 ) ) ;
#57809=VECTOR ( 'NONE', #58386, 1000.000000000000000 ) ;
#57812=EDGE_CURVE ( 'NONE', #40525, #30548, #49121, .T. ) ;
#57814=CARTESIAN_POINT ( 'NONE',  ( -10.18127202940000053, -60.18645218919000683, 7.633406483317000557 ) ) ;
#57815=CARTESIAN_POINT ( 'NONE',  ( -3.246123984833999998, -1.511824315393999862, 1.406516975900000022 ) ) ;
#57817=CARTESIAN_POINT ( 'NONE',  ( 10.12290050255000118, -60.04999997790999799, -7.648026768390999486 ) ) ;
#57818=CARTESIAN_POINT ( 'NONE',  ( -2.062597265787999845, -56.01538333533000014, 12.87024489158000051 ) ) ;
#57819=ORIENTED_EDGE ( 'NONE', *, *, #46462, .F. ) ;
#57820=CONICAL_SURFACE ( 'NONE', #25761, 13.94999999997000018, 0.7853981633972997312 ) ;
#57821=CARTESIAN_POINT ( 'NONE',  ( 9.369164850722000892, -18.75000000000000000, 7.601397897754999633 ) ) ;
#57822=CARTESIAN_POINT ( 'NONE',  ( 8.441176281578332663, -24.91652561799148913, -9.243148034841571103 ) ) ;
#57823=CARTESIAN_POINT ( 'NONE',  ( -12.50239399164999909, -17.31640749886000208, 1.003653729363000124 ) ) ;
#57825=CARTESIAN_POINT ( 'NONE',  ( -10.24998526315000014, -58.55083378327000077, -7.705142895592000052 ) ) ;
#57827=EDGE_CURVE ( 'NONE', #1239, #29230, #55431, .T. ) ;
#57829=FACE_OUTER_BOUND ( 'NONE', #52481, .T. ) ;
#57830=CARTESIAN_POINT ( 'NONE',  ( -9.397034021637606926, -77.75095410432449228, -7.223315580355283316 ) ) ;
#57831=CARTESIAN_POINT ( 'NONE',  ( -1.733997378016417734, -55.27616783188626925, -12.54437956609219640 ) ) ;
#57832=ADVANCED_FACE ( 'NONE', ( #19960 ), #51960, .F. ) ;
#57833=ORIENTED_EDGE ( 'NONE', *, *, #57788, .F. ) ;
#57834=B_SPLINE_CURVE_WITH_KNOTS ( 'NONE', 3,
 ( #9699, #45433, #4975, #22390, #26806, #5267, #9116, #40401, #23276, #4390, #50445, #49569, #58112, #13825, #49865, #27102, #17675, #18851 ),
 .UNSPECIFIED., .F., .F.,
 ( 4, 2, 2, 2, 2, 2, 2, 2, 4 ),
 ( 0.000000000000000000, 0.1250000000000000000, 0.2500000000000000000, 0.3750000000000000000, 0.5000000000000000000, 0.6250000000000000000, 0.7500000000000000000, 0.8750000000000000000, 1.000000000000000000 ),
 .UNSPECIFIED. ) ;
#57835=CARTESIAN_POINT ( 'NONE',  ( -8.798041828522000785, -53.86186490677999927, -8.790609562984000647 ) ) ;
#57840=DIRECTION ( 'NONE',  ( 0.000000000000000000, -1.000000000000000000, 0.000000000000000000 ) ) ;
#57846=CARTESIAN_POINT ( 'NONE',  ( -13.07887593023000150, -78.00016851287999486, -0.9532572298037998992 ) ) ;
#57848=CARTESIAN_POINT ( 'NONE',  ( 0.000000000000000000, -15.69705297114000331, 12.53545825868000207 ) ) ;
#57851=AXIS2_PLACEMENT_3D ( 'NONE', #20472, #11900, #34313 ) ;
#57854=CARTESIAN_POINT ( 'NONE',  ( 9.848035041034458814, -17.17131634295486720, 8.114786739975425434 ) ) ;
#57855=ORIENTED_EDGE ( 'NONE', *, *, #25244, .T. ) ;
#57857=CARTESIAN_POINT ( 'NONE',  ( 12.17088485526999975, -75.77930627215999948, 1.845041276493999849 ) ) ;
#57862=CARTESIAN_POINT ( 'NONE',  ( 1.711446453831659831, -3.183809200564340802, 3.074675725082612221 ) ) ;
#57864=CARTESIAN_POINT ( 'NONE',  ( -12.69619287815999975, -20.24916621771999914, -1.799475295154000065 ) ) ;
#57865=CARTESIAN_POINT ( 'NONE',  ( -8.385799987731649807, -61.68809827200743712, -9.298537617325708382 ) ) ;
#57869=CARTESIAN_POINT ( 'NONE',  ( 10.04116292118000153, -19.23537109840999904, -7.682344222590000271 ) ) ;
#57872=ORIENTED_EDGE ( 'NONE', *, *, #1402, .F. ) ;
#57882=CARTESIAN_POINT ( 'NONE',  ( 0.5045596072233999863, -53.66471086928999767, -12.66210649705999991 ) ) ;
#57883=CARTESIAN_POINT ( 'NONE',  ( 10.85853326491538162, -75.98070578024562849, 4.488588818805364866 ) ) ;
#57885=ORIENTED_EDGE ( 'NONE', *, *, #11660, .F. ) ;
#57887=CARTESIAN_POINT ( 'NONE',  ( 10.42531125070999920, -60.06485145371000556, -7.624341767111000756 ) ) ;
#57888=CARTESIAN_POINT ( 'NONE',  ( -3.643839868884810151, -78.79973254024228879, -11.20904019331054258 ) ) ;
#57889=TOROIDAL_SURFACE ( 'NONE', #32420, 1.250000000000000000, 0.5000000000000000000 ) ;
#57893=CARTESIAN_POINT ( 'NONE',  ( -1.779623408249566774, -17.86369130975115738, 12.71471627657126291 ) ) ;
#57895=DIRECTION ( 'NONE',  ( 0.000000000000000000, -1.000000000000000000, 0.000000000000000000 ) ) ;
#57906=DIRECTION ( 'NONE',  ( -3.788556036780999566E-11, -1.000000000000000000, 0.000000000000000000 ) ) ;
#57908=CARTESIAN_POINT ( 'NONE',  ( -7.712209501855907590, -54.73822238195494805, 10.27335463208971866 ) ) ;
#57909=DIRECTION ( 'NONE',  ( 1.000000000000000000, 0.000000000000000000, 0.000000000000000000 ) ) ;
#57911=CARTESIAN_POINT ( 'NONE',  ( -12.54673349184999864, -24.82806887810999896, 0.9076721992841999542 ) ) ;
#57914=DIRECTION ( 'NONE',  ( 0.000000000000000000, 0.000000000000000000, -1.000000000000000000 ) ) ;
#57916=ORIENTED_EDGE ( 'NONE', *, *, #3159, .T. ) ;
#57917=DIRECTION ( 'NONE',  ( 0.000000000000000000, -1.000000000000000000, 0.000000000000000000 ) ) ;
#57918=ORIENTED_EDGE ( 'NONE', *, *, #28354, .T. ) ;
#57919=CARTESIAN_POINT ( 'NONE',  ( 9.643350356168998161, -24.94034317039000115, 8.260133465584999612 ) ) ;
#57921=ADVANCED_FACE ( 'NONE', ( #10222 ), #50964, .F. ) ;
#57923=ADVANCED_FACE ( 'NONE', ( #24672 ), #29306, .F. ) ;
#57934=CARTESIAN_POINT ( 'NONE',  ( 3.585273492103000059, -75.68288930031000916, 11.57765943471000014 ) ) ;
#57939=CARTESIAN_POINT ( 'NONE',  ( 12.49837451347000084, -18.79042109296999641, -1.667049596275999912 ) ) ;
#57943=ORIENTED_EDGE ( 'NONE', *, *, #49091, .F. ) ;
#57945=CARTESIAN_POINT ( 'NONE',  ( -7.647094085174999556, -55.43104695408000282, 10.00844048069000003 ) ) ;
#57948=CARTESIAN_POINT ( 'NONE',  ( -8.652389292596000203, -16.73734871878000163, -9.414476472810001439 ) ) ;
#57949=CARTESIAN_POINT ( 'NONE',  ( 7.682344222575999915, -56.03537109808000594, 10.04116292115999975 ) ) ;
#57950=CARTESIAN_POINT ( 'NONE',  ( -1.389926494651000155, -17.37618663744999736, -12.65988803923000106 ) ) ;
#57951=DIRECTION ( 'NONE',  ( 0.7071067811865475727, 0.000000000000000000, 0.7071067811865475727 ) ) ;
#57952=CARTESIAN_POINT ( 'NONE',  ( 10.42274798266000069, -57.04634220890999785, -7.691916945423999508 ) ) ;
#57953=DIRECTION ( 'NONE',  ( 0.000000000000000000, 1.000000000000000000, 0.000000000000000000 ) ) ;
#57958=CARTESIAN_POINT ( 'NONE',  ( 0.4255534434941637967, -1.466224065903919183, 3.247433857139228053 ) ) ;
#57959=ADVANCED_FACE ( 'NONE', ( #41510 ), #38754, .F. ) ;
#57960=CARTESIAN_POINT ( 'NONE',  ( -1.288488638075999893, -54.26435060599999360, 12.54709296479000002 ) ) ;
#57962=CARTESIAN_POINT ( 'NONE',  ( -1.324107598017000065, -2.036037460020000189, 3.396848078622999978 ) ) ;
#57963=DIRECTION ( 'NONE',  ( 0.000000000000000000, 1.000000000000000000, 0.000000000000000000 ) ) ;
#57967=CARTESIAN_POINT ( 'NONE',  ( -1.389926494650000066, -61.42381336221999533, 12.65988803926999928 ) ) ;
#57968=CARTESIAN_POINT ( 'NONE',  ( 12.82202470520000048, -18.57373556878999921, 2.066041976111999467 ) ) ;
#57970=LINE ( 'NONE', #4243, #26323 ) ;
#57971=CARTESIAN_POINT ( 'NONE',  ( 11.33104788502155813, -77.23012181351045058, 4.018671469886728964 ) ) ;
#57972=CIRCLE ( 'NONE', #45778, 14.00000000000000000 ) ;
#57979=CARTESIAN_POINT ( 'NONE',  ( -12.43569926720000041, -61.68202092968000727, 0.4277578398253000236 ) ) ;
#57990=CARTESIAN_POINT ( 'NONE',  ( -3.441958447202120297, -0.7500000000000001110, 0.7329790778750402414 ) ) ;
#57991=ORIENTED_EDGE ( 'NONE', *, *, #26849, .F. ) ;
#57992=CARTESIAN_POINT ( 'NONE',  ( 9.931063218505961743, -54.67724209143890590, -7.763994034022205781 ) ) ;
#57993=EDGE_LOOP ( 'NONE', ( #15784, #42031, #26976, #49737 ) ) ;
#57994=CARTESIAN_POINT ( 'NONE',  ( 3.250000000000000444, -1.260416666666666963, 0.4254240051736247197 ) ) ;
#57998=CARTESIAN_POINT ( 'NONE',  ( 1.295048492660999973, -24.52893519126000044, -12.54716442236999896 ) ) ;
#58001=ORIENTED_EDGE ( 'NONE', *, *, #47046, .T. ) ;
#58002=DIRECTION ( 'NONE',  ( 0.000000000000000000, 0.000000000000000000, 1.000000000000000000 ) ) ;
#58003=CARTESIAN_POINT ( 'NONE',  ( -3.894252032411999576, -78.51770906870001454, -11.57248695932000082 ) ) ;
#58004=ORIENTED_EDGE ( 'NONE', *, *, #9736, .F. ) ;
#58005=ORIENTED_EDGE ( 'NONE', *, *, #46449, .F. ) ;
#58006=CARTESIAN_POINT ( 'NONE',  ( 0.000000000000000000, 4.040000000000000036, 0.000000000000000000 ) ) ;
#58011=DIRECTION ( 'NONE',  ( 0.000000000000000000, 0.1122098755727947705, 0.9936845293270585300 ) ) ;
#58013=CARTESIAN_POINT ( 'NONE',  ( 11.45970853605999906, -76.52906641171999524, 5.337786833297999856 ) ) ;
#58018=AXIS2_PLACEMENT_3D ( 'NONE', #12617, #30614, #7616 ) ;
#58019=CARTESIAN_POINT ( 'NONE',  ( -10.55910102243999837, -59.58485473249000108, 7.642147947533000085 ) ) ;
#58020=CARTESIAN_POINT ( 'NONE',  ( -2.312235755821637539, -3.038362080394761744, 2.283552099544162051 ) ) ;
#58025=CARTESIAN_POINT ( 'NONE',  ( 3.772660615778999915, -2.043216633591999898, 0.5031134774969999723 ) ) ;
#58030=DIRECTION ( 'NONE',  ( 0.000000000000000000, 1.000000000000000000, 0.000000000000000000 ) ) ;
#58033=CARTESIAN_POINT ( 'NONE',  ( 7.411516475408999050, -77.19055350637998458, -10.69619859711000132 ) ) ;
#58035=CARTESIAN_POINT ( 'NONE',  ( 12.49168433580000048, -18.70150862776000267, -1.667916687244999974 ) ) ;
#58036=ORIENTED_EDGE ( 'NONE', *, *, #8159, .F. ) ;
#58043=CARTESIAN_POINT ( 'NONE',  ( -1.488596180559999871, -0.9121139388282000215, -3.730054860412999940 ) ) ;
#58044=CARTESIAN_POINT ( 'NONE',  ( -1.931086388455000025, -60.09778595451999905, -12.71798280857999863 ) ) ;
#58047=ORIENTED_EDGE ( 'NONE', *, *, #57406, .F. ) ;
#58053=ORIENTED_EDGE ( 'NONE', *, *, #5281, .T. ) ;
#58055=DIRECTION ( 'NONE',  ( -1.000000000000000000, 0.000000000000000000, 0.000000000000000000 ) ) ;
#58061=VECTOR ( 'NONE', #47886, 1000.000000000000000 ) ;
#58062=ORIENTED_EDGE ( 'NONE', *, *, #44919, .F. ) ;
#58063=CARTESIAN_POINT ( 'NONE',  ( -2.884042199509171400, -2.639263732757689773, -1.497520329303954512 ) ) ;
#58065=LINE ( 'NONE', #17626, #47816 ) ;
#58066=ORIENTED_EDGE ( 'NONE', *, *, #47268, .F. ) ;
#58068=EDGE_LOOP ( 'NONE', ( #53633, #28208, #4823, #51335 ) ) ;
#58071=CARTESIAN_POINT ( 'NONE',  ( -8.485281374238999419, -60.04999999966999980, 8.485281374238999419 ) ) ;
#58072=CARTESIAN_POINT ( 'NONE',  ( -7.640030139755999983, -23.30716934606000024, -10.18491068059999805 ) ) ;
#58073=CARTESIAN_POINT ( 'NONE',  ( -0.7698740312961022125, -77.31791980077814230, -11.75340416254214659 ) ) ;
#58074=EDGE_CURVE ( 'NONE', #26014, #45976, #25559, .T. ) ;
#58075=CARTESIAN_POINT ( 'NONE',  ( -9.000000000000000000, -0.5000000000000000000, 0.000000000000000000 ) ) ;
#58077=DIRECTION ( 'NONE',  ( 0.7071067811865475727, 0.000000000000000000, 0.7071067811865475727 ) ) ;
#58078=EDGE_CURVE ( 'NONE', #3332, #55842, #8614, .T. ) ;
#58084=CARTESIAN_POINT ( 'NONE',  ( -1.250000000000000000, -60.24678171298000251, 12.50000000000000000 ) ) ;
#58085=CARTESIAN_POINT ( 'NONE',  ( 0.5999999999999999778, -18.84999999999999787, 10.98362417419999915 ) ) ;
#58086=DIRECTION ( 'NONE',  ( 0.000000000000000000, 1.000000000000000000, 0.000000000000000000 ) ) ;
#58088=CARTESIAN_POINT ( 'NONE',  ( -3.522236695112999971, -1.250894741108000030, 2.142266609051000081 ) ) ;
#58092=CARTESIAN_POINT ( 'NONE',  ( 12.66001556635999847, -61.43260856911000189, -1.381621105853999998 ) ) ;
#58094=CARTESIAN_POINT ( 'NONE',  ( -10.35747158362999976, -23.31584477285000290, -7.626500902217000721 ) ) ;
#58098=DIRECTION ( 'NONE',  ( 1.000000000000000000, 0.000000000000000000, 0.000000000000000000 ) ) ;
#58100=AXIS2_PLACEMENT_3D ( 'NONE', #53908, #44170, #31137 ) ;
#58101=ORIENTED_EDGE ( 'NONE', *, *, #4029, .F. ) ;
#58102=CIRCLE ( 'NONE', #9103, 9.000000000000000000 ) ;
#58103=CARTESIAN_POINT ( 'NONE',  ( -10.35747145892000098, -18.68415268018999953, -7.626500777237000150 ) ) ;
#58105=AXIS2_PLACEMENT_3D ( 'NONE', #16430, #24990, #29981 ) ;
#58106=CARTESIAN_POINT ( 'NONE',  ( -11.99999999979999821, -23.14999999072999870, 0.7999999997951999786 ) ) ;
#58109=CARTESIAN_POINT ( 'NONE',  ( -9.395758989587999821, -61.50491532550999096, 8.188252216855000043 ) ) ;
#58111=CARTESIAN_POINT ( 'NONE',  ( -2.273545738020000151, -1.203822672877000066, -2.920649130850999864 ) ) ;
#58112=CARTESIAN_POINT ( 'NONE',  ( 3.261893290220421182, -76.44721653378499582, -11.36034884816034563 ) ) ;
#58113=FACE_OUTER_BOUND ( 'NONE', #34626, .T. ) ;
#58114=CARTESIAN_POINT ( 'NONE',  ( -1.799475295154000065, -57.04916621739000249, 12.69619287815999975 ) ) ;
#58115=EDGE_LOOP ( 'NONE', ( #34923, #56845, #55434, #49266 ) ) ;
#58118=CARTESIAN_POINT ( 'NONE',  ( -3.206516299415000049, -1.613032031399000088, -0.5298615117031000299 ) ) ;
#58119=CARTESIAN_POINT ( 'NONE',  ( -10.42274798264000069, -58.55365779174999830, -7.691916945401000127 ) ) ;
#58122=VERTEX_POINT ( 'NONE', #47419 ) ;
#58124=CARTESIAN_POINT ( 'NONE',  ( -11.43989337263541373, -77.72004047834380458, -3.071150918567757238 ) ) ;
#58125=CARTESIAN_POINT ( 'NONE',  ( -1.799502287743000029, -23.30716934606000024, 12.60413652831999975 ) ) ;
#58128=CARTESIAN_POINT ( 'NONE',  ( -12.64502302236999931, -59.57129148919000272, 1.799490220168999954 ) ) ;
#58131=ORIENTED_EDGE ( 'NONE', *, *, #18932, .T. ) ;
#58132=ORIENTED_EDGE ( 'NONE', *, *, #49593, .T. ) ;
#58137=CARTESIAN_POINT ( 'NONE',  ( 10.53562613913999968, -18.79442116269000351, 7.620013630324000253 ) ) ;
#58138=VECTOR ( 'NONE', #31963, 1000.000000000000000 ) ;
#58142=CIRCLE ( 'NONE', #20455, 30.49999999999998934 ) ;
#58144=CARTESIAN_POINT ( 'NONE',  ( 12.51072239526000196, -15.69705297114000331, -0.7871079366006996647 ) ) ;
#58147=DIRECTION ( 'NONE',  ( -0.7071067811865475727, 0.000000000000000000, -0.7071067811865475727 ) ) ;
#58148=CARTESIAN_POINT ( 'NONE',  ( -12.50000000000000000, -18.75000000240999753, -1.750000000000000000 ) ) ;
#58149=EDGE_LOOP ( 'NONE', ( #8245, #38026, #35601, #46732 ) ) ;
#58151=EDGE_CURVE ( 'NONE', #393, #44413, #11469, .T. ) ;
#58152=CARTESIAN_POINT ( 'NONE',  ( -7.450482419345999752, -76.12526934845000426, -9.799277032148999922 ) ) ;
#58154=CARTESIAN_POINT ( 'NONE',  ( -1.804337680682123857, -2.766036367877359847, 3.091116340519547645 ) ) ;
#58155=CARTESIAN_POINT ( 'NONE',  ( -7.624341766647000362, -18.73514853758999976, 10.42531125024999916 ) ) ;
#58157=CARTESIAN_POINT ( 'NONE',  ( 1.568318300085000120E-14, -0.05000000003700048185, 0.000000000000000000 ) ) ;
#58160=CARTESIAN_POINT ( 'NONE',  ( 12.05967318610715466, -76.80230997908272172, 0.3521930913432630428 ) ) ;
#58162=CARTESIAN_POINT ( 'NONE',  ( -8.838834764832000701, -55.54999999966999980, 8.838834764832000701 ) ) ;
#58165=VERTEX_POINT ( 'NONE', #57117 ) ;
#58168=CARTESIAN_POINT ( 'NONE',  ( 1.034214221880000141E-14, 0.2999999999999999334, 0.000000000000000000 ) ) ;
#58175=CARTESIAN_POINT ( 'NONE',  ( -9.346069275190213688, -25.16527745691412221, -8.620894635682162743 ) ) ;
#58179=VERTEX_POINT ( 'NONE', #12247 ) ;
#58181=CARTESIAN_POINT ( 'NONE',  ( -3.785489411603719212, -77.09933145171892477, 11.15228598470222110 ) ) ;
#58182=CARTESIAN_POINT ( 'NONE',  ( 10.88639046104558794, -78.91824007476243708, -4.509380154451887002 ) ) ;
#58186=DIRECTION ( 'NONE',  ( 0.7071067811864980568, 0.7071067811865969777, 8.066391729469968668E-09 ) ) ;
#58188=CARTESIAN_POINT ( 'NONE',  ( 5.660454042118933771, -78.53486099951153676, 10.30159814769029580 ) ) ;
#58190=ORIENTED_EDGE ( 'NONE', *, *, #10862, .T. ) ;
#58191=AXIS2_PLACEMENT_3D ( 'NONE', #25849, #43005, #2562 ) ;
#58196=VECTOR ( 'NONE', #18812, 1000.000000000000000 ) ;
#58198=CARTESIAN_POINT ( 'NONE',  ( -12.50657384680346240, -53.82752586700246411, 0.3552647085964846241 ) ) ;
#58199=AXIS2_PLACEMENT_3D ( 'NONE', #19638, #16086, #29925 ) ;
#58204=CARTESIAN_POINT ( 'NONE',  ( -1.668607604626823449, -60.59381631189516781, 12.52787843855104910 ) ) ;
#58206=CARTESIAN_POINT ( 'NONE',  ( -7.601397897754999633, -60.04999999966999980, 9.369164850722000892 ) ) ;
#58207=CARTESIAN_POINT ( 'NONE',  ( 11.90000000000000036, -21.00000000000000000, -0.6999999999999999556 ) ) ;
#58209=ORIENTED_EDGE ( 'NONE', *, *, #39753, .F. ) ;
#58211=VERTEX_POINT ( 'NONE', #13692 ) ;
#58214=CARTESIAN_POINT ( 'NONE',  ( 8.220407391935999897, -24.81950084232000364, 9.523310056108000410 ) ) ;
#58218=CARTESIAN_POINT ( 'NONE',  ( -12.50000000000000000, -24.68359816828999698, -1.003641515615000035 ) ) ;
#58221=ORIENTED_EDGE ( 'NONE', *, *, #21868, .F. ) ;
#58228=CARTESIAN_POINT ( 'NONE',  ( -9.683064706975999414, -75.68874058712000874, 8.142089017637001547 ) ) ;
#58230=CARTESIAN_POINT ( 'NONE',  ( 9.433537730344784933, -53.67202052640185883, -8.532653828180887245 ) ) ;
#58232=DIRECTION ( 'NONE',  ( 0.000000000000000000, 0.000000000000000000, 1.000000000000000000 ) ) ;
#58233=CARTESIAN_POINT ( 'NONE',  ( 12.50000000000000000, -61.48359816765000119, 1.003641516062000250 ) ) ;
#58234=VECTOR ( 'NONE', #13987, 1000.000000000000000 ) ;
#58237=EDGE_LOOP ( 'NONE', ( #4748, #39969, #57943, #55025 ) ) ;
#58243=CARTESIAN_POINT ( 'NONE',  ( 0.8506806241676515556, -3.354166666666666963, 3.165411199172028844 ) ) ;
#58245=CARTESIAN_POINT ( 'NONE',  ( -0.4802748259354999716, -16.99473092717999734, -12.54896097834000024 ) ) ;
#58246=CONICAL_SURFACE ( 'NONE', #16748, 3.699999993671000187, 0.7853981633972997312 ) ;
#58247=CARTESIAN_POINT ( 'NONE',  ( 8.485281374238999419, -55.54999999966999980, -8.485281374238999419 ) ) ;
#58249=CARTESIAN_POINT ( 'NONE',  ( 10.35845616725999996, -55.50221404479999876, -7.627487606591000002 ) ) ;
#58250=B_SPLINE_CURVE_WITH_KNOTS ( 'NONE', 3,
 ( #43537, #26093, #11956, #39101, #29934, #34078 ),
 .UNSPECIFIED., .F., .F.,
 ( 4, 1, 1, 4 ),
 ( 0.000000000000000000, 0.3333333333333000081, 0.6666666666667000474, 1.000000000000000000 ),
 .UNSPECIFIED. ) ;
#58255=ORIENTED_EDGE ( 'NONE', *, *, #6596, .T. ) ;
#58256=CARTESIAN_POINT ( 'NONE',  ( 12.76303204298000082, -60.06485150663000638, -1.980584515756000030 ) ) ;
#58257=CARTESIAN_POINT ( 'NONE',  ( -0.9113424693959999434, -53.97464206407000376, 12.54674099554000044 ) ) ;
#58258=CARTESIAN_POINT ( 'NONE',  ( -12.82904091339000097, -18.67547470641000018, 2.062673488738000049 ) ) ;
#58259=CARTESIAN_POINT ( 'NONE',  ( -3.553391519525000319, -1.842240405599000042, -1.760552736492000170 ) ) ;
#58262=CARTESIAN_POINT ( 'NONE',  ( -8.838834764832000701, -60.04999999966999980, -8.838834764832000701 ) ) ;
#58263=CARTESIAN_POINT ( 'NONE',  ( 12.83675912440999944, -18.77244614031999959, 2.062833085520999976 ) ) ;
#58265=EDGE_CURVE ( 'NONE', #326, #17731, #17245, .T. ) ;
#58267=CARTESIAN_POINT ( 'NONE',  ( -11.72607011526379672, -76.97216391817583769, -2.880960420985590797 ) ) ;
#58268=CARTESIAN_POINT ( 'NONE',  ( -10.18558922015999890, -78.70658632805000821, 7.214292160837000090 ) ) ;
#58269=B_SPLINE_SURFACE_WITH_KNOTS ( 'NONE', 3, 3, ( 
 ( #20050, #10903, #54878, #19751 ),
 ( #28589, #14716, #28879, #46926 ),
 ( #28291, #46341, #32424, #15315 ),
 ( #6453, #32714, #50469, #33601 ),
 ( #50766, #24468, #19457, #23874 ),
 ( #14429, #56060, #5572, #46047 ),
 ( #37161, #38038, #33309, #51640 ),
 ( #27999, #46633, #36866, #1756 ),
 ( #33010, #23581, #15607, #5865 ),
 ( #2050, #51344, #1176, #11195 ),
 ( #42481, #24172, #6163, #29171 ) ),
 .UNSPECIFIED., .F., .F., .F.,
 ( 4, 1, 1, 1, 1, 1, 1, 1, 4 ),
 ( 4, 4 ),
 ( -0.01994534136797000007, 0.000000000000000000, 0.1666666666667000196, 0.3333333333333000081, 0.5000000000000000000, 0.6666666666667000474, 0.8333333333333000637, 1.000000000000000000, 1.020519780480000138 ),
 ( -0.3582002740325999635, 1.358566136073000141 ),
 .UNSPECIFIED. ) ;
#58273=CARTESIAN_POINT ( 'NONE',  ( 1.208267226953838591, -61.62590682120165297, 12.70228502427621997 ) ) ;
#58277=CARTESIAN_POINT ( 'NONE',  ( 12.50000000000000000, -18.55321828668999729, -1.250000000000000000 ) ) ;
#58279=CARTESIAN_POINT ( 'NONE',  ( 12.52785477533552516, -55.00586572896404647, -1.668513102962561945 ) ) ;
#58285=VERTEX_POINT ( 'NONE', #17542 ) ;
#58286=ORIENTED_EDGE ( 'NONE', *, *, #16533, .F. ) ;
#58289=CARTESIAN_POINT ( 'NONE',  ( 0.5999999999999999778, -23.15000000000999947, -11.79999999999999893 ) ) ;
#58290=ORIENTED_EDGE ( 'NONE', *, *, #9493, .T. ) ;
#58294=DIRECTION ( 'NONE',  ( 1.000000000000000000, 0.000000000000000000, 0.000000000000000000 ) ) ;
#58296=CARTESIAN_POINT ( 'NONE',  ( -0.9113424693944000010, -24.82535793559999959, -12.54674099557999867 ) ) ;
#58299=EDGE_LOOP ( 'NONE', ( #8534, #17912, #23693, #26176 ) ) ;
#58301=CARTESIAN_POINT ( 'NONE',  ( 7.050117653951000207, -79.09252343021999820, -9.969126685360000906 ) ) ;
#58304=ORIENTED_EDGE ( 'NONE', *, *, #36825, .F. ) ;
#58305=LINE ( 'NONE', #4872, #41440 ) ;
#58311=CARTESIAN_POINT ( 'NONE',  ( 5.690325051763000630, -78.25735805811000034, 11.64023780191999968 ) ) ;
#58312=CARTESIAN_POINT ( 'NONE',  ( -1.155570385622000096, -76.86209425748999990, -12.58848097821000067 ) ) ;
#58314=DIRECTION ( 'NONE',  ( -0.7071067811865475727, 0.000000000000000000, 0.7071067811865475727 ) ) ;
#58320=AXIS2_PLACEMENT_3D ( 'NONE', #31075, #14251, #54707 ) ;
#58323=CARTESIAN_POINT ( 'NONE',  ( 3.772660615778999915, -2.008549966925000430, 0.5031134774969999723 ) ) ;
#58329=CARTESIAN_POINT ( 'NONE',  ( -12.66319948256999872, -16.81851729361000380, -0.1456213732515000137 ) ) ;
#58330=CARTESIAN_POINT ( 'NONE',  ( -9.692839446179998930, -78.43249358183999220, 7.074522137259999788 ) ) ;
#58332=ADVANCED_FACE ( 'NONE', ( #739 ), #4558, .T. ) ;
#58334=CARTESIAN_POINT ( 'NONE',  ( 12.87024489156999962, -22.78461666469000235, -2.062597265787999845 ) ) ;
#58335=ORIENTED_EDGE ( 'NONE', *, *, #4837, .F. ) ;
#58342=CARTESIAN_POINT ( 'NONE',  ( 2.301364338783000285, -1.456223928488999952, -3.291430154679999998 ) ) ;
#58345=ORIENTED_EDGE ( 'NONE', *, *, #48146, .T. ) ;
#58350=ORIENTED_EDGE ( 'NONE', *, *, #4837, .T. ) ;
#58358=EDGE_LOOP ( 'NONE', ( #35741, #10292, #45227, #54814, #34600 ) ) ;
#58359=CARTESIAN_POINT ( 'NONE',  ( -1.232277669651724583, -2.694870653336070454, -3.006800154367852862 ) ) ;
#58368=CARTESIAN_POINT ( 'NONE',  ( 10.18949731070000020, -55.58470987670000341, 7.645392562244000878 ) ) ;
#58370=CARTESIAN_POINT ( 'NONE',  ( -7.668936932623999780, -22.77152778045000048, -10.21380041493000057 ) ) ;
#58371=CARTESIAN_POINT ( 'NONE',  ( 3.074306947300566861, -77.34369429684161901, -11.43804941158839306 ) ) ;
#58372=CARTESIAN_POINT ( 'NONE',  ( -11.75000000000000000, -78.79999999999999716, 1.318041981624000073E-14 ) ) ;
#58373=CARTESIAN_POINT ( 'NONE',  ( 7.691916945401000127, -58.55365779174999830, -10.42274798264000069 ) ) ;
#58375=CARTESIAN_POINT ( 'NONE',  ( -9.641208724080000181, -24.43394297700999829, 7.943747389698999406 ) ) ;
#58376=DIRECTION ( 'NONE',  ( 1.000000000000000000, 0.000000000000000000, 0.000000000000000000 ) ) ;
#58380=CARTESIAN_POINT ( 'NONE',  ( -12.66322081671000177, -16.81838367322000138, 0.1487102037789999887 ) ) ;
#58382=DIRECTION ( 'NONE',  ( 0.000000000000000000, -1.000000000000000000, 0.000000000000000000 ) ) ;
#58385=CARTESIAN_POINT ( 'NONE',  ( 1.829579065110999991, -1.222748962127999883, -3.127009326567999903 ) ) ;
#58386=DIRECTION ( 'NONE',  ( 0.07798810159162851419, -0.04890177460079911387, 0.9957542229139811907 ) ) ;
#58389=CARTESIAN_POINT ( 'NONE',  ( 12.57354097144999905, -60.52384125708999818, -1.757953070309000054 ) ) ;
#58391=LINE ( 'NONE', #8794, #42718 ) ;
#58400=ORIENTED_EDGE ( 'NONE', *, *, #33671, .F. ) ;
#58404=DIRECTION ( 'NONE',  ( 0.000000000000000000, -1.000000000000000000, 0.000000000000000000 ) ) ;
ENDSEC;
END-ISO-10303-21;
